ISO-10303-21;
HEADER;
FILE_DESCRIPTION (('STEP AP214'),
    '1' );
FILE_NAME ('spindle.step',
    '2026-10-26T19:46:16',
    ( '' ),
    ( '' ),
    'SwSTEP 2.0',
    'SolidWorks 2025',
    '' );
FILE_SCHEMA (( 'AUTOMOTIVE_DESIGN' ));
ENDSEC;

DATA;
#2=CARTESIAN_POINT ( 'NONE',  ( 3.042071309553167069, 186.8229166632527267, -11.35316468749999785 ) ) ;
#4=FACE_OUTER_BOUND ( 'NONE', #11968, .T. ) ;
#8=CARTESIAN_POINT ( 'NONE',  ( -9.832129032723418760, 182.8645833299193555, -5.676582343750004256 ) ) ;
#17=CARTESIAN_POINT ( 'NONE',  ( -8.311093377946836114, 122.9687499965860127, -8.311093377946837890 ) ) ;
#18=CARTESIAN_POINT ( 'NONE',  ( -0.4500000000000013989, 255.9999999999997726, 5.815332135061025198 ) ) ;
#30=ORIENTED_EDGE ( 'NONE', *, *, #66787, .T. ) ;
#34=CARTESIAN_POINT ( 'NONE',  ( 6.000000000000003553, 293.5625000000001137, -2.485281374238571761 ) ) ;
#48=CARTESIAN_POINT ( 'NONE',  ( -4.088227598258586603E-16, 298.3593750017070079, -6.676582343750001591 ) ) ;
#49=CARTESIAN_POINT ( 'NONE',  ( -10.00000000000000355, 117.7083333333333286, 2.679491924311223183 ) ) ;
#52=CARTESIAN_POINT ( 'NONE',  ( -4.088227598258586603E-16, 288.3593750017070079, -6.676582343750001591 ) ) ;
#63=CARTESIAN_POINT ( 'NONE',  ( 10.00000000000000178, 52.08333332650536818, -2.679491924311226736 ) ) ;
#65=CARTESIAN_POINT ( 'NONE',  ( -3.042071309553173730, 19.32291666325268409, 11.35316468749999785 ) ) ;
#66=( BOUNDED_CURVE ( )  B_SPLINE_CURVE ( 2, ( #62124, #31597, #54994, #3301, #26287, #72324, #20638, #17588, #51930, #27790, #56850, #34966, #23250 ),
 .UNSPECIFIED., .F., .F. ) 
 B_SPLINE_CURVE_WITH_KNOTS ( ( 3, 2, 2, 2, 2, 2, 3 ),
 ( 0.4866946232415507168, 0.4919272298211807559, 0.4971598364008106841, 0.5023924429804407232, 0.5076250495600707069, 0.5128576561397006905, 0.5180902627193306742 ),
 .UNSPECIFIED. ) 
 CURVE ( )  GEOMETRIC_REPRESENTATION_ITEM ( )  RATIONAL_B_SPLINE_CURVE ( ( 0.9999999999999911182, 0.9659258262890771940, 1.000000000000000000, 0.9659258262890683122, 1.000000000000000000, 0.9659258262890683122, 1.000000000000000000, 0.9659258262890683122, 1.000000000000000000, 0.9659258262890683122, 1.000000000000000000, 0.9659258262893768432, 0.9999999999996914690 ) ) 
 REPRESENTATION_ITEM ( '' )  );
#68=( BOUNDED_CURVE ( )  B_SPLINE_CURVE ( 2, ( #33279, #10252, #21187, #32531, #61186, #72505, #55916, #72881, #38182 ),
 .UNSPECIFIED., .F., .F. ) 
 B_SPLINE_CURVE_WITH_KNOTS ( ( 3, 2, 2, 2, 3 ),
 ( 0.7708333333333317050, 0.7812499999999983347, 0.7916666666666649643, 0.8020833333333317050, 0.8124999999999983347 ),
 .UNSPECIFIED. ) 
 CURVE ( )  GEOMETRIC_REPRESENTATION_ITEM ( )  RATIONAL_B_SPLINE_CURVE ( ( 1.000000000000012212, 0.9238795325112745260, 1.000000000000000000, 0.9238795325112867385, 1.000000000000000000, 0.9238795325112867385, 1.000000000000000000, 0.9238795325112989509, 0.9999999999999877875 ) ) 
 REPRESENTATION_ITEM ( '' )  );
#69=CARTESIAN_POINT ( 'NONE',  ( 3.042071309553167069, 217.1354166632526983, -11.35316468749999785 ) ) ;
#78=CARTESIAN_POINT ( 'NONE',  ( 11.35316468749999785, 25.57291666325268409, 3.042071309553174174 ) ) ;
#85=CARTESIAN_POINT ( 'NONE',  ( 11.35316468750000141, 25.78124999658601624, 0.000000000000000000 ) ) ;
#87=CARTESIAN_POINT ( 'NONE',  ( 5.676582343749993598, 129.9479166632526983, 9.832129032723422313 ) ) ;
#88=CARTESIAN_POINT ( 'NONE',  ( 7.320508075688771044, 101.2499999931720112, 7.320508075688775484 ) ) ;
#90=DIRECTION ( 'NONE',  ( 0.000000000000000000, 0.000000000000000000, 1.000000000000000000 ) ) ;
#94=CARTESIAN_POINT ( 'NONE',  ( 5.676582343750001591, 11.92708332991935016, -9.832129032723420536 ) ) ;
#95=CARTESIAN_POINT ( 'NONE',  ( -5.000000000000005329, 155.2083333265053682, 8.660254037844387298 ) ) ;
#96=CARTESIAN_POINT ( 'NONE',  ( 1.226468279477575784E-15, 298.7031250017070079, 6.676582343750001591 ) ) ;
#97=CARTESIAN_POINT ( 'NONE',  ( 11.35316468750000141, 140.7812499965860411, 0.000000000000000000 ) ) ;
#102=EDGE_LOOP ( 'NONE', ( #72383, #48157, #74168, #29001 ) ) ;
#103=VECTOR ( 'NONE', #43518, 1000.000000000000000 ) ;
#107=CARTESIAN_POINT ( 'NONE',  ( -2.085542519210945728E-15, 79.84374999658601268, 11.35316468750000141 ) ) ;
#114=CARTESIAN_POINT ( 'NONE',  ( -8.660254037844390851, 109.7916666598387110, 4.999999999999998224 ) ) ;
#140=CARTESIAN_POINT ( 'NONE',  ( 6.123233995736767268E-16, 81.25000000000000000, -10.00000000000000178 ) ) ;
#141=EDGE_CURVE ( 'NONE', #28745, #3534, #4029, .T. ) ;
#143=CARTESIAN_POINT ( 'NONE',  ( -2.085542519210945728E-15, 54.84374999658601979, 11.35316468750000141 ) ) ;
#144=CARTESIAN_POINT ( 'NONE',  ( -6.000000000000003553, 289.9375000000000000, -2.485281374238571317 ) ) ;
#145=EDGE_LOOP ( 'NONE', ( #69571, #68618, #12629, #39333 ) ) ;
#146=ADVANCED_FACE ( 'NONE', ( #37606 ), #60606, .T. ) ;
#155=CARTESIAN_POINT ( 'NONE',  ( 8.660254037844385522, 199.5833333333333428, 5.000000000000005329 ) ) ;
#157=CARTESIAN_POINT ( 'NONE',  ( 11.35316468749999785, 170.8854166632526983, 3.042071309553174174 ) ) ;
#162=CARTESIAN_POINT ( 'NONE',  ( 11.35316468749999785, 40.88541666325268409, 3.042071309553174174 ) ) ;
#172=CARTESIAN_POINT ( 'NONE',  ( 2.679491924311228956, 57.91666665983870388, -10.00000000000000000 ) ) ;
#177=CARTESIAN_POINT ( 'NONE',  ( 8.660254037844385522, 101.4583333265053824, 5.000000000000005329 ) ) ;
#178=ORIENTED_EDGE ( 'NONE', *, *, #23200, .T. ) ;
#181=CARTESIAN_POINT ( 'NONE',  ( 1.226468279477575784E-15, 298.8593750017070079, 6.676582343750001591 ) ) ;
#184=CARTESIAN_POINT ( 'NONE',  ( 8.311093377946834337, 155.1562499965860127, 8.311093377946839666 ) ) ;
#191=EDGE_LOOP ( 'NONE', ( #73079, #34833, #18935, #37812 ) ) ;
#195=CARTESIAN_POINT ( 'NONE',  ( -3.042071309553163960, 132.5520833299193555, -11.35316468749999963 ) ) ;
#199=CARTESIAN_POINT ( 'NONE',  ( 3.042071309553159519, 30.05208332991934839, 11.35316468750000141 ) ) ;
#200=ORIENTED_EDGE ( 'NONE', *, *, #53117, .T. ) ;
#201=CARTESIAN_POINT ( 'NONE',  ( 4.999999999999993783, 36.04166665983870388, 8.660254037844390851 ) ) ;
#207=CARTESIAN_POINT ( 'NONE',  ( 2.485281374238575314, 296.3750000034140157, 6.000000000000000888 ) ) ;
#211=CARTESIAN_POINT ( 'NONE',  ( 5.676582343749993598, 150.2604166632526699, 9.832129032723422313 ) ) ;
#223=ORIENTED_EDGE ( 'NONE', *, *, #26791, .F. ) ;
#227=CARTESIAN_POINT ( 'NONE',  ( -1.836970198721029983E-15, 43.75000000000000711, 10.00000000000000178 ) ) ;
#234=ADVANCED_FACE ( 'NONE', ( #9685 ), #32705, .T. ) ;
#238=CARTESIAN_POINT ( 'NONE',  ( -4.999999999999998224, 8.541666659838698550, -8.660254037844389075 ) ) ;
#242=CARTESIAN_POINT ( 'NONE',  ( -2.679491924311235618, 158.5416666666666003, 10.00000000000000000 ) ) ;
#245=CARTESIAN_POINT ( 'NONE',  ( 11.35316468750000141, 131.0937499965860127, 0.000000000000000000 ) ) ;
#246=CARTESIAN_POINT ( 'NONE',  ( -6.000000000000003553, 294.0000000034140157, -2.485281374238571317 ) ) ;
#251=ORIENTED_EDGE ( 'NONE', *, *, #53078, .F. ) ;
#254=CARTESIAN_POINT ( 'NONE',  ( -3.190679070438028606E-13, 193.7500000000000000, 10.00000000000000533 ) ) ;
#256=CARTESIAN_POINT ( 'NONE',  ( -10.00000000000000355, 19.58333332650536818, 2.679491924311223183 ) ) ;
#263=CARTESIAN_POINT ( 'NONE',  ( 9.832129032723416984, 105.3645833299193555, 5.676582343750006032 ) ) ;
#264=ORIENTED_EDGE ( 'NONE', *, *, #10411, .T. ) ;
#269=AXIS2_PLACEMENT_3D ( 'NONE', #63986, #56848, #58346 ) ;
#270=CARTESIAN_POINT ( 'NONE',  ( -11.35316468749999785, 108.0729166632526699, -3.042071309553167513 ) ) ;
#271=VERTEX_POINT ( 'NONE', #62834 ) ;
#274=CARTESIAN_POINT ( 'NONE',  ( 10.00000000000000000, 226.6666666598386541, 2.679491924311236062 ) ) ;
#278=CARTESIAN_POINT ( 'NONE',  ( -2.085542519210945728E-15, 99.53124999658602690, 11.35316468750000141 ) ) ;
#283=CARTESIAN_POINT ( 'NONE',  ( -2.679491924311235618, 190.4166666598387394, 10.00000000000000000 ) ) ;
#287=CARTESIAN_POINT ( 'NONE',  ( -8.311093377946841443, 89.21874999658602690, 8.311093377946834337 ) ) ;
#288=CARTESIAN_POINT ( 'NONE',  ( -2.765530957081996810, 290.2656250017068942, -6.676582343750003368 ) ) ;
#292=CARTESIAN_POINT ( 'NONE',  ( 11.35316468750000141, 215.7812499965860411, 0.000000000000000000 ) ) ;
#296=CARTESIAN_POINT ( 'NONE',  ( 11.35316468750000141, 220.7812499965860127, 0.000000000000000000 ) ) ;
#299=CARTESIAN_POINT ( 'NONE',  ( 4.721056650415999201, 295.0781250017069510, -4.721056650415999201 ) ) ;
#302=CARTESIAN_POINT ( 'NONE',  ( -11.35316468750000141, 203.5937499965860127, -1.390361679473963753E-15 ) ) ;
#312=CARTESIAN_POINT ( 'NONE',  ( -2.679491924311235618, 28.54166666666667140, 10.00000000000000000 ) ) ;
#323=CARTESIAN_POINT ( 'NONE',  ( 4.721056650416000089, 294.8281250017069510, 4.721056650415999201 ) ) ;
#332=CARTESIAN_POINT ( 'NONE',  ( -5.676582343750006032, 89.42708332991934128, 9.832129032723418760 ) ) ;
#341=CARTESIAN_POINT ( 'NONE',  ( 5.676582343750001591, 201.6145833299193555, -9.832129032723420536 ) ) ;
#346=CARTESIAN_POINT ( 'NONE',  ( 11.35316468750000141, 186.0937499965860411, 0.000000000000000000 ) ) ;
#350=CARTESIAN_POINT ( 'NONE',  ( -10.00000000000000000, 107.7083333333333428, 2.679491924311222295 ) ) ;
#354=CARTESIAN_POINT ( 'NONE',  ( 5.676582343749993598, 69.94791666325268409, 9.832129032723422313 ) ) ;
#358=LINE ( 'NONE', #74275, #65132 ) ;
#360=CARTESIAN_POINT ( 'NONE',  ( -9.832129032723418760, 67.86458332991935549, -5.676582343750004256 ) ) ;
#365=CARTESIAN_POINT ( 'NONE',  ( -3.042071309553173730, 59.32291666325267698, 11.35316468749999785 ) ) ;
#368=CARTESIAN_POINT ( 'NONE',  ( 6.123233995736767268E-16, 153.1249999931720538, -10.00000000000000178 ) ) ;
#372=CARTESIAN_POINT ( 'NONE',  ( -9.832129032723418760, 43.17708332991934839, -5.676582343750004256 ) ) ;
#374=CARTESIAN_POINT ( 'NONE',  ( -5.676582343750006032, 179.1145833299193555, 9.832129032723418760 ) ) ;
#380=CARTESIAN_POINT ( 'NONE',  ( 11.35316468749999785, 185.5729166632526983, 3.042071309553174174 ) ) ;
#387=CARTESIAN_POINT ( 'NONE',  ( 8.311093377946837890, 166.7187499965860127, -8.311093377946837890 ) ) ;
#389=CARTESIAN_POINT ( 'NONE',  ( 11.35316468749999963, 126.3020833299193555, -3.042071309553165293 ) ) ;
#396=( BOUNDED_CURVE ( )  B_SPLINE_CURVE ( 2, ( #48168, #19867, #36494, #24780, #47795, #35759, #30090, #2902, #53479, #70818, #36125, #65892, #2158 ),
 .UNSPECIFIED., .F., .F. ) 
 B_SPLINE_CURVE_WITH_KNOTS ( ( 3, 2, 2, 2, 2, 2, 3 ),
 ( 1.522886666904841757, 1.528120630700553040, 1.533354594496264545, 1.538588558291975827, 1.543822522087687332, 1.549056485883398615, 1.554290449679109676 ),
 .UNSPECIFIED. ) 
 CURVE ( )  GEOMETRIC_REPRESENTATION_ITEM ( )  RATIONAL_B_SPLINE_CURVE ( ( 0.9999999999999790168, 0.9659258262890890734, 0.9999999999999998890, 0.9659258262890682012, 0.9999999999999998890, 0.9659258262890682012, 0.9999999999999998890, 0.9659258262890682012, 0.9999999999999998890, 0.9659258262890682012, 0.9999999999999998890, 0.9659258262890682012, 0.9999999999999998890 ) ) 
 REPRESENTATION_ITEM ( '' )  );
#403=CARTESIAN_POINT ( 'NONE',  ( -8.660254037844389075, 187.0833333333333428, -5.000000000000006217 ) ) ;
#409=ORIENTED_EDGE ( 'NONE', *, *, #69841, .T. ) ;
#413=VERTEX_POINT ( 'NONE', #63581 ) ;
#418=CARTESIAN_POINT ( 'NONE',  ( -6.000000000000001776, 290.0625000034140157, 0.000000000000000000 ) ) ;
#420=CARTESIAN_POINT ( 'NONE',  ( -4.721056650415999201, 297.4843750017070079, -4.721056650415999201 ) ) ;
#421=CARTESIAN_POINT ( 'NONE',  ( -8.660254037844390851, 137.9166666666666856, 4.999999999999998224 ) ) ;
#424=CARTESIAN_POINT ( 'NONE',  ( 6.123233995736767268E-16, 138.1249999931720538, -10.00000000000000178 ) ) ;
#439=CARTESIAN_POINT ( 'NONE',  ( -8.311093377946836114, 32.65624999658601268, -8.311093377946837890 ) ) ;
#440=CARTESIAN_POINT ( 'NONE',  ( 10.00000000000033040, 25.00000000000018829, 0.000000000000000000 ) ) ;
#441=CARTESIAN_POINT ( 'NONE',  ( 11.35316468749999963, 226.3020833299193555, -3.042071309553165293 ) ) ;
#442=CARTESIAN_POINT ( 'NONE',  ( -7.320508075688773708, 218.7499999931720538, -7.320508075688774596 ) ) ;
#447=CARTESIAN_POINT ( 'NONE',  ( -11.35316468750000141, 18.28124999658601624, -1.390361679473963753E-15 ) ) ;
#453=CARTESIAN_POINT ( 'NONE',  ( -8.311093377946836114, 22.65624999658601979, -8.311093377946837890 ) ) ;
#455=CARTESIAN_POINT ( 'NONE',  ( 8.311093377946834337, 140.1562499965860127, 8.311093377946839666 ) ) ;
#456=CARTESIAN_POINT ( 'NONE',  ( 10.00000000000000000, 111.6666666598387110, 2.679491924311236062 ) ) ;
#463=CARTESIAN_POINT ( 'NONE',  ( -2.085542519210945728E-15, 4.843749996586016238, 11.35316468750000141 ) ) ;
#465=CARTESIAN_POINT ( 'NONE',  ( -4.721056650415999201, 297.3281250017069510, -4.721056650415999201 ) ) ;
#466=CARTESIAN_POINT ( 'NONE',  ( 3.042071309553159519, 134.7395833299193555, 11.35316468750000141 ) ) ;
#476=CARTESIAN_POINT ( 'NONE',  ( -3.042071309553173730, 84.63541666325265567, 11.35316468749999785 ) ) ;
#508=CARTESIAN_POINT ( 'NONE',  ( 4.999999999999993783, 94.16666666666667140, 8.660254037844390851 ) ) ;
#510=CARTESIAN_POINT ( 'NONE',  ( 11.35316468750000141, 61.09374999658602690, 0.000000000000000000 ) ) ;
#511=CARTESIAN_POINT ( 'NONE',  ( 2.765530957081996366, 299.2968750017070079, -6.676582343750003368 ) ) ;
#512=VERTEX_POINT ( 'NONE', #39465 ) ;
#516=CARTESIAN_POINT ( 'NONE',  ( -8.660254037844390851, 104.7916666598386968, 4.999999999999998224 ) ) ;
#519=FACE_OUTER_BOUND ( 'NONE', #6926, .T. ) ;
#521=CARTESIAN_POINT ( 'NONE',  ( -10.00000000000000178, 202.5000000000000000, -1.224646799147353454E-15 ) ) ;
#523=CARTESIAN_POINT ( 'NONE',  ( -8.311093377946836114, 182.9687499965859843, -8.311093377946837890 ) ) ;
#530=CARTESIAN_POINT ( 'NONE',  ( 6.951808397369818766E-16, 37.34374999658601979, -11.35316468750000141 ) ) ;
#533=CARTESIAN_POINT ( 'NONE',  ( -2.679491924311226292, 123.3333333265053540, -10.00000000000000178 ) ) ;
#537=EDGE_CURVE ( 'NONE', #26622, #55859, #33424, .T. ) ;
#538=CARTESIAN_POINT ( 'NONE',  ( 4.999999999999993783, 81.04166665983871098, 8.660254037844390851 ) ) ;
#541=CARTESIAN_POINT ( 'NONE',  ( 2.679491924311583784, 216.0416666666667709, -10.00000000000005151 ) ) ;
#547=CARTESIAN_POINT ( 'NONE',  ( -2.765530957081998586, 297.7968750017069510, 6.676582343750001591 ) ) ;
#549=CARTESIAN_POINT ( 'NONE',  ( 10.00000000000000178, 42.08333332650537528, -2.679491924311226736 ) ) ;
#550=CARTESIAN_POINT ( 'NONE',  ( -8.311093377946841443, 158.9062499965860411, 8.311093377946830785 ) ) ;
#560=CARTESIAN_POINT ( 'NONE',  ( -3.042071309553163960, 122.5520833299193271, -11.35316468749999963 ) ) ;
#564=CARTESIAN_POINT ( 'NONE',  ( 11.35316468750000141, 51.09374999658601268, 0.000000000000000000 ) ) ;
#566=CARTESIAN_POINT ( 'NONE',  ( 10.00000000000000178, 36.87499999317203958, 0.000000000000000000 ) ) ;
#570=EDGE_CURVE ( 'NONE', #31223, #17827, #41112, .T. ) ;
#573=CARTESIAN_POINT ( 'NONE',  ( -2.485281374238571761, 295.8750000034140157, -6.000000000000003553 ) ) ;
#590=ORIENTED_EDGE ( 'NONE', *, *, #3458, .F. ) ;
#595=CARTESIAN_POINT ( 'NONE',  ( -10.00000000000000000, 47.29166666666667140, -2.679491924311229845 ) ) ;
#598=CARTESIAN_POINT ( 'NONE',  ( -2.485281374238571761, 299.8125000000000000, -6.000000000000003553 ) ) ;
#599=VECTOR ( 'NONE', #15894, 1000.000000000000000 ) ;
#600=CARTESIAN_POINT ( 'NONE',  ( -2.485281374238288432, 288.2500000034140726, 6.000000000000285105 ) ) ;
#601=CARTESIAN_POINT ( 'NONE',  ( -1.836970198721029983E-15, 195.6249999931720254, 10.00000000000000178 ) ) ;
#608=CARTESIAN_POINT ( 'NONE',  ( 4.999999999999993783, 90.83333333333332860, -8.660254037844374864 ) ) ;
#612=CARTESIAN_POINT ( 'NONE',  ( -2.679491924311225848, 161.4583333333333144, -10.00000000000000178 ) ) ;
#616=CARTESIAN_POINT ( 'NONE',  ( 3.042071309553167069, 142.1354166632526415, -11.35316468749999785 ) ) ;
#628=CARTESIAN_POINT ( 'NONE',  ( 6.123233995736767268E-16, 18.12499999317203248, -10.00000000000000178 ) ) ;
#635=CARTESIAN_POINT ( 'NONE',  ( -8.311093377946841443, 108.9062499965860127, 8.311093377946830785 ) ) ;
#641=CARTESIAN_POINT ( 'NONE',  ( -5.676582343750006032, 109.1145833299193555, 9.832129032723418760 ) ) ;
#645=CARTESIAN_POINT ( 'NONE',  ( -2.679491924311225848, 223.3333333265053398, -10.00000000000000178 ) ) ;
#648=CARTESIAN_POINT ( 'NONE',  ( -2.679491924310645423, 183.5416666666667425, 10.00000000000033573 ) ) ;
#649=CARTESIAN_POINT ( 'NONE',  ( 9.832129032723416984, 105.3645833299193555, 5.676582343750006032 ) ) ;
#652=CARTESIAN_POINT ( 'NONE',  ( -3.166186134455097228E-13, 171.2500000000000284, -9.999999999999998224 ) ) ;
#654=CARTESIAN_POINT ( 'NONE',  ( -4.999999999999998224, 198.5416666598387110, -8.660254037844389075 ) ) ;
#657=CARTESIAN_POINT ( 'NONE',  ( -5.676582343750006032, 94.42708332991935549, 9.832129032723418760 ) ) ;
#662=CARTESIAN_POINT ( 'NONE',  ( 6.951808397369818766E-16, 222.0312499965860127, -11.35316468750000141 ) ) ;
#666=CARTESIAN_POINT ( 'NONE',  ( 3.042071309553159519, 214.7395833299193555, 11.35316468750000141 ) ) ;
#669=CARTESIAN_POINT ( 'NONE',  ( 7.320508075688774596, 47.49999999317203958, -7.320508075688774596 ) ) ;
#671=CARTESIAN_POINT ( 'NONE',  ( -6.676582343750001591, 296.4531250017069510, 0.000000000000000000 ) ) ;
#674=CARTESIAN_POINT ( 'NONE',  ( -11.35316468749999785, 203.3854166632526983, -3.042071309553167957 ) ) ;
#682=CARTESIAN_POINT ( 'NONE',  ( -7.320508075688778149, 33.12500000000000000, 7.320508075688769267 ) ) ;
#688=ADVANCED_FACE ( 'NONE', ( #24331 ), #48445, .F. ) ;
#693=CARTESIAN_POINT ( 'NONE',  ( -6.676582343750001591, 297.4531250017069510, 0.000000000000000000 ) ) ;
#702=CARTESIAN_POINT ( 'NONE',  ( -9.832129032723418760, 88.17708332991934128, -5.676582343750004256 ) ) ;
#707=CARTESIAN_POINT ( 'NONE',  ( -6.676582343750001591, 287.6093750017069510, 0.000000000000000000 ) ) ;
#712=CARTESIAN_POINT ( 'NONE',  ( 11.35316468749999963, 200.9895833299193839, -3.042071309553165293 ) ) ;
#716=CARTESIAN_POINT ( 'NONE',  ( -11.35316468749999785, 183.3854166632526699, -3.042071309553167513 ) ) ;
#724=CARTESIAN_POINT ( 'NONE',  ( -11.35316468749999785, 68.07291666325266988, -3.042071309553167513 ) ) ;
#731=CARTESIAN_POINT ( 'NONE',  ( 9.832129032723416984, 75.36458332991935549, 5.676582343750006032 ) ) ;
#736=CARTESIAN_POINT ( 'NONE',  ( 5.676582343750001591, 56.61458332991934839, -9.832129032723420536 ) ) ;
#739=CARTESIAN_POINT ( 'NONE',  ( -1.836970198721029983E-15, 150.6249999931720538, 10.00000000000000178 ) ) ;
#742=CARTESIAN_POINT ( 'NONE',  ( -5.676582343750006032, 54.42708332991935549, 9.832129032723418760 ) ) ;
#745=CARTESIAN_POINT ( 'NONE',  ( -5.676582343749998039, 177.4479166632526983, -9.832129032723420536 ) ) ;
#751=CARTESIAN_POINT ( 'NONE',  ( -3.042071309553173730, 179.3229166632526699, 11.35316468749999785 ) ) ;
#756=CARTESIAN_POINT ( 'NONE',  ( 11.35316468749999785, 170.8854166632526983, 3.042071309553174174 ) ) ;
#759=CARTESIAN_POINT ( 'NONE',  ( 11.35316468750000141, 126.0937499965860127, 0.000000000000000000 ) ) ;
#788=DIRECTION ( 'NONE',  ( -0.000000000000000000, 1.000000000000000000, -0.000000000000000000 ) ) ;
#790=CARTESIAN_POINT ( 'NONE',  ( -4.721056650415999201, 298.4843750017070079, -4.721056650415999201 ) ) ;
#791=CARTESIAN_POINT ( 'NONE',  ( 10.00000000000000178, 135.0000000000000000, 0.000000000000000000 ) ) ;
#793=CARTESIAN_POINT ( 'NONE',  ( -4.088227598258586603E-16, 289.3593750017070079, -6.676582343750001591 ) ) ;
#806=CARTESIAN_POINT ( 'NONE',  ( -2.085542519210945728E-15, 29.53124999658601624, 11.35316468750000141 ) ) ;
#808=CARTESIAN_POINT ( 'NONE',  ( -9.832129032723418760, 218.1770833299193555, -5.676582343750004256 ) ) ;
#809=CARTESIAN_POINT ( 'NONE',  ( 0.000000000000000000, 300.0000000000000000, 0.000000000000000000 ) ) ;
#814=CARTESIAN_POINT ( 'NONE',  ( -3.042071309553164404, 17.23958332991935194, -11.35316468749999963 ) ) ;
#821=CARTESIAN_POINT ( 'NONE',  ( -5.676582343749998039, 22.44791666325268409, -9.832129032723420536 ) ) ;
#824=CARTESIAN_POINT ( 'NONE',  ( -11.35316468749999785, 143.0729166632526983, -3.042071309553167513 ) ) ;
#825=CARTESIAN_POINT ( 'NONE',  ( -10.00000000000000000, 109.1666666598386968, -2.679491924311229845 ) ) ;
#830=CARTESIAN_POINT ( 'NONE',  ( -2.085542519210945728E-15, 14.84374999658601624, 11.35316468750000141 ) ) ;
#834=CARTESIAN_POINT ( 'NONE',  ( -2.765530957081998586, 296.6406250017069510, 6.676582343750001591 ) ) ;
#835=CARTESIAN_POINT ( 'NONE',  ( 5.676582343749993598, 144.9479166632526983, 9.832129032723422313 ) ) ;
#841=ORIENTED_EDGE ( 'NONE', *, *, #24658, .F. ) ;
#843=CARTESIAN_POINT ( 'NONE',  ( -10.00000000000000000, 204.1666666598387110, -2.679491924311229845 ) ) ;
#846=CARTESIAN_POINT ( 'NONE',  ( 5.676582343750001591, 91.92708332991935549, -9.832129032723420536 ) ) ;
#847=ORIENTED_EDGE ( 'NONE', *, *, #10496, .T. ) ;
#877=CARTESIAN_POINT ( 'NONE',  ( -7.320508075688773708, 91.87500000000001421, -7.320508075688774596 ) ) ;
#879=CARTESIAN_POINT ( 'NONE',  ( 5.676582343750001591, 66.92708332991935549, -9.832129032723420536 ) ) ;
#880=CARTESIAN_POINT ( 'NONE',  ( 2.765530957081996366, 298.2968750017069510, -6.676582343750003368 ) ) ;
#887=CARTESIAN_POINT ( 'NONE',  ( 7.320508075688781702, 85.62500000000000000, -7.320508075688781702 ) ) ;
#892=CARTESIAN_POINT ( 'NONE',  ( 10.00000000000000178, 220.2083333333333428, -2.679491924311226736 ) ) ;
#894=CARTESIAN_POINT ( 'NONE',  ( 11.35316468749999785, 185.8854166632526983, 3.042071309553174174 ) ) ;
#897=CARTESIAN_POINT ( 'NONE',  ( 8.660254037844385522, 86.45833332650538239, 5.000000000000005329 ) ) ;
#898=ORIENTED_EDGE ( 'NONE', *, *, #73539, .T. ) ;
#900=CARTESIAN_POINT ( 'NONE',  ( -11.35316468750000141, 38.59374999658601979, -1.390361679473963753E-15 ) ) ;
#908=CARTESIAN_POINT ( 'NONE',  ( 10.00000000000000178, 72.08333332650536818, -2.679491924311226736 ) ) ;
#911=CARTESIAN_POINT ( 'NONE',  ( 7.320508075688808347, 64.37500000000002842, 7.320508075688812788 ) ) ;
#912=CARTESIAN_POINT ( 'NONE',  ( -4.999999999999998224, 48.54166665983870388, -8.660254037844389075 ) ) ;
#913=CARTESIAN_POINT ( 'NONE',  ( 8.660254037844389075, 102.2916666598386968, -5.000000000000000000 ) ) ;
#914=EDGE_LOOP ( 'NONE', ( #12849, #200, #42003, #17496 ) ) ;
#917=CARTESIAN_POINT ( 'NONE',  ( -3.673940397442060854E-16, 288.7500000000000000, -6.000000000000001776 ) ) ;
#918=CARTESIAN_POINT ( 'NONE',  ( -2.765530957081996810, 296.4218750017070079, -6.676582343750003368 ) ) ;
#922=CARTESIAN_POINT ( 'NONE',  ( -9.832129032723420536, 153.6979166632526983, 5.676582343749997150 ) ) ;
#924=CARTESIAN_POINT ( 'NONE',  ( -1.836970198721029983E-15, 3.750000000000000444, 10.00000000000000178 ) ) ;
#932=CARTESIAN_POINT ( 'NONE',  ( -11.35316468750000141, 123.8020833299193413, 3.042071309553159963 ) ) ;
#937=CARTESIAN_POINT ( 'NONE',  ( 9.832129032723420536, 46.51041666325269119, -5.676582343749999815 ) ) ;
#943=CARTESIAN_POINT ( 'NONE',  ( 1.102182119232618108E-15, 292.3125000034140157, 6.000000000000001776 ) ) ;
#961=ORIENTED_EDGE ( 'NONE', *, *, #44827, .T. ) ;
#963=ORIENTED_EDGE ( 'NONE', *, *, #56687, .F. ) ;
#966=CARTESIAN_POINT ( 'NONE',  ( 7.320508075688771044, 59.37500000000000711, 7.320508075688775484 ) ) ;
#970=VECTOR ( 'NONE', #14893, 1000.000000000000000 ) ;
#971=CARTESIAN_POINT ( 'NONE',  ( -2.679491924311226292, 33.33333332650536107, -10.00000000000000178 ) ) ;
#978=CARTESIAN_POINT ( 'NONE',  ( -10.00000000000000355, 147.7083333333333144, 2.679491924311223183 ) ) ;
#980=CARTESIAN_POINT ( 'NONE',  ( 8.660254037844385522, 169.5833333333333428, 5.000000000000005329 ) ) ;
#983=CARTESIAN_POINT ( 'NONE',  ( -2.085542519210945728E-15, 144.8437499965860411, 11.35316468750000141 ) ) ;
#988=ORIENTED_EDGE ( 'NONE', *, *, #71663, .F. ) ;
#996=CARTESIAN_POINT ( 'NONE',  ( 8.660254037844389075, 42.29166665983870388, -5.000000000000000000 ) ) ;
#1005=CARTESIAN_POINT ( 'NONE',  ( -0.6562093533523021271, 225.9999999999999716, -10.00003937256114028 ) ) ;
#1008=CARTESIAN_POINT ( 'NONE',  ( 11.35316468749999963, 110.9895833299193697, -3.042071309553165293 ) ) ;
#1016=CARTESIAN_POINT ( 'NONE',  ( 3.042071309553167513, 96.82291666325269830, -11.35316468749999785 ) ) ;
#1020=CARTESIAN_POINT ( 'NONE',  ( 10.00000000000008882, 174.7916666666666856, 2.679491924311259154 ) ) ;
#1022=CARTESIAN_POINT ( 'NONE',  ( -8.660254037844390851, 194.7916666598387110, 4.999999999999998224 ) ) ;
#1025=CARTESIAN_POINT ( 'NONE',  ( 9.832129032723420536, 91.51041666325268409, -5.676582343749999815 ) ) ;
#1029=CARTESIAN_POINT ( 'NONE',  ( 8.311093377946837890, 6.718749996586016238, -8.311093377946837890 ) ) ;
#1031=CARTESIAN_POINT ( 'NONE',  ( -8.660254037844394404, 137.0833333333333428, -5.000000000000008882 ) ) ;
#1033=CARTESIAN_POINT ( 'NONE',  ( -9.832129032723418760, 222.8645833299193839, -5.676582343750004256 ) ) ;
#1037=CARTESIAN_POINT ( 'NONE',  ( 4.721056650415999201, 292.0781250017069510, -4.721056650415999201 ) ) ;
#1040=CARTESIAN_POINT ( 'NONE',  ( -5.676582343749998039, 202.7604166632526983, -9.832129032723420536 ) ) ;
#1050=CARTESIAN_POINT ( 'NONE',  ( 4.999999999999993783, 29.16666666666666785, 8.660254037844390851 ) ) ;
#1060=CARTESIAN_POINT ( 'NONE',  ( 2.765530957082001251, 295.7656250017069510, 6.676582343749999815 ) ) ;
#1064=ORIENTED_EDGE ( 'NONE', *, *, #62606, .T. ) ;
#1068=ORIENTED_EDGE ( 'NONE', *, *, #43318, .T. ) ;
#1070=CARTESIAN_POINT ( 'NONE',  ( 11.35316468749999785, 95.88541666325269830, 3.042071309553174174 ) ) ;
#1075=CARTESIAN_POINT ( 'NONE',  ( -1.328591152368359007E-11, 1.250000000001033174, -10.00000000000000533 ) ) ;
#1080=CARTESIAN_POINT ( 'NONE',  ( 3.042071309553159519, 209.7395833299193839, 11.35316468750000141 ) ) ;
#1086=CARTESIAN_POINT ( 'NONE',  ( -5.676582343750006032, 174.4270833299193555, 9.832129032723418760 ) ) ;
#1092=CARTESIAN_POINT ( 'NONE',  ( 9.832129032723416984, 70.36458332991936970, 5.676582343750006032 ) ) ;
#1098=CARTESIAN_POINT ( 'NONE',  ( 11.35316468749999963, 80.98958332991934128, -3.042071309553165293 ) ) ;
#1103=CARTESIAN_POINT ( 'NONE',  ( -9.832129032723418760, 62.86458332991935549, -5.676582343750004256 ) ) ;
#1108=CARTESIAN_POINT ( 'NONE',  ( -10.00000000000000355, 149.5833333265053398, 2.679491924311223183 ) ) ;
#1110=CARTESIAN_POINT ( 'NONE',  ( -7.320508075688778149, 54.99999999317203958, 7.320508075688769267 ) ) ;
#1111=CARTESIAN_POINT ( 'NONE',  ( -11.35316468750000141, 48.59374999658601268, -1.390361679473963753E-15 ) ) ;
#1113=CARTESIAN_POINT ( 'NONE',  ( -2.085542519210945728E-15, 189.5312499965860127, 11.35316468750000141 ) ) ;
#1114=ORIENTED_EDGE ( 'NONE', *, *, #36215, .T. ) ;
#1117=CARTESIAN_POINT ( 'NONE',  ( -1.836970198721029983E-15, 160.6249999931720254, 10.00000000000000178 ) ) ;
#1119=CARTESIAN_POINT ( 'NONE',  ( -11.35316468749999785, 178.0729166632526983, -3.042071309553167957 ) ) ;
#1124=CARTESIAN_POINT ( 'NONE',  ( -8.311093377946836114, 167.9687499965860127, -8.311093377946837890 ) ) ;
#1127=CARTESIAN_POINT ( 'NONE',  ( -3.042071309553173730, 134.6354166632526983, 11.35316468749999785 ) ) ;
#1135=CARTESIAN_POINT ( 'NONE',  ( -8.660254037844390851, 187.9166666666666856, 5.000000000000000000 ) ) ;
#1155=CARTESIAN_POINT ( 'NONE',  ( 2.765530957081996366, 296.2968750017070079, -6.676582343750002480 ) ) ;
#1156=CARTESIAN_POINT ( 'NONE',  ( -8.660254037844390851, 132.9166666666666856, 4.999999999999998224 ) ) ;
#1160=CARTESIAN_POINT ( 'NONE',  ( 4.242640687119285658, 290.6875000034139589, -4.242640687119286547 ) ) ;
#1172=CARTESIAN_POINT ( 'NONE',  ( 8.311093377946837890, 31.40624999658601624, -8.311093377946837890 ) ) ;
#1174=CARTESIAN_POINT ( 'NONE',  ( 6.951808397369818766E-16, 222.3437499965860127, -11.35316468750000141 ) ) ;
#1180=CARTESIAN_POINT ( 'NONE',  ( -11.35316468750000141, 38.28124999658601979, -1.390361679473963753E-15 ) ) ;
#1186=CARTESIAN_POINT ( 'NONE',  ( 3.042071309553167513, 16.82291666325268054, -11.35316468749999785 ) ) ;
#1188=CARTESIAN_POINT ( 'NONE',  ( -5.676582343750006032, 149.1145833299193555, 9.832129032723418760 ) ) ;
#1190=CARTESIAN_POINT ( 'NONE',  ( -1.836970198721029983E-15, 115.6249999931720396, 10.00000000000000178 ) ) ;
#1192=CARTESIAN_POINT ( 'NONE',  ( 10.00000000000000178, 171.8749999931720538, 0.000000000000000000 ) ) ;
#1195=CARTESIAN_POINT ( 'NONE',  ( 11.35316468749999785, 10.88541666325268409, 3.042071309553174174 ) ) ;
#1197=ORIENTED_EDGE ( 'NONE', *, *, #65708, .F. ) ;
#1198=FACE_OUTER_BOUND ( 'NONE', #54810, .T. ) ;
#1199=CARTESIAN_POINT ( 'NONE',  ( 6.676582343750003368, 297.0156250017070079, -2.765530957081997254 ) ) ;
#1201=CARTESIAN_POINT ( 'NONE',  ( 11.35316468749999963, 140.9895833299193555, -3.042071309553165293 ) ) ;
#1209=CARTESIAN_POINT ( 'NONE',  ( -7.320508075688778149, 204.9999999931720254, 7.320508075688769267 ) ) ;
#1212=CARTESIAN_POINT ( 'NONE',  ( -9.832129032723420536, 84.01041666325268409, 5.676582343749997150 ) ) ;
#1233=CYLINDRICAL_SURFACE ( 'NONE', #14076, 10.00000000000000178 ) ;
#1245=CARTESIAN_POINT ( 'NONE',  ( 7.320508075688771044, 99.37500000000000000, 7.320508075688775484 ) ) ;
#1248=CARTESIAN_POINT ( 'NONE',  ( -8.311093377946836114, 67.96874999658602690, -8.311093377946837890 ) ) ;
#1249=CARTESIAN_POINT ( 'NONE',  ( -2.765530957081996810, 295.4218750017069510, -6.676582343750003368 ) ) ;
#1254=CARTESIAN_POINT ( 'NONE',  ( 8.660254037844392627, 84.58333333333334281, 5.000000000000010658 ) ) ;
#1259=CARTESIAN_POINT ( 'NONE',  ( 4.999999999999993783, 214.1666666666666856, 8.660254037844390851 ) ) ;
#1261=CARTESIAN_POINT ( 'NONE',  ( -5.676582343750006032, 179.4270833299193555, 9.832129032723418760 ) ) ;
#1268=CARTESIAN_POINT ( 'NONE',  ( 6.951808397369818766E-16, 32.34374999658601268, -11.35316468750000141 ) ) ;
#1270=CARTESIAN_POINT ( 'NONE',  ( 8.311093377946837890, 221.7187499965860127, -8.311093377946837890 ) ) ;
#1272=CARTESIAN_POINT ( 'NONE',  ( -10.00000000000000178, 124.3749999931720396, -1.224646799147353454E-15 ) ) ;
#1279=CARTESIAN_POINT ( 'NONE',  ( -1.836970198721029983E-15, 70.62499999317203958, 10.00000000000000178 ) ) ;
#1283=CYLINDRICAL_SURFACE ( 'NONE', #13157, 10.00000000000000178 ) ;
#1287=CARTESIAN_POINT ( 'NONE',  ( -4.088227598258586603E-16, 297.3593750017070079, -6.676582343750001591 ) ) ;
#1290=CARTESIAN_POINT ( 'NONE',  ( -5.676582343749998039, 157.4479166632526983, -9.832129032723420536 ) ) ;
#1296=ORIENTED_EDGE ( 'NONE', *, *, #23196, .T. ) ;
#1298=CARTESIAN_POINT ( 'NONE',  ( 5.676582343749993598, 135.2604166632526983, 9.832129032723422313 ) ) ;
#1302=CARTESIAN_POINT ( 'NONE',  ( 5.676582343750001591, 46.92708332991934839, -9.832129032723420536 ) ) ;
#1309=CARTESIAN_POINT ( 'NONE',  ( -6.000000000000000888, 291.1250000034140157, 2.485281374238575758 ) ) ;
#1320=AXIS2_PLACEMENT_3D ( 'NONE', #19498, #54600, #37239 ) ;
#1335=CARTESIAN_POINT ( 'NONE',  ( 8.660254037844385522, 59.58333333333333570, 5.000000000000005329 ) ) ;
#1340=ORIENTED_EDGE ( 'NONE', *, *, #49128, .F. ) ;
#1346=CARTESIAN_POINT ( 'NONE',  ( -5.000000000000005329, 140.2083333265053682, 8.660254037844387298 ) ) ;
#1347=CARTESIAN_POINT ( 'NONE',  ( 10.00000000000000178, 180.0000000000000284, 0.000000000000000000 ) ) ;
#1351=CARTESIAN_POINT ( 'NONE',  ( 9.832129032723420536, 141.5104166632526699, -5.676582343749999815 ) ) ;
#1362=CARTESIAN_POINT ( 'NONE',  ( 7.320508075688771044, 41.24999999317203248, 7.320508075688775484 ) ) ;
#1370=ORIENTED_EDGE ( 'NONE', *, *, #537, .T. ) ;
#1371=( BOUNDED_CURVE ( )  B_SPLINE_CURVE ( 2, ( #6092, #44592, #11373, #57410, #4603, #27981, #45694, #45326, #57035, #22301, #74366, #51356, #5347 ),
 .UNSPECIFIED., .F., .F. ) 
 B_SPLINE_CURVE_WITH_KNOTS ( ( 3, 2, 2, 2, 2, 2, 3 ),
 ( 2.621882283550707182, 2.627116002474152889, 2.632349721397599041, 2.637583440321044304, 2.642817159244490011, 2.648050878167936162, 2.653284597091381869 ),
 .UNSPECIFIED. ) 
 CURVE ( )  GEOMETRIC_REPRESENTATION_ITEM ( )  RATIONAL_B_SPLINE_CURVE ( ( 1.000000000000350830, 0.9659258262887174817, 1.000000000000000000, 0.9659258262890683122, 1.000000000000000000, 0.9659258262890683122, 1.000000000000000000, 0.9659258262890683122, 1.000000000000000000, 0.9659258262890683122, 1.000000000000000000, 0.9659258262890662028, 1.000000000000001998 ) ) 
 REPRESENTATION_ITEM ( '' )  );
#1377=CARTESIAN_POINT ( 'NONE',  ( 9.832129032723416984, 120.3645833299193697, 5.676582343750006032 ) ) ;
#1385=CARTESIAN_POINT ( 'NONE',  ( -9.832129032723420536, 113.6979166632526983, 5.676582343749997150 ) ) ;
#1390=CARTESIAN_POINT ( 'NONE',  ( -10.00000000000000355, 199.5833333265053398, 2.679491924311223183 ) ) ;
#1393=CARTESIAN_POINT ( 'NONE',  ( -8.311093377946836114, 107.9687499965860269, -8.311093377946837890 ) ) ;
#1397=CARTESIAN_POINT ( 'NONE',  ( -11.35316468750000141, 3.593749996586016682, -1.390361679473963753E-15 ) ) ;
#1398=( BOUNDED_CURVE ( )  B_SPLINE_CURVE ( 2, ( #23400, #57756, #70539, #47513, #6798, #57380, #5690, #41497, #6439, #41131, #12446, #28688, #17365, #17738, #51702, #23032, #30176, #52088, #790, #18117, #48, #35478, #40388, #35845, #63762, #6061, #41861, #63387, #58859, #34751, #64138, #46041, #29067, #69060, #420, #69429, #11711, #53193, #24133, #29441, #46415, #52820, #12080, #35116, #58130, #52452, #1529, #23774, #58492, #46777, #69801, #18854, #29810, #1155, #70178, #71630, #48253, #3362, #60319, #20703, #60701, #36577, #9021, #25972, #43721, #43336, #26352, #19579, #7903, #13908, #66356, #2242, #42594, #72005, #13175, #13538, #48995, #37701, #42222, #49373, #54309, #36211, #59228, #20320, #59952, #19952, #65980, #7540, #70902, #71260, #30546, #1878, #32035, #30909, #2620, #42961, #53562, #14284, #65234, #37322, #14660, #59590, #24864, #19217, #55055, #53929, #8647, #47883, #25236, #65609, #36947, #8267, #31281, #72390, #2988, #25610, #48623, #31661, #54682, #21450, #50128, #66734, #73886, #10140, #44847, #73144, #67486, #5235, #15039, #51244, #44473, #32796, #38075, #10515, #3738, #74255, #15784, #55429, #38821, #28236, #72774, #62557, #22190, #22563, #67112, #10888, #4120, #61074, #61822, #26737, #39563, #67854, #33178, #4865, #45215, #56922, #27861, #39184, #9396, #33922, #68226, #32416, #56176, #9777, #49757, #38447, #16523, #4489, #21080, #44104, #27480, #15407, #50494, #27113, #61450, #55804, #73507, #21814, #16145, #62188, #33547, #56548, #50870, #68974, #23318, #46330, #35035, #6720, #64058, #34291, #35404, #40300, #707 ),
 .UNSPECIFIED., .F., .F. ) 
 B_SPLINE_CURVE_WITH_KNOTS ( ( 3, 2, 2, 2, 2, 2, 2, 2, 2, 2, 2, 2, 2, 2, 2, 2, 2, 2, 2, 2, 2, 2, 2, 2, 2, 2, 2, 2, 2, 2, 2, 2, 2, 2, 2, 2, 2, 2, 2, 2, 2, 2, 2, 2, 2, 2, 2, 2, 2, 2, 2, 2, 2, 2, 2, 2, 2, 2, 2, 2, 2, 2, 2, 2, 2, 2, 2, 2, 2, 2, 2, 2, 2, 2, 2, 2, 2, 2, 2, 2, 2, 2, 2, 2, 2, 2, 2, 2, 2, 2, 2, 2, 2, 2, 2, 2, 3 ),
 ( 0.000000000000000000, 0.01041666666666666609, 0.02083333333333333218, 0.03125000000000000000, 0.04166666666666666435, 0.05208333333333333565, 0.06250000000000000000, 0.07291666666666667129, 0.08333333333333332871, 0.09375000000000000000, 0.1041666666666666713, 0.1145833333333333287, 0.1250000000000000000, 0.1354166666666666574, 0.1458333333333333426, 0.1562500000000000000, 0.1666666666666666574, 0.1770833333333333426, 0.1875000000000000000, 0.1979166666666666574, 0.2083333333333333426, 0.2187500000000000000, 0.2291666666666666574, 0.2395833333333333426, 0.2500000000000000000, 0.2604166666666666852, 0.2708333333333333148, 0.2812500000000000000, 0.2916666666666666852, 0.3020833333333333148, 0.3125000000000000000, 0.3229166666666666852, 0.3333333333333333148, 0.3437500000000000000, 0.3541666666666666852, 0.3645833333333333148, 0.3750000000000000000, 0.3854166666666666852, 0.3958333333333333148, 0.4062500000000000000, 0.4166666666666666852, 0.4270833333333333148, 0.4375000000000000000, 0.4479166666666666852, 0.4583333333333333148, 0.4687500000000000000, 0.4791666666666666852, 0.4895833333333333148, 0.5000000000000000000, 0.5104166666666666297, 0.5208333333333333703, 0.5312500000000000000, 0.5416666666666666297, 0.5520833333333333703, 0.5625000000000000000, 0.5729166666666666297, 0.5833333333333333703, 0.5937500000000000000, 0.6041666666666666297, 0.6145833333333333703, 0.6250000000000000000, 0.6354166666666666297, 0.6458333333333333703, 0.6562500000000000000, 0.6666666666666666297, 0.6770833333333333703, 0.6875000000000000000, 0.6979166666666666297, 0.7083333333333333703, 0.7187500000000000000, 0.7291666666666666297, 0.7395833333333333703, 0.7500000000000000000, 0.7604166666666666297, 0.7708333333333333703, 0.7812500000000000000, 0.7916666666666666297, 0.8020833333333333703, 0.8125000000000000000, 0.8229166666666666297, 0.8333333333333333703, 0.8437500000000000000, 0.8541666666666666297, 0.8645833333333333703, 0.8750000000000000000, 0.8854166666666666297, 0.8958333333333333703, 0.9062500000000000000, 0.9166666666666666297, 0.9270833333333333703, 0.9375000000000000000, 0.9479166666666666297, 0.9583333333333333703, 0.9687500000000000000, 0.9791666666666666297, 0.9895833333333333703, 1.000000000000000000 ),
 .UNSPECIFIED. ) 
 CURVE ( )  GEOMETRIC_REPRESENTATION_ITEM ( )  RATIONAL_B_SPLINE_CURVE ( ( 1.000000000000000000, 0.9238795325112867385, 1.000000000000000000, 0.9238795325112867385, 1.000000000000000000, 0.9238795325112867385, 1.000000000000000000, 0.9238795325112867385, 1.000000000000000000, 0.9238795325112867385, 1.000000000000000000, 0.9238795325112867385, 1.000000000000000000, 0.9238795325112867385, 1.000000000000000000, 0.9238795325112867385, 1.000000000000000000, 0.9238795325112867385, 1.000000000000000000, 0.9238795325112867385, 1.000000000000000000, 0.9238795325112867385, 1.000000000000000000, 0.9238795325112867385, 1.000000000000000000, 0.9238795325112867385, 1.000000000000000000, 0.9238795325112867385, 1.000000000000000000, 0.9238795325112867385, 1.000000000000000000, 0.9238795325112867385, 1.000000000000000000, 0.9238795325112867385, 1.000000000000000000, 0.9238795325112867385, 1.000000000000000000, 0.9238795325112867385, 1.000000000000000000, 0.9238795325112867385, 1.000000000000000000, 0.9238795325112867385, 1.000000000000000000, 0.9238795325112867385, 1.000000000000000000, 0.9238795325112867385, 1.000000000000000000, 0.9238795325112867385, 1.000000000000000000, 0.9238795325112867385, 1.000000000000000000, 0.9238795325112867385, 1.000000000000000000, 0.9238795325112867385, 1.000000000000000000, 0.9238795325112867385, 1.000000000000000000, 0.9238795325112867385, 1.000000000000000000, 0.9238795325112867385, 1.000000000000000000, 0.9238795325112867385, 1.000000000000000000, 0.9238795325112867385, 1.000000000000000000, 0.9238795325112867385, 1.000000000000000000, 0.9238795325112867385, 1.000000000000000000, 0.9238795325112867385, 1.000000000000000000, 0.9238795325112867385, 1.000000000000000000, 0.9238795325112867385, 1.000000000000000000, 0.9238795325112867385, 1.000000000000000000, 0.9238795325112867385, 1.000000000000000000, 0.9238795325112867385, 1.000000000000000000, 0.9238795325112867385, 1.000000000000000000, 0.9238795325112867385, 1.000000000000000000, 0.9238795325112867385, 1.000000000000000000, 0.9238795325112867385, 1.000000000000000000, 0.9238795325112867385, 1.000000000000000000, 0.9238795325112867385, 1.000000000000000000, 0.9238795325112867385, 1.000000000000000000, 0.9238795325112867385, 1.000000000000000000, 0.9238795325112867385, 1.000000000000000000, 0.9238795325112867385, 1.000000000000000000, 0.9238795325112867385, 1.000000000000000000, 0.9238795325112867385, 1.000000000000000000, 0.9238795325112867385, 1.000000000000000000, 0.9238795325112867385, 1.000000000000000000, 0.9238795325112867385, 1.000000000000000000, 0.9238795325112867385, 1.000000000000000000, 0.9238795325112867385, 1.000000000000000000, 0.9238795325112867385, 1.000000000000000000, 0.9238795325112867385, 1.000000000000000000, 0.9238795325112867385, 1.000000000000000000, 0.9238795325112867385, 1.000000000000000000, 0.9238795325112867385, 1.000000000000000000, 0.9238795325112867385, 1.000000000000000000, 0.9238795325112867385, 1.000000000000000000, 0.9238795325112867385, 1.000000000000000000, 0.9238795325112867385, 1.000000000000000000, 0.9238795325112867385, 1.000000000000000000, 0.9238795325112867385, 1.000000000000000000, 0.9238795325112867385, 1.000000000000000000, 0.9238795325112867385, 1.000000000000000000, 0.9238795325112867385, 1.000000000000000000, 0.9238795325112867385, 1.000000000000000000, 0.9238795325112867385, 1.000000000000000000, 0.9238795325112867385, 1.000000000000000000, 0.9238795325112867385, 1.000000000000000000, 0.9238795325112867385, 1.000000000000000000, 0.9238795325112867385, 1.000000000000000000, 0.9238795325112867385, 1.000000000000000000, 0.9238795325112867385, 1.000000000000000000, 0.9238795325112867385, 1.000000000000000000, 0.9238795325112867385, 1.000000000000000000, 0.9238795325112867385, 1.000000000000000000, 0.9238795325112867385, 1.000000000000000000, 0.9238795325112867385, 1.000000000000000000, 0.9238795325112867385, 1.000000000000000000, 0.9238795325112867385, 1.000000000000000000, 0.9238795325112867385, 1.000000000000000000, 0.9238795325112867385, 1.000000000000000000, 0.9238795325112867385, 1.000000000000000000, 0.9238795325112867385, 1.000000000000000000, 0.9238795325112867385, 1.000000000000000000, 0.9238795325112867385, 1.000000000000000000, 0.9238795325112867385, 1.000000000000000000, 0.9238795325112867385, 1.000000000000000000, 0.9238795325112867385, 1.000000000000000000, 0.9238795325112867385, 1.000000000000000000 ) ) 
 REPRESENTATION_ITEM ( '' )  );
#1407=CARTESIAN_POINT ( 'NONE',  ( -6.676582343750000703, 291.5156250017069510, 2.765530957082001251 ) ) ;
#1409=CARTESIAN_POINT ( 'NONE',  ( -11.35316468749999785, 208.3854166632526699, -3.042071309553167957 ) ) ;
#1419=CARTESIAN_POINT ( 'NONE',  ( -4.999999999999998224, 31.66666666666666785, -8.660254037844389075 ) ) ;
#1421=CARTESIAN_POINT ( 'NONE',  ( -1.300830538084598961E-11, 173.7499999999989768, 10.00000000000000178 ) ) ;
#1426=CARTESIAN_POINT ( 'NONE',  ( 6.123233995736767268E-16, 223.1249999931720254, -10.00000000000000178 ) ) ;
#1430=CARTESIAN_POINT ( 'NONE',  ( 0.4589999999999999636, 267.1439999999997212, 5.793779103867645830 ) ) ;
#1431=CARTESIAN_POINT ( 'NONE',  ( 6.676582343750001591, 296.9531250017069510, -8.176455196517173205E-16 ) ) ;
#1442=CARTESIAN_POINT ( 'NONE',  ( -8.311093377946836114, 107.9687499965860269, -8.311093377946837890 ) ) ;
#1443=CARTESIAN_POINT ( 'NONE',  ( 1.102182119232618108E-15, 295.3125000034140157, 6.000000000000001776 ) ) ;
#1451=CARTESIAN_POINT ( 'NONE',  ( -2.679491924311226292, 178.3333333265053966, -10.00000000000000178 ) ) ;
#1452=CARTESIAN_POINT ( 'NONE',  ( -3.042071309553173730, 209.3229166632526983, 11.35316468749999785 ) ) ;
#1456=CARTESIAN_POINT ( 'NONE',  ( 3.042071309553159519, 185.0520833299193555, 11.35316468750000141 ) ) ;
#1463=CARTESIAN_POINT ( 'NONE',  ( -9.832129032723420536, 68.69791666325268409, 5.676582343749997150 ) ) ;
#1466=VERTEX_POINT ( 'NONE', #42984 ) ;
#1469=CARTESIAN_POINT ( 'NONE',  ( -8.311093377946841443, 73.90624999658601268, 8.311093377946830785 ) ) ;
#1474=CARTESIAN_POINT ( 'NONE',  ( -11.35316468750000141, 78.48958332991935549, 3.042071309553159963 ) ) ;
#1477=CARTESIAN_POINT ( 'NONE',  ( -7.320508075688773708, 158.7499999931720254, -7.320508075688774596 ) ) ;
#1479=EDGE_CURVE ( 'NONE', #27743, #58925, #3013, .T. ) ;
#1481=CARTESIAN_POINT ( 'NONE',  ( -7.320508075688773708, 53.74999999317203248, -7.320508075688774596 ) ) ;
#1482=CARTESIAN_POINT ( 'NONE',  ( -5.676582343749998039, 47.76041666325269119, -9.832129032723420536 ) ) ;
#1484=CARTESIAN_POINT ( 'NONE',  ( -9.832129032723418760, 192.8645833299193839, -5.676582343750004256 ) ) ;
#1485=ORIENTED_EDGE ( 'NONE', *, *, #72310, .F. ) ;
#1488=CARTESIAN_POINT ( 'NONE',  ( 5.000000000000001776, 162.7083333265053966, -8.660254037844389075 ) ) ;
#1490=CARTESIAN_POINT ( 'NONE',  ( -9.832129032723418760, 177.8645833299193555, -5.676582343750004256 ) ) ;
#1493=CARTESIAN_POINT ( 'NONE',  ( -2.679491924311235174, 190.4166666598387110, 10.00000000000000000 ) ) ;
#1494=ORIENTED_EDGE ( 'NONE', *, *, #21867, .T. ) ;
#1495=CARTESIAN_POINT ( 'NONE',  ( -3.042071309553173730, 174.6354166632526983, 11.35316468749999785 ) ) ;
#1497=VECTOR ( 'NONE', #16945, 1000.000000000000000 ) ;
#1499=CARTESIAN_POINT ( 'NONE',  ( 8.162799457232734923, 225.9999999999999716, -7.016166167730306213 ) ) ;
#1500=ORIENTED_EDGE ( 'NONE', *, *, #22513, .T. ) ;
#1523=ORIENTED_EDGE ( 'NONE', *, *, #9043, .T. ) ;
#1529=CARTESIAN_POINT ( 'NONE',  ( -4.721056650415998313, 296.7343750017069510, 4.721056650416000089 ) ) ;
#1530=CARTESIAN_POINT ( 'NONE',  ( 4.999999999999993783, 134.1666666666666856, 8.660254037844390851 ) ) ;
#1545=CARTESIAN_POINT ( 'NONE',  ( -8.311093377946836114, 22.65624999658601979, -8.311093377946837890 ) ) ;
#1546=CARTESIAN_POINT ( 'NONE',  ( 5.676582343750001591, 221.9270833299193555, -9.832129032723420536 ) ) ;
#1553=CARTESIAN_POINT ( 'NONE',  ( -3.042071309553164404, 32.23958332991935549, -11.35316468749999963 ) ) ;
#1559=CARTESIAN_POINT ( 'NONE',  ( -9.832129032723418760, 17.86458332991935194, -5.676582343750004256 ) ) ;
#1561=CARTESIAN_POINT ( 'NONE',  ( -9.832129032723418760, 152.8645833299193555, -5.676582343750004256 ) ) ;
#1562=CARTESIAN_POINT ( 'NONE',  ( -7.320508075688778149, 114.9999999931720112, 7.320508075688769267 ) ) ;
#1567=CARTESIAN_POINT ( 'NONE',  ( 8.311093377946834337, 5.468749996586018014, 8.311093377946839666 ) ) ;
#1571=CARTESIAN_POINT ( 'NONE',  ( 5.676582343750001591, 141.6145833299193555, -9.832129032723420536 ) ) ;
#1579=CARTESIAN_POINT ( 'NONE',  ( 5.676582343749993598, 85.26041666325268409, 9.832129032723422313 ) ) ;
#1586=EDGE_CURVE ( 'NONE', #36674, #9475, #9375, .T. ) ;
#1610=CARTESIAN_POINT ( 'NONE',  ( -1.836970198721029983E-15, 88.75000000000001421, 10.00000000000000178 ) ) ;
#1613=CARTESIAN_POINT ( 'NONE',  ( 1.226468279477575784E-15, 296.8593750017070079, 6.676582343750001591 ) ) ;
#1615=CARTESIAN_POINT ( 'NONE',  ( -7.320508075688773708, 173.7499999931719969, -7.320508075688774596 ) ) ;
#1620=CARTESIAN_POINT ( 'NONE',  ( -2.679491924299816752, 51.45833333333229831, -10.00000000000659206 ) ) ;
#1621=CARTESIAN_POINT ( 'NONE',  ( -2.062184786512628451E-11, 138.7499999999984084, 10.00000000000000178 ) ) ;
#1625=CARTESIAN_POINT ( 'NONE',  ( 2.679491924311228956, 216.0416666666666572, -10.00000000000000000 ) ) ;
#1627=CARTESIAN_POINT ( 'NONE',  ( 9.832129032723416984, 180.6770833299193555, 5.676582343750006032 ) ) ;
#1629=DIRECTION ( 'NONE',  ( -0.000000000000000000, 1.000000000000000000, -0.000000000000000000 ) ) ;
#1634=CARTESIAN_POINT ( 'NONE',  ( 9.832129032723416984, 50.67708332991935549, 5.676582343750006032 ) ) ;
#1636=CARTESIAN_POINT ( 'NONE',  ( 9.832129032723420536, 216.5104166632526983, -5.676582343749999815 ) ) ;
#1642=CARTESIAN_POINT ( 'NONE',  ( -5.000000000000005329, 70.20833332650538239, 8.660254037844387298 ) ) ;
#1650=CARTESIAN_POINT ( 'NONE',  ( 4.721056650416000089, 296.9843750017070079, 4.721056650415999201 ) ) ;
#1651=CARTESIAN_POINT ( 'NONE',  ( -1.836970198721029983E-15, 185.6249999931720538, 10.00000000000000178 ) ) ;
#1652=CARTESIAN_POINT ( 'NONE',  ( -8.660254037844396180, 17.91666666666667140, 5.000000000000002665 ) ) ;
#1653=CARTESIAN_POINT ( 'NONE',  ( 5.676582343750001591, 161.6145833299193839, -9.832129032723420536 ) ) ;
#1654=CARTESIAN_POINT ( 'NONE',  ( 0.000000000000000000, 300.0000000000000000, 0.000000000000000000 ) ) ;
#1662=CARTESIAN_POINT ( 'NONE',  ( -3.042071309553163960, 137.5520833299193555, -11.35316468749999963 ) ) ;
#1667=CARTESIAN_POINT ( 'NONE',  ( -3.042071309553173730, 44.63541666325269119, 11.35316468749999785 ) ) ;
#1673=CARTESIAN_POINT ( 'NONE',  ( 4.242640687119287435, 294.4375000034140157, 4.242640687119285658 ) ) ;
#1692=EDGE_LOOP ( 'NONE', ( #54864, #32986, #56743, #35264 ) ) ;
#1694=VERTEX_POINT ( 'NONE', #64454 ) ;
#1698=CARTESIAN_POINT ( 'NONE',  ( -2.679491924311235618, 58.54166666666666430, 10.00000000000000000 ) ) ;
#1701=CARTESIAN_POINT ( 'NONE',  ( -4.242640687119286547, 294.8750000000000000, -4.242640687119286547 ) ) ;
#1708=DIRECTION ( 'NONE',  ( -0.000000000000000000, 1.000000000000000000, -0.000000000000000000 ) ) ;
#1713=CARTESIAN_POINT ( 'NONE',  ( -10.00000000000000355, 172.7083333333333144, 2.679491924311223183 ) ) ;
#1714=CARTESIAN_POINT ( 'NONE',  ( 6.000000000000003553, 297.6250000034140157, -2.485281374238571761 ) ) ;
#1717=CARTESIAN_POINT ( 'NONE',  ( 3.042071309553167069, 147.1354166632526983, -11.35316468749999785 ) ) ;
#1718=CARTESIAN_POINT ( 'NONE',  ( 10.00000000000000000, 26.66666665983870033, 2.679491924311235618 ) ) ;
#1723=CARTESIAN_POINT ( 'NONE',  ( 5.676582343749993598, 5.260416663252683200, 9.832129032723422313 ) ) ;
#1727=CARTESIAN_POINT ( 'NONE',  ( 8.660254037844385522, 31.45833332650536818, 5.000000000000005329 ) ) ;
#1739=CARTESIAN_POINT ( 'NONE',  ( -2.085542519210945728E-15, 109.5312499965860269, 11.35316468750000141 ) ) ;
#1747=CARTESIAN_POINT ( 'NONE',  ( 11.35316468749999785, 110.5729166632526983, 3.042071309553174174 ) ) ;
#1750=CARTESIAN_POINT ( 'NONE',  ( 10.00000000000000711, 50.20833333333334281, -2.679491924311227624 ) ) ;
#1752=CARTESIAN_POINT ( 'NONE',  ( 5.000000000000001776, 207.7083333265053682, -8.660254037844389075 ) ) ;
#1755=CARTESIAN_POINT ( 'NONE',  ( 5.676582343750001591, 101.9270833299193555, -9.832129032723420536 ) ) ;
#1756=CARTESIAN_POINT ( 'NONE',  ( -6.676582343750000703, 287.5156250017069510, 2.765530957082001251 ) ) ;
#1760=CARTESIAN_POINT ( 'NONE',  ( -9.832129032723420536, 9.010416663252684089, 5.676582343749997150 ) ) ;
#1761=VERTEX_POINT ( 'NONE', #41804 ) ;
#1767=CARTESIAN_POINT ( 'NONE',  ( -4.088227598258586603E-16, 291.2031250017069510, -6.676582343750001591 ) ) ;
#1769=CARTESIAN_POINT ( 'NONE',  ( -11.35316468750000141, 223.8020833299193271, 3.042071309553159963 ) ) ;
#1784=CARTESIAN_POINT ( 'NONE',  ( -2.295000000000000373, 278.5679999999998699, 5.413231402903075029 ) ) ;
#1785=CARTESIAN_POINT ( 'NONE',  ( 6.676582343750003368, 291.8906250017069510, 2.765530957081995478 ) ) ;
#1788=ORIENTED_EDGE ( 'NONE', *, *, #39922, .F. ) ;
#1791=( BOUNDED_CURVE ( )  B_SPLINE_CURVE ( 2, ( #71488, #2476, #18350, #30408, #53426, #42819, #19442, #1750, #41363, #24372, #30772, #37178, #70763 ),
 .UNSPECIFIED., .F., .F. ) 
 B_SPLINE_CURVE_WITH_KNOTS ( ( 3, 2, 2, 2, 2, 2, 3 ),
 ( 0.6122908167314494721, 0.6175241636365315090, 0.6227575105416134349, 0.6279908574466953608, 0.6332242043517773977, 0.6384575512568593236, 0.6436908981619412495 ),
 .UNSPECIFIED. ) 
 CURVE ( )  GEOMETRIC_REPRESENTATION_ITEM ( )  RATIONAL_B_SPLINE_CURVE ( ( 0.9999999999999901190, 0.9659258262890781932, 1.000000000000000000, 0.9659258262890683122, 1.000000000000000000, 0.9659258262890683122, 1.000000000000000000, 0.9659258262890683122, 1.000000000000000000, 0.9659258262890683122, 1.000000000000000000, 0.9659258262892301827, 0.9999999999998381295 ) ) 
 REPRESENTATION_ITEM ( '' )  );
#1793=EDGE_LOOP ( 'NONE', ( #56973, #6881, #4793, #66703 ) ) ;
#1795=CARTESIAN_POINT ( 'NONE',  ( 3.042071309553167069, 102.1354166632526983, -11.35316468749999785 ) ) ;
#1801=ORIENTED_EDGE ( 'NONE', *, *, #26764, .F. ) ;
#1803=CARTESIAN_POINT ( 'NONE',  ( -11.35316468750000141, 218.4895833299193271, 3.042071309553159963 ) ) ;
#1808=CARTESIAN_POINT ( 'NONE',  ( -11.35316468750000141, 193.8020833299193271, 3.042071309553159963 ) ) ;
#1815=CARTESIAN_POINT ( 'NONE',  ( 11.35316468749999963, 70.98958332991934128, -3.042071309553165293 ) ) ;
#1822=CARTESIAN_POINT ( 'NONE',  ( 6.951808397369818766E-16, 77.03124999658601268, -11.35316468750000141 ) ) ;
#1828=CARTESIAN_POINT ( 'NONE',  ( 11.35316468749999963, 70.98958332991935549, -3.042071309553165293 ) ) ;
#1832=CARTESIAN_POINT ( 'NONE',  ( -10.00000000000000000, 174.1666666598386826, -2.679491924311229845 ) ) ;
#1836=CARTESIAN_POINT ( 'NONE',  ( -3.042071309553163960, 62.55208332991934839, -11.35316468749999963 ) ) ;
#1839=CARTESIAN_POINT ( 'NONE',  ( 9.832129032723416984, 195.3645833299193839, 5.676582343750006032 ) ) ;
#1844=CARTESIAN_POINT ( 'NONE',  ( 11.35316468749999963, 195.9895833299193555, -3.042071309553165293 ) ) ;
#1849=CARTESIAN_POINT ( 'NONE',  ( -5.676582343750006032, 184.4270833299193555, 9.832129032723418760 ) ) ;
#1854=CARTESIAN_POINT ( 'NONE',  ( -8.660254037844390851, 2.916666666666666963, 4.999999999999998224 ) ) ;
#1859=CARTESIAN_POINT ( 'NONE',  ( -10.00000000000000533, 187.5000000000000000, -1.224646799147353848E-15 ) ) ;
#1860=ORIENTED_EDGE ( 'NONE', *, *, #28662, .T. ) ;
#1871=VERTEX_POINT ( 'NONE', #71944 ) ;
#1874=CARTESIAN_POINT ( 'NONE',  ( 7.320508075688771044, 91.24999999317203958, 7.320508075688775484 ) ) ;
#1876=LINE ( 'NONE', #48251, #31423 ) ;
#1878=CARTESIAN_POINT ( 'NONE',  ( 2.765530957082001251, 293.9218750017069510, 6.676582343749999815 ) ) ;
#1879=CARTESIAN_POINT ( 'NONE',  ( 7.320508075688771044, 134.3749999999999716, 7.320508075688775484 ) ) ;
#1891=CARTESIAN_POINT ( 'NONE',  ( -3.673940397442060854E-16, 288.8125000034140157, -6.000000000000001776 ) ) ;
#1894=CARTESIAN_POINT ( 'NONE',  ( 5.676582343749993598, 24.94791666325268764, 9.832129032723422313 ) ) ;
#1896=CARTESIAN_POINT ( 'NONE',  ( 5.000000000000001776, 7.708333326505366401, -8.660254037844389075 ) ) ;
#1898=CARTESIAN_POINT ( 'NONE',  ( 0.000000000000000000, 300.0000000000000000, 10.00000000000000178 ) ) ;
#1903=CARTESIAN_POINT ( 'NONE',  ( 9.832129032723416984, 40.36458332991934839, 5.676582343750006032 ) ) ;
#1906=CARTESIAN_POINT ( 'NONE',  ( 3.490152628695403868E-12, 151.2499999999997442, -10.00000000000000178 ) ) ;
#1907=LINE ( 'NONE', #52482, #63571 ) ;
#1909=CARTESIAN_POINT ( 'NONE',  ( 8.311093377946837890, 26.40624999658601624, -8.311093377946837890 ) ) ;
#1912=CARTESIAN_POINT ( 'NONE',  ( 11.35316468749999963, 145.9895833299193839, -3.042071309553165293 ) ) ;
#1913=CARTESIAN_POINT ( 'NONE',  ( -8.660254037844390851, 119.7916666598386968, 4.999999999999998224 ) ) ;
#1918=CARTESIAN_POINT ( 'NONE',  ( -3.042071309553173730, 24.63541666325267698, 11.35316468749999785 ) ) ;
#1923=CARTESIAN_POINT ( 'NONE',  ( 11.35316468749999785, 155.5729166632526983, 3.042071309553174174 ) ) ;
#1933=CARTESIAN_POINT ( 'NONE',  ( -9.832129032723418760, 88.17708332991934128, -5.676582343750004256 ) ) ;
#1936=EDGE_LOOP ( 'NONE', ( #7898, #15824, #66533, #4482, #55209 ) ) ;
#1943=AXIS2_PLACEMENT_3D ( 'NONE', #1654, #64275, #71027 ) ;
#1964=CARTESIAN_POINT ( 'NONE',  ( 8.660254037844385522, 94.58333333333334281, 5.000000000000005329 ) ) ;
#1967=CARTESIAN_POINT ( 'NONE',  ( -4.721056650415999201, 297.4843750017070079, -4.721056650415999201 ) ) ;
#1970=CARTESIAN_POINT ( 'NONE',  ( 8.660254037844419273, 189.5833333333333712, 5.000000000000024869 ) ) ;
#1973=CARTESIAN_POINT ( 'NONE',  ( 6.123233995736767268E-16, 103.1249999931720396, -10.00000000000000178 ) ) ;
#1977=CARTESIAN_POINT ( 'NONE',  ( 8.660254037844385522, 209.5833333333333428, 5.000000000000005329 ) ) ;
#1979=CARTESIAN_POINT ( 'NONE',  ( -5.676582343749998039, 177.7604166632526699, -9.832129032723420536 ) ) ;
#1988=CARTESIAN_POINT ( 'NONE',  ( -11.35316468749999785, 53.38541666325267698, -3.042071309553167513 ) ) ;
#1990=CARTESIAN_POINT ( 'NONE',  ( -8.311093377946836114, 217.9687499965860127, -8.311093377946837890 ) ) ;
#1993=CARTESIAN_POINT ( 'NONE',  ( -2.679491924311308448, 60.41666665983868967, 9.999999999999957367 ) ) ;
#1995=CARTESIAN_POINT ( 'NONE',  ( -11.35316468749999785, 103.0729166632526841, -3.042071309553167513 ) ) ;
#1998=CARTESIAN_POINT ( 'NONE',  ( -2.679491924311235618, 80.41666665983871098, 10.00000000000000000 ) ) ;
#2002=FACE_OUTER_BOUND ( 'NONE', #20229, .T. ) ;
#2005=CARTESIAN_POINT ( 'NONE',  ( -4.721056650415998313, 295.7343750017069510, 4.721056650416000089 ) ) ;
#2007=CARTESIAN_POINT ( 'NONE',  ( -5.676582343749998039, 167.4479166632526983, -9.832129032723420536 ) ) ;
#2016=CARTESIAN_POINT ( 'NONE',  ( 8.311093377946834337, 145.4687499965860127, 8.311093377946839666 ) ) ;
#2017=CARTESIAN_POINT ( 'NONE',  ( 1.901548650871797615E-12, 218.7500000000001990, 10.00000000000000533 ) ) ;
#2020=CARTESIAN_POINT ( 'NONE',  ( 6.951808397369818766E-16, 52.34374999658601979, -11.35316468750000141 ) ) ;
#2022=VERTEX_POINT ( 'NONE', #31221 ) ;
#2029=CARTESIAN_POINT ( 'NONE',  ( 2.485281374238571317, 293.7500000034140157, -6.000000000000003553 ) ) ;
#2052=CARTESIAN_POINT ( 'NONE',  ( -7.320508075688778149, 48.12499999999999289, 7.320508075688769267 ) ) ;
#2054=CARTESIAN_POINT ( 'NONE',  ( 2.485281374238575314, 296.3124999999999432, 6.000000000000000888 ) ) ;
#2057=VERTEX_POINT ( 'NONE', #25914 ) ;
#2060=DIRECTION ( 'NONE',  ( 0.000000000000000000, 0.000000000000000000, 1.000000000000000000 ) ) ;
#2064=ADVANCED_FACE ( 'NONE', ( #31970 ), #66293, .T. ) ;
#2065=CARTESIAN_POINT ( 'NONE',  ( 4.999999999999993783, 169.1666666666666856, 8.660254037844390851 ) ) ;
#2068=CARTESIAN_POINT ( 'NONE',  ( -5.676582343749998039, 137.7604166632526983, -9.832129032723420536 ) ) ;
#2070=FACE_OUTER_BOUND ( 'NONE', #35726, .T. ) ;
#2073=CARTESIAN_POINT ( 'NONE',  ( -5.000000000000007105, 168.3333333333333428, 8.660254037844389075 ) ) ;
#2075=ORIENTED_EDGE ( 'NONE', *, *, #4466, .F. ) ;
#2076=CARTESIAN_POINT ( 'NONE',  ( -9.832129032723420536, 14.01041666325268409, 5.676582343749997150 ) ) ;
#2077=CARTESIAN_POINT ( 'NONE',  ( -8.660254037844385522, 112.9166666666666714, 4.999999999999994671 ) ) ;
#2081=CARTESIAN_POINT ( 'NONE',  ( -2.679491924311225848, 38.33333332650536818, -10.00000000000000178 ) ) ;
#2086=CARTESIAN_POINT ( 'NONE',  ( 2.485281374238247132, 291.7500000034140157, -6.000000000000325961 ) ) ;
#2089=CARTESIAN_POINT ( 'NONE',  ( 8.660254037844389075, 29.58333333333334281, 5.000000000000007994 ) ) ;
#2092=CARTESIAN_POINT ( 'NONE',  ( -11.35316468750000141, 118.4895833299193697, 3.042071309553159963 ) ) ;
#2098=FACE_OUTER_BOUND ( 'NONE', #51963, .T. ) ;
#2099=CARTESIAN_POINT ( 'NONE',  ( 1.102182119232618108E-15, 292.3125000034140157, 6.000000000000001776 ) ) ;
#2100=CARTESIAN_POINT ( 'NONE',  ( -8.311093377946841443, 118.9062499965860411, 8.311093377946834337 ) ) ;
#2104=CARTESIAN_POINT ( 'NONE',  ( 2.679491924311228956, 207.9166666598387110, -10.00000000000000000 ) ) ;
#2106=DIRECTION ( 'NONE',  ( 0.000000000000000000, 0.000000000000000000, 1.000000000000000000 ) ) ;
#2108=CARTESIAN_POINT ( 'NONE',  ( 5.676582343750001591, 96.92708332991935549, -9.832129032723420536 ) ) ;
#2113=CARTESIAN_POINT ( 'NONE',  ( 3.042071309553167069, 12.13541666325268054, -11.35316468749999785 ) ) ;
#2120=CARTESIAN_POINT ( 'NONE',  ( 6.676582343750001591, 292.9531250017069510, -8.176455196517173205E-16 ) ) ;
#2122=CARTESIAN_POINT ( 'NONE',  ( -5.676582343750006032, 219.4270833299193555, 9.832129032723418760 ) ) ;
#2142=CARTESIAN_POINT ( 'NONE',  ( 1.377000000000000002, 272.8559999999997672, 5.668132533241393212 ) ) ;
#2143=CARTESIAN_POINT ( 'NONE',  ( -4.721056650415999201, 292.3281250017069510, -4.721056650415999201 ) ) ;
#2146=CARTESIAN_POINT ( 'NONE',  ( 8.660254037844385522, 136.4583333265053682, 5.000000000000005329 ) ) ;
#2147=ORIENTED_EDGE ( 'NONE', *, *, #5446, .T. ) ;
#2148=CIRCLE ( 'NONE', #44331, 6.000000000000001776 ) ;
#2157=CARTESIAN_POINT ( 'NONE',  ( 9.832129032723416984, 95.67708332991935549, 5.676582343750006032 ) ) ;
#2158=CARTESIAN_POINT ( 'NONE',  ( -1.836970198721029983E-15, 123.7500000000000142, 10.00000000000000178 ) ) ;
#2165=CARTESIAN_POINT ( 'NONE',  ( 11.35316468750000141, 210.7812499965860411, 0.000000000000000000 ) ) ;
#2169=CARTESIAN_POINT ( 'NONE',  ( 5.676582343750001591, 196.9270833299193839, -9.832129032723420536 ) ) ;
#2171=CARTESIAN_POINT ( 'NONE',  ( -4.242640687119286547, 295.9375000034140157, -4.242640687119286547 ) ) ;
#2176=CARTESIAN_POINT ( 'NONE',  ( 5.676582343750001591, 86.61458332991936970, -9.832129032723420536 ) ) ;
#2183=CARTESIAN_POINT ( 'NONE',  ( 11.35316468749999963, 70.98958332991934128, -3.042071309553165293 ) ) ;
#2189=CARTESIAN_POINT ( 'NONE',  ( 5.676582343750001591, 76.61458332991935549, -9.832129032723420536 ) ) ;
#2193=CARTESIAN_POINT ( 'NONE',  ( -1.836970198721029983E-15, 170.6249999931720538, 10.00000000000000178 ) ) ;
#2197=CARTESIAN_POINT ( 'NONE',  ( -2.085542519210945728E-15, 59.84374999658602690, 11.35316468750000141 ) ) ;
#2199=CARTESIAN_POINT ( 'NONE',  ( -3.042071309553173730, 199.3229166632526983, 11.35316468749999785 ) ) ;
#2205=CARTESIAN_POINT ( 'NONE',  ( 11.35316468749999785, 190.5729166632526699, 3.042071309553174174 ) ) ;
#2209=CYLINDRICAL_SURFACE ( 'NONE', #69743, 10.00000000000000178 ) ;
#2211=CARTESIAN_POINT ( 'NONE',  ( 9.832129032723420536, 176.5104166632526699, -5.676582343749999815 ) ) ;
#2217=CARTESIAN_POINT ( 'NONE',  ( 2.679491924311228956, 1.041666666666666519, -10.00000000000000000 ) ) ;
#2230=VECTOR ( 'NONE', #52311, 1000.000000000000000 ) ;
#2234=EDGE_CURVE ( 'NONE', #12265, #20466, #15232, .T. ) ;
#2238=FACE_OUTER_BOUND ( 'NONE', #27645, .T. ) ;
#2242=CARTESIAN_POINT ( 'NONE',  ( 6.676582343750002480, 295.1718750017070079, -2.765530957081997254 ) ) ;
#2243=CARTESIAN_POINT ( 'NONE',  ( -1.836970198721029983E-15, 153.7500000000000000, 10.00000000000000178 ) ) ;
#2247=VECTOR ( 'NONE', #10615, 1000.000000000000000 ) ;
#2260=CARTESIAN_POINT ( 'NONE',  ( 6.951808397369818766E-16, 37.03124999658602690, -11.35316468750000141 ) ) ;
#2261=LINE ( 'NONE', #3382, #60461 ) ;
#2262=CARTESIAN_POINT ( 'NONE',  ( 4.999999999999993783, 11.04166665983870033, 8.660254037844390851 ) ) ;
#2264=LINE ( 'NONE', #36601, #53965 ) ;
#2265=ORIENTED_EDGE ( 'NONE', *, *, #27826, .F. ) ;
#2266=CARTESIAN_POINT ( 'NONE',  ( -8.660254037844390851, 129.7916666598387110, 4.999999999999998224 ) ) ;
#2268=CARTESIAN_POINT ( 'NONE',  ( 3.042071309553167069, 36.82291666325267698, -11.35316468749999785 ) ) ;
#2274=CARTESIAN_POINT ( 'NONE',  ( 3.042071309553159519, 29.73958332991934839, 11.35316468750000141 ) ) ;
#2276=CARTESIAN_POINT ( 'NONE',  ( -5.676582343750006032, 154.1145833299193555, 9.832129032723418760 ) ) ;
#2277=CARTESIAN_POINT ( 'NONE',  ( -2.679491924311235618, 130.4166666598386541, 10.00000000000000000 ) ) ;
#2282=CARTESIAN_POINT ( 'NONE',  ( 8.311093377946837890, 21.71874999658601268, -8.311093377946837890 ) ) ;
#2286=CARTESIAN_POINT ( 'NONE',  ( -11.35316468749999785, 148.0729166632526983, -3.042071309553167957 ) ) ;
#2294=CARTESIAN_POINT ( 'NONE',  ( -5.000000000000005329, 205.2083333265053682, 8.660254037844387298 ) ) ;
#2295=CARTESIAN_POINT ( 'NONE',  ( -5.676582343749998039, 97.76041666325269830, -9.832129032723420536 ) ) ;
#2306=EDGE_CURVE ( 'NONE', #71882, #46242, #46171, .T. ) ;
#2313=B_SPLINE_CURVE_WITH_KNOTS ( 'NONE', 3,
 ( #15173, #1005, #61206, #8397, #42723, #46994, #20451, #12661, #9537, #25732, #64359, #31411, #38203, #7017, #53041, #49127, #58707, #30026, #65736, #32552, #43852, #26107, #70025, #54438, #19710, #41349, #48383, #26483, #48753, #18334, #35692, #2746, #23985, #71762 ),
 .UNSPECIFIED., .F., .F.,
 ( 4, 2, 2, 2, 2, 2, 2, 2, 2, 2, 2, 2, 2, 2, 2, 2, 4 ),
 ( 0.5000000000000000000, 0.5312500000000000000, 0.5625000000000000000, 0.5937500000000000000, 0.6250000000000000000, 0.6562500000000000000, 0.6875000000000000000, 0.7187500000000000000, 0.7500000000000000000, 0.7812500000000000000, 0.8125000000000000000, 0.8437500000000000000, 0.8750000000000000000, 0.9062500000000000000, 0.9375000000000000000, 0.9687500000000000000, 1.000000000000000000 ),
 .UNSPECIFIED. ) ;
#2314=EDGE_CURVE ( 'NONE', #23507, #53794, #9963, .T. ) ;
#2316=CARTESIAN_POINT ( 'NONE',  ( 1.224646799147353454E-15, 300.0000000000000000, -10.00000000000000178 ) ) ;
#2322=ORIENTED_EDGE ( 'NONE', *, *, #23335, .T. ) ;
#2330=CARTESIAN_POINT ( 'NONE',  ( -10.00000000000000178, 102.5000000000000142, -1.224646799147353454E-15 ) ) ;
#2332=CARTESIAN_POINT ( 'NONE',  ( 2.765530957082001251, 295.9218750017070079, 6.676582343750000703 ) ) ;
#2334=ORIENTED_EDGE ( 'NONE', *, *, #30771, .T. ) ;
#2336=CARTESIAN_POINT ( 'NONE',  ( -5.000000000000005329, 145.2083333265053682, 8.660254037844387298 ) ) ;
#2340=CARTESIAN_POINT ( 'NONE',  ( 6.123233995736767268E-16, 183.1249999931720538, -10.00000000000000178 ) ) ;
#2345=CARTESIAN_POINT ( 'NONE',  ( 10.00000000000000178, 215.2083333333333144, -2.679491924311226736 ) ) ;
#2348=CARTESIAN_POINT ( 'NONE',  ( -9.832129032723418760, 193.1770833299193555, -5.676582343750004256 ) ) ;
#2350=DIRECTION ( 'NONE',  ( 0.000000000000000000, 0.000000000000000000, 1.000000000000000000 ) ) ;
#2356=CARTESIAN_POINT ( 'NONE',  ( 11.35316468749999963, 46.30208332991934128, -3.042071309553165293 ) ) ;
#2358=CARTESIAN_POINT ( 'NONE',  ( 9.832129032723416984, 225.6770833299193839, 5.676582343750006032 ) ) ;
#2363=EDGE_CURVE ( 'NONE', #10358, #56251, #17675, .T. ) ;
#2364=CARTESIAN_POINT ( 'NONE',  ( 11.35316468749999963, 105.9895833299193555, -3.042071309553165293 ) ) ;
#2365=CARTESIAN_POINT ( 'NONE',  ( 2.679491924311228956, 82.91666665983869677, -10.00000000000000000 ) ) ;
#2368=CARTESIAN_POINT ( 'NONE',  ( -7.320508075688782590, 73.12500000000001421, 7.320508075688774596 ) ) ;
#2370=VERTEX_POINT ( 'NONE', #38486 ) ;
#2372=CARTESIAN_POINT ( 'NONE',  ( 1.226468279477575784E-15, 293.8593750017070079, 6.676582343750001591 ) ) ;
#2373=CARTESIAN_POINT ( 'NONE',  ( 6.123233995736767268E-16, 188.1249999931720254, -10.00000000000000178 ) ) ;
#2374=CARTESIAN_POINT ( 'NONE',  ( 11.35316468750000141, 170.7812499965860411, 0.000000000000000000 ) ) ;
#2375=CYLINDRICAL_SURFACE ( 'NONE', #1943, 10.00000000000000178 ) ;
#2382=CARTESIAN_POINT ( 'NONE',  ( -11.35316468750000141, 138.5937499965860127, -1.390361679473963753E-15 ) ) ;
#2386=CARTESIAN_POINT ( 'NONE',  ( -9.832129032723418760, 68.17708332991935549, -5.676582343750004256 ) ) ;
#2387=EDGE_LOOP ( 'NONE', ( #69674, #2608, #58028, #62616 ) ) ;
#2395=CARTESIAN_POINT ( 'NONE',  ( -6.000000000000001776, 294.0625000034140157, 0.000000000000000000 ) ) ;
#2401=EDGE_CURVE ( 'NONE', #15401, #34004, #37360, .T. ) ;
#2413=CARTESIAN_POINT ( 'NONE',  ( -4.242640687119286547, 294.8750000000000000, -4.242640687119286547 ) ) ;
#2421=CARTESIAN_POINT ( 'NONE',  ( -7.320508075688778149, 53.12500000000000711, 7.320508075688769267 ) ) ;
#2423=CARTESIAN_POINT ( 'NONE',  ( 6.000000000000003553, 296.4375000000000000, 2.485281374238571317 ) ) ;
#2433=CARTESIAN_POINT ( 'NONE',  ( 0.000000000000000000, 300.0000000000000000, 0.000000000000000000 ) ) ;
#2435=CARTESIAN_POINT ( 'NONE',  ( 8.660254037844385522, 174.5833333333333428, 5.000000000000005329 ) ) ;
#2439=CARTESIAN_POINT ( 'NONE',  ( 5.676582343750001591, 151.9270833299193555, -9.832129032723420536 ) ) ;
#2446=CARTESIAN_POINT ( 'NONE',  ( 8.311093377946834337, 15.46874999658601624, 8.311093377946839666 ) ) ;
#2453=CARTESIAN_POINT ( 'NONE',  ( -7.320508075688773708, 33.74999999317202537, -7.320508075688774596 ) ) ;
#2467=CARTESIAN_POINT ( 'NONE',  ( 5.676582343750001591, 131.6145833299193555, -9.832129032723420536 ) ) ;
#2468=ORIENTED_EDGE ( 'NONE', *, *, #32581, .T. ) ;
#2474=CARTESIAN_POINT ( 'NONE',  ( -9.832129032723420536, 118.6979166632526841, 5.676582343749997150 ) ) ;
#2476=CARTESIAN_POINT ( 'NONE',  ( 2.679491924311923512, 48.95833333333340676, 9.999999999999605649 ) ) ;
#2480=CARTESIAN_POINT ( 'NONE',  ( -8.311093377946836114, 97.96874999658599847, -8.311093377946837890 ) ) ;
#2484=CARTESIAN_POINT ( 'NONE',  ( 8.311093377946837890, 26.71874999658601624, -8.311093377946837890 ) ) ;
#2486=CARTESIAN_POINT ( 'NONE',  ( -1.836970198721029983E-15, 110.6249999931720396, 10.00000000000000178 ) ) ;
#2490=EDGE_CURVE ( 'NONE', #14543, #64059, #49037, .T. ) ;
#2492=CARTESIAN_POINT ( 'NONE',  ( -10.00000000000000178, 149.3749999931720538, -1.224646799147353454E-15 ) ) ;
#2493=CARTESIAN_POINT ( 'NONE',  ( 1.226468279477575784E-15, 291.7031250017069510, 6.676582343750001591 ) ) ;
#2495=CARTESIAN_POINT ( 'NONE',  ( 8.311093377946837890, 216.7187499965860127, -8.311093377946837890 ) ) ;
#2496=CARTESIAN_POINT ( 'NONE',  ( -8.311093377946841443, 124.2187499965860127, 8.311093377946830785 ) ) ;
#2505=EDGE_CURVE ( 'NONE', #25744, #54290, #38858, .T. ) ;
#2516=CARTESIAN_POINT ( 'NONE',  ( 1.226468279477575784E-15, 291.7031250017069510, 6.676582343750001591 ) ) ;
#2518=CARTESIAN_POINT ( 'NONE',  ( 10.00000000000000000, 131.6666666598386826, 2.679491924311235618 ) ) ;
#2524=CARTESIAN_POINT ( 'NONE',  ( -1.836970198721029983E-15, 165.6249999931720254, 10.00000000000000178 ) ) ;
#2530=CARTESIAN_POINT ( 'NONE',  ( 5.676582343749993598, 95.26041666325268409, 9.832129032723422313 ) ) ;
#2538=CARTESIAN_POINT ( 'NONE',  ( -2.085542519210945728E-15, 214.5312499965860411, 11.35316468750000141 ) ) ;
#2542=EDGE_CURVE ( 'NONE', #51437, #53888, #32981, .T. ) ;
#2543=CARTESIAN_POINT ( 'NONE',  ( -8.311093377946836114, 197.9687499965860411, -8.311093377946837890 ) ) ;
#2550=CARTESIAN_POINT ( 'NONE',  ( 3.042071309553167069, 76.82291666325269830, -11.35316468749999785 ) ) ;
#2556=CARTESIAN_POINT ( 'NONE',  ( 0.000000000000000000, 300.0000000000000000, 0.000000000000000000 ) ) ;
#2558=CARTESIAN_POINT ( 'NONE',  ( -9.832129032723420536, 83.69791666325268409, 5.676582343749997150 ) ) ;
#2563=CARTESIAN_POINT ( 'NONE',  ( 10.00000000000003553, 75.00000000000002842, 0.000000000000000000 ) ) ;
#2565=CARTESIAN_POINT ( 'NONE',  ( -11.35316468750000141, 78.28124999658601268, -1.390361679473963753E-15 ) ) ;
#2569=CARTESIAN_POINT ( 'NONE',  ( -8.660254037844387298, 163.9583333265053966, -5.000000000000004441 ) ) ;
#2572=CARTESIAN_POINT ( 'NONE',  ( -3.042071309553163960, 57.55208332991936260, -11.35316468749999963 ) ) ;
#2573=CARTESIAN_POINT ( 'NONE',  ( 4.721056650416000089, 291.8281250017069510, 4.721056650415999201 ) ) ;
#2575=CARTESIAN_POINT ( 'NONE',  ( -8.311093377946836114, 192.6562499965860127, -8.311093377946837890 ) ) ;
#2578=CARTESIAN_POINT ( 'NONE',  ( 1.102182119232618108E-15, 290.2500000000000000, 6.000000000000001776 ) ) ;
#2581=CARTESIAN_POINT ( 'NONE',  ( -3.042071309553173730, 194.3229166632526983, 11.35316468749999785 ) ) ;
#2584=ORIENTED_EDGE ( 'NONE', *, *, #41976, .T. ) ;
#2585=EDGE_CURVE ( 'NONE', #5256, #38870, #61519, .T. ) ;
#2586=CARTESIAN_POINT ( 'NONE',  ( 11.35316468749999963, 186.3020833299193555, -3.042071309553165293 ) ) ;
#2591=CARTESIAN_POINT ( 'NONE',  ( -2.679491924311224516, 91.45833333333332860, -9.999999999999994671 ) ) ;
#2595=CARTESIAN_POINT ( 'NONE',  ( 5.000000000000001776, 0.8333333333333333703, -8.660254037844389075 ) ) ;
#2608=ORIENTED_EDGE ( 'NONE', *, *, #6508, .F. ) ;
#2615=CARTESIAN_POINT ( 'NONE',  ( -8.311093377946836114, 62.96874999658601979, -8.311093377946837890 ) ) ;
#2616=CARTESIAN_POINT ( 'NONE',  ( 10.00000000000000178, 91.87499999317203958, 0.000000000000000000 ) ) ;
#2620=CARTESIAN_POINT ( 'NONE',  ( -4.721056650415998313, 293.7343750017069510, 4.721056650416000089 ) ) ;
#2621=CARTESIAN_POINT ( 'NONE',  ( 5.000000000000001776, 150.8333333333333428, -8.660254037844389075 ) ) ;
#2632=CARTESIAN_POINT ( 'NONE',  ( -5.000000000000005329, 20.20833332650536462, 8.660254037844387298 ) ) ;
#2638=CARTESIAN_POINT ( 'NONE',  ( -5.676582343750006032, 44.11458332991935549, 9.832129032723418760 ) ) ;
#2639=CARTESIAN_POINT ( 'NONE',  ( 7.320508075688773708, 149.3750000000000000, 7.320508075688777261 ) ) ;
#2640=CARTESIAN_POINT ( 'NONE',  ( -10.00000000000000178, 14.37499999317203425, -1.224646799147353454E-15 ) ) ;
#2642=CARTESIAN_POINT ( 'NONE',  ( -10.00000000000000000, 129.1666666598387110, -2.679491924311229845 ) ) ;
#2644=CARTESIAN_POINT ( 'NONE',  ( 8.311093377946834337, 30.15624999658601624, 8.311093377946839666 ) ) ;
#2650=CARTESIAN_POINT ( 'NONE',  ( 5.676582343749993598, 29.94791666325268409, 9.832129032723422313 ) ) ;
#2652=CARTESIAN_POINT ( 'NONE',  ( -11.35316468749999785, 163.0729166632526415, -3.042071309553167513 ) ) ;
#2653=CARTESIAN_POINT ( 'NONE',  ( -1.836970198721029983E-15, 130.6249999931720254, 10.00000000000000178 ) ) ;
#2656=CARTESIAN_POINT ( 'NONE',  ( 3.042071309553167513, 17.13541666325268764, -11.35316468749999785 ) ) ;
#2658=DIRECTION ( 'NONE',  ( -0.000000000000000000, 1.000000000000000000, -0.000000000000000000 ) ) ;
#2662=CARTESIAN_POINT ( 'NONE',  ( 11.35316468750000141, 150.7812499965860411, 0.000000000000000000 ) ) ;
#2674=CARTESIAN_POINT ( 'NONE',  ( 3.042071309553167069, 97.13541666325266988, -11.35316468749999785 ) ) ;
#2706=CARTESIAN_POINT ( 'NONE',  ( -2.679491924311235618, 103.5416666666666572, 10.00000000000000000 ) ) ;
#2708=CARTESIAN_POINT ( 'NONE',  ( 4.721056650416000089, 296.9843750017070079, 4.721056650415999201 ) ) ;
#2715=CARTESIAN_POINT ( 'NONE',  ( 6.123233995736767268E-16, 198.1249999931720538, -10.00000000000000178 ) ) ;
#2719=CARTESIAN_POINT ( 'NONE',  ( 8.311093377946834337, 5.156249996586015349, 8.311093377946839666 ) ) ;
#2721=CARTESIAN_POINT ( 'NONE',  ( 3.042071309553159519, 190.0520833299193839, 11.35316468750000141 ) ) ;
#2724=DIRECTION ( 'NONE',  ( -0.000000000000000000, 1.000000000000000000, -0.000000000000000000 ) ) ;
#2729=CARTESIAN_POINT ( 'NONE',  ( 11.35316468749999785, 50.88541666325269119, 3.042071309553174174 ) ) ;
#2733=DIRECTION ( 'NONE',  ( -0.000000000000000000, 1.000000000000000000, -0.000000000000000000 ) ) ;
#2737=CARTESIAN_POINT ( 'NONE',  ( 11.35316468750000141, 115.7812499965860269, 0.000000000000000000 ) ) ;
#2740=CARTESIAN_POINT ( 'NONE',  ( -10.00000000000000000, 94.16666665983868256, -2.679491924311229845 ) ) ;
#2745=ORIENTED_EDGE ( 'NONE', *, *, #55005, .F. ) ;
#2746=CARTESIAN_POINT ( 'NONE',  ( -1.307112308314578586, 225.9999999999999432, 9.935950934677435953 ) ) ;
#2748=CARTESIAN_POINT ( 'NONE',  ( 6.676582343750004256, 295.0468750017069510, 2.765530957081995478 ) ) ;
#2749=CARTESIAN_POINT ( 'NONE',  ( 0.000000000000000000, 284.0000000000000000, 0.000000000000000000 ) ) ;
#2751=CARTESIAN_POINT ( 'NONE',  ( -2.085542519210945728E-15, 174.5312499965860411, 11.35316468750000141 ) ) ;
#2754=CARTESIAN_POINT ( 'NONE',  ( -3.190679070438028606E-13, 193.7500000000000000, 10.00000000000000533 ) ) ;
#2760=CARTESIAN_POINT ( 'NONE',  ( -11.35316468749999785, 138.3854166632526983, -3.042071309553167957 ) ) ;
#2761=CARTESIAN_POINT ( 'NONE',  ( -2.679491924310933193, 216.4583333333333144, -10.00000000000017586 ) ) ;
#2764=CARTESIAN_POINT ( 'NONE',  ( 3.042071309553167069, 62.13541666325267698, -11.35316468749999785 ) ) ;
#2770=VECTOR ( 'NONE', #32091, 1000.000000000000000 ) ;
#2772=CARTESIAN_POINT ( 'NONE',  ( 2.485281374238575314, 288.3750000034140157, 6.000000000000000888 ) ) ;
#2786=CARTESIAN_POINT ( 'NONE',  ( -6.000000000000003553, 294.9374999999998863, -2.485281374238571317 ) ) ;
#2790=ORIENTED_EDGE ( 'NONE', *, *, #11874, .F. ) ;
#2791=CARTESIAN_POINT ( 'NONE',  ( -9.999999999999996447, 2.291666666666665186, -2.679491924311228956 ) ) ;
#2795=CARTESIAN_POINT ( 'NONE',  ( 2.679491924311222739, 73.95833333333334281, 10.00000000000000355 ) ) ;
#2797=CARTESIAN_POINT ( 'NONE',  ( -6.000000000000000888, 296.0625000000000000, 2.485281374238575758 ) ) ;
#2800=ORIENTED_EDGE ( 'NONE', *, *, #24668, .F. ) ;
#2809=CARTESIAN_POINT ( 'NONE',  ( -10.00000000000000000, 192.2916666666666856, -2.679491924311229845 ) ) ;
#2812=CARTESIAN_POINT ( 'NONE',  ( 3.042071309553159519, 155.0520833299192986, 11.35316468750000141 ) ) ;
#2819=CARTESIAN_POINT ( 'NONE',  ( -8.311093377946836114, 7.968749996586014461, -8.311093377946837890 ) ) ;
#2824=CARTESIAN_POINT ( 'NONE',  ( -2.679491924311225848, 48.33333332650537528, -10.00000000000000178 ) ) ;
#2828=CARTESIAN_POINT ( 'NONE',  ( 6.123233995736767268E-16, 21.25000000000000000, -10.00000000000000178 ) ) ;
#2834=CARTESIAN_POINT ( 'NONE',  ( -5.676582343750006032, 129.1145833299193839, 9.832129032723418760 ) ) ;
#2843=CARTESIAN_POINT ( 'NONE',  ( 6.951808397369818766E-16, 107.0312499965860269, -11.35316468750000141 ) ) ;
#2845=CARTESIAN_POINT ( 'NONE',  ( 8.660254037844389075, 82.29166665983871098, -5.000000000000000000 ) ) ;
#2851=CARTESIAN_POINT ( 'NONE',  ( -3.042071309553163960, 107.5520833299193555, -11.35316468749999963 ) ) ;
#2855=CARTESIAN_POINT ( 'NONE',  ( 9.832129032723416984, 20.67708332991935194, 5.676582343750006032 ) ) ;
#2861=CARTESIAN_POINT ( 'NONE',  ( -1.903569318090136080E-11, 13.74999999999851852, 10.00000000000000178 ) ) ;
#2863=CARTESIAN_POINT ( 'NONE',  ( -2.765530957081998586, 289.6406250017070079, 6.676582343750001591 ) ) ;
#2865=CARTESIAN_POINT ( 'NONE',  ( -1.836970198721029983E-15, 125.6249999931720254, 10.00000000000000178 ) ) ;
#2866=CARTESIAN_POINT ( 'NONE',  ( 11.27292232226671054, 225.9999999999999432, 1.347431162485829281 ) ) ;
#2867=CARTESIAN_POINT ( 'NONE',  ( 8.311093377946837890, 136.7187499965860411, -8.311093377946837890 ) ) ;
#2883=CARTESIAN_POINT ( 'NONE',  ( -9.832129032723420536, 188.6979166632526983, 5.676582343749997150 ) ) ;
#2886=CARTESIAN_POINT ( 'NONE',  ( 6.676582343750002480, 291.0156250017069510, -2.765530957081997254 ) ) ;
#2888=CARTESIAN_POINT ( 'NONE',  ( 10.00000000000000178, 136.8749999931720538, 0.000000000000000000 ) ) ;
#2901=CARTESIAN_POINT ( 'NONE',  ( -11.35316468749999785, 108.3854166632526841, -3.042071309553167513 ) ) ;
#2902=CARTESIAN_POINT ( 'NONE',  ( -9.999999999999998224, 122.7083333333333428, 2.679491924311222295 ) ) ;
#2910=CARTESIAN_POINT ( 'NONE',  ( -11.35316468750000141, 223.2812499965860127, -1.390361679473963753E-15 ) ) ;
#2914=CARTESIAN_POINT ( 'NONE',  ( 6.951808397369818766E-16, 197.3437499965860127, -11.35316468750000141 ) ) ;
#2916=CARTESIAN_POINT ( 'NONE',  ( 8.571184731088893116, 225.9999999999998863, 6.322102520634380163 ) ) ;
#2920=CARTESIAN_POINT ( 'NONE',  ( 0.000000000000000000, 300.0000000000000000, 0.000000000000000000 ) ) ;
#2921=CARTESIAN_POINT ( 'NONE',  ( 8.311093377946837890, 81.40624999658601268, -8.311093377946837890 ) ) ;
#2923=CARTESIAN_POINT ( 'NONE',  ( 4.999999999999998224, 139.1666666666666856, 8.660254037844399733 ) ) ;
#2928=CARTESIAN_POINT ( 'NONE',  ( -9.832129032723418760, 82.86458332991935549, -5.676582343750004256 ) ) ;
#2934=CARTESIAN_POINT ( 'NONE',  ( 8.660254037844412167, 74.58333333333334281, 5.000000000000022204 ) ) ;
#2936=CARTESIAN_POINT ( 'NONE',  ( -3.042071309553163960, 77.23958332991935549, -11.35316468749999963 ) ) ;
#2939=CARTESIAN_POINT ( 'NONE',  ( 10.00000000000000178, 167.0833333265053682, -2.679491924311226736 ) ) ;
#2942=CARTESIAN_POINT ( 'NONE',  ( -9.832129032723418760, 63.17708332991934839, -5.676582343750004256 ) ) ;
#2943=CARTESIAN_POINT ( 'NONE',  ( 4.721056650416000089, 292.8281250017069510, 4.721056650415999201 ) ) ;
#2945=CARTESIAN_POINT ( 'NONE',  ( 8.311093377946834337, 210.1562499965860411, 8.311093377946839666 ) ) ;
#2950=CARTESIAN_POINT ( 'NONE',  ( -5.676582343750006032, 199.1145833299193555, 9.832129032723418760 ) ) ;
#2956=CARTESIAN_POINT ( 'NONE',  ( -3.042071309553163960, 187.5520833299193555, -11.35316468749999963 ) ) ;
#2972=CARTESIAN_POINT ( 'NONE',  ( 2.485281374238216490, 293.7500000034140157, -6.000000000000357048 ) ) ;
#2974=CARTESIAN_POINT ( 'NONE',  ( -2.679491924304484574, 81.45833333333280279, -10.00000000000402700 ) ) ;
#2983=CARTESIAN_POINT ( 'NONE',  ( 8.311093377946837890, 76.71874999658599847, -8.311093377946837890 ) ) ;
#2988=CARTESIAN_POINT ( 'NONE',  ( -4.721056650415999201, 292.4843750017070079, -4.721056650415999201 ) ) ;
#2989=CARTESIAN_POINT ( 'NONE',  ( 7.320508075688771044, 149.3750000000000000, 7.320508075688775484 ) ) ;
#3002=CARTESIAN_POINT ( 'NONE',  ( 1.102182119232618108E-15, 293.3125000034140157, 6.000000000000001776 ) ) ;
#3004=CARTESIAN_POINT ( 'NONE',  ( 3.178432602446558121E-13, 136.2499999999999716, -10.00000000000000533 ) ) ;
#3008=CARTESIAN_POINT ( 'NONE',  ( 11.35316468750000141, 45.78124999658601979, 0.000000000000000000 ) ) ;
#3010=CARTESIAN_POINT ( 'NONE',  ( -8.660254037844387298, 3.958333326505365957, -5.000000000000004441 ) ) ;
#3012=CARTESIAN_POINT ( 'NONE',  ( 0.000000000000000000, 300.0000000000000000, 0.000000000000000000 ) ) ;
#3013=LINE ( 'NONE', #20344, #17178 ) ;
#3014=CARTESIAN_POINT ( 'NONE',  ( 11.35316468750000141, 45.78124999658601979, 0.000000000000000000 ) ) ;
#3019=CARTESIAN_POINT ( 'NONE',  ( -2.085542519210945728E-15, 29.53124999658601624, 11.35316468750000141 ) ) ;
#3021=CARTESIAN_POINT ( 'NONE',  ( -1.836970198721029983E-15, 50.62499999317203248, 10.00000000000000178 ) ) ;
#3022=CARTESIAN_POINT ( 'NONE',  ( -3.042071309553173730, 159.3229166632526699, 11.35316468749999785 ) ) ;
#3025=CARTESIAN_POINT ( 'NONE',  ( -8.660254037844387298, 133.9583333265053682, -5.000000000000004441 ) ) ;
#3028=CARTESIAN_POINT ( 'NONE',  ( 8.660254037844385522, 21.45833332650536818, 5.000000000000005329 ) ) ;
#3029=CARTESIAN_POINT ( 'NONE',  ( 8.311093377946837890, 16.71874999658601268, -8.311093377946837890 ) ) ;
#3032=CYLINDRICAL_SURFACE ( 'NONE', #16285, 6.000000000000001776 ) ;
#3037=CARTESIAN_POINT ( 'NONE',  ( -8.311093377946836114, 152.6562499965860127, -8.311093377946837890 ) ) ;
#3043=ORIENTED_EDGE ( 'NONE', *, *, #15445, .T. ) ;
#3045=CARTESIAN_POINT ( 'NONE',  ( -2.249999999999999112, 284.0000000000000000, 7.677076266392047543 ) ) ;
#3047=CARTESIAN_POINT ( 'NONE',  ( 3.042071309553159519, 100.0520833299193555, 11.35316468750000141 ) ) ;
#3050=CARTESIAN_POINT ( 'NONE',  ( 10.00000000000001066, 15.20833333333333748, -2.679491924311229401 ) ) ;
#3069=CARTESIAN_POINT ( 'NONE',  ( 2.679491924311155682, 72.91666665983871098, -10.00000000000004441 ) ) ;
#3078=CARTESIAN_POINT ( 'NONE',  ( -9.999999999999998224, 32.70833333333333570, 2.679491924311222295 ) ) ;
#3080=CARTESIAN_POINT ( 'NONE',  ( -4.999999999999998224, 106.6666666666666714, -8.660254037844389075 ) ) ;
#3082=CARTESIAN_POINT ( 'NONE',  ( -4.721056650415998313, 291.7343750017069510, 4.721056650416000089 ) ) ;
#3086=CARTESIAN_POINT ( 'NONE',  ( 0.000000000000000000, 300.0000000000000000, 0.000000000000000000 ) ) ;
#3094=CARTESIAN_POINT ( 'NONE',  ( -7.320508075688773708, 221.8750000000000284, -7.320508075688774596 ) ) ;
#3097=CARTESIAN_POINT ( 'NONE',  ( 3.042071309553167069, 192.1354166632526130, -11.35316468749999785 ) ) ;
#3103=EDGE_LOOP ( 'NONE', ( #62471, #61789, #63324, #7428 ) ) ;
#3105=CARTESIAN_POINT ( 'NONE',  ( 9.832129032723420536, 6.197916663252683200, -5.676582343749999815 ) ) ;
#3110=LINE ( 'NONE', #26472, #6929 ) ;
#3114=CARTESIAN_POINT ( 'NONE',  ( 11.35316468749999963, 125.9895833299193271, -3.042071309553165293 ) ) ;
#3115=CARTESIAN_POINT ( 'NONE',  ( -8.660254037844387298, 83.95833332650536818, -5.000000000000004441 ) ) ;
#3122=VERTEX_POINT ( 'NONE', #2578 ) ;
#3125=CARTESIAN_POINT ( 'NONE',  ( 2.765530957082001251, 293.9218750017069510, 6.676582343750000703 ) ) ;
#3128=CARTESIAN_POINT ( 'NONE',  ( -3.042071309553173730, 164.3229166632526415, 11.35316468749999785 ) ) ;
#3131=CARTESIAN_POINT ( 'NONE',  ( 6.123233995736767268E-16, 8.124999993172032475, -10.00000000000000178 ) ) ;
#3134=CARTESIAN_POINT ( 'NONE',  ( 4.999999999999993783, 156.0416666598387110, 8.660254037844390851 ) ) ;
#3135=CARTESIAN_POINT ( 'NONE',  ( -8.311093377946841443, 154.2187499965859843, 8.311093377946834337 ) ) ;
#3136=CARTESIAN_POINT ( 'NONE',  ( -10.00000000000000711, 217.7083333333333428, 2.679491924311224516 ) ) ;
#3139=CARTESIAN_POINT ( 'NONE',  ( 5.676582343749993598, 65.26041666325268409, 9.832129032723422313 ) ) ;
#3147=CARTESIAN_POINT ( 'NONE',  ( 6.000000000000003553, 288.5000000034140157, 2.485281374238571317 ) ) ;
#3151=PLANE ( 'NONE',  #60677 ) ;
#3169=CARTESIAN_POINT ( 'NONE',  ( 10.00000000000000000, 64.79166666666665719, 2.679491924311236062 ) ) ;
#3171=CARTESIAN_POINT ( 'NONE',  ( 4.242640687119285658, 293.6249999999999432, -4.242640687119286547 ) ) ;
#3174=EDGE_CURVE ( 'NONE', #9634, #57404, #20278, .T. ) ;
#3184=CARTESIAN_POINT ( 'NONE',  ( -10.00000000000000355, 182.7083333333333428, 2.679491924311223183 ) ) ;
#3188=CARTESIAN_POINT ( 'NONE',  ( -11.35316468749999785, 158.3854166632526699, -3.042071309553167513 ) ) ;
#3196=CARTESIAN_POINT ( 'NONE',  ( 9.832129032723420536, 16.51041666325268054, -5.676582343749999815 ) ) ;
#3201=CARTESIAN_POINT ( 'NONE',  ( -10.00000000000000355, 54.58333332650536818, 2.679491924311223183 ) ) ;
#3204=CARTESIAN_POINT ( 'NONE',  ( 10.00000000000001243, 220.2083333333333428, -2.679491924311229845 ) ) ;
#3207=CARTESIAN_POINT ( 'NONE',  ( 2.679491924311222739, 5.833333326505365513, 10.00000000000000355 ) ) ;
#3208=VERTEX_POINT ( 'NONE', #8980 ) ;
#3212=CARTESIAN_POINT ( 'NONE',  ( 9.832129032723416984, 130.3645833299193555, 5.676582343750006032 ) ) ;
#3220=CARTESIAN_POINT ( 'NONE',  ( 6.951808397369818766E-16, 122.0312499965860269, -11.35316468750000141 ) ) ;
#3226=CARTESIAN_POINT ( 'NONE',  ( -9.832129032723420536, 114.0104166632526983, 5.676582343749997150 ) ) ;
#3230=CARTESIAN_POINT ( 'NONE',  ( 3.042071309553159519, 25.05208332991934483, 11.35316468750000141 ) ) ;
#3238=CARTESIAN_POINT ( 'NONE',  ( 2.765530957082001251, 287.7656250017069510, 6.676582343750000703 ) ) ;
#3239=CARTESIAN_POINT ( 'NONE',  ( 5.000000000000001776, 127.7083333265053824, -8.660254037844389075 ) ) ;
#3240=CARTESIAN_POINT ( 'NONE',  ( 5.676582343749993598, 215.2604166632526983, 9.832129032723422313 ) ) ;
#3243=CARTESIAN_POINT ( 'NONE',  ( 11.35316468749999963, 141.3020833299193271, -3.042071309553165293 ) ) ;
#3254=LINE ( 'NONE', #15672, #21145 ) ;
#3259=CARTESIAN_POINT ( 'NONE',  ( -3.042071309553173730, 184.3229166632526983, 11.35316468749999785 ) ) ;
#3262=CARTESIAN_POINT ( 'NONE',  ( -6.000000000000001776, 291.0625000034140157, 0.000000000000000000 ) ) ;
#3263=CARTESIAN_POINT ( 'NONE',  ( 4.721056650416000089, 293.8281250017069510, 4.721056650415999201 ) ) ;
#3264=CARTESIAN_POINT ( 'NONE',  ( 6.326249034914468552E-13, 178.7500000000000853, 10.00000000000000533 ) ) ;
#3265=CARTESIAN_POINT ( 'NONE',  ( 9.999999999999996447, 95.20833333333334281, -2.679491924311225848 ) ) ;
#3276=CARTESIAN_POINT ( 'NONE',  ( 9.832129032723416984, 115.6770833299193555, 5.676582343750006032 ) ) ;
#3277=CARTESIAN_POINT ( 'NONE',  ( -5.999999999999999112, 296.0625000000000000, 2.485281374238575314 ) ) ;
#3289=CARTESIAN_POINT ( 'NONE',  ( 3.042071309553159519, 200.0520833299193839, 11.35316468750000141 ) ) ;
#3295=CARTESIAN_POINT ( 'NONE',  ( 2.249999999999996003, 255.9999999999999432, 7.677076266392048431 ) ) ;
#3296=CARTESIAN_POINT ( 'NONE',  ( -9.832129032723418760, 82.86458332991935549, -5.676582343750004256 ) ) ;
#3301=CARTESIAN_POINT ( 'NONE',  ( 7.320508075688886507, 39.37500000000009237, 7.320508075688890948 ) ) ;
#3303=CARTESIAN_POINT ( 'NONE',  ( -9.832129032723418760, 87.86458332991935549, -5.676582343750004256 ) ) ;
#3304=ORIENTED_EDGE ( 'NONE', *, *, #63738, .F. ) ;
#3310=CARTESIAN_POINT ( 'NONE',  ( 8.311093377946834337, 85.15624999658602690, 8.311093377946839666 ) ) ;
#3313=CARTESIAN_POINT ( 'NONE',  ( 7.320508075688771044, 166.2499999931720822, 7.320508075688775484 ) ) ;
#3316=CARTESIAN_POINT ( 'NONE',  ( -9.832129032723420536, 69.01041666325268409, 5.676582343749997150 ) ) ;
#3317=CARTESIAN_POINT ( 'NONE',  ( -2.765530957081996810, 294.2656250017069510, -6.676582343750003368 ) ) ;
#3319=CARTESIAN_POINT ( 'NONE',  ( -9.832129032723418760, 212.8645833299193555, -5.676582343750004256 ) ) ;
#3325=CARTESIAN_POINT ( 'NONE',  ( 6.951808397369818766E-16, 197.0312499965860411, -11.35316468750000141 ) ) ;
#3327=FACE_OUTER_BOUND ( 'NONE', #191, .T. ) ;
#3331=CARTESIAN_POINT ( 'NONE',  ( -9.832129032723418760, 188.1770833299193555, -5.676582343750004256 ) ) ;
#3337=CARTESIAN_POINT ( 'NONE',  ( 7.320508075688771044, 4.374999999999999112, 7.320508075688775484 ) ) ;
#3339=( BOUNDED_CURVE ( )  B_SPLINE_CURVE ( 2, ( #17669, #7741, #40686, #51258, #57309, #69359, #74268, #23702, #51633, #16920, #53768, #45597, #34678 ),
 .UNSPECIFIED., .F., .F. ) 
 B_SPLINE_CURVE_WITH_KNOTS ( ( 3, 2, 2, 2, 2, 2, 3 ),
 ( 0.3750000000000000000, 0.3768115942028985588, 0.3786231884057971175, 0.3804347826086956763, 0.3822463768115941796, 0.3840579710144927383, 0.3858695652173912971 ),
 .UNSPECIFIED. ) 
 CURVE ( )  GEOMETRIC_REPRESENTATION_ITEM ( )  RATIONAL_B_SPLINE_CURVE ( ( 1.000000000000000000, 0.9659258262890683122, 1.000000000000000000, 0.9659258262890683122, 1.000000000000000000, 0.9659258262890683122, 1.000000000000000000, 0.9659258262890683122, 1.000000000000000000, 0.9659258262890683122, 1.000000000000000000, 0.9659258262890683122, 1.000000000000000000 ) ) 
 REPRESENTATION_ITEM ( '' )  );
#3351=ADVANCED_FACE ( 'NONE', ( #62149 ), #22902, .T. ) ;
#3357=CARTESIAN_POINT ( 'NONE',  ( 3.042071309553159519, 70.05208332991934128, 11.35316468750000141 ) ) ;
#3362=CARTESIAN_POINT ( 'NONE',  ( 6.676582343750003368, 296.0468750017069510, 2.765530957081995478 ) ) ;
#3366=AXIS2_PLACEMENT_3D ( 'NONE', #61936, #27600, #50611 ) ;
#3375=CARTESIAN_POINT ( 'NONE',  ( 6.000000000000003553, 289.6250000034140157, -2.485281374238571761 ) ) ;
#3381=CARTESIAN_POINT ( 'NONE',  ( -3.042071309553164404, 42.23958332991934128, -11.35316468749999963 ) ) ;
#3382=CARTESIAN_POINT ( 'NONE',  ( 0.000000000000000000, 300.0000000000000000, 10.00000000000000178 ) ) ;
#3383=CARTESIAN_POINT ( 'NONE',  ( 10.00000000000000178, 12.08333332650536462, -2.679491924311226736 ) ) ;
#3385=ORIENTED_EDGE ( 'NONE', *, *, #49128, .T. ) ;
#3388=CARTESIAN_POINT ( 'NONE',  ( 11.35316468749999963, 45.98958332991934128, -3.042071309553165293 ) ) ;
#3395=CARTESIAN_POINT ( 'NONE',  ( 9.832129032723420536, 36.19791666325267698, -5.676582343749999815 ) ) ;
#3397=DIRECTION ( 'NONE',  ( 0.000000000000000000, 0.000000000000000000, 1.000000000000000000 ) ) ;
#3398=CARTESIAN_POINT ( 'NONE',  ( 5.676582343750001591, 166.6145833299193555, -9.832129032723420536 ) ) ;
#3399=CARTESIAN_POINT ( 'NONE',  ( 7.320508075688774596, 127.4999999931720396, -7.320508075688774596 ) ) ;
#3403=CARTESIAN_POINT ( 'NONE',  ( 11.35316468749999785, 25.88541666325268764, 3.042071309553174174 ) ) ;
#3404=CARTESIAN_POINT ( 'NONE',  ( 0.000000000000000000, 300.0000000000000000, 10.00000000000000178 ) ) ;
#3410=CARTESIAN_POINT ( 'NONE',  ( 3.042071309553167513, 146.8229166632526983, -11.35316468749999785 ) ) ;
#3418=CARTESIAN_POINT ( 'NONE',  ( -9.832129032723418760, 98.17708332991935549, -5.676582343750004256 ) ) ;
#3422=VERTEX_POINT ( 'NONE', #57249 ) ;
#3441=CARTESIAN_POINT ( 'NONE',  ( 4.999999999999993783, 71.04166665983869677, 8.660254037844390851 ) ) ;
#3444=VERTEX_POINT ( 'NONE', #4445 ) ;
#3451=CARTESIAN_POINT ( 'NONE',  ( 4.999999999999993783, 104.1666666666666714, 8.660254037844390851 ) ) ;
#3453=CARTESIAN_POINT ( 'NONE',  ( -2.765530957081996810, 291.4218750017070079, -6.676582343750003368 ) ) ;
#3458=EDGE_CURVE ( 'NONE', #19919, #30602, #28564, .T. ) ;
#3466=CARTESIAN_POINT ( 'NONE',  ( 0.000000000000000000, 0.000000000000000000, 0.000000000000000000 ) ) ;
#3467=CARTESIAN_POINT ( 'NONE',  ( -8.311093377946836114, 2.656249996586016238, -8.311093377946837890 ) ) ;
#3470=CARTESIAN_POINT ( 'NONE',  ( -3.042071309553173730, 194.6354166632526415, 11.35316468749999785 ) ) ;
#3474=FACE_OUTER_BOUND ( 'NONE', #4624, .T. ) ;
#3475=CARTESIAN_POINT ( 'NONE',  ( 4.242640687119285658, 297.6250000000000000, -4.242640687119286547 ) ) ;
#3478=CARTESIAN_POINT ( 'NONE',  ( 8.311093377946837890, 6.406249996586016238, -8.311093377946837890 ) ) ;
#3486=CARTESIAN_POINT ( 'NONE',  ( 3.042071309553167069, 126.8229166632526841, -11.35316468749999785 ) ) ;
#3488=CARTESIAN_POINT ( 'NONE',  ( -10.00000000000000355, 94.58333332650535397, 2.679491924311223183 ) ) ;
#3496=CARTESIAN_POINT ( 'NONE',  ( -2.765530957081996810, 295.4218750017069510, -6.676582343750003368 ) ) ;
#3499=CARTESIAN_POINT ( 'NONE',  ( 3.042071309553167069, 166.8229166632526699, -11.35316468749999785 ) ) ;
#3501=CARTESIAN_POINT ( 'NONE',  ( 6.123233995736767268E-16, 203.1249999931720538, -10.00000000000000178 ) ) ;
#3506=CARTESIAN_POINT ( 'NONE',  ( -11.35316468750000141, 153.5937499965860127, -1.390361679473963753E-15 ) ) ;
#3510=CARTESIAN_POINT ( 'NONE',  ( -11.35316468749999785, 63.38541666325269119, -3.042071309553167513 ) ) ;
#3514=EDGE_LOOP ( 'NONE', ( #9765, #9260, #46273, #7213 ) ) ;
#3517=CARTESIAN_POINT ( 'NONE',  ( 6.123233995736767268E-16, 108.1249999931720396, -10.00000000000000178 ) ) ;
#3534=VERTEX_POINT ( 'NONE', #9955 ) ;
#3535=CARTESIAN_POINT ( 'NONE',  ( -3.673940397442060854E-16, 299.7500000000000000, -6.000000000000001776 ) ) ;
#3541=CARTESIAN_POINT ( 'NONE',  ( -4.999999999999998224, 61.66666666666667140, -8.660254037844389075 ) ) ;
#3544=CARTESIAN_POINT ( 'NONE',  ( 6.000000000000003553, 292.5624999999999432, -2.485281374238571761 ) ) ;
#3546=CARTESIAN_POINT ( 'NONE',  ( -10.00000000000000533, 127.2916666666666572, -2.679491924311232065 ) ) ;
#3557=CARTESIAN_POINT ( 'NONE',  ( -4.999999999999998224, 191.6666666666666856, -8.660254037844389075 ) ) ;
#3560=CARTESIAN_POINT ( 'NONE',  ( 11.35316468749999785, 155.8854166632526699, 3.042071309553174174 ) ) ;
#3565=CARTESIAN_POINT ( 'NONE',  ( 1.224646799147353454E-15, 300.0000000000000000, -10.00000000000000178 ) ) ;
#3568=CARTESIAN_POINT ( 'NONE',  ( 9.832129032723416984, 20.67708332991935194, 5.676582343750006032 ) ) ;
#3569=CARTESIAN_POINT ( 'NONE',  ( 10.00000000000000000, 96.66666665983871098, 2.679491924311235618 ) ) ;
#3571=CARTESIAN_POINT ( 'NONE',  ( 10.00000000000000000, 31.66666665983870033, 2.679491924311235618 ) ) ;
#3574=CARTESIAN_POINT ( 'NONE',  ( -1.836970198721029983E-15, 50.62499999317203248, 10.00000000000000178 ) ) ;
#3577=CARTESIAN_POINT ( 'NONE',  ( 5.000000000000000000, 219.1666666666666856, 8.660254037844401509 ) ) ;
#3585=CARTESIAN_POINT ( 'NONE',  ( 11.35316468749999785, 130.5729166632526983, 3.042071309553174174 ) ) ;
#3592=CARTESIAN_POINT ( 'NONE',  ( 5.676582343750001591, 121.6145833299193555, -9.832129032723420536 ) ) ;
#3595=VECTOR ( 'NONE', #33703, 1000.000000000000000 ) ;
#3598=CARTESIAN_POINT ( 'NONE',  ( -2.085542519210945728E-15, 119.8437499965860269, 11.35316468750000141 ) ) ;
#3602=CARTESIAN_POINT ( 'NONE',  ( 3.042071309553167069, 22.13541666325268409, -11.35316468749999785 ) ) ;
#3610=CARTESIAN_POINT ( 'NONE',  ( -4.721056650415999201, 290.3281250017069510, -4.721056650415999201 ) ) ;
#3611=CARTESIAN_POINT ( 'NONE',  ( -2.485281374238947016, 296.8125000000000568, -5.999999999999626965 ) ) ;
#3612=CARTESIAN_POINT ( 'NONE',  ( 0.000000000000000000, 300.0000000000000000, 0.000000000000000000 ) ) ;
#3615=CARTESIAN_POINT ( 'NONE',  ( 8.311093377946837890, 141.7187499965859843, -8.311093377946837890 ) ) ;
#3630=CARTESIAN_POINT ( 'NONE',  ( -8.311093377946836114, 192.6562499965860127, -8.311093377946837890 ) ) ;
#3633=CARTESIAN_POINT ( 'NONE',  ( -6.676582343750001591, 289.4531250017069510, 0.000000000000000000 ) ) ;
#3635=CARTESIAN_POINT ( 'NONE',  ( -10.00000000000000711, 67.70833333333334281, 2.679491924311224071 ) ) ;
#3636=ORIENTED_EDGE ( 'NONE', *, *, #15752, .F. ) ;
#3645=CARTESIAN_POINT ( 'NONE',  ( 8.311093377946837890, 116.7187499965859985, -8.311093377946837890 ) ) ;
#3651=CARTESIAN_POINT ( 'NONE',  ( 2.485281374238163199, 298.6875000000000000, -6.000000000000410338 ) ) ;
#3659=CARTESIAN_POINT ( 'NONE',  ( -3.042071309553164404, 212.5520833299193839, -11.35316468749999963 ) ) ;
#3661=CARTESIAN_POINT ( 'NONE',  ( 11.27292232226671054, 225.9999999999999432, 1.347431162485829281 ) ) ;
#3665=CARTESIAN_POINT ( 'NONE',  ( 2.679491924311810269, 183.9583333333334281, 9.999999999999657163 ) ) ;
#3667=CARTESIAN_POINT ( 'NONE',  ( 5.676582343749993598, 79.94791666325269830, 9.832129032723422313 ) ) ;
#3674=CARTESIAN_POINT ( 'NONE',  ( -3.042071309553173730, 89.32291666325268409, 11.35316468749999785 ) ) ;
#3676=CARTESIAN_POINT ( 'NONE',  ( 6.123233995736767268E-16, 58.12499999317203248, -10.00000000000000178 ) ) ;
#3682=CARTESIAN_POINT ( 'NONE',  ( 11.35316468749999963, 90.98958332991935549, -3.042071309553165293 ) ) ;
#3690=CARTESIAN_POINT ( 'NONE',  ( 6.123233995736767268E-16, 178.1249999931720538, -10.00000000000000178 ) ) ;
#3692=CARTESIAN_POINT ( 'NONE',  ( 5.676582343749993598, 75.26041666325268409, 9.832129032723422313 ) ) ;
#3693=CARTESIAN_POINT ( 'NONE',  ( 6.676582343750003368, 292.0156250017069510, -2.765530957081997254 ) ) ;
#3695=CARTESIAN_POINT ( 'NONE',  ( -3.042071309553173730, 204.3229166632526699, 11.35316468749999785 ) ) ;
#3698=DIRECTION ( 'NONE',  ( -0.000000000000000000, 1.000000000000000000, -0.000000000000000000 ) ) ;
#3701=CARTESIAN_POINT ( 'NONE',  ( -8.311093377946836114, 212.6562499965860411, -8.311093377946837890 ) ) ;
#3704=CARTESIAN_POINT ( 'NONE',  ( 0.000000000000000000, 300.0000000000000000, 0.000000000000000000 ) ) ;
#3705=EDGE_LOOP ( 'NONE', ( #52686, #44554, #12659, #20785, #50092, #58016 ) ) ;
#3706=CARTESIAN_POINT ( 'NONE',  ( 9.832129032723420536, 201.5104166632526983, -5.676582343749999815 ) ) ;
#3714=CARTESIAN_POINT ( 'NONE',  ( 10.00000000000000000, 9.791666666666667851, 2.679491924311236062 ) ) ;
#3720=VERTEX_POINT ( 'NONE', #28417 ) ;
#3733=CARTESIAN_POINT ( 'NONE',  ( 11.35316468750000141, 81.09374999658601268, 0.000000000000000000 ) ) ;
#3736=FACE_OUTER_BOUND ( 'NONE', #66688, .T. ) ;
#3738=CARTESIAN_POINT ( 'NONE',  ( 4.721056650415999201, 291.2343750017069510, -4.721056650415999201 ) ) ;
#3740=CARTESIAN_POINT ( 'NONE',  ( -10.00000000000000000, 164.1666666598387110, -2.679491924311229845 ) ) ;
#3748=DIRECTION ( 'NONE',  ( 0.000000000000000000, 0.000000000000000000, 1.000000000000000000 ) ) ;
#3756=CARTESIAN_POINT ( 'NONE',  ( 11.35316468749999963, 35.98958332991933418, -3.042071309553165293 ) ) ;
#3757=DIRECTION ( 'NONE',  ( -0.000000000000000000, 1.000000000000000000, -0.000000000000000000 ) ) ;
#3758=CARTESIAN_POINT ( 'NONE',  ( -1.836970198721029983E-15, 20.62499999317203603, 10.00000000000000178 ) ) ;
#3763=CARTESIAN_POINT ( 'NONE',  ( 11.35316468750000141, 50.78124999658601268, 0.000000000000000000 ) ) ;
#3770=CARTESIAN_POINT ( 'NONE',  ( 11.35316468749999785, 40.57291666325268409, 3.042071309553174174 ) ) ;
#3772=CARTESIAN_POINT ( 'NONE',  ( -8.311093377946836114, 157.6562499965860411, -8.311093377946837890 ) ) ;
#3773=CARTESIAN_POINT ( 'NONE',  ( -10.00000000000000178, 129.3749999931720254, -1.224646799147353454E-15 ) ) ;
#3777=CARTESIAN_POINT ( 'NONE',  ( 5.676582343749993598, 35.26041666325269119, 9.832129032723422313 ) ) ;
#3785=CARTESIAN_POINT ( 'NONE',  ( 3.042071309553159519, 169.7395833299193555, 11.35316468750000141 ) ) ;
#3789=EDGE_CURVE ( 'NONE', #40886, #51512, #73942, .T. ) ;
#3790=EDGE_CURVE ( 'NONE', #61682, #16277, #49885, .T. ) ;
#3797=CARTESIAN_POINT ( 'NONE',  ( -11.35316468750000141, 118.5937499965860269, -1.390361679473963753E-15 ) ) ;
#3806=EDGE_CURVE ( 'NONE', #19205, #6677, #40816, .T. ) ;
#3815=VERTEX_POINT ( 'NONE', #66232 ) ;
#3822=AXIS2_PLACEMENT_3D ( 'NONE', #35172, #58186, #42651 ) ;
#3827=CARTESIAN_POINT ( 'NONE',  ( 1.224646799147353454E-15, 300.0000000000000000, -10.00000000000000178 ) ) ;
#3832=CARTESIAN_POINT ( 'NONE',  ( 10.00000000000000178, 110.0000000000000000, 0.000000000000000000 ) ) ;
#3835=CARTESIAN_POINT ( 'NONE',  ( 2.765530957082001251, 291.9218750017069510, 6.676582343750000703 ) ) ;
#3838=LINE ( 'NONE', #26834, #72288 ) ;
#3848=CARTESIAN_POINT ( 'NONE',  ( -2.085542519210945728E-15, 4.531249996586016238, 11.35316468750000141 ) ) ;
#3850=CARTESIAN_POINT ( 'NONE',  ( 6.951808397369818766E-16, 192.3437499965860127, -11.35316468750000141 ) ) ;
#3851=CARTESIAN_POINT ( 'NONE',  ( 1.224646799147353454E-15, 300.0000000000000000, -10.00000000000000178 ) ) ;
#3857=VECTOR ( 'NONE', #49035, 1000.000000000000000 ) ;
#3860=CARTESIAN_POINT ( 'NONE',  ( 3.042071309553159519, 9.739583329919350163, 11.35316468750000141 ) ) ;
#3864=DIRECTION ( 'NONE',  ( -0.000000000000000000, 1.000000000000000000, -0.000000000000000000 ) ) ;
#3866=CARTESIAN_POINT ( 'NONE',  ( -5.676582343750006032, 4.114583329919349275, 9.832129032723418760 ) ) ;
#3868=CARTESIAN_POINT ( 'NONE',  ( 8.311093377946834337, 120.1562499965860127, 8.311093377946839666 ) ) ;
#3869=CARTESIAN_POINT ( 'NONE',  ( -10.00000000000000000, 89.16666665983868256, -2.679491924311229845 ) ) ;
#3872=CARTESIAN_POINT ( 'NONE',  ( -5.000000000000005329, 200.2083333265053682, 8.660254037844387298 ) ) ;
#3873=CARTESIAN_POINT ( 'NONE',  ( 8.660254037844392627, 145.4166666666666572, -5.000000000000003553 ) ) ;
#3876=CARTESIAN_POINT ( 'NONE',  ( 6.676582343750003368, 290.1718750017070079, -2.765530957081997254 ) ) ;
#3881=CARTESIAN_POINT ( 'NONE',  ( -10.00000000000000178, 209.3749999931720538, -1.224646799147353454E-15 ) ) ;
#3887=CARTESIAN_POINT ( 'NONE',  ( 11.35316468749999963, 156.3020833299192986, -3.042071309553165293 ) ) ;
#3888=( LENGTH_UNIT ( ) NAMED_UNIT ( * ) SI_UNIT ( .MILLI., .METRE. ) );
#3891=CARTESIAN_POINT ( 'NONE',  ( -8.311093377946836114, 67.96874999658602690, -8.311093377946837890 ) ) ;
#3897=CARTESIAN_POINT ( 'NONE',  ( -6.000000000000003553, 289.0000000034140157, -2.485281374238571317 ) ) ;
#3910=ADVANCED_FACE ( 'NONE', ( #5111 ), #55304, .T. ) ;
#3921=CARTESIAN_POINT ( 'NONE',  ( 4.242640687119287435, 299.3750000000000000, 4.242640687119285658 ) ) ;
#3927=CARTESIAN_POINT ( 'NONE',  ( -8.660254037844390851, 67.91666666666667140, 4.999999999999998224 ) ) ;
#3929=CARTESIAN_POINT ( 'NONE',  ( 1.102182119232618108E-15, 292.2500000000000000, 6.000000000000001776 ) ) ;
#3938=CARTESIAN_POINT ( 'NONE',  ( 1.268984979720182487E-11, 76.24999999999903366, -10.00000000000000178 ) ) ;
#3939=CARTESIAN_POINT ( 'NONE',  ( -7.320508075688773708, 181.8750000000000284, -7.320508075688774596 ) ) ;
#3942=CARTESIAN_POINT ( 'NONE',  ( 11.35316468749999785, 160.8854166632526983, 3.042071309553174174 ) ) ;
#3945=CARTESIAN_POINT ( 'NONE',  ( 2.696524195522682164E-11, 156.2499999999978968, -10.00000000000000178 ) ) ;
#3946=CARTESIAN_POINT ( 'NONE',  ( -10.00000000000000355, 84.58333332650538239, 2.679491924311223183 ) ) ;
#3948=EDGE_LOOP ( 'NONE', ( #17612, #33910, #70776, #26423 ) ) ;
#3949=CARTESIAN_POINT ( 'NONE',  ( 11.35316468749999785, 25.88541666325268764, 3.042071309553174174 ) ) ;
#3956=CARTESIAN_POINT ( 'NONE',  ( -5.000000000000005329, 50.20833332650537528, 8.660254037844387298 ) ) ;
#3959=CARTESIAN_POINT ( 'NONE',  ( 2.679491924316444784, 98.95833333333378334, 9.999999999996969535 ) ) ;
#3962=CARTESIAN_POINT ( 'NONE',  ( 8.660254037844399733, 159.5833333333333712, 5.000000000000014211 ) ) ;
#3971=CARTESIAN_POINT ( 'NONE',  ( -8.311093377946836114, 122.6562499965860269, -8.311093377946837890 ) ) ;
#3973=CARTESIAN_POINT ( 'NONE',  ( -8.000000000000003553, 284.0000000000000000, 0.000000000000000000 ) ) ;
#3977=CARTESIAN_POINT ( 'NONE',  ( 8.660254037844408614, 45.41666666666667851, -5.000000000000012434 ) ) ;
#3978=CARTESIAN_POINT ( 'NONE',  ( -2.085542519210945728E-15, 124.5312499965860269, 11.35316468750000141 ) ) ;
#3981=ADVANCED_FACE ( 'NONE', ( #63607 ), #34965, .T. ) ;
#3984=CARTESIAN_POINT ( 'NONE',  ( -11.35316468750000141, 113.5937499965860127, -1.390361679473963753E-15 ) ) ;
#3988=CARTESIAN_POINT ( 'NONE',  ( 11.35316468749999785, 25.88541666325268764, 3.042071309553174174 ) ) ;
#3995=CARTESIAN_POINT ( 'NONE',  ( 6.676582343750004256, 289.8906250017069510, 2.765530957081995478 ) ) ;
#3999=CARTESIAN_POINT ( 'NONE',  ( -5.676582343750006032, 139.4270833299193555, 9.832129032723418760 ) ) ;
#4010=EDGE_CURVE ( 'NONE', #17570, #512, #2313, .T. ) ;
#4016=CARTESIAN_POINT ( 'NONE',  ( -5.676582343749998039, 187.4479166632526983, -9.832129032723420536 ) ) ;
#4018=CARTESIAN_POINT ( 'NONE',  ( -4.242640687119286547, 290.9375000034140157, -4.242640687119286547 ) ) ;
#4019=CARTESIAN_POINT ( 'NONE',  ( 6.676582343750001591, 287.9531250017069510, -8.176455196517173205E-16 ) ) ;
#4027=VECTOR ( 'NONE', #14571, 1000.000000000000000 ) ;
#4029=LINE ( 'NONE', #73788, #4027 ) ;
#4032=CARTESIAN_POINT ( 'NONE',  ( -9.832129032723420536, 109.0104166632526841, 5.676582343749997150 ) ) ;
#4039=CARTESIAN_POINT ( 'NONE',  ( 9.973997309829867319, 225.0610850109414969, -0.7786812090345707205 ) ) ;
#4041=CARTESIAN_POINT ( 'NONE',  ( -3.673940397442060854E-16, 287.8125000034140157, -6.000000000000001776 ) ) ;
#4044=CARTESIAN_POINT ( 'NONE',  ( -9.832129032723420536, 214.0104166632526699, 5.676582343749997150 ) ) ;
#4047=CARTESIAN_POINT ( 'NONE',  ( 10.72662151423591226, 225.9999999999999432, 3.025688605616037030 ) ) ;
#4052=CARTESIAN_POINT ( 'NONE',  ( -2.085542519210945728E-15, 99.53124999658602690, 11.35316468750000141 ) ) ;
#4059=CARTESIAN_POINT ( 'NONE',  ( -8.311093377946841443, 93.90624999658599847, 8.311093377946830785 ) ) ;
#4060=ORIENTED_EDGE ( 'NONE', *, *, #33788, .F. ) ;
#4063=DIRECTION ( 'NONE',  ( -0.000000000000000000, 1.000000000000000000, -0.000000000000000000 ) ) ;
#4065=CARTESIAN_POINT ( 'NONE',  ( -1.836970198721029983E-15, 75.62499999317203958, 10.00000000000000178 ) ) ;
#4067=CARTESIAN_POINT ( 'NONE',  ( 8.311093377946834337, 80.15624999658601268, 8.311093377946839666 ) ) ;
#4071=CARTESIAN_POINT ( 'NONE',  ( 8.660254037844389075, 187.2916666598387110, -5.000000000000000000 ) ) ;
#4073=CARTESIAN_POINT ( 'NONE',  ( 3.042071309553159519, 75.05208332991934128, 11.35316468750000141 ) ) ;
#4074=CARTESIAN_POINT ( 'NONE',  ( -6.676582343750003368, 294.3906250017070079, -2.765530957081996810 ) ) ;
#4076=CARTESIAN_POINT ( 'NONE',  ( -5.676582343749998039, 207.4479166632527267, -9.832129032723420536 ) ) ;
#4082=CARTESIAN_POINT ( 'NONE',  ( -8.311093377946836114, 202.6562499965860127, -8.311093377946837890 ) ) ;
#4087=CARTESIAN_POINT ( 'NONE',  ( -11.35316468750000141, 198.5937499965860127, -1.390361679473963753E-15 ) ) ;
#4093=CARTESIAN_POINT ( 'NONE',  ( -2.679491924311235618, 18.54166666666666785, 10.00000000000000000 ) ) ;
#4094=VECTOR ( 'NONE', #26234, 1000.000000000000000 ) ;
#4112=EDGE_LOOP ( 'NONE', ( #9168, #48486, #34745, #31175 ) ) ;
#4115=CARTESIAN_POINT ( 'NONE',  ( -9.832129032723418760, 68.17708332991935549, -5.676582343750004256 ) ) ;
#4120=CARTESIAN_POINT ( 'NONE',  ( -4.721056650415999201, 290.4843750017070079, -4.721056650415999201 ) ) ;
#4131=CARTESIAN_POINT ( 'NONE',  ( -11.35316468750000141, 163.8020833299193555, 3.042071309553159963 ) ) ;
#4140=CARTESIAN_POINT ( 'NONE',  ( 11.35316468749999785, 60.57291666325269830, 3.042071309553174174 ) ) ;
#4142=CARTESIAN_POINT ( 'NONE',  ( -10.00000000000000178, 19.37499999317203603, -1.224646799147353454E-15 ) ) ;
#4145=CARTESIAN_POINT ( 'NONE',  ( 2.679491924311222739, 140.8333333265053966, 10.00000000000000355 ) ) ;
#4147=CARTESIAN_POINT ( 'NONE',  ( 3.042071309553159519, 49.73958332991934839, 11.35316468750000141 ) ) ;
#4153=CARTESIAN_POINT ( 'NONE',  ( -2.085542519210945728E-15, 44.53124999658601979, 11.35316468750000141 ) ) ;
#4155=CARTESIAN_POINT ( 'NONE',  ( 7.320508075688771932, 205.6250000000000284, -7.320508075688771932 ) ) ;
#4156=CARTESIAN_POINT ( 'NONE',  ( 11.35316468750000141, 155.7812499965860127, 0.000000000000000000 ) ) ;
#4158=CARTESIAN_POINT ( 'NONE',  ( -7.320508075688778149, 139.9999999931720538, 7.320508075688769267 ) ) ;
#4162=CARTESIAN_POINT ( 'NONE',  ( 6.951808397369818766E-16, 37.34374999658601979, -11.35316468750000141 ) ) ;
#4169=CARTESIAN_POINT ( 'NONE',  ( 8.311093377946837890, 171.4062499965860127, -8.311093377946837890 ) ) ;
#4175=ORIENTED_EDGE ( 'NONE', *, *, #68445, .F. ) ;
#4178=CARTESIAN_POINT ( 'NONE',  ( 3.042071309553167069, 112.1354166632526699, -11.35316468749999785 ) ) ;
#4205=CARTESIAN_POINT ( 'NONE',  ( 0.000000000000000000, 300.0000000000000000, 6.000000000000001776 ) ) ;
#4206=CARTESIAN_POINT ( 'NONE',  ( 10.00000000000000178, 125.0000000000000000, 0.000000000000000000 ) ) ;
#4209=CARTESIAN_POINT ( 'NONE',  ( 2.765530957081996366, 290.2968750017069510, -6.676582343750003368 ) ) ;
#4211=ORIENTED_EDGE ( 'NONE', *, *, #48966, .F. ) ;
#4222=( BOUNDED_CURVE ( )  B_SPLINE_CURVE ( 2, ( #40960, #6632, #12280, #35315, #13732, #1718, #6997, #48450, #19047, #30375, #30008, #8465, #7734 ),
 .UNSPECIFIED., .F., .F. ) 
 B_SPLINE_CURVE_WITH_KNOTS ( ( 3, 2, 2, 2, 2, 2, 3 ),
 ( 0.1032608695652173919, 0.1050724637681159368, 0.1068840579710144956, 0.1086956521739130405, 0.1105072463768115992, 0.1123188405797101441, 0.1141304347826086890 ),
 .UNSPECIFIED. ) 
 CURVE ( )  GEOMETRIC_REPRESENTATION_ITEM ( )  RATIONAL_B_SPLINE_CURVE ( ( 1.000000000000000000, 0.9659258262890683122, 1.000000000000000000, 0.9659258262890683122, 1.000000000000000000, 0.9659258262890683122, 1.000000000000000000, 0.9659258262890683122, 1.000000000000000000, 0.9659258262890683122, 1.000000000000000000, 0.9659258262890683122, 1.000000000000000000 ) ) 
 REPRESENTATION_ITEM ( '' )  );
#4223=CARTESIAN_POINT ( 'NONE',  ( -8.311093377946841443, 3.906249996586016682, 8.311093377946830785 ) ) ;
#4225=CARTESIAN_POINT ( 'NONE',  ( -2.085542519210945728E-15, 204.8437499965860411, 11.35316468750000141 ) ) ;
#4226=CARTESIAN_POINT ( 'NONE',  ( 1.224646799147353454E-15, 300.0000000000000000, -10.00000000000000178 ) ) ;
#4233=CARTESIAN_POINT ( 'NONE',  ( -3.042071309553164404, 12.23958332991935194, -11.35316468749999963 ) ) ;
#4235=CARTESIAN_POINT ( 'NONE',  ( 6.123233995736767268E-16, 158.1249999931720254, -10.00000000000000178 ) ) ;
#4236=ADVANCED_FACE ( 'NONE', ( #50114 ), #62544, .T. ) ;
#4240=CARTESIAN_POINT ( 'NONE',  ( -8.311093377946836114, 2.656249996586016238, -8.311093377946837890 ) ) ;
#4242=CARTESIAN_POINT ( 'NONE',  ( -3.042071309553173730, 119.3229166632526699, 11.35316468749999785 ) ) ;
#4243=CARTESIAN_POINT ( 'NONE',  ( 7.320508075688774596, 97.49999999317203958, -7.320508075688774596 ) ) ;
#4247=CARTESIAN_POINT ( 'NONE',  ( 7.320508075688776373, 144.3750000000000000, 7.320508075688779925 ) ) ;
#4251=CARTESIAN_POINT ( 'NONE',  ( -6.676582343750003368, 288.5468750017070079, -2.765530957081996810 ) ) ;
#4258=CARTESIAN_POINT ( 'NONE',  ( 10.00000000000000178, 157.0833333265053398, -2.679491924311226736 ) ) ;
#4259=CARTESIAN_POINT ( 'NONE',  ( -9.832129032723418760, 158.1770833299193555, -5.676582343750004256 ) ) ;
#4263=CARTESIAN_POINT ( 'NONE',  ( 3.042071309553167069, 72.13541666325268409, -11.35316468749999785 ) ) ;
#4267=VERTEX_POINT ( 'NONE', #10499 ) ;
#4269=CARTESIAN_POINT ( 'NONE',  ( -6.000000000000000888, 290.1250000034140157, 2.485281374238575758 ) ) ;
#4270=CARTESIAN_POINT ( 'NONE',  ( 6.123233995736767268E-16, 68.12499999317203958, -10.00000000000000178 ) ) ;
#4287=ORIENTED_EDGE ( 'NONE', *, *, #4737, .F. ) ;
#4292=CARTESIAN_POINT ( 'NONE',  ( 2.679491924311222739, 63.95833333333334281, 10.00000000000000355 ) ) ;
#4295=CARTESIAN_POINT ( 'NONE',  ( 6.000000000000003553, 292.4375000000000000, 2.485281374238571317 ) ) ;
#4301=VECTOR ( 'NONE', #63942, 1000.000000000000000 ) ;
#4304=DIRECTION ( 'NONE',  ( -0.000000000000000000, 1.000000000000000000, -0.000000000000000000 ) ) ;
#4308=CARTESIAN_POINT ( 'NONE',  ( 7.320508075688771044, 184.3750000000000000, 7.320508075688775484 ) ) ;
#4311=CARTESIAN_POINT ( 'NONE',  ( 11.35316468750000141, 171.0937499965860127, 0.000000000000000000 ) ) ;
#4317=ORIENTED_EDGE ( 'NONE', *, *, #8619, .F. ) ;
#4318=CARTESIAN_POINT ( 'NONE',  ( 3.042071309553159519, 20.05208332991934839, 11.35316468750000141 ) ) ;
#4324=CARTESIAN_POINT ( 'NONE',  ( -8.660254037844387298, 48.95833332650536818, -5.000000000000004441 ) ) ;
#4327=CARTESIAN_POINT ( 'NONE',  ( 9.999999999999985789, 100.0000000000000142, 0.000000000000000000 ) ) ;
#4335=CARTESIAN_POINT ( 'NONE',  ( 8.311093377946834337, 145.1562499965860127, 8.311093377946839666 ) ) ;
#4343=VERTEX_POINT ( 'NONE', #44088 ) ;
#4348=CARTESIAN_POINT ( 'NONE',  ( -9.832129032723418760, 113.1770833299193555, -5.676582343750004256 ) ) ;
#4352=CARTESIAN_POINT ( 'NONE',  ( 11.35316468750000141, 36.09374999658601979, 0.000000000000000000 ) ) ;
#4359=CARTESIAN_POINT ( 'NONE',  ( -6.000000000000001776, 299.0625000034140157, 0.000000000000000000 ) ) ;
#4360=CARTESIAN_POINT ( 'NONE',  ( -6.000000000000003553, 296.9374999999999432, -2.485281374238571317 ) ) ;
#4363=CARTESIAN_POINT ( 'NONE',  ( 3.042071309553167069, 147.1354166632526983, -11.35316468749999785 ) ) ;
#4374=ORIENTED_EDGE ( 'NONE', *, *, #19554, .T. ) ;
#4378=CARTESIAN_POINT ( 'NONE',  ( 11.35316468750000141, 190.7812499965860127, 0.000000000000000000 ) ) ;
#4381=CARTESIAN_POINT ( 'NONE',  ( -4.721056650415999201, 289.3281250017069510, -4.721056650415999201 ) ) ;
#4383=CARTESIAN_POINT ( 'NONE',  ( 10.00000000000011546, 80.00000000000007105, 0.000000000000000000 ) ) ;
#4389=CARTESIAN_POINT ( 'NONE',  ( -8.660254037844390851, 9.791666659838700326, 4.999999999999998224 ) ) ;
#4393=CARTESIAN_POINT ( 'NONE',  ( -8.660254037844387298, 147.0833333333333428, -5.000000000000004441 ) ) ;
#4397=CARTESIAN_POINT ( 'NONE',  ( 5.676582343750001591, 111.9270833299193555, -9.832129032723420536 ) ) ;
#4398=CARTESIAN_POINT ( 'NONE',  ( 5.000000000000001776, 212.7083333265053682, -8.660254037844389075 ) ) ;
#4404=CARTESIAN_POINT ( 'NONE',  ( 7.869550824153699331, 225.5298564079165544, -6.197952182080146422 ) ) ;
#4405=CARTESIAN_POINT ( 'NONE',  ( 5.676582343749993598, 224.9479166632526983, 9.832129032723422313 ) ) ;
#4408=CARTESIAN_POINT ( 'NONE',  ( 9.832129032723416984, 210.6770833299193555, 5.676582343750006032 ) ) ;
#4414=CARTESIAN_POINT ( 'NONE',  ( 8.311093377946837890, 101.4062499965859985, -8.311093377946837890 ) ) ;
#4415=ORIENTED_EDGE ( 'NONE', *, *, #50379, .T. ) ;
#4421=CARTESIAN_POINT ( 'NONE',  ( 9.832129032723420536, 96.19791666325269830, -5.676582343749999815 ) ) ;
#4423=LINE ( 'NONE', #44410, #56062 ) ;
#4429=CARTESIAN_POINT ( 'NONE',  ( 5.676582343749993598, 84.94791666325268409, 9.832129032723422313 ) ) ;
#4434=CARTESIAN_POINT ( 'NONE',  ( -10.00000000000000000, 179.1666666598387394, -2.679491924311229845 ) ) ;
#4437=CARTESIAN_POINT ( 'NONE',  ( 1.459323541827198180E-11, 81.24999999999886313, -10.00000000000000533 ) ) ;
#4438=CARTESIAN_POINT ( 'NONE',  ( 11.35316468749999785, 75.88541666325268409, 3.042071309553174174 ) ) ;
#4439=CARTESIAN_POINT ( 'NONE',  ( 1.226468279477575784E-15, 287.7031250017069510, 6.676582343750001591 ) ) ;
#4442=CARTESIAN_POINT ( 'NONE',  ( -5.676582343749998039, 202.4479166632526983, -9.832129032723420536 ) ) ;
#4445=CARTESIAN_POINT ( 'NONE',  ( -6.676582343750001591, 287.6093750017069510, 0.000000000000000000 ) ) ;
#4447=CARTESIAN_POINT ( 'NONE',  ( -9.832129032723418760, 212.8645833299193555, -5.676582343750004256 ) ) ;
#4449=CARTESIAN_POINT ( 'NONE',  ( 6.123233995736767268E-16, 18.12499999317203248, -10.00000000000000178 ) ) ;
#4451=CARTESIAN_POINT ( 'NONE',  ( -8.311093377946841443, 194.2187499965860127, 8.311093377946834337 ) ) ;
#4463=CARTESIAN_POINT ( 'NONE',  ( -1.836970198721029983E-15, 18.75000000000000355, 10.00000000000000178 ) ) ;
#4466=EDGE_CURVE ( 'NONE', #73371, #271, #48951, .T. ) ;
#4482=ORIENTED_EDGE ( 'NONE', *, *, #37486, .F. ) ;
#4484=CARTESIAN_POINT ( 'NONE',  ( 11.35316468749999785, 75.88541666325268409, 3.042071309553174174 ) ) ;
#4489=CARTESIAN_POINT ( 'NONE',  ( 6.676582343750002480, 289.1718750017071216, -2.765530957081997254 ) ) ;
#4497=CARTESIAN_POINT ( 'NONE',  ( 11.35316468750000141, 166.0937499965860127, 0.000000000000000000 ) ) ;
#4505=CARTESIAN_POINT ( 'NONE',  ( -5.676582343749998039, 52.44791666325268409, -9.832129032723420536 ) ) ;
#4506=CARTESIAN_POINT ( 'NONE',  ( -1.836970198721029983E-15, 55.62499999317203958, 10.00000000000000178 ) ) ;
#4507=CARTESIAN_POINT ( 'NONE',  ( -5.000000000000005329, 25.20833332650536818, 8.660254037844387298 ) ) ;
#4512=CARTESIAN_POINT ( 'NONE',  ( -8.311093377946836114, 47.65624999658601268, -8.311093377946837890 ) ) ;
#4518=CARTESIAN_POINT ( 'NONE',  ( -3.042071309553163960, 52.23958332991934128, -11.35316468749999963 ) ) ;
#4521=CARTESIAN_POINT ( 'NONE',  ( -8.311093377946841443, 178.9062499965859843, 8.311093377946830785 ) ) ;
#4522=CARTESIAN_POINT ( 'NONE',  ( -5.000000000000005329, 140.2083333265053682, 8.660254037844387298 ) ) ;
#4526=CARTESIAN_POINT ( 'NONE',  ( -5.676582343749998039, 37.76041666325267698, -9.832129032723420536 ) ) ;
#4527=CARTESIAN_POINT ( 'NONE',  ( -7.320508075688773708, 78.74999999317202537, -7.320508075688774596 ) ) ;
#4528=ORIENTED_EDGE ( 'NONE', *, *, #51032, .T. ) ;
#4529=CYLINDRICAL_SURFACE ( 'NONE', #50073, 6.000000000000001776 ) ;
#4534=CARTESIAN_POINT ( 'NONE',  ( 9.832129032723420536, 161.1979166632526983, -5.676582343749999815 ) ) ;
#4543=CARTESIAN_POINT ( 'NONE',  ( -3.042071309553173730, 119.6354166632526841, 11.35316468749999785 ) ) ;
#4545=ORIENTED_EDGE ( 'NONE', *, *, #43452, .F. ) ;
#4547=ORIENTED_EDGE ( 'NONE', *, *, #63139, .F. ) ;
#4570=CARTESIAN_POINT ( 'NONE',  ( 4.242640687119287435, 288.3750000000000000, 4.242640687119285658 ) ) ;
#4575=CARTESIAN_POINT ( 'NONE',  ( 4.999999999999993783, 119.1666666666666714, 8.660254037844390851 ) ) ;
#4578=CARTESIAN_POINT ( 'NONE',  ( -4.721056650415998313, 293.7343750017069510, 4.721056650416000089 ) ) ;
#4592=CARTESIAN_POINT ( 'NONE',  ( -2.679491924311226292, 213.3333333265053682, -10.00000000000000178 ) ) ;
#4593=CARTESIAN_POINT ( 'NONE',  ( -11.35316468750000141, 13.28124999658601624, -1.390361679473963753E-15 ) ) ;
#4595=CARTESIAN_POINT ( 'NONE',  ( 3.042071309553167069, 212.1354166632526983, -11.35316468749999785 ) ) ;
#4601=CARTESIAN_POINT ( 'NONE',  ( -9.832129032723420536, 8.697916663252684089, 5.676582343749997150 ) ) ;
#4603=CARTESIAN_POINT ( 'NONE',  ( 8.660254037844385522, 209.5833333333333428, 5.000000000000006217 ) ) ;
#4607=CARTESIAN_POINT ( 'NONE',  ( -8.311093377946836114, 12.65624999658601624, -8.311093377946837890 ) ) ;
#4609=CARTESIAN_POINT ( 'NONE',  ( -11.35316468750000141, 138.2812499965860411, -1.390361679473963753E-15 ) ) ;
#4610=CARTESIAN_POINT ( 'NONE',  ( -10.00000000000000000, 104.1666666598386968, -2.679491924311229845 ) ) ;
#4617=CARTESIAN_POINT ( 'NONE',  ( -4.721056650415998313, 290.7343750017069510, 4.721056650416000089 ) ) ;
#4622=AXIS2_PLACEMENT_3D ( 'NONE', #22841, #57572, #22459 ) ;
#4624=EDGE_LOOP ( 'NONE', ( #44465, #12342, #67187, #23154 ) ) ;
#4629=CARTESIAN_POINT ( 'NONE',  ( -3.042071309553163960, 167.5520833299193271, -11.35316468749999963 ) ) ;
#4630=FACE_BOUND ( 'NONE', #52260, .T. ) ;
#4633=CARTESIAN_POINT ( 'NONE',  ( -9.832129032723420536, 74.01041666325268409, 5.676582343749997150 ) ) ;
#4641=CARTESIAN_POINT ( 'NONE',  ( -2.679491924311161455, 110.4166666598387110, 10.00000000000004441 ) ) ;
#4643=CARTESIAN_POINT ( 'NONE',  ( 2.679491924311222739, 65.83333332650536818, 10.00000000000000355 ) ) ;
#4666=CARTESIAN_POINT ( 'NONE',  ( -2.679491924311235618, 78.54166666666667140, 10.00000000000000000 ) ) ;
#4668=CARTESIAN_POINT ( 'NONE',  ( -3.673940397442060854E-16, 290.7500000000000000, -6.000000000000001776 ) ) ;
#4675=LINE ( 'NONE', #63116, #53894 ) ;
#4679=CARTESIAN_POINT ( 'NONE',  ( -2.679491924311235618, 198.5416666666666288, 10.00000000000000000 ) ) ;
#4680=( BOUNDED_CURVE ( )  B_SPLINE_CURVE ( 2, ( #31860, #54884, #16345, #56742, #40869, #11086, #34490, #51814, #39382 ),
 .UNSPECIFIED., .F., .F. ) 
 B_SPLINE_CURVE_WITH_KNOTS ( ( 3, 2, 2, 2, 3 ),
 ( 0.1458333333333311499, 0.1562499999999978073, 0.1666666666666644647, 0.1770833333333311777, 0.1874999999999978351 ),
 .UNSPECIFIED. ) 
 CURVE ( )  GEOMETRIC_REPRESENTATION_ITEM ( )  RATIONAL_B_SPLINE_CURVE ( ( 1.000000000000015987, 0.9238795325112707513, 1.000000000000000000, 0.9238795325112867385, 1.000000000000000000, 0.9238795325112867385, 1.000000000000000000, 0.9238795325113025037, 0.9999999999999842348 ) ) 
 REPRESENTATION_ITEM ( '' )  );
#4683=CARTESIAN_POINT ( 'NONE',  ( 9.832129032723416984, 165.6770833299193555, 5.676582343750006032 ) ) ;
#4690=CARTESIAN_POINT ( 'NONE',  ( 9.832129032723420536, 26.51041666325268409, -5.676582343749999815 ) ) ;
#4692=DIRECTION ( 'NONE',  ( 0.000000000000000000, 0.000000000000000000, 1.000000000000000000 ) ) ;
#4697=CARTESIAN_POINT ( 'NONE',  ( 10.00000000000000000, 56.66666665983868967, 2.679491924311236062 ) ) ;
#4700=CARTESIAN_POINT ( 'NONE',  ( 6.123233995736767268E-16, 101.2500000000000000, -10.00000000000000178 ) ) ;
#4708=CARTESIAN_POINT ( 'NONE',  ( 6.951808397369818766E-16, 147.0312499965860411, -11.35316468750000141 ) ) ;
#4721=CARTESIAN_POINT ( 'NONE',  ( 5.676582343750001591, 111.9270833299193555, -9.832129032723420536 ) ) ;
#4725=CARTESIAN_POINT ( 'NONE',  ( 8.311093377946834337, 40.46874999658601979, 8.311093377946839666 ) ) ;
#4727=CARTESIAN_POINT ( 'NONE',  ( 0.000000000000000000, 284.0000000000000000, 0.000000000000000000 ) ) ;
#4734=CARTESIAN_POINT ( 'NONE',  ( -6.000000000000000888, 297.1250000034141294, 2.485281374238575758 ) ) ;
#4735=CARTESIAN_POINT ( 'NONE',  ( -6.000000000000001776, 297.0000000000000000, 0.000000000000000000 ) ) ;
#4737=EDGE_CURVE ( 'NONE', #13964, #69323, #64401, .T. ) ;
#4738=CARTESIAN_POINT ( 'NONE',  ( 9.832129032723420536, 156.5104166632526983, -5.676582343749999815 ) ) ;
#4745=CIRCLE ( 'NONE', #52936, 10.00000000000000178 ) ;
#4753=CARTESIAN_POINT ( 'NONE',  ( 6.123233995736767268E-16, 208.1249999931720538, -10.00000000000000178 ) ) ;
#4755=CARTESIAN_POINT ( 'NONE',  ( 10.00000000000000178, 40.20833333333334281, -2.679491924311226736 ) ) ;
#4758=CARTESIAN_POINT ( 'NONE',  ( -6.676582343750001591, 288.4531250017069510, 0.000000000000000000 ) ) ;
#4769=CARTESIAN_POINT ( 'NONE',  ( -10.00000000000000178, 152.5000000000000000, -1.224646799147353454E-15 ) ) ;
#4773=CARTESIAN_POINT ( 'NONE',  ( 5.676582343750001591, 121.9270833299193413, -9.832129032723420536 ) ) ;
#4774=CARTESIAN_POINT ( 'NONE',  ( -3.673940397442060854E-16, 295.7500000000000000, -6.000000000000001776 ) ) ;
#4780=CARTESIAN_POINT ( 'NONE',  ( 9.088647732546041524, 225.3440916664238785, -4.181359934662540745 ) ) ;
#4785=CARTESIAN_POINT ( 'NONE',  ( 8.311093377946837890, 206.7187499965859843, -8.311093377946837890 ) ) ;
#4792=CARTESIAN_POINT ( 'NONE',  ( 3.042071309553159519, 99.73958332991934128, 11.35316468750000141 ) ) ;
#4793=ORIENTED_EDGE ( 'NONE', *, *, #24640, .T. ) ;
#4798=CARTESIAN_POINT ( 'NONE',  ( -3.042071309553164404, 97.23958332991936970, -11.35316468749999963 ) ) ;
#4801=CARTESIAN_POINT ( 'NONE',  ( 6.123233995736767268E-16, 208.1249999931720538, -10.00000000000000178 ) ) ;
#4807=CARTESIAN_POINT ( 'NONE',  ( 3.042071309553167513, 91.82291666325269830, -11.35316468749999785 ) ) ;
#4812=CARTESIAN_POINT ( 'NONE',  ( -2.679491924311225848, 183.3333333265053113, -10.00000000000000178 ) ) ;
#4815=CARTESIAN_POINT ( 'NONE',  ( 11.35316468749999963, 81.30208332991935549, -3.042071309553165293 ) ) ;
#4816=CARTESIAN_POINT ( 'NONE',  ( -2.765530957081996810, 289.2656250017069510, -6.676582343750003368 ) ) ;
#4819=CARTESIAN_POINT ( 'NONE',  ( 9.832129032723416984, 225.3645833299193839, 5.676582343750006032 ) ) ;
#4824=CARTESIAN_POINT ( 'NONE',  ( 6.951808397369818766E-16, 207.0312499965860411, -11.35316468750000141 ) ) ;
#4826=CARTESIAN_POINT ( 'NONE',  ( 0.000000000000000000, 300.0000000000000000, 0.000000000000000000 ) ) ;
#4827=CARTESIAN_POINT ( 'NONE',  ( -4.088227598258586603E-16, 299.2031250017070079, -6.676582343750001591 ) ) ;
#4829=CARTESIAN_POINT ( 'NONE',  ( 9.832129032723420536, 191.5104166632526983, -5.676582343749999815 ) ) ;
#4836=EDGE_CURVE ( 'NONE', #46242, #70220, #5127, .T. ) ;
#4837=CARTESIAN_POINT ( 'NONE',  ( 8.660254037844385522, 9.583333333333333925, 5.000000000000005329 ) ) ;
#4852=SHAPE_DEFINITION_REPRESENTATION ( #21604, #43124 ) ;
#4860=CARTESIAN_POINT ( 'NONE',  ( 5.676582343749993598, 85.26041666325268409, 9.832129032723422313 ) ) ;
#4865=CARTESIAN_POINT ( 'NONE',  ( 6.676582343750003368, 290.0468750017070079, 2.765530957081995478 ) ) ;
#4869=CARTESIAN_POINT ( 'NONE',  ( 3.042071309553167069, 196.8229166632526983, -11.35316468749999785 ) ) ;
#4874=CARTESIAN_POINT ( 'NONE',  ( -8.311093377946836114, 162.9687499965860411, -8.311093377946837890 ) ) ;
#4877=CARTESIAN_POINT ( 'NONE',  ( -8.660254037844387298, 207.9166666666667140, 4.999999999999995559 ) ) ;
#4881=CARTESIAN_POINT ( 'NONE',  ( -3.042071309553173730, 59.32291666325268409, 11.35316468749999785 ) ) ;
#4886=CARTESIAN_POINT ( 'NONE',  ( -9.832129032723420536, 63.69791666325269830, 5.676582343749997150 ) ) ;
#4892=CARTESIAN_POINT ( 'NONE',  ( -9.832129032723420536, 43.69791666325268409, 5.676582343749997150 ) ) ;
#4894=EDGE_CURVE ( 'NONE', #19485, #38928, #59116, .T. ) ;
#4896=CARTESIAN_POINT ( 'NONE',  ( -3.042071309553164404, 172.2395833299193839, -11.35316468749999963 ) ) ;
#4898=CARTESIAN_POINT ( 'NONE',  ( -7.320508075688773708, 148.7499999931720538, -7.320508075688774596 ) ) ;
#4901=CARTESIAN_POINT ( 'NONE',  ( -11.35316468749999785, 33.38541666325269119, -3.042071309553167957 ) ) ;
#4904=CARTESIAN_POINT ( 'NONE',  ( -1.836970198721029983E-15, 80.62499999317203958, 10.00000000000000178 ) ) ;
#4905=CARTESIAN_POINT ( 'NONE',  ( -9.832129032723418760, 182.8645833299193555, -5.676582343750004256 ) ) ;
#4913=CARTESIAN_POINT ( 'NONE',  ( -2.085542519210945728E-15, 164.5312499965860127, 11.35316468750000141 ) ) ;
#4923=CARTESIAN_POINT ( 'NONE',  ( 5.676582343749993598, 120.2604166632526841, 9.832129032723422313 ) ) ;
#4937=ORIENTED_EDGE ( 'NONE', *, *, #12145, .T. ) ;
#4947=CARTESIAN_POINT ( 'NONE',  ( 2.485281374238838215, 288.3125000000000000, 5.999999999999736211 ) ) ;
#4951=CARTESIAN_POINT ( 'NONE',  ( 7.320508075688828775, 59.37500000000004263, 7.320508075688831440 ) ) ;
#4953=CARTESIAN_POINT ( 'NONE',  ( 10.00000000000000000, 124.7916666666666572, 2.679491924311236062 ) ) ;
#4955=CARTESIAN_POINT ( 'NONE',  ( -6.676582343750001591, 288.6093750017069510, 0.000000000000000000 ) ) ;
#4966=CARTESIAN_POINT ( 'NONE',  ( -7.320508075688773708, 93.74999999317202537, -7.320508075688774596 ) ) ;
#4968=CARTESIAN_POINT ( 'NONE',  ( 11.35316468749999963, 10.98958332991935016, -3.042071309553165293 ) ) ;
#4969=CARTESIAN_POINT ( 'NONE',  ( 5.000000000000001776, 0.8333333333333323711, -8.660254037844389075 ) ) ;
#4970=CARTESIAN_POINT ( 'NONE',  ( -8.311093377946841443, 204.2187499965860411, 8.311093377946830785 ) ) ;
#4974=DIRECTION ( 'NONE',  ( 0.000000000000000000, 0.000000000000000000, 1.000000000000000000 ) ) ;
#4978=CARTESIAN_POINT ( 'NONE',  ( 5.676582343750001591, 16.61458332991935194, -9.832129032723420536 ) ) ;
#4984=CARTESIAN_POINT ( 'NONE',  ( 11.35316468749999785, 5.572916663252682312, 3.042071309553174174 ) ) ;
#4986=EDGE_CURVE ( 'NONE', #5468, #42176, #29787, .T. ) ;
#4987=CARTESIAN_POINT ( 'NONE',  ( 3.042071309553167069, 141.8229166632526983, -11.35316468749999785 ) ) ;
#4988=CARTESIAN_POINT ( 'NONE',  ( 10.00000000000000178, 96.87499999317203958, 0.000000000000000000 ) ) ;
#4997=CARTESIAN_POINT ( 'NONE',  ( -2.765530957081996810, 290.4218750017068942, -6.676582343750003368 ) ) ;
#5009=CARTESIAN_POINT ( 'NONE',  ( -3.042071309553164404, 82.55208332991936970, -11.35316468749999963 ) ) ;
#5041=CARTESIAN_POINT ( 'NONE',  ( -8.660254037844387298, 87.08333333333332860, -5.000000000000004441 ) ) ;
#5044=CARTESIAN_POINT ( 'NONE',  ( -2.765530957081998586, 298.7968750017069510, 6.676582343750001591 ) ) ;
#5047=CARTESIAN_POINT ( 'NONE',  ( 0.000000000000000000, 300.0000000000000000, 10.00000000000000178 ) ) ;
#5051=LINE ( 'NONE', #10697, #63523 ) ;
#5055=CARTESIAN_POINT ( 'NONE',  ( 2.679491924311222739, 198.9583333333333144, 10.00000000000000355 ) ) ;
#5057=CARTESIAN_POINT ( 'NONE',  ( -8.311093377946841443, 169.2187499965859843, 8.311093377946830785 ) ) ;
#5058=CARTESIAN_POINT ( 'NONE',  ( -7.320508075688771932, 36.87500000000001421, -7.320508075688772820 ) ) ;
#5059=CARTESIAN_POINT ( 'NONE',  ( 5.000000000000094147, 155.8333333333334565, -8.660254037844545394 ) ) ;
#5063=CARTESIAN_POINT ( 'NONE',  ( 8.311093377946837890, 26.71874999658601624, -8.311093377946837890 ) ) ;
#5071=CARTESIAN_POINT ( 'NONE',  ( 8.660254037844385522, 66.45833332650536818, 5.000000000000005329 ) ) ;
#5078=EDGE_LOOP ( 'NONE', ( #61814, #67294, #13238, #74063 ) ) ;
#5084=CARTESIAN_POINT ( 'NONE',  ( -11.35316468750000141, 143.2812499965860411, -1.390361679473963753E-15 ) ) ;
#5097=CARTESIAN_POINT ( 'NONE',  ( 3.042071309553167513, 132.1354166632526699, -11.35316468749999785 ) ) ;
#5101=CARTESIAN_POINT ( 'NONE',  ( 3.042071309553167069, 42.13541666325267698, -11.35316468749999785 ) ) ;
#5109=CARTESIAN_POINT ( 'NONE',  ( -6.000000000000003553, 296.0000000034139589, -2.485281374238571317 ) ) ;
#5110=DIRECTION ( 'NONE',  ( -0.000000000000000000, 1.000000000000000000, -0.000000000000000000 ) ) ;
#5111=FACE_OUTER_BOUND ( 'NONE', #28828, .T. ) ;
#5112=CARTESIAN_POINT ( 'NONE',  ( 11.35316468750000141, 156.0937499965860127, 0.000000000000000000 ) ) ;
#5114=( BOUNDED_CURVE ( )  B_SPLINE_CURVE ( 2, ( #50227, #4592, #27586, #26455, #16251, #44579, #56651, #55910, #45312, #22289, #39659, #15144, #50595 ),
 .UNSPECIFIED., .F., .F. ) 
 B_SPLINE_CURVE_WITH_KNOTS ( ( 3, 2, 2, 2, 2, 2, 3 ),
 ( 0.9184782608695651884, 0.9202898550724637472, 0.9221014492753623060, 0.9239130434782609758, 0.9257246376811595345, 0.9275362318840580933, 0.9293478260869566521 ),
 .UNSPECIFIED. ) 
 CURVE ( )  GEOMETRIC_REPRESENTATION_ITEM ( )  RATIONAL_B_SPLINE_CURVE ( ( 1.000000000000000000, 0.9659258262890683122, 1.000000000000000000, 0.9659258262890683122, 1.000000000000000000, 0.9659258262890683122, 1.000000000000000000, 0.9659258262890683122, 1.000000000000000000, 0.9659258262890683122, 1.000000000000000000, 0.9659258262890662028, 1.000000000000001998 ) ) 
 REPRESENTATION_ITEM ( '' )  );
#5124=CARTESIAN_POINT ( 'NONE',  ( -5.000000000000038192, 56.66666666666672114, -8.660254037844456576 ) ) ;
#5125=ORIENTED_EDGE ( 'NONE', *, *, #29937, .F. ) ;
#5127=( BOUNDED_CURVE ( )  B_SPLINE_CURVE ( 2, ( #37597, #43998, #14562, #20973, #55330, #56441, #72286, #3635, #27376, #50396, #15683, #27012, #26632 ),
 .UNSPECIFIED., .F., .F. ) 
 B_SPLINE_CURVE_WITH_KNOTS ( ( 3, 2, 2, 2, 2, 2, 3 ),
 ( 0.8320903676337926269, 0.8373236054718522503, 0.8425568433099117627, 0.8477900811479713861, 0.8530233189860307874, 0.8582565568240904108, 0.8634897946621500342 ),
 .UNSPECIFIED. ) 
 CURVE ( )  GEOMETRIC_REPRESENTATION_ITEM ( )  RATIONAL_B_SPLINE_CURVE ( ( 1.000000000000390576, 0.9659258262886779578, 1.000000000000000000, 0.9659258262890684232, 1.000000000000000000, 0.9659258262890684232, 1.000000000000000000, 0.9659258262890684232, 1.000000000000000000, 0.9659258262890684232, 1.000000000000000000, 0.9659258262890632052, 1.000000000000005329 ) ) 
 REPRESENTATION_ITEM ( '' )  );
#5129=CARTESIAN_POINT ( 'NONE',  ( -10.00000000000000178, 42.50000000000000000, -1.224646799147353454E-15 ) ) ;
#5132=CARTESIAN_POINT ( 'NONE',  ( -4.721056650415998313, 287.5781250017069510, 4.721056650416000089 ) ) ;
#5141=CARTESIAN_POINT ( 'NONE',  ( -8.660254037844390851, 147.9166666666666572, 4.999999999999998224 ) ) ;
#5143=CARTESIAN_POINT ( 'NONE',  ( -10.00000000000000000, 167.2916666666666856, -2.679491924311229845 ) ) ;
#5144=CARTESIAN_POINT ( 'NONE',  ( -4.242640687119286547, 299.8750000000000000, -4.242640687119286547 ) ) ;
#5147=CARTESIAN_POINT ( 'NONE',  ( -9.832129032723420536, 129.0104166632526983, 5.676582343749997150 ) ) ;
#5160=CARTESIAN_POINT ( 'NONE',  ( 8.311093377946834337, 205.4687499965859843, 8.311093377946839666 ) ) ;
#5166=CARTESIAN_POINT ( 'NONE',  ( 11.35316468750000141, 95.78124999658602690, 0.000000000000000000 ) ) ;
#5171=CARTESIAN_POINT ( 'NONE',  ( 5.676582343749993598, 99.94791666325268409, 9.832129032723422313 ) ) ;
#5175=CARTESIAN_POINT ( 'NONE',  ( 10.00000000000000178, 222.0833333265053682, -2.679491924311226736 ) ) ;
#5178=CARTESIAN_POINT ( 'NONE',  ( 11.35316468750000141, 95.78124999658602690, 0.000000000000000000 ) ) ;
#5183=ORIENTED_EDGE ( 'NONE', *, *, #58993, .T. ) ;
#5184=CARTESIAN_POINT ( 'NONE',  ( 2.679491924311228956, 182.9166666598386826, -10.00000000000000000 ) ) ;
#5187=CARTESIAN_POINT ( 'NONE',  ( 5.676582343750001591, 86.92708332991935549, -9.832129032723420536 ) ) ;
#5188=CARTESIAN_POINT ( 'NONE',  ( 6.676582343750003368, 288.0156250017069510, -2.765530957081997254 ) ) ;
#5191=CARTESIAN_POINT ( 'NONE',  ( 8.311093377946837890, 221.4062499965860411, -8.311093377946837890 ) ) ;
#5193=CARTESIAN_POINT ( 'NONE',  ( -2.679491924311226292, 68.33333332650535397, -10.00000000000000178 ) ) ;
#5196=CARTESIAN_POINT ( 'NONE',  ( 5.676582343749993598, 199.9479166632526983, 9.832129032723422313 ) ) ;
#5199=CARTESIAN_POINT ( 'NONE',  ( 4.721056650415999201, 296.0781250017069510, -4.721056650415999201 ) ) ;
#5200=ORIENTED_EDGE ( 'NONE', *, *, #30328, .T. ) ;
#5201=CARTESIAN_POINT ( 'NONE',  ( 8.311093377946837890, 191.7187499965860411, -8.311093377946837890 ) ) ;
#5206=AXIS2_PLACEMENT_3D ( 'NONE', #72646, #20949, #43971 ) ;
#5208=CARTESIAN_POINT ( 'NONE',  ( -10.00000000000000355, 17.70833333333332860, 2.679491924311223183 ) ) ;
#5210=ORIENTED_EDGE ( 'NONE', *, *, #20527, .T. ) ;
#5217=CARTESIAN_POINT ( 'NONE',  ( 5.000000000000001776, 152.7083333265053682, -8.660254037844389075 ) ) ;
#5228=ORIENTED_EDGE ( 'NONE', *, *, #64835, .T. ) ;
#5230=CARTESIAN_POINT ( 'NONE',  ( 8.311093377946837890, 91.71874999658599847, -8.311093377946837890 ) ) ;
#5235=CARTESIAN_POINT ( 'NONE',  ( -6.676582343749999815, 291.6718750017070079, 2.765530957082001251 ) ) ;
#5240=CARTESIAN_POINT ( 'NONE',  ( 8.311093377946837890, 201.4062499965860127, -8.311093377946837890 ) ) ;
#5246=CARTESIAN_POINT ( 'NONE',  ( 11.35316468750000141, 161.0937499965860127, 0.000000000000000000 ) ) ;
#5247=CYLINDRICAL_SURFACE ( 'NONE', #50384, 10.00000000000000178 ) ;
#5249=CARTESIAN_POINT ( 'NONE',  ( -5.000000000000002665, 208.3333333333333712, 8.660254037844383745 ) ) ;
#5253=CARTESIAN_POINT ( 'NONE',  ( -8.311093377946841443, 53.90624999658602690, 8.311093377946830785 ) ) ;
#5256=VERTEX_POINT ( 'NONE', #25045 ) ;
#5259=CARTESIAN_POINT ( 'NONE',  ( -3.042071309553173730, 64.32291666325269830, 11.35316468749999785 ) ) ;
#5265=CARTESIAN_POINT ( 'NONE',  ( 11.35316468750000141, 60.78124999658601979, 0.000000000000000000 ) ) ;
#5269=CARTESIAN_POINT ( 'NONE',  ( -11.35316468749999785, 173.0729166632526983, -3.042071309553167513 ) ) ;
#5270=CARTESIAN_POINT ( 'NONE',  ( -2.679491924311225848, 148.3333333265053398, -10.00000000000000178 ) ) ;
#5273=CARTESIAN_POINT ( 'NONE',  ( 5.676582343749993598, 30.26041666325268409, 9.832129032723422313 ) ) ;
#5274=CARTESIAN_POINT ( 'NONE',  ( 6.123233995736767268E-16, 78.12499999317202537, -10.00000000000000178 ) ) ;
#5275=CARTESIAN_POINT ( 'NONE',  ( -11.35316468750000141, 188.2812499965860127, -1.390361679473963753E-15 ) ) ;
#5282=CARTESIAN_POINT ( 'NONE',  ( -11.35316468749999785, 168.0729166632526983, -3.042071309553167957 ) ) ;
#5285=CARTESIAN_POINT ( 'NONE',  ( 2.250000000000001332, 267.1999999999996476, 5.427798388956546205 ) ) ;
#5291=CARTESIAN_POINT ( 'NONE',  ( -9.832129032723420536, 119.0104166632526841, 5.676582343749997150 ) ) ;
#5307=CARTESIAN_POINT ( 'NONE',  ( 2.485281374238919927, 293.3125000000000568, 5.999999999999654499 ) ) ;
#5310=ORIENTED_EDGE ( 'NONE', *, *, #29310, .F. ) ;
#5320=CARTESIAN_POINT ( 'NONE',  ( -10.00000000000000000, 122.2916666666666430, -2.679491924311229845 ) ) ;
#5322=CARTESIAN_POINT ( 'NONE',  ( 6.676582343750003368, 288.1718750017069510, -2.765530957081997254 ) ) ;
#5328=VECTOR ( 'NONE', #43033, 1000.000000000000000 ) ;
#5336=CARTESIAN_POINT ( 'NONE',  ( 8.311093377946837890, 21.40624999658601268, -8.311093377946837890 ) ) ;
#5338=DIRECTION ( 'NONE',  ( 0.000000000000000000, 0.000000000000000000, 1.000000000000000000 ) ) ;
#5339=CARTESIAN_POINT ( 'NONE',  ( 8.311093377946834337, 205.4687499965859843, 8.311093377946839666 ) ) ;
#5343=ORIENTED_EDGE ( 'NONE', *, *, #11362, .T. ) ;
#5345=CARTESIAN_POINT ( 'NONE',  ( -8.311093377946836114, 17.65624999658601979, -8.311093377946837890 ) ) ;
#5347=CARTESIAN_POINT ( 'NONE',  ( -3.166186134455097228E-13, 211.2500000000000568, -9.999999999999998224 ) ) ;
#5350=CARTESIAN_POINT ( 'NONE',  ( 11.35316468749999963, 5.989583329919350163, -3.042071309553165293 ) ) ;
#5352=CARTESIAN_POINT ( 'NONE',  ( 5.676582343750001591, 131.6145833299193555, -9.832129032723420536 ) ) ;
#5354=CARTESIAN_POINT ( 'NONE',  ( -2.679491924311225848, 103.3333333265053824, -10.00000000000000178 ) ) ;
#5363=CARTESIAN_POINT ( 'NONE',  ( -4.721056650415998313, 288.7343750017069510, 4.721056650416000089 ) ) ;
#5364=CARTESIAN_POINT ( 'NONE',  ( 8.311093377946834337, 120.1562499965860127, 8.311093377946839666 ) ) ;
#5374=EDGE_CURVE ( 'NONE', #2057, #47752, #56637, .T. ) ;
#5375=CARTESIAN_POINT ( 'NONE',  ( 8.311093377946834337, 70.46874999658599847, 8.311093377946839666 ) ) ;
#5394=EDGE_CURVE ( 'NONE', #16317, #23374, #68682, .T. ) ;
#5399=ORIENTED_EDGE ( 'NONE', *, *, #20267, .F. ) ;
#5400=EDGE_CURVE ( 'NONE', #28551, #23989, #9538, .T. ) ;
#5401=CARTESIAN_POINT ( 'NONE',  ( -5.999999999999999112, 292.0625000000000000, 2.485281374238575314 ) ) ;
#5402=ORIENTED_EDGE ( 'NONE', *, *, #60670, .F. ) ;
#5407=CARTESIAN_POINT ( 'NONE',  ( -8.660254037844387298, 77.08333333333334281, -5.000000000000004441 ) ) ;
#5409=CARTESIAN_POINT ( 'NONE',  ( -6.000000000000001776, 290.0000000000000000, 0.000000000000000000 ) ) ;
#5410=VERTEX_POINT ( 'NONE', #34380 ) ;
#5418=CARTESIAN_POINT ( 'NONE',  ( -10.00000000000000355, 202.7083333333333144, 2.679491924311223183 ) ) ;
#5420=CARTESIAN_POINT ( 'NONE',  ( -11.35316468750000141, 163.8020833299193555, 3.042071309553159963 ) ) ;
#5427=CARTESIAN_POINT ( 'NONE',  ( 11.35316468749999785, 30.88541666325268409, 3.042071309553174174 ) ) ;
#5432=CARTESIAN_POINT ( 'NONE',  ( 2.679491924311376394, 222.9166666598387110, -9.999999999999914735 ) ) ;
#5437=CARTESIAN_POINT ( 'NONE',  ( 7.320508075688774596, 67.49999999317201116, -7.320508075688774596 ) ) ;
#5441=CARTESIAN_POINT ( 'NONE',  ( 8.660254037844429931, 64.58333333333337123, 5.000000000000031086 ) ) ;
#5446=EDGE_CURVE ( 'NONE', #30484, #3444, #1398, .T. ) ;
#5447=CARTESIAN_POINT ( 'NONE',  ( -7.320508075688851868, 196.8750000000001421, -7.320508075688852756 ) ) ;
#5450=CARTESIAN_POINT ( 'NONE',  ( -10.00000000000000355, 87.70833333333332860, 2.679491924311222739 ) ) ;
#5451=CARTESIAN_POINT ( 'NONE',  ( -3.042071309553164404, 147.2395833299193555, -11.35316468749999963 ) ) ;
#5452=CARTESIAN_POINT ( 'NONE',  ( 9.999999999999987566, 105.0000000000000000, 0.000000000000000000 ) ) ;
#5460=( BOUNDED_CURVE ( )  B_SPLINE_CURVE ( 2, ( #44116, #72018, #67125, #3375, #43349, #72403, #32046, #15420, #32809 ),
 .UNSPECIFIED., .F., .F. ) 
 B_SPLINE_CURVE_WITH_KNOTS ( ( 3, 2, 2, 2, 3 ),
 ( 0.7708333333333317050, 0.7812499999999983347, 0.7916666666666649643, 0.8020833333333317050, 0.8124999999999983347 ),
 .UNSPECIFIED. ) 
 CURVE ( )  GEOMETRIC_REPRESENTATION_ITEM ( )  RATIONAL_B_SPLINE_CURVE ( ( 1.000000000000012212, 0.9238795325112745260, 1.000000000000000000, 0.9238795325112867385, 1.000000000000000000, 0.9238795325112867385, 1.000000000000000000, 0.9238795325112989509, 0.9999999999999877875 ) ) 
 REPRESENTATION_ITEM ( '' )  );
#5463=CARTESIAN_POINT ( 'NONE',  ( -11.35316468749999785, 133.3854166632526699, -3.042071309553167957 ) ) ;
#5467=CARTESIAN_POINT ( 'NONE',  ( -8.311093377946841443, 39.21874999658600558, 8.311093377946830785 ) ) ;
#5468=VERTEX_POINT ( 'NONE', #12731 ) ;
#5469=CARTESIAN_POINT ( 'NONE',  ( 7.320508075688771044, 36.24999999317202537, 7.320508075688775484 ) ) ;
#5474=CARTESIAN_POINT ( 'NONE',  ( 1.102182119232618108E-15, 298.3125000034140157, 6.000000000000001776 ) ) ;
#5478=CARTESIAN_POINT ( 'NONE',  ( -3.042071309553164404, 152.5520833299193271, -11.35316468749999963 ) ) ;
#5490=CARTESIAN_POINT ( 'NONE',  ( -8.660254037844458352, 57.91666666666671404, 5.000000000000038192 ) ) ;
#5493=EDGE_CURVE ( 'NONE', #70220, #64059, #73643, .T. ) ;
#5495=CARTESIAN_POINT ( 'NONE',  ( 0.000000000000000000, 300.0000000000000000, 0.000000000000000000 ) ) ;
#5496=DIRECTION ( 'NONE',  ( 0.000000000000000000, 0.000000000000000000, 1.000000000000000000 ) ) ;
#5497=CARTESIAN_POINT ( 'NONE',  ( 8.660254037844385522, 44.58333333333333570, 5.000000000000005329 ) ) ;
#5500=CARTESIAN_POINT ( 'NONE',  ( 4.242640687119285658, 298.6250000000000000, -4.242640687119286547 ) ) ;
#5501=CARTESIAN_POINT ( 'NONE',  ( 4.999999999999992006, 34.16666666666667140, 8.660254037844389075 ) ) ;
#5507=CARTESIAN_POINT ( 'NONE',  ( -3.171697045051319909E-12, 121.2500000000002558, -10.00000000000000178 ) ) ;
#5510=CARTESIAN_POINT ( 'NONE',  ( 2.679491924311228956, 156.0416666666666856, -10.00000000000000000 ) ) ;
#5514=CARTESIAN_POINT ( 'NONE',  ( -11.35316468750000141, 123.5937499965860269, -1.390361679473963753E-15 ) ) ;
#5515=CARTESIAN_POINT ( 'NONE',  ( -2.485281374238927032, 293.8750000034140157, -5.999999999999647393 ) ) ;
#5520=VERTEX_POINT ( 'NONE', #1075 ) ;
#5521=CARTESIAN_POINT ( 'NONE',  ( 1.181652764918876164, 223.8432429321183292, 9.934327413902742876 ) ) ;
#5522=CYLINDRICAL_SURFACE ( 'NONE', #7254, 10.00000000000000178 ) ;
#5525=CARTESIAN_POINT ( 'NONE',  ( -3.042071309553164404, 217.5520833299193555, -11.35316468749999963 ) ) ;
#5532=CARTESIAN_POINT ( 'NONE',  ( -3.042071309553173730, 99.32291666325268409, 11.35316468749999785 ) ) ;
#5534=CARTESIAN_POINT ( 'NONE',  ( -1.836970198721029983E-15, 145.6249999931720538, 10.00000000000000178 ) ) ;
#5537=CARTESIAN_POINT ( 'NONE',  ( 3.042071309553159519, 99.73958332991934128, 11.35316468750000141 ) ) ;
#5538=VERTEX_POINT ( 'NONE', #18034 ) ;
#5541=CARTESIAN_POINT ( 'NONE',  ( 10.00000000000000178, 221.8749999931720254, 0.000000000000000000 ) ) ;
#5545=CARTESIAN_POINT ( 'NONE',  ( 11.35316468749999785, 95.57291666325269830, 3.042071309553174174 ) ) ;
#5550=CARTESIAN_POINT ( 'NONE',  ( -8.660254037844387298, 198.9583333265053682, -5.000000000000004441 ) ) ;
#5554=CARTESIAN_POINT ( 'NONE',  ( 3.042071309553159519, 90.05208332991932707, 11.35316468750000141 ) ) ;
#5555=CARTESIAN_POINT ( 'NONE',  ( -2.765530957081998586, 288.6406250017069510, 6.676582343750001591 ) ) ;
#5559=CARTESIAN_POINT ( 'NONE',  ( 6.951808397369818766E-16, 2.343749996586016682, -11.35316468750000141 ) ) ;
#5564=CARTESIAN_POINT ( 'NONE',  ( -3.042071309553173730, 214.3229166632526699, 11.35316468749999785 ) ) ;
#5567=CARTESIAN_POINT ( 'NONE',  ( 6.676582343750001591, 296.9531250017069510, -8.176455196517173205E-16 ) ) ;
#5570=CARTESIAN_POINT ( 'NONE',  ( 9.832129032723416984, 210.6770833299193555, 5.676582343750006032 ) ) ;
#5577=ORIENTED_EDGE ( 'NONE', *, *, #12046, .F. ) ;
#5582=CARTESIAN_POINT ( 'NONE',  ( -8.660254037844390851, 22.91666666666666785, 4.999999999999998224 ) ) ;
#5585=ORIENTED_EDGE ( 'NONE', *, *, #8619, .T. ) ;
#5593=CARTESIAN_POINT ( 'NONE',  ( -6.676582343750001591, 295.4531250017069510, 0.000000000000000000 ) ) ;
#5596=CARTESIAN_POINT ( 'NONE',  ( 1.102182119232618108E-15, 289.3125000034140157, 6.000000000000001776 ) ) ;
#5604=CARTESIAN_POINT ( 'NONE',  ( 3.042071309553167069, 92.13541666325266988, -11.35316468749999785 ) ) ;
#5612=CARTESIAN_POINT ( 'NONE',  ( -11.35316468750000141, 193.4895833299193271, 3.042071309553159963 ) ) ;
#5616=CARTESIAN_POINT ( 'NONE',  ( 11.35316468749999963, 176.3020833299193839, -3.042071309553165293 ) ) ;
#5619=CARTESIAN_POINT ( 'NONE',  ( -8.660254037844383745, 207.0833333333333997, -5.000000000000001776 ) ) ;
#5620=CARTESIAN_POINT ( 'NONE',  ( -7.320508075688774596, 108.1250000000000142, 7.320508075688765715 ) ) ;
#5624=CARTESIAN_POINT ( 'NONE',  ( -3.042071309553164404, 57.23958332991934839, -11.35316468749999963 ) ) ;
#5630=CARTESIAN_POINT ( 'NONE',  ( -9.832129032723420536, 68.69791666325268409, 5.676582343749997150 ) ) ;
#5635=CARTESIAN_POINT ( 'NONE',  ( 11.35316468749999785, 60.57291666325268409, 3.042071309553174174 ) ) ;
#5637=CARTESIAN_POINT ( 'NONE',  ( -4.999999999999998224, 13.54166665983870033, -8.660254037844389075 ) ) ;
#5638=CARTESIAN_POINT ( 'NONE',  ( 5.676582343749993598, 174.9479166632526699, 9.832129032723422313 ) ) ;
#5639=CARTESIAN_POINT ( 'NONE',  ( -4.999999999999998224, 148.5416666598387110, -8.660254037844389075 ) ) ;
#5642=CARTESIAN_POINT ( 'NONE',  ( 6.951808397369818766E-16, 52.34374999658601979, -11.35316468750000141 ) ) ;
#5643=CARTESIAN_POINT ( 'NONE',  ( 6.000000000000003553, 295.6250000034140157, -2.485281374238571761 ) ) ;
#5644=CARTESIAN_POINT ( 'NONE',  ( 9.832129032723420536, 176.1979166632526983, -5.676582343749999815 ) ) ;
#5645=ORIENTED_EDGE ( 'NONE', *, *, #43204, .F. ) ;
#5649=CARTESIAN_POINT ( 'NONE',  ( -5.676582343749998039, 182.4479166632526983, -9.832129032723420536 ) ) ;
#5657=ORIENTED_EDGE ( 'NONE', *, *, #23020, .T. ) ;
#5659=CARTESIAN_POINT ( 'NONE',  ( -9.832129032723420536, 129.0104166632526983, 5.676582343749997150 ) ) ;
#5663=ADVANCED_FACE ( 'NONE', ( #60614 ), #71547, .T. ) ;
#5678=CARTESIAN_POINT ( 'NONE',  ( 2.485281374238225816, 293.6875000000000000, -6.000000000000346390 ) ) ;
#5690=CARTESIAN_POINT ( 'NONE',  ( 4.721056650415999201, 299.2343750017069510, -4.721056650415999201 ) ) ;
#5691=CARTESIAN_POINT ( 'NONE',  ( 8.660254037844389075, 125.4166666666666714, -5.000000000000000000 ) ) ;
#5693=CARTESIAN_POINT ( 'NONE',  ( 1.226468279477575784E-15, 288.8593750017070079, 6.676582343750001591 ) ) ;
#5700=LINE ( 'NONE', #17377, #2247 ) ;
#5705=CARTESIAN_POINT ( 'NONE',  ( 3.042071309553167069, 16.82291666325268054, -11.35316468749999785 ) ) ;
#5707=CARTESIAN_POINT ( 'NONE',  ( -11.35316468749999785, 208.3854166632526415, -3.042071309553167513 ) ) ;
#5709=CARTESIAN_POINT ( 'NONE',  ( -2.679491924311521167, 218.3333333265053966, -9.999999999999833022 ) ) ;
#5711=CARTESIAN_POINT ( 'NONE',  ( -7.320508075688897165, 43.12500000000009237, 7.320508075688889171 ) ) ;
#5714=CARTESIAN_POINT ( 'NONE',  ( -11.35316468750000141, 23.48958332991934483, 3.042071309553159963 ) ) ;
#5720=CARTESIAN_POINT ( 'NONE',  ( 3.042071309553159519, 19.73958332991934483, 11.35316468750000141 ) ) ;
#5722=CARTESIAN_POINT ( 'NONE',  ( 3.042071309553159519, 134.7395833299193839, 11.35316468750000141 ) ) ;
#5724=CARTESIAN_POINT ( 'NONE',  ( -7.320508075688778149, 104.9999999931720396, 7.320508075688769267 ) ) ;
#5731=CARTESIAN_POINT ( 'NONE',  ( 3.042071309553167513, 7.135416663252683200, -11.35316468749999785 ) ) ;
#5733=CARTESIAN_POINT ( 'NONE',  ( -4.721056650415998313, 298.5781250017069510, 4.721056650416000089 ) ) ;
#5734=CARTESIAN_POINT ( 'NONE',  ( -8.311093377946836114, 132.6562499965860411, -8.311093377946837890 ) ) ;
#5741=CYLINDRICAL_SURFACE ( 'NONE', #6339, 6.000000000000001776 ) ;
#5743=CARTESIAN_POINT ( 'NONE',  ( -3.042071309553173730, 79.63541666325268409, 11.35316468749999785 ) ) ;
#5752=CARTESIAN_POINT ( 'NONE',  ( 5.000000000000001776, 115.8333333333333712, -8.660254037844389075 ) ) ;
#5758=( BOUNDED_SURFACE ( )  B_SPLINE_SURFACE ( 1, 2, ( 
 ( #40965, #40216, #24343, #46243, #35678, #63590, #46614, #11919, #6271, #69635, #17949, #58694, #71460, #24703, #19411, #30745, #25809, #43539, #25065, #37147, #1723, #59427, #42424, #53400, #60901, #47713, #66184, #37526, #7739, #8104, #70733, #66553, #48828, #2819, #42056, #31862, #8470, #65063, #71835, #72212, #19785, #65442, #59792, #31490, #48455, #20152, #43168, #60150, #14864, #31107, #13737, #14487, #53765, #60527, #8854, #49202, #65809, #30380, #19053, #13375, #36782, #36413, #2076, #54513, #54135, #48084, #71093, #54886, #37903, #2446, #42793, #25438, #14115, #26183, #3196, #20525, #74082, #10344, #68056, #15240, #62019, #50691, #32625, #33004, #9223, #55633, #16347, #32245, #33368, #38652, #73710, #4318, #67689, #26558, #3568, #22021, #39384, #72599, #27307, #62381, #21277, #61278, #55262, #15986, #49581, #20905, #39017, #43926, #56369, #44674, #10709, #33741, #22382, #72972, #49957, #66936, #45047, #44300, #26938, #3949, #51070, #56744, #4690, #5063, #67316, #28059, #45403, #27685, #68419, #16720, #38274, #39747, #9606, #15613, #61654, #9973, #56004, #50323, #73345, #21648, #64253, #17478, #18230, #5427, #12190, #28431, #11458, #11089, #40124, #17101, #1268, #58603, #11826, #52938, #63131, #70287, #40498, #68792, #29552, #34115, #18601, #62748, #52561, #63504, #69544, #40873, #6909, #28800, #47260, #51818, #45781, #63878, #57869, #35589, #530, #6546, #34864, #35228, #57115, #6177, #900, #17854, #23509, #34493, #29184, #46525, #57500, #58246, #5803, #51439, #46152, #162, #24248, #74450, #23140, #29920, #69169, #23887, #46896, #22759, #69920, #52199, #41245, #12562, #8014, #43077, #31021, #35955, #64625, #64978, #48366, #7282, #24615, #42706, #30290, #8381, #54045, #2356, #12921, #71744, #66093, #7652, #65718, #36694, #30658, #20059, #31396, #37060, #54423, #41610, #25350, #60060, #71370, #19695, #13286, #14022, #58975, #48738, #1634, #2729, #59705, #25717, #47995, #53310, #47623, #70645, #18965, #41968, #36326, #59340, #53675, #1988, #24978, #71009, #19324, #42337, #65354, #13654, #143, #47239, #17835, #42956, #8262, #13903, #59947, #57477, #18209, #70266, #69898, #41223, #34842, #12540, #65975, #36942, #28779, #18579, #6524, #64231, #46501, #29531, #46875, #51796, #71625, #69521, #41590, #35208, #40477, #31276, #510, #64603, #19947, #6889, #54304, #35568, #23119, #14279, #24225, #2615, #63482, #29900, #40849, #52541, #69149, #58581, #25605, #12172, #48618, #46131, #52913, #17456, #6155, #5783, #57849, #11804, #29163, #52178, #879, #23489, #63857, #58225, #23865, #1248, #4115, #8642, #44842, #67849, #27108, #15034, #44099, #15403, #56171, #3357, #21809, #26347, #20315, #38442, #32411, #10135, #49752, #55799, #38070, #61445, #37317, #61069, #50123, #67107, #72769, #9016, #55424, #21075, #60696, #9772, #37696, #54677, #20698, #43332, #50489, #73502, #55050, #4484, #66351, #73139, #32791, #2983, #21445, #9391, #32030, #27475, #44468, #60314, #67481, #25968, #31656, #49368, #15780, #48990, #14655, #38818, #61817, #72385, #33173, #43716, #72000, #66730, #3733, #26732, #29360, #33917, #58042, #45210, #28975, #40295, #56543, #11624, #16900, #39558, #6356, #45952, #23685, #68969, #33542, #62183, #56917, #34662, #4860, #68221, #51995, #50865, #17649, #17278, #22945, #10510, #52366, #27856, #45579, #73881, #5972, #51239, #702, #40668, #46325, #63671, #16140, #51613, #332, #28602, #74629, #16518, #63296, #46691, #69339, #22185, #23313, #39926, #57665, #5230, #62932, #5604, #62552, #39179, #28231, #11998, #68594, #10883, #35030, #74250, #22558, #11257, #34286, #57290, #53478, #64053, #2530, #36493, #2157, #1070, #42134, #30089, #64788, #6715, #59145, #71175, #24423, #25150, #12364, #19129, #35399, #18400, #18029, #47057, #24048, #8184, #65526, #18772, #59871, #70094, #25522, #47430, #41415, #59506, #41045, #69715, #58409, #7819, #70454, #1795, #47794, #13819, #35758, #54219, #58775, #52736, #70817, #13089, #42509, #7454, #13456, #41777, #65146, #29722, #36124, #30822, #24779, #30461, #64427, #53844, #12725, #48167, #19493, #7083, #36863, #53108, #31195, #1442, #26263, #2901, #38738, #20611, #4032, #73051, #14946, #42872, #37609, #48905, #44010, #61737, #43251, #55342, #19866, #25886, #60609, #71542, #4397, #65891, #9688, #55717, #71919, #49283, #14197, #10054, #67020, #20986, #60232, #50037, #26645, #8557, #15317, #15696, #37985, #8933, #3276, #49667, #66639, #38353, #61361, #3645, #33091, #72299, #31944, #32708, #20232, #27026, #21359, #67394, #9305, #48534, #37234, #31571, #54967, #54595, #66267, #72684, #43629, #14574, #60984, #44383, #56088, #32329, #16805, #16432, #4773, #23226, #34195, #34945, #17564, #28514, #11540, #33455, #5514, #68878, #56456, #62465, #74162, #63211, #34572, #27390, #51523, #56826, #17188, #22466, #11173, #44758, #21728, #40207, #57578, #16065, #45486, #5888, #39468, #27765, #50409, #57199, #73423, #67771, #5147, #10425, #39099, #50777, #28886, #51905, #40583, #10793, #68137, #62102, #245, #33829, #45125, #73791, #69254, #46236, #22849, #22100, #63584, #68505, #11912, #28140, #57957, #51155, #39833, #62837, #74538, #45863, #63966, #64336, #29268, #17942, #59057, #12640, #6264, #35313, #19045, #65434, #70004, #70370, #18313, #58324, #2068, #13003, #13730, #71086, #7365, #65056, #12278, #30373, #47706, #6630, #41326, #53020, #42049, #13367, #52280, #53392, #35671, #70726, #1351, #64705, #23596, #616, #36406, #59419, #69628, #24335, #7732, #58686, #29635, #46605, #36041, #40958, #52648, #6995, #983, #23966, #46974, #30739, #53757, #19404, #30006, #47345, #18686, #25057, #41692, #1717, #24695, #48078, #42416, #36775, #37140, #49950, #26174, #60143, #20897, #49193, #67308, #32618, #54128, #14855, #71450, #37520, #14108, #72965, #31855, #15235, #9599, #72204, #2439, #48821, #8463, #55253, #21270, #54506, #66546, #31099, #31483, #71828, #8096, #15606, #25432, #43919, #66930, #2812, #60519, #48448, #44294, #3560, #32236, #19778, #61270, #37895, #42786, #26550, #26931, #20517, #20145, #14481, #60893, #3188, #49574, #72592, #9215, #59786, #8845, #43161, #43531, #55626, #54878, #38266, #65802, #3942, #25801, #66177, #61647, #15979, #67682, #51810, #34486, #62375, #28794, #39009, #46145, #16341, #44668, #5420, #9966, #69162, #38645, #28425, #39378, #45396, #16712, #57492, #4683, #23133, #27678, #21642, #39742, #33736, #11451, #51062, #57107, #10702, #62742, #32997, #56738, #51432, #68412, #74075, #10337, #5057, #22375, #62012, #11082, #33362, #55997, #22015, #56363, #157, #4311, #50684, #5797, #73703, #74444, #34109, #27301, #22751, #28053, #45041, #50317, #45774, #73338, #68786, #68050, #17095, #40117, #63123, #6168, #46518, #53303, #52192, #18957, #70280, #24240, #63497, #30649, #11819, #46889, #34856, #7275, #52555, #1979, #41961, #47615, #64969, #17471, #52930, #30282, #29913, #1261, #69537, #47253, #24971, #70638, #57862, #1627, #41238, #18592, #6538, #64244, #6902, #29177, #53667, #29544, #24607, #69913, #523, #13278, #35220, #36318, #47987, #41603, #59333, #64618, #23503, #40492, #58967, #7644, #17848, #12914, #894, #12554, #40865, #35949, #63871, #18223, #23880, #12183, #58240, #35582, #58596, #15147, #31766, #71000, #65346, #54037, #54414, #19316, #8005, #49103, #2721, #42328, #25342, #9127, #55540, #60051, #60428, #8372, #48356, #66844, #3097, #3850, #61183, #72115, #55164, #2348, #20428, #37806, #71362, #31388, #43068, #32144, #3470, #13647, #43444, #25709, #60802, #66084, #54785, #36686, #59697, #26459, #49483, #31012, #14394, #72502, #48730, #19688, #42697, #26082, #65710, #14014, #71736, #37051, #20052, #37428, #20811, #43829, #9513, #8755, #66459, #14768, #38179, #32528, #26846, #21556, #17010, #74356, #45316, #27213, #40036, #16255, #50230, #10995, #39294, #57399, #22666, #44209, #4970, #61559, #27589, #4225, #63039, #21924, #5339, #45685, #62294, #67222, #38923, #73251, #68331, #11364, #44583, #56655, #21184, #67595, #61924, #72879, #5707, #15518, #34028, #57026, #15892, #50599, #38558, #34398, #16628, #22292, #9880, #51346, #27972, #32908, #39663, #49861, #10623, #10250, #4595, #50976, #67962, #62661, #28338, #55913, #33277, #73619, #56276, #68700, #44955, #33649, #73990, #58881, #30196, #28706, #64160, #41515, #41153, #12467, #6080, #58511, #36232, #7191, #69, #64531, #52472, #35498, #17760, #808, #18137, #23049, #41880, #40774, #18506, #6459, #11733, #53213, #46435, #12829, #64892, #52842, #35864, #6817, #46060, #59248, #70198, #1546, #34773, #1174, #63782, #23796, #40410, #29829, #24526, #58151, #47532, #69079, #24153, #17385, #52108, #51720, #29088, #57776, #13193, #70557, #46799, #18873, #441, #63407, #29462, #23420, #69452, #12099 ),
 ( #35135, #69821, #47166, #20722, #25256, #49392, #36599, #20340, #31682, #47902, #3010, #8289, #30927, #72411, #37341, #15058, #60339, #24883, #53584, #48275, #25992, #70921, #59609, #43357, #42242, #9041, #8667, #14305, #1896, #66374, #54701, #19235, #49016, #31299, #53949, #43739, #72026, #38093, #14681, #65256, #13560, #71280, #37722, #7922, #2262, #60720, #19600, #32055, #55074, #3383, #42615, #66754, #65629, #36965, #13926, #26370, #59971, #7559, #30565, #54329, #2640, #25628, #42981, #48643, #19973, #66000, #71652, #16164, #69639, #17577, #32438, #23239, #10161, #44867, #50147, #33198, #50513, #55448, #628, #73163, #51918, #38839, #44124, #11923, #4142, #256, #23609, #10532, #69266, #67872, #3758, #17953, #28900, #40595, #67132, #34584, #21471, #56194, #72793, #73527, #63596, #15804, #34955, #26759, #57590, #49777, #9794, #9419, #38466, #15428, #46619, #57970, #4507, #52291, #61469, #61091, #61842, #32816, #46246, #21101, #55824, #27133, #6276, #27501, #39205, #62208, #29282, #44492, #67505, #21835, #5900, #42061, #36053, #13744, #53405, #59434, #41705, #65069, #40971, #64719, #7745, #70741, #1727, #12652, #59070, #24708, #64348, #47720, #41339, #58338, #24348, #46985, #54144, #2453, #58698, #8111, #70017, #18698, #18324, #30751, #12291, #48461, #71466, #53772, #13015, #19059, #13381, #59798, #7009, #25445, #30018, #23977, #36420, #7378, #36788, #2081, #25073, #30386, #48090, #63978, #71099, #19418, #42432, #65448, #35683, #31116, #35326, #53032, #6642, #1362, #29645, #47357, #70382, #52660, #996, #37532, #61661, #48834, #32632, #43932, #60158, #15246, #20533, #43174, #9980, #49589, #27313, #72606, #37156, #65815, #60533, #38280, #8477, #71840, #55640, #54518, #21284, #20912, #26566, #14122, #33011, #31496, #49209, #2824, #9612, #54890, #4324, #44307, #49963, #67322, #19791, #55269, #3956, #32251, #3574, #20157, #66942, #50329, #72978, #25814, #26945, #43546, #61285, #8859, #66561, #9229, #66190, #56012, #31868, #15619, #72218, #14494, #38659, #3201, #42799, #26189, #14870, #37909, #60906, #67695, #6184, #40134, #5813, #4697, #45790, #33749, #68426, #10351, #62757, #172, #28066, #28808, #15993, #22767, #39023, #22027, #21655, #50699, #27690, #11836, #69178, #22390, #63512, #73716, #29192, #45053, #68800, #56752, #16729, #33375, #11099, #23148, #51077, #51826, #62026, #17111, #56376, #68063, #44680, #16353, #39391, #34871, #17488, #45410, #57877, #62390, #73351, #74090, #10717, #63140, #5071, #39755, #34123, #11467, #57123, #5437, #51446, #40508, #28440, #74459, #34502, #57507, #46161, #47268, #24988, #64633, #70656, #52946, #1642, #52205, #1279, #18973, #7291, #12930, #23894, #70295, #35966, #908, #58986, #52571, #69552, #35597, #58253, #65364, #13663, #69927, #19335, #6554, #64988, #24623, #17863, #47633, #24256, #46903, #42347, #30299, #59714, #53318, #40880, #23519, #18237, #41977, #63886, #29560, #13297, #12197, #53686, #36335, #59350, #46534, #36703, #35234, #6919, #41252, #7661, #12569, #8023, #1998, #30667, #48005, #538, #71018, #64261, #58613, #29930, #18610, #41620, #38577, #61200, #2365, #66859, #54805, #14785, #20069, #3115, #20446, #25360, #44229, #43086, #20829, #8773, #14032, #55556, #48747, #43846, #67240, #55183, #38197, #37825, #48377, #61576, #72521, #9531, #15536, #31785, #66103, #15166, #8391, #32545, #3869, #49879, #66477, #31031, #71380, #37069, #14413, #54056, #42717, #9144, #37445, #19704, #60072, #26865, #65728, #60443, #43463, #26101, #31405, #72894, #60822, #54432, #21201, #32162, #2740, #25726, #3488, #71755, #49120, #72133, #26477, #49502, #17027, #9896, #11014, #39314, #51363, #4988, #68350, #27230, #4243, #22685, #40053, #73269, #27989, #68716, #21943, #61941, #32926, #16645, #55932, #50247, #62312, #67612, #21573, #10269, #63056, #11380, #88, #73636, #50617, #44599, #45703, #44971, #27607, #56294, #51739, #34415, #5354, #33295, #23066, #50994, #4610, #57417, #74005, #17401, #5724, #15908, #39678, #38940, #10638, #67977, #46075, #56672, #28723, #69094, #22308, #16272, #33667, #45333, #28355, #40424, #62677, #34047, #57042, #74374, #825, #11750, #19249, #34788, #24541, #70573, #17778, #41168, #57792, #24900, #58898, #35881, #456, #64905, #41531, #23435, #7209, #30579, #52858, #23813, #18153, #64547, #6833, #30211, #53230, #70214, #63423, #40790, #1562, #47917, #52487, #1190, #46815, #63797, #59264, #18523, #70936, #53601, #12843, #47549, #69468, #18890, #41896, #12115, #69840, #35513, #13211, #36249, #6100, #7575, #64179, #1913, #58526, #47182, #29105, #52124, #46450, #35153, #58169, #29847, #6474, #12483, #29478, #24171, #49031, #13578, #59624, #71667, #25272, #7939, #19617, #20737, #26383, #32454, #31315, #8305, #36614, #55093, #54342, #59988, #13941, #9437, #66769, #37736, #42632, #55464, #8681, #65644, #3399, #31696, #49793, #15073, #30944, #72039, #53966, #19986, #71297, #3773, #14322, #72429, #38107, #54718, #2277, #2653, #36983, #60735, #26775, #25643, #20356, #48290, #48658, #42995, #65272, #72808, #66015, #49408, #43755, #37355, #60354, #3025, #42260, #9057, #14696, #26008, #61107, #43373, #66389, #32071, #62970, #10548, #33212, #50529, #73918, #39222, #68261, #16556, #27894, #57328, #73545, #10178, #10921, #73179, #51278, #74287, #39965, #56585, #21116, #15446, #4158, #4522, #44139, #32831, #22222, #27518, #28639, #62590, #28271, #27146, #39594, #56209, #16180, #55841, #33581, #22597, #21852, #45618, #38482, #45249, #61485, #44509, #67151, #21488, #50163, #34327, #16941, #44883, #11295, #67520, #51654, #67888, #15818, #33956, #9809, #38853, #61858, #56954, #62222, #50904, #5270, #5639, #4898, #68632, #40705, #57704, #1108, #69752, #47468, #12400, #18438, #739, #24084, #6874, #23723, #41451, #29755, #35434, #46362, #18065, #58443, #23350, #6752, #368, #17313, #58079, #6011, #13126, #36161, #17688, #41813, #29014, #12763, #47092, #40333, #70131, #46727, #69378, #64824, #52770, #7491, #64464, #63336, #45991, #63709, #35795, #11661, #52031, #58810, #34696, #1477, #7121, #30129, #69006, #59182, #12033, #29396, #35067, #53144, #6390, #30495, #24460, #70491, #18809, #22985, #52404, #41081, #64091, #65930, #30863, #8594, #61022, #8971, #24820, #14612, #2569, #37274, #42548, #25557, #42910, #47833, #66681, #65560, #43291, #31233, #36532, #3313, #71211, #66306, #14985, #2939, #60649, #60268, #70855, #19167, #36900, #59542, #38022, #9347, #19530, #20652, #7858, #37650, #25927, #42169, #48944, #54258, #2193, #43668, #31608, #53515, #54630, #65182, #13493, #13855, #71954, #53882, #25189, #31984, #48203, #55008, #20268, #26300, #59908, #1832, #8222, #48571, #71581, #49324, #19903, #14235, #72339, #62505, #33868, #32366, #67808, #45164, #44795, #16100, #9725, #62139, #39874, #10833, #3690, #68175, #56125, #39135, #21398, #4434, #21768, #26686, #45527, #44421, #22137, #10093, #15360, #56868, #50077, #16472, #68543, #56495, #39509, #10462, #49709, #62876, #73830, #5184, #38395, #4812, #67436, #27428, #44051, #33492, #28180, #61776, #51192, #72722, #27808, #21026, #55755, #55380, #32747, #61399, #16847, #74201, #50443, #22506, #4071, #67061, #33130, #27064, #73092, #15734, #38773, #73460, #50819, #63622, #17978, #64005, #30043, #51946, #70406, #283, #68917, #12320, #6303, #58725, #23640, #29671, #11951, #35351, #11210, #34983, #52688, #40998, #46647, #57617, #29309, #69665, #34610, #58362, #11576, #17227, #1022, #57239, #18721, #41730, #24001, #57998, #6668, #47011, #53058, #23265, #34237, #46274, #40248, #70043, #52318, #7036, #18353, #41366, #654, #64375, #5550, #12676, #35709, #1390, #24376, #5927, #47382, #28554, #28929, #51560, #69294, #74577, #17604, #63250, #22891, #45903, #40622, #49891, #47742, #43858, #3501, #7403, #49515, #48115, #42084, #72905, #31138, #67253, #55195, #59095, #13040, #13407, #72533, #30410, #70766, #66870, #53429, #32557, #26489, #20840, #36077, #21213, #1752, #2104, #24733, #15178, #30775, #44240, #55567, #61212, #3881, #64741, #38209, #15548, #9544, #26876, #25098, #19081, #65096, #36445, #7771, #59457, #53795, #71123, #19445, #42457, #65473, #36811, #13767, #59821, #8135, #40612, #57989, #62867, #68164, #34973, #34227, #39865, #68534, #63995, #46636, #17594, #74191, #12310, #63240, #22496, #6293, #11566, #29662, #69656, #16463, #51936, #33859, #74569, #51183, #35342, #68908, #52309, #17969, #34600, #39500, #11200, #45518, #63614, #58354, #16838, #28920, #6659, #57229, #45154, #5541, #5175, #52678, #28543, #29299, #22129, #46265, #645, #5917, #62495, #10824, #11941, #23629, #28171, #69285, #51551, #17219, #56858, #57607, #40988, #22882, #45894, #40238, #274, #23256, #24365, #23992, #53049, #30033, #14137, #71481 ) ),
 .UNSPECIFIED., .F., .F., .F. ) 
 B_SPLINE_SURFACE_WITH_KNOTS ( ( 2, 2 ),
 ( 3, 2, 2, 2, 2, 2, 2, 2, 2, 2, 2, 2, 2, 2, 2, 2, 2, 2, 2, 2, 2, 2, 2, 2, 2, 2, 2, 2, 2, 2, 2, 2, 2, 2, 2, 2, 2, 2, 2, 2, 2, 2, 2, 2, 2, 2, 2, 2, 2, 2, 2, 2, 2, 2, 2, 2, 2, 2, 2, 2, 2, 2, 2, 2, 2, 2, 2, 2, 2, 2, 2, 2, 2, 2, 2, 2, 2, 2, 2, 2, 2, 2, 2, 2, 2, 2, 2, 2, 2, 2, 2, 2, 2, 2, 2, 2, 2, 2, 2, 2, 2, 2, 2, 2, 2, 2, 2, 2, 2, 2, 2, 2, 2, 2, 2, 2, 2, 2, 2, 2, 2, 2, 2, 2, 2, 2, 2, 2, 2, 2, 2, 2, 2, 2, 2, 2, 2, 2, 2, 2, 2, 2, 2, 2, 2, 2, 2, 2, 2, 2, 2, 2, 2, 2, 2, 2, 2, 2, 2, 2, 2, 2, 2, 2, 2, 2, 2, 2, 2, 2, 2, 2, 2, 2, 2, 2, 2, 2, 2, 2, 2, 2, 2, 2, 2, 2, 2, 2, 2, 2, 2, 2, 2, 2, 2, 2, 2, 2, 2, 2, 2, 2, 2, 2, 2, 2, 2, 2, 2, 2, 2, 2, 2, 2, 2, 2, 2, 2, 2, 2, 2, 2, 2, 2, 2, 2, 2, 2, 2, 2, 2, 2, 2, 2, 2, 2, 2, 2, 2, 2, 2, 2, 2, 2, 2, 2, 2, 2, 2, 2, 2, 2, 2, 2, 2, 2, 2, 2, 2, 2, 2, 2, 2, 2, 2, 2, 2, 2, 2, 2, 2, 2, 2, 2, 2, 2, 2, 2, 2, 2, 2, 2, 2, 2, 2, 2, 2, 2, 2, 2, 2, 2, 2, 2, 2, 2, 2, 2, 2, 2, 2, 2, 2, 2, 2, 2, 2, 2, 2, 2, 2, 2, 2, 2, 2, 2, 2, 2, 2, 2, 2, 2, 2, 2, 2, 2, 2, 2, 2, 2, 2, 2, 2, 2, 2, 2, 2, 2, 2, 2, 2, 2, 2, 2, 2, 2, 2, 2, 2, 2, 2, 2, 2, 2, 2, 2, 2, 2, 2, 2, 2, 2, 2, 2, 2, 2, 2, 2, 2, 2, 2, 2, 2, 2, 2, 2, 2, 2, 2, 2, 2, 2, 2, 2, 2, 2, 2, 2, 2, 2, 2, 2, 2, 2, 2, 2, 2, 2, 2, 2, 2, 2, 2, 2, 2, 2, 2, 2, 2, 2, 2, 2, 2, 2, 2, 2, 2, 2, 2, 2, 2, 2, 2, 2, 2, 2, 2, 2, 2, 2, 2, 2, 2, 2, 2, 2, 2, 2, 2, 2, 2, 2, 2, 2, 2, 2, 2, 2, 2, 2, 2, 2, 2, 2, 2, 2, 2, 2, 2, 2, 2, 2, 2, 2, 2, 2, 2, 2, 2, 2, 2, 2, 2, 2, 2, 2, 2, 2, 2, 2, 2, 2, 2, 2, 2, 2, 2, 2, 2, 2, 2, 2, 2, 2, 2, 2, 2, 2, 2, 2, 2, 2, 2, 2, 2, 2, 2, 2, 2, 2, 2, 2, 2, 2, 2, 2, 2, 2, 2, 2, 2, 2, 2, 2, 2, 2, 2, 2, 2, 2, 2, 2, 2, 2, 2, 2, 2, 2, 2, 2, 2, 2, 2, 3 ),
 ( 0.000000000000000000, 1.000000000000000000 ),
 ( 0.000000000000000000, 0.001811594202898550747, 0.003623188405797101493, 0.005434782608695652023, 0.007246376811594202987, 0.009057971014492753950, 0.01086956521739130405, 0.01268115942028985588, 0.01449275362318840597, 0.01630434782608695607, 0.01811594202898550790, 0.01992753623188405626, 0.02173913043478260809, 0.02355072463768115992, 0.02536231884057971175, 0.02717391304347826012, 0.02898550724637681195, 0.03079710144927536378, 0.03260869565217391214, 0.03442028985507246397, 0.03623188405797101580, 0.03804347826086956763, 0.03985507246376811252, 0.04166666666666666435, 0.04347826086956521618, 0.04528985507246376802, 0.04710144927536231985, 0.04891304347826087168, 0.05072463768115942351, 0.05253623188405796840, 0.05434782608695652023, 0.05615942028985507206, 0.05797101449275362389, 0.05978260869565217572, 0.06159420289855072755, 0.06340579710144927938, 0.06521739130434782428, 0.06702898550724638305, 0.06884057971014492794, 0.07065217391304347283, 0.07246376811594203160, 0.07427536231884057649, 0.07608695652173913526, 0.07789855072463768015, 0.07971014492753622505, 0.08152173913043478382, 0.08333333333333332871, 0.08514492753623188748, 0.08695652173913043237, 0.08876811594202899114, 0.09057971014492753603, 0.09239130434782608092, 0.09420289855072463969, 0.09601449275362318458, 0.09782608695652174335, 0.09963768115942028825, 0.1014492753623188470, 0.1032608695652173919, 0.1050724637681159368, 0.1068840579710144956, 0.1086956521739130405, 0.1105072463768115992, 0.1123188405797101441, 0.1141304347826086890, 0.1159420289855072478, 0.1177536231884057927, 0.1195652173913043514, 0.1213768115942028963, 0.1231884057971014551, 0.1250000000000000000, 0.1268115942028985588, 0.1286231884057970898, 0.1304347826086956486, 0.1322463768115942073, 0.1340579710144927661, 0.1358695652173912971, 0.1376811594202898559, 0.1394927536231884146, 0.1413043478260869457, 0.1431159420289855044, 0.1449275362318840632, 0.1467391304347826220, 0.1485507246376811530, 0.1503623188405797118, 0.1521739130434782705, 0.1539855072463768015, 0.1557971014492753603, 0.1576086956521739191, 0.1594202898550724501, 0.1612318840579710089, 0.1630434782608695676, 0.1648550724637681264, 0.1666666666666666574, 0.1684782608695652162, 0.1702898550724637750, 0.1721014492753623060, 0.1739130434782608647, 0.1757246376811594235, 0.1775362318840579823, 0.1793478260869565133, 0.1811594202898550721, 0.1829710144927536308, 0.1847826086956521618, 0.1865942028985507206, 0.1884057971014492794, 0.1902173913043478382, 0.1920289855072463692, 0.1938405797101449279, 0.1956521739130434867, 0.1974637681159420177, 0.1992753623188405765, 0.2010869565217391353, 0.2028985507246376940, 0.2047101449275362250, 0.2065217391304347838, 0.2083333333333333426, 0.2101449275362318736, 0.2119565217391304324, 0.2137681159420289911, 0.2155797101449275499, 0.2173913043478260809, 0.2192028985507246397, 0.2210144927536231985, 0.2228260869565217295, 0.2246376811594202882, 0.2264492753623188470, 0.2282608695652173780, 0.2300724637681159368, 0.2318840579710144956, 0.2336956521739130543, 0.2355072463768115854, 0.2373188405797101441, 0.2391304347826087029, 0.2409420289855072339, 0.2427536231884057927, 0.2445652173913043514, 0.2463768115942029102, 0.2481884057971014412, 0.2500000000000000000, 0.2518115942028985588, 0.2536231884057971175, 0.2554347826086956763, 0.2572463768115941796, 0.2590579710144927383, 0.2608695652173912971, 0.2626811594202898559, 0.2644927536231884146, 0.2663043478260869734, 0.2681159420289855322, 0.2699275362318840354, 0.2717391304347825942, 0.2735507246376811530, 0.2753623188405797118, 0.2771739130434782705, 0.2789855072463768293, 0.2807971014492753881, 0.2826086956521738913, 0.2844202898550724501, 0.2862318840579710089, 0.2880434782608695676, 0.2898550724637681264, 0.2916666666666666852, 0.2934782608695652439, 0.2952898550724637472, 0.2971014492753623060, 0.2989130434782608647, 0.3007246376811594235, 0.3025362318840579823, 0.3043478260869565410, 0.3061594202898550998, 0.3079710144927536031, 0.3097826086956521618, 0.3115942028985507206, 0.3134057971014492794, 0.3152173913043478382, 0.3170289855072463969, 0.3188405797101449002, 0.3206521739130434590, 0.3224637681159420177, 0.3242753623188405765, 0.3260869565217391353, 0.3278985507246376940, 0.3297101449275362528, 0.3315217391304347561, 0.3333333333333333148, 0.3351449275362318736, 0.3369565217391304324, 0.3387681159420289911, 0.3405797101449275499, 0.3423913043478261087, 0.3442028985507246119, 0.3460144927536231707, 0.3478260869565217295, 0.3496376811594202882, 0.3514492753623188470, 0.3532608695652174058, 0.3550724637681159646, 0.3568840579710144678, 0.3586956521739130266, 0.3605072463768115854, 0.3623188405797101441, 0.3641304347826087029, 0.3659420289855072617, 0.3677536231884058204, 0.3695652173913043237, 0.3713768115942028825, 0.3731884057971014412, 0.3750000000000000000, 0.3768115942028985588, 0.3786231884057971175, 0.3804347826086956763, 0.3822463768115941796, 0.3840579710144927383, 0.3858695652173912971, 0.3876811594202898559, 0.3894927536231884146, 0.3913043478260869734, 0.3931159420289855322, 0.3949275362318840354, 0.3967391304347825942, 0.3985507246376811530, 0.4003623188405797118, 0.4021739130434782705, 0.4039855072463768293, 0.4057971014492753881, 0.4076086956521738913, 0.4094202898550724501, 0.4112318840579710089, 0.4130434782608695676, 0.4148550724637681264, 0.4166666666666666852, 0.4184782608695652439, 0.4202898550724637472, 0.4221014492753623060, 0.4239130434782608647, 0.4257246376811594235, 0.4275362318840579823, 0.4293478260869565410, 0.4311594202898550998, 0.4329710144927536031, 0.4347826086956521618, 0.4365942028985507206, 0.4384057971014492794, 0.4402173913043478382, 0.4420289855072463969, 0.4438405797101449002, 0.4456521739130434590, 0.4474637681159420177, 0.4492753623188405765, 0.4510869565217391353, 0.4528985507246376940, 0.4547101449275362528, 0.4565217391304347561, 0.4583333333333333148, 0.4601449275362318736, 0.4619565217391304324, 0.4637681159420289911, 0.4655797101449275499, 0.4673913043478261087, 0.4692028985507246119, 0.4710144927536231707, 0.4728260869565217295, 0.4746376811594202882, 0.4764492753623188470, 0.4782608695652174058, 0.4800724637681159646, 0.4818840579710144678, 0.4836956521739130266, 0.4855072463768115854, 0.4873188405797101441, 0.4891304347826087029, 0.4909420289855072617, 0.4927536231884058204, 0.4945652173913043237, 0.4963768115942028825, 0.4981884057971014412, 0.5000000000000000000, 0.5018115942028985588, 0.5036231884057971175, 0.5054347826086956763, 0.5072463768115942351, 0.5090579710144927938, 0.5108695652173913526, 0.5126811594202898004, 0.5144927536231883591, 0.5163043478260869179, 0.5181159420289854767, 0.5199275362318840354, 0.5217391304347825942, 0.5235507246376811530, 0.5253623188405797118, 0.5271739130434782705, 0.5289855072463768293, 0.5307971014492753881, 0.5326086956521739468, 0.5344202898550725056, 0.5362318840579710644, 0.5380434782608695121, 0.5398550724637680709, 0.5416666666666666297, 0.5434782608695651884, 0.5452898550724637472, 0.5471014492753623060, 0.5489130434782608647, 0.5507246376811594235, 0.5525362318840579823, 0.5543478260869565410, 0.5561594202898550998, 0.5579710144927536586, 0.5597826086956522174, 0.5615942028985507761, 0.5634057971014492239, 0.5652173913043477826, 0.5670289855072463414, 0.5688405797101449002, 0.5706521739130434590, 0.5724637681159420177, 0.5742753623188405765, 0.5760869565217391353, 0.5778985507246376940, 0.5797101449275362528, 0.5815217391304348116, 0.5833333333333333703, 0.5851449275362319291, 0.5869565217391304879, 0.5887681159420289356, 0.5905797101449274944, 0.5923913043478260532, 0.5942028985507246119, 0.5960144927536231707, 0.5978260869565217295, 0.5996376811594202882, 0.6014492753623188470, 0.6032608695652174058, 0.6050724637681159646, 0.6068840579710145233, 0.6086956521739130821, 0.6105072463768116409, 0.6123188405797101996, 0.6141304347826086474, 0.6159420289855072062, 0.6177536231884057649, 0.6195652173913043237, 0.6213768115942028825, 0.6231884057971014412, 0.6250000000000000000, 0.6268115942028985588, 0.6286231884057971175, 0.6304347826086956763, 0.6322463768115942351, 0.6340579710144927938, 0.6358695652173913526, 0.6376811594202898004, 0.6394927536231883591, 0.6413043478260869179, 0.6431159420289854767, 0.6449275362318840354, 0.6467391304347825942, 0.6485507246376811530, 0.6503623188405797118, 0.6521739130434782705, 0.6539855072463768293, 0.6557971014492753881, 0.6576086956521739468, 0.6594202898550725056, 0.6612318840579710644, 0.6630434782608695121, 0.6648550724637680709, 0.6666666666666666297, 0.6684782608695651884, 0.6702898550724637472, 0.6721014492753623060, 0.6739130434782608647, 0.6757246376811594235, 0.6775362318840579823, 0.6793478260869565410, 0.6811594202898550998, 0.6829710144927536586, 0.6847826086956522174, 0.6865942028985507761, 0.6884057971014492239, 0.6902173913043477826, 0.6920289855072463414, 0.6938405797101449002, 0.6956521739130434590, 0.6974637681159420177, 0.6992753623188405765, 0.7010869565217391353, 0.7028985507246376940, 0.7047101449275362528, 0.7065217391304348116, 0.7083333333333333703, 0.7101449275362319291, 0.7119565217391304879, 0.7137681159420289356, 0.7155797101449274944, 0.7173913043478260532, 0.7192028985507246119, 0.7210144927536231707, 0.7228260869565217295, 0.7246376811594202882, 0.7264492753623188470, 0.7282608695652174058, 0.7300724637681159646, 0.7318840579710145233, 0.7336956521739130821, 0.7355072463768116409, 0.7373188405797101996, 0.7391304347826086474, 0.7409420289855072062, 0.7427536231884057649, 0.7445652173913043237, 0.7463768115942028825, 0.7481884057971014412, 0.7500000000000000000, 0.7518115942028985588, 0.7536231884057971175, 0.7554347826086956763, 0.7572463768115942351, 0.7590579710144927938, 0.7608695652173913526, 0.7626811594202898004, 0.7644927536231883591, 0.7663043478260869179, 0.7681159420289854767, 0.7699275362318840354, 0.7717391304347825942, 0.7735507246376811530, 0.7753623188405797118, 0.7771739130434782705, 0.7789855072463768293, 0.7807971014492753881, 0.7826086956521739468, 0.7844202898550725056, 0.7862318840579710644, 0.7880434782608695121, 0.7898550724637680709, 0.7916666666666666297, 0.7934782608695651884, 0.7952898550724637472, 0.7971014492753623060, 0.7989130434782608647, 0.8007246376811594235, 0.8025362318840579823, 0.8043478260869565410, 0.8061594202898550998, 0.8079710144927536586, 0.8097826086956522174, 0.8115942028985507761, 0.8134057971014492239, 0.8152173913043477826, 0.8170289855072463414, 0.8188405797101449002, 0.8206521739130434590, 0.8224637681159420177, 0.8242753623188405765, 0.8260869565217391353, 0.8278985507246376940, 0.8297101449275362528, 0.8315217391304348116, 0.8333333333333333703, 0.8351449275362319291, 0.8369565217391304879, 0.8387681159420289356, 0.8405797101449274944, 0.8423913043478260532, 0.8442028985507246119, 0.8460144927536231707, 0.8478260869565217295, 0.8496376811594202882, 0.8514492753623188470, 0.8532608695652174058, 0.8550724637681159646, 0.8568840579710145233, 0.8586956521739130821, 0.8605072463768116409, 0.8623188405797101996, 0.8641304347826086474, 0.8659420289855072062, 0.8677536231884057649, 0.8695652173913043237, 0.8713768115942028825, 0.8731884057971014412, 0.8750000000000000000, 0.8768115942028985588, 0.8786231884057971175, 0.8804347826086956763, 0.8822463768115942351, 0.8840579710144927938, 0.8858695652173913526, 0.8876811594202898004, 0.8894927536231883591, 0.8913043478260869179, 0.8931159420289854767, 0.8949275362318840354, 0.8967391304347825942, 0.8985507246376811530, 0.9003623188405797118, 0.9021739130434782705, 0.9039855072463768293, 0.9057971014492753881, 0.9076086956521739468, 0.9094202898550725056, 0.9112318840579710644, 0.9130434782608695121, 0.9148550724637680709, 0.9166666666666666297, 0.9184782608695651884, 0.9202898550724637472, 0.9221014492753623060, 0.9239130434782608647, 0.9257246376811594235, 0.9275362318840579823, 0.9293478260869565410, 0.9311594202898550998, 0.9329710144927536586, 0.9347826086956522174, 0.9365942028985507761, 0.9384057971014492239, 0.9402173913043477826, 0.9420289855072463414, 0.9438405797101449002, 0.9456521739130434590, 0.9474637681159420177, 0.9492753623188405765, 0.9510869565217391353, 0.9528985507246376940, 0.9547101449275362528, 0.9565217391304348116, 0.9583333333333333703, 0.9601449275362319291, 0.9619565217391304879, 0.9637681159420289356, 0.9655797101449274944, 0.9673913043478260532, 0.9692028985507246119, 0.9710144927536231707, 0.9728260869565217295, 0.9746376811594202882, 0.9764492753623188470, 0.9782608695652174058, 0.9800724637681159646, 0.9818840579710145233, 0.9826096977668656862 ),
 .UNSPECIFIED. ) 
 GEOMETRIC_REPRESENTATION_ITEM ( )  RATIONAL_B_SPLINE_SURFACE ( (
 ( 1.000000000000000000, 0.9659258262890683122, 1.000000000000000000, 0.9659258262890683122, 1.000000000000000000, 0.9659258262890683122, 1.000000000000000000, 0.9659258262890683122, 1.000000000000000000, 0.9659258262890683122, 1.000000000000000000, 0.9659258262890683122, 1.000000000000000000, 0.9659258262890683122, 1.000000000000000000, 0.9659258262890683122, 1.000000000000000000, 0.9659258262890683122, 1.000000000000000000, 0.9659258262890683122, 1.000000000000000000, 0.9659258262890683122, 1.000000000000000000, 0.9659258262890683122, 1.000000000000000000, 0.9659258262890683122, 1.000000000000000000, 0.9659258262890683122, 1.000000000000000000, 0.9659258262890683122, 1.000000000000000000, 0.9659258262890683122, 1.000000000000000000, 0.9659258262890683122, 1.000000000000000000, 0.9659258262890683122, 1.000000000000000000, 0.9659258262890683122, 1.000000000000000000, 0.9659258262890683122, 1.000000000000000000, 0.9659258262890683122, 1.000000000000000000, 0.9659258262890683122, 1.000000000000000000, 0.9659258262890683122, 1.000000000000000000, 0.9659258262890683122, 1.000000000000000000, 0.9659258262890683122, 1.000000000000000000, 0.9659258262890683122, 1.000000000000000000, 0.9659258262890683122, 1.000000000000000000, 0.9659258262890683122, 1.000000000000000000, 0.9659258262890683122, 1.000000000000000000, 0.9659258262890683122, 1.000000000000000000, 0.9659258262890683122, 1.000000000000000000, 0.9659258262890683122, 1.000000000000000000, 0.9659258262890683122, 1.000000000000000000, 0.9659258262890683122, 1.000000000000000000, 0.9659258262890683122, 1.000000000000000000, 0.9659258262890683122, 1.000000000000000000, 0.9659258262890683122, 1.000000000000000000, 0.9659258262890683122, 1.000000000000000000, 0.9659258262890683122, 1.000000000000000000, 0.9659258262890683122, 1.000000000000000000, 0.9659258262890683122, 1.000000000000000000, 0.9659258262890683122, 1.000000000000000000, 0.9659258262890683122, 1.000000000000000000, 0.9659258262890683122, 1.000000000000000000, 0.9659258262890683122, 1.000000000000000000, 0.9659258262890683122, 1.000000000000000000, 0.9659258262890683122, 1.000000000000000000, 0.9659258262890683122, 1.000000000000000000, 0.9659258262890683122, 1.000000000000000000, 0.9659258262890683122, 1.000000000000000000, 0.9659258262890683122, 1.000000000000000000, 0.9659258262890683122, 1.000000000000000000, 0.9659258262890683122, 1.000000000000000000, 0.9659258262890683122, 1.000000000000000000, 0.9659258262890683122, 1.000000000000000000, 0.9659258262890683122, 1.000000000000000000, 0.9659258262890683122, 1.000000000000000000, 0.9659258262890683122, 1.000000000000000000, 0.9659258262890683122, 1.000000000000000000, 0.9659258262890683122, 1.000000000000000000, 0.9659258262890683122, 1.000000000000000000, 0.9659258262890683122, 1.000000000000000000, 0.9659258262890683122, 1.000000000000000000, 0.9659258262890683122, 1.000000000000000000, 0.9659258262890683122, 1.000000000000000000, 0.9659258262890683122, 1.000000000000000000, 0.9659258262890683122, 1.000000000000000000, 0.9659258262890683122, 1.000000000000000000, 0.9659258262890683122, 1.000000000000000000, 0.9659258262890683122, 1.000000000000000000, 0.9659258262890683122, 1.000000000000000000, 0.9659258262890683122, 1.000000000000000000, 0.9659258262890683122, 1.000000000000000000, 0.9659258262890683122, 1.000000000000000000, 0.9659258262890683122, 1.000000000000000000, 0.9659258262890683122, 1.000000000000000000, 0.9659258262890683122, 1.000000000000000000, 0.9659258262890683122, 1.000000000000000000, 0.9659258262890683122, 1.000000000000000000, 0.9659258262890683122, 1.000000000000000000, 0.9659258262890683122, 1.000000000000000000, 0.9659258262890683122, 1.000000000000000000, 0.9659258262890683122, 1.000000000000000000, 0.9659258262890683122, 1.000000000000000000, 0.9659258262890683122, 1.000000000000000000, 0.9659258262890683122, 1.000000000000000000, 0.9659258262890683122, 1.000000000000000000, 0.9659258262890683122, 1.000000000000000000, 0.9659258262890683122, 1.000000000000000000, 0.9659258262890683122, 1.000000000000000000, 0.9659258262890683122, 1.000000000000000000, 0.9659258262890683122, 1.000000000000000000, 0.9659258262890683122, 1.000000000000000000, 0.9659258262890683122, 1.000000000000000000, 0.9659258262890683122, 1.000000000000000000, 0.9659258262890683122, 1.000000000000000000, 0.9659258262890683122, 1.000000000000000000, 0.9659258262890683122, 1.000000000000000000, 0.9659258262890683122, 1.000000000000000000, 0.9659258262890683122, 1.000000000000000000, 0.9659258262890683122, 1.000000000000000000, 0.9659258262890683122, 1.000000000000000000, 0.9659258262890683122, 1.000000000000000000, 0.9659258262890683122, 1.000000000000000000, 0.9659258262890683122, 1.000000000000000000, 0.9659258262890683122, 1.000000000000000000, 0.9659258262890683122, 1.000000000000000000, 0.9659258262890683122, 1.000000000000000000, 0.9659258262890683122, 1.000000000000000000, 0.9659258262890683122, 1.000000000000000000, 0.9659258262890683122, 1.000000000000000000, 0.9659258262890683122, 1.000000000000000000, 0.9659258262890683122, 1.000000000000000000, 0.9659258262890683122, 1.000000000000000000, 0.9659258262890683122, 1.000000000000000000, 0.9659258262890683122, 1.000000000000000000, 0.9659258262890683122, 1.000000000000000000, 0.9659258262890683122, 1.000000000000000000, 0.9659258262890683122, 1.000000000000000000, 0.9659258262890683122, 1.000000000000000000, 0.9659258262890683122, 1.000000000000000000, 0.9659258262890683122, 1.000000000000000000, 0.9659258262890683122, 1.000000000000000000, 0.9659258262890683122, 1.000000000000000000, 0.9659258262890683122, 1.000000000000000000, 0.9659258262890683122, 1.000000000000000000, 0.9659258262890683122, 1.000000000000000000, 0.9659258262890683122, 1.000000000000000000, 0.9659258262890683122, 1.000000000000000000, 0.9659258262890683122, 1.000000000000000000, 0.9659258262890683122, 1.000000000000000000, 0.9659258262890683122, 1.000000000000000000, 0.9659258262890683122, 1.000000000000000000, 0.9659258262890683122, 1.000000000000000000, 0.9659258262890683122, 1.000000000000000000, 0.9659258262890683122, 1.000000000000000000, 0.9659258262890683122, 1.000000000000000000, 0.9659258262890683122, 1.000000000000000000, 0.9659258262890683122, 1.000000000000000000, 0.9659258262890683122, 1.000000000000000000, 0.9659258262890683122, 1.000000000000000000, 0.9659258262890683122, 1.000000000000000000, 0.9659258262890683122, 1.000000000000000000, 0.9659258262890683122, 1.000000000000000000, 0.9659258262890683122, 1.000000000000000000, 0.9659258262890683122, 1.000000000000000000, 0.9659258262890683122, 1.000000000000000000, 0.9659258262890683122, 1.000000000000000000, 0.9659258262890683122, 1.000000000000000000, 0.9659258262890683122, 1.000000000000000000, 0.9659258262890683122, 1.000000000000000000, 0.9659258262890683122, 1.000000000000000000, 0.9659258262890683122, 1.000000000000000000, 0.9659258262890683122, 1.000000000000000000, 0.9659258262890683122, 1.000000000000000000, 0.9659258262890683122, 1.000000000000000000, 0.9659258262890683122, 1.000000000000000000, 0.9659258262890683122, 1.000000000000000000, 0.9659258262890683122, 1.000000000000000000, 0.9659258262890683122, 1.000000000000000000, 0.9659258262890683122, 1.000000000000000000, 0.9659258262890683122, 1.000000000000000000, 0.9659258262890683122, 1.000000000000000000, 0.9659258262890683122, 1.000000000000000000, 0.9659258262890683122, 1.000000000000000000, 0.9659258262890683122, 1.000000000000000000, 0.9659258262890683122, 1.000000000000000000, 0.9659258262890683122, 1.000000000000000000, 0.9659258262890683122, 1.000000000000000000, 0.9659258262890683122, 1.000000000000000000, 0.9659258262890683122, 1.000000000000000000, 0.9659258262890683122, 1.000000000000000000, 0.9659258262890683122, 1.000000000000000000, 0.9659258262890683122, 1.000000000000000000, 0.9659258262890683122, 1.000000000000000000, 0.9659258262890683122, 1.000000000000000000, 0.9659258262890683122, 1.000000000000000000, 0.9659258262890683122, 1.000000000000000000, 0.9659258262890683122, 1.000000000000000000, 0.9659258262890683122, 1.000000000000000000, 0.9659258262890683122, 1.000000000000000000, 0.9659258262890683122, 1.000000000000000000, 0.9659258262890683122, 1.000000000000000000, 0.9659258262890683122, 1.000000000000000000, 0.9659258262890683122, 1.000000000000000000, 0.9659258262890683122, 1.000000000000000000, 0.9659258262890683122, 1.000000000000000000, 0.9659258262890683122, 1.000000000000000000, 0.9659258262890683122, 1.000000000000000000, 0.9659258262890683122, 1.000000000000000000, 0.9659258262890683122, 1.000000000000000000, 0.9659258262890683122, 1.000000000000000000, 0.9659258262890683122, 1.000000000000000000, 0.9659258262890683122, 1.000000000000000000, 0.9659258262890683122, 1.000000000000000000, 0.9659258262890683122, 1.000000000000000000, 0.9659258262890683122, 1.000000000000000000, 0.9659258262890683122, 1.000000000000000000, 0.9659258262890683122, 1.000000000000000000, 0.9659258262890683122, 1.000000000000000000, 0.9659258262890683122, 1.000000000000000000, 0.9659258262890683122, 1.000000000000000000, 0.9659258262890683122, 1.000000000000000000, 0.9659258262890683122, 1.000000000000000000, 0.9659258262890683122, 1.000000000000000000, 0.9659258262890683122, 1.000000000000000000, 0.9659258262890683122, 1.000000000000000000, 0.9659258262890683122, 1.000000000000000000, 0.9659258262890683122, 1.000000000000000000, 0.9659258262890683122, 1.000000000000000000, 0.9659258262890683122, 1.000000000000000000, 0.9659258262890683122, 1.000000000000000000, 0.9659258262890683122, 1.000000000000000000, 0.9659258262890683122, 1.000000000000000000, 0.9659258262890683122, 1.000000000000000000, 0.9659258262890683122, 1.000000000000000000, 0.9659258262890683122, 1.000000000000000000, 0.9659258262890683122, 1.000000000000000000, 0.9659258262890683122, 1.000000000000000000, 0.9659258262890683122, 1.000000000000000000, 0.9659258262890683122, 1.000000000000000000, 0.9659258262890683122, 1.000000000000000000, 0.9659258262890683122, 1.000000000000000000, 0.9659258262890683122, 1.000000000000000000, 0.9659258262890683122, 1.000000000000000000, 0.9659258262890683122, 1.000000000000000000, 0.9659258262890683122, 1.000000000000000000, 0.9659258262890683122, 1.000000000000000000, 0.9659258262890683122, 1.000000000000000000, 0.9659258262890683122, 1.000000000000000000, 0.9659258262890683122, 1.000000000000000000, 0.9659258262890683122, 1.000000000000000000, 0.9659258262890683122, 1.000000000000000000, 0.9659258262890683122, 1.000000000000000000, 0.9659258262890683122, 1.000000000000000000, 0.9659258262890683122, 1.000000000000000000, 0.9659258262890683122, 1.000000000000000000, 0.9659258262890683122, 1.000000000000000000, 0.9659258262890683122, 1.000000000000000000, 0.9659258262890683122, 1.000000000000000000, 0.9659258262890683122, 1.000000000000000000, 0.9659258262890683122, 1.000000000000000000, 0.9659258262890683122, 1.000000000000000000, 0.9659258262890683122, 1.000000000000000000, 0.9659258262890683122, 1.000000000000000000, 0.9659258262890683122, 1.000000000000000000, 0.9659258262890683122, 1.000000000000000000, 0.9659258262890683122, 1.000000000000000000, 0.9659258262890683122, 1.000000000000000000, 0.9659258262890683122, 1.000000000000000000, 0.9659258262890683122, 1.000000000000000000, 0.9659258262890683122, 1.000000000000000000, 0.9659258262890683122, 1.000000000000000000, 0.9659258262890683122, 1.000000000000000000, 0.9659258262890683122, 1.000000000000000000, 0.9659258262890683122, 1.000000000000000000, 0.9659258262890683122, 1.000000000000000000, 0.9659258262890683122, 1.000000000000000000, 0.9659258262890683122, 1.000000000000000000, 0.9659258262890683122, 1.000000000000000000, 0.9659258262890683122, 1.000000000000000000, 0.9659258262890683122, 1.000000000000000000, 0.9659258262890683122, 1.000000000000000000, 0.9659258262890683122, 1.000000000000000000, 0.9659258262890683122, 1.000000000000000000, 0.9659258262890683122, 1.000000000000000000, 0.9659258262890683122, 1.000000000000000000, 0.9659258262890683122, 1.000000000000000000, 0.9659258262890683122, 1.000000000000000000, 0.9659258262890683122, 1.000000000000000000, 0.9659258262890683122, 1.000000000000000000, 0.9659258262890683122, 1.000000000000000000, 0.9659258262890683122, 1.000000000000000000, 0.9659258262890683122, 1.000000000000000000, 0.9659258262890683122, 1.000000000000000000, 0.9659258262890683122, 1.000000000000000000, 0.9659258262890683122, 1.000000000000000000, 0.9659258262890683122, 1.000000000000000000, 0.9659258262890683122, 1.000000000000000000, 0.9659258262890683122, 1.000000000000000000, 0.9659258262890683122, 1.000000000000000000, 0.9659258262890683122, 1.000000000000000000, 0.9659258262890683122, 1.000000000000000000, 0.9659258262890683122, 1.000000000000000000, 0.9659258262890683122, 1.000000000000000000, 0.9659258262890683122, 1.000000000000000000, 0.9659258262890683122, 1.000000000000000000, 0.9659258262890683122, 1.000000000000000000, 0.9659258262890683122, 1.000000000000000000, 0.9659258262890683122, 1.000000000000000000, 0.9659258262890683122, 1.000000000000000000, 0.9659258262890683122, 1.000000000000000000, 0.9659258262890683122, 1.000000000000000000, 0.9659258262890683122, 1.000000000000000000, 0.9659258262890683122, 1.000000000000000000, 0.9659258262890683122, 1.000000000000000000, 0.9659258262890683122, 1.000000000000000000, 0.9659258262890683122, 1.000000000000000000, 0.9659258262890683122, 1.000000000000000000, 0.9659258262890683122, 1.000000000000000000, 0.9659258262890683122, 1.000000000000000000, 0.9659258262890683122, 1.000000000000000000, 0.9659258262890683122, 1.000000000000000000, 0.9659258262890683122, 1.000000000000000000, 0.9659258262890683122, 1.000000000000000000, 0.9659258262890683122, 1.000000000000000000, 0.9659258262890683122, 1.000000000000000000, 0.9659258262890683122, 1.000000000000000000, 0.9659258262890683122, 1.000000000000000000, 0.9659258262890683122, 1.000000000000000000, 0.9659258262890683122, 1.000000000000000000, 0.9659258262890683122, 1.000000000000000000, 0.9659258262890683122, 1.000000000000000000, 0.9659258262890683122, 1.000000000000000000, 0.9659258262890683122, 1.000000000000000000, 0.9659258262890683122, 1.000000000000000000, 0.9659258262890683122, 1.000000000000000000, 0.9659258262890683122, 1.000000000000000000, 0.9659258262890683122, 1.000000000000000000, 0.9659258262890683122, 1.000000000000000000, 0.9659258262890683122, 1.000000000000000000, 0.9659258262890683122, 1.000000000000000000, 0.9659258262890683122, 1.000000000000000000, 0.9659258262890683122, 1.000000000000000000, 0.9659258262890683122, 1.000000000000000000, 0.9659258262890683122, 1.000000000000000000, 0.9659258262890683122, 1.000000000000000000, 0.9659258262890683122, 1.000000000000000000, 0.9659258262890683122, 1.000000000000000000, 0.9659258262890683122, 1.000000000000000000, 0.9659258262890683122, 1.000000000000000000, 0.9659258262890683122, 1.000000000000000000, 0.9659258262890683122, 1.000000000000000000, 0.9659258262890683122, 1.000000000000000000, 0.9659258262890683122, 1.000000000000000000, 0.9659258262890683122, 1.000000000000000000, 0.9659258262890683122, 1.000000000000000000, 0.9659258262890683122, 1.000000000000000000, 0.9659258262890683122, 1.000000000000000000, 0.9659258262890683122, 1.000000000000000000, 0.9659258262890683122, 1.000000000000000000, 0.9659258262890683122, 1.000000000000000000, 0.9659258262890683122, 1.000000000000000000, 0.9659258262890683122, 1.000000000000000000, 0.9659258262890683122, 1.000000000000000000, 0.9659258262890683122, 1.000000000000000000, 0.9659258262890683122, 1.000000000000000000, 0.9659258262890683122, 1.000000000000000000, 0.9659258262890683122, 1.000000000000000000, 0.9659258262890683122, 1.000000000000000000, 0.9659258262890683122, 1.000000000000000000, 0.9659258262890683122, 1.000000000000000000, 0.9659258262890683122, 1.000000000000000000, 0.9659258262890683122, 1.000000000000000000, 0.9659258262890683122, 1.000000000000000000, 0.9659258262890683122, 1.000000000000000000, 0.9659258262890683122, 1.000000000000000000, 0.9659258262890683122, 1.000000000000000000, 0.9659258262890683122, 1.000000000000000000, 0.9659258262890683122, 1.000000000000000000, 0.9659258262890683122, 1.000000000000000000, 0.9659258262890683122, 1.000000000000000000, 0.9659258262890683122, 1.000000000000000000, 0.9659258262890683122, 1.000000000000000000, 0.9659258262890683122, 1.000000000000000000, 0.9659258262890683122, 1.000000000000000000, 0.9659258262890683122, 1.000000000000000000, 0.9659258262890683122, 1.000000000000000000, 0.9659258262890683122, 1.000000000000000000, 0.9659258262890683122, 1.000000000000000000, 0.9659258262890683122, 1.000000000000000000, 0.9659258262890683122, 1.000000000000000000, 0.9659258262890683122, 1.000000000000000000, 0.9659258262890683122, 1.000000000000000000, 0.9659258262890683122, 1.000000000000000000, 0.9659258262890683122, 1.000000000000000000, 0.9659258262890683122, 1.000000000000000000, 0.9659258262890683122, 1.000000000000000000, 0.9659258262890683122, 1.000000000000000000, 0.9659258262890683122, 1.000000000000000000, 0.9659258262890683122, 1.000000000000000000, 0.9659258262890683122, 1.000000000000000000, 0.9659258262890683122, 1.000000000000000000, 0.9659258262890683122, 1.000000000000000000, 0.9659258262890683122, 1.000000000000000000, 0.9659258262890683122, 1.000000000000000000, 0.9659258262890683122, 1.000000000000000000, 0.9659258262890683122, 1.000000000000000000, 0.9659258262890683122, 1.000000000000000000, 0.9659258262890683122, 1.000000000000000000, 0.9659258262890683122, 1.000000000000000000, 0.9659258262890683122, 1.000000000000000000, 0.9659258262890683122, 1.000000000000000000, 0.9659258262890683122, 1.000000000000000000, 0.9659258262890683122, 1.000000000000000000, 0.9659258262890683122, 1.000000000000000000, 0.9659258262890683122, 1.000000000000000000, 0.9659258262890683122, 1.000000000000000000, 0.9659258262890683122, 1.000000000000000000, 0.9659258262890683122, 1.000000000000000000, 0.9659258262890683122, 1.000000000000000000, 0.9659258262890683122, 1.000000000000000000, 0.9659258262890683122, 1.000000000000000000, 0.9659258262890683122, 1.000000000000000000, 0.9659258262890683122, 1.000000000000000000, 0.9659258262890683122, 1.000000000000000000, 0.9659258262890683122, 1.000000000000000000, 0.9659258262890683122, 1.000000000000000000, 0.9659258262890683122, 1.000000000000000000, 0.9659258262890683122, 1.000000000000000000, 0.9659258262890683122, 1.000000000000000000, 0.9659258262890683122, 1.000000000000000000, 0.9659258262890683122, 1.000000000000000000, 0.9659258262890683122, 1.000000000000000000, 0.9659258262890683122, 1.000000000000000000, 0.9659258262890683122, 1.000000000000000000, 0.9659258262890683122, 1.000000000000000000, 0.9659258262890683122, 1.000000000000000000, 0.9659258262890683122, 1.000000000000000000, 0.9659258262890683122, 1.000000000000000000, 0.9659258262890683122, 1.000000000000000000, 0.9659258262890683122, 1.000000000000000000, 0.9659258262890683122, 1.000000000000000000, 0.9659258262890683122, 1.000000000000000000, 0.9659258262890683122, 1.000000000000000000, 0.9659258262890683122, 1.000000000000000000, 0.9659258262890683122, 1.000000000000000000, 0.9659258262890683122, 1.000000000000000000, 0.9659258262890683122, 1.000000000000000000, 0.9659258262890683122, 1.000000000000000000, 0.9659258262890683122, 1.000000000000000000, 0.9659258262890683122, 1.000000000000000000, 0.9659258262890683122, 1.000000000000000000, 0.9659258262890683122, 1.000000000000000000, 0.9659258262890683122, 1.000000000000000000, 0.9659258262890683122, 1.000000000000000000, 0.9659258262890683122, 1.000000000000000000, 0.9659258262890683122, 1.000000000000000000, 0.9659258262890683122, 1.000000000000000000, 0.9659258262890683122, 1.000000000000000000, 0.9659258262890683122, 1.000000000000000000, 0.9659258262890683122, 1.000000000000000000, 0.9659258262890683122, 1.000000000000000000, 0.9659258262890683122, 1.000000000000000000, 0.9659258262890683122, 1.000000000000000000, 0.9659258262890683122, 1.000000000000000000, 0.9659258262890683122, 1.000000000000000000, 0.9659258262890683122, 1.000000000000000000, 0.9659258262890683122, 1.000000000000000000, 0.9659258262890683122, 1.000000000000000000, 0.9659258262890683122, 1.000000000000000000, 0.9659258262890683122, 1.000000000000000000, 0.9659258262890683122, 1.000000000000000000, 0.9659258262890683122, 1.000000000000000000, 0.9659258262890683122, 1.000000000000000000, 0.9659258262890683122, 1.000000000000000000, 0.9659258262890683122, 1.000000000000000000, 0.9659258262890683122, 1.000000000000000000, 0.9659258262890683122, 1.000000000000000000, 0.9659258262890683122, 1.000000000000000000, 0.9659258262890683122, 1.000000000000000000, 0.9659258262890683122, 1.000000000000000000, 0.9659258262890683122, 1.000000000000000000, 0.9659258262890683122, 1.000000000000000000, 0.9659258262890683122, 1.000000000000000000, 0.9659258262890683122, 1.000000000000000000, 0.9659258262890683122, 1.000000000000000000, 0.9659258262890683122, 1.000000000000000000, 0.9659258262890683122, 1.000000000000000000, 0.9659258262890683122, 1.000000000000000000, 0.9659258262890683122, 1.000000000000000000, 0.9659258262890683122, 1.000000000000000000, 0.9659258262890683122, 1.000000000000000000, 0.9659258262890683122, 1.000000000000000000, 0.9659258262890683122, 1.000000000000000000, 0.9659258262890683122, 1.000000000000000000, 0.9659258262890683122, 1.000000000000000000, 0.9659258262890683122, 1.000000000000000000, 0.9659258262890683122, 1.000000000000000000, 0.9659258262890683122, 1.000000000000000000, 0.9659258262890683122, 1.000000000000000000, 0.9659258262890683122, 1.000000000000000000, 0.9659258262890683122, 1.000000000000000000, 0.9659258262890683122, 1.000000000000000000, 0.9659258262890683122, 1.000000000000000000, 0.9659258262890683122, 1.000000000000000000, 0.9659258262890683122, 1.000000000000000000, 0.9659258262890683122, 1.000000000000000000, 0.9659258262890683122, 1.000000000000000000, 0.9659258262890683122, 1.000000000000000000, 0.9659258262890683122, 1.000000000000000000, 0.9659258262890683122, 1.000000000000000000, 0.9659258262890683122, 1.000000000000000000, 0.9659258262890683122, 1.000000000000000000, 0.9659258262890683122, 1.000000000000000000, 0.9659258262890683122, 1.000000000000000000, 0.9659258262890683122, 1.000000000000000000, 0.9659258262890683122, 1.000000000000000000, 0.9659258262890683122, 1.000000000000000000, 0.9659258262890683122, 1.000000000000000000, 0.9659258262890683122, 1.000000000000000000, 0.9659258262890683122, 1.000000000000000000, 0.9659258262890683122, 1.000000000000000000, 0.9659258262890683122, 1.000000000000000000, 0.9659258262890683122, 1.000000000000000000, 0.9659258262890683122, 1.000000000000000000, 0.9659258262890683122, 1.000000000000000000, 0.9659258262890683122, 1.000000000000000000, 0.9659258262890683122, 1.000000000000000000, 0.9659258262890683122, 1.000000000000000000, 0.9659258262890683122, 1.000000000000000000, 0.9659258262890683122, 1.000000000000000000, 0.9659258262890683122, 1.000000000000000000, 0.9659258262890683122, 1.000000000000000000, 0.9659258262890683122, 1.000000000000000000, 0.9659258262890683122, 1.000000000000000000, 0.9659258262890683122, 1.000000000000000000, 0.9659258262890683122, 1.000000000000000000, 0.9659258262890683122, 1.000000000000000000, 0.9659258262890683122, 1.000000000000000000, 0.9659258262890683122, 1.000000000000000000, 0.9659258262890683122, 1.000000000000000000, 0.9659258262890683122, 1.000000000000000000, 0.9659258262890683122, 1.000000000000000000, 0.9659258262890683122, 1.000000000000000000, 0.9659258262890683122, 1.000000000000000000, 0.9659258262890683122, 1.000000000000000000, 0.9659258262890683122, 1.000000000000000000, 0.9659258262890683122, 1.000000000000000000, 0.9659258262890683122, 1.000000000000000000, 0.9659258262890683122, 1.000000000000000000, 0.9659258262890683122, 1.000000000000000000, 0.9659258262890683122, 1.000000000000000000, 0.9659258262890683122, 1.000000000000000000, 0.9659258262890683122, 1.000000000000000000, 0.9659258262890683122, 1.000000000000000000, 0.9659258262890683122, 1.000000000000000000, 0.9659258262890683122, 1.000000000000000000, 0.9659258262890683122, 1.000000000000000000, 0.9659258262890683122, 1.000000000000000000, 0.9659258262890683122, 1.000000000000000000, 0.9659258262890683122, 1.000000000000000000, 0.9863514817966205772, 0.9836368779841404564),
 ( 1.000000000000000000, 0.9659258262890683122, 1.000000000000000000, 0.9659258262890683122, 1.000000000000000000, 0.9659258262890683122, 1.000000000000000000, 0.9659258262890683122, 1.000000000000000000, 0.9659258262890683122, 1.000000000000000000, 0.9659258262890683122, 1.000000000000000000, 0.9659258262890683122, 1.000000000000000000, 0.9659258262890683122, 1.000000000000000000, 0.9659258262890683122, 1.000000000000000000, 0.9659258262890683122, 1.000000000000000000, 0.9659258262890683122, 1.000000000000000000, 0.9659258262890683122, 1.000000000000000000, 0.9659258262890683122, 1.000000000000000000, 0.9659258262890683122, 1.000000000000000000, 0.9659258262890683122, 1.000000000000000000, 0.9659258262890683122, 1.000000000000000000, 0.9659258262890683122, 1.000000000000000000, 0.9659258262890683122, 1.000000000000000000, 0.9659258262890683122, 1.000000000000000000, 0.9659258262890683122, 1.000000000000000000, 0.9659258262890683122, 1.000000000000000000, 0.9659258262890683122, 1.000000000000000000, 0.9659258262890683122, 1.000000000000000000, 0.9659258262890683122, 1.000000000000000000, 0.9659258262890683122, 1.000000000000000000, 0.9659258262890683122, 1.000000000000000000, 0.9659258262890683122, 1.000000000000000000, 0.9659258262890683122, 1.000000000000000000, 0.9659258262890683122, 1.000000000000000000, 0.9659258262890683122, 1.000000000000000000, 0.9659258262890683122, 1.000000000000000000, 0.9659258262890683122, 1.000000000000000000, 0.9659258262890683122, 1.000000000000000000, 0.9659258262890683122, 1.000000000000000000, 0.9659258262890683122, 1.000000000000000000, 0.9659258262890683122, 1.000000000000000000, 0.9659258262890683122, 1.000000000000000000, 0.9659258262890683122, 1.000000000000000000, 0.9659258262890683122, 1.000000000000000000, 0.9659258262890683122, 1.000000000000000000, 0.9659258262890683122, 1.000000000000000000, 0.9659258262890683122, 1.000000000000000000, 0.9659258262890683122, 1.000000000000000000, 0.9659258262890683122, 1.000000000000000000, 0.9659258262890683122, 1.000000000000000000, 0.9659258262890683122, 1.000000000000000000, 0.9659258262890683122, 1.000000000000000000, 0.9659258262890683122, 1.000000000000000000, 0.9659258262890683122, 1.000000000000000000, 0.9659258262890683122, 1.000000000000000000, 0.9659258262890683122, 1.000000000000000000, 0.9659258262890683122, 1.000000000000000000, 0.9659258262890683122, 1.000000000000000000, 0.9659258262890683122, 1.000000000000000000, 0.9659258262890683122, 1.000000000000000000, 0.9659258262890683122, 1.000000000000000000, 0.9659258262890683122, 1.000000000000000000, 0.9659258262890683122, 1.000000000000000000, 0.9659258262890683122, 1.000000000000000000, 0.9659258262890683122, 1.000000000000000000, 0.9659258262890683122, 1.000000000000000000, 0.9659258262890683122, 1.000000000000000000, 0.9659258262890683122, 1.000000000000000000, 0.9659258262890683122, 1.000000000000000000, 0.9659258262890683122, 1.000000000000000000, 0.9659258262890683122, 1.000000000000000000, 0.9659258262890683122, 1.000000000000000000, 0.9659258262890683122, 1.000000000000000000, 0.9659258262890683122, 1.000000000000000000, 0.9659258262890683122, 1.000000000000000000, 0.9659258262890683122, 1.000000000000000000, 0.9659258262890683122, 1.000000000000000000, 0.9659258262890683122, 1.000000000000000000, 0.9659258262890683122, 1.000000000000000000, 0.9659258262890683122, 1.000000000000000000, 0.9659258262890683122, 1.000000000000000000, 0.9659258262890683122, 1.000000000000000000, 0.9659258262890683122, 1.000000000000000000, 0.9659258262890683122, 1.000000000000000000, 0.9659258262890683122, 1.000000000000000000, 0.9659258262890683122, 1.000000000000000000, 0.9659258262890683122, 1.000000000000000000, 0.9659258262890683122, 1.000000000000000000, 0.9659258262890683122, 1.000000000000000000, 0.9659258262890683122, 1.000000000000000000, 0.9659258262890683122, 1.000000000000000000, 0.9659258262890683122, 1.000000000000000000, 0.9659258262890683122, 1.000000000000000000, 0.9659258262890683122, 1.000000000000000000, 0.9659258262890683122, 1.000000000000000000, 0.9659258262890683122, 1.000000000000000000, 0.9659258262890683122, 1.000000000000000000, 0.9659258262890683122, 1.000000000000000000, 0.9659258262890683122, 1.000000000000000000, 0.9659258262890683122, 1.000000000000000000, 0.9659258262890683122, 1.000000000000000000, 0.9659258262890683122, 1.000000000000000000, 0.9659258262890683122, 1.000000000000000000, 0.9659258262890683122, 1.000000000000000000, 0.9659258262890683122, 1.000000000000000000, 0.9659258262890683122, 1.000000000000000000, 0.9659258262890683122, 1.000000000000000000, 0.9659258262890683122, 1.000000000000000000, 0.9659258262890683122, 1.000000000000000000, 0.9659258262890683122, 1.000000000000000000, 0.9659258262890683122, 1.000000000000000000, 0.9659258262890683122, 1.000000000000000000, 0.9659258262890683122, 1.000000000000000000, 0.9659258262890683122, 1.000000000000000000, 0.9659258262890683122, 1.000000000000000000, 0.9659258262890683122, 1.000000000000000000, 0.9659258262890683122, 1.000000000000000000, 0.9659258262890683122, 1.000000000000000000, 0.9659258262890683122, 1.000000000000000000, 0.9659258262890683122, 1.000000000000000000, 0.9659258262890683122, 1.000000000000000000, 0.9659258262890683122, 1.000000000000000000, 0.9659258262890683122, 1.000000000000000000, 0.9659258262890683122, 1.000000000000000000, 0.9659258262890683122, 1.000000000000000000, 0.9659258262890683122, 1.000000000000000000, 0.9659258262890683122, 1.000000000000000000, 0.9659258262890683122, 1.000000000000000000, 0.9659258262890683122, 1.000000000000000000, 0.9659258262890683122, 1.000000000000000000, 0.9659258262890683122, 1.000000000000000000, 0.9659258262890683122, 1.000000000000000000, 0.9659258262890683122, 1.000000000000000000, 0.9659258262890683122, 1.000000000000000000, 0.9659258262890683122, 1.000000000000000000, 0.9659258262890683122, 1.000000000000000000, 0.9659258262890683122, 1.000000000000000000, 0.9659258262890683122, 1.000000000000000000, 0.9659258262890683122, 1.000000000000000000, 0.9659258262890683122, 1.000000000000000000, 0.9659258262890683122, 1.000000000000000000, 0.9659258262890683122, 1.000000000000000000, 0.9659258262890683122, 1.000000000000000000, 0.9659258262890683122, 1.000000000000000000, 0.9659258262890683122, 1.000000000000000000, 0.9659258262890683122, 1.000000000000000000, 0.9659258262890683122, 1.000000000000000000, 0.9659258262890683122, 1.000000000000000000, 0.9659258262890683122, 1.000000000000000000, 0.9659258262890683122, 1.000000000000000000, 0.9659258262890683122, 1.000000000000000000, 0.9659258262890683122, 1.000000000000000000, 0.9659258262890683122, 1.000000000000000000, 0.9659258262890683122, 1.000000000000000000, 0.9659258262890683122, 1.000000000000000000, 0.9659258262890683122, 1.000000000000000000, 0.9659258262890683122, 1.000000000000000000, 0.9659258262890683122, 1.000000000000000000, 0.9659258262890683122, 1.000000000000000000, 0.9659258262890683122, 1.000000000000000000, 0.9659258262890683122, 1.000000000000000000, 0.9659258262890683122, 1.000000000000000000, 0.9659258262890683122, 1.000000000000000000, 0.9659258262890683122, 1.000000000000000000, 0.9659258262890683122, 1.000000000000000000, 0.9659258262890683122, 1.000000000000000000, 0.9659258262890683122, 1.000000000000000000, 0.9659258262890683122, 1.000000000000000000, 0.9659258262890683122, 1.000000000000000000, 0.9659258262890683122, 1.000000000000000000, 0.9659258262890683122, 1.000000000000000000, 0.9659258262890683122, 1.000000000000000000, 0.9659258262890683122, 1.000000000000000000, 0.9659258262890683122, 1.000000000000000000, 0.9659258262890683122, 1.000000000000000000, 0.9659258262890683122, 1.000000000000000000, 0.9659258262890683122, 1.000000000000000000, 0.9659258262890683122, 1.000000000000000000, 0.9659258262890683122, 1.000000000000000000, 0.9659258262890683122, 1.000000000000000000, 0.9659258262890683122, 1.000000000000000000, 0.9659258262890683122, 1.000000000000000000, 0.9659258262890683122, 1.000000000000000000, 0.9659258262890683122, 1.000000000000000000, 0.9659258262890683122, 1.000000000000000000, 0.9659258262890683122, 1.000000000000000000, 0.9659258262890683122, 1.000000000000000000, 0.9659258262890683122, 1.000000000000000000, 0.9659258262890683122, 1.000000000000000000, 0.9659258262890683122, 1.000000000000000000, 0.9659258262890683122, 1.000000000000000000, 0.9659258262890683122, 1.000000000000000000, 0.9659258262890683122, 1.000000000000000000, 0.9659258262890683122, 1.000000000000000000, 0.9659258262890683122, 1.000000000000000000, 0.9659258262890683122, 1.000000000000000000, 0.9659258262890683122, 1.000000000000000000, 0.9659258262890683122, 1.000000000000000000, 0.9659258262890683122, 1.000000000000000000, 0.9659258262890683122, 1.000000000000000000, 0.9659258262890683122, 1.000000000000000000, 0.9659258262890683122, 1.000000000000000000, 0.9659258262890683122, 1.000000000000000000, 0.9659258262890683122, 1.000000000000000000, 0.9659258262890683122, 1.000000000000000000, 0.9659258262890683122, 1.000000000000000000, 0.9659258262890683122, 1.000000000000000000, 0.9659258262890683122, 1.000000000000000000, 0.9659258262890683122, 1.000000000000000000, 0.9659258262890683122, 1.000000000000000000, 0.9659258262890683122, 1.000000000000000000, 0.9659258262890683122, 1.000000000000000000, 0.9659258262890683122, 1.000000000000000000, 0.9659258262890683122, 1.000000000000000000, 0.9659258262890683122, 1.000000000000000000, 0.9659258262890683122, 1.000000000000000000, 0.9659258262890683122, 1.000000000000000000, 0.9659258262890683122, 1.000000000000000000, 0.9659258262890683122, 1.000000000000000000, 0.9659258262890683122, 1.000000000000000000, 0.9659258262890683122, 1.000000000000000000, 0.9659258262890683122, 1.000000000000000000, 0.9659258262890683122, 1.000000000000000000, 0.9659258262890683122, 1.000000000000000000, 0.9659258262890683122, 1.000000000000000000, 0.9659258262890683122, 1.000000000000000000, 0.9659258262890683122, 1.000000000000000000, 0.9659258262890683122, 1.000000000000000000, 0.9659258262890683122, 1.000000000000000000, 0.9659258262890683122, 1.000000000000000000, 0.9659258262890683122, 1.000000000000000000, 0.9659258262890683122, 1.000000000000000000, 0.9659258262890683122, 1.000000000000000000, 0.9659258262890683122, 1.000000000000000000, 0.9659258262890683122, 1.000000000000000000, 0.9659258262890683122, 1.000000000000000000, 0.9659258262890683122, 1.000000000000000000, 0.9659258262890683122, 1.000000000000000000, 0.9659258262890683122, 1.000000000000000000, 0.9659258262890683122, 1.000000000000000000, 0.9659258262890683122, 1.000000000000000000, 0.9659258262890683122, 1.000000000000000000, 0.9659258262890683122, 1.000000000000000000, 0.9659258262890683122, 1.000000000000000000, 0.9659258262890683122, 1.000000000000000000, 0.9659258262890683122, 1.000000000000000000, 0.9659258262890683122, 1.000000000000000000, 0.9659258262890683122, 1.000000000000000000, 0.9659258262890683122, 1.000000000000000000, 0.9659258262890683122, 1.000000000000000000, 0.9659258262890683122, 1.000000000000000000, 0.9659258262890683122, 1.000000000000000000, 0.9659258262890683122, 1.000000000000000000, 0.9659258262890683122, 1.000000000000000000, 0.9659258262890683122, 1.000000000000000000, 0.9659258262890683122, 1.000000000000000000, 0.9659258262890683122, 1.000000000000000000, 0.9659258262890683122, 1.000000000000000000, 0.9659258262890683122, 1.000000000000000000, 0.9659258262890683122, 1.000000000000000000, 0.9659258262890683122, 1.000000000000000000, 0.9659258262890683122, 1.000000000000000000, 0.9659258262890683122, 1.000000000000000000, 0.9659258262890683122, 1.000000000000000000, 0.9659258262890683122, 1.000000000000000000, 0.9659258262890683122, 1.000000000000000000, 0.9659258262890683122, 1.000000000000000000, 0.9659258262890683122, 1.000000000000000000, 0.9659258262890683122, 1.000000000000000000, 0.9659258262890683122, 1.000000000000000000, 0.9659258262890683122, 1.000000000000000000, 0.9659258262890683122, 1.000000000000000000, 0.9659258262890683122, 1.000000000000000000, 0.9659258262890683122, 1.000000000000000000, 0.9659258262890683122, 1.000000000000000000, 0.9659258262890683122, 1.000000000000000000, 0.9659258262890683122, 1.000000000000000000, 0.9659258262890683122, 1.000000000000000000, 0.9659258262890683122, 1.000000000000000000, 0.9659258262890683122, 1.000000000000000000, 0.9659258262890683122, 1.000000000000000000, 0.9659258262890683122, 1.000000000000000000, 0.9659258262890683122, 1.000000000000000000, 0.9659258262890683122, 1.000000000000000000, 0.9659258262890683122, 1.000000000000000000, 0.9659258262890683122, 1.000000000000000000, 0.9659258262890683122, 1.000000000000000000, 0.9659258262890683122, 1.000000000000000000, 0.9659258262890683122, 1.000000000000000000, 0.9659258262890683122, 1.000000000000000000, 0.9659258262890683122, 1.000000000000000000, 0.9659258262890683122, 1.000000000000000000, 0.9659258262890683122, 1.000000000000000000, 0.9659258262890683122, 1.000000000000000000, 0.9659258262890683122, 1.000000000000000000, 0.9659258262890683122, 1.000000000000000000, 0.9659258262890683122, 1.000000000000000000, 0.9659258262890683122, 1.000000000000000000, 0.9659258262890683122, 1.000000000000000000, 0.9659258262890683122, 1.000000000000000000, 0.9659258262890683122, 1.000000000000000000, 0.9659258262890683122, 1.000000000000000000, 0.9659258262890683122, 1.000000000000000000, 0.9659258262890683122, 1.000000000000000000, 0.9659258262890683122, 1.000000000000000000, 0.9659258262890683122, 1.000000000000000000, 0.9659258262890683122, 1.000000000000000000, 0.9659258262890683122, 1.000000000000000000, 0.9659258262890683122, 1.000000000000000000, 0.9659258262890683122, 1.000000000000000000, 0.9659258262890683122, 1.000000000000000000, 0.9659258262890683122, 1.000000000000000000, 0.9659258262890683122, 1.000000000000000000, 0.9659258262890683122, 1.000000000000000000, 0.9659258262890683122, 1.000000000000000000, 0.9659258262890683122, 1.000000000000000000, 0.9659258262890683122, 1.000000000000000000, 0.9659258262890683122, 1.000000000000000000, 0.9659258262890683122, 1.000000000000000000, 0.9659258262890683122, 1.000000000000000000, 0.9659258262890683122, 1.000000000000000000, 0.9659258262890683122, 1.000000000000000000, 0.9659258262890683122, 1.000000000000000000, 0.9659258262890683122, 1.000000000000000000, 0.9659258262890683122, 1.000000000000000000, 0.9659258262890683122, 1.000000000000000000, 0.9659258262890683122, 1.000000000000000000, 0.9659258262890683122, 1.000000000000000000, 0.9659258262890683122, 1.000000000000000000, 0.9659258262890683122, 1.000000000000000000, 0.9659258262890683122, 1.000000000000000000, 0.9659258262890683122, 1.000000000000000000, 0.9659258262890683122, 1.000000000000000000, 0.9659258262890683122, 1.000000000000000000, 0.9659258262890683122, 1.000000000000000000, 0.9659258262890683122, 1.000000000000000000, 0.9659258262890683122, 1.000000000000000000, 0.9659258262890683122, 1.000000000000000000, 0.9659258262890683122, 1.000000000000000000, 0.9659258262890683122, 1.000000000000000000, 0.9659258262890683122, 1.000000000000000000, 0.9659258262890683122, 1.000000000000000000, 0.9659258262890683122, 1.000000000000000000, 0.9659258262890683122, 1.000000000000000000, 0.9659258262890683122, 1.000000000000000000, 0.9659258262890683122, 1.000000000000000000, 0.9659258262890683122, 1.000000000000000000, 0.9659258262890683122, 1.000000000000000000, 0.9659258262890683122, 1.000000000000000000, 0.9659258262890683122, 1.000000000000000000, 0.9659258262890683122, 1.000000000000000000, 0.9659258262890683122, 1.000000000000000000, 0.9659258262890683122, 1.000000000000000000, 0.9659258262890683122, 1.000000000000000000, 0.9659258262890683122, 1.000000000000000000, 0.9659258262890683122, 1.000000000000000000, 0.9659258262890683122, 1.000000000000000000, 0.9659258262890683122, 1.000000000000000000, 0.9659258262890683122, 1.000000000000000000, 0.9659258262890683122, 1.000000000000000000, 0.9659258262890683122, 1.000000000000000000, 0.9659258262890683122, 1.000000000000000000, 0.9659258262890683122, 1.000000000000000000, 0.9659258262890683122, 1.000000000000000000, 0.9659258262890683122, 1.000000000000000000, 0.9659258262890683122, 1.000000000000000000, 0.9659258262890683122, 1.000000000000000000, 0.9659258262890683122, 1.000000000000000000, 0.9659258262890683122, 1.000000000000000000, 0.9659258262890683122, 1.000000000000000000, 0.9659258262890683122, 1.000000000000000000, 0.9659258262890683122, 1.000000000000000000, 0.9659258262890683122, 1.000000000000000000, 0.9659258262890683122, 1.000000000000000000, 0.9659258262890683122, 1.000000000000000000, 0.9659258262890683122, 1.000000000000000000, 0.9659258262890683122, 1.000000000000000000, 0.9659258262890683122, 1.000000000000000000, 0.9659258262890683122, 1.000000000000000000, 0.9659258262890683122, 1.000000000000000000, 0.9659258262890683122, 1.000000000000000000, 0.9659258262890683122, 1.000000000000000000, 0.9659258262890683122, 1.000000000000000000, 0.9659258262890683122, 1.000000000000000000, 0.9659258262890683122, 1.000000000000000000, 0.9659258262890683122, 1.000000000000000000, 0.9659258262890683122, 1.000000000000000000, 0.9659258262890683122, 1.000000000000000000, 0.9659258262890683122, 1.000000000000000000, 0.9659258262890683122, 1.000000000000000000, 0.9659258262890683122, 1.000000000000000000, 0.9659258262890683122, 1.000000000000000000, 0.9659258262890683122, 1.000000000000000000, 0.9659258262890683122, 1.000000000000000000, 0.9659258262890683122, 1.000000000000000000, 0.9659258262890683122, 1.000000000000000000, 0.9659258262890683122, 1.000000000000000000, 0.9659258262890683122, 1.000000000000000000, 0.9659258262890683122, 1.000000000000000000, 0.9659258262890683122, 1.000000000000000000, 0.9659258262890683122, 1.000000000000000000, 0.9659258262890683122, 1.000000000000000000, 0.9659258262890683122, 1.000000000000000000, 0.9659258262890683122, 1.000000000000000000, 0.9659258262890683122, 1.000000000000000000, 0.9659258262890683122, 1.000000000000000000, 0.9659258262890683122, 1.000000000000000000, 0.9659258262890683122, 1.000000000000000000, 0.9659258262890683122, 1.000000000000000000, 0.9659258262890683122, 1.000000000000000000, 0.9659258262890683122, 1.000000000000000000, 0.9659258262890683122, 1.000000000000000000, 0.9659258262890683122, 1.000000000000000000, 0.9659258262890683122, 1.000000000000000000, 0.9659258262890683122, 1.000000000000000000, 0.9659258262890683122, 1.000000000000000000, 0.9659258262890683122, 1.000000000000000000, 0.9659258262890683122, 1.000000000000000000, 0.9659258262890683122, 1.000000000000000000, 0.9659258262890683122, 1.000000000000000000, 0.9659258262890683122, 1.000000000000000000, 0.9659258262890683122, 1.000000000000000000, 0.9659258262890683122, 1.000000000000000000, 0.9659258262890683122, 1.000000000000000000, 0.9659258262890683122, 1.000000000000000000, 0.9659258262890683122, 1.000000000000000000, 0.9659258262890683122, 1.000000000000000000, 0.9659258262890683122, 1.000000000000000000, 0.9659258262890683122, 1.000000000000000000, 0.9659258262890683122, 1.000000000000000000, 0.9659258262890683122, 1.000000000000000000, 0.9659258262890683122, 1.000000000000000000, 0.9659258262890683122, 1.000000000000000000, 0.9659258262890683122, 1.000000000000000000, 0.9659258262890683122, 1.000000000000000000, 0.9659258262890683122, 1.000000000000000000, 0.9659258262890683122, 1.000000000000000000, 0.9659258262890683122, 1.000000000000000000, 0.9659258262890683122, 1.000000000000000000, 0.9659258262890683122, 1.000000000000000000, 0.9659258262890683122, 1.000000000000000000, 0.9659258262890683122, 1.000000000000000000, 0.9659258262890683122, 1.000000000000000000, 0.9659258262890683122, 1.000000000000000000, 0.9659258262890683122, 1.000000000000000000, 0.9659258262890683122, 1.000000000000000000, 0.9659258262890683122, 1.000000000000000000, 0.9659258262890683122, 1.000000000000000000, 0.9659258262890683122, 1.000000000000000000, 0.9659258262890683122, 1.000000000000000000, 0.9659258262890683122, 1.000000000000000000, 0.9659258262890683122, 1.000000000000000000, 0.9659258262890683122, 1.000000000000000000, 0.9659258262890683122, 1.000000000000000000, 0.9659258262890683122, 1.000000000000000000, 0.9659258262890683122, 1.000000000000000000, 0.9659258262890683122, 1.000000000000000000, 0.9659258262890683122, 1.000000000000000000, 0.9659258262890683122, 1.000000000000000000, 0.9659258262890683122, 1.000000000000000000, 0.9659258262890683122, 1.000000000000000000, 0.9659258262890683122, 1.000000000000000000, 0.9659258262890683122, 1.000000000000000000, 0.9659258262890683122, 1.000000000000000000, 0.9659258262890683122, 1.000000000000000000, 0.9659258262890683122, 1.000000000000000000, 0.9659258262890683122, 1.000000000000000000, 0.9659258262890683122, 1.000000000000000000, 0.9659258262890683122, 1.000000000000000000, 0.9659258262890683122, 1.000000000000000000, 0.9659258262890683122, 1.000000000000000000, 0.9659258262890683122, 1.000000000000000000, 0.9659258262890683122, 1.000000000000000000, 0.9659258262890683122, 1.000000000000000000, 0.9659258262890683122, 1.000000000000000000, 0.9659258262890683122, 1.000000000000000000, 0.9659258262890683122, 1.000000000000000000, 0.9659258262890683122, 1.000000000000000000, 0.9659258262890683122, 1.000000000000000000, 0.9659258262890683122, 1.000000000000000000, 0.9659258262890683122, 1.000000000000000000, 0.9659258262890683122, 1.000000000000000000, 0.9659258262890683122, 1.000000000000000000, 0.9659258262890683122, 1.000000000000000000, 0.9659258262890683122, 1.000000000000000000, 0.9659258262890683122, 1.000000000000000000, 0.9659258262890683122, 1.000000000000000000, 0.9659258262890683122, 1.000000000000000000, 0.9659258262890683122, 1.000000000000000000, 0.9659258262890683122, 1.000000000000000000, 0.9659258262890683122, 1.000000000000000000, 0.9659258262890683122, 1.000000000000000000, 0.9659258262890683122, 1.000000000000000000, 0.9659258262890683122, 1.000000000000000000, 0.9659258262890683122, 1.000000000000000000, 0.9659258262890683122, 1.000000000000000000, 0.9659258262890683122, 1.000000000000000000, 0.9659258262890683122, 1.000000000000000000, 0.9659258262890683122, 1.000000000000000000, 0.9659258262890683122, 1.000000000000000000, 0.9659258262890683122, 1.000000000000000000, 0.9659258262890683122, 1.000000000000000000, 0.9659258262890683122, 1.000000000000000000, 0.9659258262890683122, 1.000000000000000000, 0.9659258262890683122, 1.000000000000000000, 0.9659258262890683122, 1.000000000000000000, 0.9659258262890683122, 1.000000000000000000, 0.9659258262890683122, 1.000000000000000000, 0.9659258262890683122, 1.000000000000000000, 0.9659258262890683122, 1.000000000000000000, 0.9659258262890683122, 1.000000000000000000, 0.9659258262890683122, 1.000000000000000000, 0.9659258262890683122, 1.000000000000000000, 0.9659258262890683122, 1.000000000000000000, 0.9659258262890683122, 1.000000000000000000, 0.9659258262890683122, 1.000000000000000000, 0.9659258262890683122, 1.000000000000000000, 0.9659258262890683122, 1.000000000000000000, 0.9659258262890683122, 1.000000000000000000, 0.9659258262890683122, 1.000000000000000000, 0.9659258262890683122, 1.000000000000000000, 0.9659258262890683122, 1.000000000000000000, 0.9659258262890683122, 1.000000000000000000, 0.9659258262890683122, 1.000000000000000000, 0.9659258262890683122, 1.000000000000000000, 0.9659258262890683122, 1.000000000000000000, 0.9659258262890683122, 1.000000000000000000, 0.9659258262890683122, 1.000000000000000000, 0.9659258262890683122, 1.000000000000000000, 0.9659258262890683122, 1.000000000000000000, 0.9659258262890683122, 1.000000000000000000, 0.9659258262890683122, 1.000000000000000000, 0.9659258262890683122, 1.000000000000000000, 0.9659258262890683122, 1.000000000000000000, 0.9659258262890683122, 1.000000000000000000, 0.9659258262890683122, 1.000000000000000000, 0.9659258262890683122, 1.000000000000000000, 0.9659258262890683122, 1.000000000000000000, 0.9659258262890683122, 1.000000000000000000, 0.9659258262890683122, 1.000000000000000000, 0.9659258262890683122, 1.000000000000000000, 0.9659258262890683122, 1.000000000000000000, 0.9659258262890683122, 1.000000000000000000, 0.9659258262890683122, 1.000000000000000000, 0.9659258262890683122, 1.000000000000000000, 0.9659258262890683122, 1.000000000000000000, 0.9659258262890683122, 1.000000000000000000, 0.9863514817966205772, 0.9836368779841404564) ) ) 
 REPRESENTATION_ITEM ( '' )  SURFACE ( )  );
#5781=CARTESIAN_POINT ( 'NONE',  ( -7.320508075688778149, 78.12499999999998579, 7.320508075688769267 ) ) ;
#5783=CARTESIAN_POINT ( 'NONE',  ( 11.35316468749999785, 65.88541666325268409, 3.042071309553174174 ) ) ;
#5784=CARTESIAN_POINT ( 'NONE',  ( 1.102182119232618108E-15, 289.2500000000000000, 6.000000000000001776 ) ) ;
#5790=CARTESIAN_POINT ( 'NONE',  ( 2.679491924311260043, 55.83333332650537528, 9.999999999999982236 ) ) ;
#5795=CARTESIAN_POINT ( 'NONE',  ( -2.679491924311225848, 201.4583333333333144, -10.00000000000000178 ) ) ;
#5797=CARTESIAN_POINT ( 'NONE',  ( 9.832129032723420536, 171.5104166632526983, -5.676582343749999815 ) ) ;
#5800=CARTESIAN_POINT ( 'NONE',  ( 5.000000000000001776, 87.70833332650538239, -8.660254037844389075 ) ) ;
#5803=CARTESIAN_POINT ( 'NONE',  ( 5.676582343749993598, 40.26041666325268409, 9.832129032723422313 ) ) ;
#5813=CARTESIAN_POINT ( 'NONE',  ( 8.660254037844385522, 56.45833332650536818, 5.000000000000005329 ) ) ;
#5821=CARTESIAN_POINT ( 'NONE',  ( -1.967015505459129087E-11, 198.7499999999984936, 10.00000000000000533 ) ) ;
#5822=CARTESIAN_POINT ( 'NONE',  ( 2.765530957082001251, 298.9218750017070647, 6.676582343750000703 ) ) ;
#5824=CARTESIAN_POINT ( 'NONE',  ( -10.00000000000000178, 87.50000000000001421, -1.224646799147353256E-15 ) ) ;
#5825=CARTESIAN_POINT ( 'NONE',  ( -2.085542519210945728E-15, 144.5312499965860411, 11.35316468750000141 ) ) ;
#5834=VERTEX_POINT ( 'NONE', #62470 ) ;
#5838=CARTESIAN_POINT ( 'NONE',  ( -8.311093377946841443, 134.2187499965860411, 8.311093377946834337 ) ) ;
#5842=EDGE_CURVE ( 'NONE', #64770, #1466, #14534, .T. ) ;
#5843=CARTESIAN_POINT ( 'NONE',  ( -3.042071309553164404, 37.55208332991935549, -11.35316468749999963 ) ) ;
#5850=CARTESIAN_POINT ( 'NONE',  ( -6.000000000000003553, 298.0000000034140726, -2.485281374238571317 ) ) ;
#5853=CARTESIAN_POINT ( 'NONE',  ( 9.832129032723416984, 160.6770833299193555, 5.676582343750006032 ) ) ;
#5864=CARTESIAN_POINT ( 'NONE',  ( -7.320508075688831440, 56.87500000000004974, -7.320508075688833216 ) ) ;
#5868=CARTESIAN_POINT ( 'NONE',  ( -10.00000000000000000, 209.1666666598386541, -2.679491924311229845 ) ) ;
#5870=CARTESIAN_POINT ( 'NONE',  ( 6.123233995736767268E-16, 36.25000000000000711, -10.00000000000000178 ) ) ;
#5877=( BOUNDED_CURVE ( )  B_SPLINE_CURVE ( 2, ( #59218, #7529, #24854, #47872, #18107, #41121, #34623, #69306, #22906, #51961, #51206, #16862, #29323 ),
 .UNSPECIFIED., .F., .F. ) 
 B_SPLINE_CURVE_WITH_KNOTS ( ( 3, 2, 2, 2, 2, 2, 3 ),
 ( 1.962484770107478571, 1.967718660707278744, 1.972952551307078695, 1.978186441906878867, 1.983420332506679040, 1.988654223106478769, 1.993888113706278942 ),
 .UNSPECIFIED. ) 
 CURVE ( )  GEOMETRIC_REPRESENTATION_ITEM ( )  RATIONAL_B_SPLINE_CURVE ( ( 1.000000000000355049, 0.9659258262887133739, 1.000000000000000000, 0.9659258262890684232, 1.000000000000000000, 0.9659258262890684232, 1.000000000000000000, 0.9659258262890684232, 1.000000000000000000, 0.9659258262890684232, 1.000000000000000000, 0.9659258262890663138, 1.000000000000001998 ) ) 
 REPRESENTATION_ITEM ( '' )  );
#5878=ORIENTED_EDGE ( 'NONE', *, *, #54143, .F. ) ;
#5883=CARTESIAN_POINT ( 'NONE',  ( 5.000000000000001776, 202.7083333265053682, -8.660254037844389075 ) ) ;
#5884=CARTESIAN_POINT ( 'NONE',  ( -8.660254037844390851, 157.9166666666666856, 4.999999999999998224 ) ) ;
#5888=CARTESIAN_POINT ( 'NONE',  ( -3.042071309553164404, 127.5520833299193555, -11.35316468749999963 ) ) ;
#5898=( BOUNDED_CURVE ( )  B_SPLINE_CURVE ( 2, ( #36026, #600, #64321, #65043, #29622, #57944, #7350, #52635, #53744 ),
 .UNSPECIFIED., .F., .F. ) 
 B_SPLINE_CURVE_WITH_KNOTS ( ( 3, 2, 2, 2, 3 ),
 ( 0.8958333333333318160, 0.9062499999999984457, 0.9166666666666650753, 0.9270833333333318160, 0.9374999999999984457 ),
 .UNSPECIFIED. ) 
 CURVE ( )  GEOMETRIC_REPRESENTATION_ITEM ( )  RATIONAL_B_SPLINE_CURVE ( ( 1.000000000000011324, 0.9238795325112754142, 1.000000000000000000, 0.9238795325112867385, 1.000000000000000000, 0.9238795325112867385, 1.000000000000000000, 0.9238795325112980628, 0.9999999999999886757 ) ) 
 REPRESENTATION_ITEM ( '' )  );
#5900=CARTESIAN_POINT ( 'NONE',  ( -8.660254037844387298, 28.95833332650536818, -5.000000000000004441 ) ) ;
#5907=CARTESIAN_POINT ( 'NONE',  ( -8.311093377946841443, 113.9062499965859985, 8.311093377946830785 ) ) ;
#5909=CARTESIAN_POINT ( 'NONE',  ( 0.000000000000000000, 300.0000000000000000, 10.00000000000000178 ) ) ;
#5913=CARTESIAN_POINT ( 'NONE',  ( -5.676582343749998039, 107.4479166632526983, -9.832129032723420536 ) ) ;
#5917=CARTESIAN_POINT ( 'NONE',  ( -4.999999999999998224, 223.5416666598387110, -8.660254037844389075 ) ) ;
#5921=CARTESIAN_POINT ( 'NONE',  ( -3.042071309553163960, 97.23958332991935549, -11.35316468749999963 ) ) ;
#5924=EDGE_CURVE ( 'NONE', #55396, #50470, #38358, .T. ) ;
#5925=CARTESIAN_POINT ( 'NONE',  ( 5.000000000000001776, 170.8333333333333428, -8.660254037844389075 ) ) ;
#5927=CARTESIAN_POINT ( 'NONE',  ( -7.320508075688778149, 199.9999999931720254, 7.320508075688769267 ) ) ;
#5928=AXIS2_PLACEMENT_3D ( 'NONE', #70455, #59507, #43252 ) ;
#5931=CARTESIAN_POINT ( 'NONE',  ( 11.35316468750000141, 86.09374999658601268, 0.000000000000000000 ) ) ;
#5932=CARTESIAN_POINT ( 'NONE',  ( 2.765530957082001251, 287.7656250017069510, 6.676582343750000703 ) ) ;
#5936=CARTESIAN_POINT ( 'NONE',  ( 9.832129032723420536, 216.1979166632526983, -5.676582343749999815 ) ) ;
#5940=CARTESIAN_POINT ( 'NONE',  ( -5.676582343750006032, 219.1145833299193839, 9.832129032723418760 ) ) ;
#5944=CARTESIAN_POINT ( 'NONE',  ( -2.765530957081996810, 295.2656250017070079, -6.676582343750003368 ) ) ;
#5946=CARTESIAN_POINT ( 'NONE',  ( -7.320508075688778149, 119.9999999931720396, 7.320508075688769267 ) ) ;
#5947=CARTESIAN_POINT ( 'NONE',  ( -5.676582343749998039, 212.7604166632526699, -9.832129032723420536 ) ) ;
#5953=CARTESIAN_POINT ( 'NONE',  ( -1.836970198721029983E-15, 33.75000000000000000, 10.00000000000000178 ) ) ;
#5961=CARTESIAN_POINT ( 'NONE',  ( 2.765530957081996366, 296.1406250017070647, -6.676582343750002480 ) ) ;
#5964=CARTESIAN_POINT ( 'NONE',  ( -3.673940397442060854E-16, 288.8125000034140157, -6.000000000000001776 ) ) ;
#5968=VECTOR ( 'NONE', #51775, 1000.000000000000000 ) ;
#5971=LINE ( 'NONE', #70453, #35546 ) ;
#5972=CARTESIAN_POINT ( 'NONE',  ( -5.676582343749998039, 87.76041666325268409, -9.832129032723420536 ) ) ;
#5982=CARTESIAN_POINT ( 'NONE',  ( -5.676582343749998039, 202.4479166632526983, -9.832129032723420536 ) ) ;
#5988=CARTESIAN_POINT ( 'NONE',  ( -3.042071309553173730, 184.6354166632526983, 11.35316468749999785 ) ) ;
#5996=CARTESIAN_POINT ( 'NONE',  ( -2.085542519210945728E-15, 64.53124999658602690, 11.35316468750000141 ) ) ;
#6003=CARTESIAN_POINT ( 'NONE',  ( 5.676582343749993598, 64.94791666325269830, 9.832129032723422313 ) ) ;
#6008=CARTESIAN_POINT ( 'NONE',  ( 8.311093377946837890, 61.40624999658601979, -8.311093377946837890 ) ) ;
#6010=CARTESIAN_POINT ( 'NONE',  ( -3.673940397442060854E-16, 287.8125000034140157, -6.000000000000001776 ) ) ;
#6011=CARTESIAN_POINT ( 'NONE',  ( -7.320508075688773708, 153.7499999931720538, -7.320508075688774596 ) ) ;
#6013=CARTESIAN_POINT ( 'NONE',  ( -9.832129032723420536, 44.01041666325268409, 5.676582343749997150 ) ) ;
#6015=CARTESIAN_POINT ( 'NONE',  ( -3.042071309553164404, 177.2395833299193555, -11.35316468749999963 ) ) ;
#6021=CARTESIAN_POINT ( 'NONE',  ( 6.951808397369818766E-16, 182.0312499965860411, -11.35316468750000141 ) ) ;
#6027=CARTESIAN_POINT ( 'NONE',  ( 5.676582343750001591, 166.9270833299193555, -9.832129032723420536 ) ) ;
#6028=VECTOR ( 'NONE', #15224, 1000.000000000000000 ) ;
#6030=CARTESIAN_POINT ( 'NONE',  ( 5.676582343749993598, 135.2604166632526983, 9.832129032723422313 ) ) ;
#6044=CARTESIAN_POINT ( 'NONE',  ( -2.679491924326700136, 176.4583333333347639, -9.999999999991132427 ) ) ;
#6059=FACE_OUTER_BOUND ( 'NONE', #48415, .T. ) ;
#6061=CARTESIAN_POINT ( 'NONE',  ( 6.676582343750003368, 298.0468750017070079, 2.765530957081995478 ) ) ;
#6062=CARTESIAN_POINT ( 'NONE',  ( -10.00000000000000000, 137.2916666666666572, -2.679491924311229845 ) ) ;
#6078=CARTESIAN_POINT ( 'NONE',  ( 5.676582343750001591, 16.61458332991935194, -9.832129032723420536 ) ) ;
#6079=CARTESIAN_POINT ( 'NONE',  ( -2.319934922699201535E-11, 23.74999999999819522, 10.00000000000000178 ) ) ;
#6080=CARTESIAN_POINT ( 'NONE',  ( 11.35316468749999963, 216.3020833299193555, -3.042071309553165293 ) ) ;
#6081=DIRECTION ( 'NONE',  ( 0.000000000000000000, 0.000000000000000000, 1.000000000000000000 ) ) ;
#6083=CARTESIAN_POINT ( 'NONE',  ( 2.752039609470550924E-11, 41.24999999999786127, -9.999999999999998224 ) ) ;
#6089=EDGE_CURVE ( 'NONE', #18394, #35448, #21732, .T. ) ;
#6090=CARTESIAN_POINT ( 'NONE',  ( -3.042071309553164404, 22.23958332991935549, -11.35316468749999963 ) ) ;
#6092=CARTESIAN_POINT ( 'NONE',  ( -2.664923566518097392E-11, 208.7499999999979252, 10.00000000000000178 ) ) ;
#6096=CARTESIAN_POINT ( 'NONE',  ( 11.35316468750000141, 15.78124999658601624, 0.000000000000000000 ) ) ;
#6098=CARTESIAN_POINT ( 'NONE',  ( -3.042071309553164404, 137.2395833299193271, -11.35316468749999963 ) ) ;
#6099=EDGE_CURVE ( 'NONE', #20100, #17783, #9081, .T. ) ;
#6100=CARTESIAN_POINT ( 'NONE',  ( -10.00000000000000000, 119.1666666598387110, -2.679491924311229845 ) ) ;
#6102=CARTESIAN_POINT ( 'NONE',  ( -7.320508075688778149, 4.999999993172033363, 7.320508075688769267 ) ) ;
#6106=CARTESIAN_POINT ( 'NONE',  ( -9.832129032723418760, 13.17708332991935194, -5.676582343750004256 ) ) ;
#6107=CARTESIAN_POINT ( 'NONE',  ( -2.679491924311226292, 153.3333333265053682, -10.00000000000000178 ) ) ;
#6108=CARTESIAN_POINT ( 'NONE',  ( 6.676582343750004256, 295.8906250017069510, 2.765530957081995478 ) ) ;
#6109=CARTESIAN_POINT ( 'NONE',  ( 9.832129032723420536, 141.1979166632526699, -5.676582343749999815 ) ) ;
#6121=CARTESIAN_POINT ( 'NONE',  ( 3.042071309553159519, 95.05208332991935549, 11.35316468750000141 ) ) ;
#6132=CIRCLE ( 'NONE', #67563, 10.00000000000000178 ) ;
#6152=CARTESIAN_POINT ( 'NONE',  ( 8.660254037844389075, 100.4166666666666714, -5.000000000000000000 ) ) ;
#6155=CARTESIAN_POINT ( 'NONE',  ( 9.832129032723416984, 65.67708332991935549, 5.676582343750006032 ) ) ;
#6156=CARTESIAN_POINT ( 'NONE',  ( -6.000000000000000888, 288.0625000000000000, 2.485281374238575758 ) ) ;
#6161=CARTESIAN_POINT ( 'NONE',  ( -10.00000000000000000, 104.1666666598386968, -2.679491924311229845 ) ) ;
#6166=CARTESIAN_POINT ( 'NONE',  ( -7.320508075688778149, 203.1249999999999432, 7.320508075688769267 ) ) ;
#6168=CARTESIAN_POINT ( 'NONE',  ( -2.085542519210945728E-15, 174.8437499965860411, 11.35316468750000141 ) ) ;
#6169=CARTESIAN_POINT ( 'NONE',  ( -10.00000000000022560, 212.7083333333334565, 2.679491924311282691 ) ) ;
#6177=CARTESIAN_POINT ( 'NONE',  ( -11.35316468749999785, 38.38541666325268409, -3.042071309553167513 ) ) ;
#6181=CARTESIAN_POINT ( 'NONE',  ( 10.00000000000000000, 221.6666666598386826, 2.679491924311235618 ) ) ;
#6184=CARTESIAN_POINT ( 'NONE',  ( 4.999999999999993783, 56.04166665983870388, 8.660254037844390851 ) ) ;
#6187=CARTESIAN_POINT ( 'NONE',  ( 7.320508075688770155, 55.62499999999998579, -7.320508075688770155 ) ) ;
#6193=CARTESIAN_POINT ( 'NONE',  ( 4.721056650415999201, 297.2343750017069510, -4.721056650415999201 ) ) ;
#6196=CARTESIAN_POINT ( 'NONE',  ( -5.676582343749998039, 152.4479166632526983, -9.832129032723420536 ) ) ;
#6208=CARTESIAN_POINT ( 'NONE',  ( 11.35316468749999785, 125.8854166632526983, 3.042071309553174174 ) ) ;
#6213=CARTESIAN_POINT ( 'NONE',  ( -2.085542519210945728E-15, 44.84374999658602690, 11.35316468750000141 ) ) ;
#6215=CARTESIAN_POINT ( 'NONE',  ( 2.679491924311228956, 37.91666665983869677, -10.00000000000000000 ) ) ;
#6223=CARTESIAN_POINT ( 'NONE',  ( 6.000000000000003553, 296.6250000034139589, -2.485281374238571761 ) ) ;
#6233=EDGE_LOOP ( 'NONE', ( #19872, #60171, #53952, #5183 ) ) ;
#6243=EDGE_LOOP ( 'NONE', ( #58554, #19382, #56979, #64425 ) ) ;
#6246=CARTESIAN_POINT ( 'NONE',  ( 7.320508075688771044, 44.37500000000000000, 7.320508075688775484 ) ) ;
#6250=CARTESIAN_POINT ( 'NONE',  ( -10.00000000000000178, 34.37499999317203248, -1.224646799147353454E-15 ) ) ;
#6261=CARTESIAN_POINT ( 'NONE',  ( 6.123233995736767268E-16, 156.2500000000000000, -10.00000000000000178 ) ) ;
#6262=DIRECTION ( 'NONE',  ( -0.000000000000000000, 1.000000000000000000, -0.000000000000000000 ) ) ;
#6264=CARTESIAN_POINT ( 'NONE',  ( 11.35316468750000141, 136.0937499965860127, 0.000000000000000000 ) ) ;
#6271=CARTESIAN_POINT ( 'NONE',  ( -5.676582343749998039, 2.760416663252683644, -9.832129032723420536 ) ) ;
#6276=CARTESIAN_POINT ( 'NONE',  ( 8.660254037844389075, 27.29166665983870033, -5.000000000000000000 ) ) ;
#6282=CARTESIAN_POINT ( 'NONE',  ( 5.676582343749993598, 104.9479166632526841, 9.832129032723422313 ) ) ;
#6286=DIRECTION ( 'NONE',  ( 0.000000000000000000, 0.000000000000000000, 1.000000000000000000 ) ) ;
#6289=CARTESIAN_POINT ( 'NONE',  ( -9.832129032723418760, 112.8645833299193555, -5.676582343750004256 ) ) ;
#6293=CARTESIAN_POINT ( 'NONE',  ( 10.00000000000000178, 216.8749999931720538, 0.000000000000000000 ) ) ;
#6296=CARTESIAN_POINT ( 'NONE',  ( -10.00000000000000000, 182.5000000000000568, -1.224646799147353059E-15 ) ) ;
#6297=CARTESIAN_POINT ( 'NONE',  ( 5.676582343749993598, 104.9479166632526841, 9.832129032723422313 ) ) ;
#6303=CARTESIAN_POINT ( 'NONE',  ( 4.999999999999993783, 191.0416666598387110, 8.660254037844390851 ) ) ;
#6307=CARTESIAN_POINT ( 'NONE',  ( -3.042071309553173730, 84.63541666325266988, 11.35316468749999785 ) ) ;
#6308=CARTESIAN_POINT ( 'NONE',  ( -2.765530957081998586, 287.6406250017069510, 6.676582343750001591 ) ) ;
#6312=CARTESIAN_POINT ( 'NONE',  ( -9.832129032723418760, 217.8645833299193839, -5.676582343750004256 ) ) ;
#6316=CARTESIAN_POINT ( 'NONE',  ( -5.676582343750006032, 224.1145833299193839, 9.832129032723418760 ) ) ;
#6320=CARTESIAN_POINT ( 'NONE',  ( 2.765530957082001251, 295.7656250017069510, 6.676582343750000703 ) ) ;
#6322=CARTESIAN_POINT ( 'NONE',  ( -10.00000000000000355, 119.5833333265053824, 2.679491924311223183 ) ) ;
#6323=CARTESIAN_POINT ( 'NONE',  ( -8.311093377946841443, 214.2187499965860127, 8.311093377946834337 ) ) ;
#6331=( BOUNDED_CURVE ( )  B_SPLINE_CURVE ( 2, ( #28132, #17180, #238, #21720, #27382, #63204, #40573, #22458, #4389, #51897, #23219, #16057, #50401 ),
 .UNSPECIFIED., .F., .F. ) 
 B_SPLINE_CURVE_WITH_KNOTS ( ( 3, 2, 2, 2, 2, 2, 3 ),
 ( 0.02717391304347826012, 0.02898550724637681195, 0.03079710144927536378, 0.03260869565217391214, 0.03442028985507246397, 0.03623188405797101580, 0.03804347826086956763 ),
 .UNSPECIFIED. ) 
 CURVE ( )  GEOMETRIC_REPRESENTATION_ITEM ( )  RATIONAL_B_SPLINE_CURVE ( ( 1.000000000000000000, 0.9659258262890683122, 1.000000000000000000, 0.9659258262890683122, 1.000000000000000000, 0.9659258262890683122, 1.000000000000000000, 0.9659258262890683122, 1.000000000000000000, 0.9659258262890683122, 1.000000000000000000, 0.9659258262890683122, 1.000000000000000000 ) ) 
 REPRESENTATION_ITEM ( '' )  );
#6332=CARTESIAN_POINT ( 'NONE',  ( -10.00000000000000178, 27.50000000000000000, -1.224646799147353454E-15 ) ) ;
#6339=AXIS2_PLACEMENT_3D ( 'NONE', #40070, #34434, #34063 ) ;
#6343=CARTESIAN_POINT ( 'NONE',  ( -4.088227598258586603E-16, 298.2031250017070079, -6.676582343750001591 ) ) ;
#6344=EDGE_CURVE ( 'NONE', #9485, #52532, #14347, .T. ) ;
#6349=ORIENTED_EDGE ( 'NONE', *, *, #27893, .F. ) ;
#6356=CARTESIAN_POINT ( 'NONE',  ( -11.35316468750000141, 83.59374999658601268, -1.390361679473963753E-15 ) ) ;
#6361=ORIENTED_EDGE ( 'NONE', *, *, #53078, .T. ) ;
#6364=CARTESIAN_POINT ( 'NONE',  ( 9.832129032723416984, 205.3645833299193555, 5.676582343750006032 ) ) ;
#6368=CARTESIAN_POINT ( 'NONE',  ( -8.311093377946841443, 179.2187499965859843, 8.311093377946830785 ) ) ;
#6375=CARTESIAN_POINT ( 'NONE',  ( -11.35316468750000141, 63.48958332991935549, 3.042071309553159963 ) ) ;
#6382=CARTESIAN_POINT ( 'NONE',  ( 9.832129032723416984, 60.36458332991934839, 5.676582343750006032 ) ) ;
#6387=CARTESIAN_POINT ( 'NONE',  ( -3.042071309553163960, 57.23958332991935549, -11.35316468749999963 ) ) ;
#6390=CARTESIAN_POINT ( 'NONE',  ( -1.836970198721029983E-15, 160.6249999931720254, 10.00000000000000178 ) ) ;
#6393=CARTESIAN_POINT ( 'NONE',  ( 3.042071309553167513, 42.13541666325267698, -11.35316468749999785 ) ) ;
#6395=CARTESIAN_POINT ( 'NONE',  ( 11.35316468749999963, 185.9895833299193839, -3.042071309553165293 ) ) ;
#6399=CARTESIAN_POINT ( 'NONE',  ( 10.00000000000000178, 61.87499999317203958, 0.000000000000000000 ) ) ;
#6401=CARTESIAN_POINT ( 'NONE',  ( 5.676582343749993598, 179.9479166632526983, 9.832129032723422313 ) ) ;
#6407=CARTESIAN_POINT ( 'NONE',  ( 3.042071309553159519, 170.0520833299193271, 11.35316468750000141 ) ) ;
#6409=CARTESIAN_POINT ( 'NONE',  ( -2.085542519210945728E-15, 129.8437499965860127, 11.35316468750000141 ) ) ;
#6430=( BOUNDED_CURVE ( )  B_SPLINE_CURVE ( 2, ( #4753, #34555, #50388, #50756, #57560, #5868, #23206, #69235, #16412, #73772, #17544, #39444, #40563 ),
 .UNSPECIFIED., .F., .F. ) 
 B_SPLINE_CURVE_WITH_KNOTS ( ( 3, 2, 2, 2, 2, 2, 3 ),
 ( 0.8967391304347825942, 0.8985507246376811530, 0.9003623188405797118, 0.9021739130434782705, 0.9039855072463767183, 0.9057971014492752770, 0.9076086956521738358 ),
 .UNSPECIFIED. ) 
 CURVE ( )  GEOMETRIC_REPRESENTATION_ITEM ( )  RATIONAL_B_SPLINE_CURVE ( ( 1.000000000000000000, 0.9659258262890683122, 1.000000000000000000, 0.9659258262890683122, 1.000000000000000000, 0.9659258262890683122, 1.000000000000000000, 0.9659258262890683122, 1.000000000000000000, 0.9659258262890683122, 1.000000000000000000, 0.9659258262890704216, 0.9999999999999978906 ) ) 
 REPRESENTATION_ITEM ( '' )  );
#6439=CARTESIAN_POINT ( 'NONE',  ( 6.676582343750001591, 299.1093750017069510, -8.176455196517173205E-16 ) ) ;
#6440=CARTESIAN_POINT ( 'NONE',  ( 8.660254037844385522, 134.5833333333333428, 5.000000000000005329 ) ) ;
#6443=CARTESIAN_POINT ( 'NONE',  ( 4.180849123998743089, 225.9999999999999716, 9.092589271092984760 ) ) ;
#6455=CARTESIAN_POINT ( 'NONE',  ( 2.679491924311222739, 50.83333332650537528, 10.00000000000000355 ) ) ;
#6457=CARTESIAN_POINT ( 'NONE',  ( -9.832129032723420536, 28.69791666325268409, 5.676582343749997150 ) ) ;
#6458=CARTESIAN_POINT ( 'NONE',  ( 5.000000000000158096, 24.16666666666685614, 8.660254037844676844 ) ) ;
#6459=CARTESIAN_POINT ( 'NONE',  ( -5.676582343750006032, 219.4270833299193555, 9.832129032723418760 ) ) ;
#6465=CARTESIAN_POINT ( 'NONE',  ( 5.676582343750001591, 21.61458332991935194, -9.832129032723420536 ) ) ;
#6468=CARTESIAN_POINT ( 'NONE',  ( -2.485281374238197394, 295.2500000034139589, 6.000000000000376588 ) ) ;
#6471=CARTESIAN_POINT ( 'NONE',  ( 9.832129032723416984, 20.36458332991935194, 5.676582343750006032 ) ) ;
#6473=CARTESIAN_POINT ( 'NONE',  ( 8.311093377946834337, 155.1562499965860127, 8.311093377946839666 ) ) ;
#6474=CARTESIAN_POINT ( 'NONE',  ( 10.00000000000000000, 121.6666666598386968, 2.679491924311236062 ) ) ;
#6476=DIRECTION ( 'NONE',  ( 0.000000000000000000, 0.000000000000000000, 1.000000000000000000 ) ) ;
#6479=ORIENTED_EDGE ( 'NONE', *, *, #48677, .F. ) ;
#6480=CARTESIAN_POINT ( 'NONE',  ( 9.832129032723420536, 6.510416663252683200, -5.676582343749999815 ) ) ;
#6481=VERTEX_POINT ( 'NONE', #8468 ) ;
#6482=CARTESIAN_POINT ( 'NONE',  ( 6.000000000000003553, 289.4375000000000000, 2.485281374238571317 ) ) ;
#6483=CARTESIAN_POINT ( 'NONE',  ( 6.676582343750004256, 297.8906250017069510, 2.765530957081995478 ) ) ;
#6484=CARTESIAN_POINT ( 'NONE',  ( 11.35316468749999963, 135.9895833299192986, -3.042071309553165293 ) ) ;
#6490=CARTESIAN_POINT ( 'NONE',  ( -8.660254037844387298, 203.9583333265053682, -5.000000000000004441 ) ) ;
#6492=CARTESIAN_POINT ( 'NONE',  ( 8.311093377946837890, 91.71874999658599847, -8.311093377946837890 ) ) ;
#6508=EDGE_CURVE ( 'NONE', #29716, #7760, #7107, .T. ) ;
#6522=CARTESIAN_POINT ( 'NONE',  ( 8.660254037844389075, 90.41666666666667140, -5.000000000000000000 ) ) ;
#6524=CARTESIAN_POINT ( 'NONE',  ( -11.35316468750000141, 58.59374999658601979, -1.390361679473963753E-15 ) ) ;
#6525=CARTESIAN_POINT ( 'NONE',  ( -4.721056650415999201, 298.4843750017070079, -4.721056650415999201 ) ) ;
#6531=CARTESIAN_POINT ( 'NONE',  ( -2.679491924311235174, 105.4166666598386968, 10.00000000000000000 ) ) ;
#6536=CARTESIAN_POINT ( 'NONE',  ( 5.000000000000001776, 215.8333333333333428, -8.660254037844389075 ) ) ;
#6538=CARTESIAN_POINT ( 'NONE',  ( 11.35316468749999963, 181.3020833299192986, -3.042071309553165293 ) ) ;
#6546=CARTESIAN_POINT ( 'NONE',  ( -3.042071309553164404, 37.55208332991935549, -11.35316468749999963 ) ) ;
#6554=CARTESIAN_POINT ( 'NONE',  ( -10.00000000000000000, 74.16666665983868256, -2.679491924311229845 ) ) ;
#6557=CARTESIAN_POINT ( 'NONE',  ( 6.350741970897364085E-13, 216.2499999999999432, -9.999999999999998224 ) ) ;
#6559=LINE ( 'NONE', #29565, #29386 ) ;
#6563=CARTESIAN_POINT ( 'NONE',  ( -4.721056650415999201, 299.4843750017070079, -4.721056650415999201 ) ) ;
#6565=CARTESIAN_POINT ( 'NONE',  ( -8.660254037844389075, 87.91666666666667140, 4.999999999999998224 ) ) ;
#6566=CARTESIAN_POINT ( 'NONE',  ( 3.042071309553167069, 151.8229166632526699, -11.35316468749999785 ) ) ;
#6576=CARTESIAN_POINT ( 'NONE',  ( -8.311093377946836114, 127.9687499965860269, -8.311093377946837890 ) ) ;
#6580=CARTESIAN_POINT ( 'NONE',  ( -9.832129032723420536, 44.01041666325268409, 5.676582343749997150 ) ) ;
#6582=CARTESIAN_POINT ( 'NONE',  ( 10.00000000000000178, 37.08333332650536107, -2.679491924311226736 ) ) ;
#6587=CARTESIAN_POINT ( 'NONE',  ( -2.485281374238572649, 294.2500000034140157, 6.000000000000002665 ) ) ;
#6611=CARTESIAN_POINT ( 'NONE',  ( 10.00000000000000178, 55.20833333333332860, -2.679491924311226736 ) ) ;
#6617=CARTESIAN_POINT ( 'NONE',  ( -1.836970198721029983E-15, 35.62499999317203248, 10.00000000000000178 ) ) ;
#6622=AXIS2_PLACEMENT_3D ( 'NONE', #28962, #32214, #20495 ) ;
#6626=CARTESIAN_POINT ( 'NONE',  ( 10.00000000000000178, 201.8749999931720538, 0.000000000000000000 ) ) ;
#6627=CARTESIAN_POINT ( 'NONE',  ( 5.000000000000001776, 165.8333333333333428, -8.660254037844389075 ) ) ;
#6630=CARTESIAN_POINT ( 'NONE',  ( -3.042071309553173730, 139.6354166632526415, 11.35316468749999785 ) ) ;
#6631=CARTESIAN_POINT ( 'NONE',  ( -4.242640687119286547, 293.9375000034140157, -4.242640687119286547 ) ) ;
#6632=CARTESIAN_POINT ( 'NONE',  ( 2.679491924311222739, 25.83333332650536462, 10.00000000000000355 ) ) ;
#6636=ORIENTED_EDGE ( 'NONE', *, *, #29310, .T. ) ;
#6642=CARTESIAN_POINT ( 'NONE',  ( 4.999999999999993783, 41.04166665983870388, 8.660254037844390851 ) ) ;
#6648=DIRECTION ( 'NONE',  ( 0.000000000000000000, 0.000000000000000000, 1.000000000000000000 ) ) ;
#6651=LINE ( 'NONE', #5909, #31578 ) ;
#6653=CARTESIAN_POINT ( 'NONE',  ( -1.836970198721029983E-15, 63.75000000000000000, 10.00000000000000178 ) ) ;
#6655=CARTESIAN_POINT ( 'NONE',  ( 3.042071309553167069, 121.8229166632526841, -11.35316468749999785 ) ) ;
#6659=CARTESIAN_POINT ( 'NONE',  ( 7.320508075688771044, 221.2499999931720538, 7.320508075688775484 ) ) ;
#6662=CARTESIAN_POINT ( 'NONE',  ( 1.267086777181619559E-12, 183.7500000000001137, 10.00000000000000178 ) ) ;
#6663=CARTESIAN_POINT ( 'NONE',  ( -8.311093377946836114, 102.6562499965860269, -8.311093377946837890 ) ) ;
#6666=LINE ( 'NONE', #47009, #63814 ) ;
#6667=ORIENTED_EDGE ( 'NONE', *, *, #57299, .T. ) ;
#6668=CARTESIAN_POINT ( 'NONE',  ( 4.999999999999993783, 196.0416666598387110, 8.660254037844390851 ) ) ;
#6671=CARTESIAN_POINT ( 'NONE',  ( -8.311093377946841443, 84.21874999658599847, 8.311093377946834337 ) ) ;
#6675=CARTESIAN_POINT ( 'NONE',  ( -3.042071309553173730, 14.63541666325268231, 11.35316468749999785 ) ) ;
#6677=VERTEX_POINT ( 'NONE', #27683 ) ;
#6678=CARTESIAN_POINT ( 'NONE',  ( -5.000000000000002665, 136.6666666666666856, -8.660254037844396180 ) ) ;
#6680=CARTESIAN_POINT ( 'NONE',  ( -8.311093377946836114, 222.6562499965860411, -8.311093377946837890 ) ) ;
#6684=CARTESIAN_POINT ( 'NONE',  ( -4.088227598258586603E-16, 298.2031250017070079, -6.676582343750001591 ) ) ;
#6688=CARTESIAN_POINT ( 'NONE',  ( 9.832129032723420536, 211.5104166632526699, -5.676582343749999815 ) ) ;
#6695=CARTESIAN_POINT ( 'NONE',  ( -8.660254037844390851, 27.91666666666666785, 4.999999999999998224 ) ) ;
#6696=EDGE_CURVE ( 'NONE', #13863, #15764, #20902, .T. ) ;
#6704=CARTESIAN_POINT ( 'NONE',  ( -2.295000000000000373, 255.7199999999997715, 5.414445227810388950 ) ) ;
#6705=CARTESIAN_POINT ( 'NONE',  ( -2.765530957081996810, 297.2656250017069510, -6.676582343750002480 ) ) ;
#6707=CARTESIAN_POINT ( 'NONE',  ( -4.242640687119286547, 288.9375000034140157, -4.242640687119286547 ) ) ;
#6715=CARTESIAN_POINT ( 'NONE',  ( 8.311093377946837890, 96.71874999658599847, -8.311093377946837890 ) ) ;
#6720=CARTESIAN_POINT ( 'NONE',  ( 2.765530957082001251, 287.9218750017069510, 6.676582343749999815 ) ) ;
#6723=CARTESIAN_POINT ( 'NONE',  ( -10.00000000000000178, 179.3749999931720538, -1.224646799147353454E-15 ) ) ;
#6725=CARTESIAN_POINT ( 'NONE',  ( -11.35316468749999785, 218.0729166632526699, -3.042071309553167513 ) ) ;
#6731=CARTESIAN_POINT ( 'NONE',  ( 11.35316468750000141, 181.0937499965860411, 0.000000000000000000 ) ) ;
#6737=CARTESIAN_POINT ( 'NONE',  ( -8.311093377946841443, 68.90624999658602690, 8.311093377946830785 ) ) ;
#6738=EDGE_CURVE ( 'NONE', #17827, #31901, #4680, .T. ) ;
#6744=CARTESIAN_POINT ( 'NONE',  ( 9.832129032723416984, 80.36458332991935549, 5.676582343750006032 ) ) ;
#6749=CARTESIAN_POINT ( 'NONE',  ( -11.35316468750000141, 53.48958332991934839, 3.042071309553159963 ) ) ;
#6751=CARTESIAN_POINT ( 'NONE',  ( -7.320508075688773708, 13.74999999317203070, -7.320508075688774596 ) ) ;
#6752=CARTESIAN_POINT ( 'NONE',  ( 2.679491924311228956, 152.9166666598387394, -10.00000000000000000 ) ) ;
#6755=CARTESIAN_POINT ( 'NONE',  ( 9.832129032723420536, 46.51041666325269119, -5.676582343749999815 ) ) ;
#6757=CARTESIAN_POINT ( 'NONE',  ( -11.35316468750000141, 193.2812499965860127, -1.390361679473963753E-15 ) ) ;
#6763=CARTESIAN_POINT ( 'NONE',  ( -11.35316468750000141, 183.2812499965860411, -1.390361679473963753E-15 ) ) ;
#6765=DIRECTION ( 'NONE',  ( -0.000000000000000000, 1.000000000000000000, -0.000000000000000000 ) ) ;
#6770=CARTESIAN_POINT ( 'NONE',  ( -3.042071309553163960, 172.5520833299193555, -11.35316468749999963 ) ) ;
#6771=( BOUNDED_CURVE ( )  B_SPLINE_CURVE ( 2, ( #32246, #66185, #65810, #55263, #14488, #3569, #26559, #15614, #72600, #20907, #8855, #38653, #61656 ),
 .UNSPECIFIED., .F., .F. ) 
 B_SPLINE_CURVE_WITH_KNOTS ( ( 3, 2, 2, 2, 2, 2, 3 ),
 ( 0.4076086956521738913, 0.4094202898550724501, 0.4112318840579710089, 0.4130434782608695121, 0.4148550724637680709, 0.4166666666666666297, 0.4184782608695651884 ),
 .UNSPECIFIED. ) 
 CURVE ( )  GEOMETRIC_REPRESENTATION_ITEM ( )  RATIONAL_B_SPLINE_CURVE ( ( 1.000000000000000000, 0.9659258262890683122, 1.000000000000000000, 0.9659258262890683122, 1.000000000000000000, 0.9659258262890683122, 1.000000000000000000, 0.9659258262890683122, 1.000000000000000000, 0.9659258262890683122, 1.000000000000000000, 0.9659258262890693114, 0.9999999999999990008 ) ) 
 REPRESENTATION_ITEM ( '' )  );
#6773=CARTESIAN_POINT ( 'NONE',  ( -5.676582343750006032, 124.4270833299193555, 9.832129032723418760 ) ) ;
#6776=ORIENTED_EDGE ( 'NONE', *, *, #24459, .T. ) ;
#6778=VECTOR ( 'NONE', #2724, 1000.000000000000000 ) ;
#6780=CYLINDRICAL_SURFACE ( 'NONE', #25181, 10.00000000000000178 ) ;
#6785=CARTESIAN_POINT ( 'NONE',  ( 10.00000000000005507, 180.0000000000000568, 0.000000000000000000 ) ) ;
#6798=CARTESIAN_POINT ( 'NONE',  ( -4.088227598258586603E-16, 299.3593750017070079, -6.676582343750001591 ) ) ;
#6799=CARTESIAN_POINT ( 'NONE',  ( 10.00000000000000178, 140.2083333333333712, -2.679491924311226736 ) ) ;
#6812=CARTESIAN_POINT ( 'NONE',  ( 8.660254037844389075, 52.29166665983870388, -5.000000000000000000 ) ) ;
#6814=CARTESIAN_POINT ( 'NONE',  ( -5.676582343750006032, 24.11458332991935194, 9.832129032723418760 ) ) ;
#6817=CARTESIAN_POINT ( 'NONE',  ( 11.35316468750000141, 221.0937499965860127, 0.000000000000000000 ) ) ;
#6823=CARTESIAN_POINT ( 'NONE',  ( -5.676582343750006032, 34.11458332991934839, 9.832129032723418760 ) ) ;
#6827=CARTESIAN_POINT ( 'NONE',  ( -7.320508075688779925, 151.8750000000000284, -7.320508075688779925 ) ) ;
#6830=CARTESIAN_POINT ( 'NONE',  ( -11.35316468750000141, 13.28124999658601624, -1.390361679473963753E-15 ) ) ;
#6832=CARTESIAN_POINT ( 'NONE',  ( -11.35316468750000141, 143.2812499965860411, -1.390361679473963753E-15 ) ) ;
#6833=CARTESIAN_POINT ( 'NONE',  ( -7.320508075688773708, 113.7499999931720112, -7.320508075688774596 ) ) ;
#6835=CARTESIAN_POINT ( 'NONE',  ( -1.836970198721029983E-15, 3.750000000000000444, 10.00000000000000178 ) ) ;
#6838=CARTESIAN_POINT ( 'NONE',  ( 11.35316468749999785, 5.885416663252683200, 3.042071309553174174 ) ) ;
#6839=ORIENTED_EDGE ( 'NONE', *, *, #38495, .T. ) ;
#6841=CARTESIAN_POINT ( 'NONE',  ( -2.765530957081998586, 297.6406250017070079, 6.676582343750001591 ) ) ;
#6843=CARTESIAN_POINT ( 'NONE',  ( -11.35316468750000141, 133.4895833299193555, 3.042071309553159963 ) ) ;
#6853=UNCERTAINTY_MEASURE_WITH_UNIT (LENGTH_MEASURE( 1.000000000000000082E-05 ), #3888, 'distance_accuracy_value', 'NONE');
#6854=CARTESIAN_POINT ( 'NONE',  ( 6.951808397369818766E-16, 92.34374999658602690, -11.35316468750000141 ) ) ;
#6856=EDGE_CURVE ( 'NONE', #11129, #40340, #37484, .T. ) ;
#6868=( BOUNDED_CURVE ( )  B_SPLINE_CURVE ( 2, ( #52219, #69565, #74473, #17876, #19257, #34137, #5452, #40893, #11848, #51460, #59272, #68439, #57521 ),
 .UNSPECIFIED., .F., .F. ) 
 B_SPLINE_CURVE_WITH_KNOTS ( ( 3, 2, 2, 2, 2, 2, 3 ),
 ( 1.303087675546690472, 1.308321663417258307, 1.313555651287826143, 1.318789639158393756, 1.324023627028961592, 1.329257614899529427, 1.334491602770097263 ),
 .UNSPECIFIED. ) 
 CURVE ( )  GEOMETRIC_REPRESENTATION_ITEM ( )  RATIONAL_B_SPLINE_CURVE ( ( 1.000000000000101252, 0.9659258262889670599, 1.000000000000000000, 0.9659258262890683122, 1.000000000000000000, 0.9659258262890683122, 1.000000000000000000, 0.9659258262890683122, 1.000000000000000000, 0.9659258262890683122, 1.000000000000000000, 0.9659258262890704216, 0.9999999999999978906 ) ) 
 REPRESENTATION_ITEM ( '' )  );
#6874=CARTESIAN_POINT ( 'NONE',  ( 4.999999999999993783, 151.0416666598387110, 8.660254037844390851 ) ) ;
#6876=CARTESIAN_POINT ( 'NONE',  ( -10.00000000000000178, 224.3749999931720254, -1.224646799147353454E-15 ) ) ;
#6878=CARTESIAN_POINT ( 'NONE',  ( 7.320508075688774596, 122.4999999931720254, -7.320508075688774596 ) ) ;
#6881=ORIENTED_EDGE ( 'NONE', *, *, #6856, .T. ) ;
#6887=CARTESIAN_POINT ( 'NONE',  ( 10.00000000000000178, 95.20833333333334281, -2.679491924311226736 ) ) ;
#6889=CARTESIAN_POINT ( 'NONE',  ( 8.311093377946837890, 61.71874999658601979, -8.311093377946837890 ) ) ;
#6890=CARTESIAN_POINT ( 'NONE',  ( -4.088227598258586603E-16, 296.3593750017070079, -6.676582343750001591 ) ) ;
#6895=CARTESIAN_POINT ( 'NONE',  ( 2.679491924310495765, 86.04166666666674246, -10.00000000000043343 ) ) ;
#6898=CARTESIAN_POINT ( 'NONE',  ( -2.485281374238227592, 293.1874999999999432, 6.000000000000345501 ) ) ;
#6900=CARTESIAN_POINT ( 'NONE',  ( 6.123233995736767268E-16, 221.2500000000000000, -10.00000000000000178 ) ) ;
#6902=CARTESIAN_POINT ( 'NONE',  ( 8.311093377946837890, 181.7187499965859843, -8.311093377946837890 ) ) ;
#6909=CARTESIAN_POINT ( 'NONE',  ( 9.832129032723416984, 35.67708332991935549, 5.676582343750006032 ) ) ;
#6911=CARTESIAN_POINT ( 'NONE',  ( 11.35316468749999785, 220.8854166632526699, 3.042071309553174174 ) ) ;
#6914=CARTESIAN_POINT ( 'NONE',  ( 3.410844894484189267E-12, 36.24999999999974420, -10.00000000000000178 ) ) ;
#6915=CARTESIAN_POINT ( 'NONE',  ( -9.999999999999978684, 102.2916666666666572, -2.679491924311224516 ) ) ;
#6918=EDGE_CURVE ( 'NONE', #57818, #50631, #22515, .T. ) ;
#6919=CARTESIAN_POINT ( 'NONE',  ( -10.00000000000000178, 79.37499999317202537, -1.224646799147353454E-15 ) ) ;
#6922=CARTESIAN_POINT ( 'NONE',  ( -6.000000000000001776, 299.0625000034140157, 0.000000000000000000 ) ) ;
#6926=EDGE_LOOP ( 'NONE', ( #56541, #14651, #26106, #22412 ) ) ;
#6927=CARTESIAN_POINT ( 'NONE',  ( -6.676582343750000703, 298.6718750017070079, 2.765530957082001251 ) ) ;
#6928=CARTESIAN_POINT ( 'NONE',  ( -5.000000000000004441, 141.6666666666666856, -8.660254037844399733 ) ) ;
#6929=VECTOR ( 'NONE', #60064, 1000.000000000000000 ) ;
#6931=CARTESIAN_POINT ( 'NONE',  ( -8.311093377946841443, 153.9062499965860127, 8.311093377946830785 ) ) ;
#6933=CARTESIAN_POINT ( 'NONE',  ( 7.320508075688771932, 4.374999999999999112, 7.320508075688776373 ) ) ;
#6937=ORIENTED_EDGE ( 'NONE', *, *, #30633, .F. ) ;
#6940=CARTESIAN_POINT ( 'NONE',  ( 5.676582343749993598, 140.2604166632526983, 9.832129032723422313 ) ) ;
#6944=CARTESIAN_POINT ( 'NONE',  ( -9.832129032723420536, 49.01041666325269119, 5.676582343749997150 ) ) ;
#6946=CARTESIAN_POINT ( 'NONE',  ( -10.00000000000000888, 27.50000000000000355, -1.224646799147354243E-15 ) ) ;
#6950=CARTESIAN_POINT ( 'NONE',  ( -4.242640687119286547, 293.9375000034140157, -4.242640687119286547 ) ) ;
#6974=CARTESIAN_POINT ( 'NONE',  ( -5.000000000000005329, 53.33333333333333570, 8.660254037844387298 ) ) ;
#6981=ORIENTED_EDGE ( 'NONE', *, *, #37201, .F. ) ;
#6986=CARTESIAN_POINT ( 'NONE',  ( 7.347880794884121708E-16, 300.0000000000000000, -6.000000000000001776 ) ) ;
#6991=CARTESIAN_POINT ( 'NONE',  ( -7.320508075688773708, 171.8749999999999716, -7.320508075688774596 ) ) ;
#6995=CARTESIAN_POINT ( 'NONE',  ( -3.042071309553173730, 144.6354166632526983, 11.35316468749999785 ) ) ;
#6997=CARTESIAN_POINT ( 'NONE',  ( 10.00000000000000178, 26.87499999317203603, 0.000000000000000000 ) ) ;
#6999=CARTESIAN_POINT ( 'NONE',  ( 7.320508075688771044, 106.2499999931720396, 7.320508075688775484 ) ) ;
#7000=CARTESIAN_POINT ( 'NONE',  ( -2.679491924312266349, 168.5416666666666288, 9.999999999999408473 ) ) ;
#7005=CARTESIAN_POINT ( 'NONE',  ( 7.320508075688850091, 194.3750000000000853, 7.320508075688853644 ) ) ;
#7008=( BOUNDED_CURVE ( )  B_SPLINE_CURVE ( 2, ( #57153, #17518, #201, #5469, #63540, #34901, #566, #6582, #46561, #70323, #23178, #6215, #11865 ),
 .UNSPECIFIED., .F., .F. ) 
 B_SPLINE_CURVE_WITH_KNOTS ( ( 3, 2, 2, 2, 2, 2, 3 ),
 ( 0.1467391304347825942, 0.1485507246376811252, 0.1503623188405796840, 0.1521739130434782705, 0.1539855072463768015, 0.1557971014492753603, 0.1576086956521739191 ),
 .UNSPECIFIED. ) 
 CURVE ( )  GEOMETRIC_REPRESENTATION_ITEM ( )  RATIONAL_B_SPLINE_CURVE ( ( 1.000000000000000444, 0.9659258262890677571, 1.000000000000000000, 0.9659258262890683122, 1.000000000000000000, 0.9659258262890683122, 1.000000000000000000, 0.9659258262890683122, 1.000000000000000000, 0.9659258262890683122, 1.000000000000000000, 0.9659258262890683122, 1.000000000000000000 ) ) 
 REPRESENTATION_ITEM ( '' )  );
#7009=CARTESIAN_POINT ( 'NONE',  ( 10.00000000000000178, 36.87499999317203958, 0.000000000000000000 ) ) ;
#7017=CARTESIAN_POINT ( 'NONE',  ( -9.489952148308621105, 225.9999999999999716, -3.220591000268780313 ) ) ;
#7018=CARTESIAN_POINT ( 'NONE',  ( -10.00000000000005684, 62.70833333333337833, 2.679491924311237394 ) ) ;
#7020=CARTESIAN_POINT ( 'NONE',  ( -8.311093377946841443, 113.9062499965859985, 8.311093377946830785 ) ) ;
#7030=CARTESIAN_POINT ( 'NONE',  ( 11.35316468749999963, 115.9895833299193697, -3.042071309553165293 ) ) ;
#7033=CARTESIAN_POINT ( 'NONE',  ( 7.320508075688771044, 146.2499999931719969, 7.320508075688775484 ) ) ;
#7036=CARTESIAN_POINT ( 'NONE',  ( 2.679491924311228956, 197.9166666598386826, -10.00000000000000000 ) ) ;
#7039=CARTESIAN_POINT ( 'NONE',  ( -9.832129032723420536, 104.0104166632526841, 5.676582343749997150 ) ) ;
#7043=CARTESIAN_POINT ( 'NONE',  ( -5.676582343749998039, 12.76041666325268409, -9.832129032723420536 ) ) ;
#7047=CARTESIAN_POINT ( 'NONE',  ( 5.676582343749993598, 224.9479166632526983, 9.832129032723422313 ) ) ;
#7049=DIRECTION ( 'NONE',  ( -0.000000000000000000, 1.000000000000000000, -0.000000000000000000 ) ) ;
#7051=CARTESIAN_POINT ( 'NONE',  ( 6.676582343750001591, 293.9531250017069510, -8.176455196517173205E-16 ) ) ;
#7054=CARTESIAN_POINT ( 'NONE',  ( -11.35316468750000141, 203.8020833299193555, 3.042071309553159963 ) ) ;
#7063=CARTESIAN_POINT ( 'NONE',  ( 10.00000000000000000, 24.79166666666666785, 2.679491924311236062 ) ) ;
#7072=CARTESIAN_POINT ( 'NONE',  ( 2.295000000000000373, 267.1439999999997212, 5.415577408903852863 ) ) ;
#7073=CARTESIAN_POINT ( 'NONE',  ( -4.721056650415999201, 295.3281250017069510, -4.721056650415999201 ) ) ;
#7075=CARTESIAN_POINT ( 'NONE',  ( -1.836970198721029983E-15, 135.6249999931720538, 10.00000000000000178 ) ) ;
#7083=CARTESIAN_POINT ( 'NONE',  ( 3.042071309553167069, 107.1354166632526983, -11.35316468749999785 ) ) ;
#7092=DIRECTION ( 'NONE',  ( -0.000000000000000000, 1.000000000000000000, -0.000000000000000000 ) ) ;
#7093=CARTESIAN_POINT ( 'NONE',  ( -11.35316468750000141, 208.4895833299193555, 3.042071309553159963 ) ) ;
#7098=CARTESIAN_POINT ( 'NONE',  ( -8.311093377946841443, 184.2187499965860127, 8.311093377946830785 ) ) ;
#7105=CARTESIAN_POINT ( 'NONE',  ( 8.311093377946837890, 66.40624999658602690, -8.311093377946837890 ) ) ;
#7106=CYLINDRICAL_SURFACE ( 'NONE', #20711, 10.00000000000000178 ) ;
#7107=( BOUNDED_CURVE ( )  B_SPLINE_CURVE ( 2, ( #42421, #47350, #65439, #31488, #25436, #48453, #54511, #25806, #48826 ),
 .UNSPECIFIED., .F., .F. ) 
 B_SPLINE_CURVE_WITH_KNOTS ( ( 3, 2, 2, 2, 3 ),
 ( 0.4791666666666647423, 0.4895833333333313719, 0.4999999999999981126, 0.5104166666666647423, 0.5208333333333314830 ),
 .UNSPECIFIED. ) 
 CURVE ( )  GEOMETRIC_REPRESENTATION_ITEM ( )  RATIONAL_B_SPLINE_CURVE ( ( 1.000000000000014211, 0.9238795325112725276, 1.000000000000000000, 0.9238795325112867385, 1.000000000000000000, 0.9238795325112867385, 1.000000000000000000, 0.9238795325113005052, 0.9999999999999862332 ) ) 
 REPRESENTATION_ITEM ( '' )  );
#7110=CARTESIAN_POINT ( 'NONE',  ( -1.836970198721029983E-15, 140.6249999931720538, 10.00000000000000178 ) ) ;
#7112=CARTESIAN_POINT ( 'NONE',  ( 5.676582343749993598, 79.94791666325269830, 9.832129032723422313 ) ) ;
#7118=CARTESIAN_POINT ( 'NONE',  ( -11.35316468750000141, 68.28124999658602690, -1.390361679473963753E-15 ) ) ;
#7121=CARTESIAN_POINT ( 'NONE',  ( -8.660254037844387298, 158.9583333265053966, -5.000000000000004441 ) ) ;
#7123=CARTESIAN_POINT ( 'NONE',  ( 6.123233995736767268E-16, 21.25000000000000000, -10.00000000000000178 ) ) ;
#7124=CARTESIAN_POINT ( 'NONE',  ( 3.042071309553167513, 47.13541666325269119, -11.35316468749999785 ) ) ;
#7126=CARTESIAN_POINT ( 'NONE',  ( 3.042071309553167069, 196.8229166632526983, -11.35316468749999785 ) ) ;
#7132=CARTESIAN_POINT ( 'NONE',  ( -11.35316468750000141, 183.4895833299193839, 3.042071309553159963 ) ) ;
#7138=CARTESIAN_POINT ( 'NONE',  ( -11.35316468750000141, 173.5937499965860411, -1.390361679473963753E-15 ) ) ;
#7141=CARTESIAN_POINT ( 'NONE',  ( 9.086704206008372253, 225.9999999999998579, -6.074962670943044429 ) ) ;
#7142=ORIENTED_EDGE ( 'NONE', *, *, #16874, .T. ) ;
#7145=VECTOR ( 'NONE', #60610, 1000.000000000000000 ) ;
#7172=CARTESIAN_POINT ( 'NONE',  ( -10.00000000000000178, 137.5000000000000000, -1.224646799147353454E-15 ) ) ;
#7188=CARTESIAN_POINT ( 'NONE',  ( -2.085542519210945728E-15, 34.53124999658601979, 11.35316468750000141 ) ) ;
#7189=EDGE_CURVE ( 'NONE', #61945, #53587, #24487, .T. ) ;
#7190=CARTESIAN_POINT ( 'NONE',  ( 8.660254037844669739, 24.58333333333352400, 5.000000000000169642 ) ) ;
#7191=CARTESIAN_POINT ( 'NONE',  ( 5.676582343750001591, 216.9270833299193555, -9.832129032723420536 ) ) ;
#7195=CARTESIAN_POINT ( 'NONE',  ( -10.00000000000000355, 129.5833333265053966, 2.679491924311223183 ) ) ;
#7197=CARTESIAN_POINT ( 'NONE',  ( 9.832129032723420536, 31.19791666325268409, -5.676582343749999815 ) ) ;
#7203=CARTESIAN_POINT ( 'NONE',  ( 11.35316468749999963, 15.98958332991934661, -3.042071309553165293 ) ) ;
#7205=( BOUNDED_CURVE ( )  B_SPLINE_CURVE ( 2, ( #17943, #40584, #11913, #28887, #62466, #246, #6631, #5515, #52281 ),
 .UNSPECIFIED., .F., .F. ) 
 B_SPLINE_CURVE_WITH_KNOTS ( ( 3, 2, 2, 2, 3 ),
 ( 0.3958333333333313164, 0.4062499999999980016, 0.4166666666666647423, 0.4270833333333313719, 0.4374999999999980571 ),
 .UNSPECIFIED. ) 
 CURVE ( )  GEOMETRIC_REPRESENTATION_ITEM ( )  RATIONAL_B_SPLINE_CURVE ( ( 1.000000000000014655, 0.9238795325112720835, 1.000000000000000000, 0.9238795325112867385, 1.000000000000000000, 0.9238795325112867385, 1.000000000000000000, 0.9238795325113009493, 0.9999999999999857891 ) ) 
 REPRESENTATION_ITEM ( '' )  );
#7206=CARTESIAN_POINT ( 'NONE',  ( 6.951808397369818766E-16, 152.0312499965860411, -11.35316468750000141 ) ) ;
#7209=CARTESIAN_POINT ( 'NONE',  ( 7.320508075688774596, 112.4999999931720396, -7.320508075688774596 ) ) ;
#7213=ORIENTED_EDGE ( 'NONE', *, *, #53452, .F. ) ;
#7214=CARTESIAN_POINT ( 'NONE',  ( 8.311093377946837890, 11.71874999658601801, -8.311093377946837890 ) ) ;
#7219=DIRECTION ( 'NONE',  ( 0.000000000000000000, 0.000000000000000000, 1.000000000000000000 ) ) ;
#7220=CARTESIAN_POINT ( 'NONE',  ( -8.311093377946836114, 137.6562499965859843, -8.311093377946837890 ) ) ;
#7227=FACE_OUTER_BOUND ( 'NONE', #17870, .T. ) ;
#7229=CARTESIAN_POINT ( 'NONE',  ( -8.311093377946836114, 82.96874999658601268, -8.311093377946837890 ) ) ;
#7233=ORIENTED_EDGE ( 'NONE', *, *, #34980, .F. ) ;
#7254=AXIS2_PLACEMENT_3D ( 'NONE', #10434, #68886, #17198 ) ;
#7257=CARTESIAN_POINT ( 'NONE',  ( -2.679491924290171578, 31.45833333333144211, -10.00000000001215383 ) ) ;
#7258=CARTESIAN_POINT ( 'NONE',  ( -1.836970198721029983E-15, 93.75000000000000000, 10.00000000000000178 ) ) ;
#7261=CARTESIAN_POINT ( 'NONE',  ( -6.676582343750000703, 294.6718750017070079, 2.765530957082001251 ) ) ;
#7264=CARTESIAN_POINT ( 'NONE',  ( -4.999999999999998224, 173.5416666598387110, -8.660254037844389075 ) ) ;
#7267=CARTESIAN_POINT ( 'NONE',  ( 0.000000000000000000, 300.0000000000000000, 6.000000000000001776 ) ) ;
#7272=CARTESIAN_POINT ( 'NONE',  ( -1.836970198721029983E-15, 213.7500000000000284, 10.00000000000000178 ) ) ;
#7275=CARTESIAN_POINT ( 'NONE',  ( 6.951808397369818766E-16, 177.3437499965860411, -11.35316468750000141 ) ) ;
#7282=CARTESIAN_POINT ( 'NONE',  ( 3.042071309553159519, 45.05208332991935549, 11.35316468750000141 ) ) ;
#7284=CARTESIAN_POINT ( 'NONE',  ( -9.832129032723420536, 224.0104166632526983, 5.676582343749997150 ) ) ;
#7286=CARTESIAN_POINT ( 'NONE',  ( -3.673940397442060854E-16, 295.7500000000000000, -6.000000000000001776 ) ) ;
#7291=CARTESIAN_POINT ( 'NONE',  ( 4.999999999999993783, 71.04166665983869677, 8.660254037844390851 ) ) ;
#7294=CARTESIAN_POINT ( 'NONE',  ( -10.00000000000000711, 72.50000000000002842, -1.224646799147354243E-15 ) ) ;
#7298=ORIENTED_EDGE ( 'NONE', *, *, #35388, .T. ) ;
#7299=CARTESIAN_POINT ( 'NONE',  ( 6.676582343750004256, 298.0468750017070647, 2.765530957081995478 ) ) ;
#7301=CARTESIAN_POINT ( 'NONE',  ( -10.00000000000001066, 17.50000000000000355, -1.224646799147354637E-15 ) ) ;
#7302=CARTESIAN_POINT ( 'NONE',  ( 8.311093377946837890, 161.4062499965860411, -8.311093377946837890 ) ) ;
#7303=CARTESIAN_POINT ( 'NONE',  ( 6.123233995736767268E-16, 3.124999993172032919, -10.00000000000000178 ) ) ;
#7310=LINE ( 'NONE', #65749, #60544 ) ;
#7311=CARTESIAN_POINT ( 'NONE',  ( 9.832129032723420536, 146.5104166632526699, -5.676582343749999815 ) ) ;
#7315=CARTESIAN_POINT ( 'NONE',  ( -8.311093377946836114, 52.96874999658601268, -8.311093377946837890 ) ) ;
#7324=CARTESIAN_POINT ( 'NONE',  ( 4.242640687119287435, 293.4375000034140157, 4.242640687119285658 ) ) ;
#7326=FACE_OUTER_BOUND ( 'NONE', #5078, .T. ) ;
#7345=CARTESIAN_POINT ( 'NONE',  ( 4.242640687119287435, 296.3750000000000000, 4.242640687119285658 ) ) ;
#7347=CARTESIAN_POINT ( 'NONE',  ( 5.000000000000001776, 55.83333333333333570, -8.660254037844389075 ) ) ;
#7349=CARTESIAN_POINT ( 'NONE',  ( -3.673940397442060854E-16, 295.7500000000000000, -6.000000000000001776 ) ) ;
#7350=CARTESIAN_POINT ( 'NONE',  ( -4.242640687119286547, 287.9375000034140157, -4.242640687119286547 ) ) ;
#7353=EDGE_LOOP ( 'NONE', ( #15276, #50205, #5657, #5210 ) ) ;
#7357=CARTESIAN_POINT ( 'NONE',  ( 6.123233995736767268E-16, 73.12499999317203958, -10.00000000000000178 ) ) ;
#7361=CARTESIAN_POINT ( 'NONE',  ( 7.320508075688774596, 180.6250000000000284, -7.320508075688774596 ) ) ;
#7362=CARTESIAN_POINT ( 'NONE',  ( 6.000000000000001776, 297.5625000034140157, -7.347880794884121708E-16 ) ) ;
#7365=CARTESIAN_POINT ( 'NONE',  ( -11.35316468750000141, 138.5937499965860127, -1.390361679473963753E-15 ) ) ;
#7367=DIRECTION ( 'NONE',  ( -0.000000000000000000, -0.000000000000000000, 1.000000000000000000 ) ) ;
#7378=CARTESIAN_POINT ( 'NONE',  ( 2.679491924311228956, 37.91666665983870388, -10.00000000000000000 ) ) ;
#7387=CARTESIAN_POINT ( 'NONE',  ( 1.102182119232618108E-15, 292.3125000034140157, 6.000000000000001776 ) ) ;
#7391=CARTESIAN_POINT ( 'NONE',  ( 8.311093377946834337, 120.1562499965860127, 8.311093377946839666 ) ) ;
#7399=CARTESIAN_POINT ( 'NONE',  ( -5.676582343750006032, 114.1145833299193555, 9.832129032723418760 ) ) ;
#7403=CARTESIAN_POINT ( 'NONE',  ( -2.679491924311225848, 203.3333333265053966, -10.00000000000000178 ) ) ;
#7406=CARTESIAN_POINT ( 'NONE',  ( 8.311093377946834337, 100.4687499965860127, 8.311093377946839666 ) ) ;
#7410=CARTESIAN_POINT ( 'NONE',  ( -2.085542519210945728E-15, 14.84374999658601624, 11.35316468750000141 ) ) ;
#7419=CARTESIAN_POINT ( 'NONE',  ( -6.676582343750003368, 291.3906250017070079, -2.765530957081996810 ) ) ;
#7421=CARTESIAN_POINT ( 'NONE',  ( 3.042071309553159519, 225.0520833299193555, 11.35316468750000141 ) ) ;
#7428=ORIENTED_EDGE ( 'NONE', *, *, #15952, .F. ) ;
#7440=ADVANCED_FACE ( 'NONE', ( #37811 ), #10254, .T. ) ;
#7443=CARTESIAN_POINT ( 'NONE',  ( -2.765530957081998142, 290.6406250017069510, 6.676582343750000703 ) ) ;
#7454=CARTESIAN_POINT ( 'NONE',  ( -8.311093377946841443, 104.2187499965859985, 8.311093377946830785 ) ) ;
#7465=CARTESIAN_POINT ( 'NONE',  ( -5.676582343749998039, 217.4479166632526983, -9.832129032723420536 ) ) ;
#7469=CARTESIAN_POINT ( 'NONE',  ( 11.35316468749999785, 195.8854166632526415, 3.042071309553174174 ) ) ;
#7476=CARTESIAN_POINT ( 'NONE',  ( 6.951808397369818766E-16, 72.03124999658602690, -11.35316468750000141 ) ) ;
#7482=CARTESIAN_POINT ( 'NONE',  ( -9.832129032723418760, 72.86458332991935549, -5.676582343750004256 ) ) ;
#7488=CARTESIAN_POINT ( 'NONE',  ( -11.35316468749999785, 68.07291666325266988, -3.042071309553167957 ) ) ;
#7491=CARTESIAN_POINT ( 'NONE',  ( 10.00000000000000000, 156.6666666598386826, 2.679491924311236062 ) ) ;
#7494=CARTESIAN_POINT ( 'NONE',  ( -11.35316468749999785, 58.38541666325268409, -3.042071309553167957 ) ) ;
#7496=CARTESIAN_POINT ( 'NONE',  ( 3.042071309553159519, 189.7395833299193271, 11.35316468750000141 ) ) ;
#7500=CARTESIAN_POINT ( 'NONE',  ( 8.660254037844389075, 62.29166665983869677, -5.000000000000000000 ) ) ;
#7502=CARTESIAN_POINT ( 'NONE',  ( 8.311093377946834337, 190.1562499965860127, 8.311093377946839666 ) ) ;
#7507=CARTESIAN_POINT ( 'NONE',  ( 9.832129032723416984, 180.6770833299193555, 5.676582343750006032 ) ) ;
#7523=CARTESIAN_POINT ( 'NONE',  ( 7.347880794884121708E-16, 300.0000000000000000, -6.000000000000001776 ) ) ;
#7527=VERTEX_POINT ( 'NONE', #62665 ) ;
#7529=CARTESIAN_POINT ( 'NONE',  ( -2.679491924286246718, 156.4583333333312396, -10.00000000001463540 ) ) ;
#7532=ORIENTED_EDGE ( 'NONE', *, *, #24290, .T. ) ;
#7540=CARTESIAN_POINT ( 'NONE',  ( 6.676582343750002480, 294.1718750017070079, -2.765530957081997254 ) ) ;
#7541=CARTESIAN_POINT ( 'NONE',  ( -2.679491924311225848, 131.4583333333333428, -10.00000000000000178 ) ) ;
#7543=ADVANCED_FACE ( 'NONE', ( #68335 ), #39298, .T. ) ;
#7557=CARTESIAN_POINT ( 'NONE',  ( -9.832129032723418760, 32.86458332991935549, -5.676582343750004256 ) ) ;
#7559=CARTESIAN_POINT ( 'NONE',  ( -7.320508075688773708, 13.74999999317203070, -7.320508075688774596 ) ) ;
#7566=CARTESIAN_POINT ( 'NONE',  ( 11.35316468749999963, 35.98958332991933418, -3.042071309553165293 ) ) ;
#7572=CARTESIAN_POINT ( 'NONE',  ( -2.085542519210945728E-15, 39.53124999658601268, 11.35316468750000141 ) ) ;
#7574=CARTESIAN_POINT ( 'NONE',  ( 11.35316468749999785, 145.5729166632527267, 3.042071309553174174 ) ) ;
#7575=CARTESIAN_POINT ( 'NONE',  ( -10.00000000000000178, 119.3749999931720396, -1.224646799147353454E-15 ) ) ;
#7576=ADVANCED_FACE ( 'NONE', ( #56658 ), #28710, .T. ) ;
#7581=CARTESIAN_POINT ( 'NONE',  ( -11.35316468750000141, 23.80208332991935194, 3.042071309553159963 ) ) ;
#7585=CARTESIAN_POINT ( 'NONE',  ( 6.951808397369818766E-16, 152.0312499965860411, -11.35316468750000141 ) ) ;
#7593=CARTESIAN_POINT ( 'NONE',  ( 11.35316468750000141, 86.09374999658601268, 0.000000000000000000 ) ) ;
#7603=CARTESIAN_POINT ( 'NONE',  ( -1.836970198721029983E-15, 160.6249999931720254, 10.00000000000000178 ) ) ;
#7609=VECTOR ( 'NONE', #60755, 1000.000000000000000 ) ;
#7625=CARTESIAN_POINT ( 'NONE',  ( -8.660254037844387298, 97.08333333333334281, -5.000000000000004441 ) ) ;
#7627=CARTESIAN_POINT ( 'NONE',  ( -6.676582343750003368, 297.5468750017069510, -2.765530957081996810 ) ) ;
#7633=EDGE_CURVE ( 'NONE', #21472, #37922, #20080, .T. ) ;
#7636=CARTESIAN_POINT ( 'NONE',  ( -7.320508075688779925, 53.12500000000001421, 7.320508075688771044 ) ) ;
#7641=CARTESIAN_POINT ( 'NONE',  ( 10.00000000000000178, 210.0000000000000284, 0.000000000000000000 ) ) ;
#7644=CARTESIAN_POINT ( 'NONE',  ( 5.676582343749993598, 185.2604166632526983, 9.832129032723422313 ) ) ;
#7652=CARTESIAN_POINT ( 'NONE',  ( 3.042071309553167069, 47.13541666325268409, -11.35316468749999785 ) ) ;
#7654=CARTESIAN_POINT ( 'NONE',  ( 11.35316468750000141, 216.0937499965860411, 0.000000000000000000 ) ) ;
#7660=CARTESIAN_POINT ( 'NONE',  ( -3.042071309553173730, 104.3229166632526983, 11.35316468749999785 ) ) ;
#7661=CARTESIAN_POINT ( 'NONE',  ( -8.660254037844390851, 79.79166665983871098, 4.999999999999998224 ) ) ;
#7669=CARTESIAN_POINT ( 'NONE',  ( 6.676582343750003368, 294.1718750017070079, -2.765530957081997254 ) ) ;
#7671=CARTESIAN_POINT ( 'NONE',  ( -11.35316468749999785, 153.0729166632527267, -3.042071309553167513 ) ) ;
#7679=CARTESIAN_POINT ( 'NONE',  ( -8.311093377946836114, 147.9687499965860127, -8.311093377946837890 ) ) ;
#7681=CARTESIAN_POINT ( 'NONE',  ( 6.000000000000001776, 298.5625000034140157, -7.347880794884121708E-16 ) ) ;
#7683=CARTESIAN_POINT ( 'NONE',  ( 11.35316468750000141, 56.09374999658601979, 0.000000000000000000 ) ) ;
#7690=CARTESIAN_POINT ( 'NONE',  ( 2.485281374238575314, 293.3750000034140157, 6.000000000000000888 ) ) ;
#7706=CARTESIAN_POINT ( 'NONE',  ( 0.000000000000000000, 300.0000000000000000, 0.000000000000000000 ) ) ;
#7708=EDGE_LOOP ( 'NONE', ( #30168, #37672, #4545 ) ) ;
#7716=CARTESIAN_POINT ( 'NONE',  ( 2.679491924311222739, 53.95833333333333570, 10.00000000000000355 ) ) ;
#7719=CARTESIAN_POINT ( 'NONE',  ( 6.000000000000001776, 297.5000000000000000, -7.347880794884121708E-16 ) ) ;
#7720=CYLINDRICAL_SURFACE ( 'NONE', #30963, 10.00000000000000178 ) ;
#7728=CARTESIAN_POINT ( 'NONE',  ( 8.660254037844389075, 170.4166666666666856, -5.000000000000000000 ) ) ;
#7732=CARTESIAN_POINT ( 'NONE',  ( -9.832129032723418760, 143.1770833299193555, -5.676582343750004256 ) ) ;
#7734=CARTESIAN_POINT ( 'NONE',  ( 6.123233995736767268E-16, 28.12499999317203603, -10.00000000000000178 ) ) ;
#7739=CARTESIAN_POINT ( 'NONE',  ( 5.676582343750001591, 6.927083329919350163, -9.832129032723420536 ) ) ;
#7741=CARTESIAN_POINT ( 'NONE',  ( -2.679491924311226292, 88.33333332650536818, -10.00000000000000178 ) ) ;
#7745=CARTESIAN_POINT ( 'NONE',  ( 4.999999999999993783, 31.04166665983870033, 8.660254037844390851 ) ) ;
#7752=CARTESIAN_POINT ( 'NONE',  ( 10.00000000000000178, 6.874999993172033363, 0.000000000000000000 ) ) ;
#7759=CARTESIAN_POINT ( 'NONE',  ( 6.951808397369818766E-16, 117.0312499965860269, -11.35316468750000141 ) ) ;
#7760=VERTEX_POINT ( 'NONE', #59890 ) ;
#7766=CARTESIAN_POINT ( 'NONE',  ( -9.999999999999996447, 182.2916666666666856, -2.679491924311229401 ) ) ;
#7767=CARTESIAN_POINT ( 'NONE',  ( -11.35316468750000141, 118.2812499965860269, -1.390361679473963753E-15 ) ) ;
#7769=CARTESIAN_POINT ( 'NONE',  ( 2.679491924311228956, 82.91666665983871098, -10.00000000000000000 ) ) ;
#7771=CARTESIAN_POINT ( 'NONE',  ( 8.660254037844385522, 211.4583333265053682, 5.000000000000005329 ) ) ;
#7774=CARTESIAN_POINT ( 'NONE',  ( 11.35316468749999785, 100.8854166632526841, 3.042071309553174174 ) ) ;
#7778=CARTESIAN_POINT ( 'NONE',  ( -5.676582343749998039, 7.760416663252684089, -9.832129032723420536 ) ) ;
#7782=CARTESIAN_POINT ( 'NONE',  ( 7.320508075688771044, 116.2499999931720254, 7.320508075688775484 ) ) ;
#7784=VECTOR ( 'NONE', #18308, 1000.000000000000227 ) ;
#7786=CARTESIAN_POINT ( 'NONE',  ( 7.320508075688774596, 200.6250000000000000, -7.320508075688774596 ) ) ;
#7787=CARTESIAN_POINT ( 'NONE',  ( 2.765530957082001251, 292.7656250017069510, 6.676582343750000703 ) ) ;
#7789=CARTESIAN_POINT ( 'NONE',  ( -5.676582343749998039, 217.7604166632526983, -9.832129032723420536 ) ) ;
#7793=ADVANCED_FACE ( 'NONE', ( #48553 ), #20250, .T. ) ;
#7806=CARTESIAN_POINT ( 'NONE',  ( -8.660254037844387298, 28.95833332650536818, -5.000000000000004441 ) ) ;
#7808=CARTESIAN_POINT ( 'NONE',  ( 0.4589999999999999636, 278.5679999999998699, 5.805293472045523373 ) ) ;
#7809=CARTESIAN_POINT ( 'NONE',  ( -2.765530957081996810, 294.2656250017069510, -6.676582343750002480 ) ) ;
#7819=CARTESIAN_POINT ( 'NONE',  ( 8.311093377946837890, 101.7187499965860269, -8.311093377946837890 ) ) ;
#7827=CARTESIAN_POINT ( 'NONE',  ( -8.311093377946841443, 213.9062499965860411, 8.311093377946830785 ) ) ;
#7831=CARTESIAN_POINT ( 'NONE',  ( 9.832129032723416984, 190.6770833299193555, 5.676582343750006032 ) ) ;
#7833=CARTESIAN_POINT ( 'NONE',  ( -4.242640687119285658, 296.1875000034139589, 4.242640687119287435 ) ) ;
#7838=CARTESIAN_POINT ( 'NONE',  ( 11.35316468749999963, 80.98958332991934128, -3.042071309553165293 ) ) ;
#7839=CARTESIAN_POINT ( 'NONE',  ( 5.000000000000006217, 140.8333333333333428, -8.660254037844396180 ) ) ;
#7842=CARTESIAN_POINT ( 'NONE',  ( 1.425702245604163669E-12, 48.75000000000012079, 10.00000000000000178 ) ) ;
#7844=CARTESIAN_POINT ( 'NONE',  ( 9.832129032723420536, 71.19791666325268409, -5.676582343749999815 ) ) ;
#7851=CARTESIAN_POINT ( 'NONE',  ( 3.042071309553159519, 69.73958332991936970, 11.35316468750000141 ) ) ;
#7852=AXIS2_PLACEMENT_3D ( 'NONE', #52348, #29702, #41026 ) ;
#7855=( BOUNDED_CURVE ( )  B_SPLINE_CURVE ( 2, ( #36749, #37116, #54101, #31456, #25772, #2786, #2413, #25408, #48422 ),
 .UNSPECIFIED., .F., .F. ) 
 B_SPLINE_CURVE_WITH_KNOTS ( ( 3, 2, 2, 2, 3 ),
 ( 0.3958333333333313164, 0.4062499999999980016, 0.4166666666666647423, 0.4270833333333313719, 0.4374999999999980571 ),
 .UNSPECIFIED. ) 
 CURVE ( )  GEOMETRIC_REPRESENTATION_ITEM ( )  RATIONAL_B_SPLINE_CURVE ( ( 1.000000000000014655, 0.9238795325112720835, 1.000000000000000000, 0.9238795325112867385, 1.000000000000000000, 0.9238795325112867385, 1.000000000000000000, 0.9238795325113009493, 0.9999999999999857891 ) ) 
 REPRESENTATION_ITEM ( '' )  );
#7858=CARTESIAN_POINT ( 'NONE',  ( -10.00000000000000178, 169.3749999931720538, -1.224646799147353454E-15 ) ) ;
#7860=VECTOR ( 'NONE', #20895, 1000.000000000000000 ) ;
#7862=CARTESIAN_POINT ( 'NONE',  ( 3.042071309553167513, 62.13541666325268409, -11.35316468749999785 ) ) ;
#7864=CARTESIAN_POINT ( 'NONE',  ( 3.042071309553159519, 194.7395833299193555, 11.35316468750000141 ) ) ;
#7867=CARTESIAN_POINT ( 'NONE',  ( 8.660254037844385522, 161.4583333265053966, 5.000000000000005329 ) ) ;
#7869=CARTESIAN_POINT ( 'NONE',  ( -5.676582343749998039, 192.4479166632526983, -9.832129032723420536 ) ) ;
#7870=DIRECTION ( 'NONE',  ( 0.000000000000000000, 0.000000000000000000, 1.000000000000000000 ) ) ;
#7875=CARTESIAN_POINT ( 'NONE',  ( -3.042071309553173730, 179.6354166632526699, 11.35316468749999785 ) ) ;
#7882=CARTESIAN_POINT ( 'NONE',  ( 8.660254037844389075, 5.416666666666666963, -5.000000000000000000 ) ) ;
#7887=ORIENTED_EDGE ( 'NONE', *, *, #10091, .F. ) ;
#7891=CARTESIAN_POINT ( 'NONE',  ( 6.123233995736767268E-16, 188.1249999931720254, -10.00000000000000178 ) ) ;
#7898=ORIENTED_EDGE ( 'NONE', *, *, #39415, .T. ) ;
#7900=CARTESIAN_POINT ( 'NONE',  ( -10.00000000000000355, 114.5833333265053540, 2.679491924311223183 ) ) ;
#7903=CARTESIAN_POINT ( 'NONE',  ( -4.088227598258586603E-16, 295.3593750017070079, -6.676582343750001591 ) ) ;
#7904=CARTESIAN_POINT ( 'NONE',  ( -7.320508075688778149, 153.1250000000000284, 7.320508075688769267 ) ) ;
#7917=CARTESIAN_POINT ( 'NONE',  ( 6.000000000000003553, 288.6250000034139589, -2.485281374238571761 ) ) ;
#7920=CARTESIAN_POINT ( 'NONE',  ( 11.35316468750000141, 30.78124999658601979, 0.000000000000000000 ) ) ;
#7921=CARTESIAN_POINT ( 'NONE',  ( 10.00000000000000533, 150.2083333333333428, -2.679491924311227624 ) ) ;
#7922=CARTESIAN_POINT ( 'NONE',  ( 2.679491924311222739, 10.83333332650536818, 10.00000000000000355 ) ) ;
#7923=PLANE ( 'NONE',  #46399 ) ;
#7927=EDGE_CURVE ( 'NONE', #42303, #29697, #54988, .T. ) ;
#7929=DIRECTION ( 'NONE',  ( -0.000000000000000000, 1.000000000000000000, -0.000000000000000000 ) ) ;
#7930=CARTESIAN_POINT ( 'NONE',  ( 8.311093377946837890, 31.40624999658601624, -8.311093377946837890 ) ) ;
#7936=CARTESIAN_POINT ( 'NONE',  ( 5.676582343750001591, 26.61458332991935194, -9.832129032723420536 ) ) ;
#7938=CARTESIAN_POINT ( 'NONE',  ( -11.35316468749999785, 148.0729166632527267, -3.042071309553167513 ) ) ;
#7939=CARTESIAN_POINT ( 'NONE',  ( -4.999999999999998224, 123.5416666598387110, -8.660254037844389075 ) ) ;
#7941=CARTESIAN_POINT ( 'NONE',  ( 8.660254037844389075, 172.2916666598387110, -5.000000000000000000 ) ) ;
#7945=CARTESIAN_POINT ( 'NONE',  ( 3.042071309553167513, 27.13541666325268409, -11.35316468749999785 ) ) ;
#7950=CARTESIAN_POINT ( 'NONE',  ( -3.042071309553173730, 154.3229166632526983, 11.35316468749999785 ) ) ;
#7962=CARTESIAN_POINT ( 'NONE',  ( -8.311093377946841443, 99.21874999658601268, 8.311093377946830785 ) ) ;
#7975=DIRECTION ( 'NONE',  ( -0.000000000000000000, 1.000000000000000000, -0.000000000000000000 ) ) ;
#7992=CARTESIAN_POINT ( 'NONE',  ( -8.660254037844390851, 102.9166666666666714, 4.999999999999998224 ) ) ;
#7994=CARTESIAN_POINT ( 'NONE',  ( 2.765530957081996366, 297.2968750017070079, -6.676582343750003368 ) ) ;
#7996=CARTESIAN_POINT ( 'NONE',  ( -10.00000000000000355, 144.5833333265053682, 2.679491924311223183 ) ) ;
#7999=CARTESIAN_POINT ( 'NONE',  ( -8.660254037844387298, 183.9583333265053682, -5.000000000000004441 ) ) ;
#8003=CARTESIAN_POINT ( 'NONE',  ( -2.679491924311235618, 218.5416666666667140, 10.00000000000000000 ) ) ;
#8005=CARTESIAN_POINT ( 'NONE',  ( -3.042071309553173730, 189.6354166632526983, 11.35316468749999785 ) ) ;
#8006=CARTESIAN_POINT ( 'NONE',  ( 5.000000000000001776, 192.7083333265053966, -8.660254037844389075 ) ) ;
#8014=CARTESIAN_POINT ( 'NONE',  ( -11.35316468750000141, 43.59374999658601979, -1.390361679473963753E-15 ) ) ;
#8016=CARTESIAN_POINT ( 'NONE',  ( 3.042071309553159519, 215.0520833299193555, 11.35316468750000141 ) ) ;
#8021=CARTESIAN_POINT ( 'NONE',  ( -8.311093377946836114, 107.6562499965860127, -8.311093377946837890 ) ) ;
#8023=CARTESIAN_POINT ( 'NONE',  ( -5.000000000000005329, 80.20833332650536818, 8.660254037844387298 ) ) ;
#8030=CARTESIAN_POINT ( 'NONE',  ( -2.765530957081996810, 292.4218750017069510, -6.676582343750003368 ) ) ;
#8032=CARTESIAN_POINT ( 'NONE',  ( -8.311093377946841443, 163.9062499965859843, 8.311093377946830785 ) ) ;
#8034=CARTESIAN_POINT ( 'NONE',  ( 2.679491924328703423, 6.041666666665100216, -9.999999999989912070 ) ) ;
#8036=CARTESIAN_POINT ( 'NONE',  ( -2.679491924305053896, 191.4583333333328312, -10.00000000000361489 ) ) ;
#8038=EDGE_LOOP ( 'NONE', ( #33889, #46854, #40984, #1788 ) ) ;
#8042=CARTESIAN_POINT ( 'NONE',  ( -8.311093377946841443, 139.2187499965859843, 8.311093377946834337 ) ) ;
#8044=CARTESIAN_POINT ( 'NONE',  ( -6.000000000000003553, 290.9375000000000568, -2.485281374238571317 ) ) ;
#8046=CARTESIAN_POINT ( 'NONE',  ( -5.676582343749998039, 57.76041666325268409, -9.832129032723420536 ) ) ;
#8054=CARTESIAN_POINT ( 'NONE',  ( 1.102182119232618108E-15, 291.3125000034140157, 6.000000000000001776 ) ) ;
#8062=CARTESIAN_POINT ( 'NONE',  ( -7.320508075688773708, 63.74999999317203248, -7.320508075688774596 ) ) ;
#8068=( BOUNDED_CURVE ( )  B_SPLINE_CURVE ( 2, ( #65147, #42873, #14198, #37235, #20987, #27027, #39100, #49284, #33456, #9306, #4398, #27766, #15697 ),
 .UNSPECIFIED., .F., .F. ) 
 B_SPLINE_CURVE_WITH_KNOTS ( ( 3, 2, 2, 2, 2, 2, 3 ),
 ( 0.9076086956521738358, 0.9094202898550723946, 0.9112318840579709534, 0.9130434782608694011, 0.9148550724637680709, 0.9166666666666666297, 0.9184782608695651884 ),
 .UNSPECIFIED. ) 
 CURVE ( )  GEOMETRIC_REPRESENTATION_ITEM ( )  RATIONAL_B_SPLINE_CURVE ( ( 1.000000000000001998, 0.9659258262890662028, 1.000000000000000000, 0.9659258262890683122, 1.000000000000000000, 0.9659258262890683122, 1.000000000000000000, 0.9659258262890683122, 1.000000000000000000, 0.9659258262890683122, 1.000000000000000000, 0.9659258262890683122, 1.000000000000000000 ) ) 
 REPRESENTATION_ITEM ( '' )  );
#8072=FACE_OUTER_BOUND ( 'NONE', #33367, .T. ) ;
#8077=CARTESIAN_POINT ( 'NONE',  ( -7.320508075688779037, 203.1249999999999716, 7.320508075688769267 ) ) ;
#8080=CARTESIAN_POINT ( 'NONE',  ( 10.00000000000000178, 55.00000000000000000, 0.000000000000000000 ) ) ;
#8082=CARTESIAN_POINT ( 'NONE',  ( -6.000000000000001776, 297.0000000000000000, 0.000000000000000000 ) ) ;
#8088=DIRECTION ( 'NONE',  ( -0.000000000000000000, 1.000000000000000000, -0.000000000000000000 ) ) ;
#8089=CARTESIAN_POINT ( 'NONE',  ( 6.123233995736767268E-16, 131.2500000000000000, -10.00000000000000178 ) ) ;
#8092=CARTESIAN_POINT ( 'NONE',  ( -2.679491924311225848, 171.4583333333332860, -10.00000000000000178 ) ) ;
#8096=CARTESIAN_POINT ( 'NONE',  ( -9.832129032723420536, 154.0104166632526983, 5.676582343749997150 ) ) ;
#8101=CARTESIAN_POINT ( 'NONE',  ( -2.222453528114265639E-12, 168.7499999999998295, 10.00000000000000178 ) ) ;
#8104=CARTESIAN_POINT ( 'NONE',  ( 3.042071309553167069, 7.135416663252682312, -11.35316468749999785 ) ) ;
#8111=CARTESIAN_POINT ( 'NONE',  ( -10.00000000000000000, 34.16666665983870388, -2.679491924311229845 ) ) ;
#8117=CARTESIAN_POINT ( 'NONE',  ( 2.679491924311228956, 7.916666659838700326, -10.00000000000000000 ) ) ;
#8118=VERTEX_POINT ( 'NONE', #16451 ) ;
#8123=CARTESIAN_POINT ( 'NONE',  ( -8.311093377946841443, 123.9062499965860411, 8.311093377946830785 ) ) ;
#8130=CARTESIAN_POINT ( 'NONE',  ( 2.679491924311228956, 43.95833333333335702, 10.00000000000002842 ) ) ;
#8131=CARTESIAN_POINT ( 'NONE',  ( 9.832129032723420536, 111.1979166632526983, -5.676582343749999815 ) ) ;
#8133=CARTESIAN_POINT ( 'NONE',  ( -1.836970198721029983E-15, 145.6249999931720538, 10.00000000000000178 ) ) ;
#8135=CARTESIAN_POINT ( 'NONE',  ( -4.999999999999998224, 213.5416666598387110, -8.660254037844389075 ) ) ;
#8136=EDGE_CURVE ( 'NONE', #59562, #18479, #56845, .T. ) ;
#8137=CARTESIAN_POINT ( 'NONE',  ( 0.000000000000000000, 284.0000000000000000, 0.000000000000000000 ) ) ;
#8139=CARTESIAN_POINT ( 'NONE',  ( -9.832129032723418760, 103.1770833299193555, -5.676582343750004256 ) ) ;
#8143=CARTESIAN_POINT ( 'NONE',  ( 6.951808397369818766E-16, 12.34374999658601801, -11.35316468750000141 ) ) ;
#8150=CARTESIAN_POINT ( 'NONE',  ( 6.676582343750001591, 291.9531250017069510, -8.176455196517173205E-16 ) ) ;
#8151=CARTESIAN_POINT ( 'NONE',  ( 8.660254037844385522, 126.4583333265053540, 5.000000000000005329 ) ) ;
#8152=CARTESIAN_POINT ( 'NONE',  ( 3.042071309553159519, 220.0520833299193271, 11.35316468750000141 ) ) ;
#8153=CARTESIAN_POINT ( 'NONE',  ( 5.676582343750001591, 126.9270833299193697, -9.832129032723420536 ) ) ;
#8162=AXIS2_PLACEMENT_3D ( 'NONE', #35710, #17980, #52689 ) ;
#8166=( BOUNDED_CURVE ( )  B_SPLINE_CURVE ( 2, ( #40005, #5678, #10964, #34, #33999, #62263, #28309, #5307, #52438 ),
 .UNSPECIFIED., .F., .F. ) 
 B_SPLINE_CURVE_WITH_KNOTS ( ( 3, 2, 2, 2, 3 ),
 ( 0.5208333333333314830, 0.5312499999999981126, 0.5416666666666647423, 0.5520833333333314830, 0.5624999999999981126 ),
 .UNSPECIFIED. ) 
 CURVE ( )  GEOMETRIC_REPRESENTATION_ITEM ( )  RATIONAL_B_SPLINE_CURVE ( ( 1.000000000000013767, 0.9238795325112729717, 1.000000000000000000, 0.9238795325112867385, 1.000000000000000000, 0.9238795325112867385, 1.000000000000000000, 0.9238795325113005052, 0.9999999999999862332 ) ) 
 REPRESENTATION_ITEM ( '' )  );
#8169=CYLINDRICAL_SURFACE ( 'NONE', #49932, 6.000000000000001776 ) ;
#8172=CARTESIAN_POINT ( 'NONE',  ( 4.721056650415999201, 293.0781250017069510, -4.721056650415999201 ) ) ;
#8173=CARTESIAN_POINT ( 'NONE',  ( 8.660254037844389075, 132.2916666598387110, -5.000000000000000000 ) ) ;
#8184=CARTESIAN_POINT ( 'NONE',  ( -8.311093377946841443, 99.21874999658601268, 8.311093377946830785 ) ) ;
#8193=CARTESIAN_POINT ( 'NONE',  ( -3.042071309553164404, 207.2395833299193555, -11.35316468749999963 ) ) ;
#8197=CARTESIAN_POINT ( 'NONE',  ( -2.085542519210945728E-15, 199.8437499965860127, 11.35316468750000141 ) ) ;
#8204=CARTESIAN_POINT ( 'NONE',  ( 3.042071309553167069, 81.82291666325268409, -11.35316468749999785 ) ) ;
#8207=CARTESIAN_POINT ( 'NONE',  ( 10.00000000000001243, 140.2083333333333428, -2.679491924311229401 ) ) ;
#8211=CARTESIAN_POINT ( 'NONE',  ( -11.35316468749999785, 73.07291666325268409, -3.042071309553167513 ) ) ;
#8218=CARTESIAN_POINT ( 'NONE',  ( 5.676582343749993598, 74.94791666325269830, 9.832129032723422313 ) ) ;
#8220=AXIS2_PLACEMENT_3D ( 'NONE', #48900, #14941, #26639 ) ;
#8222=CARTESIAN_POINT ( 'NONE',  ( -10.00000000000000178, 174.3749999931720538, -1.224646799147353454E-15 ) ) ;
#8226=CARTESIAN_POINT ( 'NONE',  ( -11.35316468750000141, 63.59374999658601268, -1.390361679473963753E-15 ) ) ;
#8227=CARTESIAN_POINT ( 'NONE',  ( 4.721056650416000089, 298.8281250017069510, 4.721056650415999201 ) ) ;
#8229=CARTESIAN_POINT ( 'NONE',  ( -9.832129032723418760, 197.8645833299193555, -5.676582343750004256 ) ) ;
#8234=CARTESIAN_POINT ( 'NONE',  ( -8.311093377946841443, 188.9062499965860127, 8.311093377946834337 ) ) ;
#8239=CARTESIAN_POINT ( 'NONE',  ( -2.085542519210945728E-15, 184.8437499965860411, 11.35316468750000141 ) ) ;
#8260=ORIENTED_EDGE ( 'NONE', *, *, #24640, .F. ) ;
#8262=CARTESIAN_POINT ( 'NONE',  ( 9.832129032723416984, 55.67708332991935549, 5.676582343750006032 ) ) ;
#8267=CARTESIAN_POINT ( 'NONE',  ( -6.676582343749999815, 292.6718750017069510, 2.765530957082001251 ) ) ;
#8268=CARTESIAN_POINT ( 'NONE',  ( 2.679491924311222739, 143.9583333333333712, 10.00000000000000355 ) ) ;
#8271=CARTESIAN_POINT ( 'NONE',  ( -2.679491924311226292, 163.3333333265053682, -10.00000000000000178 ) ) ;
#8281=CARTESIAN_POINT ( 'NONE',  ( -10.00000000000000178, 19.37499999317203603, -1.224646799147353454E-15 ) ) ;
#8283=CARTESIAN_POINT ( 'NONE',  ( 10.00000000000000355, 134.7916666666666288, 2.679491924311236506 ) ) ;
#8287=CARTESIAN_POINT ( 'NONE',  ( -5.676582343749998039, 42.44791666325269119, -9.832129032723420536 ) ) ;
#8289=CARTESIAN_POINT ( 'NONE',  ( -10.00000000000000000, 4.166666659838700326, -2.679491924311229845 ) ) ;
#8292=FACE_OUTER_BOUND ( 'NONE', #26987, .T. ) ;
#8294=CARTESIAN_POINT ( 'NONE',  ( 5.676582343750001591, 41.61458332991934839, -9.832129032723420536 ) ) ;
#8300=CARTESIAN_POINT ( 'NONE',  ( -8.311093377946841443, 38.90624999658600558, 8.311093377946834337 ) ) ;
#8302=CARTESIAN_POINT ( 'NONE',  ( 11.35316468749999963, 165.9895833299193271, -3.042071309553165293 ) ) ;
#8303=( BOUNDED_CURVE ( )  B_SPLINE_CURVE ( 2, ( #55000, #73452, #21758, #16091, #8343, #53271, #58568, #25312, #24583, #25681, #48329, #41935, #59667 ),
 .UNSPECIFIED., .F., .F. ) 
 B_SPLINE_CURVE_WITH_KNOTS ( ( 3, 2, 2, 2, 2, 2, 3 ),
 ( 0.2668949058765136551, 0.2721276204148235789, 0.2773603349531335027, 0.2825930494914434266, 0.2878257640297532949, 0.2930584785680632742, 0.2982911931063731426 ),
 .UNSPECIFIED. ) 
 CURVE ( )  GEOMETRIC_REPRESENTATION_ITEM ( )  RATIONAL_B_SPLINE_CURVE ( ( 1.000000000000000444, 0.9659258262890677571, 1.000000000000000000, 0.9659258262890683122, 1.000000000000000000, 0.9659258262890683122, 1.000000000000000000, 0.9659258262890683122, 1.000000000000000000, 0.9659258262890683122, 1.000000000000000000, 0.9659258262893742897, 0.9999999999996940225 ) ) 
 REPRESENTATION_ITEM ( '' )  );
#8305=CARTESIAN_POINT ( 'NONE',  ( -8.660254037844390851, 124.7916666598387110, 4.999999999999998224 ) ) ;
#8309=CARTESIAN_POINT ( 'NONE',  ( -8.311093377946836114, 27.96874999658601624, -8.311093377946837890 ) ) ;
#8311=DIRECTION ( 'NONE',  ( 0.000000000000000000, 0.000000000000000000, 1.000000000000000000 ) ) ;
#8315=CARTESIAN_POINT ( 'NONE',  ( 9.832129032723420536, 156.1979166632526983, -5.676582343749999815 ) ) ;
#8318=CARTESIAN_POINT ( 'NONE',  ( 4.529167459315944555, 225.9997407208379911, 8.915528146188176351 ) ) ;
#8321=ORIENTED_EDGE ( 'NONE', *, *, #54723, .F. ) ;
#8323=LINE ( 'NONE', #20377, #7609 ) ;
#8325=CARTESIAN_POINT ( 'NONE',  ( -5.676582343750006032, 99.42708332991935549, 9.832129032723418760 ) ) ;
#8335=ADVANCED_FACE ( 'NONE', ( #29288 ), #52298, .T. ) ;
#8343=CARTESIAN_POINT ( 'NONE',  ( -8.660254037844671515, 22.08333333333352400, -5.000000000000169642 ) ) ;
#8354=CARTESIAN_POINT ( 'NONE',  ( -7.320508075688774596, 33.12500000000000000, 7.320508075688766603 ) ) ;
#8355=CARTESIAN_POINT ( 'NONE',  ( 10.00000000000000178, 105.2083333333333286, -2.679491924311226736 ) ) ;
#8357=EDGE_CURVE ( 'NONE', #9076, #31698, #35093, .T. ) ;
#8359=CARTESIAN_POINT ( 'NONE',  ( -4.088227598258586603E-16, 294.3593750017070079, -6.676582343750001591 ) ) ;
#8361=CARTESIAN_POINT ( 'NONE',  ( 2.679491924317424001, 191.0416666666661456, -9.999999999996470379 ) ) ;
#8365=CARTESIAN_POINT ( 'NONE',  ( -10.00000000000000000, 184.1666666598386826, -2.679491924311229845 ) ) ;
#8370=CARTESIAN_POINT ( 'NONE',  ( 11.35316468749999963, 5.989583329919348387, -3.042071309553165293 ) ) ;
#8372=CARTESIAN_POINT ( 'NONE',  ( 9.832129032723420536, 191.5104166632526983, -5.676582343749999815 ) ) ;
#8381=CARTESIAN_POINT ( 'NONE',  ( 11.35316468749999785, 45.88541666325268409, 3.042071309553174174 ) ) ;
#8386=CARTESIAN_POINT ( 'NONE',  ( 3.170472398252169882E-12, 128.7500000000002558, 10.00000000000000178 ) ) ;
#8390=CARTESIAN_POINT ( 'NONE',  ( -2.085542519210945728E-15, 114.5312499965860269, 11.35316468750000141 ) ) ;
#8391=CARTESIAN_POINT ( 'NONE',  ( -7.320508075688773708, 88.74999999317202537, -7.320508075688774596 ) ) ;
#8396=ORIENTED_EDGE ( 'NONE', *, *, #6738, .F. ) ;
#8397=CARTESIAN_POINT ( 'NONE',  ( -2.594511375997793134, 225.9999999999999716, -9.679871326005304866 ) ) ;
#8400=CARTESIAN_POINT ( 'NONE',  ( 2.765530957081996366, 293.2968750017069510, -6.676582343750003368 ) ) ;
#8403=CARTESIAN_POINT ( 'NONE',  ( -5.676582343750006032, 174.1145833299193555, 9.832129032723418760 ) ) ;
#8411=CARTESIAN_POINT ( 'NONE',  ( -2.085542519210945728E-15, 139.8437499965860127, 11.35316468750000141 ) ) ;
#8415=CARTESIAN_POINT ( 'NONE',  ( -9.832129032723418760, 58.17708332991936260, -5.676582343750004256 ) ) ;
#8422=CARTESIAN_POINT ( 'NONE',  ( -6.000000000000001776, 289.0625000034140157, 0.000000000000000000 ) ) ;
#8430=EDGE_LOOP ( 'NONE', ( #49633, #6981, #31421, #73550, #70250, #63825, #63824, #71669, #46030, #38383, #13958, #43885, #14419, #21803, #33928, #70862, #19371, #74211, #38202, #29038, #57867, #26341, #26879, #35696, #21356, #4547, #68705, #27594, #71742, #66042, #34463, #26385, #16700, #51744, #14975, #29152, #9189, #4287, #50285, #56709, #49867, #24195, #41940, #33602, #48718, #65737, #70615, #64196, #1801, #16689, #54368, #55387, #47135, #5402, #71322, #28659, #42766, #72449, #14349, #21512, #18945, #45173, #47392, #10236, #56535, #47933, #30215, #4060, #33025, #72705, #55723, #66820, #2265, #61800, #5577, #52667, #42564, #50845, #12438, #25477, #38689, #5310, #28837, #20557, #11702, #9421, #27188, #67760, #72674, #62527, #55513, #63745, #65455, #31577 ) ) ;
#8436=DIRECTION ( 'NONE',  ( -0.000000000000000000, 1.000000000000000000, -0.000000000000000000 ) ) ;
#8445=CARTESIAN_POINT ( 'NONE',  ( -4.999999999999998224, 71.66666666666667140, -8.660254037844389075 ) ) ;
#8448=CARTESIAN_POINT ( 'NONE',  ( 2.485281374238575314, 297.3125000000000000, 6.000000000000000888 ) ) ;
#8452=EDGE_LOOP ( 'NONE', ( #50110, #11107, #72992, #70119, #26781, #28146 ) ) ;
#8460=CARTESIAN_POINT ( 'NONE',  ( 7.320508075688771044, 194.3750000000000284, 7.320508075688775484 ) ) ;
#8463=CARTESIAN_POINT ( 'NONE',  ( 6.951808397369818766E-16, 152.3437499965860411, -11.35316468750000141 ) ) ;
#8465=CARTESIAN_POINT ( 'NONE',  ( 2.679491924311228956, 27.91666665983870033, -10.00000000000000000 ) ) ;
#8467=CARTESIAN_POINT ( 'NONE',  ( -7.320508075688778149, 84.99999999317203958, 7.320508075688769267 ) ) ;
#8468=CARTESIAN_POINT ( 'NONE',  ( 1.102182119232618108E-15, 292.2500000000000000, 6.000000000000001776 ) ) ;
#8469=ORIENTED_EDGE ( 'NONE', *, *, #40215, .F. ) ;
#8470=CARTESIAN_POINT ( 'NONE',  ( -11.35316468750000141, 8.593749996586016238, -1.390361679473963753E-15 ) ) ;
#8473=CARTESIAN_POINT ( 'NONE',  ( 7.320508075688771044, 31.24999999317203603, 7.320508075688775484 ) ) ;
#8476=ADVANCED_FACE ( 'NONE', ( #31122 ), #20163, .T. ) ;
#8477=CARTESIAN_POINT ( 'NONE',  ( 4.999999999999993783, 46.04166665983869677, 8.660254037844390851 ) ) ;
#8485=CARTESIAN_POINT ( 'NONE',  ( 0.000000000000000000, 300.0000000000000000, 6.000000000000001776 ) ) ;
#8487=EDGE_CURVE ( 'NONE', #35448, #8939, #19640, .T. ) ;
#8489=CARTESIAN_POINT ( 'NONE',  ( -8.311093377946841443, 128.9062499965860411, 8.311093377946830785 ) ) ;
#8499=CARTESIAN_POINT ( 'NONE',  ( 11.35316468749999785, 115.5729166632526841, 3.042071309553174174 ) ) ;
#8502=ORIENTED_EDGE ( 'NONE', *, *, #56567, .T. ) ;
#8503=CARTESIAN_POINT ( 'NONE',  ( -10.00000000000000355, 24.58333332650536818, 2.679491924311223183 ) ) ;
#8504=EDGE_CURVE ( 'NONE', #12433, #9485, #17235, .T. ) ;
#8506=CARTESIAN_POINT ( 'NONE',  ( 9.832129032723420536, 96.51041666325268409, -5.676582343749999815 ) ) ;
#8510=CARTESIAN_POINT ( 'NONE',  ( -11.35316468749999785, 28.38541666325268054, -3.042071309553167513 ) ) ;
#8518=CARTESIAN_POINT ( 'NONE',  ( -2.765530957081998586, 292.6406250017070079, 6.676582343750001591 ) ) ;
#8520=CARTESIAN_POINT ( 'NONE',  ( -11.35316468750000141, 218.8020833299193271, 3.042071309553159963 ) ) ;
#8523=CARTESIAN_POINT ( 'NONE',  ( -3.042071309553173730, 139.6354166632526415, 11.35316468749999785 ) ) ;
#8535=EDGE_LOOP ( 'NONE', ( #36016, #9353, #41484, #29131 ) ) ;
#8539=CARTESIAN_POINT ( 'NONE',  ( -2.679491924311235174, 30.41666665983870033, 10.00000000000000000 ) ) ;
#8540=CARTESIAN_POINT ( 'NONE',  ( 5.676582343749993598, 179.9479166632526983, 9.832129032723422313 ) ) ;
#8543=CARTESIAN_POINT ( 'NONE',  ( -0.4590000000000000746, 261.4319999999996753, 5.805293472044576575 ) ) ;
#8544=CARTESIAN_POINT ( 'NONE',  ( -2.765530957081996810, 291.2656250017070079, -6.676582343750002480 ) ) ;
#8557=CARTESIAN_POINT ( 'NONE',  ( -3.042071309553173730, 114.6354166632526983, 11.35316468749999785 ) ) ;
#8565=CARTESIAN_POINT ( 'NONE',  ( 9.832129032723420536, 221.1979166632526983, -5.676582343749999815 ) ) ;
#8570=CARTESIAN_POINT ( 'NONE',  ( -9.832129032723418760, 198.1770833299193555, -5.676582343750004256 ) ) ;
#8577=CARTESIAN_POINT ( 'NONE',  ( -5.676582343749998039, 87.44791666325268409, -9.832129032723420536 ) ) ;
#8580=CARTESIAN_POINT ( 'NONE',  ( -2.062184786512628451E-11, 138.7499999999984084, 10.00000000000000178 ) ) ;
#8581=CARTESIAN_POINT ( 'NONE',  ( -2.249999999999998668, 255.9999999999999432, 7.677076266392047543 ) ) ;
#8584=CARTESIAN_POINT ( 'NONE',  ( -5.676582343749998039, 92.44791666325269830, -9.832129032723420536 ) ) ;
#8585=ORIENTED_EDGE ( 'NONE', *, *, #30348, .F. ) ;
#8589=CARTESIAN_POINT ( 'NONE',  ( 5.000000000000010658, 74.16666666666669983, 8.660254037844419273 ) ) ;
#8591=CARTESIAN_POINT ( 'NONE',  ( 8.311093377946837890, 66.40624999658604111, -8.311093377946837890 ) ) ;
#8594=CARTESIAN_POINT ( 'NONE',  ( 2.679491924311228956, 162.9166666598387110, -10.00000000000000000 ) ) ;
#8597=CARTESIAN_POINT ( 'NONE',  ( -8.311093377946836114, 62.96874999658602690, -8.311093377946837890 ) ) ;
#8598=CARTESIAN_POINT ( 'NONE',  ( 2.765530957082001251, 291.7656250017069510, 6.676582343750000703 ) ) ;
#8601=CARTESIAN_POINT ( 'NONE',  ( 11.35316468750000141, 205.7812499965860411, 0.000000000000000000 ) ) ;
#8606=CARTESIAN_POINT ( 'NONE',  ( 9.832129032723420536, 191.1979166632526983, -5.676582343749999815 ) ) ;
#8612=CARTESIAN_POINT ( 'NONE',  ( 11.35316468749999785, 185.8854166632526983, 3.042071309553174174 ) ) ;
#8619=EDGE_CURVE ( 'NONE', #23507, #37922, #6559, .T. ) ;
#8622=CARTESIAN_POINT ( 'NONE',  ( -10.00000000000000355, 7.708333333333332149, 2.679491924311223183 ) ) ;
#8639=EDGE_CURVE ( 'NONE', #74042, #9014, #74073, .T. ) ;
#8642=CARTESIAN_POINT ( 'NONE',  ( -11.35316468749999785, 68.38541666325268409, -3.042071309553167513 ) ) ;
#8643=CARTESIAN_POINT ( 'NONE',  ( -10.00000000000000000, 114.1666666598386968, -2.679491924311229845 ) ) ;
#8647=CARTESIAN_POINT ( 'NONE',  ( 4.721056650416000089, 292.9843750017070079, 4.721056650415999201 ) ) ;
#8648=CARTESIAN_POINT ( 'NONE',  ( 7.320508075688774596, 150.6250000000000000, -7.320508075688774596 ) ) ;
#8661=CARTESIAN_POINT ( 'NONE',  ( 5.000000000000003553, 135.8333333333333712, -8.660254037844390851 ) ) ;
#8665=CARTESIAN_POINT ( 'NONE',  ( 11.35316468749999785, 40.57291666325269119, 3.042071309553174174 ) ) ;
#8667=CARTESIAN_POINT ( 'NONE',  ( 8.660254037844389075, 7.291666659838699438, -5.000000000000000000 ) ) ;
#8671=CARTESIAN_POINT ( 'NONE',  ( -11.35316468749999785, 53.07291666325266988, -3.042071309553167513 ) ) ;
#8677=CARTESIAN_POINT ( 'NONE',  ( -11.35316468750000141, 33.28124999658601268, -1.390361679473963753E-15 ) ) ;
#8680=CARTESIAN_POINT ( 'NONE',  ( -9.832129032723418760, 162.8645833299193839, -5.676582343750004256 ) ) ;
#8681=CARTESIAN_POINT ( 'NONE',  ( 10.00000000000000178, 127.0833333265053682, -2.679491924311226736 ) ) ;
#8685=CARTESIAN_POINT ( 'NONE',  ( -9.832129032723420536, 19.01041666325268409, 5.676582343749997150 ) ) ;
#8692=CARTESIAN_POINT ( 'NONE',  ( 9.832129032723416984, 150.3645833299193555, 5.676582343750006032 ) ) ;
#8701=CARTESIAN_POINT ( 'NONE',  ( 6.123233995736767268E-16, 118.1249999931720396, -10.00000000000000178 ) ) ;
#8702=CARTESIAN_POINT ( 'NONE',  ( -6.000000000000003553, 292.0000000034139589, -2.485281374238571317 ) ) ;
#8703=CARTESIAN_POINT ( 'NONE',  ( -8.311093377946841443, 104.2187499965859985, 8.311093377946830785 ) ) ;
#8705=CARTESIAN_POINT ( 'NONE',  ( 10.00000000000000888, 14.79166666666667140, 2.679491924311238282 ) ) ;
#8722=( BOUNDED_CURVE ( )  B_SPLINE_CURVE ( 2, ( #21165, #61161, #9110, #4951, #32125, #20791, #66441, #9493, #38903, #33630, #49464, #67202, #72860 ),
 .UNSPECIFIED., .F., .F. ) 
 B_SPLINE_CURVE_WITH_KNOTS ( ( 3, 2, 2, 2, 2, 2, 3 ),
 ( 0.7378893796947577632, 0.7431232142107645489, 0.7483570487267714455, 0.7535908832427783421, 0.7588247177587852388, 0.7640585522747921354, 0.7692923867907990321 ),
 .UNSPECIFIED. ) 
 CURVE ( )  GEOMETRIC_REPRESENTATION_ITEM ( )  RATIONAL_B_SPLINE_CURVE ( ( 1.000000000000083489, 0.9659258262889848234, 1.000000000000000000, 0.9659258262890683122, 1.000000000000000000, 0.9659258262890683122, 1.000000000000000000, 0.9659258262890683122, 1.000000000000000000, 0.9659258262890683122, 1.000000000000000000, 0.9659258262888741342, 1.000000000000194289 ) ) 
 REPRESENTATION_ITEM ( '' )  );
#8726=AXIS2_PLACEMENT_3D ( 'NONE', #44429, #51202, #21776 ) ;
#8737=CARTESIAN_POINT ( 'NONE',  ( -5.000000000000005329, 103.3333333333333428, 8.660254037844387298 ) ) ;
#8740=CARTESIAN_POINT ( 'NONE',  ( 6.676582343750001591, 292.1093750017069510, -8.176455196517173205E-16 ) ) ;
#8745=( BOUNDED_CURVE ( )  B_SPLINE_CURVE ( 2, ( #37006, #61508, #32858, #14348, #55863, #8705, #54741, #3050, #26034, #37760, #60760, #9082, #68653 ),
 .UNSPECIFIED., .F., .F. ) 
 B_SPLINE_CURVE_WITH_KNOTS ( ( 3, 2, 2, 2, 2, 2, 3 ),
 ( 0.1726919338016095207, 0.1779254737324397762, 0.1831590136632700316, 0.1883925535941002871, 0.1936260935249305426, 0.1988596334557607981, 0.2040931733865910258 ),
 .UNSPECIFIED. ) 
 CURVE ( )  GEOMETRIC_REPRESENTATION_ITEM ( )  RATIONAL_B_SPLINE_CURVE ( ( 1.000000000000187850, 0.9659258262888803515, 1.000000000000000000, 0.9659258262890683122, 1.000000000000000000, 0.9659258262890683122, 1.000000000000000000, 0.9659258262890683122, 1.000000000000000000, 0.9659258262890683122, 1.000000000000000000, 0.9659258262890675351, 1.000000000000000888 ) ) 
 REPRESENTATION_ITEM ( '' )  );
#8753=CARTESIAN_POINT ( 'NONE',  ( -3.042071309553173730, 4.322916663252682312, 11.35316468749999785 ) ) ;
#8755=CARTESIAN_POINT ( 'NONE',  ( 5.676582343749993598, 200.2604166632526983, 9.832129032723422313 ) ) ;
#8756=CARTESIAN_POINT ( 'NONE',  ( 10.00000000000000000, 191.6666666598387110, 2.679491924311235618 ) ) ;
#8761=EDGE_LOOP ( 'NONE', ( #54885, #33884, #47659, #6937 ) ) ;
#8764=CARTESIAN_POINT ( 'NONE',  ( 11.35316468749999963, 5.989583329919348387, -3.042071309553165293 ) ) ;
#8770=CARTESIAN_POINT ( 'NONE',  ( -5.000000000000005329, 60.20833332650536818, 8.660254037844387298 ) ) ;
#8772=CARTESIAN_POINT ( 'NONE',  ( -11.35316468749999785, 123.0729166632526983, -3.042071309553167513 ) ) ;
#8773=CARTESIAN_POINT ( 'NONE',  ( -5.000000000000005329, 85.20833332650538239, 8.660254037844387298 ) ) ;
#8778=ORIENTED_EDGE ( 'NONE', *, *, #47047, .T. ) ;
#8781=CARTESIAN_POINT ( 'NONE',  ( 1.226468279477575784E-15, 294.8593750017070079, 6.676582343750001591 ) ) ;
#8782=DIRECTION ( 'NONE',  ( -0.000000000000000000, 1.000000000000000000, -0.000000000000000000 ) ) ;
#8784=CARTESIAN_POINT ( 'NONE',  ( -8.311093377946836114, 162.6562499965859843, -8.311093377946837890 ) ) ;
#8791=CARTESIAN_POINT ( 'NONE',  ( 6.123233995736767268E-16, 158.1249999931720254, -10.00000000000000178 ) ) ;
#8792=CARTESIAN_POINT ( 'NONE',  ( 3.042071309553167513, 157.1354166632526983, -11.35316468749999785 ) ) ;
#8793=CARTESIAN_POINT ( 'NONE',  ( -5.000000000000000000, 216.6666666666666856, -8.660254037844390851 ) ) ;
#8796=CARTESIAN_POINT ( 'NONE',  ( 5.676582343750001591, 66.92708332991935549, -9.832129032723420536 ) ) ;
#8797=EDGE_LOOP ( 'NONE', ( #21511, #14259, #49835, #56911 ) ) ;
#8803=ADVANCED_FACE ( 'NONE', ( #2002 ), #54060, .T. ) ;
#8805=CARTESIAN_POINT ( 'NONE',  ( -4.242640687119285658, 288.1875000034139589, 4.242640687119287435 ) ) ;
#8821=ORIENTED_EDGE ( 'NONE', *, *, #16361, .T. ) ;
#8828=CARTESIAN_POINT ( 'NONE',  ( -8.660254037844387298, 62.08333333333333570, -5.000000000000004441 ) ) ;
#8830=CARTESIAN_POINT ( 'NONE',  ( -4.242640687119286547, 295.8750000000000000, -4.242640687119286547 ) ) ;
#8842=CARTESIAN_POINT ( 'NONE',  ( -1.836970198721029983E-15, 183.7500000000000284, 10.00000000000000178 ) ) ;
#8845=CARTESIAN_POINT ( 'NONE',  ( -5.676582343750006032, 159.4270833299193555, 9.832129032723418760 ) ) ;
#8853=AXIS2_PLACEMENT_3D ( 'NONE', #70300, #18615, #41626 ) ;
#8854=CARTESIAN_POINT ( 'NONE',  ( 6.951808397369818766E-16, 12.34374999658601801, -11.35316468750000141 ) ) ;
#8855=CARTESIAN_POINT ( 'NONE',  ( 5.000000000000001776, 97.70833332650536818, -8.660254037844389075 ) ) ;
#8856=CARTESIAN_POINT ( 'NONE',  ( 4.999999999999993783, 31.04166665983870033, 8.660254037844390851 ) ) ;
#8859=CARTESIAN_POINT ( 'NONE',  ( 7.320508075688774596, 52.49999999317203248, -7.320508075688774596 ) ) ;
#8862=CYLINDRICAL_SURFACE ( 'NONE', #69896, 10.00000000000000178 ) ;
#8865=CARTESIAN_POINT ( 'NONE',  ( 4.999999999999993783, 6.041666659838699438, 8.660254037844390851 ) ) ;
#8869=CARTESIAN_POINT ( 'NONE',  ( -3.042071309553164404, 127.2395833299193555, -11.35316468749999963 ) ) ;
#8877=CARTESIAN_POINT ( 'NONE',  ( 11.35316468749999785, 125.5729166632526841, 3.042071309553174174 ) ) ;
#8883=CARTESIAN_POINT ( 'NONE',  ( 5.676582343750001591, 116.9270833299193555, -9.832129032723420536 ) ) ;
#8887=CARTESIAN_POINT ( 'NONE',  ( -3.042071309553164404, 22.55208332991935194, -11.35316468749999963 ) ) ;
#8895=CARTESIAN_POINT ( 'NONE',  ( -4.721056650415999201, 288.3281250017069510, -4.721056650415999201 ) ) ;
#8897=CARTESIAN_POINT ( 'NONE',  ( 3.042071309553167513, 217.1354166632526983, -11.35316468749999785 ) ) ;
#8900=CARTESIAN_POINT ( 'NONE',  ( -11.35316468750000141, 138.8020833299193271, 3.042071309553159963 ) ) ;
#8916=CARTESIAN_POINT ( 'NONE',  ( 3.042071309553167069, 191.8229166632526415, -11.35316468749999785 ) ) ;
#8919=CARTESIAN_POINT ( 'NONE',  ( -6.676582343750002480, 293.3906250017069510, -2.765530957081996810 ) ) ;
#8933=CARTESIAN_POINT ( 'NONE',  ( 8.311093377946834337, 115.4687499965860269, 8.311093377946839666 ) ) ;
#8939=VERTEX_POINT ( 'NONE', #25730 ) ;
#8941=CARTESIAN_POINT ( 'NONE',  ( -9.832129032723420536, 223.6979166632526983, 5.676582343749997150 ) ) ;
#8945=CARTESIAN_POINT ( 'NONE',  ( -11.35316468749999785, 193.3854166632526415, -3.042071309553167513 ) ) ;
#8947=DIRECTION ( 'NONE',  ( 0.000000000000000000, 0.000000000000000000, 1.000000000000000000 ) ) ;
#8952=CARTESIAN_POINT ( 'NONE',  ( -5.676582343749998039, 82.44791666325268409, -9.832129032723420536 ) ) ;
#8957=VECTOR ( 'NONE', #39813, 1000.000000000000000 ) ;
#8959=CARTESIAN_POINT ( 'NONE',  ( -11.35316468749999785, 83.07291666325268409, -3.042071309553167513 ) ) ;
#8967=CARTESIAN_POINT ( 'NONE',  ( 8.311093377946834337, 90.15624999658602690, 8.311093377946839666 ) ) ;
#8970=( BOUNDED_CURVE ( )  B_SPLINE_CURVE ( 2, ( #23984, #41348, #46993, #53780, #2089, #25081, #13752, #60541, #9238, #16001, #49601, #20921, #72987 ),
 .UNSPECIFIED., .F., .F. ) 
 B_SPLINE_CURVE_WITH_KNOTS ( ( 3, 2, 2, 2, 2, 2, 3 ),
 ( 0.3610969255903727637, 0.3663293280448572387, 0.3715617304993417136, 0.3767941329538261885, 0.3820265354083106635, 0.3872589378627951939, 0.3924913403172796134 ),
 .UNSPECIFIED. ) 
 CURVE ( )  GEOMETRIC_REPRESENTATION_ITEM ( )  RATIONAL_B_SPLINE_CURVE ( ( 1.000000000000000000, 0.9659258262890683122, 1.000000000000000000, 0.9659258262890683122, 1.000000000000000000, 0.9659258262890683122, 1.000000000000000000, 0.9659258262890683122, 1.000000000000000000, 0.9659258262890683122, 1.000000000000000000, 0.9659258262893669622, 0.9999999999997013500 ) ) 
 REPRESENTATION_ITEM ( '' )  );
#8971=CARTESIAN_POINT ( 'NONE',  ( -2.679491924311225848, 163.3333333265053682, -10.00000000000000178 ) ) ;
#8974=CARTESIAN_POINT ( 'NONE',  ( -9.832129032723420536, 59.01041666325268409, 5.676582343749997150 ) ) ;
#8975=CARTESIAN_POINT ( 'NONE',  ( 6.676582343750004256, 292.8906250017068942, 2.765530957081995478 ) ) ;
#8977=CARTESIAN_POINT ( 'NONE',  ( 3.042071309553167069, 206.8229166632526699, -11.35316468749999785 ) ) ;
#8979=CARTESIAN_POINT ( 'NONE',  ( -1.173938163346586453E-11, 213.7499999999991189, 10.00000000000000178 ) ) ;
#8980=CARTESIAN_POINT ( 'NONE',  ( 7.347880794884121708E-16, 300.0000000000000000, -6.000000000000001776 ) ) ;
#8981=CARTESIAN_POINT ( 'NONE',  ( -2.485281374238308860, 288.1875000000000568, 6.000000000000264677 ) ) ;
#8983=CARTESIAN_POINT ( 'NONE',  ( -11.35316468749999785, 193.0729166632526699, -3.042071309553167957 ) ) ;
#8986=DIRECTION ( 'NONE',  ( 0.000000000000000000, 0.000000000000000000, 1.000000000000000000 ) ) ;
#8988=CARTESIAN_POINT ( 'NONE',  ( -8.311093377946836114, 177.9687499965860127, -8.311093377946837890 ) ) ;
#8989=ADVANCED_FACE ( 'NONE', ( #29934 ), #48751, .T. ) ;
#8997=EDGE_CURVE ( 'NONE', #34004, #10894, #32679, .T. ) ;
#9014=VERTEX_POINT ( 'NONE', #54809 ) ;
#9016=CARTESIAN_POINT ( 'NONE',  ( -11.35316468749999785, 73.38541666325268409, -3.042071309553167513 ) ) ;
#9019=DIRECTION ( 'NONE',  ( 0.000000000000000000, 0.000000000000000000, 1.000000000000000000 ) ) ;
#9021=CARTESIAN_POINT ( 'NONE',  ( -4.721056650415998313, 295.7343750017069510, 4.721056650416000089 ) ) ;
#9023=LINE ( 'NONE', #55431, #34815 ) ;
#9026=LINE ( 'NONE', #55059, #20532 ) ;
#9035=CARTESIAN_POINT ( 'NONE',  ( -5.711993833409989278E-12, 133.7499999999995737, 9.999999999999998224 ) ) ;
#9039=CARTESIAN_POINT ( 'NONE',  ( -3.042071309553164404, 37.23958332991934839, -11.35316468749999963 ) ) ;
#9041=CARTESIAN_POINT ( 'NONE',  ( 10.00000000000000178, 7.083333326505365513, -2.679491924311226736 ) ) ;
#9043=EDGE_CURVE ( 'NONE', #23294, #23507, #40365, .T. ) ;
#9044=DIRECTION ( 'NONE',  ( -0.000000000000000000, 1.000000000000000000, -0.000000000000000000 ) ) ;
#9046=CARTESIAN_POINT ( 'NONE',  ( -8.311093377946841443, 43.90624999658601268, 8.311093377946830785 ) ) ;
#9050=DIRECTION ( 'NONE',  ( 0.000000000000000000, 0.000000000000000000, 1.000000000000000000 ) ) ;
#9052=CARTESIAN_POINT ( 'NONE',  ( 9.832129032723416984, 35.36458332991934839, 5.676582343750006032 ) ) ;
#9056=CARTESIAN_POINT ( 'NONE',  ( 9.832129032723420536, 166.1979166632526983, -5.676582343749999815 ) ) ;
#9057=CARTESIAN_POINT ( 'NONE',  ( -10.00000000000000178, 134.3749999931720254, -1.224646799147353454E-15 ) ) ;
#9060=CARTESIAN_POINT ( 'NONE',  ( 5.000000000000001776, 22.70833332650536818, -8.660254037844389075 ) ) ;
#9061=CARTESIAN_POINT ( 'NONE',  ( -2.085542519210945728E-15, 24.84374999658601624, 11.35316468750000141 ) ) ;
#9070=CARTESIAN_POINT ( 'NONE',  ( -8.311093377946836114, 147.6562499965860127, -8.311093377946837890 ) ) ;
#9076=VERTEX_POINT ( 'NONE', #15913 ) ;
#9079=CARTESIAN_POINT ( 'NONE',  ( -9.832129032723418760, 103.1770833299193555, -5.676582343750004256 ) ) ;
#9081=( BOUNDED_CURVE ( )  B_SPLINE_CURVE ( 2, ( #22105, #3651, #26651, #72689, #20991, #15322, #17569, #28891, #62843 ),
 .UNSPECIFIED., .F., .F. ) 
 B_SPLINE_CURVE_WITH_KNOTS ( ( 3, 2, 2, 2, 3 ),
 ( 0.1041666666666644370, 0.1145833333333311083, 0.1249999999999977796, 0.1354166666666644647, 0.1458333333333311499 ),
 .UNSPECIFIED. ) 
 CURVE ( )  GEOMETRIC_REPRESENTATION_ITEM ( )  RATIONAL_B_SPLINE_CURVE ( ( 1.000000000000016431, 0.9238795325112704182, 1.000000000000000000, 0.9238795325112867385, 1.000000000000000000, 0.9238795325112867385, 1.000000000000000000, 0.9238795325113027257, 0.9999999999999840128 ) ) 
 REPRESENTATION_ITEM ( '' )  );
#9082=CARTESIAN_POINT ( 'NONE',  ( 2.679491924311176554, 16.04166666666667496, -10.00000000000004263 ) ) ;
#9102=CARTESIAN_POINT ( 'NONE',  ( 2.765530957081996366, 299.1406250017068942, -6.676582343750002480 ) ) ;
#9110=CARTESIAN_POINT ( 'NONE',  ( 5.000000000000032863, 59.16666666666672114, 8.660254037844458352 ) ) ;
#9111=CARTESIAN_POINT ( 'NONE',  ( -8.660254037844390851, 107.9166666666666714, 4.999999999999998224 ) ) ;
#9114=CARTESIAN_POINT ( 'NONE',  ( -6.676582343750003368, 292.5468750017068942, -2.765530957081996810 ) ) ;
#9117=CARTESIAN_POINT ( 'NONE',  ( -10.00000000000000355, 174.5833333265053966, 2.679491924311223183 ) ) ;
#9125=CARTESIAN_POINT ( 'NONE',  ( -11.35316468750000141, 8.281249996586016238, -1.390361679473963753E-15 ) ) ;
#9127=CARTESIAN_POINT ( 'NONE',  ( 9.832129032723416984, 190.6770833299193555, 5.676582343750006032 ) ) ;
#9135=CARTESIAN_POINT ( 'NONE',  ( -3.042071309553173730, 14.32291666325268231, 11.35316468749999785 ) ) ;
#9143=CARTESIAN_POINT ( 'NONE',  ( -2.085542519210945728E-15, 124.5312499965860269, 11.35316468750000141 ) ) ;
#9144=CARTESIAN_POINT ( 'NONE',  ( 4.999999999999993783, 91.04166665983871098, 8.660254037844390851 ) ) ;
#9153=CARTESIAN_POINT ( 'NONE',  ( -4.721056650415999201, 292.4843750017070079, -4.721056650415999201 ) ) ;
#9156=CARTESIAN_POINT ( 'NONE',  ( 6.951808397369818766E-16, 167.0312499965860411, -11.35316468750000141 ) ) ;
#9161=ORIENTED_EDGE ( 'NONE', *, *, #14652, .T. ) ;
#9162=CARTESIAN_POINT ( 'NONE',  ( 8.660254037844389075, 157.2916666598387110, -5.000000000000000000 ) ) ;
#9163=CARTESIAN_POINT ( 'NONE',  ( -2.085542519210945728E-15, 149.8437499965860411, 11.35316468750000141 ) ) ;
#9167=CARTESIAN_POINT ( 'NONE',  ( 9.832129032723420536, 66.51041666325268409, -5.676582343749999815 ) ) ;
#9168=ORIENTED_EDGE ( 'NONE', *, *, #27605, .T. ) ;
#9173=CARTESIAN_POINT ( 'NONE',  ( 4.242640687119287435, 290.4375000034140157, 4.242640687119285658 ) ) ;
#9189=ORIENTED_EDGE ( 'NONE', *, *, #12241, .F. ) ;
#9192=ORIENTED_EDGE ( 'NONE', *, *, #4010, .F. ) ;
#9197=CARTESIAN_POINT ( 'NONE',  ( 6.123233995736767268E-16, 66.25000000000000000, -10.00000000000000178 ) ) ;
#9199=CARTESIAN_POINT ( 'NONE',  ( 1.102182119232618108E-15, 293.2500000000000000, 6.000000000000001776 ) ) ;
#9201=CARTESIAN_POINT ( 'NONE',  ( -7.320508075688779037, 126.8750000000000142, -7.320508075688779925 ) ) ;
#9203=EDGE_CURVE ( 'NONE', #43617, #5520, #51367, .T. ) ;
#9212=CARTESIAN_POINT ( 'NONE',  ( -10.00000000000000178, 182.5000000000000284, -1.224646799147353454E-15 ) ) ;
#9215=CARTESIAN_POINT ( 'NONE',  ( -9.832129032723420536, 159.0104166632526983, 5.676582343749997150 ) ) ;
#9222=ORIENTED_EDGE ( 'NONE', *, *, #8487, .T. ) ;
#9223=CARTESIAN_POINT ( 'NONE',  ( -11.35316468750000141, 18.59374999658601979, -1.390361679473963753E-15 ) ) ;
#9226=CARTESIAN_POINT ( 'NONE',  ( -1.836970198721029983E-15, 30.62499999317203248, 10.00000000000000178 ) ) ;
#9227=CYLINDRICAL_SURFACE ( 'NONE', #26516, 10.00000000000000178 ) ;
#9229=CARTESIAN_POINT ( 'NONE',  ( 2.679491924311228956, 52.91666665983869677, -10.00000000000000000 ) ) ;
#9232=CARTESIAN_POINT ( 'NONE',  ( 8.660254037844373087, 99.58333333333334281, 4.999999999999997335 ) ) ;
#9237=ORIENTED_EDGE ( 'NONE', *, *, #38360, .T. ) ;
#9238=CARTESIAN_POINT ( 'NONE',  ( 8.660254037844390851, 30.41666666666667140, -5.000000000000002665 ) ) ;
#9241=CARTESIAN_POINT ( 'NONE',  ( 8.311093377946837890, 131.4062499965860411, -8.311093377946837890 ) ) ;
#9243=CARTESIAN_POINT ( 'NONE',  ( -2.485281374238172081, 298.1875000000000568, 6.000000000000400568 ) ) ;
#9248=CARTESIAN_POINT ( 'NONE',  ( 10.00000000000002487, 44.79166666666667851, 2.679491924311242279 ) ) ;
#9249=CARTESIAN_POINT ( 'NONE',  ( 3.042071309553159519, 124.7395833299193555, 11.35316468750000141 ) ) ;
#9253=CARTESIAN_POINT ( 'NONE',  ( -6.000000000000001776, 288.0000000000000000, 0.000000000000000000 ) ) ;
#9255=CARTESIAN_POINT ( 'NONE',  ( 11.35316468749999963, 116.3020833299193413, -3.042071309553165293 ) ) ;
#9259=CARTESIAN_POINT ( 'NONE',  ( -11.35316468750000141, 18.80208332991934839, 3.042071309553159963 ) ) ;
#9260=ORIENTED_EDGE ( 'NONE', *, *, #141, .T. ) ;
#9261=FACE_OUTER_BOUND ( 'NONE', #74481, .T. ) ;
#9266=CARTESIAN_POINT ( 'NONE',  ( 6.676582343750003368, 289.0156250017070079, -2.765530957081997254 ) ) ;
#9270=CARTESIAN_POINT ( 'NONE',  ( -11.35316468750000141, 143.8020833299193555, 3.042071309553159963 ) ) ;
#9276=VERTEX_POINT ( 'NONE', #51714 ) ;
#9280=ADVANCED_FACE ( 'NONE', ( #29455 ), #18499, .T. ) ;
#9286=VECTOR ( 'NONE', #71729, 1000.000000000000000 ) ;
#9288=CARTESIAN_POINT ( 'NONE',  ( -3.042071309553164404, 187.2395833299193839, -11.35316468749999963 ) ) ;
#9298=CARTESIAN_POINT ( 'NONE',  ( 8.660254037844385522, 166.4583333265053682, 5.000000000000005329 ) ) ;
#9305=CARTESIAN_POINT ( 'NONE',  ( -11.35316468750000141, 118.5937499965860269, -1.390361679473963753E-15 ) ) ;
#9306=CARTESIAN_POINT ( 'NONE',  ( 7.320508075688774596, 212.4999999931720254, -7.320508075688774596 ) ) ;
#9310=CARTESIAN_POINT ( 'NONE',  ( 0.000000000000000000, 225.9999999999999432, 0.000000000000000000 ) ) ;
#9318=VECTOR ( 'NONE', #37644, 1000.000000000000000 ) ;
#9321=CARTESIAN_POINT ( 'NONE',  ( -3.042071309553164404, 202.5520833299193839, -11.35316468749999963 ) ) ;
#9328=CARTESIAN_POINT ( 'NONE',  ( 8.311093377946834337, 85.15624999658602690, 8.311093377946839666 ) ) ;
#9334=CARTESIAN_POINT ( 'NONE',  ( 5.676582343749993598, 84.94791666325268409, 9.832129032723422313 ) ) ;
#9342=CARTESIAN_POINT ( 'NONE',  ( 9.832129032723416984, 85.36458332991936970, 5.676582343750006032 ) ) ;
#9347=CARTESIAN_POINT ( 'NONE',  ( -7.320508075688773708, 168.7499999931720822, -7.320508075688774596 ) ) ;
#9349=CARTESIAN_POINT ( 'NONE',  ( -8.311093377946836114, 72.96874999658602690, -8.311093377946837890 ) ) ;
#9350=CARTESIAN_POINT ( 'NONE',  ( 6.676582343750001591, 293.9531250017069510, -8.176455196517173205E-16 ) ) ;
#9352=CARTESIAN_POINT ( 'NONE',  ( -8.311093377946836114, 212.6562499965860411, -8.311093377946837890 ) ) ;
#9353=ORIENTED_EDGE ( 'NONE', *, *, #70144, .T. ) ;
#9358=CARTESIAN_POINT ( 'NONE',  ( 11.35316468750000141, 205.7812499965860411, 0.000000000000000000 ) ) ;
#9363=CARTESIAN_POINT ( 'NONE',  ( -9.832129032723420536, 199.0104166632526983, 5.676582343749997150 ) ) ;
#9375=( BOUNDED_CURVE ( )  B_SPLINE_CURVE ( 2, ( #39953, #73531, #33568, #22211, #21839, #27505, #26763, #28259, #21105, #67509, #10165, #68250, #68620 ),
 .UNSPECIFIED., .F., .F. ) 
 B_SPLINE_CURVE_WITH_KNOTS ( ( 3, 2, 2, 2, 2, 2, 3 ),
 ( 0.7228260869565217295, 0.7246376811594202882, 0.7264492753623188470, 0.7282608695652172948, 0.7300724637681158535, 0.7318840579710144123, 0.7336956521739129711 ),
 .UNSPECIFIED. ) 
 CURVE ( )  GEOMETRIC_REPRESENTATION_ITEM ( )  RATIONAL_B_SPLINE_CURVE ( ( 1.000000000000000000, 0.9659258262890683122, 1.000000000000000000, 0.9659258262890683122, 1.000000000000000000, 0.9659258262890683122, 1.000000000000000000, 0.9659258262890683122, 1.000000000000000000, 0.9659258262890683122, 1.000000000000000000, 0.9659258262890704216, 0.9999999999999978906 ) ) 
 REPRESENTATION_ITEM ( '' )  );
#9379=CARTESIAN_POINT ( 'NONE',  ( 6.000000000000003553, 293.5000000034140157, 2.485281374238571317 ) ) ;
#9391=CARTESIAN_POINT ( 'NONE',  ( 3.042071309553167069, 77.13541666325266988, -11.35316468749999785 ) ) ;
#9396=CARTESIAN_POINT ( 'NONE',  ( -4.721056650415998313, 289.7343750017069510, 4.721056650416000089 ) ) ;
#9411=CARTESIAN_POINT ( 'NONE',  ( -2.485281374238916374, 292.8750000034140157, -5.999999999999657163 ) ) ;
#9413=CARTESIAN_POINT ( 'NONE',  ( 2.679491924308573747, 133.9583333333331154, 10.00000000000153655 ) ) ;
#9417=CARTESIAN_POINT ( 'NONE',  ( -3.042071309553173730, 39.32291666325268409, 11.35316468749999785 ) ) ;
#9419=CARTESIAN_POINT ( 'NONE',  ( -10.00000000000000000, 24.16666665983869677, -2.679491924311229845 ) ) ;
#9421=ORIENTED_EDGE ( 'NONE', *, *, #65946, .F. ) ;
#9424=CARTESIAN_POINT ( 'NONE',  ( 9.832129032723416984, 55.36458332991934839, 5.676582343750006032 ) ) ;
#9431=CARTESIAN_POINT ( 'NONE',  ( 8.311093377946834337, 45.15624999658601268, 8.311093377946839666 ) ) ;
#9434=CARTESIAN_POINT ( 'NONE',  ( -2.085542519210945728E-15, 159.5312499965860127, 11.35316468750000141 ) ) ;
#9436=EDGE_CURVE ( 'NONE', #46215, #48362, #57348, .T. ) ;
#9437=CARTESIAN_POINT ( 'NONE',  ( 4.999999999999993783, 126.0416666598387110, 8.660254037844390851 ) ) ;
#9441=CARTESIAN_POINT ( 'NONE',  ( 5.676582343749993598, 40.26041666325268409, 9.832129032723422313 ) ) ;
#9442=DIRECTION ( 'NONE',  ( -0.000000000000000000, 1.000000000000000000, -0.000000000000000000 ) ) ;
#9448=CARTESIAN_POINT ( 'NONE',  ( -9.832129032723418760, 167.8645833299193555, -5.676582343750004256 ) ) ;
#9457=CARTESIAN_POINT ( 'NONE',  ( -4.999999999999998224, 118.5416666598386968, -8.660254037844389075 ) ) ;
#9459=CARTESIAN_POINT ( 'NONE',  ( 11.35316468750000141, 101.0937499965860127, 0.000000000000000000 ) ) ;
#9475=VERTEX_POINT ( 'NONE', #31675 ) ;
#9481=VECTOR ( 'NONE', #54321, 1000.000000000000000 ) ;
#9483=CARTESIAN_POINT ( 'NONE',  ( -4.088227598258586603E-16, 299.2031250017070079, -6.676582343750001591 ) ) ;
#9485=VERTEX_POINT ( 'NONE', #48266 ) ;
#9489=CARTESIAN_POINT ( 'NONE',  ( 2.752039609470550924E-11, 41.24999999999786127, -9.999999999999998224 ) ) ;
#9493=CARTESIAN_POINT ( 'NONE',  ( 10.00000000000007816, 60.20833333333337833, -2.679491924311247608 ) ) ;
#9494=CARTESIAN_POINT ( 'NONE',  ( -7.320508075688773708, 101.8750000000000000, -7.320508075688774596 ) ) ;
#9496=CARTESIAN_POINT ( 'NONE',  ( 6.676582343750004256, 292.0468750017070079, 2.765530957081995478 ) ) ;
#9509=CARTESIAN_POINT ( 'NONE',  ( -2.679491924311235174, 95.41666665983869677, 10.00000000000000000 ) ) ;
#9511=CARTESIAN_POINT ( 'NONE',  ( 6.951808397369818766E-16, 2.031249996586016682, -11.35316468750000141 ) ) ;
#9513=CARTESIAN_POINT ( 'NONE',  ( 3.042071309553159519, 200.0520833299193839, 11.35316468750000141 ) ) ;
#9514=CARTESIAN_POINT ( 'NONE',  ( -7.320508075688778149, 134.9999999931720538, 7.320508075688769267 ) ) ;
#9516=LINE ( 'NONE', #43832, #599 ) ;
#9521=CARTESIAN_POINT ( 'NONE',  ( -2.085542519210945728E-15, 4.531249996586016238, 11.35316468750000141 ) ) ;
#9525=CYLINDRICAL_SURFACE ( 'NONE', #32243, 10.00000000000000178 ) ;
#9527=CARTESIAN_POINT ( 'NONE',  ( -5.676582343749998039, 2.447916663252682756, -9.832129032723420536 ) ) ;
#9529=CARTESIAN_POINT ( 'NONE',  ( 8.311093377946837890, 116.4062499965860269, -8.311093377946837890 ) ) ;
#9531=CARTESIAN_POINT ( 'NONE',  ( 5.000000000000001776, 87.70833332650538239, -8.660254037844389075 ) ) ;
#9534=CARTESIAN_POINT ( 'NONE',  ( -10.00000000000000178, 199.3749999931720538, -1.224646799147353454E-15 ) ) ;
#9537=CARTESIAN_POINT ( 'NONE',  ( -6.607029887627752451, 225.9999999999999716, -7.535050054892760585 ) ) ;
#9538=( BOUNDED_CURVE ( )  B_SPLINE_CURVE ( 2, ( #43148, #66532, #37883, #9201, #60879, #3546, #67943, #16237, #39274, #62275, #10603, #24509, #40753 ),
 .UNSPECIFIED., .F., .F. ) 
 B_SPLINE_CURVE_WITH_KNOTS ( ( 3, 2, 2, 2, 2, 2, 3 ),
 ( 1.585692104212438336, 1.590924485345288186, 1.596156866478138037, 1.601389247610987887, 1.606621628743837960, 1.611854009876687810, 1.617086391009537660 ),
 .UNSPECIFIED. ) 
 CURVE ( )  GEOMETRIC_REPRESENTATION_ITEM ( )  RATIONAL_B_SPLINE_CURVE ( ( 1.000000000000000000, 0.9659258262890683122, 1.000000000000000000, 0.9659258262890683122, 1.000000000000000000, 0.9659258262890683122, 1.000000000000000000, 0.9659258262890683122, 1.000000000000000000, 0.9659258262890683122, 1.000000000000000000, 0.9659258262890474400, 1.000000000000020872 ) ) 
 REPRESENTATION_ITEM ( '' )  );
#9539=CARTESIAN_POINT ( 'NONE',  ( -6.676582343750000703, 288.6718750017069510, 2.765530957082001251 ) ) ;
#9544=CARTESIAN_POINT ( 'NONE',  ( -5.000000000000005329, 210.2083333265053682, 8.660254037844387298 ) ) ;
#9547=EDGE_LOOP ( 'NONE', ( #62629, #58293, #44144, #45059 ) ) ;
#9549=CARTESIAN_POINT ( 'NONE',  ( -11.35316468750000141, 158.5937499965860127, -1.390361679473963753E-15 ) ) ;
#9553=CARTESIAN_POINT ( 'NONE',  ( -9.832129032723420536, 64.01041666325268409, 5.676582343749997150 ) ) ;
#9554=VERTEX_POINT ( 'NONE', #37713 ) ;
#9559=CARTESIAN_POINT ( 'NONE',  ( 4.242640687119285658, 289.6875000034139589, -4.242640687119286547 ) ) ;
#9574=CARTESIAN_POINT ( 'NONE',  ( -4.242640687119285658, 290.1249999999999432, 4.242640687119287435 ) ) ;
#9577=ADVANCED_FACE ( 'NONE', ( #49385 ), #72787, .T. ) ;
#9580=CARTESIAN_POINT ( 'NONE',  ( -5.000000000000002665, 3.333333333333331261, 8.660254037844383745 ) ) ;
#9583=CARTESIAN_POINT ( 'NONE',  ( -10.00000000000000355, 67.70833333333334281, 2.679491924311223183 ) ) ;
#9586=CARTESIAN_POINT ( 'NONE',  ( -6.000000000000001776, 294.0000000000000000, 0.000000000000000000 ) ) ;
#9588=ORIENTED_EDGE ( 'NONE', *, *, #66589, .T. ) ;
#9595=FACE_OUTER_BOUND ( 'NONE', #10185, .T. ) ;
#9596=CARTESIAN_POINT ( 'NONE',  ( -2.679491924311225848, 181.4583333333333428, -10.00000000000000178 ) ) ;
#9599=CARTESIAN_POINT ( 'NONE',  ( 9.832129032723420536, 151.5104166632526699, -5.676582343749999815 ) ) ;
#9603=CARTESIAN_POINT ( 'NONE',  ( -8.660254037844387298, 83.95833332650536818, -5.000000000000004441 ) ) ;
#9606=CARTESIAN_POINT ( 'NONE',  ( -11.35316468750000141, 28.59374999658601624, -1.390361679473963753E-15 ) ) ;
#9612=CARTESIAN_POINT ( 'NONE',  ( -4.999999999999998224, 48.54166665983870388, -8.660254037844389075 ) ) ;
#9615=LINE ( 'NONE', #60536, #49354 ) ;
#9625=CARTESIAN_POINT ( 'NONE',  ( -11.35316468749999785, 123.0729166632526983, -3.042071309553167513 ) ) ;
#9627=CARTESIAN_POINT ( 'NONE',  ( -4.242640687119285658, 298.1250000000000000, 4.242640687119287435 ) ) ;
#9632=CARTESIAN_POINT ( 'NONE',  ( -9.832129032723420536, 128.6979166632526983, 5.676582343749997150 ) ) ;
#9634=VERTEX_POINT ( 'NONE', #66746 ) ;
#9638=CARTESIAN_POINT ( 'NONE',  ( -3.042071309553173730, 119.6354166632526841, 11.35316468749999785 ) ) ;
#9642=CARTESIAN_POINT ( 'NONE',  ( 8.311093377946834337, 20.46874999658601624, 8.311093377946839666 ) ) ;
#9650=CARTESIAN_POINT ( 'NONE',  ( 2.765530957082001251, 289.7656250017069510, 6.676582343750000703 ) ) ;
#9651=CARTESIAN_POINT ( 'NONE',  ( 10.00000000000000178, 111.8749999931720396, 0.000000000000000000 ) ) ;
#9655=CARTESIAN_POINT ( 'NONE',  ( -11.35316468749999785, 143.3854166632526983, -3.042071309553167513 ) ) ;
#9662=EDGE_CURVE ( 'NONE', #50631, #45507, #3339, .T. ) ;
#9671=CARTESIAN_POINT ( 'NONE',  ( -9.832129032723420536, 183.6979166632526983, 5.676582343749997150 ) ) ;
#9674=CARTESIAN_POINT ( 'NONE',  ( -6.676582343750002480, 289.3906250017070079, -2.765530957081996810 ) ) ;
#9681=CARTESIAN_POINT ( 'NONE',  ( 8.660254037844389075, 167.2916666598387110, -5.000000000000000000 ) ) ;
#9684=LINE ( 'NONE', #22095, #18598 ) ;
#9685=FACE_OUTER_BOUND ( 'NONE', #30806, .T. ) ;
#9688=CARTESIAN_POINT ( 'NONE',  ( 6.951808397369818766E-16, 112.3437499965860127, -11.35316468750000141 ) ) ;
#9695=CARTESIAN_POINT ( 'NONE',  ( 6.042744113992383426, 224.2641768943893794, 7.989819569021650025 ) ) ;
#9699=CARTESIAN_POINT ( 'NONE',  ( -11.35316468749999785, 213.3854166632526983, -3.042071309553167513 ) ) ;
#9707=CARTESIAN_POINT ( 'NONE',  ( 3.042071309553167069, 91.82291666325269830, -11.35316468749999785 ) ) ;
#9712=CARTESIAN_POINT ( 'NONE',  ( 3.042071309553159519, 89.73958332991935549, 11.35316468750000141 ) ) ;
#9720=CARTESIAN_POINT ( 'NONE',  ( 5.676582343750001591, 86.61458332991936970, -9.832129032723420536 ) ) ;
#9725=CARTESIAN_POINT ( 'NONE',  ( 8.660254037844389075, 177.2916666598387110, -5.000000000000000000 ) ) ;
#9727=CARTESIAN_POINT ( 'NONE',  ( -3.042071309553173730, 74.63541666325268409, 11.35316468749999785 ) ) ;
#9728=CARTESIAN_POINT ( 'NONE',  ( 4.721056650416000089, 294.8281250017069510, 4.721056650415999201 ) ) ;
#9730=CARTESIAN_POINT ( 'NONE',  ( 9.832129032723416984, 210.3645833299193555, 5.676582343750006032 ) ) ;
#9731=ORIENTED_EDGE ( 'NONE', *, *, #6089, .F. ) ;
#9736=CARTESIAN_POINT ( 'NONE',  ( -3.042071309553163960, 212.2395833299193839, -11.35316468749999963 ) ) ;
#9738=CARTESIAN_POINT ( 'NONE',  ( -2.765530957081996810, 299.2656250017070647, -6.676582343750003368 ) ) ;
#9740=CARTESIAN_POINT ( 'NONE',  ( 9.832129032723416984, 195.6770833299193839, 5.676582343750006032 ) ) ;
#9743=( BOUNDED_CURVE ( )  B_SPLINE_CURVE ( 2, ( #64813, #53870, #36150, #24806, #59895, #12753, #30117, #64453, #19154, #24073, #13114, #36520, #7842 ),
 .UNSPECIFIED., .F., .F. ) 
 B_SPLINE_CURVE_WITH_KNOTS ( ( 3, 2, 2, 2, 2, 2, 3 ),
 ( 0.5808961537982215706, 0.5861285976204262393, 0.5913610414426307971, 0.5965934852648355768, 0.6018259290870402456, 0.6070583729092448033, 0.6122908167314494721 ),
 .UNSPECIFIED. ) 
 CURVE ( )  GEOMETRIC_REPRESENTATION_ITEM ( )  RATIONAL_B_SPLINE_CURVE ( ( 1.000000000000001110, 0.9659258262890673130, 1.000000000000000000, 0.9659258262890683122, 1.000000000000000000, 0.9659258262890683122, 1.000000000000000000, 0.9659258262890683122, 1.000000000000000000, 0.9659258262890683122, 1.000000000000000000, 0.9659258262890584312, 1.000000000000009992 ) ) 
 REPRESENTATION_ITEM ( '' )  );
#9748=EDGE_CURVE ( 'NONE', #13929, #30170, #50059, .T. ) ;
#9751=CARTESIAN_POINT ( 'NONE',  ( 7.320508075688771044, 14.37500000000000178, 7.320508075688775484 ) ) ;
#9760=EDGE_CURVE ( 'NONE', #16864, #9554, #52493, .T. ) ;
#9765=ORIENTED_EDGE ( 'NONE', *, *, #54026, .T. ) ;
#9772=CARTESIAN_POINT ( 'NONE',  ( -8.311093377946841443, 74.21874999658601268, 8.311093377946830785 ) ) ;
#9777=CARTESIAN_POINT ( 'NONE',  ( -2.765530957081996810, 289.4218750017069510, -6.676582343750002480 ) ) ;
#9785=CARTESIAN_POINT ( 'NONE',  ( -11.35316468750000141, 173.8020833299193839, 3.042071309553159963 ) ) ;
#9792=CARTESIAN_POINT ( 'NONE',  ( 11.35316468749999963, 60.98958332991935549, -3.042071309553165293 ) ) ;
#9794=CARTESIAN_POINT ( 'NONE',  ( -8.660254037844387298, 23.95833332650536462, -5.000000000000004441 ) ) ;
#9798=CARTESIAN_POINT ( 'NONE',  ( -5.676582343750006032, 44.11458332991934839, 9.832129032723418760 ) ) ;
#9805=CARTESIAN_POINT ( 'NONE',  ( 11.35316468750000141, 40.78124999658601268, 0.000000000000000000 ) ) ;
#9808=CARTESIAN_POINT ( 'NONE',  ( -8.311093377946836114, 167.6562499965860411, -8.311093377946837890 ) ) ;
#9809=CARTESIAN_POINT ( 'NONE',  ( 10.00000000000000178, 147.0833333265053682, -2.679491924311226736 ) ) ;
#9812=CARTESIAN_POINT ( 'NONE',  ( -11.35316468749999785, 38.38541666325268409, -3.042071309553167957 ) ) ;
#9817=CARTESIAN_POINT ( 'NONE',  ( -11.35316468750000141, 168.2812499965860411, -1.390361679473963753E-15 ) ) ;
#9828=CARTESIAN_POINT ( 'NONE',  ( -3.042071309553164404, 122.5520833299193413, -11.35316468749999963 ) ) ;
#9852=CARTESIAN_POINT ( 'NONE',  ( 10.00000000000000178, 72.08333332650536818, -2.679491924311226736 ) ) ;
#9862=CARTESIAN_POINT ( 'NONE',  ( 10.00000000000000000, 114.7916666666666856, 2.679491924311236062 ) ) ;
#9864=CARTESIAN_POINT ( 'NONE',  ( 2.765530957082001251, 290.9218750017070647, 6.676582343750000703 ) ) ;
#9878=CARTESIAN_POINT ( 'NONE',  ( 7.320508075688774596, 225.6249999999999716, -7.320508075688774596 ) ) ;
#9880=CARTESIAN_POINT ( 'NONE',  ( 8.311093377946834337, 210.4687499965859843, 8.311093377946839666 ) ) ;
#9888=CARTESIAN_POINT ( 'NONE',  ( 8.311093377946837890, 11.40624999658601624, -8.311093377946837890 ) ) ;
#9895=CARTESIAN_POINT ( 'NONE',  ( -3.042071309553164404, 117.2395833299193555, -11.35316468749999963 ) ) ;
#9896=CARTESIAN_POINT ( 'NONE',  ( 4.999999999999993783, 96.04166665983871098, 8.660254037844390851 ) ) ;
#9899=CARTESIAN_POINT ( 'NONE',  ( -10.00000000000000000, 199.1666666598386826, -2.679491924311229845 ) ) ;
#9900=CARTESIAN_POINT ( 'NONE',  ( 6.123233995736767268E-16, 38.12499999317203958, -10.00000000000000178 ) ) ;
#9903=CARTESIAN_POINT ( 'NONE',  ( 1.226468279477575784E-15, 290.8593750017070079, 6.676582343750001591 ) ) ;
#9910=CARTESIAN_POINT ( 'NONE',  ( 6.123233995736767268E-16, 88.12499999317203958, -10.00000000000000178 ) ) ;
#9911=CARTESIAN_POINT ( 'NONE',  ( -8.311093377946841443, 149.2187499965860127, 8.311093377946834337 ) ) ;
#9914=CARTESIAN_POINT ( 'NONE',  ( 11.35316468749999785, 75.88541666325268409, 3.042071309553174174 ) ) ;
#9921=CARTESIAN_POINT ( 'NONE',  ( -2.485281374238572649, 290.2500000034139589, 6.000000000000002665 ) ) ;
#9938=CARTESIAN_POINT ( 'NONE',  ( -2.485281374238875962, 289.8125000000000000, -5.999999999999697131 ) ) ;
#9942=EDGE_CURVE ( 'NONE', #7527, #61049, #42326, .T. ) ;
#9943=CARTESIAN_POINT ( 'NONE',  ( 2.485281374238152097, 299.6875000000000568, -6.000000000000420997 ) ) ;
#9944=EDGE_LOOP ( 'NONE', ( #54448, #28486, #13719, #20920 ) ) ;
#9945=CARTESIAN_POINT ( 'NONE',  ( -4.999999999999995559, 1.666666666666664520, -8.660254037844385522 ) ) ;
#9949=CARTESIAN_POINT ( 'NONE',  ( 10.00000000000000178, 65.20833333333334281, -2.679491924311226736 ) ) ;
#9951=CARTESIAN_POINT ( 'NONE',  ( 6.000000000000003553, 293.5625000000001137, -2.485281374238571761 ) ) ;
#9955=CARTESIAN_POINT ( 'NONE',  ( 6.350741970897364085E-13, 216.2499999999999432, -9.999999999999998224 ) ) ;
#9962=CARTESIAN_POINT ( 'NONE',  ( -2.679491924311225848, 191.4583333333333428, -10.00000000000000178 ) ) ;
#9963=( BOUNDED_CURVE ( )  B_SPLINE_CURVE ( 2, ( #69188, #12208, #35246, #52216, #29204, #17501, #64271, #549, #35608, #40518, #23531, #46544, #51089 ),
 .UNSPECIFIED., .F., .F. ) 
 B_SPLINE_CURVE_WITH_KNOTS ( ( 3, 2, 2, 2, 2, 2, 3 ),
 ( 0.1684782608695652162, 0.1702898550724637750, 0.1721014492753623060, 0.1739130434782608647, 0.1757246376811594235, 0.1775362318840579823, 0.1793478260869565133 ),
 .UNSPECIFIED. ) 
 CURVE ( )  GEOMETRIC_REPRESENTATION_ITEM ( )  RATIONAL_B_SPLINE_CURVE ( ( 1.000000000000000000, 0.9659258262890683122, 1.000000000000000000, 0.9659258262890683122, 1.000000000000000000, 0.9659258262890683122, 1.000000000000000000, 0.9659258262890683122, 1.000000000000000000, 0.9659258262890683122, 1.000000000000000000, 0.9659258262890683122, 1.000000000000000000 ) ) 
 REPRESENTATION_ITEM ( '' )  );
#9966=CARTESIAN_POINT ( 'NONE',  ( -9.832129032723420536, 164.0104166632526983, 5.676582343749997150 ) ) ;
#9973=CARTESIAN_POINT ( 'NONE',  ( -8.311093377946841443, 29.21874999658601979, 8.311093377946830785 ) ) ;
#9975=CYLINDRICAL_SURFACE ( 'NONE', #14289, 10.00000000000000178 ) ;
#9980=CARTESIAN_POINT ( 'NONE',  ( -10.00000000000000178, 44.37499999317203248, -1.224646799147353454E-15 ) ) ;
#9986=ORIENTED_EDGE ( 'NONE', *, *, #27826, .T. ) ;
#9994=CARTESIAN_POINT ( 'NONE',  ( 3.042071309553167069, 146.8229166632527267, -11.35316468749999785 ) ) ;
#10001=CARTESIAN_POINT ( 'NONE',  ( -11.35316468750000141, 128.2812499965860127, -1.390361679473963753E-15 ) ) ;
#10005=CARTESIAN_POINT ( 'NONE',  ( 6.123233995736767268E-16, 23.12499999317203603, -10.00000000000000178 ) ) ;
#10007=CARTESIAN_POINT ( 'NONE',  ( 5.676582343749993598, 120.2604166632526841, 9.832129032723422313 ) ) ;
#10012=CARTESIAN_POINT ( 'NONE',  ( -9.832129032723420536, 29.01041666325268764, 5.676582343749997150 ) ) ;
#10014=DIRECTION ( 'NONE',  ( -0.000000000000000000, 1.000000000000000000, -0.000000000000000000 ) ) ;
#10019=CARTESIAN_POINT ( 'NONE',  ( 6.676582343750003368, 288.0156250017069510, -2.765530957081997254 ) ) ;
#10023=CARTESIAN_POINT ( 'NONE',  ( -5.676582343750006032, 149.4270833299193555, 9.832129032723418760 ) ) ;
#10038=CARTESIAN_POINT ( 'NONE',  ( 11.35316468749999785, 180.5729166632526983, 3.042071309553174174 ) ) ;
#10040=CARTESIAN_POINT ( 'NONE',  ( -4.721056650415999201, 288.3281250017069510, -4.721056650415999201 ) ) ;
#10041=DIRECTION ( 'NONE',  ( 0.000000000000000000, 0.000000000000000000, 1.000000000000000000 ) ) ;
#10050=CARTESIAN_POINT ( 'NONE',  ( 8.660254037844385522, 144.5833333333333428, 5.000000000000005329 ) ) ;
#10054=CARTESIAN_POINT ( 'NONE',  ( -11.35316468749999785, 113.3854166632526841, -3.042071309553167513 ) ) ;
#10062=CARTESIAN_POINT ( 'NONE',  ( 9.969536597484252027, 224.9231957930772410, 0.9796593664695627535 ) ) ;
#10063=CARTESIAN_POINT ( 'NONE',  ( 6.951808397369818766E-16, 222.0312499965860127, -11.35316468750000141 ) ) ;
#10064=( BOUNDED_CURVE ( )  B_SPLINE_CURVE ( 2, ( #12544, #35572, #7264, #1615, #18947, #41951, #64959, #9117, #49472, #61912, #32134, #50218, #66074 ),
 .UNSPECIFIED., .F., .F. ) 
 B_SPLINE_CURVE_WITH_KNOTS ( ( 3, 2, 2, 2, 2, 2, 3 ),
 ( 0.7445652173913043237, 0.7463768115942028825, 0.7481884057971014412, 0.7500000000000000000, 0.7518115942028985588, 0.7536231884057971175, 0.7554347826086956763 ),
 .UNSPECIFIED. ) 
 CURVE ( )  GEOMETRIC_REPRESENTATION_ITEM ( )  RATIONAL_B_SPLINE_CURVE ( ( 1.000000000000000000, 0.9659258262890683122, 1.000000000000000000, 0.9659258262890683122, 1.000000000000000000, 0.9659258262890683122, 1.000000000000000000, 0.9659258262890683122, 1.000000000000000000, 0.9659258262890683122, 1.000000000000000000, 0.9659258262890683122, 1.000000000000000000 ) ) 
 REPRESENTATION_ITEM ( '' )  );
#10066=CARTESIAN_POINT ( 'NONE',  ( -8.311093377946841443, 204.2187499965860411, 8.311093377946830785 ) ) ;
#10072=CARTESIAN_POINT ( 'NONE',  ( 8.660254037844383745, 185.4166666666666856, -4.999999999999997335 ) ) ;
#10074=CARTESIAN_POINT ( 'NONE',  ( -11.35316468750000141, 98.48958332991936970, 3.042071309553159963 ) ) ;
#10080=CARTESIAN_POINT ( 'NONE',  ( 9.832129032723416984, 105.3645833299193555, 5.676582343750006032 ) ) ;
#10088=CARTESIAN_POINT ( 'NONE',  ( -11.35316468750000141, 83.48958332991935549, 3.042071309553159963 ) ) ;
#10091=EDGE_CURVE ( 'NONE', #3422, #54835, #69888, .T. ) ;
#10093=CARTESIAN_POINT ( 'NONE',  ( -2.679491924311235618, 180.4166666598387394, 10.00000000000000000 ) ) ;
#10095=CARTESIAN_POINT ( 'NONE',  ( -2.085542519210945728E-15, 69.84374999658601268, 11.35316468750000141 ) ) ;
#10096=CARTESIAN_POINT ( 'NONE',  ( -2.765530957081998586, 290.6406250017069510, 6.676582343750001591 ) ) ;
#10099=CARTESIAN_POINT ( 'NONE',  ( 11.35316468750000141, 210.7812499965860411, 0.000000000000000000 ) ) ;
#10104=CARTESIAN_POINT ( 'NONE',  ( -3.042071309553173730, 209.3229166632526983, 11.35316468749999785 ) ) ;
#10109=CARTESIAN_POINT ( 'NONE',  ( -5.676582343750006032, 189.4270833299193555, 9.832129032723418760 ) ) ;
#10115=CARTESIAN_POINT ( 'NONE',  ( -4.999999999999998224, 16.66666666666666785, -8.660254037844389075 ) ) ;
#10135=CARTESIAN_POINT ( 'NONE',  ( 11.35316468749999963, 71.30208332991932707, -3.042071309553165293 ) ) ;
#10140=CARTESIAN_POINT ( 'NONE',  ( 2.765530957082001251, 291.9218750017069510, 6.676582343749999815 ) ) ;
#10145=ADVANCED_FACE ( 'NONE', ( #51823 ), #35961, .T. ) ;
#10151=CARTESIAN_POINT ( 'NONE',  ( -5.676582343750006032, 169.4270833299193555, 9.832129032723418760 ) ) ;
#10159=CARTESIAN_POINT ( 'NONE',  ( 11.35316468749999963, 50.98958332991934839, -3.042071309553165293 ) ) ;
#10161=CARTESIAN_POINT ( 'NONE',  ( 10.00000000000000178, 16.87499999317203248, 0.000000000000000000 ) ) ;
#10165=CARTESIAN_POINT ( 'NONE',  ( -5.000000000000005329, 170.2083333265053682, 8.660254037844387298 ) ) ;
#10167=CARTESIAN_POINT ( 'NONE',  ( -9.832129032723420536, 48.69791666325268409, 5.676582343749997150 ) ) ;
#10171=CARTESIAN_POINT ( 'NONE',  ( -7.320508075688779037, 13.12500000000000355, 7.320508075688770155 ) ) ;
#10173=CARTESIAN_POINT ( 'NONE',  ( -5.676582343750006032, 44.11458332991934839, 9.832129032723418760 ) ) ;
#10176=CARTESIAN_POINT ( 'NONE',  ( -11.35316468750000141, 178.2812499965860411, -1.390361679473963753E-15 ) ) ;
#10178=CARTESIAN_POINT ( 'NONE',  ( 6.123233995736767268E-16, 138.1249999931720538, -10.00000000000000178 ) ) ;
#10182=CARTESIAN_POINT ( 'NONE',  ( -8.311093377946841443, 34.21874999658601268, 8.311093377946834337 ) ) ;
#10184=CARTESIAN_POINT ( 'NONE',  ( -8.660254037844390851, 79.79166665983871098, 4.999999999999998224 ) ) ;
#10185=EDGE_LOOP ( 'NONE', ( #847, #18597, #30637, #40077 ) ) ;
#10191=CARTESIAN_POINT ( 'NONE',  ( 11.35316468749999963, 170.9895833299193839, -3.042071309553165293 ) ) ;
#10200=CARTESIAN_POINT ( 'NONE',  ( 11.35316468749999963, 121.3020833299193697, -3.042071309553165293 ) ) ;
#10201=CARTESIAN_POINT ( 'NONE',  ( 4.999999999999993783, 11.04166665983870033, 8.660254037844390851 ) ) ;
#10202=ORIENTED_EDGE ( 'NONE', *, *, #43967, .T. ) ;
#10231=CARTESIAN_POINT ( 'NONE',  ( -4.999999999999998224, 126.6666666666666714, -8.660254037844389075 ) ) ;
#10234=CARTESIAN_POINT ( 'NONE',  ( 2.765530957081996366, 293.2968750017069510, -6.676582343750003368 ) ) ;
#10236=ORIENTED_EDGE ( 'NONE', *, *, #69038, .F. ) ;
#10247=DIRECTION ( 'NONE',  ( -0.000000000000000000, 1.000000000000000000, -0.000000000000000000 ) ) ;
#10248=CARTESIAN_POINT ( 'NONE',  ( -11.35316468750000141, 18.28124999658601624, -1.390361679473963753E-15 ) ) ;
#10250=CARTESIAN_POINT ( 'NONE',  ( 5.676582343750001591, 211.9270833299193555, -9.832129032723420536 ) ) ;
#10252=CARTESIAN_POINT ( 'NONE',  ( 2.485281374238266672, 290.6874999999999432, -6.000000000000306422 ) ) ;
#10254=CYLINDRICAL_SURFACE ( 'NONE', #54354, 6.000000000000001776 ) ;
#10258=EDGE_CURVE ( 'NONE', #71793, #24215, #44339, .T. ) ;
#10259=CARTESIAN_POINT ( 'NONE',  ( 3.042071309553159519, 14.73958332991935016, 11.35316468750000141 ) ) ;
#10261=CARTESIAN_POINT ( 'NONE',  ( 6.000000000000003553, 292.5625000000000000, -2.485281374238571761 ) ) ;
#10265=CARTESIAN_POINT ( 'NONE',  ( 6.951808397369818766E-16, 12.03124999658601801, -11.35316468750000141 ) ) ;
#10267=CARTESIAN_POINT ( 'NONE',  ( -11.35316468749999785, 128.0729166632526983, -3.042071309553167513 ) ) ;
#10269=CARTESIAN_POINT ( 'NONE',  ( -1.836970198721029983E-15, 100.6249999931720396, 10.00000000000000178 ) ) ;
#10272=CARTESIAN_POINT ( 'NONE',  ( -4.999999999999998224, 198.5416666598387110, -8.660254037844389075 ) ) ;
#10276=CARTESIAN_POINT ( 'NONE',  ( -2.765530957081996810, 288.4218750017070079, -6.676582343750003368 ) ) ;
#10283=VERTEX_POINT ( 'NONE', #43083 ) ;
#10284=( BOUNDED_CURVE ( )  B_SPLINE_CURVE ( 2, ( #10848, #23654, #74593, #40261, #46661, #69680, #11588, #28195, #17993, #33507, #50833, #73844, #56882 ),
 .UNSPECIFIED., .F., .F. ) 
 B_SPLINE_CURVE_WITH_KNOTS ( ( 3, 2, 2, 2, 2, 2, 3 ),
 ( 0.4184782608695651884, 0.4202898550724636917, 0.4221014492753622505, 0.4239130434782608092, 0.4257246376811593680, 0.4275362318840579268, 0.4293478260869564855 ),
 .UNSPECIFIED. ) 
 CURVE ( )  GEOMETRIC_REPRESENTATION_ITEM ( )  RATIONAL_B_SPLINE_CURVE ( ( 1.000000000000001110, 0.9659258262890673130, 1.000000000000000000, 0.9659258262890683122, 1.000000000000000000, 0.9659258262890683122, 1.000000000000000000, 0.9659258262890683122, 1.000000000000000000, 0.9659258262890683122, 1.000000000000000000, 0.9659258262890693114, 0.9999999999999990008 ) ) 
 REPRESENTATION_ITEM ( '' )  );
#10287=CARTESIAN_POINT ( 'NONE',  ( 8.311093377946837890, 151.7187499965860127, -8.311093377946837890 ) ) ;
#10290=CARTESIAN_POINT ( 'NONE',  ( 9.832129032723420536, 81.51041666325268409, -5.676582343749999815 ) ) ;
#10297=CARTESIAN_POINT ( 'NONE',  ( 4.999999999999993783, 66.04166665983871098, 8.660254037844390851 ) ) ;
#10314=ORIENTED_EDGE ( 'NONE', *, *, #53452, .T. ) ;
#10319=CARTESIAN_POINT ( 'NONE',  ( -1.836970198721029983E-15, 83.75000000000000000, 10.00000000000000178 ) ) ;
#10322=CARTESIAN_POINT ( 'NONE',  ( 6.000000000000003553, 291.5625000000000000, -2.485281374238571761 ) ) ;
#10323=AXIS2_PLACEMENT_3D ( 'NONE', #43002, #49799, #65651 ) ;
#10334=CARTESIAN_POINT ( 'NONE',  ( -10.00000000000000000, 197.2916666666666856, -2.679491924311229845 ) ) ;
#10337=CARTESIAN_POINT ( 'NONE',  ( -9.832129032723420536, 169.0104166632526983, 5.676582343749997150 ) ) ;
#10340=CARTESIAN_POINT ( 'NONE',  ( 10.00000000000018119, 154.7916666666667993, 2.679491924311284468 ) ) ;
#10344=CARTESIAN_POINT ( 'NONE',  ( 3.042071309553167069, 17.13541666325268409, -11.35316468749999785 ) ) ;
#10351=CARTESIAN_POINT ( 'NONE',  ( 7.320508075688774596, 57.49999999317203958, -7.320508075688774596 ) ) ;
#10358=VERTEX_POINT ( 'NONE', #26096 ) ;
#10359=CARTESIAN_POINT ( 'NONE',  ( -10.00000000000000355, 222.7083333333333428, 2.679491924311223183 ) ) ;
#10360=CARTESIAN_POINT ( 'NONE',  ( 1.479685137562080274E-15, 225.9999999999999432, -10.00000000000000178 ) ) ;
#10363=CARTESIAN_POINT ( 'NONE',  ( -11.35316468750000141, 143.4895833299193839, 3.042071309553159963 ) ) ;
#10376=CARTESIAN_POINT ( 'NONE',  ( 11.35316468750000141, 121.0937499965860269, 0.000000000000000000 ) ) ;
#10380=CARTESIAN_POINT ( 'NONE',  ( 3.042071309553167069, 37.13541666325268409, -11.35316468749999785 ) ) ;
#10387=CARTESIAN_POINT ( 'NONE',  ( -4.242640687119285658, 296.1875000034139589, 4.242640687119287435 ) ) ;
#10388=VECTOR ( 'NONE', #10014, 1000.000000000000000 ) ;
#10390=DIRECTION ( 'NONE',  ( -0.000000000000000000, 1.000000000000000000, -0.000000000000000000 ) ) ;
#10392=CARTESIAN_POINT ( 'NONE',  ( -5.676582343749998039, 152.7604166632526983, -9.832129032723420536 ) ) ;
#10406=DIRECTION ( 'NONE',  ( 0.000000000000000000, 0.000000000000000000, 1.000000000000000000 ) ) ;
#10407=CARTESIAN_POINT ( 'NONE',  ( 6.123233995736767268E-16, 46.25000000000000711, -10.00000000000000178 ) ) ;
#10410=CARTESIAN_POINT ( 'NONE',  ( -4.088227598258586603E-16, 289.2031250017069510, -6.676582343750001591 ) ) ;
#10411=EDGE_CURVE ( 'NONE', #33509, #65401, #13453, .T. ) ;
#10412=CARTESIAN_POINT ( 'NONE',  ( 2.679491924311227624, 96.04166666666665719, -9.999999999999994671 ) ) ;
#10421=CARTESIAN_POINT ( 'NONE',  ( -7.320508075688773708, 146.8749999999999716, -7.320508075688774596 ) ) ;
#10425=CARTESIAN_POINT ( 'NONE',  ( -8.311093377946841443, 129.2187499965860127, 8.311093377946830785 ) ) ;
#10432=CARTESIAN_POINT ( 'NONE',  ( 9.543466050813522727, 224.7571304811999937, 3.001353285571292773 ) ) ;
#10434=CARTESIAN_POINT ( 'NONE',  ( 0.000000000000000000, 300.0000000000000000, 0.000000000000000000 ) ) ;
#10437=CARTESIAN_POINT ( 'NONE',  ( 5.676582343749993598, 205.2604166632526983, 9.832129032723422313 ) ) ;
#10444=CARTESIAN_POINT ( 'NONE',  ( 8.311093377946837890, 96.40624999658602690, -8.311093377946837890 ) ) ;
#10450=CARTESIAN_POINT ( 'NONE',  ( -3.042071309553173730, 104.3229166632526983, 11.35316468749999785 ) ) ;
#10457=CARTESIAN_POINT ( 'NONE',  ( -11.35316468750000141, 88.48958332991934128, 3.042071309553159963 ) ) ;
#10462=CARTESIAN_POINT ( 'NONE',  ( 10.00000000000000178, 182.0833333265053682, -2.679491924311226736 ) ) ;
#10465=CARTESIAN_POINT ( 'NONE',  ( 6.000000000000003553, 296.6250000034139589, -2.485281374238571761 ) ) ;
#10466=CARTESIAN_POINT ( 'NONE',  ( -5.676582343750006032, 69.42708332991935549, 9.832129032723418760 ) ) ;
#10467=CARTESIAN_POINT ( 'NONE',  ( 4.721056650416000089, 290.8281250017069510, 4.721056650415999201 ) ) ;
#10469=CARTESIAN_POINT ( 'NONE',  ( -11.35316468749999785, 223.0729166632527267, -3.042071309553167513 ) ) ;
#10474=CARTESIAN_POINT ( 'NONE',  ( -11.35316468749999785, 203.0729166632526699, -3.042071309553167957 ) ) ;
#10477=CARTESIAN_POINT ( 'NONE',  ( 6.676582343750003368, 299.0156250017069510, -2.765530957081997254 ) ) ;
#10478=ORIENTED_EDGE ( 'NONE', *, *, #30261, .F. ) ;
#10479=CARTESIAN_POINT ( 'NONE',  ( 3.042071309553167513, 192.1354166632526130, -11.35316468749999785 ) ) ;
#10484=ORIENTED_EDGE ( 'NONE', *, *, #39807, .T. ) ;
#10487=CARTESIAN_POINT ( 'NONE',  ( -7.320508075688778149, 13.12500000000000178, 7.320508075688769267 ) ) ;
#10496=EDGE_CURVE ( 'NONE', #5834, #21207, #23618, .T. ) ;
#10499=CARTESIAN_POINT ( 'NONE',  ( -2.319934922699201535E-11, 23.74999999999819522, 10.00000000000000178 ) ) ;
#10508=ORIENTED_EDGE ( 'NONE', *, *, #20267, .T. ) ;
#10510=CARTESIAN_POINT ( 'NONE',  ( 8.311093377946837890, 86.71874999658601268, -8.311093377946837890 ) ) ;
#10515=CARTESIAN_POINT ( 'NONE',  ( 2.765530957081996366, 291.2968750017069510, -6.676582343750002480 ) ) ;
#10518=CARTESIAN_POINT ( 'NONE',  ( 9.832129032723420536, 206.1979166632526983, -5.676582343749999815 ) ) ;
#10523=CARTESIAN_POINT ( 'NONE',  ( -9.832129032723418760, 173.1770833299193555, -5.676582343750004256 ) ) ;
#10526=CARTESIAN_POINT ( 'NONE',  ( -9.999999999999992895, 207.2916666666666856, -2.679491924311228512 ) ) ;
#10530=CARTESIAN_POINT ( 'NONE',  ( 11.35316468750000141, 60.78124999658601979, 0.000000000000000000 ) ) ;
#10532=CARTESIAN_POINT ( 'NONE',  ( -7.320508075688778149, 19.99999999317203603, 7.320508075688769267 ) ) ;
#10538=CARTESIAN_POINT ( 'NONE',  ( 9.832129032723420536, 61.19791666325267698, -5.676582343749999815 ) ) ;
#10544=CARTESIAN_POINT ( 'NONE',  ( 5.676582343750001591, 41.61458332991934839, -9.832129032723420536 ) ) ;
#10547=CARTESIAN_POINT ( 'NONE',  ( -9.832129032723420536, 173.6979166632526983, 5.676582343749997150 ) ) ;
#10548=CARTESIAN_POINT ( 'NONE',  ( 4.999999999999993783, 136.0416666598387110, 8.660254037844390851 ) ) ;
#10552=CARTESIAN_POINT ( 'NONE',  ( -3.042071309553173730, 29.63541666325268409, 11.35316468749999785 ) ) ;
#10554=CARTESIAN_POINT ( 'NONE',  ( 11.35316468749999785, 165.5729166632526415, 3.042071309553174174 ) ) ;
#10561=CARTESIAN_POINT ( 'NONE',  ( 5.676582343750001591, 166.6145833299193555, -9.832129032723420536 ) ) ;
#10570=CARTESIAN_POINT ( 'NONE',  ( -3.042071309553164404, 117.5520833299193413, -11.35316468749999963 ) ) ;
#10577=EDGE_CURVE ( 'NONE', #6677, #65401, #67305, .T. ) ;
#10584=ORIENTED_EDGE ( 'NONE', *, *, #5374, .T. ) ;
#10603=CARTESIAN_POINT ( 'NONE',  ( -5.000000000000008882, 128.3333333333333428, 8.660254037844390851 ) ) ;
#10604=CARTESIAN_POINT ( 'NONE',  ( -8.660254037844387298, 122.0833333333333286, -5.000000000000004441 ) ) ;
#10615=DIRECTION ( 'NONE',  ( 0.000000000000000000, -1.000000000000000000, 0.000000000000000000 ) ) ;
#10620=CARTESIAN_POINT ( 'NONE',  ( 9.832129032723416984, 15.36458332991935016, 5.676582343750006032 ) ) ;
#10622=DIRECTION ( 'NONE',  ( -0.000000000000000000, 1.000000000000000000, -0.000000000000000000 ) ) ;
#10623=CARTESIAN_POINT ( 'NONE',  ( 8.311093377946837890, 211.7187499965860127, -8.311093377946837890 ) ) ;
#10624=FACE_OUTER_BOUND ( 'NONE', #57710, .T. ) ;
#10629=CARTESIAN_POINT ( 'NONE',  ( -5.676582343750006032, 24.11458332991935194, 9.832129032723418760 ) ) ;
#10635=CARTESIAN_POINT ( 'NONE',  ( 9.832129032723416984, 10.36458332991935016, 5.676582343750006032 ) ) ;
#10637=CARTESIAN_POINT ( 'NONE',  ( 8.311093377946837890, 141.4062499965860127, -8.311093377946837890 ) ) ;
#10638=CARTESIAN_POINT ( 'NONE',  ( 2.679491924311222739, 105.8333333265053824, 10.00000000000000355 ) ) ;
#10645=CARTESIAN_POINT ( 'NONE',  ( 2.765530957081996366, 291.2968750017069510, -6.676582343750003368 ) ) ;
#10656=CARTESIAN_POINT ( 'NONE',  ( 5.676582343750001591, 76.92708332991935549, -9.832129032723420536 ) ) ;
#10663=VECTOR ( 'NONE', #50949, 1000.000000000000000 ) ;
#10688=CARTESIAN_POINT ( 'NONE',  ( 5.000000000000001776, 80.83333333333334281, -8.660254037844389075 ) ) ;
#10690=CARTESIAN_POINT ( 'NONE',  ( 4.242640687119285658, 290.6249999999999432, -4.242640687119286547 ) ) ;
#10697=CARTESIAN_POINT ( 'NONE',  ( 0.000000000000000000, 300.0000000000000000, 6.000000000000001776 ) ) ;
#10700=CARTESIAN_POINT ( 'NONE',  ( 10.00000000000000178, 205.0000000000000284, 0.000000000000000000 ) ) ;
#10702=CARTESIAN_POINT ( 'NONE',  ( -3.042071309553164404, 167.5520833299193271, -11.35316468749999963 ) ) ;
#10703=CARTESIAN_POINT ( 'NONE',  ( -3.166186134455097228E-13, 211.2500000000000568, -9.999999999999998224 ) ) ;
#10709=CARTESIAN_POINT ( 'NONE',  ( -9.832129032723420536, 24.01041666325268409, 5.676582343749997150 ) ) ;
#10711=CARTESIAN_POINT ( 'NONE',  ( 6.123233995736767268E-16, 133.1249999931720254, -10.00000000000000178 ) ) ;
#10717=CARTESIAN_POINT ( 'NONE',  ( 4.999999999999993783, 66.04166665983871098, 8.660254037844390851 ) ) ;
#10720=CARTESIAN_POINT ( 'NONE',  ( 2.679491924311236506, 63.95833333333336412, 10.00000000000005507 ) ) ;
#10722=CARTESIAN_POINT ( 'NONE',  ( 7.320508075688774596, 165.6250000000000568, -7.320508075688774596 ) ) ;
#10729=CARTESIAN_POINT ( 'NONE',  ( 11.35316468749999963, 135.9895833299193271, -3.042071309553165293 ) ) ;
#10731=DIRECTION ( 'NONE',  ( -0.000000000000000000, 1.000000000000000000, 0.000000000000000000 ) ) ;
#10742=CARTESIAN_POINT ( 'NONE',  ( 5.676582343750001591, 131.9270833299193555, -9.832129032723420536 ) ) ;
#10746=CARTESIAN_POINT ( 'NONE',  ( -11.35316468749999785, 33.38541666325269119, -3.042071309553167513 ) ) ;
#10754=CARTESIAN_POINT ( 'NONE',  ( -3.673940397442060854E-16, 296.8125000034140157, -6.000000000000001776 ) ) ;
#10755=CARTESIAN_POINT ( 'NONE',  ( 6.123233995736767268E-16, 113.1249999931720396, -10.00000000000000178 ) ) ;
#10756=CARTESIAN_POINT ( 'NONE',  ( 6.951808397369818766E-16, 157.3437499965860127, -11.35316468750000141 ) ) ;
#10758=CIRCLE ( 'NONE', #5928, 10.00000000000000178 ) ;
#10772=CARTESIAN_POINT ( 'NONE',  ( 1.102182119232618108E-15, 298.3125000034140157, 6.000000000000001776 ) ) ;
#10774=CARTESIAN_POINT ( 'NONE',  ( -4.999999999999998224, 36.66666666666666430, -8.660254037844389075 ) ) ;
#10777=CARTESIAN_POINT ( 'NONE',  ( 6.676582343750001591, 288.9531250017069510, -8.176455196517173205E-16 ) ) ;
#10779=CARTESIAN_POINT ( 'NONE',  ( 8.660254037844385522, 35.41666666666665719, -4.999999999999998224 ) ) ;
#10780=CARTESIAN_POINT ( 'NONE',  ( 8.660254037844389075, 197.2916666598387110, -5.000000000000000000 ) ) ;
#10787=CARTESIAN_POINT ( 'NONE',  ( -5.000000000000005329, 148.3333333333333428, 8.660254037844387298 ) ) ;
#10790=CARTESIAN_POINT ( 'NONE',  ( -7.320508075688773708, 166.8750000000000284, -7.320508075688774596 ) ) ;
#10793=CARTESIAN_POINT ( 'NONE',  ( 8.311093377946834337, 130.4687499965860127, 8.311093377946839666 ) ) ;
#10807=CARTESIAN_POINT ( 'NONE',  ( -11.35316468750000141, 208.5937499965860411, -1.390361679473963753E-15 ) ) ;
#10813=CARTESIAN_POINT ( 'NONE',  ( -5.676582343750006032, 94.11458332991935549, 9.832129032723418760 ) ) ;
#10819=CARTESIAN_POINT ( 'NONE',  ( -9.832129032723420536, 103.6979166632526841, 5.676582343749997150 ) ) ;
#10824=CARTESIAN_POINT ( 'NONE',  ( -8.660254037844387298, 223.9583333265053966, -5.000000000000004441 ) ) ;
#10828=CARTESIAN_POINT ( 'NONE',  ( -5.676582343750006032, 94.11458332991935549, 9.832129032723418760 ) ) ;
#10833=CARTESIAN_POINT ( 'NONE',  ( 2.679491924311228956, 177.9166666598387110, -10.00000000000000000 ) ) ;
#10835=CARTESIAN_POINT ( 'NONE',  ( 1.102182119232618108E-15, 296.3125000034140157, 6.000000000000001776 ) ) ;
#10836=CARTESIAN_POINT ( 'NONE',  ( -11.35316468750000141, 78.59374999658601268, -1.390361679473963753E-15 ) ) ;
#10837=CARTESIAN_POINT ( 'NONE',  ( -2.765530957081996810, 288.2656250017069510, -6.676582343750003368 ) ) ;
#10839=( BOUNDED_CURVE ( )  B_SPLINE_CURVE ( 2, ( #64962, #46882, #29170, #30276, #1254, #52185, #17841, #18217, #57855, #887, #58589, #6895, #18585 ),
 .UNSPECIFIED., .F., .F. ) 
 B_SPLINE_CURVE_WITH_KNOTS ( ( 3, 2, 2, 2, 2, 2, 3 ),
 ( 1.051889995858769966, 1.057123116408781094, 1.062356236958792222, 1.067589357508803127, 1.072822478058814255, 1.078055598608825383, 1.083288719158836511 ),
 .UNSPECIFIED. ) 
 CURVE ( )  GEOMETRIC_REPRESENTATION_ITEM ( )  RATIONAL_B_SPLINE_CURVE ( ( 1.000000000000000000, 0.9659258262890683122, 1.000000000000000000, 0.9659258262890683122, 1.000000000000000000, 0.9659258262890683122, 1.000000000000000000, 0.9659258262890683122, 1.000000000000000000, 0.9659258262890683122, 1.000000000000000000, 0.9659258262890578761, 1.000000000000010436 ) ) 
 REPRESENTATION_ITEM ( '' )  );
#10841=CARTESIAN_POINT ( 'NONE',  ( 9.832129032723416984, 220.3645833299193839, 5.676582343750006032 ) ) ;
#10843=CARTESIAN_POINT ( 'NONE',  ( 6.123233995736767268E-16, 68.12499999317203958, -10.00000000000000178 ) ) ;
#10845=CARTESIAN_POINT ( 'NONE',  ( 2.485281374238247132, 291.6874999999999432, -6.000000000000325961 ) ) ;
#10846=CARTESIAN_POINT ( 'NONE',  ( 5.676582343750001591, 211.6145833299193555, -9.832129032723420536 ) ) ;
#10848=CARTESIAN_POINT ( 'NONE',  ( 6.123233995736767268E-16, 98.12499999317203958, -10.00000000000000178 ) ) ;
#10849=CARTESIAN_POINT ( 'NONE',  ( 4.721056650416000089, 296.8281250017069510, 4.721056650415999201 ) ) ;
#10851=CARTESIAN_POINT ( 'NONE',  ( -9.832129032723418760, 193.1770833299193555, -5.676582343750004256 ) ) ;
#10858=CARTESIAN_POINT ( 'NONE',  ( 8.660254037844389075, 20.41666666666666785, -5.000000000000000000 ) ) ;
#10876=EDGE_CURVE ( 'NONE', #60165, #12530, #11061, .T. ) ;
#10883=CARTESIAN_POINT ( 'NONE',  ( -11.35316468749999785, 93.38541666325269830, -3.042071309553167513 ) ) ;
#10888=CARTESIAN_POINT ( 'NONE',  ( -6.676582343750002480, 290.5468750017070647, -2.765530957081996810 ) ) ;
#10892=CARTESIAN_POINT ( 'NONE',  ( 11.35316468750000141, 200.7812499965860411, 0.000000000000000000 ) ) ;
#10894=VERTEX_POINT ( 'NONE', #52066 ) ;
#10897=CARTESIAN_POINT ( 'NONE',  ( 11.35316468749999963, 161.3020833299193555, -3.042071309553165293 ) ) ;
#10900=CARTESIAN_POINT ( 'NONE',  ( 3.178432602446558121E-13, 206.2500000000000000, -10.00000000000000533 ) ) ;
#10901=CARTESIAN_POINT ( 'NONE',  ( -5.000000000000001776, 113.3333333333333286, 8.660254037844381969 ) ) ;
#10904=CARTESIAN_POINT ( 'NONE',  ( 9.832129032723416984, 55.36458332991934839, 5.676582343750006032 ) ) ;
#10911=CARTESIAN_POINT ( 'NONE',  ( -9.832129032723418760, 57.86458332991935549, -5.676582343750004256 ) ) ;
#10917=CARTESIAN_POINT ( 'NONE',  ( 11.35316468750000141, 45.78124999658601979, 0.000000000000000000 ) ) ;
#10920=CARTESIAN_POINT ( 'NONE',  ( -5.676582343749998039, 172.4479166632526983, -9.832129032723420536 ) ) ;
#10921=CARTESIAN_POINT ( 'NONE',  ( -2.679491924311225848, 138.3333333265053966, -10.00000000000000178 ) ) ;
#10924=CARTESIAN_POINT ( 'NONE',  ( 9.832129032723420536, 41.51041666325268409, -5.676582343749999815 ) ) ;
#10925=DIRECTION ( 'NONE',  ( -0.000000000000000000, 1.000000000000000000, -0.000000000000000000 ) ) ;
#10926=CARTESIAN_POINT ( 'NONE',  ( 8.311093377946834337, 180.1562499965859843, 8.311093377946839666 ) ) ;
#10933=CARTESIAN_POINT ( 'NONE',  ( -8.311093377946841443, 163.9062499965859843, 8.311093377946834337 ) ) ;
#10939=FACE_OUTER_BOUND ( 'NONE', #60914, .T. ) ;
#10942=VERTEX_POINT ( 'NONE', #26718 ) ;
#10945=CARTESIAN_POINT ( 'NONE',  ( 5.676582343750001591, 116.9270833299193555, -9.832129032723420536 ) ) ;
#10947=CARTESIAN_POINT ( 'NONE',  ( 8.660254037844389075, 12.29166665983870033, -5.000000000000000000 ) ) ;
#10964=CARTESIAN_POINT ( 'NONE',  ( 4.242640687119285658, 293.6249999999999432, -4.242640687119286547 ) ) ;
#10975=CARTESIAN_POINT ( 'NONE',  ( -4.242640687119285658, 290.1875000034139589, 4.242640687119287435 ) ) ;
#10977=CARTESIAN_POINT ( 'NONE',  ( -2.679491924311235618, 118.5416666666666572, 10.00000000000000000 ) ) ;
#10979=CARTESIAN_POINT ( 'NONE',  ( -2.765530957081998586, 287.7968750017070079, 6.676582343750001591 ) ) ;
#10993=CARTESIAN_POINT ( 'NONE',  ( 11.35316468749999785, 20.57291666325268409, 3.042071309553174174 ) ) ;
#10994=CARTESIAN_POINT ( 'NONE',  ( 0.000000000000000000, 300.0000000000000000, 0.000000000000000000 ) ) ;
#10995=CARTESIAN_POINT ( 'NONE',  ( -9.832129032723418760, 203.1770833299193555, -5.676582343750004256 ) ) ;
#11003=CARTESIAN_POINT ( 'NONE',  ( 11.35316468749999963, 15.98958332991934839, -3.042071309553165293 ) ) ;
#11005=CARTESIAN_POINT ( 'NONE',  ( 6.000000000000001776, 292.5000000000000000, -7.347880794884121708E-16 ) ) ;
#11009=CARTESIAN_POINT ( 'NONE',  ( 11.35316468750000141, 5.781249996586016238, 0.000000000000000000 ) ) ;
#11011=CARTESIAN_POINT ( 'NONE',  ( 11.35316468749999785, 130.5729166632526983, 3.042071309553174174 ) ) ;
#11014=CARTESIAN_POINT ( 'NONE',  ( 7.320508075688771044, 96.24999999317202537, 7.320508075688775484 ) ) ;
#11020=CARTESIAN_POINT ( 'NONE',  ( -7.320508075688777261, 116.8750000000000000, -7.320508075688778149 ) ) ;
#11022=CARTESIAN_POINT ( 'NONE',  ( -2.765530957081998586, 290.7968750017069510, 6.676582343750001591 ) ) ;
#11034=CARTESIAN_POINT ( 'NONE',  ( -5.676582343749998039, 82.76041666325268409, -9.832129032723420536 ) ) ;
#11035=ORIENTED_EDGE ( 'NONE', *, *, #33182, .T. ) ;
#11047=AXIS2_PLACEMENT_3D ( 'NONE', #10994, #10622, #5338 ) ;
#11051=DIRECTION ( 'NONE',  ( -0.000000000000000000, 1.000000000000000000, -0.000000000000000000 ) ) ;
#11061=( BOUNDED_CURVE ( )  B_SPLINE_CURVE ( 2, ( #29791, #46758, #30526, #53544, #403, #52801, #1859, #24845, #1135, #47863, #70884, #24113, #42200 ),
 .UNSPECIFIED., .F., .F. ) 
 B_SPLINE_CURVE_WITH_KNOTS ( ( 3, 2, 2, 2, 2, 2, 3 ),
 ( 2.339288409473456287, 2.344521723505997635, 2.349755037538538982, 2.354988351571080329, 2.360221665603621677, 2.365454979636163024, 2.370688293668704372 ),
 .UNSPECIFIED. ) 
 CURVE ( )  GEOMETRIC_REPRESENTATION_ITEM ( )  RATIONAL_B_SPLINE_CURVE ( ( 1.000000000000008438, 0.9659258262890599855, 1.000000000000000000, 0.9659258262890683122, 1.000000000000000000, 0.9659258262890683122, 1.000000000000000000, 0.9659258262890683122, 1.000000000000000000, 0.9659258262890683122, 1.000000000000000000, 0.9659258262890662028, 1.000000000000001998 ) ) 
 REPRESENTATION_ITEM ( '' )  );
#11067=CARTESIAN_POINT ( 'NONE',  ( -1.836970198721029983E-15, 78.75000000000000000, 10.00000000000000178 ) ) ;
#11071=CARTESIAN_POINT ( 'NONE',  ( -4.242640687119286547, 289.8750000000000000, -4.242640687119286547 ) ) ;
#11076=CARTESIAN_POINT ( 'NONE',  ( 0.000000000000000000, 300.0000000000000000, 10.00000000000000178 ) ) ;
#11079=CARTESIAN_POINT ( 'NONE',  ( -5.000000000000023093, 78.33333333333335702, 8.660254037844417496 ) ) ;
#11080=CARTESIAN_POINT ( 'NONE',  ( 2.679491924311228956, 206.0416666666666856, -10.00000000000000000 ) ) ;
#11082=CARTESIAN_POINT ( 'NONE',  ( -2.085542519210945728E-15, 169.8437499965860127, 11.35316468750000141 ) ) ;
#11086=CARTESIAN_POINT ( 'NONE',  ( -6.000000000000003553, 297.0000000034139589, -2.485281374238571317 ) ) ;
#11089=CARTESIAN_POINT ( 'NONE',  ( 8.311093377946837890, 31.71874999658601624, -8.311093377946837890 ) ) ;
#11099=CARTESIAN_POINT ( 'NONE',  ( 8.660254037844389075, 62.29166665983869677, -5.000000000000000000 ) ) ;
#11105=CARTESIAN_POINT ( 'NONE',  ( 10.00000000000000000, 101.6666666598386826, 2.679491924311235618 ) ) ;
#11107=ORIENTED_EDGE ( 'NONE', *, *, #54143, .T. ) ;
#11112=CARTESIAN_POINT ( 'NONE',  ( 3.042071309553159519, 144.7395833299193839, 11.35316468750000141 ) ) ;
#11124=CARTESIAN_POINT ( 'NONE',  ( 11.35316468749999785, 130.8854166632526699, 3.042071309553174174 ) ) ;
#11128=CARTESIAN_POINT ( 'NONE',  ( 11.35316468749999963, 36.30208332991935549, -3.042071309553165293 ) ) ;
#11129=VERTEX_POINT ( 'NONE', #73124 ) ;
#11131=CARTESIAN_POINT ( 'NONE',  ( -1.836970198721029983E-15, 43.75000000000000711, 10.00000000000000178 ) ) ;
#11135=CARTESIAN_POINT ( 'NONE',  ( -4.242640687119286547, 296.9375000034140157, -4.242640687119286547 ) ) ;
#11140=CARTESIAN_POINT ( 'NONE',  ( -3.042071309553173730, 159.6354166632526983, 11.35316468749999785 ) ) ;
#11150=ORIENTED_EDGE ( 'NONE', *, *, #12710, .F. ) ;
#11154=CARTESIAN_POINT ( 'NONE',  ( 2.679491924311228956, 41.04166666666667851, -10.00000000000000000 ) ) ;
#11157=CARTESIAN_POINT ( 'NONE',  ( -3.673940397442060854E-16, 299.7500000000000000, -6.000000000000001776 ) ) ;
#11158=CARTESIAN_POINT ( 'NONE',  ( 5.000000000000058620, 80.83333333333341386, -8.660254037844484998 ) ) ;
#11169=CARTESIAN_POINT ( 'NONE',  ( 4.999999999999993783, 159.1666666666666856, 8.660254037844390851 ) ) ;
#11171=DIRECTION ( 'NONE',  ( -0.000000000000000000, 1.000000000000000000, -0.000000000000000000 ) ) ;
#11173=CARTESIAN_POINT ( 'NONE',  ( 11.35316468750000141, 126.0937499965860127, 0.000000000000000000 ) ) ;
#11182=( BOUNDED_CURVE ( )  B_SPLINE_CURVE ( 2, ( #26700, #53895, #42561, #65572, #13869, #36912, #74491, #40909, #34154, #68460, #22799, #28095, #33784 ),
 .UNSPECIFIED., .F., .F. ) 
 B_SPLINE_CURVE_WITH_KNOTS ( ( 3, 2, 2, 2, 2, 2, 3 ),
 ( 0.8315217391304348116, 0.8333333333333333703, 0.8351449275362319291, 0.8369565217391304879, 0.8387681159420289356, 0.8405797101449274944, 0.8423913043478260532 ),
 .UNSPECIFIED. ) 
 CURVE ( )  GEOMETRIC_REPRESENTATION_ITEM ( )  RATIONAL_B_SPLINE_CURVE ( ( 1.000000000000000000, 0.9659258262890683122, 1.000000000000000000, 0.9659258262890683122, 1.000000000000000000, 0.9659258262890683122, 1.000000000000000000, 0.9659258262890683122, 1.000000000000000000, 0.9659258262890683122, 1.000000000000000000, 0.9659258262890683122, 1.000000000000000000 ) ) 
 REPRESENTATION_ITEM ( '' )  );
#11184=CARTESIAN_POINT ( 'NONE',  ( 5.676582343750001591, 216.9270833299193555, -9.832129032723420536 ) ) ;
#11190=CARTESIAN_POINT ( 'NONE',  ( 3.042071309553167069, 96.82291666325269830, -11.35316468749999785 ) ) ;
#11195=CARTESIAN_POINT ( 'NONE',  ( 11.35316468750000141, 100.7812499965860269, 0.000000000000000000 ) ) ;
#11200=CARTESIAN_POINT ( 'NONE',  ( -7.320508075688778149, 219.9999999931720538, 7.320508075688769267 ) ) ;
#11202=CARTESIAN_POINT ( 'NONE',  ( -3.673940397442060854E-16, 297.7500000000000000, -6.000000000000001776 ) ) ;
#11204=CARTESIAN_POINT ( 'NONE',  ( -11.35316468750000141, 93.28124999658602690, -1.390361679473963753E-15 ) ) ;
#11210=CARTESIAN_POINT ( 'NONE',  ( 8.660254037844389075, 192.2916666598387110, -5.000000000000000000 ) ) ;
#11212=CARTESIAN_POINT ( 'NONE',  ( 5.676582343750001591, 81.92708332991935549, -9.832129032723420536 ) ) ;
#11213=CARTESIAN_POINT ( 'NONE',  ( -2.765530957081998586, 291.6406250017068942, 6.676582343750001591 ) ) ;
#11216=CARTESIAN_POINT ( 'NONE',  ( -5.676582343750006032, 224.1145833299193839, 9.832129032723418760 ) ) ;
#11218=CARTESIAN_POINT ( 'NONE',  ( -10.00000000000000355, 69.58333332650538239, 2.679491924311223183 ) ) ;
#11220=CARTESIAN_POINT ( 'NONE',  ( 1.102182119232618108E-15, 291.2500000000000000, 6.000000000000001776 ) ) ;
#11221=CARTESIAN_POINT ( 'NONE',  ( 10.92737078412413787, 225.9999999999999147, -3.080083792328916825 ) ) ;
#11222=CARTESIAN_POINT ( 'NONE',  ( 8.660254037844385522, 46.45833332650536818, 5.000000000000005329 ) ) ;
#11223=CARTESIAN_POINT ( 'NONE',  ( 7.320508075688771044, 199.3750000000000000, 7.320508075688775484 ) ) ;
#11224=CARTESIAN_POINT ( 'NONE',  ( -4.088227598258586603E-16, 297.2031250017070079, -6.676582343750001591 ) ) ;
#11226=ORIENTED_EDGE ( 'NONE', *, *, #2505, .T. ) ;
#11228=CARTESIAN_POINT ( 'NONE',  ( 3.042071309553167513, 212.1354166632526983, -11.35316468749999785 ) ) ;
#11236=CARTESIAN_POINT ( 'NONE',  ( 5.000000000000001776, 10.83333333333333393, -8.660254037844389075 ) ) ;
#11253=VECTOR ( 'NONE', #65652, 1000.000000000000000 ) ;
#11257=CARTESIAN_POINT ( 'NONE',  ( -8.311093377946841443, 94.21874999658601268, 8.311093377946830785 ) ) ;
#11262=CARTESIAN_POINT ( 'NONE',  ( 2.679491924311591333, 68.95833333333338544, 9.999999999999793943 ) ) ;
#11265=CARTESIAN_POINT ( 'NONE',  ( -9.832129032723418760, 202.8645833299193555, -5.676582343750004256 ) ) ;
#11269=CARTESIAN_POINT ( 'NONE',  ( -5.676582343749998039, 167.7604166632526983, -9.832129032723420536 ) ) ;
#11273=CARTESIAN_POINT ( 'NONE',  ( -8.660254037844381969, 107.0833333333333428, -5.000000000000002665 ) ) ;
#11277=CARTESIAN_POINT ( 'NONE',  ( 9.832129032723420536, 56.19791666325269119, -5.676582343749999815 ) ) ;
#11285=CARTESIAN_POINT ( 'NONE',  ( 3.042071309553167069, 61.82291666325266988, -11.35316468749999785 ) ) ;
#11288=FACE_OUTER_BOUND ( 'NONE', #72755, .T. ) ;
#11290=CARTESIAN_POINT ( 'NONE',  ( -5.676582343749998039, 57.44791666325268409, -9.832129032723420536 ) ) ;
#11292=CYLINDRICAL_SURFACE ( 'NONE', #15590, 6.000000000000001776 ) ;
#11293=CARTESIAN_POINT ( 'NONE',  ( -5.676582343750006032, 174.1145833299193555, 9.832129032723418760 ) ) ;
#11295=CARTESIAN_POINT ( 'NONE',  ( 2.679491924311222739, 145.8333333265053398, 10.00000000000000355 ) ) ;
#11297=CARTESIAN_POINT ( 'NONE',  ( -5.000000000000005329, 55.20833332650536818, 8.660254037844387298 ) ) ;
#11298=CARTESIAN_POINT ( 'NONE',  ( 5.676582343749993598, 50.26041666325269119, 9.832129032723422313 ) ) ;
#11299=CARTESIAN_POINT ( 'NONE',  ( -10.00000000000000178, 79.37499999317202537, -1.224646799147353454E-15 ) ) ;
#11300=CARTESIAN_POINT ( 'NONE',  ( -2.085542519210945728E-15, 179.5312499965860411, 11.35316468750000141 ) ) ;
#11307=CARTESIAN_POINT ( 'NONE',  ( -9.832129032723420536, 183.6979166632526983, 5.676582343749997150 ) ) ;
#11316=CARTESIAN_POINT ( 'NONE',  ( -11.35316468750000141, 113.8020833299193555, 3.042071309553159963 ) ) ;
#11319=VERTEX_POINT ( 'NONE', #1426 ) ;
#11338=ORIENTED_EDGE ( 'NONE', *, *, #53117, .F. ) ;
#11346=CARTESIAN_POINT ( 'NONE',  ( 8.660254037844389075, 115.4166666666666714, -5.000000000000000000 ) ) ;
#11348=CARTESIAN_POINT ( 'NONE',  ( -4.721056650415999201, 289.4843750017070079, -4.721056650415999201 ) ) ;
#11351=LINE ( 'NONE', #33636, #32580 ) ;
#11361=CARTESIAN_POINT ( 'NONE',  ( -2.085542519210945728E-15, 9.531249996586018014, 11.35316468750000141 ) ) ;
#11362=EDGE_CURVE ( 'NONE', #49698, #56133, #29344, .T. ) ;
#11364=CARTESIAN_POINT ( 'NONE',  ( 5.676582343750001591, 206.9270833299193555, -9.832129032723420536 ) ) ;
#11368=DIRECTION ( 'NONE',  ( -0.000000000000000000, 1.000000000000000000, -0.000000000000000000 ) ) ;
#11371=CARTESIAN_POINT ( 'NONE',  ( -3.042071309553164404, 27.23958332991934839, -11.35316468749999963 ) ) ;
#11373=CARTESIAN_POINT ( 'NONE',  ( 4.999999999999994671, 209.1666666666666572, 8.660254037844390851 ) ) ;
#11377=CARTESIAN_POINT ( 'NONE',  ( 5.676582343749993598, 14.94791666325268409, 9.832129032723422313 ) ) ;
#11379=CARTESIAN_POINT ( 'NONE',  ( -2.085542519210945728E-15, 129.5312499965860127, 11.35316468750000141 ) ) ;
#11380=CARTESIAN_POINT ( 'NONE',  ( 4.999999999999993783, 101.0416666598386968, 8.660254037844390851 ) ) ;
#11386=CARTESIAN_POINT ( 'NONE',  ( -2.679491924311088624, 118.5416666666666714, 10.00000000000009237 ) ) ;
#11387=DIRECTION ( 'NONE',  ( 0.000000000000000000, 0.000000000000000000, 1.000000000000000000 ) ) ;
#11388=CARTESIAN_POINT ( 'NONE',  ( -4.088227598258586603E-16, 299.2031250017070079, -6.676582343750001591 ) ) ;
#11389=CARTESIAN_POINT ( 'NONE',  ( 11.35316468749999963, 130.9895833299193555, -3.042071309553165293 ) ) ;
#11396=ORIENTED_EDGE ( 'NONE', *, *, #22684, .T. ) ;
#11402=CARTESIAN_POINT ( 'NONE',  ( 8.311093377946837890, 71.71874999658601268, -8.311093377946837890 ) ) ;
#11403=ORIENTED_EDGE ( 'NONE', *, *, #49676, .F. ) ;
#11422=DIRECTION ( 'NONE',  ( 0.000000000000000000, 0.000000000000000000, 1.000000000000000000 ) ) ;
#11430=CARTESIAN_POINT ( 'NONE',  ( -1.967015505459129087E-11, 198.7499999999984936, 10.00000000000000533 ) ) ;
#11434=CARTESIAN_POINT ( 'NONE',  ( 10.00000000000000178, 80.00000000000000000, 0.000000000000000000 ) ) ;
#11436=CARTESIAN_POINT ( 'NONE',  ( 2.765530957082001251, 298.9218750017070647, 6.676582343750000703 ) ) ;
#11438=ORIENTED_EDGE ( 'NONE', *, *, #23025, .T. ) ;
#11447=CARTESIAN_POINT ( 'NONE',  ( -8.660254037844387298, 197.0833333333333428, -5.000000000000004441 ) ) ;
#11451=CARTESIAN_POINT ( 'NONE',  ( 5.676582343750001591, 166.9270833299193555, -9.832129032723420536 ) ) ;
#11455=CARTESIAN_POINT ( 'NONE',  ( 6.123233995736767268E-16, 88.12499999317203958, -10.00000000000000178 ) ) ;
#11458=CARTESIAN_POINT ( 'NONE',  ( 9.832129032723420536, 31.51041666325268764, -5.676582343749999815 ) ) ;
#11467=CARTESIAN_POINT ( 'NONE',  ( 10.00000000000000178, 67.08333332650536818, -2.679491924311226736 ) ) ;
#11471=CARTESIAN_POINT ( 'NONE',  ( 7.320508075688811900, 65.62500000000002842, -7.320508075688811900 ) ) ;
#11477=CARTESIAN_POINT ( 'NONE',  ( 1.226468279477575784E-15, 296.8593750017070079, 6.676582343750001591 ) ) ;
#11480=CARTESIAN_POINT ( 'NONE',  ( -8.311093377946841443, 148.9062499965860127, 8.311093377946830785 ) ) ;
#11487=ORIENTED_EDGE ( 'NONE', *, *, #68085, .T. ) ;
#11490=CARTESIAN_POINT ( 'NONE',  ( -9.832129032723420536, 134.0104166632526983, 5.676582343749997150 ) ) ;
#11495=CARTESIAN_POINT ( 'NONE',  ( -2.085542519210945728E-15, 34.84374999658601268, 11.35316468750000141 ) ) ;
#11502=CARTESIAN_POINT ( 'NONE',  ( 6.000000000000003553, 297.5000000034139589, 2.485281374238571317 ) ) ;
#11505=CARTESIAN_POINT ( 'NONE',  ( 3.042071309553159519, 160.0520833299193555, 11.35316468750000141 ) ) ;
#11518=CARTESIAN_POINT ( 'NONE',  ( 7.347880794884121708E-16, 300.0000000000000000, -6.000000000000001776 ) ) ;
#11522=CARTESIAN_POINT ( 'NONE',  ( -7.320508075688773708, 43.74999999317202537, -7.320508075688774596 ) ) ;
#11523=CARTESIAN_POINT ( 'NONE',  ( 5.000000000000001776, 35.83333333333333570, -8.660254037844389075 ) ) ;
#11526=CARTESIAN_POINT ( 'NONE',  ( 6.000000000000003553, 298.4375000000000000, 2.485281374238571317 ) ) ;
#11528=CARTESIAN_POINT ( 'NONE',  ( 10.00000000000000000, 196.6666666598386826, 2.679491924311235618 ) ) ;
#11533=CARTESIAN_POINT ( 'NONE',  ( -2.485281374238308860, 287.2500000034139589, 6.000000000000264677 ) ) ;
#11535=CARTESIAN_POINT ( 'NONE',  ( 8.660254037844385522, 201.4583333265053682, 5.000000000000005329 ) ) ;
#11536=CARTESIAN_POINT ( 'NONE',  ( 2.679491924311228956, 161.0416666666666288, -10.00000000000000000 ) ) ;
#11540=CARTESIAN_POINT ( 'NONE',  ( -9.832129032723418760, 123.1770833299193555, -5.676582343750004256 ) ) ;
#11546=CARTESIAN_POINT ( 'NONE',  ( 4.204081362154476587, 225.9042189071305700, -9.092352784983953384 ) ) ;
#11550=CARTESIAN_POINT ( 'NONE',  ( 11.35316468749999963, 226.3020833299193555, -3.042071309553165293 ) ) ;
#11557=CARTESIAN_POINT ( 'NONE',  ( 5.676582343750001591, 111.6145833299193555, -9.832129032723420536 ) ) ;
#11561=CARTESIAN_POINT ( 'NONE',  ( 3.490152628695403868E-12, 151.2499999999997442, -10.00000000000000178 ) ) ;
#11563=CARTESIAN_POINT ( 'NONE',  ( 3.042071309553159519, 104.7395833299193555, 11.35316468750000141 ) ) ;
#11566=CARTESIAN_POINT ( 'NONE',  ( 10.00000000000000178, 217.0833333265053682, -2.679491924311226736 ) ) ;
#11570=CARTESIAN_POINT ( 'NONE',  ( -3.042071309553173730, 104.3229166632526841, 11.35316468749999785 ) ) ;
#11574=CARTESIAN_POINT ( 'NONE',  ( 2.679491924305209327, 173.9583333333328312, 10.00000000000357581 ) ) ;
#11576=CARTESIAN_POINT ( 'NONE',  ( -10.00000000000000178, 194.3749999931720254, -1.224646799147353454E-15 ) ) ;
#11578=CARTESIAN_POINT ( 'NONE',  ( 3.042071309553159519, 85.05208332991934128, 11.35316468750000141 ) ) ;
#11579=CARTESIAN_POINT ( 'NONE',  ( -2.765530957081996810, 291.2656250017070079, -6.676582343750003368 ) ) ;
#11582=CARTESIAN_POINT ( 'NONE',  ( 11.35316468749999785, 220.5729166632526983, 3.042071309553174174 ) ) ;
#11583=ORIENTED_EDGE ( 'NONE', *, *, #30252, .T. ) ;
#11586=CARTESIAN_POINT ( 'NONE',  ( -11.35316468749999785, 218.0729166632526699, -3.042071309553167957 ) ) ;
#11588=CARTESIAN_POINT ( 'NONE',  ( -10.00000000000000178, 99.37499999317203958, -1.224646799147353454E-15 ) ) ;
#11589=CARTESIAN_POINT ( 'NONE',  ( -4.721056650415999201, 295.3281250017069510, -4.721056650415999201 ) ) ;
#11590=ORIENTED_EDGE ( 'NONE', *, *, #37503, .T. ) ;
#11592=CARTESIAN_POINT ( 'NONE',  ( 5.676582343750001591, 211.9270833299193555, -9.832129032723420536 ) ) ;
#11603=CARTESIAN_POINT ( 'NONE',  ( -5.000000000000005329, 23.33333333333333570, 8.660254037844387298 ) ) ;
#11612=CARTESIAN_POINT ( 'NONE',  ( 10.00000000000000000, 151.6666666598387110, 2.679491924311235618 ) ) ;
#11613=CARTESIAN_POINT ( 'NONE',  ( -2.765530957081998142, 294.6406250017069510, 6.676582343750000703 ) ) ;
#11622=ORIENTED_EDGE ( 'NONE', *, *, #5842, .F. ) ;
#11624=CARTESIAN_POINT ( 'NONE',  ( -8.311093377946836114, 82.96874999658601268, -8.311093377946837890 ) ) ;
#11634=CARTESIAN_POINT ( 'NONE',  ( 5.676582343750001591, 196.6145833299193839, -9.832129032723420536 ) ) ;
#11639=CARTESIAN_POINT ( 'NONE',  ( 11.35316468749999785, 180.8854166632526699, 3.042071309553174174 ) ) ;
#11642=DIRECTION ( 'NONE',  ( -0.000000000000000000, 1.000000000000000000, -0.000000000000000000 ) ) ;
#11647=CARTESIAN_POINT ( 'NONE',  ( 8.311093377946834337, 65.15624999658602690, 8.311093377946839666 ) ) ;
#11653=CARTESIAN_POINT ( 'NONE',  ( -8.311093377946836114, 57.65624999658601979, -8.311093377946837890 ) ) ;
#11658=CARTESIAN_POINT ( 'NONE',  ( -2.085542519210945728E-15, 59.53124999658601979, 11.35316468750000141 ) ) ;
#11660=CARTESIAN_POINT ( 'NONE',  ( -5.000000000000005329, 15.20833332650536640, 8.660254037844387298 ) ) ;
#11661=CARTESIAN_POINT ( 'NONE',  ( 2.679491924311228956, 157.9166666598386826, -10.00000000000000000 ) ) ;
#11664=CARTESIAN_POINT ( 'NONE',  ( -5.676582343749998039, 42.76041666325268409, -9.832129032723420536 ) ) ;
#11666=CARTESIAN_POINT ( 'NONE',  ( -11.35316468750000141, 178.2812499965860411, -1.390361679473963753E-15 ) ) ;
#11672=CARTESIAN_POINT ( 'NONE',  ( 11.35316468749999963, 185.9895833299193555, -3.042071309553165293 ) ) ;
#11677=CARTESIAN_POINT ( 'NONE',  ( 3.042071309553159519, 174.7395833299193555, 11.35316468750000141 ) ) ;
#11679=CARTESIAN_POINT ( 'NONE',  ( 3.042071309553159519, 165.0520833299193839, 11.35316468750000141 ) ) ;
#11681=CARTESIAN_POINT ( 'NONE',  ( -9.832129032723420536, 124.0104166632526841, 5.676582343749997150 ) ) ;
#11684=ADVANCED_FACE ( 'NONE', ( #19479 ), #49265, .T. ) ;
#11695=ADVANCED_FACE ( 'NONE', ( #43234 ), #20592, .T. ) ;
#11702=ORIENTED_EDGE ( 'NONE', *, *, #43051, .F. ) ;
#11711=CARTESIAN_POINT ( 'NONE',  ( -4.088227598258586603E-16, 297.3593750017070079, -6.676582343750001591 ) ) ;
#11712=CARTESIAN_POINT ( 'NONE',  ( -2.679491924311225848, 136.4583333333333428, -10.00000000000000178 ) ) ;
#11716=ADVANCED_FACE ( 'NONE', ( #14181 ), #8169, .T. ) ;
#11717=CARTESIAN_POINT ( 'NONE',  ( 1.522769729196201526E-11, 196.2499999999988063, -10.00000000000000178 ) ) ;
#11731=CARTESIAN_POINT ( 'NONE',  ( 3.042071309553167069, 11.82291666325268231, -11.35316468749999785 ) ) ;
#11733=CARTESIAN_POINT ( 'NONE',  ( -3.042071309553173730, 219.6354166632526699, 11.35316468749999785 ) ) ;
#11734=CARTESIAN_POINT ( 'NONE',  ( -2.679491924311087736, 220.4166666598387110, 10.00000000000008349 ) ) ;
#11738=ADVANCED_FACE ( 'NONE', ( #48519 ), #66620, .T. ) ;
#11739=EDGE_CURVE ( 'NONE', #62422, #7527, #21182, .T. ) ;
#11741=CARTESIAN_POINT ( 'NONE',  ( -11.35316468750000141, 18.48958332991934483, 3.042071309553159963 ) ) ;
#11747=CARTESIAN_POINT ( 'NONE',  ( -9.832129032723420536, 13.69791666325268409, 5.676582343749997150 ) ) ;
#11749=CARTESIAN_POINT ( 'NONE',  ( 5.676582343750001591, 136.6145833299193555, -9.832129032723420536 ) ) ;
#11750=CARTESIAN_POINT ( 'NONE',  ( -10.00000000000000178, 109.3749999931720396, -1.224646799147353454E-15 ) ) ;
#11756=ORIENTED_EDGE ( 'NONE', *, *, #42196, .T. ) ;
#11757=CARTESIAN_POINT ( 'NONE',  ( -5.676582343750006032, 4.427083329919350163, 9.832129032723418760 ) ) ;
#11759=CARTESIAN_POINT ( 'NONE',  ( -4.721056650415998313, 296.5781250017069510, 4.721056650416000089 ) ) ;
#11760=CARTESIAN_POINT ( 'NONE',  ( -11.35316468750000141, 138.2812499965860411, -1.390361679473963753E-15 ) ) ;
#11767=CARTESIAN_POINT ( 'NONE',  ( 2.679491924311370177, 215.8333333265053682, 9.999999999999918288 ) ) ;
#11769=CARTESIAN_POINT ( 'NONE',  ( 8.311093377946837890, 86.71874999658601268, -8.311093377946837890 ) ) ;
#11784=CARTESIAN_POINT ( 'NONE',  ( 4.999999999999999112, 110.8333333333333428, -8.660254037844383745 ) ) ;
#11802=CARTESIAN_POINT ( 'NONE',  ( 5.000000000000001776, 85.83333333333334281, -8.660254037844389075 ) ) ;
#11804=CARTESIAN_POINT ( 'NONE',  ( 11.35316468749999963, 66.30208332991935549, -3.042071309553165293 ) ) ;
#11805=CARTESIAN_POINT ( 'NONE',  ( 6.000000000000003553, 288.5625000000000000, -2.485281374238571761 ) ) ;
#11806=ORIENTED_EDGE ( 'NONE', *, *, #23306, .F. ) ;
#11816=CARTESIAN_POINT ( 'NONE',  ( 10.00000000000000178, 205.2083333333333428, -2.679491924311226736 ) ) ;
#11819=CARTESIAN_POINT ( 'NONE',  ( 8.311093377946837890, 176.7187499965860127, -8.311093377946837890 ) ) ;
#11823=CARTESIAN_POINT ( 'NONE',  ( 2.679491924311228956, 87.91666665983868256, -10.00000000000000000 ) ) ;
#11826=CARTESIAN_POINT ( 'NONE',  ( -5.676582343749998039, 32.76041666325269119, -9.832129032723420536 ) ) ;
#11831=CARTESIAN_POINT ( 'NONE',  ( -2.679491924311220519, 101.4583333333333286, -9.999999999999978684 ) ) ;
#11832=CARTESIAN_POINT ( 'NONE',  ( 6.123233995736767268E-16, 68.12499999317203958, -10.00000000000000178 ) ) ;
#11836=CARTESIAN_POINT ( 'NONE',  ( -7.320508075688778149, 59.99999999317203248, 7.320508075688769267 ) ) ;
#11844=CARTESIAN_POINT ( 'NONE',  ( 6.676582343750001591, 298.1093750017069510, -8.176455196517173205E-16 ) ) ;
#11845=CARTESIAN_POINT ( 'NONE',  ( -7.320508075688787919, 163.1250000000000568, 7.320508075688779925 ) ) ;
#11847=CARTESIAN_POINT ( 'NONE',  ( 3.042071309553167069, 156.8229166632526983, -11.35316468749999785 ) ) ;
#11848=CARTESIAN_POINT ( 'NONE',  ( 8.660254037844376640, 105.4166666666666714, -4.999999999999992895 ) ) ;
#11859=CARTESIAN_POINT ( 'NONE',  ( 5.676582343749993598, 130.2604166632526983, 9.832129032723422313 ) ) ;
#11863=CARTESIAN_POINT ( 'NONE',  ( -2.085542519210945728E-15, 39.84374999658601979, 11.35316468750000141 ) ) ;
#11865=CARTESIAN_POINT ( 'NONE',  ( 6.123233995736767268E-16, 38.12499999317203958, -10.00000000000000178 ) ) ;
#11870=CARTESIAN_POINT ( 'NONE',  ( 2.485281374238571317, 294.7500000034140157, -6.000000000000003553 ) ) ;
#11874=EDGE_CURVE ( 'NONE', #70240, #23624, #67754, .T. ) ;
#11894=CARTESIAN_POINT ( 'NONE',  ( -5.000000000000005329, 38.33333333333333570, 8.660254037844387298 ) ) ;
#11898=CARTESIAN_POINT ( 'NONE',  ( -7.320508075688773708, 33.74999999317202537, -7.320508075688774596 ) ) ;
#11899=CARTESIAN_POINT ( 'NONE',  ( 7.320508075688774596, 197.4999999931720254, -7.320508075688774596 ) ) ;
#11901=AXIS2_PLACEMENT_3D ( 'NONE', #33558, #58425, #53125 ) ;
#11908=CARTESIAN_POINT ( 'NONE',  ( 8.660254037844385522, 159.5833333333333428, 5.000000000000005329 ) ) ;
#11912=CARTESIAN_POINT ( 'NONE',  ( -9.832129032723418760, 133.1770833299193555, -5.676582343750004256 ) ) ;
#11913=CARTESIAN_POINT ( 'NONE',  ( -4.242640687119285658, 294.1875000034139589, 4.242640687119287435 ) ) ;
#11919=CARTESIAN_POINT ( 'NONE',  ( -3.042071309553164404, 2.552083329919349275, -11.35316468749999963 ) ) ;
#11923=CARTESIAN_POINT ( 'NONE',  ( -10.00000000000000000, 19.16666665983869322, -2.679491924311229845 ) ) ;
#11930=CARTESIAN_POINT ( 'NONE',  ( 8.311093377946834337, 115.1562499965859985, 8.311093377946839666 ) ) ;
#11932=( BOUNDED_CURVE ( )  B_SPLINE_CURVE ( 2, ( #8133, #58722, #31136, #7033, #54168, #48485, #49229, #62046, #38301, #60554, #44329, #26209, #31891 ),
 .UNSPECIFIED., .F., .F. ) 
 B_SPLINE_CURVE_WITH_KNOTS ( ( 3, 2, 2, 2, 2, 2, 3 ),
 ( 0.6250000000000001110, 0.6268115942028986698, 0.6286231884057972286, 0.6304347826086957873, 0.6322463768115942351, 0.6340579710144927938, 0.6358695652173913526 ),
 .UNSPECIFIED. ) 
 CURVE ( )  GEOMETRIC_REPRESENTATION_ITEM ( )  RATIONAL_B_SPLINE_CURVE ( ( 0.9999999999999978906, 0.9659258262890704216, 1.000000000000000000, 0.9659258262890683122, 1.000000000000000000, 0.9659258262890683122, 1.000000000000000000, 0.9659258262890683122, 1.000000000000000000, 0.9659258262890683122, 1.000000000000000000, 0.9659258262890683122, 1.000000000000000000 ) ) 
 REPRESENTATION_ITEM ( '' )  );
#11934=CARTESIAN_POINT ( 'NONE',  ( 0.000000000000000000, 300.0000000000000000, 0.000000000000000000 ) ) ;
#11937=CARTESIAN_POINT ( 'NONE',  ( 3.042071309553159519, 114.7395833299193555, 11.35316468750000141 ) ) ;
#11941=CARTESIAN_POINT ( 'NONE',  ( -10.00000000000000000, 224.1666666598386826, -2.679491924311229845 ) ) ;
#11944=CARTESIAN_POINT ( 'NONE',  ( -2.679491924311519835, 181.4583333333333428, -9.999999999999827693 ) ) ;
#11945=CARTESIAN_POINT ( 'NONE',  ( -5.676582343749998039, 97.44791666325269830, -9.832129032723420536 ) ) ;
#11948=CARTESIAN_POINT ( 'NONE',  ( -1.836970198721029983E-15, 63.75000000000000000, 10.00000000000000178 ) ) ;
#11951=CARTESIAN_POINT ( 'NONE',  ( 10.00000000000000178, 191.8749999931720254, 0.000000000000000000 ) ) ;
#11955=CARTESIAN_POINT ( 'NONE',  ( -11.35316468750000141, 93.80208332991935549, 3.042071309553159963 ) ) ;
#11959=CARTESIAN_POINT ( 'NONE',  ( -5.676582343749998039, 2.760416663252683644, -9.832129032723420536 ) ) ;
#11964=CARTESIAN_POINT ( 'NONE',  ( -9.832129032723420536, 223.6979166632526983, 5.676582343749997150 ) ) ;
#11965=CARTESIAN_POINT ( 'NONE',  ( 0.000000000000000000, 300.0000000000000000, 0.000000000000000000 ) ) ;
#11967=CARTESIAN_POINT ( 'NONE',  ( -2.765530957081996810, 296.2656250017069510, -6.676582343750003368 ) ) ;
#11968=EDGE_LOOP ( 'NONE', ( #63092, #4211, #33598, #49729 ) ) ;
#11969=CARTESIAN_POINT ( 'NONE',  ( -8.660254037844390851, 119.7916666598386968, 4.999999999999998224 ) ) ;
#11970=CARTESIAN_POINT ( 'NONE',  ( -11.35316468750000141, 213.5937499965860411, -1.390361679473963753E-15 ) ) ;
#11973=EDGE_CURVE ( 'NONE', #29697, #47641, #25848, .T. ) ;
#11979=CARTESIAN_POINT ( 'NONE',  ( -7.320508075688773708, 21.87500000000000355, -7.320508075688774596 ) ) ;
#11987=CARTESIAN_POINT ( 'NONE',  ( -6.676582343750002480, 297.3906250017069510, -2.765530957081996810 ) ) ;
#11995=AXIS2_PLACEMENT_3D ( 'NONE', #29808, #59588, #53560 ) ;
#11998=CARTESIAN_POINT ( 'NONE',  ( -8.311093377946836114, 92.96874999658602690, -8.311093377946837890 ) ) ;
#12008=CARTESIAN_POINT ( 'NONE',  ( 5.676582343749993598, 204.9479166632526983, 9.832129032723422313 ) ) ;
#12012=CARTESIAN_POINT ( 'NONE',  ( -5.676582343749998039, 177.7604166632526699, -9.832129032723420536 ) ) ;
#12015=CARTESIAN_POINT ( 'NONE',  ( -5.000000000000003553, 108.3333333333333570, 8.660254037844381969 ) ) ;
#12019=CARTESIAN_POINT ( 'NONE',  ( -5.676582343749998039, 67.44791666325268409, -9.832129032723420536 ) ) ;
#12025=CARTESIAN_POINT ( 'NONE',  ( -3.042071309553173730, 59.32291666325267698, 11.35316468749999785 ) ) ;
#12030=CARTESIAN_POINT ( 'NONE',  ( 3.042071309553159519, 54.73958332991934839, 11.35316468750000141 ) ) ;
#12033=CARTESIAN_POINT ( 'NONE',  ( -8.660254037844390851, 159.7916666598387110, 4.999999999999998224 ) ) ;
#12036=CARTESIAN_POINT ( 'NONE',  ( 3.042071309553159519, 50.05208332991935549, 11.35316468750000141 ) ) ;
#12038=CARTESIAN_POINT ( 'NONE',  ( 11.35316468749999785, 180.5729166632526983, 3.042071309553174174 ) ) ;
#12039=VERTEX_POINT ( 'NONE', #46957 ) ;
#12044=CARTESIAN_POINT ( 'NONE',  ( 9.832129032723420536, 176.1979166632526983, -5.676582343749999815 ) ) ;
#12046=EDGE_CURVE ( 'NONE', #53794, #18299, #13885, .T. ) ;
#12050=CARTESIAN_POINT ( 'NONE',  ( -3.042071309553163960, 162.5520833299193555, -11.35316468749999963 ) ) ;
#12053=CARTESIAN_POINT ( 'NONE',  ( 11.35316468749999785, 135.8854166632526983, 3.042071309553174174 ) ) ;
#12080=CARTESIAN_POINT ( 'NONE',  ( 4.721056650416000089, 296.9843750017070079, 4.721056650415999201 ) ) ;
#12081=CARTESIAN_POINT ( 'NONE',  ( -10.00000000000000178, 132.5000000000000000, -1.224646799147353454E-15 ) ) ;
#12083=CARTESIAN_POINT ( 'NONE',  ( 2.710081836398223309, 225.9999999999999716, 9.633870074142324214 ) ) ;
#12097=CARTESIAN_POINT ( 'NONE',  ( 8.311093377946834337, 30.15624999658601624, 8.311093377946839666 ) ) ;
#12099=CARTESIAN_POINT ( 'NONE',  ( 3.508297656242422846, 227.0932911785184842, -10.79750878567371153 ) ) ;
#12106=CARTESIAN_POINT ( 'NONE',  ( -3.042071309553173730, 24.32291666325268764, 11.35316468749999785 ) ) ;
#12109=CARTESIAN_POINT ( 'NONE',  ( 1.102182119232618108E-15, 295.3125000034140157, 6.000000000000001776 ) ) ;
#12110=DIRECTION ( 'NONE',  ( -0.000000000000000000, 1.000000000000000000, -0.000000000000000000 ) ) ;
#12112=CARTESIAN_POINT ( 'NONE',  ( -8.311093377946836114, 17.65624999658601624, -8.311093377946837890 ) ) ;
#12114=CARTESIAN_POINT ( 'NONE',  ( -9.832129032723418760, 142.8645833299193555, -5.676582343750004256 ) ) ;
#12115=CARTESIAN_POINT ( 'NONE',  ( 6.123233995736767268E-16, 118.1249999931720396, -10.00000000000000178 ) ) ;
#12117=CYLINDRICAL_SURFACE ( 'NONE', #40920, 10.00000000000000178 ) ;
#12120=CARTESIAN_POINT ( 'NONE',  ( -11.35316468750000141, 13.59374999658601801, -1.390361679473963753E-15 ) ) ;
#12123=CARTESIAN_POINT ( 'NONE',  ( 4.721056650416000089, 295.8281250017069510, 4.721056650415999201 ) ) ;
#12124=CARTESIAN_POINT ( 'NONE',  ( -3.042071309553173730, 139.3229166632526699, 11.35316468749999785 ) ) ;
#12136=CARTESIAN_POINT ( 'NONE',  ( 11.35316468750000141, 96.09374999658601268, 0.000000000000000000 ) ) ;
#12141=EDGE_LOOP ( 'NONE', ( #6776, #24937, #29484 ) ) ;
#12145=EDGE_CURVE ( 'NONE', #14276, #55396, #15890, .T. ) ;
#12149=( BOUNDED_CURVE ( )  B_SPLINE_CURVE ( 2, ( #1651, #14794, #43471, #61210, #26109, #60830, #32171, #48386, #37078, #15544, #49510, #54815, #2373 ),
 .UNSPECIFIED., .F., .F. ) 
 B_SPLINE_CURVE_WITH_KNOTS ( ( 3, 2, 2, 2, 2, 2, 3 ),
 ( 0.7989130434782609758, 0.8007246376811595345, 0.8025362318840579823, 0.8043478260869565410, 0.8061594202898550998, 0.8079710144927535476, 0.8097826086956521063 ),
 .UNSPECIFIED. ) 
 CURVE ( )  GEOMETRIC_REPRESENTATION_ITEM ( )  RATIONAL_B_SPLINE_CURVE ( ( 0.9999999999999978906, 0.9659258262890704216, 1.000000000000000000, 0.9659258262890683122, 1.000000000000000000, 0.9659258262890683122, 1.000000000000000000, 0.9659258262890683122, 1.000000000000000000, 0.9659258262890683122, 1.000000000000000000, 0.9659258262890704216, 0.9999999999999978906 ) ) 
 REPRESENTATION_ITEM ( '' )  );
#12152=( BOUNDED_CURVE ( )  B_SPLINE_CURVE ( 2, ( #26429, #44552, #3441, #15491, #39912, #15119, #72088, #9852, #50203, #32878, #38527, #3069, #27186 ),
 .UNSPECIFIED., .F., .F. ) 
 B_SPLINE_CURVE_WITH_KNOTS ( ( 3, 2, 2, 2, 2, 2, 3 ),
 ( 0.2989130434782608647, 0.3007246376811594235, 0.3025362318840579823, 0.3043478260869565410, 0.3061594202898551553, 0.3079710144927536586, 0.3097826086956522174 ),
 .UNSPECIFIED. ) 
 CURVE ( )  GEOMETRIC_REPRESENTATION_ITEM ( )  RATIONAL_B_SPLINE_CURVE ( ( 1.000000000000000000, 0.9659258262890683122, 1.000000000000000000, 0.9659258262890683122, 1.000000000000000000, 0.9659258262890683122, 1.000000000000000000, 0.9659258262890683122, 1.000000000000000000, 0.9659258262890683122, 1.000000000000000000, 0.9659258262890673130, 1.000000000000001110 ) ) 
 REPRESENTATION_ITEM ( '' )  );
#12154=VERTEX_POINT ( 'NONE', #43512 ) ;
#12170=CARTESIAN_POINT ( 'NONE',  ( 8.660254037844389075, 95.41666666666667140, -5.000000000000000000 ) ) ;
#12172=CARTESIAN_POINT ( 'NONE',  ( -3.042071309553173730, 64.63541666325269830, 11.35316468749999785 ) ) ;
#12173=CARTESIAN_POINT ( 'NONE',  ( 6.676582343750001591, 299.1093750017069510, -8.176455196517173205E-16 ) ) ;
#12181=CARTESIAN_POINT ( 'NONE',  ( -8.660254037844390851, 217.9166666666666856, 4.999999999999998224 ) ) ;
#12183=CARTESIAN_POINT ( 'NONE',  ( 6.951808397369818766E-16, 187.3437499965860127, -11.35316468750000141 ) ) ;
#12184=CARTESIAN_POINT ( 'NONE',  ( -5.000000000000003553, 38.33333333333333570, 8.660254037844385522 ) ) ;
#12190=CARTESIAN_POINT ( 'NONE',  ( 11.35316468750000141, 31.09374999658601979, 0.000000000000000000 ) ) ;
#12193=CARTESIAN_POINT ( 'NONE',  ( 6.123233995736767268E-16, 11.25000000000000178, -10.00000000000000178 ) ) ;
#12195=CARTESIAN_POINT ( 'NONE',  ( 0.000000000000000000, 300.0000000000000000, 0.000000000000000000 ) ) ;
#12197=CARTESIAN_POINT ( 'NONE',  ( 2.679491924311228956, 77.91666665983871098, -10.00000000000000000 ) ) ;
#12201=CARTESIAN_POINT ( 'NONE',  ( -1.836970198721029983E-15, 150.6249999931720538, 10.00000000000000178 ) ) ;
#12206=CARTESIAN_POINT ( 'NONE',  ( -6.676582343750001591, 296.6093750017069510, 0.000000000000000000 ) ) ;
#12208=CARTESIAN_POINT ( 'NONE',  ( 2.679491924311222739, 40.83333332650536818, 10.00000000000000355 ) ) ;
#12209=CARTESIAN_POINT ( 'NONE',  ( -11.35316468750000141, 158.4895833299193839, 3.042071309553159963 ) ) ;
#12211=CARTESIAN_POINT ( 'NONE',  ( 8.660254037844389075, 2.291666659838699438, -5.000000000000000000 ) ) ;
#12217=ORIENTED_EDGE ( 'NONE', *, *, #53092, .F. ) ;
#12222=CARTESIAN_POINT ( 'NONE',  ( 3.042071309553159519, 130.0520833299193555, 11.35316468750000141 ) ) ;
#12226=CARTESIAN_POINT ( 'NONE',  ( -3.042071309553164404, 52.55208332991934839, -11.35316468749999963 ) ) ;
#12234=CARTESIAN_POINT ( 'NONE',  ( -4.242640687119286547, 290.9375000034140157, -4.242640687119286547 ) ) ;
#12239=EDGE_CURVE ( 'NONE', #68967, #70895, #9684, .T. ) ;
#12241=EDGE_CURVE ( 'NONE', #69323, #15401, #59750, .T. ) ;
#12250=ADVANCED_FACE ( 'NONE', ( #40203 ), #69623, .T. ) ;
#12259=CARTESIAN_POINT ( 'NONE',  ( 10.00000000000000000, 49.79166666666667140, 2.679491924311236062 ) ) ;
#12265=VERTEX_POINT ( 'NONE', #35667 ) ;
#12266=( BOUNDED_CURVE ( )  B_SPLINE_CURVE ( 2, ( #53970, #48294, #31699, #54721, #3028, #72042, #43376, #14701, #37739, #52579, #9060, #32074, #69936 ),
 .UNSPECIFIED., .F., .F. ) 
 B_SPLINE_CURVE_WITH_KNOTS ( ( 3, 2, 2, 2, 2, 2, 3 ),
 ( 0.08152173913043478382, 0.08333333333333332871, 0.08514492753623188748, 0.08695652173913043237, 0.08876811594202899114, 0.09057971014492753603, 0.09239130434782608092 ),
 .UNSPECIFIED. ) 
 CURVE ( )  GEOMETRIC_REPRESENTATION_ITEM ( )  RATIONAL_B_SPLINE_CURVE ( ( 1.000000000000000000, 0.9659258262890683122, 1.000000000000000000, 0.9659258262890683122, 1.000000000000000000, 0.9659258262890683122, 1.000000000000000000, 0.9659258262890683122, 1.000000000000000000, 0.9659258262890683122, 1.000000000000000000, 0.9659258262890683122, 1.000000000000000000 ) ) 
 REPRESENTATION_ITEM ( '' )  );
#12271=CARTESIAN_POINT ( 'NONE',  ( -5.000000000000005329, 75.20833332650536818, 8.660254037844387298 ) ) ;
#12273=CARTESIAN_POINT ( 'NONE',  ( 10.00000000000000000, 201.6666666598387110, 2.679491924311235618 ) ) ;
#12274=CARTESIAN_POINT ( 'NONE',  ( 10.00000000000000178, 160.2083333333333144, -2.679491924311226736 ) ) ;
#12278=CARTESIAN_POINT ( 'NONE',  ( -9.832129032723420536, 139.0104166632526983, 5.676582343749997150 ) ) ;
#12280=CARTESIAN_POINT ( 'NONE',  ( 4.999999999999993783, 26.04166665983870388, 8.660254037844390851 ) ) ;
#12282=CARTESIAN_POINT ( 'NONE',  ( 6.123233995736767268E-16, 108.1249999931720396, -10.00000000000000178 ) ) ;
#12285=ORIENTED_EDGE ( 'NONE', *, *, #2306, .F. ) ;
#12291=CARTESIAN_POINT ( 'NONE',  ( -5.000000000000005329, 35.20833332650536818, 8.660254037844387298 ) ) ;
#12303=PLANE ( 'NONE',  #23001 ) ;
#12306=CARTESIAN_POINT ( 'NONE',  ( 9.832129032723420536, 121.1979166632526983, -5.676582343749999815 ) ) ;
#12310=CARTESIAN_POINT ( 'NONE',  ( 7.320508075688771044, 216.2499999931720538, 7.320508075688775484 ) ) ;
#12314=CARTESIAN_POINT ( 'NONE',  ( 11.35316468750000141, 100.7812499965860269, 0.000000000000000000 ) ) ;
#12317=CARTESIAN_POINT ( 'NONE',  ( 10.00000000000009059, 175.2083333333333997, -2.679491924311250273 ) ) ;
#12320=CARTESIAN_POINT ( 'NONE',  ( 2.679491924311222739, 190.8333333265053682, 10.00000000000000355 ) ) ;
#12323=CARTESIAN_POINT ( 'NONE',  ( 11.35316468749999785, 90.88541666325266988, 3.042071309553174174 ) ) ;
#12327=CARTESIAN_POINT ( 'NONE',  ( -3.042071309553164404, 7.552083329919349275, -11.35316468749999963 ) ) ;
#12330=CARTESIAN_POINT ( 'NONE',  ( 5.676582343750001591, 221.6145833299193839, -9.832129032723420536 ) ) ;
#12333=CARTESIAN_POINT ( 'NONE',  ( 8.660254037844389075, 200.4166666666666856, -5.000000000000000000 ) ) ;
#12334=CARTESIAN_POINT ( 'NONE',  ( 6.676582343750001591, 297.9531250017069510, -8.176455196517173205E-16 ) ) ;
#12337=CARTESIAN_POINT ( 'NONE',  ( 5.676582343749993598, 205.2604166632526983, 9.832129032723422313 ) ) ;
#12342=ORIENTED_EDGE ( 'NONE', *, *, #28115, .T. ) ;
#12345=CARTESIAN_POINT ( 'NONE',  ( 8.660254037844385522, 24.58333333333333570, 5.000000000000005329 ) ) ;
#12349=CARTESIAN_POINT ( 'NONE',  ( 0.000000000000000000, 300.0000000000000000, 10.00000000000000178 ) ) ;
#12354=CARTESIAN_POINT ( 'NONE',  ( 4.721056650415999201, 296.0781250017069510, -4.721056650415999201 ) ) ;
#12364=CARTESIAN_POINT ( 'NONE',  ( -5.676582343749998039, 97.76041666325269830, -9.832129032723420536 ) ) ;
#12372=EDGE_CURVE ( 'NONE', #3444, #25788, #47340, .T. ) ;
#12373=CARTESIAN_POINT ( 'NONE',  ( -5.676582343750006032, 209.1145833299193555, 9.832129032723418760 ) ) ;
#12377=CARTESIAN_POINT ( 'NONE',  ( -3.042071309553173730, 174.6354166632526983, 11.35316468749999785 ) ) ;
#12379=CARTESIAN_POINT ( 'NONE',  ( -3.673940397442060854E-16, 295.8125000034140157, -6.000000000000001776 ) ) ;
#12380=CARTESIAN_POINT ( 'NONE',  ( -7.320508075688768379, 111.8750000000000000, -7.320508075688769267 ) ) ;
#12384=CARTESIAN_POINT ( 'NONE',  ( 11.35316468749999785, 65.57291666325269830, 3.042071309553174174 ) ) ;
#12385=EDGE_CURVE ( 'NONE', #68967, #10283, #31320, .T. ) ;
#12392=CARTESIAN_POINT ( 'NONE',  ( -3.042071309553173730, 79.32291666325271251, 11.35316468749999785 ) ) ;
#12397=CARTESIAN_POINT ( 'NONE',  ( -5.676582343750006032, 54.11458332991934839, 9.832129032723418760 ) ) ;
#12400=CARTESIAN_POINT ( 'NONE',  ( -5.000000000000005329, 150.2083333265053682, 8.660254037844387298 ) ) ;
#12402=CARTESIAN_POINT ( 'NONE',  ( -1.836970198721029983E-15, 10.62499999317203425, 10.00000000000000178 ) ) ;
#12403=CARTESIAN_POINT ( 'NONE',  ( 5.676582343750001591, 41.92708332991934839, -9.832129032723420536 ) ) ;
#12405=CARTESIAN_POINT ( 'NONE',  ( 11.35316468749999785, 190.5729166632526699, 3.042071309553174174 ) ) ;
#12411=CARTESIAN_POINT ( 'NONE',  ( -3.042071309553163960, 182.2395833299193555, -11.35316468749999963 ) ) ;
#12416=CARTESIAN_POINT ( 'NONE',  ( 9.832129032723416984, 170.6770833299193555, 5.676582343750006032 ) ) ;
#12418=CARTESIAN_POINT ( 'NONE',  ( -11.35316468750000141, 128.8020833299193555, 3.042071309553159963 ) ) ;
#12423=FACE_OUTER_BOUND ( 'NONE', #8797, .T. ) ;
#12428=CARTESIAN_POINT ( 'NONE',  ( 6.326249034914468552E-13, 178.7500000000000853, 10.00000000000000533 ) ) ;
#12433=VERTEX_POINT ( 'NONE', #46969 ) ;
#12438=ORIENTED_EDGE ( 'NONE', *, *, #39801, .F. ) ;
#12444=CARTESIAN_POINT ( 'NONE',  ( -5.999999999999999112, 290.1250000034140157, 2.485281374238575314 ) ) ;
#12446=CARTESIAN_POINT ( 'NONE',  ( 4.721056650416000089, 298.9843750017070079, 4.721056650415999201 ) ) ;
#12447=CARTESIAN_POINT ( 'NONE',  ( 10.00000000000000178, 135.2083333333333144, -2.679491924311226736 ) ) ;
#12449=AXIS2_PLACEMENT_3D ( 'NONE', #37449, #43090, #66107 ) ;
#12454=CARTESIAN_POINT ( 'NONE',  ( 6.000000000000001776, 290.5625000034140157, -7.347880794884121708E-16 ) ) ;
#12465=CARTESIAN_POINT ( 'NONE',  ( -3.042071309553164404, 27.23958332991934839, -11.35316468749999963 ) ) ;
#12466=CARTESIAN_POINT ( 'NONE',  ( 6.123233995736767268E-16, 26.25000000000000355, -10.00000000000000178 ) ) ;
#12467=CARTESIAN_POINT ( 'NONE',  ( 11.35316468750000141, 216.0937499965860411, 0.000000000000000000 ) ) ;
#12473=CARTESIAN_POINT ( 'NONE',  ( -8.311093377946836114, 37.65624999658601268, -8.311093377946837890 ) ) ;
#12479=CARTESIAN_POINT ( 'NONE',  ( -9.832129032723418760, 22.86458332991934839, -5.676582343750004256 ) ) ;
#12482=CARTESIAN_POINT ( 'NONE',  ( -5.676582343749998039, 147.4479166632526983, -9.832129032723420536 ) ) ;
#12483=CARTESIAN_POINT ( 'NONE',  ( 10.00000000000000178, 121.8749999931720396, 0.000000000000000000 ) ) ;
#12489=CARTESIAN_POINT ( 'NONE',  ( -11.35316468750000141, 3.593749996586016682, -1.390361679473963753E-15 ) ) ;
#12492=CARTESIAN_POINT ( 'NONE',  ( 6.676582343750001591, 297.9531250017069510, -8.176455196517173205E-16 ) ) ;
#12494=CARTESIAN_POINT ( 'NONE',  ( 11.35316468749999785, 140.5729166632526983, 3.042071309553174174 ) ) ;
#12501=CARTESIAN_POINT ( 'NONE',  ( 2.679491924311371065, 118.9583333333333570, 9.999999999999920064 ) ) ;
#12503=CARTESIAN_POINT ( 'NONE',  ( 9.832129032723416984, 85.67708332991935549, 5.676582343750006032 ) ) ;
#12530=VERTEX_POINT ( 'NONE', #42782 ) ;
#12536=CARTESIAN_POINT ( 'NONE',  ( -7.320508075688778149, 93.12500000000000000, 7.320508075688769267 ) ) ;
#12540=CARTESIAN_POINT ( 'NONE',  ( -3.042071309553164404, 57.55208332991936260, -11.35316468749999963 ) ) ;
#12541=CARTESIAN_POINT ( 'NONE',  ( 6.676582343750001591, 298.1093750017069510, -8.176455196517173205E-16 ) ) ;
#12544=CARTESIAN_POINT ( 'NONE',  ( 6.123233995736767268E-16, 173.1249999931720538, -10.00000000000000178 ) ) ;
#12550=DIRECTION ( 'NONE',  ( 0.000000000000000000, 0.000000000000000000, 1.000000000000000000 ) ) ;
#12552=CARTESIAN_POINT ( 'NONE',  ( 2.679491924311228956, 221.0416666666667140, -10.00000000000000000 ) ) ;
#12554=CARTESIAN_POINT ( 'NONE',  ( 11.35316468750000141, 186.0937499965860411, 0.000000000000000000 ) ) ;
#12556=CARTESIAN_POINT ( 'NONE',  ( 2.679491924311228956, 177.9166666598387110, -10.00000000000000000 ) ) ;
#12562=CARTESIAN_POINT ( 'NONE',  ( -11.35316468749999785, 43.38541666325269119, -3.042071309553167513 ) ) ;
#12567=CARTESIAN_POINT ( 'NONE',  ( -2.679491924318369911, 103.5416666666660319, 9.999999999995861089 ) ) ;
#12569=CARTESIAN_POINT ( 'NONE',  ( -7.320508075688778149, 79.99999999317203958, 7.320508075688769267 ) ) ;
#12577=CARTESIAN_POINT ( 'NONE',  ( 6.676582343750003368, 298.1718750017070079, -2.765530957081997254 ) ) ;
#12580=CARTESIAN_POINT ( 'NONE',  ( -8.311093377946836114, 157.6562499965860411, -8.311093377946837890 ) ) ;
#12590=CARTESIAN_POINT ( 'NONE',  ( -11.35316468750000141, 143.8020833299193555, 3.042071309553159963 ) ) ;
#12594=CARTESIAN_POINT ( 'NONE',  ( -8.311093377946841443, 44.21874999658602690, 8.311093377946830785 ) ) ;
#12597=CARTESIAN_POINT ( 'NONE',  ( -7.320508075688779037, 26.87500000000001066, -7.320508075688779037 ) ) ;
#12602=CARTESIAN_POINT ( 'NONE',  ( 2.485281374238575314, 292.3750000034139589, 6.000000000000000888 ) ) ;
#12611=EDGE_CURVE ( 'NONE', #44635, #10894, #55249, .T. ) ;
#12622=CARTESIAN_POINT ( 'NONE',  ( -1.836970198721029983E-15, 48.75000000000000000, 10.00000000000000178 ) ) ;
#12624=CARTESIAN_POINT ( 'NONE',  ( 1.102182119232618108E-15, 299.2500000000000000, 6.000000000000001776 ) ) ;
#12628=ORIENTED_EDGE ( 'NONE', *, *, #22011, .T. ) ;
#12629=ORIENTED_EDGE ( 'NONE', *, *, #56034, .T. ) ;
#12634=CARTESIAN_POINT ( 'NONE',  ( 7.347880794884121708E-16, 300.0000000000000000, -6.000000000000001776 ) ) ;
#12637=CARTESIAN_POINT ( 'NONE',  ( -8.660254037844387298, 177.0833333333333428, -5.000000000000004441 ) ) ;
#12640=CARTESIAN_POINT ( 'NONE',  ( 11.35316468749999785, 135.8854166632526983, 3.042071309553174174 ) ) ;
#12649=CARTESIAN_POINT ( 'NONE',  ( 7.320508075688852756, 195.6250000000001421, -7.320508075688852756 ) ) ;
#12652=CARTESIAN_POINT ( 'NONE',  ( 10.00000000000000000, 31.66666665983870033, 2.679491924311236062 ) ) ;
#12659=ORIENTED_EDGE ( 'NONE', *, *, #70739, .T. ) ;
#12661=CARTESIAN_POINT ( 'NONE',  ( -6.101342341038383132, 225.9999999999999716, -7.950158476763387938 ) ) ;
#12664=CARTESIAN_POINT ( 'NONE',  ( -5.676582343750006032, 119.1145833299193697, 9.832129032723418760 ) ) ;
#12671=CARTESIAN_POINT ( 'NONE',  ( 9.832129032723416984, 115.3645833299193555, 5.676582343750006032 ) ) ;
#12676=CARTESIAN_POINT ( 'NONE',  ( -10.00000000000000000, 199.1666666598386826, -2.679491924311229845 ) ) ;
#12679=CARTESIAN_POINT ( 'NONE',  ( -5.676582343750006032, 89.42708332991934128, 9.832129032723418760 ) ) ;
#12683=CARTESIAN_POINT ( 'NONE',  ( 8.311093377946834337, 5.468749996586017126, 8.311093377946839666 ) ) ;
#12685=CARTESIAN_POINT ( 'NONE',  ( -2.679491924330377639, 138.5416666666649803, 9.999999999988961719 ) ) ;
#12687=CARTESIAN_POINT ( 'NONE',  ( 11.35316468749999785, 215.5729166632526699, 3.042071309553174174 ) ) ;
#12689=CARTESIAN_POINT ( 'NONE',  ( 2.679491924311192097, 47.91666665983871098, -10.00000000000002309 ) ) ;
#12691=CARTESIAN_POINT ( 'NONE',  ( -6.676582343750000703, 294.5156250017069510, 2.765530957082001251 ) ) ;
#12695=CARTESIAN_POINT ( 'NONE',  ( 8.311093377946837890, 206.7187499965859843, -8.311093377946837890 ) ) ;
#12696=( BOUNDED_CURVE ( )  B_SPLINE_CURVE ( 2, ( #61248, #32977, #9945, #14086, #37121, #2791, #66155, #72942, #60123, #49172, #9580, #32597, #60870 ),
 .UNSPECIFIED., .F., .F. ) 
 B_SPLINE_CURVE_WITH_KNOTS ( ( 3, 2, 2, 2, 2, 2, 3 ),
 ( 0.01569808486621994056, 0.02093092178115263380, 0.02616375869608532703, 0.03139659561101801333, 0.03662943252595071697, 0.04186226944088339980, 0.04709510635581609650 ),
 .UNSPECIFIED. ) 
 CURVE ( )  GEOMETRIC_REPRESENTATION_ITEM ( )  RATIONAL_B_SPLINE_CURVE ( ( 0.9999999999999127365, 0.9659258262891555757, 1.000000000000000000, 0.9659258262890683122, 1.000000000000000000, 0.9659258262890683122, 1.000000000000000000, 0.9659258262890683122, 1.000000000000000000, 0.9659258262890683122, 1.000000000000000000, 0.9659258262890683122, 1.000000000000000000 ) ) 
 REPRESENTATION_ITEM ( '' )  );
#12705=CARTESIAN_POINT ( 'NONE',  ( -1.836970198721029983E-15, 23.75000000000000000, 10.00000000000000178 ) ) ;
#12710=EDGE_CURVE ( 'NONE', #48053, #16277, #65022, .T. ) ;
#12714=CARTESIAN_POINT ( 'NONE',  ( -2.765530957081996810, 298.2656250017069510, -6.676582343750002480 ) ) ;
#12722=ORIENTED_EDGE ( 'NONE', *, *, #55857, .T. ) ;
#12725=CARTESIAN_POINT ( 'NONE',  ( 9.832129032723420536, 106.5104166632526841, -5.676582343749999815 ) ) ;
#12731=CARTESIAN_POINT ( 'NONE',  ( -1.836970198721029983E-15, 195.6249999931720254, 10.00000000000000178 ) ) ;
#12734=CARTESIAN_POINT ( 'NONE',  ( 1.224646799147353454E-15, 300.0000000000000000, -10.00000000000000178 ) ) ;
#12735=AXIS2_PLACEMENT_3D ( 'NONE', #69955, #51479, #18265 ) ;
#12736=CARTESIAN_POINT ( 'NONE',  ( 8.311093377946837890, 211.4062499965860411, -8.311093377946837890 ) ) ;
#12742=CARTESIAN_POINT ( 'NONE',  ( 6.951808397369818766E-16, 182.3437499965860411, -11.35316468750000141 ) ) ;
#12749=CARTESIAN_POINT ( 'NONE',  ( 8.311093377946834337, 70.15624999658602690, 8.311093377946839666 ) ) ;
#12753=CARTESIAN_POINT ( 'NONE',  ( -10.00000000000002665, 47.29166666666668561, -2.679491924311236950 ) ) ;
#12755=CARTESIAN_POINT ( 'NONE',  ( 11.35316468749999785, 70.57291666325269830, 3.042071309553174174 ) ) ;
#12760=CARTESIAN_POINT ( 'NONE',  ( -11.35316468750000141, 58.28124999658601268, -1.390361679473963753E-15 ) ) ;
#12763=CARTESIAN_POINT ( 'NONE',  ( -7.320508075688778149, 154.9999999931720538, 7.320508075688769267 ) ) ;
#12766=CARTESIAN_POINT ( 'NONE',  ( -3.042071309553173730, 54.63541666325268409, 11.35316468749999785 ) ) ;
#12768=CARTESIAN_POINT ( 'NONE',  ( 8.311093377946837890, 191.4062499965860127, -8.311093377946837890 ) ) ;
#12774=CARTESIAN_POINT ( 'NONE',  ( -9.832129032723420536, 178.6979166632526983, 5.676582343749997150 ) ) ;
#12778=ORIENTED_EDGE ( 'NONE', *, *, #71796, .T. ) ;
#12779=CARTESIAN_POINT ( 'NONE',  ( -8.311093377946836114, 172.9687499965860127, -8.311093377946837890 ) ) ;
#12786=( BOUNDED_CURVE ( )  B_SPLINE_CURVE ( 2, ( #38555, #67958, #55537, #4966, #27967, #68326, #38920, #66841, #38176, #61179, #21553, #9509, #44205 ),
 .UNSPECIFIED., .F., .F. ) 
 B_SPLINE_CURVE_WITH_KNOTS ( ( 3, 2, 2, 2, 2, 2, 3 ),
 ( 0.3967391304347826497, 0.3985507246376812085, 0.4003623188405797673, 0.4021739130434782705, 0.4039855072463768293, 0.4057971014492753881, 0.4076086956521738913 ),
 .UNSPECIFIED. ) 
 CURVE ( )  GEOMETRIC_REPRESENTATION_ITEM ( )  RATIONAL_B_SPLINE_CURVE ( ( 0.9999999999999990008, 0.9659258262890693114, 1.000000000000000000, 0.9659258262890683122, 1.000000000000000000, 0.9659258262890683122, 1.000000000000000000, 0.9659258262890683122, 1.000000000000000000, 0.9659258262890683122, 1.000000000000000000, 0.9659258262890683122, 1.000000000000000000 ) ) 
 REPRESENTATION_ITEM ( '' )  );
#12798=DIRECTION ( 'NONE',  ( -0.000000000000000000, 1.000000000000000000, -0.000000000000000000 ) ) ;
#12802=DIRECTION ( 'NONE',  ( 0.000000000000000000, 0.000000000000000000, 1.000000000000000000 ) ) ;
#12812=CARTESIAN_POINT ( 'NONE',  ( 7.320508075688771044, 129.3750000000000000, 7.320508075688775484 ) ) ;
#12825=CARTESIAN_POINT ( 'NONE',  ( 2.679491924311228956, 52.91666665983869677, -10.00000000000000000 ) ) ;
#12827=CARTESIAN_POINT ( 'NONE',  ( 3.042071309553167069, 26.82291666325268054, -11.35316468749999785 ) ) ;
#12829=CARTESIAN_POINT ( 'NONE',  ( 5.676582343749993598, 220.2604166632526983, 9.832129032723422313 ) ) ;
#12834=CARTESIAN_POINT ( 'NONE',  ( -9.832129032723420536, 38.69791666325268409, 5.676582343749997150 ) ) ;
#12840=CARTESIAN_POINT ( 'NONE',  ( 8.311093377946834337, 25.15624999658601268, 8.311093377946839666 ) ) ;
#12842=CARTESIAN_POINT ( 'NONE',  ( 9.832129032723420536, 146.1979166632526983, -5.676582343749999815 ) ) ;
#12843=CARTESIAN_POINT ( 'NONE',  ( 10.00000000000000178, 117.0833333265053682, -2.679491924311226736 ) ) ;
#12845=CARTESIAN_POINT ( 'NONE',  ( 8.660254037844385522, 171.4583333265053682, 5.000000000000005329 ) ) ;
#12848=CARTESIAN_POINT ( 'NONE',  ( 8.311093377946837890, 6.718749996586015349, -8.311093377946837890 ) ) ;
#12849=ORIENTED_EDGE ( 'NONE', *, *, #49032, .T. ) ;
#12851=CARTESIAN_POINT ( 'NONE',  ( -2.765530957081996810, 299.2656250017070647, -6.676582343750003368 ) ) ;
#12853=CARTESIAN_POINT ( 'NONE',  ( -11.35316468749999785, 138.0729166632526699, -3.042071309553167957 ) ) ;
#12863=ADVANCED_FACE ( 'NONE', ( #9595 ), #32614, .T. ) ;
#12864=CARTESIAN_POINT ( 'NONE',  ( -8.660254037844390851, 204.7916666598387110, 4.999999999999998224 ) ) ;
#12866=CARTESIAN_POINT ( 'NONE',  ( 3.042071309553167069, 92.13541666325266988, -11.35316468749999785 ) ) ;
#12897=CARTESIAN_POINT ( 'NONE',  ( -4.999999999999996447, 31.66666666666666785, -8.660254037844385522 ) ) ;
#12898=CARTESIAN_POINT ( 'NONE',  ( 6.123233995736767268E-16, 101.2500000000000000, -10.00000000000000178 ) ) ;
#12900=CARTESIAN_POINT ( 'NONE',  ( -4.721056650415998313, 296.7343750017069510, 4.721056650416000089 ) ) ;
#12903=VECTOR ( 'NONE', #44413, 1000.000000000000000 ) ;
#12904=DIRECTION ( 'NONE',  ( 0.000000000000000000, 0.000000000000000000, 1.000000000000000000 ) ) ;
#12907=CARTESIAN_POINT ( 'NONE',  ( -7.320508075688773708, 103.7499999931720396, -7.320508075688774596 ) ) ;
#12908=CARTESIAN_POINT ( 'NONE',  ( 0.000000000000000000, 284.0000000000000000, 0.000000000000000000 ) ) ;
#12912=CARTESIAN_POINT ( 'NONE',  ( 7.320508075688771044, 209.3750000000000000, 7.320508075688775484 ) ) ;
#12914=CARTESIAN_POINT ( 'NONE',  ( 9.832129032723416984, 185.6770833299193555, 5.676582343750006032 ) ) ;
#12919=ORIENTED_EDGE ( 'NONE', *, *, #53389, .T. ) ;
#12921=CARTESIAN_POINT ( 'NONE',  ( 9.832129032723420536, 46.51041666325269119, -5.676582343749999815 ) ) ;
#12923=CARTESIAN_POINT ( 'NONE',  ( 11.35316468749999963, 216.3020833299193555, -3.042071309553165293 ) ) ;
#12925=CARTESIAN_POINT ( 'NONE',  ( 8.660254037844385522, 9.583333333333333925, 5.000000000000006217 ) ) ;
#12930=CARTESIAN_POINT ( 'NONE',  ( 7.320508075688771044, 71.24999999317203958, 7.320508075688775484 ) ) ;
#12936=EDGE_LOOP ( 'NONE', ( #2468, #14324, #35188, #42191 ) ) ;
#12938=CARTESIAN_POINT ( 'NONE',  ( 6.676582343750003368, 297.1718750017071216, -2.765530957081997254 ) ) ;
#12939=CARTESIAN_POINT ( 'NONE',  ( -8.660254037844401509, 142.9166666666666572, 5.000000000000004441 ) ) ;
#12940=VECTOR ( 'NONE', #4304, 1000.000000000000000 ) ;
#12941=CARTESIAN_POINT ( 'NONE',  ( -3.042071309553164404, 157.2395833299193555, -11.35316468749999963 ) ) ;
#12943=CARTESIAN_POINT ( 'NONE',  ( 4.999999999999994671, 4.166666666666666963, 8.660254037844390851 ) ) ;
#12949=CARTESIAN_POINT ( 'NONE',  ( -9.832129032723420536, 139.0104166632526983, 5.676582343749997150 ) ) ;
#12951=CARTESIAN_POINT ( 'NONE',  ( -3.673940397442060854E-16, 290.7500000000000000, -6.000000000000001776 ) ) ;
#12953=CARTESIAN_POINT ( 'NONE',  ( 11.35316468750000141, 46.09374999658602690, 0.000000000000000000 ) ) ;
#12958=ADVANCED_FACE ( 'NONE', ( #519 ), #58963, .T. ) ;
#12959=EDGE_CURVE ( 'NONE', #57671, #70231, #57799, .T. ) ;
#12961=CARTESIAN_POINT ( 'NONE',  ( -2.485281374238571761, 290.8750000034140157, -6.000000000000003553 ) ) ;
#12965=AXIS2_PLACEMENT_3D ( 'NONE', #52195, #59337, #63874 ) ;
#12985=CARTESIAN_POINT ( 'NONE',  ( 4.999999999999993783, 54.16666666666667140, 8.660254037844390851 ) ) ;
#12987=CARTESIAN_POINT ( 'NONE',  ( -2.485281374238571761, 297.8124999999999432, -6.000000000000003553 ) ) ;
#12989=DIRECTION ( 'NONE',  ( 0.000000000000000000, 0.000000000000000000, 1.000000000000000000 ) ) ;
#12991=ORIENTED_EDGE ( 'NONE', *, *, #4894, .T. ) ;
#12995=CARTESIAN_POINT ( 'NONE',  ( -2.679491924311300011, 73.33333332650538239, -9.999999999999959144 ) ) ;
#12998=CARTESIAN_POINT ( 'NONE',  ( -8.660254037844390851, 139.7916666598387110, 4.999999999999998224 ) ) ;
#12999=CARTESIAN_POINT ( 'NONE',  ( 4.999999999999993783, 174.1666666666666572, 8.660254037844390851 ) ) ;
#13003=CARTESIAN_POINT ( 'NONE',  ( -8.311093377946836114, 137.9687499965860411, -8.311093377946837890 ) ) ;
#13015=CARTESIAN_POINT ( 'NONE',  ( 4.999999999999993783, 36.04166665983870388, 8.660254037844390851 ) ) ;
#13025=CARTESIAN_POINT ( 'NONE',  ( -2.250000000000000000, 300.0000000000000000, 7.677076266392047543 ) ) ;
#13027=CARTESIAN_POINT ( 'NONE',  ( 3.042071309553167069, 116.8229166632526983, -11.35316468749999785 ) ) ;
#13036=CARTESIAN_POINT ( 'NONE',  ( -9.832129032723420536, 108.6979166632526983, 5.676582343749997150 ) ) ;
#13038=CARTESIAN_POINT ( 'NONE',  ( -1.300830538084598961E-11, 173.7499999999989768, 10.00000000000000178 ) ) ;
#13040=CARTESIAN_POINT ( 'NONE',  ( -5.000000000000005329, 205.2083333265053682, 8.660254037844387298 ) ) ;
#13042=CARTESIAN_POINT ( 'NONE',  ( -11.35316468750000141, 98.80208332991934128, 3.042071309553159963 ) ) ;
#13046=CARTESIAN_POINT ( 'NONE',  ( 9.832129032723416984, 10.67708332991935016, 5.676582343750006032 ) ) ;
#13055=CARTESIAN_POINT ( 'NONE',  ( -6.676582343750000703, 293.5156250017070647, 2.765530957082001251 ) ) ;
#13057=CARTESIAN_POINT ( 'NONE',  ( -8.311093377946841443, 224.2187499965860411, 8.311093377946834337 ) ) ;
#13060=AXIS2_PLACEMENT_3D ( 'NONE', #39215, #33573, #61477 ) ;
#13064=EDGE_LOOP ( 'NONE', ( #409, #49248, #53180, #55977 ) ) ;
#13071=CARTESIAN_POINT ( 'NONE',  ( -5.000000000000054179, 173.3333333333333712, 8.660254037844469011 ) ) ;
#13073=ORIENTED_EDGE ( 'NONE', *, *, #32847, .F. ) ;
#13077=CARTESIAN_POINT ( 'NONE',  ( 2.295000000000000373, 278.5679999999998699, 5.413230550749199566 ) ) ;
#13078=CARTESIAN_POINT ( 'NONE',  ( 2.765530957082001251, 290.7656250017070079, 6.676582343749999815 ) ) ;
#13089=CARTESIAN_POINT ( 'NONE',  ( -11.35316468750000141, 103.8020833299193413, 3.042071309553159963 ) ) ;
#13097=CARTESIAN_POINT ( 'NONE',  ( -2.679491924311235174, 180.4166666598387110, 10.00000000000000000 ) ) ;
#13098=CARTESIAN_POINT ( 'NONE',  ( 11.35316468749999963, 215.9895833299192986, -3.042071309553165293 ) ) ;
#13103=CARTESIAN_POINT ( 'NONE',  ( -2.085542519210945728E-15, 179.8437499965860411, 11.35316468750000141 ) ) ;
#13110=CARTESIAN_POINT ( 'NONE',  ( -5.676582343750006032, 64.11458332991935549, 9.832129032723418760 ) ) ;
#13114=CARTESIAN_POINT ( 'NONE',  ( -5.000000000000018652, 48.33333333333334991, 8.660254037844408614 ) ) ;
#13116=CARTESIAN_POINT ( 'NONE',  ( 3.042071309553167069, 71.82291666325269830, -11.35316468749999785 ) ) ;
#13122=CARTESIAN_POINT ( 'NONE',  ( 8.311093377946834337, 70.15624999658602690, 8.311093377946839666 ) ) ;
#13124=CARTESIAN_POINT ( 'NONE',  ( 4.999999999999993783, 129.1666666666666856, 8.660254037844390851 ) ) ;
#13126=CARTESIAN_POINT ( 'NONE',  ( -8.660254037844387298, 153.9583333265053682, -5.000000000000004441 ) ) ;
#13129=CARTESIAN_POINT ( 'NONE',  ( 3.042071309553167513, 57.13541666325268409, -11.35316468749999785 ) ) ;
#13132=CARTESIAN_POINT ( 'NONE',  ( -2.085542519210945728E-15, 199.5312499965860411, 11.35316468750000141 ) ) ;
#13135=CARTESIAN_POINT ( 'NONE',  ( 8.660254037844385522, 61.45833332650536818, 5.000000000000005329 ) ) ;
#13137=CARTESIAN_POINT ( 'NONE',  ( 5.676582343750001591, 186.6145833299193839, -9.832129032723420536 ) ) ;
#13140=CARTESIAN_POINT ( 'NONE',  ( -1.836970198721029983E-15, 190.6249999931720254, 10.00000000000000178 ) ) ;
#13142=CARTESIAN_POINT ( 'NONE',  ( -9.832129032723420536, 164.0104166632526983, 5.676582343749997150 ) ) ;
#13146=CARTESIAN_POINT ( 'NONE',  ( 5.994779237468493172, 226.0000000000000000, -8.522275728953271567 ) ) ;
#13157=AXIS2_PLACEMENT_3D ( 'NONE', #66387, #24260, #3397 ) ;
#13159=CARTESIAN_POINT ( 'NONE',  ( -7.320508075688813676, 176.8750000000000568, -7.320508075688814564 ) ) ;
#13161=CARTESIAN_POINT ( 'NONE',  ( 8.660254037844431707, 179.5833333333333712, 5.000000000000031974 ) ) ;
#13167=ORIENTED_EDGE ( 'NONE', *, *, #2314, .T. ) ;
#13169=VERTEX_POINT ( 'NONE', #54410 ) ;
#13175=CARTESIAN_POINT ( 'NONE',  ( 4.721056650416000089, 294.9843750017070079, 4.721056650415999201 ) ) ;
#13176=CARTESIAN_POINT ( 'NONE',  ( 8.660254037844389075, 135.4166666666666856, -5.000000000000000000 ) ) ;
#13191=CARTESIAN_POINT ( 'NONE',  ( 11.35316468749999785, 30.57291666325268409, 3.042071309553174174 ) ) ;
#13193=CARTESIAN_POINT ( 'NONE',  ( 8.311093377946834337, 225.4687499965860411, 8.311093377946839666 ) ) ;
#13200=CARTESIAN_POINT ( 'NONE',  ( 9.832129032723416984, 35.36458332991934839, 5.676582343750006032 ) ) ;
#13206=CARTESIAN_POINT ( 'NONE',  ( 3.042071309553159519, 34.73958332991934839, 11.35316468750000141 ) ) ;
#13209=CARTESIAN_POINT ( 'NONE',  ( -3.042071309553173730, 144.3229166632527267, 11.35316468749999785 ) ) ;
#13211=CARTESIAN_POINT ( 'NONE',  ( -7.320508075688773708, 118.7499999931720396, -7.320508075688774596 ) ) ;
#13216=CARTESIAN_POINT ( 'NONE',  ( -3.042071309553163960, 22.55208332991935194, -11.35316468749999963 ) ) ;
#13222=CARTESIAN_POINT ( 'NONE',  ( 3.042071309553159519, 144.7395833299193839, 11.35316468750000141 ) ) ;
#13223=DIRECTION ( 'NONE',  ( -0.000000000000000000, 1.000000000000000000, -0.000000000000000000 ) ) ;
#13230=CARTESIAN_POINT ( 'NONE',  ( 8.660254037844389075, 119.5833333333333428, 5.000000000000007105 ) ) ;
#13233=CARTESIAN_POINT ( 'NONE',  ( 11.35316468749999963, 91.30208332991934128, -3.042071309553165293 ) ) ;
#13238=ORIENTED_EDGE ( 'NONE', *, *, #30497, .F. ) ;
#13254=CARTESIAN_POINT ( 'NONE',  ( -4.999999999999998224, 223.5416666598387110, -8.660254037844389075 ) ) ;
#13265=CARTESIAN_POINT ( 'NONE',  ( 7.320508075688774596, 90.62499999999998579, -7.320508075688774596 ) ) ;
#13267=CARTESIAN_POINT ( 'NONE',  ( -2.765530957081996810, 297.4218750017069510, -6.676582343750003368 ) ) ;
#13271=CARTESIAN_POINT ( 'NONE',  ( -10.00000000000000355, 52.50000000000000711, -1.224646799147353651E-15 ) ) ;
#13276=CARTESIAN_POINT ( 'NONE',  ( -8.660254037844387298, 217.0833333333333428, -5.000000000000004441 ) ) ;
#13278=CARTESIAN_POINT ( 'NONE',  ( -9.832129032723418760, 183.1770833299193555, -5.676582343750004256 ) ) ;
#13281=LINE ( 'NONE', #19691, #6778 ) ;
#13282=DIRECTION ( 'NONE',  ( 0.000000000000000000, 0.000000000000000000, 1.000000000000000000 ) ) ;
#13284=ORIENTED_EDGE ( 'NONE', *, *, #29937, .T. ) ;
#13286=CARTESIAN_POINT ( 'NONE',  ( -2.085542519210945728E-15, 49.84374999658601268, 11.35316468750000141 ) ) ;
#13288=CARTESIAN_POINT ( 'NONE',  ( -5.676582343749998039, 222.7604166632526983, -9.832129032723420536 ) ) ;
#13290=CARTESIAN_POINT ( 'NONE',  ( 7.320508075688771932, 9.375000000000001776, 7.320508075688776373 ) ) ;
#13296=CARTESIAN_POINT ( 'NONE',  ( -11.35316468749999785, 113.0729166632526841, -3.042071309553167513 ) ) ;
#13297=CARTESIAN_POINT ( 'NONE',  ( 5.000000000000001776, 77.70833332650536818, -8.660254037844389075 ) ) ;
#13305=CARTESIAN_POINT ( 'NONE',  ( -2.765530957081998586, 291.7968750017070079, 6.676582343750001591 ) ) ;
#13307=CARTESIAN_POINT ( 'NONE',  ( 11.35316468749999963, 150.9895833299193271, -3.042071309553165293 ) ) ;
#13308=CARTESIAN_POINT ( 'NONE',  ( 7.320508075688774596, 2.499999993172032031, -7.320508075688774596 ) ) ;
#13312=ORIENTED_EDGE ( 'NONE', *, *, #24290, .F. ) ;
#13315=CARTESIAN_POINT ( 'NONE',  ( -5.676582343749998039, 147.7604166632526699, -9.832129032723420536 ) ) ;
#13319=CARTESIAN_POINT ( 'NONE',  ( 8.311093377946834337, 55.46874999658601268, 8.311093377946839666 ) ) ;
#13326=CARTESIAN_POINT ( 'NONE',  ( 4.242640687119285658, 293.6875000034139589, -4.242640687119286547 ) ) ;
#13345=ORIENTED_EDGE ( 'NONE', *, *, #22371, .F. ) ;
#13349=CARTESIAN_POINT ( 'NONE',  ( -4.999999999999998224, 51.66666666666667140, -8.660254037844389075 ) ) ;
#13351=CARTESIAN_POINT ( 'NONE',  ( 6.000000000000003553, 297.5625000000000568, -2.485281374238571761 ) ) ;
#13354=ORIENTED_EDGE ( 'NONE', *, *, #56867, .T. ) ;
#13363=CARTESIAN_POINT ( 'NONE',  ( -8.660254037844387298, 172.0833333333333428, -5.000000000000004441 ) ) ;
#13367=CARTESIAN_POINT ( 'NONE',  ( 8.311093377946834337, 140.4687499965859843, 8.311093377946839666 ) ) ;
#13372=CARTESIAN_POINT ( 'NONE',  ( -10.00000000000000178, 167.2916666666666856, -2.679491924311230733 ) ) ;
#13375=CARTESIAN_POINT ( 'NONE',  ( -11.35316468749999785, 13.38541666325268409, -3.042071309553167513 ) ) ;
#13381=CARTESIAN_POINT ( 'NONE',  ( 8.660254037844385522, 36.45833332650536818, 5.000000000000005329 ) ) ;
#13388=CARTESIAN_POINT ( 'NONE',  ( 7.320508075688771044, 6.249999993172032475, 7.320508075688775484 ) ) ;
#13394=CARTESIAN_POINT ( 'NONE',  ( 9.832129032723420536, 116.1979166632526841, -5.676582343749999815 ) ) ;
#13402=CARTESIAN_POINT ( 'NONE',  ( -8.311093377946836114, 117.6562499965860269, -8.311093377946837890 ) ) ;
#13406=ORIENTED_EDGE ( 'NONE', *, *, #30419, .T. ) ;
#13407=CARTESIAN_POINT ( 'NONE',  ( -2.679491924311235618, 205.4166666598387394, 10.00000000000000000 ) ) ;
#13410=CARTESIAN_POINT ( 'NONE',  ( -11.35316468749999785, 103.3854166632526699, -3.042071309553167957 ) ) ;
#13414=CARTESIAN_POINT ( 'NONE',  ( 8.311093377946837890, 11.71874999658601801, -8.311093377946837890 ) ) ;
#13423=CARTESIAN_POINT ( 'NONE',  ( -4.088227598258586603E-16, 292.2031250017069510, -6.676582343750001591 ) ) ;
#13424=CARTESIAN_POINT ( 'NONE',  ( 6.123233995736767268E-16, 128.1249999931720254, -10.00000000000000178 ) ) ;
#13425=CARTESIAN_POINT ( 'NONE',  ( -11.35316468750000141, 223.5937499965860127, -1.390361679473963753E-15 ) ) ;
#13445=CARTESIAN_POINT ( 'NONE',  ( 4.721056650415999201, 292.0781250017069510, -4.721056650415999201 ) ) ;
#13453=( BOUNDED_CURVE ( )  B_SPLINE_CURVE ( 2, ( #32923, #22681, #16269, #38193, #55929, #67974, #45699, #15532, #9527, #4240, #55553, #39310, #50613, #45330, #27985, #27227, #3866, #62674, #44968, #50990, #15162, #74002, #22305, #4984, #11009, #5350, #16642, #39675, #34042, #57039, #50243, #67236, #73633, #28351, #21938, #61938, #62308, #51360, #74370, #61197, #73265, #26861, #49876, #72891, #21198, #21569, #10635, #44223, #38573, #44596, #67608, #33662, #15905, #38936, #10265, #56289, #33292, #4607, #27602, #53227, #6830, #23432, #11747, #34411, #24167, #18520, #35150, #63052, #11377, #69464, #17024, #46446, #6096, #7203, #23062, #29102, #52854, #1186, #18150, #52484, #52121, #12112, #1559, #57414, #46811, #58523, #35510, #58165, #47179, #17772, #23808, #5720, #30207, #29842, #6471, #41528, #64543, #40787, #35877, #29474, #57788, #46071, #40048, #28720, #821, #453, #12479, #51735, #24538, #70211, #69835, #41165, #63793, #69091, #17397, #40421, #68713, #12840, #34785, #58894, #85, #64175, #63419, #1909, #7936, #31692, #54712, #71662, #31311, #30941, #37732, #19983, #55087, #59621, #25639, #37351, #14316, #65641, #3019, #2274, #2650, #42256, #48287, #26002, #36611, #43368, #25268, #59984, #48654, #60350, #72035, #24897, #60730, #66010, #49027, #20351, #8677, #30576, #47914, #71292, #53598, #66385, #42992, #13206, #65268, #14691, #9052, #32066, #70933, #53961, #3395, #19245, #47546, #19613, #13573, #70570, #18886, #41892, #42626, #64902, #36245, #13937, #36979, #8300, #59260, #54339, #7572, #26379, #62585, #21846, #27142, #3770, #9805, #32827, #49403, #39218, #10544, #67884, #22218, #16552, #62218, #39589, #44503, #50523, #45245, #55837, #4892, #32449, #10173, #38477, #4153, #16175, #50158, #9431, #50899, #33951, #10917, #72424, #15069, #21112, #73538, #67515, #49789, #20733, #73175, #61102, #38102, #68257, #15814, #21482, #38849, #61853, #56949, #43751, #66765, #56205, #61480, #26771, #33576, #56579, #55458, #72803, #44135, #27889, #33209, #73914, #67145, #4518, #15440, #27513, #44878, #28635, #41448, #6749, #63705, #58439, #12397, #35430, #52028, #12030, #58076, #34320, #18062, #29393, #45613, #21306, #52400, #64460, #736, #62965, #17309, #6387, #11290, #29752, #63332, #51649, #12760, #23718, #28266, #22980, #46722, #365, #11658, #57324, #40328, #69748, #45986, #5635, #5265, #35792, #41077, #6008, #69002, #34692, #57700, #51273, #64087, #52766, #1103, #24080, #70127, #47089, #18433, #23347, #74283, #22593, #29009, #68627, #46357, #35063, #69374, #17684, #16936, #40701, #39961, #8591, #66302, #71950, #58806, #47464, #53510, #70487, #25186, #7488, #7118, #42166, #18806, #41810, #36158, #24455, #64820, #7851, #42905, #13122, #59178, #53141, #13490, #1828, #30493, #14229, #31605, #20263, #54627, #24815, #19899, #47830, #13851, #36894, #70851, #59904, #25554, #48568, #37271, #65925, #48940, #19164, #8218, #65179, #30858, #60264, #36529, #31230, #59539, #53879, #2189, #48199, #54254, #2936, #30124, #71208, #19526, #42544, #2565, #1474, #43287, #71577, #65557, #25922, #14609, #14981, #38017, #4067, #31980, #55004, #38390, #60646, #67056, #49705, #50814, #66676, #72718, #21762, #44791, #61770, #21394, #21022, #27801, #10088, #45158, #44046, #15728, #15355, #61017, #67804, #4429, #3310, #9342, #32362, #61394, #16095, #26681, #33488, #9720, #50072, #38769, #50439, #62134, #55376, #73825, #56120, #39130, #10457, #56490, #32741, #44417, #33126, #26297, #20649, #55750, #8967, #27060, #73086, #73455, #3682, #67431, #49318, #27424, #4807, #22132, #68168, #37648, #72334, #43664, #39504, #11204, #69288, #23996, #16842, #10828, #34231, #56862, #17598, #51940, #46640, #29303, #5545, #5178, #63999, #46269, #52313, #47006, #1016, #22886, #5921, #11945, #57233, #34977, #29666, #34604, #40616, #35346, #45898, #69660, #22500, #278, #28547, #51554, #17222, #17973, #74573, #12314, #68912, #58358, #28924, #40242, #39869, #52682, #40992, #23260, #6663, #23633, #16467, #63244, #63618, #57993, #33863, #74195, #11570, #62499, #57611, #6297, #28175, #649, #45522, #51187, #68538, #62871, #48483, #53424, #41725, #2843, #71119, #18346, #64737, #48109, #25833, #70402, #64370, #13036, #35703, #19440, #24369, #70037, #31516, #65469, #70761, #47376, #1747, #24728, #41360, #8131, #54166, #36807, #65834, #60177, #31134, #25466, #71485, #19811, #36072, #18717, #42817, #1385, #53791, #7399, #47737, #59817, #19077, #53053, #14141, #12671, #8499, #58719, #7030, #59090, #42451, #30037, #30406, #42081, #65091, #13763, #13402, #36440, #59453, #7767, #30769, #2474, #2100, #25094, #37176, #54537, #66585, #14515, #5364, #74383, #15267, #43193, #66210, #49612, #71861, #3592, #26965, #3220, #49981, #15637, #38678, #17037, #38300, #55288, #72627, #66962, #57427, #37553, #60553, #3978, #9249, #49228, #56033, #61680, #8877, #20555, #31890, #60928, #72998, #68724, #20175, #54911, #61308, #32271, #67341, #26208, #34425, #10001, #32652, #9632, #20931, #72239, #43568, #14889, #63067, #45712, #43953, #37928, #26588, #55661, #11389, #21305, #44328, #33031, #28364, #51373, #22694, #40062, #5734, #48852, #36260, #40801, #6843, #18534, #70224, #46826, #41541, #46085, #466, #23444, #29487, #58909, #17788, #24552, #6484, #41179, #29857, #64557, #53240, #57802, #18899, #47193, #7220, #30222, #12853, #11760, #35524, #52869, #23075, #34797, #12124, #51748, #52497, #63808, #35892, #46459, #12494, #97, #1201, #6109, #58536, #1571, #35162, #69104, #24182, #47558, #69477, #70582, #59275, #29114, #17411, #58178, #40433, #41906, #64189, #64914, #13222, #835, #63433, #28732, #52133, #23822, #69851, #18163, #66780, #13950, #3410, #72441, #43384, #37747, #9070, #60747, #2286, #59634, #43006, #14709, #66026, #54352, #37366, #32082, #66401, #20750, #71308, #8692, #65654, #2662, #70945, #25282, #54730, #47927, #19260, #7585, #42272, #48300, #3037, #65284, #13590, #36628, #19628, #31707, #26394, #30590, #7950, #48670, #42642, #26020, #30955, #53976, #1923, #36991, #59998, #8315, #55102, #49419, #71677, #24911, #31325, #25654, #53610, #19998, #14334, #43766, #60366, #49043, #15084, #38119, #72050, #20367, #51290, #33592, #68644, #73191, #39234, #50916, #27907, #4534, #45261, #15829, #16193, #55472, #22609, #22235, #27529, #33970, #56967, #38864, #62234, #73930, #10933, #15457, #74301, #4913, #39606, #62603, #68273, #44147, #61495, #61868, #67162, #38492, #16569, #10561, #26786, #55852, #56597, #45630, #44894, #9448, #5282, #9817, #28284, #16953, #21499, #32465, #67901, #61118, #3785, #44518, #49803, #56220, #67530, #32842, #10191, #72819, #4169, #27156, #21126, #50173, #33222, #50541, #73556, #21865, #70502, #35078, #24471, #46375, #29407, #35445, #57715, #58456, #53156, #58090, #64101, #58821, #69390, #18449, #23734, #12044, #69763, #41463, #24095, #30140, #29025, #41092, #23360, #1490, #1119, #70142, #64477, #12774, #34706, #17324, #751, #47104, #46739, #6401, #17698, #29767, #40716, #22995, #35806, #47478, #39977, #62984, #28650, #6021, #12411, #5649, #51665, #8, #52044, #6763, #7132, #11307, #46002, #52415, #63722, #34340, #69020, #40345, #57340, #18076, #380, #63347, #11672, #52781, #59919, #13137, #36172, #19542, #41824, #48214, #30875, #31998, #47846, #53893, #60280, #60661, #8234, #25201, #42559, #36911, #26313, #59192, #7502, #48583, #2205, #19178, #25940, #8606, #30508, #65193, #13504, #65571, #48957, #7869, #14624, #71222, #8983, #31245, #13868, #42181, #55018, #20281, #2581, #71967, #43303, #66318, #54271, #25570, #71593, #53526, #1844, #19915, #64834, #42923, #65942, #3325, #14250, #24830, #37287, #31621, #70867, #37663, #54642, #36543, #49336, #2950, #59554, #18821, #50453, #5196, #72734, #66693, #67072, #38034, #44062, #26699, #72352, #33880, #67818, #73103, #49719, #55766, #4082, #20664, #10474, #56507, #39147, #68189, #27076, #15371, #61033, #27821, #22148, #38783, #16485, #38408, #33505, #9358, #27438, #73469, #21038, #21778, #62151, #4824, #39522, #61786, #50089, #21410, #15744, #28193, #14996, #32377, #44805, #32758, #10104, #50831, #44432, #16110, #55392, #56880, #73842, #33142, #45176, #62518, #67447, #10846, #56137, #61410, #9736, #43682, #3701, #4447, #29682, #58374, #34249, #51573, #28940, #57251, #5564, #64017, #666, #16860, #45916, #23651, #12687, #46658, #28565, #63260, #52329, #74590, #52699, #34621, #22904, #58736, #34995, #24013, #11586, #58010, #46284, #57627, #68928, #5940, #69677, #17239, #40258, #51204, #35721, #17990, #51959, #296, #23276, #69304, #74215, #12330, #41008, #47022, #41378, #35363, #6680, #1033, #70054, #17615, #40633, #11964, #18364, #6316, #63633, #29320, #64389, #7047, #22520, #45540, #68557, #39885, #62888, #11221 ),
 .UNSPECIFIED., .F., .F. ) 
 B_SPLINE_CURVE_WITH_KNOTS ( ( 3, 2, 2, 2, 2, 2, 2, 2, 2, 2, 2, 2, 2, 2, 2, 2, 2, 2, 2, 2, 2, 2, 2, 2, 2, 2, 2, 2, 2, 2, 2, 2, 2, 2, 2, 2, 2, 2, 2, 2, 2, 2, 2, 2, 2, 2, 2, 2, 2, 2, 2, 2, 2, 2, 2, 2, 2, 2, 2, 2, 2, 2, 2, 2, 2, 2, 2, 2, 2, 2, 2, 2, 2, 2, 2, 2, 2, 2, 2, 2, 2, 2, 2, 2, 2, 2, 2, 2, 2, 2, 2, 2, 2, 2, 2, 2, 2, 2, 2, 2, 2, 2, 2, 2, 2, 2, 2, 2, 2, 2, 2, 2, 2, 2, 2, 2, 2, 2, 2, 2, 2, 2, 2, 2, 2, 2, 2, 2, 2, 2, 2, 2, 2, 2, 2, 2, 2, 2, 2, 2, 2, 2, 2, 2, 2, 2, 2, 2, 2, 2, 2, 2, 2, 2, 2, 2, 2, 2, 2, 2, 2, 2, 2, 2, 2, 2, 2, 2, 2, 2, 2, 2, 2, 2, 2, 2, 2, 2, 2, 2, 2, 2, 2, 2, 2, 2, 2, 2, 2, 2, 2, 2, 2, 2, 2, 2, 2, 2, 2, 2, 2, 2, 2, 2, 2, 2, 2, 2, 2, 2, 2, 2, 2, 2, 2, 2, 2, 2, 2, 2, 2, 2, 2, 2, 2, 2, 2, 2, 2, 2, 2, 2, 2, 2, 2, 2, 2, 2, 2, 2, 2, 2, 2, 2, 2, 2, 2, 2, 2, 2, 2, 2, 2, 2, 2, 2, 2, 2, 2, 2, 2, 2, 2, 2, 2, 2, 2, 2, 2, 2, 2, 2, 2, 2, 2, 2, 2, 2, 2, 2, 2, 2, 2, 2, 2, 2, 2, 2, 2, 2, 2, 2, 2, 2, 2, 2, 2, 2, 2, 2, 2, 2, 2, 2, 2, 2, 2, 2, 2, 2, 2, 2, 2, 2, 2, 2, 2, 2, 2, 2, 2, 2, 2, 2, 2, 2, 2, 2, 2, 2, 2, 2, 2, 2, 2, 2, 2, 2, 2, 2, 2, 2, 2, 2, 2, 2, 2, 2, 2, 2, 2, 2, 2, 2, 2, 2, 2, 2, 2, 2, 2, 2, 2, 2, 2, 2, 2, 2, 2, 2, 2, 2, 2, 2, 2, 2, 2, 2, 2, 2, 2, 2, 2, 2, 2, 2, 2, 2, 2, 2, 2, 2, 2, 2, 2, 2, 2, 2, 2, 2, 2, 2, 2, 2, 2, 2, 2, 2, 2, 2, 2, 2, 2, 2, 2, 2, 2, 2, 2, 2, 2, 2, 2, 2, 2, 2, 2, 2, 2, 2, 2, 2, 2, 2, 2, 2, 2, 2, 2, 2, 2, 2, 2, 2, 2, 2, 2, 2, 2, 2, 2, 2, 2, 2, 2, 2, 2, 2, 2, 2, 2, 2, 2, 2, 2, 2, 2, 2, 2, 2, 2, 2, 2, 2, 2, 2, 2, 2, 2, 2, 2, 2, 2, 2, 2, 2, 2, 2, 2, 2, 2, 2, 2, 2, 2, 2, 2, 2, 2, 2, 2, 2, 2, 2, 2, 2, 2, 2, 2, 2, 2, 2, 2, 2, 2, 2, 2, 2, 2, 2, 2, 2, 2, 2, 2, 2, 2, 2, 2, 2, 2, 2, 2, 2, 2, 2, 2, 2, 2, 2, 2, 3 ),
 ( 0.000000000000000000, 0.001843655950715879319, 0.003687311901431758639, 0.005530967852147637524, 0.007374623802863517277, 0.009218279753579396163, 0.01106193570429527505, 0.01290559165501115740, 0.01474924760572703455, 0.01659290355644291171, 0.01843655950715879233, 0.02028021545787467295, 0.02212387140859055010, 0.02396752735930643072, 0.02581118331002231481, 0.02765483926073818849, 0.02949849521145406911, 0.03134215116216994973, 0.03318580711288582341, 0.03502946306360171097, 0.03687311901431758465, 0.03871677496503346527, 0.04056043091574934589, 0.04240408686646521957, 0.04424774281718110019, 0.04609139876789698775, 0.04793505471861286144, 0.04977871066932874206, 0.05162236662004462961, 0.05346602257076049636, 0.05530967852147637698, 0.05715333447219225760, 0.05899699042290813822, 0.06084064637362401884, 0.06268430232433989946, 0.06452795827505578008, 0.06637161422577164682, 0.06821527017648754132, 0.07005892612720342194, 0.07190258207791928868, 0.07374623802863516930, 0.07558989397935104992, 0.07743354993006693054, 0.07927720588078279729, 0.08112086183149869179, 0.08296451778221457241, 0.08480817373293043915, 0.08665182968364633365, 0.08849548563436220039, 0.09033914158507809489, 0.09218279753579397551, 0.09402645348650984225, 0.09587010943722572287, 0.09771376538794160349, 0.09955742133865748411, 0.1014010772893733647, 0.1032447332400892592, 0.1050883891908051260, 0.1069320451415209927, 0.1087757010922368733, 0.1106193570429527540, 0.1124630129936686485, 0.1143066689443845152, 0.1161503248951003958, 0.1179939808458162764, 0.1198376367965321432, 0.1216812927472480377, 0.1235249486979639183, 0.1253686046486797989, 0.1272122605993956657, 0.1290559165501115602, 0.1308995725008274269, 0.1327432284515432936, 0.1345868844022591881, 0.1364305403529750826, 0.1382741963036909494, 0.1401178522544068439, 0.1419615082051227106, 0.1438051641558385774, 0.1456488201065544441, 0.1474924760572703386, 0.1493361320079862609, 0.1511797879587020998, 0.1530234439094179943, 0.1548670998601338611, 0.1567107558108497278, 0.1585544117615655946, 0.1603980677122815168, 0.1622417236629973836, 0.1640853796137132503, 0.1659290355644291448, 0.1677726915151450116, 0.1696163474658608783, 0.1714600034165768006, 0.1733036593672926673, 0.1751473153180085340, 0.1769909712687244008, 0.1788346272194402953, 0.1806782831701561898, 0.1825219391208720288, 0.1843655950715879510, 0.1862092510223038178, 0.1880529069730196845, 0.1898965629237355512, 0.1917402188744514457, 0.1935838748251673402, 0.1954275307758832070, 0.1972711867265991015, 0.1991148426773149682, 0.2009584986280308350, 0.2028021545787467295, 0.2046458105294625962, 0.2064894664801785185, 0.2083331224308943574, 0.2101767783816102519, 0.2120204343323261187, 0.2138640902830419854, 0.2157077462337578799, 0.2175514021844737467, 0.2193950581351896689, 0.2212387140859055079, 0.2230823700366214024, 0.2249260259873372969, 0.2267696819380531359, 0.2286133378887690304, 0.2304569938394849249, 0.2323006497902007916, 0.2341443057409166861, 0.2359879616916325529, 0.2378316176423484474, 0.2396752735930642864, 0.2415189295437801809, 0.2433625854944960754, 0.2452062414452119421, 0.2470498973959278366, 0.2488935533466437033, 0.2507372092973595978, 0.2525808652480754368, 0.2544245211987913313, 0.2562681771495072258, 0.2581118331002231203, 0.2599554890509390148, 0.2617991450016548538, 0.2636428009523706928, 0.2654864569030865873, 0.2673301128538024818, 0.2691737688045183763, 0.2710174247552342708, 0.2728610807059501653, 0.2747047366566660043, 0.2765483926073818988, 0.2783920485580977933, 0.2802357045088136878, 0.2820793604595295268, 0.2839230164102454212, 0.2857666723609613157, 0.2876103283116771547, 0.2894539842623930492, 0.2912976402131088882, 0.2931412961638247827, 0.2949849521145406772, 0.2968286080652566272, 0.2986722640159725217, 0.3005159199666883052, 0.3023595759174041997, 0.3042032318681200942, 0.3060468878188359887, 0.3078905437695518832, 0.3097341997202677222, 0.3115778556709836167, 0.3134215116216994557, 0.3152651675724153502, 0.3171088235231311891, 0.3189524794738471392, 0.3207961354245630337, 0.3226397913752789282, 0.3244834473259947671, 0.3263271032767106061, 0.3281707592274265006, 0.3300144151781423951, 0.3318580711288582896, 0.3337017270795741841, 0.3355453830302900231, 0.3373890389810058621, 0.3392326949317217566, 0.3410763508824376511, 0.3429200068331536011, 0.3447636627838694401, 0.3466073187345853346, 0.3484509746853012291, 0.3502946306360170681, 0.3521382865867329626, 0.3539819425374488016, 0.3558255984881646961, 0.3576692544388805906, 0.3595129103895964851, 0.3613565663403123795, 0.3632002222910281630, 0.3650438782417440575, 0.3668875341924600075, 0.3687311901431759020, 0.3705748460938917410, 0.3724185020446076355, 0.3742621579953235300, 0.3761058139460393690, 0.3779494698967552635, 0.3797931258474711025, 0.3816367817981869970, 0.3834804377489028915, 0.3853240936996187860, 0.3871677496503346805, 0.3890114056010504640, 0.3908550615517664140, 0.3926987175024823085, 0.3945423734531982030, 0.3963860294039140975, 0.3982296853546299364, 0.4000733413053458309, 0.4019169972560616699, 0.4037606532067775644, 0.4056043091574934589, 0.4074479651082092979, 0.4092916210589251924, 0.4111352770096410869, 0.4129789329603570369, 0.4148225889110728759, 0.4166662448617887149, 0.4185099008125046094, 0.4203535567632205039, 0.4221972127139363984, 0.4240408686646522374, 0.4258845246153681319, 0.4277281805660839709, 0.4295718365167998654, 0.4314154924675157599, 0.4332591484182315988, 0.4351028043689474933, 0.4369464603196634434, 0.4387901162703793378, 0.4406337722210951768, 0.4424774281718110158, 0.4443210841225269103, 0.4461647400732428048, 0.4480083960239586993, 0.4498520519746745938, 0.4516957079253903773, 0.4535393638761062718, 0.4553830198268221663, 0.4572266757775380608, 0.4590703317282539553, 0.4609139876789698498, 0.4627576436296857443, 0.4646012995804015833, 0.4664449555311174778, 0.4682886114818333723, 0.4701322674325492113, 0.4719759233832651057, 0.4738195793339810002, 0.4756632352846968947, 0.4775068912354127337, 0.4793505471861285727, 0.4811942031368444672, 0.4830378590875603617, 0.4848815150382763117, 0.4867251709889921507, 0.4885688269397080452, 0.4904124828904238842, 0.4922561388411397787, 0.4940997947918556732, 0.4959434507425715122, 0.4977871066932874067, 0.4996307626440033012, 0.5014744185947191957, 0.5033180745454350902, 0.5051617304961508736, 0.5070053864468667681, 0.5088490423975826626, 0.5106926983482985571, 0.5125363542990144516, 0.5143800102497303461, 0.5162236662004462406, 0.5180673221511620241, 0.5199109781018780296, 0.5217546340525938131, 0.5235982900033097076, 0.5254419459540256021, 0.5272856019047413856, 0.5291292578554573911, 0.5309729138061731746, 0.5328165697568891801, 0.5346602257076049636, 0.5365038816583208581, 0.5383475376090367526, 0.5401911935597526471, 0.5420348495104685416, 0.5438785054611844361, 0.5457221614119003306, 0.5475658173626161140, 0.5494094733133320085, 0.5512531292640479030, 0.5530967852147637975, 0.5549404411654795810, 0.5567840971161955865, 0.5586277530669113700, 0.5604714090176273755, 0.5623150649683431590, 0.5641587209190590535, 0.5660023768697749480, 0.5678460328204908425, 0.5696896887712068480, 0.5715333447219226315, 0.5733770006726384150, 0.5752206566233543095, 0.5770643125740702040, 0.5789079685247860985, 0.5807516244755019930, 0.5825952804262177764, 0.5844389363769337820, 0.5862825923276495654, 0.5881262482783655710, 0.5899699042290813544, 0.5918135601797972489, 0.5936572161305132544, 0.5955008720812290379, 0.5973445280319450434, 0.5991881839826607159, 0.6010318399333766104, 0.6028754958840925049, 0.6047191518348083994, 0.6065628077855242939, 0.6084064637362401884, 0.6102501196869559719, 0.6120937756376719774, 0.6139374315883877609, 0.6157810875391037664, 0.6176247434898196609, 0.6194683994405354444, 0.6213120553912514499, 0.6231557113419672334, 0.6249993672926830168, 0.6268430232433989113, 0.6286866791941148058, 0.6305303351448307003, 0.6323739910955465948, 0.6342176470462623783, 0.6360613029969783838, 0.6379049589476942783, 0.6397486148984101728, 0.6415922708491260673, 0.6434359267998418508, 0.6452795827505578563, 0.6471232387012736398, 0.6489668946519895343, 0.6508105506027053178, 0.6526542065534212123, 0.6544978625041371068, 0.6563415184548530013, 0.6581851744055688958, 0.6600288303562847902, 0.6618724863070006847, 0.6637161422577165792, 0.6655597982084324737, 0.6674034541591483682, 0.6692471101098642627, 0.6710907660605800462, 0.6729344220112960517, 0.6747780779620117242, 0.6766217339127277297, 0.6784653898634435132, 0.6803090458141594077, 0.6821527017648753022, 0.6839963577155911967, 0.6858400136663072022, 0.6876836696170229857, 0.6895273255677388802, 0.6913709815184547747, 0.6932146374691706692, 0.6950582934198865637, 0.6969019493706024582, 0.6987456053213182416, 0.7005892612720341361, 0.7024329172227499196, 0.7042765731734659251, 0.7061202291241817086, 0.7079638850748976031, 0.7098075410256136086, 0.7116511969763293921, 0.7134948529270453976, 0.7153385088777611811, 0.7171821648284770756, 0.7190258207791929701, 0.7208694767299088646, 0.7227131326806247591, 0.7245567886313406536, 0.7264004445820563260, 0.7282441005327723316, 0.7300877564834881150, 0.7319314124342041206, 0.7337750683849200151, 0.7356187243356357985, 0.7374623802863518041, 0.7393060362370675875, 0.7411496921877834820, 0.7429933481384993765, 0.7448370040892152710, 0.7466806600399311655, 0.7485243159906470600, 0.7503679719413628435, 0.7522116278920787380, 0.7540552838427945215, 0.7558989397935105270, 0.7577425957442264215, 0.7595862516949422050, 0.7614299076456582105, 0.7632735635963739940, 0.7651172195470899995, 0.7669608754978057830, 0.7688045314485216775, 0.7706481873992375720, 0.7724918433499534665, 0.7743354993006693610, 0.7761791552513851444, 0.7780228112021009279, 0.7798664671528169334, 0.7817101231035328279, 0.7835537790542487224, 0.7853974350049646169, 0.7872410909556804004, 0.7890847469063964059, 0.7909284028571121894, 0.7927720588078281949, 0.7946157147585439784, 0.7964593707092598729, 0.7983030266599757674, 0.8001466826106916619, 0.8019903385614074454, 0.8038339945121233399, 0.8056776504628392344, 0.8075213064135551289, 0.8093649623642710234, 0.8112086183149869179, 0.8130522742657028124, 0.8148959302164185958, 0.8167395861671346013, 0.8185832421178503848, 0.8204268980685663903, 0.8222705540192821738, 0.8241142099699980683, 0.8259578659207140738, 0.8278015218714297463, 0.8296451778221457518, 0.8314888337728615353, 0.8333324897235774298, 0.8351761456742933243, 0.8370198016250092188, 0.8388634575757251133, 0.8407071135264410078, 0.8425507694771567913, 0.8443944254278727968, 0.8462380813785885803, 0.8480817373293044747, 0.8499253932800204803, 0.8517690492307362637, 0.8536127051814521582, 0.8554563611321679417, 0.8573000170828838362, 0.8591436730335997307, 0.8609873289843156252, 0.8628309849350315197, 0.8646746408857474142, 0.8665182968364631977, 0.8683619527871792032, 0.8702056087378949867, 0.8720492646886109922, 0.8738929206393268867, 0.8757365765900426702, 0.8775802325407586757, 0.8794238884914743482, 0.8812675444421903537, 0.8831112003929061371, 0.8849548563436220316, 0.8867985122943379261, 0.8886421682450538206, 0.8904858241957697151, 0.8923294801464856096, 0.8941731360972013931, 0.8960167920479173986, 0.8978604479986332931, 0.8997041039493491876, 0.9015477599000650821, 0.9033914158507807546, 0.9052350718014967601, 0.9070787277522125436, 0.9089223837029285491, 0.9107660396536443326, 0.9126096956043602271, 0.9144533515550761216, 0.9162970075057920161, 0.9181406634565079106, 0.9199843194072238051, 0.9218279753579396996, 0.9236716313086555941, 0.9255152872593714886, 0.9273589432100873831, 0.9292025991608031665, 0.9310462551115189500, 0.9328899110622349555, 0.9347335670129507390, 0.9365772229636667445, 0.9384208789143825280, 0.9402645348650984225, 0.9421081908158143170, 0.9439518467665302115, 0.9457955027172462170, 0.9476391586679620005, 0.9494828146186778950, 0.9513264705693937895, 0.9531701265201096840, 0.9550137824708254675, 0.9568574384215413620, 0.9587010943722571454, 0.9605447503229731510, 0.9623884062736889344, 0.9642320622244048289, 0.9660757181751207234, 0.9679193741258366179, 0.9697630300765526234, 0.9716066860272684069, 0.9734503419779843014, 0.9752939979287001959, 0.9771376538794160904, 0.9789813098301319849, 0.9808249657808477684, 0.9826686217315635519, 0.9845122776822795574, 0.9863559336329953409, 0.9881995895837113464, 0.9900432455344271299, 0.9918869014851430244, 0.9937305574358590299, 0.9955742133865748134, 0.9965413494093805502 ),
 .UNSPECIFIED. ) 
 CURVE ( )  GEOMETRIC_REPRESENTATION_ITEM ( )  RATIONAL_B_SPLINE_CURVE ( ( 1.000000000000000000, 0.9659258262890683122, 1.000000000000000000, 0.9659258262890683122, 1.000000000000000000, 0.9659258262890683122, 1.000000000000000000, 0.9659258262890683122, 1.000000000000000000, 0.9659258262890683122, 1.000000000000000000, 0.9659258262890683122, 1.000000000000000000, 0.9659258262890683122, 1.000000000000000000, 0.9659258262890683122, 1.000000000000000000, 0.9659258262890683122, 1.000000000000000000, 0.9659258262890683122, 1.000000000000000000, 0.9659258262890683122, 1.000000000000000000, 0.9659258262890683122, 1.000000000000000000, 0.9659258262890683122, 1.000000000000000000, 0.9659258262890683122, 1.000000000000000000, 0.9659258262890683122, 1.000000000000000000, 0.9659258262890683122, 1.000000000000000000, 0.9659258262890683122, 1.000000000000000000, 0.9659258262890683122, 1.000000000000000000, 0.9659258262890683122, 1.000000000000000000, 0.9659258262890683122, 1.000000000000000000, 0.9659258262890683122, 1.000000000000000000, 0.9659258262890683122, 1.000000000000000000, 0.9659258262890683122, 1.000000000000000000, 0.9659258262890683122, 1.000000000000000000, 0.9659258262890683122, 1.000000000000000000, 0.9659258262890683122, 1.000000000000000000, 0.9659258262890683122, 1.000000000000000000, 0.9659258262890683122, 1.000000000000000000, 0.9659258262890683122, 1.000000000000000000, 0.9659258262890683122, 1.000000000000000000, 0.9659258262890683122, 1.000000000000000000, 0.9659258262890683122, 1.000000000000000000, 0.9659258262890683122, 1.000000000000000000, 0.9659258262890683122, 1.000000000000000000, 0.9659258262890683122, 1.000000000000000000, 0.9659258262890683122, 1.000000000000000000, 0.9659258262890683122, 1.000000000000000000, 0.9659258262890683122, 1.000000000000000000, 0.9659258262890683122, 1.000000000000000000, 0.9659258262890683122, 1.000000000000000000, 0.9659258262890683122, 1.000000000000000000, 0.9659258262890683122, 1.000000000000000000, 0.9659258262890683122, 1.000000000000000000, 0.9659258262890683122, 1.000000000000000000, 0.9659258262890683122, 1.000000000000000000, 0.9659258262890683122, 1.000000000000000000, 0.9659258262890683122, 1.000000000000000000, 0.9659258262890683122, 1.000000000000000000, 0.9659258262890683122, 1.000000000000000000, 0.9659258262890683122, 1.000000000000000000, 0.9659258262890683122, 1.000000000000000000, 0.9659258262890683122, 1.000000000000000000, 0.9659258262890683122, 1.000000000000000000, 0.9659258262890683122, 1.000000000000000000, 0.9659258262890683122, 1.000000000000000000, 0.9659258262890683122, 1.000000000000000000, 0.9659258262890683122, 1.000000000000000000, 0.9659258262890683122, 1.000000000000000000, 0.9659258262890683122, 1.000000000000000000, 0.9659258262890683122, 1.000000000000000000, 0.9659258262890683122, 1.000000000000000000, 0.9659258262890683122, 1.000000000000000000, 0.9659258262890683122, 1.000000000000000000, 0.9659258262890683122, 1.000000000000000000, 0.9659258262890683122, 1.000000000000000000, 0.9659258262890683122, 1.000000000000000000, 0.9659258262890683122, 1.000000000000000000, 0.9659258262890683122, 1.000000000000000000, 0.9659258262890683122, 1.000000000000000000, 0.9659258262890683122, 1.000000000000000000, 0.9659258262890683122, 1.000000000000000000, 0.9659258262890683122, 1.000000000000000000, 0.9659258262890683122, 1.000000000000000000, 0.9659258262890683122, 1.000000000000000000, 0.9659258262890683122, 1.000000000000000000, 0.9659258262890683122, 1.000000000000000000, 0.9659258262890683122, 1.000000000000000000, 0.9659258262890683122, 1.000000000000000000, 0.9659258262890683122, 1.000000000000000000, 0.9659258262890683122, 1.000000000000000000, 0.9659258262890683122, 1.000000000000000000, 0.9659258262890683122, 1.000000000000000000, 0.9659258262890683122, 1.000000000000000000, 0.9659258262890683122, 1.000000000000000000, 0.9659258262890683122, 1.000000000000000000, 0.9659258262890683122, 1.000000000000000000, 0.9659258262890683122, 1.000000000000000000, 0.9659258262890683122, 1.000000000000000000, 0.9659258262890683122, 1.000000000000000000, 0.9659258262890683122, 1.000000000000000000, 0.9659258262890683122, 1.000000000000000000, 0.9659258262890683122, 1.000000000000000000, 0.9659258262890683122, 1.000000000000000000, 0.9659258262890683122, 1.000000000000000000, 0.9659258262890683122, 1.000000000000000000, 0.9659258262890683122, 1.000000000000000000, 0.9659258262890683122, 1.000000000000000000, 0.9659258262890683122, 1.000000000000000000, 0.9659258262890683122, 1.000000000000000000, 0.9659258262890683122, 1.000000000000000000, 0.9659258262890683122, 1.000000000000000000, 0.9659258262890683122, 1.000000000000000000, 0.9659258262890683122, 1.000000000000000000, 0.9659258262890683122, 1.000000000000000000, 0.9659258262890683122, 1.000000000000000000, 0.9659258262890683122, 1.000000000000000000, 0.9659258262890683122, 1.000000000000000000, 0.9659258262890683122, 1.000000000000000000, 0.9659258262890683122, 1.000000000000000000, 0.9659258262890683122, 1.000000000000000000, 0.9659258262890683122, 1.000000000000000000, 0.9659258262890683122, 1.000000000000000000, 0.9659258262890683122, 1.000000000000000000, 0.9659258262890683122, 1.000000000000000000, 0.9659258262890683122, 1.000000000000000000, 0.9659258262890683122, 1.000000000000000000, 0.9659258262890683122, 1.000000000000000000, 0.9659258262890683122, 1.000000000000000000, 0.9659258262890683122, 1.000000000000000000, 0.9659258262890683122, 1.000000000000000000, 0.9659258262890683122, 1.000000000000000000, 0.9659258262890683122, 1.000000000000000000, 0.9659258262890683122, 1.000000000000000000, 0.9659258262890683122, 1.000000000000000000, 0.9659258262890683122, 1.000000000000000000, 0.9659258262890683122, 1.000000000000000000, 0.9659258262890683122, 1.000000000000000000, 0.9659258262890683122, 1.000000000000000000, 0.9659258262890683122, 1.000000000000000000, 0.9659258262890683122, 1.000000000000000000, 0.9659258262890683122, 1.000000000000000000, 0.9659258262890683122, 1.000000000000000000, 0.9659258262890683122, 1.000000000000000000, 0.9659258262890683122, 1.000000000000000000, 0.9659258262890683122, 1.000000000000000000, 0.9659258262890683122, 1.000000000000000000, 0.9659258262890683122, 1.000000000000000000, 0.9659258262890683122, 1.000000000000000000, 0.9659258262890683122, 1.000000000000000000, 0.9659258262890683122, 1.000000000000000000, 0.9659258262890683122, 1.000000000000000000, 0.9659258262890683122, 1.000000000000000000, 0.9659258262890683122, 1.000000000000000000, 0.9659258262890683122, 1.000000000000000000, 0.9659258262890683122, 1.000000000000000000, 0.9659258262890683122, 1.000000000000000000, 0.9659258262890683122, 1.000000000000000000, 0.9659258262890683122, 1.000000000000000000, 0.9659258262890683122, 1.000000000000000000, 0.9659258262890683122, 1.000000000000000000, 0.9659258262890683122, 1.000000000000000000, 0.9659258262890683122, 1.000000000000000000, 0.9659258262890683122, 1.000000000000000000, 0.9659258262890683122, 1.000000000000000000, 0.9659258262890683122, 1.000000000000000000, 0.9659258262890683122, 1.000000000000000000, 0.9659258262890683122, 1.000000000000000000, 0.9659258262890683122, 1.000000000000000000, 0.9659258262890683122, 1.000000000000000000, 0.9659258262890683122, 1.000000000000000000, 0.9659258262890683122, 1.000000000000000000, 0.9659258262890683122, 1.000000000000000000, 0.9659258262890683122, 1.000000000000000000, 0.9659258262890683122, 1.000000000000000000, 0.9659258262890683122, 1.000000000000000000, 0.9659258262890683122, 1.000000000000000000, 0.9659258262890683122, 1.000000000000000000, 0.9659258262890683122, 1.000000000000000000, 0.9659258262890683122, 1.000000000000000000, 0.9659258262890683122, 1.000000000000000000, 0.9659258262890683122, 1.000000000000000000, 0.9659258262890683122, 1.000000000000000000, 0.9659258262890683122, 1.000000000000000000, 0.9659258262890683122, 1.000000000000000000, 0.9659258262890683122, 1.000000000000000000, 0.9659258262890683122, 1.000000000000000000, 0.9659258262890683122, 1.000000000000000000, 0.9659258262890683122, 1.000000000000000000, 0.9659258262890683122, 1.000000000000000000, 0.9659258262890683122, 1.000000000000000000, 0.9659258262890683122, 1.000000000000000000, 0.9659258262890683122, 1.000000000000000000, 0.9659258262890683122, 1.000000000000000000, 0.9659258262890683122, 1.000000000000000000, 0.9659258262890683122, 1.000000000000000000, 0.9659258262890683122, 1.000000000000000000, 0.9659258262890683122, 1.000000000000000000, 0.9659258262890683122, 1.000000000000000000, 0.9659258262890683122, 1.000000000000000000, 0.9659258262890683122, 1.000000000000000000, 0.9659258262890683122, 1.000000000000000000, 0.9659258262890683122, 1.000000000000000000, 0.9659258262890683122, 1.000000000000000000, 0.9659258262890683122, 1.000000000000000000, 0.9659258262890683122, 1.000000000000000000, 0.9659258262890683122, 1.000000000000000000, 0.9659258262890683122, 1.000000000000000000, 0.9659258262890683122, 1.000000000000000000, 0.9659258262890683122, 1.000000000000000000, 0.9659258262890683122, 1.000000000000000000, 0.9659258262890683122, 1.000000000000000000, 0.9659258262890683122, 1.000000000000000000, 0.9659258262890683122, 1.000000000000000000, 0.9659258262890683122, 1.000000000000000000, 0.9659258262890683122, 1.000000000000000000, 0.9659258262890683122, 1.000000000000000000, 0.9659258262890683122, 1.000000000000000000, 0.9659258262890683122, 1.000000000000000000, 0.9659258262890683122, 1.000000000000000000, 0.9659258262890683122, 1.000000000000000000, 0.9659258262890683122, 1.000000000000000000, 0.9659258262890683122, 1.000000000000000000, 0.9659258262890683122, 1.000000000000000000, 0.9659258262890683122, 1.000000000000000000, 0.9659258262890683122, 1.000000000000000000, 0.9659258262890683122, 1.000000000000000000, 0.9659258262890683122, 1.000000000000000000, 0.9659258262890683122, 1.000000000000000000, 0.9659258262890683122, 1.000000000000000000, 0.9659258262890683122, 1.000000000000000000, 0.9659258262890683122, 1.000000000000000000, 0.9659258262890683122, 1.000000000000000000, 0.9659258262890683122, 1.000000000000000000, 0.9659258262890683122, 1.000000000000000000, 0.9659258262890683122, 1.000000000000000000, 0.9659258262890683122, 1.000000000000000000, 0.9659258262890683122, 1.000000000000000000, 0.9659258262890683122, 1.000000000000000000, 0.9659258262890683122, 1.000000000000000000, 0.9659258262890683122, 1.000000000000000000, 0.9659258262890683122, 1.000000000000000000, 0.9659258262890683122, 1.000000000000000000, 0.9659258262890683122, 1.000000000000000000, 0.9659258262890683122, 1.000000000000000000, 0.9659258262890683122, 1.000000000000000000, 0.9659258262890683122, 1.000000000000000000, 0.9659258262890683122, 1.000000000000000000, 0.9659258262890683122, 1.000000000000000000, 0.9659258262890683122, 1.000000000000000000, 0.9659258262890683122, 1.000000000000000000, 0.9659258262890683122, 1.000000000000000000, 0.9659258262890683122, 1.000000000000000000, 0.9659258262890683122, 1.000000000000000000, 0.9659258262890683122, 1.000000000000000000, 0.9659258262890683122, 1.000000000000000000, 0.9659258262890683122, 1.000000000000000000, 0.9659258262890683122, 1.000000000000000000, 0.9659258262890683122, 1.000000000000000000, 0.9659258262890683122, 1.000000000000000000, 0.9659258262890683122, 1.000000000000000000, 0.9659258262890683122, 1.000000000000000000, 0.9659258262890683122, 1.000000000000000000, 0.9659258262890683122, 1.000000000000000000, 0.9659258262890683122, 1.000000000000000000, 0.9659258262890683122, 1.000000000000000000, 0.9659258262890683122, 1.000000000000000000, 0.9659258262890683122, 1.000000000000000000, 0.9659258262890683122, 1.000000000000000000, 0.9659258262890683122, 1.000000000000000000, 0.9659258262890683122, 1.000000000000000000, 0.9659258262890683122, 1.000000000000000000, 0.9659258262890683122, 1.000000000000000000, 0.9659258262890683122, 1.000000000000000000, 0.9659258262890683122, 1.000000000000000000, 0.9659258262890683122, 1.000000000000000000, 0.9659258262890683122, 1.000000000000000000, 0.9659258262890683122, 1.000000000000000000, 0.9659258262890683122, 1.000000000000000000, 0.9659258262890683122, 1.000000000000000000, 0.9659258262890683122, 1.000000000000000000, 0.9659258262890683122, 1.000000000000000000, 0.9659258262890683122, 1.000000000000000000, 0.9659258262890683122, 1.000000000000000000, 0.9659258262890683122, 1.000000000000000000, 0.9659258262890683122, 1.000000000000000000, 0.9659258262890683122, 1.000000000000000000, 0.9659258262890683122, 1.000000000000000000, 0.9659258262890683122, 1.000000000000000000, 0.9659258262890683122, 1.000000000000000000, 0.9659258262890683122, 1.000000000000000000, 0.9659258262890683122, 1.000000000000000000, 0.9659258262890683122, 1.000000000000000000, 0.9659258262890683122, 1.000000000000000000, 0.9659258262890683122, 1.000000000000000000, 0.9659258262890683122, 1.000000000000000000, 0.9659258262890683122, 1.000000000000000000, 0.9659258262890683122, 1.000000000000000000, 0.9659258262890683122, 1.000000000000000000, 0.9659258262890683122, 1.000000000000000000, 0.9659258262890683122, 1.000000000000000000, 0.9659258262890683122, 1.000000000000000000, 0.9659258262890683122, 1.000000000000000000, 0.9659258262890683122, 1.000000000000000000, 0.9659258262890683122, 1.000000000000000000, 0.9659258262890683122, 1.000000000000000000, 0.9659258262890683122, 1.000000000000000000, 0.9659258262890683122, 1.000000000000000000, 0.9659258262890683122, 1.000000000000000000, 0.9659258262890683122, 1.000000000000000000, 0.9659258262890683122, 1.000000000000000000, 0.9659258262890683122, 1.000000000000000000, 0.9659258262890683122, 1.000000000000000000, 0.9659258262890683122, 1.000000000000000000, 0.9659258262890683122, 1.000000000000000000, 0.9659258262890683122, 1.000000000000000000, 0.9659258262890683122, 1.000000000000000000, 0.9659258262890683122, 1.000000000000000000, 0.9659258262890683122, 1.000000000000000000, 0.9659258262890683122, 1.000000000000000000, 0.9659258262890683122, 1.000000000000000000, 0.9659258262890683122, 1.000000000000000000, 0.9659258262890683122, 1.000000000000000000, 0.9659258262890683122, 1.000000000000000000, 0.9659258262890683122, 1.000000000000000000, 0.9659258262890683122, 1.000000000000000000, 0.9659258262890683122, 1.000000000000000000, 0.9659258262890683122, 1.000000000000000000, 0.9659258262890683122, 1.000000000000000000, 0.9659258262890683122, 1.000000000000000000, 0.9659258262890683122, 1.000000000000000000, 0.9659258262890683122, 1.000000000000000000, 0.9659258262890683122, 1.000000000000000000, 0.9659258262890683122, 1.000000000000000000, 0.9659258262890683122, 1.000000000000000000, 0.9659258262890683122, 1.000000000000000000, 0.9659258262890683122, 1.000000000000000000, 0.9659258262890683122, 1.000000000000000000, 0.9659258262890683122, 1.000000000000000000, 0.9659258262890683122, 1.000000000000000000, 0.9659258262890683122, 1.000000000000000000, 0.9659258262890683122, 1.000000000000000000, 0.9659258262890683122, 1.000000000000000000, 0.9659258262890683122, 1.000000000000000000, 0.9659258262890683122, 1.000000000000000000, 0.9659258262890683122, 1.000000000000000000, 0.9659258262890683122, 1.000000000000000000, 0.9659258262890683122, 1.000000000000000000, 0.9659258262890683122, 1.000000000000000000, 0.9659258262890683122, 1.000000000000000000, 0.9659258262890683122, 1.000000000000000000, 0.9659258262890683122, 1.000000000000000000, 0.9659258262890683122, 1.000000000000000000, 0.9659258262890683122, 1.000000000000000000, 0.9659258262890683122, 1.000000000000000000, 0.9659258262890683122, 1.000000000000000000, 0.9659258262890683122, 1.000000000000000000, 0.9659258262890683122, 1.000000000000000000, 0.9659258262890683122, 1.000000000000000000, 0.9659258262890683122, 1.000000000000000000, 0.9659258262890683122, 1.000000000000000000, 0.9659258262890683122, 1.000000000000000000, 0.9659258262890683122, 1.000000000000000000, 0.9659258262890683122, 1.000000000000000000, 0.9659258262890683122, 1.000000000000000000, 0.9659258262890683122, 1.000000000000000000, 0.9659258262890683122, 1.000000000000000000, 0.9659258262890683122, 1.000000000000000000, 0.9659258262890683122, 1.000000000000000000, 0.9659258262890683122, 1.000000000000000000, 0.9659258262890683122, 1.000000000000000000, 0.9659258262890683122, 1.000000000000000000, 0.9659258262890683122, 1.000000000000000000, 0.9659258262890683122, 1.000000000000000000, 0.9659258262890683122, 1.000000000000000000, 0.9659258262890683122, 1.000000000000000000, 0.9659258262890683122, 1.000000000000000000, 0.9659258262890683122, 1.000000000000000000, 0.9659258262890683122, 1.000000000000000000, 0.9659258262890683122, 1.000000000000000000, 0.9659258262890683122, 1.000000000000000000, 0.9659258262890683122, 1.000000000000000000, 0.9659258262890683122, 1.000000000000000000, 0.9659258262890683122, 1.000000000000000000, 0.9659258262890683122, 1.000000000000000000, 0.9659258262890683122, 1.000000000000000000, 0.9659258262890683122, 1.000000000000000000, 0.9659258262890683122, 1.000000000000000000, 0.9659258262890683122, 1.000000000000000000, 0.9659258262890683122, 1.000000000000000000, 0.9659258262890683122, 1.000000000000000000, 0.9659258262890683122, 1.000000000000000000, 0.9659258262890683122, 1.000000000000000000, 0.9659258262890683122, 1.000000000000000000, 0.9659258262890683122, 1.000000000000000000, 0.9659258262890683122, 1.000000000000000000, 0.9659258262890683122, 1.000000000000000000, 0.9659258262890683122, 1.000000000000000000, 0.9659258262890683122, 1.000000000000000000, 0.9659258262890683122, 1.000000000000000000, 0.9659258262890683122, 1.000000000000000000, 0.9659258262890683122, 1.000000000000000000, 0.9659258262890683122, 1.000000000000000000, 0.9659258262890683122, 1.000000000000000000, 0.9659258262890683122, 1.000000000000000000, 0.9659258262890683122, 1.000000000000000000, 0.9659258262890683122, 1.000000000000000000, 0.9659258262890683122, 1.000000000000000000, 0.9659258262890683122, 1.000000000000000000, 0.9659258262890683122, 1.000000000000000000, 0.9659258262890683122, 1.000000000000000000, 0.9659258262890683122, 1.000000000000000000, 0.9659258262890683122, 1.000000000000000000, 0.9659258262890683122, 1.000000000000000000, 0.9659258262890683122, 1.000000000000000000, 0.9659258262890683122, 1.000000000000000000, 0.9659258262890683122, 1.000000000000000000, 0.9659258262890683122, 1.000000000000000000, 0.9659258262890683122, 1.000000000000000000, 0.9659258262890683122, 1.000000000000000000, 0.9659258262890683122, 1.000000000000000000, 0.9659258262890683122, 1.000000000000000000, 0.9659258262890683122, 1.000000000000000000, 0.9659258262890683122, 1.000000000000000000, 0.9659258262890683122, 1.000000000000000000, 0.9659258262890683122, 1.000000000000000000, 0.9659258262890683122, 1.000000000000000000, 0.9659258262890683122, 1.000000000000000000, 0.9659258262890683122, 1.000000000000000000, 0.9659258262890683122, 1.000000000000000000, 0.9659258262890683122, 1.000000000000000000, 0.9659258262890683122, 1.000000000000000000, 0.9659258262890683122, 1.000000000000000000, 0.9659258262890683122, 1.000000000000000000, 0.9659258262890683122, 1.000000000000000000, 0.9659258262890683122, 1.000000000000000000, 0.9659258262890683122, 1.000000000000000000, 0.9659258262890683122, 1.000000000000000000, 0.9659258262890683122, 1.000000000000000000, 0.9659258262890683122, 1.000000000000000000, 0.9659258262890683122, 1.000000000000000000, 0.9659258262890683122, 1.000000000000000000, 0.9659258262890683122, 1.000000000000000000, 0.9659258262890683122, 1.000000000000000000, 0.9659258262890683122, 1.000000000000000000, 0.9659258262890683122, 1.000000000000000000, 0.9659258262890683122, 1.000000000000000000, 0.9659258262890683122, 1.000000000000000000, 0.9659258262890683122, 1.000000000000000000, 0.9659258262890683122, 1.000000000000000000, 0.9659258262890683122, 1.000000000000000000, 0.9659258262890683122, 1.000000000000000000, 0.9659258262890683122, 1.000000000000000000, 0.9659258262890683122, 1.000000000000000000, 0.9659258262890683122, 1.000000000000000000, 0.9659258262890683122, 1.000000000000000000, 0.9659258262890683122, 1.000000000000000000, 0.9659258262890683122, 1.000000000000000000, 0.9659258262890683122, 1.000000000000000000, 0.9659258262890683122, 1.000000000000000000, 0.9659258262890683122, 1.000000000000000000, 0.9659258262890683122, 1.000000000000000000, 0.9659258262890683122, 1.000000000000000000, 0.9659258262890683122, 1.000000000000000000, 0.9659258262890683122, 1.000000000000000000, 0.9659258262890683122, 1.000000000000000000, 0.9659258262890683122, 1.000000000000000000, 0.9659258262890683122, 1.000000000000000000, 0.9659258262890683122, 1.000000000000000000, 0.9659258262890683122, 1.000000000000000000, 0.9659258262890683122, 1.000000000000000000, 0.9659258262890683122, 1.000000000000000000, 0.9659258262890683122, 1.000000000000000000, 0.9659258262890683122, 1.000000000000000000, 0.9659258262890683122, 1.000000000000000000, 0.9659258262890683122, 1.000000000000000000, 0.9659258262890683122, 1.000000000000000000, 0.9659258262890683122, 1.000000000000000000, 0.9659258262890683122, 1.000000000000000000, 0.9659258262890683122, 1.000000000000000000, 0.9659258262890683122, 1.000000000000000000, 0.9659258262890683122, 1.000000000000000000, 0.9659258262890683122, 1.000000000000000000, 0.9659258262890683122, 1.000000000000000000, 0.9659258262890683122, 1.000000000000000000, 0.9659258262890683122, 1.000000000000000000, 0.9659258262890683122, 1.000000000000000000, 0.9659258262890683122, 1.000000000000000000, 0.9659258262890683122, 1.000000000000000000, 0.9659258262890683122, 1.000000000000000000, 0.9659258262890683122, 1.000000000000000000, 0.9659258262890683122, 1.000000000000000000, 0.9659258262890683122, 1.000000000000000000, 0.9659258262890683122, 1.000000000000000000, 0.9659258262890683122, 1.000000000000000000, 0.9659258262890683122, 1.000000000000000000, 0.9659258262890683122, 1.000000000000000000, 0.9659258262890683122, 1.000000000000000000, 0.9659258262890683122, 1.000000000000000000, 0.9659258262890683122, 1.000000000000000000, 0.9659258262890683122, 1.000000000000000000, 0.9659258262890683122, 1.000000000000000000, 0.9659258262890683122, 1.000000000000000000, 0.9659258262890683122, 1.000000000000000000, 0.9659258262890683122, 1.000000000000000000, 0.9659258262890683122, 1.000000000000000000, 0.9659258262890683122, 1.000000000000000000, 0.9659258262890683122, 1.000000000000000000, 0.9659258262890683122, 1.000000000000000000, 0.9659258262890683122, 1.000000000000000000, 0.9659258262890683122, 1.000000000000000000, 0.9659258262890683122, 1.000000000000000000, 0.9659258262890683122, 1.000000000000000000, 0.9659258262890683122, 1.000000000000000000, 0.9659258262890683122, 1.000000000000000000, 0.9659258262890683122, 1.000000000000000000, 0.9659258262890683122, 1.000000000000000000, 0.9659258262890683122, 1.000000000000000000, 0.9659258262890683122, 1.000000000000000000, 0.9659258262890683122, 1.000000000000000000, 0.9659258262890683122, 1.000000000000000000, 0.9659258262890683122, 1.000000000000000000, 0.9659258262890683122, 1.000000000000000000, 0.9659258262890683122, 1.000000000000000000, 0.9659258262890683122, 1.000000000000000000, 0.9659258262890683122, 1.000000000000000000, 0.9659258262890683122, 1.000000000000000000, 0.9659258262890683122, 1.000000000000000000, 0.9659258262890683122, 1.000000000000000000, 0.9659258262890683122, 1.000000000000000000, 0.9659258262890683122, 1.000000000000000000, 0.9659258262890683122, 1.000000000000000000, 0.9659258262890683122, 1.000000000000000000, 0.9659258262890683122, 1.000000000000000000, 0.9659258262890683122, 1.000000000000000000, 0.9659258262890683122, 1.000000000000000000, 0.9659258262890683122, 1.000000000000000000, 0.9659258262890683122, 1.000000000000000000, 0.9659258262890683122, 1.000000000000000000, 0.9659258262890683122, 1.000000000000000000, 0.9659258262890683122, 1.000000000000000000, 0.9659258262890683122, 1.000000000000000000, 0.9659258262890683122, 1.000000000000000000, 0.9659258262890683122, 1.000000000000000000, 0.9659258262890683122, 1.000000000000000000, 0.9659258262890683122, 1.000000000000000000, 0.9659258262890683122, 1.000000000000000000, 0.9659258262890683122, 1.000000000000000000, 0.9659258262890683122, 1.000000000000000000, 0.9659258262890683122, 1.000000000000000000, 0.9659258262890683122, 1.000000000000000000, 0.9821255365837726625, 0.9830040703864066920 ) ) 
 REPRESENTATION_ITEM ( '' )  );
#13456=CARTESIAN_POINT ( 'NONE',  ( -5.676582343750006032, 104.4270833299193555, 9.832129032723418760 ) ) ;
#13465=CARTESIAN_POINT ( 'NONE',  ( -11.35316468750000141, 208.2812499965860411, -1.390361679473963753E-15 ) ) ;
#13470=CARTESIAN_POINT ( 'NONE',  ( -3.042071309553164404, 192.5520833299193271, -11.35316468749999963 ) ) ;
#13477=CARTESIAN_POINT ( 'NONE',  ( 6.951808397369818766E-16, 77.03124999658601268, -11.35316468750000141 ) ) ;
#13483=CARTESIAN_POINT ( 'NONE',  ( -9.832129032723420536, 73.69791666325268409, 5.676582343749997150 ) ) ;
#13488=CARTESIAN_POINT ( 'NONE',  ( 8.660254037844415720, 75.41666666666669983, -5.000000000000016875 ) ) ;
#13490=CARTESIAN_POINT ( 'NONE',  ( 11.35316468750000141, 70.78124999658602690, 0.000000000000000000 ) ) ;
#13493=CARTESIAN_POINT ( 'NONE',  ( 10.00000000000000178, 171.8749999931720538, 0.000000000000000000 ) ) ;
#13495=AXIS2_PLACEMENT_3D ( 'NONE', #5495, #62083, #10406 ) ;
#13497=CARTESIAN_POINT ( 'NONE',  ( 8.311093377946837890, 66.71874999658601268, -8.311093377946837890 ) ) ;
#13499=CARTESIAN_POINT ( 'NONE',  ( 11.35316468750000141, 200.7812499965860411, 0.000000000000000000 ) ) ;
#13502=CARTESIAN_POINT ( 'NONE',  ( 7.320508075688774596, 62.49999999317203248, -7.320508075688774596 ) ) ;
#13504=CARTESIAN_POINT ( 'NONE',  ( 3.042071309553167513, 191.8229166632526699, -11.35316468749999785 ) ) ;
#13508=CARTESIAN_POINT ( 'NONE',  ( -9.832129032723418760, 178.1770833299193555, -5.676582343750004256 ) ) ;
#13516=CARTESIAN_POINT ( 'NONE',  ( -7.320508075688778149, 3.125000000000000444, 7.320508075688769267 ) ) ;
#13538=CARTESIAN_POINT ( 'NONE',  ( 2.765530957082001251, 294.9218750017070647, 6.676582343749999815 ) ) ;
#13539=CARTESIAN_POINT ( 'NONE',  ( 10.00000000000000000, 149.7916666666666856, 2.679491924311236062 ) ) ;
#13550=CARTESIAN_POINT ( 'NONE',  ( 0.000000000000000000, 300.0000000000000000, 0.000000000000000000 ) ) ;
#13558=CARTESIAN_POINT ( 'NONE',  ( 9.832129032723416984, 25.36458332991935194, 5.676582343750006032 ) ) ;
#13559=CARTESIAN_POINT ( 'NONE',  ( 5.000000000000003553, 150.8333333333333428, -8.660254037844390851 ) ) ;
#13560=CARTESIAN_POINT ( 'NONE',  ( -5.000000000000005329, 10.20833332650536640, 8.660254037844387298 ) ) ;
#13564=CARTESIAN_POINT ( 'NONE',  ( -2.679491924311382611, 130.4166666598386541, 9.999999999999914735 ) ) ;
#13567=CARTESIAN_POINT ( 'NONE',  ( 6.951808397369818766E-16, 32.03124999658601268, -11.35316468750000141 ) ) ;
#13570=CARTESIAN_POINT ( 'NONE',  ( -3.673940397442060854E-16, 298.7500000000000000, -6.000000000000001776 ) ) ;
#13571=CARTESIAN_POINT ( 'NONE',  ( -1.836970198721029983E-15, 175.6249999931720538, 10.00000000000000178 ) ) ;
#13573=CARTESIAN_POINT ( 'NONE',  ( 6.951808397369818766E-16, 37.03124999658601979, -11.35316468750000141 ) ) ;
#13575=CARTESIAN_POINT ( 'NONE',  ( -9.832129032723420536, 153.6979166632526983, 5.676582343749997150 ) ) ;
#13577=ADVANCED_FACE ( 'NONE', ( #38046 ), #59566, .T. ) ;
#13578=CARTESIAN_POINT ( 'NONE',  ( 5.000000000000001776, 122.7083333265053682, -8.660254037844389075 ) ) ;
#13580=LINE ( 'NONE', #36617, #54170 ) ;
#13584=CARTESIAN_POINT ( 'NONE',  ( 8.311093377946837890, 26.71874999658601624, -8.311093377946837890 ) ) ;
#13585=ADVANCED_FACE ( 'NONE', ( #66330 ), #65482, .F. ) ;
#13590=CARTESIAN_POINT ( 'NONE',  ( -11.35316468749999785, 153.0729166632526983, -3.042071309553167957 ) ) ;
#13598=CARTESIAN_POINT ( 'NONE',  ( -1.836970198721029983E-15, 205.6249999931720538, 10.00000000000000178 ) ) ;
#13600=CARTESIAN_POINT ( 'NONE',  ( 9.832129032723420536, 106.5104166632526841, -5.676582343749999815 ) ) ;
#13614=EDGE_CURVE ( 'NONE', #28203, #38699, #37049, .T. ) ;
#13633=CARTESIAN_POINT ( 'NONE',  ( -1.836970198721029983E-15, 98.75000000000000000, 10.00000000000000178 ) ) ;
#13635=CARTESIAN_POINT ( 'NONE',  ( -4.721056650415999201, 294.4843750017070079, -4.721056650415999201 ) ) ;
#13641=LINE ( 'NONE', #52922, #14188 ) ;
#13645=CARTESIAN_POINT ( 'NONE',  ( 10.00000000000000178, 210.2083333333333428, -2.679491924311226736 ) ) ;
#13647=CARTESIAN_POINT ( 'NONE',  ( -2.085542519210945728E-15, 194.8437499965860127, 11.35316468750000141 ) ) ;
#13654=CARTESIAN_POINT ( 'NONE',  ( -3.042071309553173730, 54.63541666325268409, 11.35316468749999785 ) ) ;
#13656=CARTESIAN_POINT ( 'NONE',  ( -11.35316468750000141, 223.8020833299192986, 3.042071309553159963 ) ) ;
#13661=CARTESIAN_POINT ( 'NONE',  ( 11.35316468749999963, 110.9895833299193697, -3.042071309553165293 ) ) ;
#13662=ADVANCED_FACE ( 'NONE', ( #34205 ), #16813, .T. ) ;
#13663=CARTESIAN_POINT ( 'NONE',  ( -4.999999999999998224, 73.54166665983869677, -8.660254037844389075 ) ) ;
#13671=CARTESIAN_POINT ( 'NONE',  ( -4.088227598258586603E-16, 295.3593750017070079, -6.676582343750001591 ) ) ;
#13673=CARTESIAN_POINT ( 'NONE',  ( 9.832129032723416984, 170.3645833299193555, 5.676582343750006032 ) ) ;
#13676=CARTESIAN_POINT ( 'NONE',  ( 1.332431167089188095E-11, 191.2499999999989768, -10.00000000000000533 ) ) ;
#13680=CARTESIAN_POINT ( 'NONE',  ( 9.832129032723416984, 135.6770833299193555, 5.676582343750006032 ) ) ;
#13684=CARTESIAN_POINT ( 'NONE',  ( -5.676582343750006032, 59.42708332991934839, 9.832129032723418760 ) ) ;
#13691=CARTESIAN_POINT ( 'NONE',  ( 4.242640687119285658, 290.6875000034139589, -4.242640687119286547 ) ) ;
#13698=EDGE_LOOP ( 'NONE', ( #14194, #2790, #28031, #21190, #20057 ) ) ;
#13713=CARTESIAN_POINT ( 'NONE',  ( -10.00000000000000178, 57.50000000000000000, -1.224646799147353454E-15 ) ) ;
#13716=CARTESIAN_POINT ( 'NONE',  ( 1.102182119232618108E-15, 298.2500000000000000, 6.000000000000001776 ) ) ;
#13719=ORIENTED_EDGE ( 'NONE', *, *, #34980, .T. ) ;
#13722=CARTESIAN_POINT ( 'NONE',  ( 10.00000000000000178, 0.000000000000000000, 0.000000000000000000 ) ) ;
#13726=CARTESIAN_POINT ( 'NONE',  ( -5.000000000000005329, 173.3333333333333428, 8.660254037844387298 ) ) ;
#13730=CARTESIAN_POINT ( 'NONE',  ( -9.832129032723418760, 138.1770833299193555, -5.676582343750004256 ) ) ;
#13731=CARTESIAN_POINT ( 'NONE',  ( -3.673940397442060854E-16, 294.8125000034140157, -6.000000000000001776 ) ) ;
#13732=CARTESIAN_POINT ( 'NONE',  ( 8.660254037844385522, 26.45833332650536818, 5.000000000000005329 ) ) ;
#13734=CARTESIAN_POINT ( 'NONE',  ( 2.679491924311222739, 105.8333333265053540, 10.00000000000000355 ) ) ;
#13737=CARTESIAN_POINT ( 'NONE',  ( 9.832129032723420536, 11.51041666325268409, -5.676582343749999815 ) ) ;
#13744=CARTESIAN_POINT ( 'NONE',  ( -10.00000000000000355, 29.58333332650536818, 2.679491924311223183 ) ) ;
#13752=CARTESIAN_POINT ( 'NONE',  ( 10.00000000000000711, 30.00000000000000711, 0.000000000000000000 ) ) ;
#13753=CARTESIAN_POINT ( 'NONE',  ( -2.679491924324933105, 61.45833333333461468, -9.999999999992150279 ) ) ;
#13755=CARTESIAN_POINT ( 'NONE',  ( -9.832129032723418760, 127.8645833299193697, -5.676582343750004256 ) ) ;
#13761=CARTESIAN_POINT ( 'NONE',  ( -1.836970198721029983E-15, 130.6249999931720254, 10.00000000000000178 ) ) ;
#13762=CARTESIAN_POINT ( 'NONE',  ( 5.000000000000006217, 44.16666666666667851, 8.660254037844412167 ) ) ;
#13763=CARTESIAN_POINT ( 'NONE',  ( -5.676582343749998039, 117.4479166632526841, -9.832129032723420536 ) ) ;
#13767=CARTESIAN_POINT ( 'NONE',  ( 6.123233995736767268E-16, 213.1249999931720538, -10.00000000000000178 ) ) ;
#13770=CARTESIAN_POINT ( 'NONE',  ( 5.676582343749993598, 95.26041666325268409, 9.832129032723422313 ) ) ;
#13774=CARTESIAN_POINT ( 'NONE',  ( -9.832129032723420536, 4.010416663252683200, 5.676582343749997150 ) ) ;
#13781=CARTESIAN_POINT ( 'NONE',  ( -8.660254037844387298, 148.9583333265053682, -5.000000000000004441 ) ) ;
#13782=CARTESIAN_POINT ( 'NONE',  ( 6.676582343750004256, 290.8906250017069510, 2.765530957081995478 ) ) ;
#13787=ADVANCED_FACE ( 'NONE', ( #33463 ), #5522, .T. ) ;
#13788=CARTESIAN_POINT ( 'NONE',  ( 3.042071309553167069, 127.1354166632526699, -11.35316468749999785 ) ) ;
#13793=ORIENTED_EDGE ( 'NONE', *, *, #66704, .F. ) ;
#13804=DIRECTION ( 'NONE',  ( -0.000000000000000000, 1.000000000000000000, -0.000000000000000000 ) ) ;
#13806=CARTESIAN_POINT ( 'NONE',  ( 0.4589999999999999636, 255.7199999999997715, 5.818592113973279467 ) ) ;
#13807=CARTESIAN_POINT ( 'NONE',  ( 4.721056650416000089, 291.8281250017069510, 4.721056650415999201 ) ) ;
#13809=CARTESIAN_POINT ( 'NONE',  ( 2.679491924311228956, 137.9166666598387110, -10.00000000000000000 ) ) ;
#13816=ORIENTED_EDGE ( 'NONE', *, *, #57548, .T. ) ;
#13819=CARTESIAN_POINT ( 'NONE',  ( -3.042071309553164404, 102.5520833299193555, -11.35316468749999963 ) ) ;
#13825=ORIENTED_EDGE ( 'NONE', *, *, #18214, .T. ) ;
#13826=CARTESIAN_POINT ( 'NONE',  ( 5.676582343750001591, 216.6145833299193555, -9.832129032723420536 ) ) ;
#13830=CARTESIAN_POINT ( 'NONE',  ( -3.042071309553173730, 199.6354166632526699, 11.35316468749999785 ) ) ;
#13838=CARTESIAN_POINT ( 'NONE',  ( 6.951808397369818766E-16, 87.03124999658602690, -11.35316468750000141 ) ) ;
#13844=CARTESIAN_POINT ( 'NONE',  ( 5.676582343749993598, 74.94791666325269830, 9.832129032723422313 ) ) ;
#13845=EDGE_LOOP ( 'NONE', ( #35994, #65228, #9237, #72271 ) ) ;
#13851=CARTESIAN_POINT ( 'NONE',  ( -9.832129032723418760, 72.86458332991935549, -5.676582343750004256 ) ) ;
#13855=CARTESIAN_POINT ( 'NONE',  ( 10.00000000000000178, 172.0833333265053398, -2.679491924311226736 ) ) ;
#13860=CARTESIAN_POINT ( 'NONE',  ( -9.832129032723420536, 64.01041666325268409, 5.676582343749997150 ) ) ;
#13862=CARTESIAN_POINT ( 'NONE',  ( 11.35316468749999785, 195.5729166632526983, 3.042071309553174174 ) ) ;
#13863=VERTEX_POINT ( 'NONE', #68145 ) ;
#13868=CARTESIAN_POINT ( 'NONE',  ( -11.35316468750000141, 193.4895833299193271, 3.042071309553159963 ) ) ;
#13869=CARTESIAN_POINT ( 'NONE',  ( -8.660254037844387298, 193.9583333265053966, -5.000000000000004441 ) ) ;
#13873=CARTESIAN_POINT ( 'NONE',  ( -11.35316468750000141, 183.5937499965860411, -1.390361679473963753E-15 ) ) ;
#13882=CARTESIAN_POINT ( 'NONE',  ( 4.999999999999993783, 4.166666666666666963, 8.660254037844390851 ) ) ;
#13885=( BOUNDED_CURVE ( )  B_SPLINE_CURVE ( 2, ( #18293, #40189, #41309, #11522, #64317, #29249, #23207, #63948, #23577, #52261, #28866, #46219, #69236 ),
 .UNSPECIFIED., .F., .F. ) 
 B_SPLINE_CURVE_WITH_KNOTS ( ( 3, 2, 2, 2, 2, 2, 3 ),
 ( 0.1793478260869565133, 0.1811594202898550721, 0.1829710144927536308, 0.1847826086956521618, 0.1865942028985506929, 0.1884057971014492516, 0.1902173913043478104 ),
 .UNSPECIFIED. ) 
 CURVE ( )  GEOMETRIC_REPRESENTATION_ITEM ( )  RATIONAL_B_SPLINE_CURVE ( ( 1.000000000000000000, 0.9659258262890683122, 1.000000000000000000, 0.9659258262890683122, 1.000000000000000000, 0.9659258262890683122, 1.000000000000000000, 0.9659258262890683122, 1.000000000000000000, 0.9659258262890683122, 1.000000000000000000, 0.9659258262890688673, 0.9999999999999994449 ) ) 
 REPRESENTATION_ITEM ( '' )  );
#13903=CARTESIAN_POINT ( 'NONE',  ( 11.35316468749999785, 55.88541666325266988, 3.042071309553174174 ) ) ;
#13908=CARTESIAN_POINT ( 'NONE',  ( 2.765530957081996366, 295.2968750017070079, -6.676582343750002480 ) ) ;
#13909=CARTESIAN_POINT ( 'NONE',  ( -4.999999999999998224, 141.6666666666666572, -8.660254037844389075 ) ) ;
#13920=CARTESIAN_POINT ( 'NONE',  ( 4.999999999999995559, 134.1666666666666856, 8.660254037844392627 ) ) ;
#13924=CARTESIAN_POINT ( 'NONE',  ( -8.311093377946836114, 37.65624999658601979, -8.311093377946837890 ) ) ;
#13926=CARTESIAN_POINT ( 'NONE',  ( 6.123233995736767268E-16, 13.12499999317203425, -10.00000000000000178 ) ) ;
#13928=DIRECTION ( 'NONE',  ( -0.000000000000000000, 1.000000000000000000, -0.000000000000000000 ) ) ;
#13929=VERTEX_POINT ( 'NONE', #73801 ) ;
#13931=CARTESIAN_POINT ( 'NONE',  ( 11.35316468750000141, 35.78124999658601268, 0.000000000000000000 ) ) ;
#13937=CARTESIAN_POINT ( 'NONE',  ( -11.35316468750000141, 38.48958332991934839, 3.042071309553159963 ) ) ;
#13940=CARTESIAN_POINT ( 'NONE',  ( -11.35316468750000141, 163.4895833299193271, 3.042071309553159963 ) ) ;
#13941=CARTESIAN_POINT ( 'NONE',  ( 2.679491924311222739, 125.8333333265053682, 10.00000000000000355 ) ) ;
#13945=CARTESIAN_POINT ( 'NONE',  ( -5.676582343749998039, 27.76041666325268409, -9.832129032723420536 ) ) ;
#13950=CARTESIAN_POINT ( 'NONE',  ( 5.676582343750001591, 146.6145833299193555, -9.832129032723420536 ) ) ;
#13958=ORIENTED_EDGE ( 'NONE', *, *, #51032, .F. ) ;
#13960=LINE ( 'NONE', #53620, #67696 ) ;
#13961=CARTESIAN_POINT ( 'NONE',  ( 6.951808397369818766E-16, 97.34374999658601268, -11.35316468750000141 ) ) ;
#13964=VERTEX_POINT ( 'NONE', #62473 ) ;
#13982=CARTESIAN_POINT ( 'NONE',  ( 6.123233995736767268E-16, 223.1249999931720254, -10.00000000000000178 ) ) ;
#13994=CARTESIAN_POINT ( 'NONE',  ( 2.997893585525398702E-11, 31.24999999999767653, -10.00000000000000178 ) ) ;
#13995=CARTESIAN_POINT ( 'NONE',  ( -1.836970198721029983E-15, 113.7500000000000000, 10.00000000000000178 ) ) ;
#13999=CARTESIAN_POINT ( 'NONE',  ( 6.676582343750004256, 298.0468750017070647, 2.765530957081995478 ) ) ;
#14002=CARTESIAN_POINT ( 'NONE',  ( -4.999999999999998224, 143.5416666598386826, -8.660254037844389075 ) ) ;
#14012=CARTESIAN_POINT ( 'NONE',  ( 8.660254037844385522, 224.5833333333333712, 5.000000000000005329 ) ) ;
#14014=CARTESIAN_POINT ( 'NONE',  ( -11.35316468750000141, 198.5937499965860127, -1.390361679473963753E-15 ) ) ;
#14019=CARTESIAN_POINT ( 'NONE',  ( 2.485281374238175189, 297.6875000000000568, -6.000000000000396128 ) ) ;
#14022=CARTESIAN_POINT ( 'NONE',  ( 3.042071309553159519, 50.05208332991935549, 11.35316468750000141 ) ) ;
#14028=CARTESIAN_POINT ( 'NONE',  ( -4.999999999999998224, 58.54166665983870388, -8.660254037844389075 ) ) ;
#14030=CARTESIAN_POINT ( 'NONE',  ( 9.832129032723420536, 106.1979166632526983, -5.676582343749999815 ) ) ;
#14031=AXIS2_PLACEMENT_3D ( 'NONE', #59555, #26314, #7870 ) ;
#14032=CARTESIAN_POINT ( 'NONE',  ( -2.679491924311235618, 85.41666665983869677, 10.00000000000000000 ) ) ;
#14041=CARTESIAN_POINT ( 'NONE',  ( -6.676582343750001591, 295.6093750017069510, 0.000000000000000000 ) ) ;
#14044=CARTESIAN_POINT ( 'NONE',  ( 8.311093377946837890, 166.4062499965860127, -8.311093377946837890 ) ) ;
#14045=LINE ( 'NONE', #21583, #58611 ) ;
#14049=VERTEX_POINT ( 'NONE', #59066 ) ;
#14052=CARTESIAN_POINT ( 'NONE',  ( 11.35316468750000141, 136.0937499965860127, 0.000000000000000000 ) ) ;
#14057=CARTESIAN_POINT ( 'NONE',  ( -11.35316468750000141, 68.59374999658601268, -1.390361679473963753E-15 ) ) ;
#14059=CARTESIAN_POINT ( 'NONE',  ( -1.836970198721029983E-15, 28.75000000000000000, 10.00000000000000178 ) ) ;
#14065=FACE_OUTER_BOUND ( 'NONE', #29802, .T. ) ;
#14076=AXIS2_PLACEMENT_3D ( 'NONE', #47587, #47223, #31357 ) ;
#14086=CARTESIAN_POINT ( 'NONE',  ( -7.320508075688770155, 1.874999999999997780, -7.320508075688771044 ) ) ;
#14087=CARTESIAN_POINT ( 'NONE',  ( -7.320508075688773708, 201.8750000000000000, -7.320508075688774596 ) ) ;
#14090=CARTESIAN_POINT ( 'NONE',  ( -10.00000000000000178, 72.50000000000001421, -1.224646799147353454E-15 ) ) ;
#14092=CARTESIAN_POINT ( 'NONE',  ( -6.000000000000001776, 296.0000000000000000, 0.000000000000000000 ) ) ;
#14105=CARTESIAN_POINT ( 'NONE',  ( 4.999999999999993783, 179.1666666666666572, 8.660254037844390851 ) ) ;
#14108=CARTESIAN_POINT ( 'NONE',  ( 9.832129032723416984, 150.6770833299193555, 5.676582343750006032 ) ) ;
#14109=CARTESIAN_POINT ( 'NONE',  ( 1.102182119232618108E-15, 294.3125000034140157, 6.000000000000001776 ) ) ;
#14112=CARTESIAN_POINT ( 'NONE',  ( -4.999999999999998224, 83.54166665983869677, -8.660254037844389075 ) ) ;
#14115=CARTESIAN_POINT ( 'NONE',  ( 11.35316468750000141, 16.09374999658601979, 0.000000000000000000 ) ) ;
#14118=DIRECTION ( 'NONE',  ( -0.000000000000000000, -0.000000000000000000, 1.000000000000000000 ) ) ;
#14122=CARTESIAN_POINT ( 'NONE',  ( 7.320508075688774596, 47.49999999317203958, -7.320508075688774596 ) ) ;
#14128=CARTESIAN_POINT ( 'NONE',  ( 8.660254037844385522, 6.458333326505366401, 5.000000000000005329 ) ) ;
#14133=CARTESIAN_POINT ( 'NONE',  ( -11.35316468750000141, 133.4895833299193839, 3.042071309553159963 ) ) ;
#14137=CARTESIAN_POINT ( 'NONE',  ( 4.089761226760953328, 227.7900538254533558, -9.185780638600787640 ) ) ;
#14141=CARTESIAN_POINT ( 'NONE',  ( 8.311093377946834337, 115.1562499965859985, 8.311093377946839666 ) ) ;
#14144=CARTESIAN_POINT ( 'NONE',  ( 7.320508075688771044, 81.24999999317202537, 7.320508075688775484 ) ) ;
#14147=CARTESIAN_POINT ( 'NONE',  ( 1.224646799147353454E-15, 300.0000000000000000, -10.00000000000000178 ) ) ;
#14149=CARTESIAN_POINT ( 'NONE',  ( 5.676582343750001591, 106.9270833299193413, -9.832129032723420536 ) ) ;
#14155=CARTESIAN_POINT ( 'NONE',  ( -3.042071309553164404, 27.55208332991935194, -11.35316468749999963 ) ) ;
#14157=CARTESIAN_POINT ( 'NONE',  ( 6.123233995736767268E-16, 183.1249999931720538, -10.00000000000000178 ) ) ;
#14159=CARTESIAN_POINT ( 'NONE',  ( -1.836970198721029983E-15, 115.6249999931720396, 10.00000000000000178 ) ) ;
#14163=CARTESIAN_POINT ( 'NONE',  ( 6.676582343750004256, 292.8906250017068942, 2.765530957081995478 ) ) ;
#14165=CARTESIAN_POINT ( 'NONE',  ( 11.35316468749999963, 221.3020833299193271, -3.042071309553165293 ) ) ;
#14166=CARTESIAN_POINT ( 'NONE',  ( 8.311093377946837890, 126.7187499965860269, -8.311093377946837890 ) ) ;
#14172=VERTEX_POINT ( 'NONE', #19788 ) ;
#14181=FACE_OUTER_BOUND ( 'NONE', #7708, .T. ) ;
#14183=CARTESIAN_POINT ( 'NONE',  ( 1.377000000000000002, 278.5679999999998699, 5.673918265505059289 ) ) ;
#14184=CARTESIAN_POINT ( 'NONE',  ( 6.676582343750002480, 294.0156250017068942, -2.765530957081997254 ) ) ;
#14185=CARTESIAN_POINT ( 'NONE',  ( 10.00000000000000178, 131.8749999931720254, 0.000000000000000000 ) ) ;
#14186=CARTESIAN_POINT ( 'NONE',  ( 5.000000000000001776, 137.7083333265053682, -8.660254037844389075 ) ) ;
#14188=VECTOR ( 'NONE', #65704, 1000.000000000000000 ) ;
#14194=ORIENTED_EDGE ( 'NONE', *, *, #74053, .T. ) ;
#14197=CARTESIAN_POINT ( 'NONE',  ( -9.832129032723418760, 113.1770833299193555, -5.676582343750004256 ) ) ;
#14198=CARTESIAN_POINT ( 'NONE',  ( 4.999999999999993783, 211.0416666598387110, 8.660254037844390851 ) ) ;
#14205=CARTESIAN_POINT ( 'NONE',  ( 4.242640687119285658, 287.6875000034139589, -4.242640687119286547 ) ) ;
#14210=CARTESIAN_POINT ( 'NONE',  ( 5.676582343750001591, 191.9270833299193555, -9.832129032723420536 ) ) ;
#14217=CARTESIAN_POINT ( 'NONE',  ( 3.042071309553159519, 84.73958332991936970, 11.35316468750000141 ) ) ;
#14222=CARTESIAN_POINT ( 'NONE',  ( -5.676582343750006032, 94.11458332991935549, 9.832129032723418760 ) ) ;
#14229=CARTESIAN_POINT ( 'NONE',  ( 8.311093377946837890, 71.40624999658602690, -8.311093377946837890 ) ) ;
#14232=ADVANCED_FACE ( 'NONE', ( #20530 ), #9227, .T. ) ;
#14235=CARTESIAN_POINT ( 'NONE',  ( -2.679491924311235618, 175.4166666598387110, 10.00000000000000000 ) ) ;
#14239=CARTESIAN_POINT ( 'NONE',  ( -11.35316468749999785, 68.38541666325268409, -3.042071309553167957 ) ) ;
#14240=CARTESIAN_POINT ( 'NONE',  ( -2.765530957081996810, 292.2656250017069510, -6.676582343750003368 ) ) ;
#14244=CARTESIAN_POINT ( 'NONE',  ( 6.951808397369818766E-16, 212.0312499965860411, -11.35316468750000141 ) ) ;
#14250=CARTESIAN_POINT ( 'NONE',  ( -3.042071309553163960, 197.2395833299193555, -11.35316468749999963 ) ) ;
#14252=AXIS2_PLACEMENT_3D ( 'NONE', #50497, #68600, #16908 ) ;
#14256=CARTESIAN_POINT ( 'NONE',  ( -9.832129032723420536, 184.0104166632526983, 5.676582343749997150 ) ) ;
#14259=ORIENTED_EDGE ( 'NONE', *, *, #36582, .T. ) ;
#14261=CARTESIAN_POINT ( 'NONE',  ( -7.320508075688773708, 6.874999999999999112, -7.320508075688774596 ) ) ;
#14276=VERTEX_POINT ( 'NONE', #31865 ) ;
#14279=CARTESIAN_POINT ( 'NONE',  ( -3.042071309553164404, 62.55208332991934839, -11.35316468749999963 ) ) ;
#14280=CARTESIAN_POINT ( 'NONE',  ( -8.660254037844387298, 113.9583333265053682, -5.000000000000004441 ) ) ;
#14284=CARTESIAN_POINT ( 'NONE',  ( -6.676582343750002480, 293.5468750017070079, -2.765530957081996810 ) ) ;
#14285=CARTESIAN_POINT ( 'NONE',  ( 10.00000000000000000, 144.7916666666666572, 2.679491924311236062 ) ) ;
#14289=AXIS2_PLACEMENT_3D ( 'NONE', #33371, #56372, #4692 ) ;
#14298=CARTESIAN_POINT ( 'NONE',  ( -2.679491924313885054, 133.5416666666664298, 9.999999999998470557 ) ) ;
#14303=CARTESIAN_POINT ( 'NONE',  ( -9.832129032723420536, 43.69791666325269119, 5.676582343749997150 ) ) ;
#14304=CARTESIAN_POINT ( 'NONE',  ( 3.490152628695403868E-12, 151.2499999999997442, -10.00000000000000178 ) ) ;
#14305=CARTESIAN_POINT ( 'NONE',  ( 7.320508075688774596, 7.499999993172031587, -7.320508075688774596 ) ) ;
#14309=EDGE_CURVE ( 'NONE', #67735, #47641, #14868, .T. ) ;
#14310=CARTESIAN_POINT ( 'NONE',  ( 11.35316468749999785, 45.57291666325266988, 3.042071309553174174 ) ) ;
#14316=CARTESIAN_POINT ( 'NONE',  ( -5.676582343750006032, 29.11458332991935194, 9.832129032723418760 ) ) ;
#14319=CARTESIAN_POINT ( 'NONE',  ( 3.042071309553159519, 159.7395833299193839, 11.35316468750000141 ) ) ;
#14321=B_SPLINE_SURFACE_WITH_KNOTS ( 'NONE', 5, 5, ( 
 ( #6704, #16889, #18390, #13806, #25508, #64774 ),
 ( #47781, #42496, #8543, #58762, #31181, #70802 ),
 ( #59134, #19481, #37220, #1430, #24769, #7072 ),
 ( #30078, #53096, #59495, #36481, #2142, #25136 ),
 ( #1784, #36112, #60218, #7808, #14183, #13077 ),
 ( #47048, #30810, #52725, #19116, #30450, #47418 ) ),
 .UNSPECIFIED., .F., .F., .F.,
 ( 6, 6 ),
 ( 6, 6 ),
 ( -14.28000000000008640, 14.28000000000005976 ),
 ( -2.294999999999999485, 2.295000000000000373 ),
 .UNSPECIFIED. ) ;
#14322=CARTESIAN_POINT ( 'NONE',  ( -10.00000000000000355, 129.5833333265053966, 2.679491924311223183 ) ) ;
#14324=ORIENTED_EDGE ( 'NONE', *, *, #3174, .T. ) ;
#14326=CARTESIAN_POINT ( 'NONE',  ( 11.35316468749999963, 16.30208332991935194, -3.042071309553165293 ) ) ;
#14328=CARTESIAN_POINT ( 'NONE',  ( -5.394762896564973355E-12, 18.74999999999958433, 10.00000000000000178 ) ) ;
#14334=CARTESIAN_POINT ( 'NONE',  ( -11.35316468749999785, 158.0729166632526699, -3.042071309553167957 ) ) ;
#14345=CARTESIAN_POINT ( 'NONE',  ( -8.311093377946841443, 109.2187499965860269, 8.311093377946830785 ) ) ;
#14347=( BOUNDED_CURVE ( )  B_SPLINE_CURVE ( 2, ( #65061, #59061, #19783, #31104, #35676, #13372, #37145, #30011, #58691, #42791, #2073, #7000, #8101 ),
 .UNSPECIFIED., .F., .F. ) 
 B_SPLINE_CURVE_WITH_KNOTS ( ( 3, 2, 2, 2, 2, 2, 3 ),
 ( 2.088085437352556362, 2.093319447082276685, 2.098553456811997009, 2.103787466541717777, 2.109021476271438100, 2.114255486001158424, 2.119489495730878748 ),
 .UNSPECIFIED. ) 
 CURVE ( )  GEOMETRIC_REPRESENTATION_ITEM ( )  RATIONAL_B_SPLINE_CURVE ( ( 1.000000000000267342, 0.9659258262888009705, 1.000000000000000000, 0.9659258262890683122, 1.000000000000000000, 0.9659258262890683122, 1.000000000000000000, 0.9659258262890683122, 1.000000000000000000, 0.9659258262890683122, 1.000000000000000000, 0.9659258262890829672, 0.9999999999999853451 ) ) 
 REPRESENTATION_ITEM ( '' )  );
#14348=CARTESIAN_POINT ( 'NONE',  ( 7.320508075688778149, 14.37500000000000533, 7.320508075688781702 ) ) ;
#14349=ORIENTED_EDGE ( 'NONE', *, *, #40352, .F. ) ;
#14357=CARTESIAN_POINT ( 'NONE',  ( -4.999999999999998224, 158.5416666598387110, -8.660254037844389075 ) ) ;
#14366=CARTESIAN_POINT ( 'NONE',  ( -6.676582343749999815, 298.5156250017069510, 2.765530957082001251 ) ) ;
#14376=CARTESIAN_POINT ( 'NONE',  ( -7.320508075688778149, 103.1249999999999858, 7.320508075688769267 ) ) ;
#14379=CARTESIAN_POINT ( 'NONE',  ( 6.676582343750003368, 291.1718750017069510, -2.765530957081997254 ) ) ;
#14392=CARTESIAN_POINT ( 'NONE',  ( -24.05663304117221557, 228.2939914580040863, -18.33101321549810692 ) ) ;
#14394=CARTESIAN_POINT ( 'NONE',  ( 3.042071309553167069, 197.1354166632526415, -11.35316468749999785 ) ) ;
#14395=CARTESIAN_POINT ( 'NONE',  ( 10.00000000000000178, 192.0833333265053682, -2.679491924311226736 ) ) ;
#14401=VECTOR ( 'NONE', #26569, 1000.000000000000000 ) ;
#14411=CARTESIAN_POINT ( 'NONE',  ( 11.35316468749999963, 120.9895833299193413, -3.042071309553165293 ) ) ;
#14413=CARTESIAN_POINT ( 'NONE',  ( -2.679491924311235618, 90.41666665983869677, 10.00000000000000000 ) ) ;
#14419=ORIENTED_EDGE ( 'NONE', *, *, #30771, .F. ) ;
#14420=CARTESIAN_POINT ( 'NONE',  ( 2.765530957081996366, 294.2968750017070079, -6.676582343750003368 ) ) ;
#14422=CARTESIAN_POINT ( 'NONE',  ( -8.311093377946836114, 167.6562499965860411, -8.311093377946837890 ) ) ;
#14429=CARTESIAN_POINT ( 'NONE',  ( -11.35316468749999785, 153.3854166632526699, -3.042071309553167957 ) ) ;
#14433=CARTESIAN_POINT ( 'NONE',  ( -5.676582343750006032, 69.42708332991935549, 9.832129032723418760 ) ) ;
#14440=CARTESIAN_POINT ( 'NONE',  ( -6.000000000000000888, 288.1250000034140157, 2.485281374238575758 ) ) ;
#14449=ORIENTED_EDGE ( 'NONE', *, *, #39997, .T. ) ;
#14455=CARTESIAN_POINT ( 'NONE',  ( -2.485281374238268004, 290.1875000000000000, 6.000000000000304645 ) ) ;
#14458=CARTESIAN_POINT ( 'NONE',  ( 4.242640687119285658, 299.6250000000000000, -4.242640687119286547 ) ) ;
#14464=CARTESIAN_POINT ( 'NONE',  ( -4.999999999999998224, 66.66666666666667140, -8.660254037844389075 ) ) ;
#14466=CARTESIAN_POINT ( 'NONE',  ( -6.000000000000001776, 298.0000000000000000, 0.000000000000000000 ) ) ;
#14478=CARTESIAN_POINT ( 'NONE',  ( -8.660254037844387298, 182.0833333333333428, -5.000000000000004441 ) ) ;
#14481=CARTESIAN_POINT ( 'NONE',  ( -8.311093377946836114, 157.9687499965860127, -8.311093377946837890 ) ) ;
#14487=CARTESIAN_POINT ( 'NONE',  ( 8.311093377946837890, 11.71874999658601801, -8.311093377946837890 ) ) ;
#14488=CARTESIAN_POINT ( 'NONE',  ( 8.660254037844385522, 96.45833332650536818, 5.000000000000005329 ) ) ;
#14494=CARTESIAN_POINT ( 'NONE',  ( -10.00000000000000000, 54.16666665983869677, -2.679491924311229845 ) ) ;
#14499=DIRECTION ( 'NONE',  ( 0.000000000000000000, 0.000000000000000000, 1.000000000000000000 ) ) ;
#14500=CARTESIAN_POINT ( 'NONE',  ( 5.000000000000002665, 159.1666666666666856, 8.660254037844406838 ) ) ;
#14502=CARTESIAN_POINT ( 'NONE',  ( -3.673940397442060854E-16, 289.7500000000000000, -6.000000000000001776 ) ) ;
#14506=CARTESIAN_POINT ( 'NONE',  ( -11.35316468749999785, 133.0729166632526983, -3.042071309553167513 ) ) ;
#14515=CARTESIAN_POINT ( 'NONE',  ( 5.676582343749993598, 119.9479166632526841, 9.832129032723422313 ) ) ;
#14519=CARTESIAN_POINT ( 'NONE',  ( -10.00000000000000178, 24.37499999317203603, -1.224646799147353454E-15 ) ) ;
#14521=CARTESIAN_POINT ( 'NONE',  ( 9.832129032723416984, 110.6770833299193555, 5.676582343750006032 ) ) ;
#14526=CARTESIAN_POINT ( 'NONE',  ( -5.676582343750006032, 19.42708332991934839, 9.832129032723418760 ) ) ;
#14528=CARTESIAN_POINT ( 'NONE',  ( 2.679491924311222739, 180.8333333265053966, 10.00000000000000355 ) ) ;
#14532=CARTESIAN_POINT ( 'NONE',  ( 2.765530957081996366, 288.1406250017070647, -6.676582343750003368 ) ) ;
#14534=CIRCLE ( 'NONE', #21767, 15.99999999999998579 ) ;
#14536=CARTESIAN_POINT ( 'NONE',  ( 6.951808397369818766E-16, 137.3437499965860127, -11.35316468750000141 ) ) ;
#14543=VERTEX_POINT ( 'NONE', #11832 ) ;
#14555=CARTESIAN_POINT ( 'NONE',  ( 8.311093377946837890, 186.4062499965860411, -8.311093377946837890 ) ) ;
#14559=CARTESIAN_POINT ( 'NONE',  ( 6.676582343750003368, 290.8906250017069510, 2.765530957081995478 ) ) ;
#14562=CARTESIAN_POINT ( 'NONE',  ( -5.000000000000000000, 66.66666666666667140, -8.660254037844390851 ) ) ;
#14567=CARTESIAN_POINT ( 'NONE',  ( 5.000000000000001776, 167.7083333265053682, -8.660254037844389075 ) ) ;
#14570=ADVANCED_FACE ( 'NONE', ( #8292 ), #42983, .T. ) ;
#14571=DIRECTION ( 'NONE',  ( -0.000000000000000000, 1.000000000000000000, -0.000000000000000000 ) ) ;
#14574=CARTESIAN_POINT ( 'NONE',  ( 8.311093377946834337, 120.4687499965860269, 8.311093377946839666 ) ) ;
#14583=CARTESIAN_POINT ( 'NONE',  ( 5.676582343750001591, 221.6145833299193839, -9.832129032723420536 ) ) ;
#14586=CARTESIAN_POINT ( 'NONE',  ( -9.832129032723418760, 193.1770833299193555, -5.676582343750004256 ) ) ;
#14593=CARTESIAN_POINT ( 'NONE',  ( 9.832129032723420536, 81.19791666325269830, -5.676582343749999815 ) ) ;
#14601=CARTESIAN_POINT ( 'NONE',  ( 9.832129032723420536, 91.19791666325269830, -5.676582343749999815 ) ) ;
#14609=CARTESIAN_POINT ( 'NONE',  ( -2.085542519210945728E-15, 79.53124999658602690, 11.35316468750000141 ) ) ;
#14611=CARTESIAN_POINT ( 'NONE',  ( 6.123233995736767268E-16, 131.2500000000000000, -10.00000000000000178 ) ) ;
#14612=CARTESIAN_POINT ( 'NONE',  ( -7.320508075688773708, 163.7499999931720538, -7.320508075688774596 ) ) ;
#14615=CARTESIAN_POINT ( 'NONE',  ( 11.35316468749999785, 65.88541666325268409, 3.042071309553174174 ) ) ;
#14616=CARTESIAN_POINT ( 'NONE',  ( -4.721056650415998313, 292.5781250017069510, 4.721056650416000089 ) ) ;
#14618=CARTESIAN_POINT ( 'NONE',  ( 8.311093377946834337, 205.1562499965859843, 8.311093377946839666 ) ) ;
#14622=CARTESIAN_POINT ( 'NONE',  ( -6.000000000000001776, 288.0000000000000000, 0.000000000000000000 ) ) ;
#14624=CARTESIAN_POINT ( 'NONE',  ( -8.311093377946836114, 192.6562499965860127, -8.311093377946837890 ) ) ;
#14629=CARTESIAN_POINT ( 'NONE',  ( 9.832129032723416984, 185.6770833299193555, 5.676582343750006032 ) ) ;
#14633=ORIENTED_EDGE ( 'NONE', *, *, #68500, .T. ) ;
#14635=CARTESIAN_POINT ( 'NONE',  ( -10.00000000000000000, 2.291666666666666963, -2.679491924311229845 ) ) ;
#14651=ORIENTED_EDGE ( 'NONE', *, *, #65153, .T. ) ;
#14652=EDGE_CURVE ( 'NONE', #28748, #61990, #53581, .T. ) ;
#14655=CARTESIAN_POINT ( 'NONE',  ( -5.676582343750006032, 79.42708332991935549, 9.832129032723418760 ) ) ;
#14656=CARTESIAN_POINT ( 'NONE',  ( 6.123233995736767268E-16, 93.12499999317203958, -10.00000000000000178 ) ) ;
#14660=CARTESIAN_POINT ( 'NONE',  ( -4.088227598258586603E-16, 293.3593750017070079, -6.676582343750001591 ) ) ;
#14679=CARTESIAN_POINT ( 'NONE',  ( 3.042071309553159519, 39.73958332991934128, 11.35316468750000141 ) ) ;
#14681=CARTESIAN_POINT ( 'NONE',  ( -8.660254037844390851, 9.791666659838700326, 4.999999999999998224 ) ) ;
#14685=CARTESIAN_POINT ( 'NONE',  ( -2.085542519210945728E-15, 54.53124999658601979, 11.35316468750000141 ) ) ;
#14691=CARTESIAN_POINT ( 'NONE',  ( 8.311093377946834337, 35.15624999658601268, 8.311093377946839666 ) ) ;
#14695=CARTESIAN_POINT ( 'NONE',  ( 5.676582343749993598, 164.9479166632526983, 9.832129032723422313 ) ) ;
#14696=CARTESIAN_POINT ( 'NONE',  ( -10.00000000000000355, 134.5833333265053966, 2.679491924311223183 ) ) ;
#14699=( BOUNDED_CURVE ( )  B_SPLINE_CURVE ( 2, ( #10843, #5193, #28190, #44058, #22517, #16857, #62885, #11218, #34246, #57248, #21034, #38404, #61406 ),
 .UNSPECIFIED., .F., .F. ) 
 B_SPLINE_CURVE_WITH_KNOTS ( ( 3, 2, 2, 2, 2, 2, 3 ),
 ( 0.2880434782608695676, 0.2898550724637681264, 0.2916666666666666852, 0.2934782608695652439, 0.2952898550724637472, 0.2971014492753623060, 0.2989130434782608647 ),
 .UNSPECIFIED. ) 
 CURVE ( )  GEOMETRIC_REPRESENTATION_ITEM ( )  RATIONAL_B_SPLINE_CURVE ( ( 1.000000000000000000, 0.9659258262890683122, 1.000000000000000000, 0.9659258262890683122, 1.000000000000000000, 0.9659258262890683122, 1.000000000000000000, 0.9659258262890683122, 1.000000000000000000, 0.9659258262890683122, 1.000000000000000000, 0.9659258262890683122, 1.000000000000000000 ) ) 
 REPRESENTATION_ITEM ( '' )  );
#14701=CARTESIAN_POINT ( 'NONE',  ( 10.00000000000000178, 22.08333332650536818, -2.679491924311226736 ) ) ;
#14702=CARTESIAN_POINT ( 'NONE',  ( -3.042071309553173730, 19.63541666325268764, 11.35316468749999785 ) ) ;
#14705=CYLINDRICAL_SURFACE ( 'NONE', #10323, 6.000000000000001776 ) ;
#14709=CARTESIAN_POINT ( 'NONE',  ( -9.832129032723420536, 148.6979166632526983, 5.676582343749997150 ) ) ;
#14719=CARTESIAN_POINT ( 'NONE',  ( -3.042071309553164404, 97.55208332991932707, -11.35316468749999963 ) ) ;
#14723=ORIENTED_EDGE ( 'NONE', *, *, #74053, .F. ) ;
#14739=CARTESIAN_POINT ( 'NONE',  ( 6.123233995736767268E-16, 96.25000000000000000, -10.00000000000000178 ) ) ;
#14741=CARTESIAN_POINT ( 'NONE',  ( -6.676582343750001591, 299.4531250017069510, 0.000000000000000000 ) ) ;
#14750=CARTESIAN_POINT ( 'NONE',  ( -10.00000000000000000, 107.2916666666666856, -2.679491924311229845 ) ) ;
#14753=CARTESIAN_POINT ( 'NONE',  ( 6.676582343750001591, 290.1093750017069510, -8.176455196517173205E-16 ) ) ;
#14757=DIRECTION ( 'NONE',  ( -0.000000000000000000, 1.000000000000000000, -0.000000000000000000 ) ) ;
#14760=CARTESIAN_POINT ( 'NONE',  ( -7.320508075688773708, 183.7499999931720254, -7.320508075688774596 ) ) ;
#14766=CARTESIAN_POINT ( 'NONE',  ( 8.311093377946837890, 6.406249996586016238, -8.311093377946837890 ) ) ;
#14768=CARTESIAN_POINT ( 'NONE',  ( 9.832129032723416984, 200.6770833299193555, 5.676582343750006032 ) ) ;
#14776=CARTESIAN_POINT ( 'NONE',  ( -11.35316468750000141, 3.281249996586016238, -1.390361679473963753E-15 ) ) ;
#14784=CARTESIAN_POINT ( 'NONE',  ( 6.951808397369818766E-16, 122.0312499965860269, -11.35316468750000141 ) ) ;
#14785=CARTESIAN_POINT ( 'NONE',  ( -4.999999999999998224, 83.54166665983869677, -8.660254037844389075 ) ) ;
#14793=CARTESIAN_POINT ( 'NONE',  ( 2.765530957082001251, 292.9218750017069510, 6.676582343750000703 ) ) ;
#14794=CARTESIAN_POINT ( 'NONE',  ( 2.679491924311370177, 185.8333333265053966, 9.999999999999918288 ) ) ;
#14796=CARTESIAN_POINT ( 'NONE',  ( -5.676582343750006032, 169.1145833299193555, 9.832129032723418760 ) ) ;
#14804=CARTESIAN_POINT ( 'NONE',  ( 8.311093377946837890, 161.7187499965860411, -8.311093377946837890 ) ) ;
#14808=CARTESIAN_POINT ( 'NONE',  ( 5.676582343750001591, 61.92708332991934839, -9.832129032723420536 ) ) ;
#14812=ORIENTED_EDGE ( 'NONE', *, *, #62889, .T. ) ;
#14813=AXIS2_PLACEMENT_3D ( 'NONE', #49245, #21326, #26985 ) ;
#14822=EDGE_CURVE ( 'NONE', #15401, #44635, #25578, .T. ) ;
#14831=ORIENTED_EDGE ( 'NONE', *, *, #58814, .F. ) ;
#14838=CARTESIAN_POINT ( 'NONE',  ( -10.00000000000000000, 72.29166666666667140, -2.679491924311229845 ) ) ;
#14840=CARTESIAN_POINT ( 'NONE',  ( 6.000000000000001776, 290.5000000000000000, -7.347880794884121708E-16 ) ) ;
#14842=DIRECTION ( 'NONE',  ( -0.000000000000000000, 1.000000000000000000, -0.000000000000000000 ) ) ;
#14852=CARTESIAN_POINT ( 'NONE',  ( 6.123233995736767268E-16, 191.2500000000000000, -10.00000000000000178 ) ) ;
#14855=CARTESIAN_POINT ( 'NONE',  ( 3.042071309553159519, 150.0520833299193555, 11.35316468750000141 ) ) ;
#14856=CARTESIAN_POINT ( 'NONE',  ( 0.000000000000000000, 300.0000000000000000, 0.000000000000000000 ) ) ;
#14864=CARTESIAN_POINT ( 'NONE',  ( 11.35316468750000141, 11.09374999658601624, 0.000000000000000000 ) ) ;
#14868=LINE ( 'NONE', #20910, #23093 ) ;
#14870=CARTESIAN_POINT ( 'NONE',  ( -5.000000000000005329, 55.20833332650536818, 8.660254037844387298 ) ) ;
#14873=CARTESIAN_POINT ( 'NONE',  ( 2.679491924311232953, 221.0416666666666856, -10.00000000000001066 ) ) ;
#14876=CARTESIAN_POINT ( 'NONE',  ( 10.00000000000001954, 160.0000000000000000, 0.000000000000000000 ) ) ;
#14881=CARTESIAN_POINT ( 'NONE',  ( 6.951808397369818766E-16, 127.0312499965860269, -11.35316468750000141 ) ) ;
#14889=CARTESIAN_POINT ( 'NONE',  ( -2.085542519210945728E-15, 129.5312499965860127, 11.35316468750000141 ) ) ;
#14893=DIRECTION ( 'NONE',  ( -0.000000000000000000, 1.000000000000000000, -0.000000000000000000 ) ) ;
#14896=CARTESIAN_POINT ( 'NONE',  ( 9.832129032723420536, 116.5104166632526841, -5.676582343749999815 ) ) ;
#14900=CARTESIAN_POINT ( 'NONE',  ( -9.832129032723420536, 24.01041666325268409, 5.676582343749997150 ) ) ;
#14908=CARTESIAN_POINT ( 'NONE',  ( 2.485281374238571317, 298.7500000034140157, -6.000000000000003553 ) ) ;
#14912=CARTESIAN_POINT ( 'NONE',  ( -9.832129032723420536, 139.0104166632526983, 5.676582343749997150 ) ) ;
#14915=LINE ( 'NONE', #62072, #4094 ) ;
#14927=CARTESIAN_POINT ( 'NONE',  ( -11.35316468750000141, 188.4895833299193555, 3.042071309553159963 ) ) ;
#14929=CARTESIAN_POINT ( 'NONE',  ( -4.242640687119285658, 291.1875000034139589, 4.242640687119287435 ) ) ;
#14930=CARTESIAN_POINT ( 'NONE',  ( 6.676582343750003368, 288.8906250017070079, 2.765530957081995478 ) ) ;
#14931=EDGE_CURVE ( 'NONE', #48188, #65462, #49780, .T. ) ;
#14933=CARTESIAN_POINT ( 'NONE',  ( 7.320508075688766603, 94.37500000000000000, 7.320508075688770155 ) ) ;
#14941=DIRECTION ( 'NONE',  ( -0.000000000000000000, 1.000000000000000000, -0.000000000000000000 ) ) ;
#14944=LINE ( 'NONE', #25520, #19843 ) ;
#14946=CARTESIAN_POINT ( 'NONE',  ( -5.676582343750006032, 109.4270833299193555, 9.832129032723418760 ) ) ;
#14954=CARTESIAN_POINT ( 'NONE',  ( 3.153939666463620179E-13, 158.7500000000000284, 9.999999999999998224 ) ) ;
#14955=CARTESIAN_POINT ( 'NONE',  ( -3.042071309553164404, 222.2395833299193555, -11.35316468749999963 ) ) ;
#14960=CARTESIAN_POINT ( 'NONE',  ( -9.832129032723420536, 189.0104166632526983, 5.676582343749997150 ) ) ;
#14961=CARTESIAN_POINT ( 'NONE',  ( -7.320508075688773708, 123.7499999931720396, -7.320508075688774596 ) ) ;
#14967=CARTESIAN_POINT ( 'NONE',  ( -8.311093377946836114, 77.65624999658602690, -8.311093377946837890 ) ) ;
#14972=AXIS2_PLACEMENT_3D ( 'NONE', #37591, #31927, #47778 ) ;
#14974=CARTESIAN_POINT ( 'NONE',  ( 9.832129032723416984, 95.36458332991935549, 5.676582343750006032 ) ) ;
#14975=ORIENTED_EDGE ( 'NONE', *, *, #56884, .F. ) ;
#14981=CARTESIAN_POINT ( 'NONE',  ( 3.042071309553159519, 79.73958332991934128, 11.35316468750000141 ) ) ;
#14985=CARTESIAN_POINT ( 'NONE',  ( 10.00000000000000178, 166.8749999931720538, 0.000000000000000000 ) ) ;
#14986=CARTESIAN_POINT ( 'NONE',  ( 4.242640687119287435, 296.4375000034140157, 4.242640687119285658 ) ) ;
#14987=CARTESIAN_POINT ( 'NONE',  ( -9.832129032723420536, 79.01041666325268409, 5.676582343749997150 ) ) ;
#14988=CARTESIAN_POINT ( 'NONE',  ( -6.676582343750001591, 292.4531250017069510, 0.000000000000000000 ) ) ;
#14990=CARTESIAN_POINT ( 'NONE',  ( -9.832129032723420536, 203.6979166632526983, 5.676582343749997150 ) ) ;
#14992=FACE_OUTER_BOUND ( 'NONE', #44808, .T. ) ;
#14996=CARTESIAN_POINT ( 'NONE',  ( -11.35316468750000141, 208.4895833299193839, 3.042071309553159963 ) ) ;
#15002=CARTESIAN_POINT ( 'NONE',  ( 6.951808397369818766E-16, 182.3437499965860411, -11.35316468750000141 ) ) ;
#15007=CARTESIAN_POINT ( 'NONE',  ( -4.999999999999994671, 91.66666666666665719, -8.660254037844383745 ) ) ;
#15012=EDGE_CURVE ( 'NONE', #24662, #46560, #358, .T. ) ;
#15023=CARTESIAN_POINT ( 'NONE',  ( -10.00000000000011546, 82.29166666666672825, -2.679491924311261375 ) ) ;
#15031=ORIENTED_EDGE ( 'NONE', *, *, #30348, .T. ) ;
#15034=CARTESIAN_POINT ( 'NONE',  ( -8.311093377946841443, 69.21874999658602690, 8.311093377946830785 ) ) ;
#15037=CARTESIAN_POINT ( 'NONE',  ( -1.836970198721029983E-15, 70.62499999317203958, 10.00000000000000178 ) ) ;
#15039=CARTESIAN_POINT ( 'NONE',  ( -6.676582343750001591, 291.6093750017069510, 0.000000000000000000 ) ) ;
#15042=AXIS2_PLACEMENT_3D ( 'NONE', #3973, #10731, #61302 ) ;
#15057=CARTESIAN_POINT ( 'NONE',  ( 8.311093377946837890, 46.40624999658601268, -8.311093377946837890 ) ) ;
#15058=CARTESIAN_POINT ( 'NONE',  ( -7.320508075688778149, 4.999999993172032475, 7.320508075688769267 ) ) ;
#15063=CARTESIAN_POINT ( 'NONE',  ( -5.676582343749998039, 52.44791666325268409, -9.832129032723420536 ) ) ;
#15069=CARTESIAN_POINT ( 'NONE',  ( 9.832129032723420536, 46.19791666325268409, -5.676582343749999815 ) ) ;
#15072=CARTESIAN_POINT ( 'NONE',  ( -9.832129032723418760, 157.8645833299193839, -5.676582343750004256 ) ) ;
#15073=CARTESIAN_POINT ( 'NONE',  ( 6.123233995736767268E-16, 128.1249999931720254, -10.00000000000000178 ) ) ;
#15076=CYLINDRICAL_SURFACE ( 'NONE', #36431, 10.00000000000000178 ) ;
#15077=CARTESIAN_POINT ( 'NONE',  ( 8.311093377946834337, 35.46874999658600558, 8.311093377946839666 ) ) ;
#15080=CARTESIAN_POINT ( 'NONE',  ( 0.000000000000000000, 300.0000000000000000, 0.000000000000000000 ) ) ;
#15084=CARTESIAN_POINT ( 'NONE',  ( -8.311093377946841443, 158.9062499965860411, 8.311093377946834337 ) ) ;
#15094=CARTESIAN_POINT ( 'NONE',  ( 3.042071309553167069, 102.1354166632526983, -11.35316468749999785 ) ) ;
#15119=CARTESIAN_POINT ( 'NONE',  ( 10.00000000000000000, 71.66666665983869677, 2.679491924311235618 ) ) ;
#15122=ORIENTED_EDGE ( 'NONE', *, *, #14931, .F. ) ;
#15124=CARTESIAN_POINT ( 'NONE',  ( 5.000000000000002665, 125.8333333333333570, -8.660254037844390851 ) ) ;
#15129=CARTESIAN_POINT ( 'NONE',  ( -4.999999999999998224, 101.6666666666666714, -8.660254037844389075 ) ) ;
#15131=CARTESIAN_POINT ( 'NONE',  ( -4.721056650415999201, 290.4843750017070079, -4.721056650415999201 ) ) ;
#15133=ORIENTED_EDGE ( 'NONE', *, *, #6696, .T. ) ;
#15144=CARTESIAN_POINT ( 'NONE',  ( -2.679491924311087736, 215.4166666598387110, 10.00000000000008349 ) ) ;
#15145=CARTESIAN_POINT ( 'NONE',  ( -2.679491924311225848, 221.4583333333333428, -10.00000000000000178 ) ) ;
#15147=CARTESIAN_POINT ( 'NONE',  ( -9.832129032723418760, 188.1770833299193555, -5.676582343750004256 ) ) ;
#15151=CARTESIAN_POINT ( 'NONE',  ( 8.248616681371277227E-12, 116.2499999999993747, -10.00000000000000178 ) ) ;
#15155=CARTESIAN_POINT ( 'NONE',  ( -8.311093377946836114, 2.656249996586016238, -8.311093377946837890 ) ) ;
#15162=CARTESIAN_POINT ( 'NONE',  ( 5.676582343749993598, 4.947916663252683200, 9.832129032723422313 ) ) ;
#15164=CARTESIAN_POINT ( 'NONE',  ( 11.35316468749999785, 115.5729166632526841, 3.042071309553174174 ) ) ;
#15166=CARTESIAN_POINT ( 'NONE',  ( -4.999999999999998224, 88.54166665983869677, -8.660254037844389075 ) ) ;
#15173=CARTESIAN_POINT ( 'NONE',  ( 1.479685137562080274E-15, 225.9999999999999432, -10.00000000000000178 ) ) ;
#15174=CARTESIAN_POINT ( 'NONE',  ( 6.676582343750004256, 291.0468750017070079, 2.765530957081995478 ) ) ;
#15178=CARTESIAN_POINT ( 'NONE',  ( -2.679491924311225848, 208.3333333265053966, -10.00000000000000178 ) ) ;
#15183=AXIS2_PLACEMENT_3D ( 'NONE', #46917, #64999, #18623 ) ;
#15184=CARTESIAN_POINT ( 'NONE',  ( -9.832129032723420536, 159.0104166632526983, 5.676582343749997150 ) ) ;
#15185=CARTESIAN_POINT ( 'NONE',  ( -2.679491924311236506, 218.5416666666667140, 10.00000000000000355 ) ) ;
#15190=CARTESIAN_POINT ( 'NONE',  ( -8.311093377946841443, 59.21874999658601979, 8.311093377946830785 ) ) ;
#15196=CARTESIAN_POINT ( 'NONE',  ( -6.000000000000003553, 288.0000000034140157, -2.485281374238571317 ) ) ;
#15208=CARTESIAN_POINT ( 'NONE',  ( -6.000000000000003553, 289.9375000000000000, -2.485281374238571317 ) ) ;
#15218=CARTESIAN_POINT ( 'NONE',  ( 7.320508075688771044, 69.37499999999998579, 7.320508075688775484 ) ) ;
#15220=CARTESIAN_POINT ( 'NONE',  ( -6.000000000000003553, 293.9374999999999432, -2.485281374238571317 ) ) ;
#15223=AXIS2_PLACEMENT_3D ( 'NONE', #40436, #68361, #34801 ) ;
#15224=DIRECTION ( 'NONE',  ( -0.000000000000000000, 1.000000000000000000, -0.000000000000000000 ) ) ;
#15231=CARTESIAN_POINT ( 'NONE',  ( -2.679491924311225848, 186.4583333333332860, -10.00000000000000178 ) ) ;
#15232=( BOUNDED_CURVE ( )  B_SPLINE_CURVE ( 2, ( #62768, #28075, #68810, #57888, #34134, #28452, #5824, #5450, #6565, #63524, #34883, #17874, #74471 ),
 .UNSPECIFIED., .F., .F. ) 
 B_SPLINE_CURVE_WITH_KNOTS ( ( 3, 2, 2, 2, 2, 2, 3 ),
 ( 1.083288719158836511, 1.088522722798160647, 1.093756726437484783, 1.098990730076808697, 1.104224733716132612, 1.109458737355456748, 1.114692740994780884 ),
 .UNSPECIFIED. ) 
 CURVE ( )  GEOMETRIC_REPRESENTATION_ITEM ( )  RATIONAL_B_SPLINE_CURVE ( ( 0.9999999999999895639, 0.9659258262890787483, 1.000000000000000000, 0.9659258262890683122, 1.000000000000000000, 0.9659258262890683122, 1.000000000000000000, 0.9659258262890683122, 1.000000000000000000, 0.9659258262890683122, 1.000000000000000000, 0.9659258262890725311, 0.9999999999999957812 ) ) 
 REPRESENTATION_ITEM ( '' )  );
#15235=CARTESIAN_POINT ( 'NONE',  ( 11.35316468749999963, 151.3020833299193555, -3.042071309553165293 ) ) ;
#15240=CARTESIAN_POINT ( 'NONE',  ( -3.042071309553164404, 17.55208332991935194, -11.35316468749999963 ) ) ;
#15246=CARTESIAN_POINT ( 'NONE',  ( -7.320508075688773708, 43.74999999317202537, -7.320508075688774596 ) ) ;
#15249=CARTESIAN_POINT ( 'NONE',  ( 7.320508075688767491, 54.37500000000000000, 7.320508075688771044 ) ) ;
#15253=EDGE_LOOP ( 'NONE', ( #62317, #22350, #13816, #61456 ) ) ;
#15254=ORIENTED_EDGE ( 'NONE', *, *, #2585, .T. ) ;
#15258=CARTESIAN_POINT ( 'NONE',  ( 3.042071309553159519, 134.7395833299193839, 11.35316468750000141 ) ) ;
#15267=CARTESIAN_POINT ( 'NONE',  ( 11.35316468749999785, 120.5729166632526841, 3.042071309553174174 ) ) ;
#15271=CARTESIAN_POINT ( 'NONE',  ( 11.35316468749999785, 115.8854166632526983, 3.042071309553174174 ) ) ;
#15275=CARTESIAN_POINT ( 'NONE',  ( -3.042071309553173730, 24.63541666325268054, 11.35316468749999785 ) ) ;
#15276=ORIENTED_EDGE ( 'NONE', *, *, #35813, .F. ) ;
#15281=CARTESIAN_POINT ( 'NONE',  ( -2.765530957081998586, 287.6406250017069510, 6.676582343750001591 ) ) ;
#15286=CARTESIAN_POINT ( 'NONE',  ( 11.35316468749999785, 140.8854166632526415, 3.042071309553174174 ) ) ;
#15300=CARTESIAN_POINT ( 'NONE',  ( -1.836970198721029983E-15, 30.62499999317203248, 10.00000000000000178 ) ) ;
#15301=CARTESIAN_POINT ( 'NONE',  ( 5.676582343749993598, 184.9479166632526983, 9.832129032723422313 ) ) ;
#15304=CARTESIAN_POINT ( 'NONE',  ( -6.676582343750002480, 290.3906250017070647, -2.765530957081996810 ) ) ;
#15311=CARTESIAN_POINT ( 'NONE',  ( 0.000000000000000000, 0.000000000000000000, 0.000000000000000000 ) ) ;
#15317=CARTESIAN_POINT ( 'NONE',  ( -2.085542519210945728E-15, 114.8437499965860127, 11.35316468750000141 ) ) ;
#15322=CARTESIAN_POINT ( 'NONE',  ( 6.000000000000003553, 298.4375000000000000, 2.485281374238571317 ) ) ;
#15325=CARTESIAN_POINT ( 'NONE',  ( 9.627422524176592944, 224.7807405533921212, 2.720186965506536936 ) ) ;
#15326=CARTESIAN_POINT ( 'NONE',  ( -8.311093377946836114, 222.6562499965860411, -8.311093377946837890 ) ) ;
#15332=CARTESIAN_POINT ( 'NONE',  ( 5.676582343750001591, 201.9270833299193555, -9.832129032723420536 ) ) ;
#15338=CARTESIAN_POINT ( 'NONE',  ( 4.999999999999999112, 185.8333333333333428, -8.660254037844383745 ) ) ;
#15340=CARTESIAN_POINT ( 'NONE',  ( 8.311093377946834337, 90.15624999658604111, 8.311093377946839666 ) ) ;
#15346=CARTESIAN_POINT ( 'NONE',  ( 5.676582343749993598, 89.94791666325269830, 9.832129032723422313 ) ) ;
#15347=ORIENTED_EDGE ( 'NONE', *, *, #15752, .T. ) ;
#15355=CARTESIAN_POINT ( 'NONE',  ( -3.042071309553173730, 84.32291666325268409, 11.35316468749999785 ) ) ;
#15360=CARTESIAN_POINT ( 'NONE',  ( -1.836970198721029983E-15, 180.6249999931720538, 10.00000000000000178 ) ) ;
#15362=CARTESIAN_POINT ( 'NONE',  ( 5.676582343750001591, 76.92708332991935549, -9.832129032723420536 ) ) ;
#15363=CARTESIAN_POINT ( 'NONE',  ( -4.721056650415998313, 294.5781250017069510, 4.721056650416000089 ) ) ;
#15365=CARTESIAN_POINT ( 'NONE',  ( -11.35316468750000141, 203.2812499965860411, -1.390361679473963753E-15 ) ) ;
#15371=CARTESIAN_POINT ( 'NONE',  ( -5.676582343750006032, 204.1145833299193555, 9.832129032723418760 ) ) ;
#15376=VERTEX_POINT ( 'NONE', #58799 ) ;
#15377=CARTESIAN_POINT ( 'NONE',  ( -9.832129032723420536, 189.0104166632526983, 5.676582343749997150 ) ) ;
#15379=CARTESIAN_POINT ( 'NONE',  ( -8.660254037844385522, 92.91666666666667140, 4.999999999999994671 ) ) ;
#15383=CARTESIAN_POINT ( 'NONE',  ( -5.000000000000005329, 18.33333333333333215, 8.660254037844387298 ) ) ;
#15392=CARTESIAN_POINT ( 'NONE',  ( 7.320508075688774596, 17.49999999317202892, -7.320508075688774596 ) ) ;
#15401=VERTEX_POINT ( 'NONE', #7110 ) ;
#15403=CARTESIAN_POINT ( 'NONE',  ( -3.042071309553173730, 69.63541666325268409, 11.35316468749999785 ) ) ;
#15407=CARTESIAN_POINT ( 'NONE',  ( 2.765530957082001251, 288.9218750017069510, 6.676582343749999815 ) ) ;
#15409=CARTESIAN_POINT ( 'NONE',  ( -8.660254037844387298, 163.9583333265053966, -5.000000000000004441 ) ) ;
#15410=VECTOR ( 'NONE', #12110, 1000.000000000000000 ) ;
#15417=CARTESIAN_POINT ( 'NONE',  ( -9.832129032723420536, 169.0104166632526983, 5.676582343749997150 ) ) ;
#15420=CARTESIAN_POINT ( 'NONE',  ( 2.485281374238878627, 289.3750000034139589, 5.999999999999694467 ) ) ;
#15425=CARTESIAN_POINT ( 'NONE',  ( 5.676582343750001591, 46.61458332991935549, -9.832129032723420536 ) ) ;
#15428=CARTESIAN_POINT ( 'NONE',  ( -10.00000000000000355, 24.58333332650536462, 2.679491924311223183 ) ) ;
#15433=CARTESIAN_POINT ( 'NONE',  ( -11.35316468749999785, 43.07291666325267698, -3.042071309553167513 ) ) ;
#15434=VECTOR ( 'NONE', #71001, 1000.000000000000000 ) ;
#15440=CARTESIAN_POINT ( 'NONE',  ( -5.676582343749998039, 52.44791666325268409, -9.832129032723420536 ) ) ;
#15443=CARTESIAN_POINT ( 'NONE',  ( 3.042071309553167069, 166.8229166632526699, -11.35316468749999785 ) ) ;
#15444=VECTOR ( 'NONE', #59611, 1000.000000000000000 ) ;
#15445=EDGE_CURVE ( 'NONE', #36060, #8118, #9743, .T. ) ;
#15446=CARTESIAN_POINT ( 'NONE',  ( -8.660254037844390851, 139.7916666598387110, 4.999999999999998224 ) ) ;
#15448=CARTESIAN_POINT ( 'NONE',  ( 1.224646799147353454E-15, 300.0000000000000000, -10.00000000000000178 ) ) ;
#15449=CARTESIAN_POINT ( 'NONE',  ( 8.311093377946837890, 36.71874999658601979, -8.311093377946837890 ) ) ;
#15451=ORIENTED_EDGE ( 'NONE', *, *, #55111, .T. ) ;
#15453=DIRECTION ( 'NONE',  ( -0.000000000000000000, 1.000000000000000000, -0.000000000000000000 ) ) ;
#15456=CARTESIAN_POINT ( 'NONE',  ( -1.836970198721029983E-15, 8.750000000000000000, 10.00000000000000178 ) ) ;
#15457=CARTESIAN_POINT ( 'NONE',  ( -5.676582343750006032, 164.1145833299193555, 9.832129032723418760 ) ) ;
#15465=CARTESIAN_POINT ( 'NONE',  ( -10.00000000000000000, 119.1666666598386968, -2.679491924311229845 ) ) ;
#15467=CARTESIAN_POINT ( 'NONE',  ( -3.042071309553173730, 109.6354166632526557, 11.35316468749999785 ) ) ;
#15471=VERTEX_POINT ( 'NONE', #41441 ) ;
#15472=EDGE_LOOP ( 'NONE', ( #50168, #58303, #60312, #51993 ) ) ;
#15491=CARTESIAN_POINT ( 'NONE',  ( 7.320508075688771044, 71.24999999317203958, 7.320508075688775484 ) ) ;
#15492=CARTESIAN_POINT ( 'NONE',  ( 1.224646799147353454E-15, 300.0000000000000000, -10.00000000000000178 ) ) ;
#15494=ORIENTED_EDGE ( 'NONE', *, *, #6099, .F. ) ;
#15501=CARTESIAN_POINT ( 'NONE',  ( -8.660254037844390851, 112.9166666666666856, 4.999999999999998224 ) ) ;
#15503=CARTESIAN_POINT ( 'NONE',  ( -4.721056650415998313, 292.7343750017069510, 4.721056650416000089 ) ) ;
#15515=CARTESIAN_POINT ( 'NONE',  ( -5.676582343750006032, 4.114583329919350163, 9.832129032723418760 ) ) ;
#15518=CARTESIAN_POINT ( 'NONE',  ( -11.35316468750000141, 208.5937499965860411, -1.390361679473963753E-15 ) ) ;
#15526=CARTESIAN_POINT ( 'NONE',  ( 3.042071309553159519, 4.739583329919349275, 11.35316468750000141 ) ) ;
#15532=CARTESIAN_POINT ( 'NONE',  ( -3.042071309553163960, 2.239583329919349719, -11.35316468749999963 ) ) ;
#15534=CARTESIAN_POINT ( 'NONE',  ( 6.951808397369818766E-16, 117.0312499965860269, -11.35316468750000141 ) ) ;
#15536=CARTESIAN_POINT ( 'NONE',  ( 2.679491924311228956, 87.91666665983868256, -10.00000000000000000 ) ) ;
#15542=CARTESIAN_POINT ( 'NONE',  ( -5.000000000000007994, 118.3333333333333428, 8.660254037844390851 ) ) ;
#15543=CARTESIAN_POINT ( 'NONE',  ( -4.088227598258586603E-16, 289.3593750017070079, -6.676582343750001591 ) ) ;
#15544=CARTESIAN_POINT ( 'NONE',  ( 7.320508075688774596, 187.4999999931720254, -7.320508075688774596 ) ) ;
#15548=CARTESIAN_POINT ( 'NONE',  ( -7.320508075688778149, 209.9999999931719969, 7.320508075688769267 ) ) ;
#15553=CARTESIAN_POINT ( 'NONE',  ( 8.660254037844385522, 156.4583333265053966, 5.000000000000005329 ) ) ;
#15554=CARTESIAN_POINT ( 'NONE',  ( -5.676582343750006032, 159.4270833299193555, 9.832129032723418760 ) ) ;
#15557=CARTESIAN_POINT ( 'NONE',  ( -3.042071309553173730, 74.63541666325268409, 11.35316468749999785 ) ) ;
#15563=CARTESIAN_POINT ( 'NONE',  ( -6.000000000000000888, 287.1250000034140157, 2.485281374238575758 ) ) ;
#15589=CARTESIAN_POINT ( 'NONE',  ( 5.000000000000001776, 70.83333333333332860, -8.660254037844389075 ) ) ;
#15590=AXIS2_PLACEMENT_3D ( 'NONE', #41450, #58442, #63707 ) ;
#15592=CARTESIAN_POINT ( 'NONE',  ( -6.000000000000001776, 291.0000000000000000, 0.000000000000000000 ) ) ;
#15602=CARTESIAN_POINT ( 'NONE',  ( -7.320508075688801242, 76.87500000000002842, -7.320508075688802130 ) ) ;
#15603=CARTESIAN_POINT ( 'NONE',  ( -1.836970198721029983E-15, 188.7500000000000000, 10.00000000000000178 ) ) ;
#15606=CARTESIAN_POINT ( 'NONE',  ( -8.311093377946841443, 154.2187499965859843, 8.311093377946830785 ) ) ;
#15609=CARTESIAN_POINT ( 'NONE',  ( 7.320508075688905159, 154.3750000000001137, 7.320508075688908711 ) ) ;
#15612=ORIENTED_EDGE ( 'NONE', *, *, #23367, .T. ) ;
#15613=CARTESIAN_POINT ( 'NONE',  ( -11.35316468750000141, 28.80208332991935194, 3.042071309553159963 ) ) ;
#15614=CARTESIAN_POINT ( 'NONE',  ( 10.00000000000000178, 97.08333332650536818, -2.679491924311226736 ) ) ;
#15619=CARTESIAN_POINT ( 'NONE',  ( -7.320508075688773708, 53.74999999317203248, -7.320508075688774596 ) ) ;
#15622=CARTESIAN_POINT ( 'NONE',  ( -6.000000000000001776, 299.5312500017070079, 0.000000000000000000 ) ) ;
#15624=CARTESIAN_POINT ( 'NONE',  ( 5.000000000000001776, 165.8333333333333428, -8.660254037844389075 ) ) ;
#15627=CARTESIAN_POINT ( 'NONE',  ( -2.679491924311226292, 221.4583333333333428, -10.00000000000000178 ) ) ;
#15631=CARTESIAN_POINT ( 'NONE',  ( 11.35316468750000141, 140.7812499965860411, 0.000000000000000000 ) ) ;
#15637=CARTESIAN_POINT ( 'NONE',  ( -5.676582343749998039, 122.4479166632526983, -9.832129032723420536 ) ) ;
#15643=CARTESIAN_POINT ( 'NONE',  ( 8.311093377946837890, 116.7187499965859985, -8.311093377946837890 ) ) ;
#15647=CARTESIAN_POINT ( 'NONE',  ( -11.35316468750000141, 28.80208332991935194, 3.042071309553159963 ) ) ;
#15655=CARTESIAN_POINT ( 'NONE',  ( -6.676582343750003368, 290.3906250017070647, -2.765530957081996810 ) ) ;
#15659=CARTESIAN_POINT ( 'NONE',  ( -11.35316468750000141, 148.5937499965860411, -1.390361679473963753E-15 ) ) ;
#15672=CARTESIAN_POINT ( 'NONE',  ( 0.000000000000000000, 300.0000000000000000, 10.00000000000000178 ) ) ;
#15677=CARTESIAN_POINT ( 'NONE',  ( 11.35316468749999963, 185.9895833299193839, -3.042071309553165293 ) ) ;
#15681=CARTESIAN_POINT ( 'NONE',  ( -2.765530957081998142, 289.6406250017069510, 6.676582343750000703 ) ) ;
#15683=CARTESIAN_POINT ( 'NONE',  ( -5.000000000000007105, 68.33333333333335702, 8.660254037844389075 ) ) ;
#15692=CARTESIAN_POINT ( 'NONE',  ( -10.00000000000000000, 142.2916666666666856, -2.679491924311229845 ) ) ;
#15696=CARTESIAN_POINT ( 'NONE',  ( 3.042071309553159519, 115.0520833299193555, 11.35316468750000141 ) ) ;
#15697=CARTESIAN_POINT ( 'NONE',  ( 6.123233995736767268E-16, 213.1249999931720538, -10.00000000000000178 ) ) ;
#15705=CARTESIAN_POINT ( 'NONE',  ( 2.485281374238838215, 287.3750000034139020, 5.999999999999736211 ) ) ;
#15707=CARTESIAN_POINT ( 'NONE',  ( 11.35316468749999963, 201.3020833299193839, -3.042071309553165293 ) ) ;
#15712=CARTESIAN_POINT ( 'NONE',  ( 7.320508075688767491, 184.3750000000000000, 7.320508075688771044 ) ) ;
#15714=CARTESIAN_POINT ( 'NONE',  ( -3.042071309553173730, 89.32291666325268409, 11.35316468749999785 ) ) ;
#15720=CARTESIAN_POINT ( 'NONE',  ( 8.311093377946834337, 95.15624999658601268, 8.311093377946839666 ) ) ;
#15722=CARTESIAN_POINT ( 'NONE',  ( 8.660254037844385522, 206.4583333265053682, 5.000000000000005329 ) ) ;
#15728=CARTESIAN_POINT ( 'NONE',  ( -5.676582343750006032, 84.11458332991935549, 9.832129032723418760 ) ) ;
#15734=CARTESIAN_POINT ( 'NONE',  ( -2.679491924311225848, 188.3333333265053682, -10.00000000000000178 ) ) ;
#15735=CARTESIAN_POINT ( 'NONE',  ( 4.242640687119285658, 296.6875000034139589, -4.242640687119286547 ) ) ;
#15736=CARTESIAN_POINT ( 'NONE',  ( -3.042071309553173730, 79.63541666325268409, 11.35316468749999785 ) ) ;
#15737=CARTESIAN_POINT ( 'NONE',  ( -6.676582343750000703, 292.5156250017068942, 2.765530957082001251 ) ) ;
#15739=CARTESIAN_POINT ( 'NONE',  ( -11.35316468750000141, 213.4895833299193839, 3.042071309553159963 ) ) ;
#15743=CARTESIAN_POINT ( 'NONE',  ( -3.673940397442060854E-16, 291.7500000000000000, -6.000000000000001776 ) ) ;
#15744=CARTESIAN_POINT ( 'NONE',  ( -11.35316468749999785, 208.0729166632526983, -3.042071309553167957 ) ) ;
#15747=CARTESIAN_POINT ( 'NONE',  ( -11.35316468749999785, 193.3854166632526415, -3.042071309553167957 ) ) ;
#15751=ORIENTED_EDGE ( 'NONE', *, *, #69177, .F. ) ;
#15752=EDGE_CURVE ( 'NONE', #54774, #21472, #66, .T. ) ;
#15755=CARTESIAN_POINT ( 'NONE',  ( -10.00000000000000000, 12.29166666666666785, -2.679491924311229845 ) ) ;
#15764=VERTEX_POINT ( 'NONE', #11561 ) ;
#15780=CARTESIAN_POINT ( 'NONE',  ( -9.832129032723420536, 79.01041666325268409, 5.676582343749997150 ) ) ;
#15781=LINE ( 'NONE', #21446, #16770 ) ;
#15784=CARTESIAN_POINT ( 'NONE',  ( 6.676582343750001591, 291.1093750017069510, -8.176455196517173205E-16 ) ) ;
#15794=CARTESIAN_POINT ( 'NONE',  ( 8.311093377946837890, 161.7187499965860411, -8.311093377946837890 ) ) ;
#15802=CARTESIAN_POINT ( 'NONE',  ( -3.042071309553173730, 49.32291666325266988, 11.35316468749999785 ) ) ;
#15804=CARTESIAN_POINT ( 'NONE',  ( 2.679491924311228956, 22.91666665983870033, -10.00000000000000000 ) ) ;
#15806=ORIENTED_EDGE ( 'NONE', *, *, #64987, .F. ) ;
#15808=CARTESIAN_POINT ( 'NONE',  ( -8.311093377946836114, 52.65624999658601268, -8.311093377946837890 ) ) ;
#15814=CARTESIAN_POINT ( 'NONE',  ( -11.35316468750000141, 48.28124999658601268, -1.390361679473963753E-15 ) ) ;
#15817=CARTESIAN_POINT ( 'NONE',  ( 3.042071309553167069, 176.8229166632526415, -11.35316468749999785 ) ) ;
#15818=CARTESIAN_POINT ( 'NONE',  ( 10.00000000000000000, 146.6666666598386826, 2.679491924311236062 ) ) ;
#15820=AXIS2_PLACEMENT_3D ( 'NONE', #53241, #13223, #17789 ) ;
#15822=CARTESIAN_POINT ( 'NONE',  ( 3.042071309553159519, 30.05208332991934839, 11.35316468750000141 ) ) ;
#15824=ORIENTED_EDGE ( 'NONE', *, *, #39510, .F. ) ;
#15828=CARTESIAN_POINT ( 'NONE',  ( -5.000000000000008882, 8.333333333333337478, 8.660254037844390851 ) ) ;
#15829=CARTESIAN_POINT ( 'NONE',  ( 5.676582343750001591, 161.6145833299193839, -9.832129032723420536 ) ) ;
#15839=CARTESIAN_POINT ( 'NONE',  ( 11.35316468749999963, 111.3020833299193271, -3.042071309553165293 ) ) ;
#15840=CARTESIAN_POINT ( 'NONE',  ( -2.249999999999999556, 255.9999999999998295, 5.427273995024871844 ) ) ;
#15872=CARTESIAN_POINT ( 'NONE',  ( 6.123233995736767268E-16, 121.2500000000000142, -10.00000000000000178 ) ) ;
#15874=CARTESIAN_POINT ( 'NONE',  ( -6.676582343750000703, 292.6718750017069510, 2.765530957082001251 ) ) ;
#15889=CARTESIAN_POINT ( 'NONE',  ( -8.311093377946841443, 8.906249996586018014, 8.311093377946830785 ) ) ;
#15890=( BOUNDED_CURVE ( )  B_SPLINE_CURVE ( 2, ( #22827, #41675, #64684, #20127, #53739, #42768, #7345, #60125, #36385 ),
 .UNSPECIFIED., .F., .F. ) 
 B_SPLINE_CURVE_WITH_KNOTS ( ( 3, 2, 2, 2, 3 ),
 ( 0.2708333333333312609, 0.2812499999999979461, 0.2916666666666646313, 0.3020833333333312609, 0.3124999999999979461 ),
 .UNSPECIFIED. ) 
 CURVE ( )  GEOMETRIC_REPRESENTATION_ITEM ( )  RATIONAL_B_SPLINE_CURVE ( ( 1.000000000000015099, 0.9238795325112717505, 1.000000000000000000, 0.9238795325112867385, 1.000000000000000000, 0.9238795325112867385, 1.000000000000000000, 0.9238795325113017265, 0.9999999999999850120 ) ) 
 REPRESENTATION_ITEM ( '' )  );
#15892=CARTESIAN_POINT ( 'NONE',  ( -8.311093377946841443, 209.2187499965859843, 8.311093377946830785 ) ) ;
#15894=DIRECTION ( 'NONE',  ( -0.000000000000000000, 1.000000000000000000, -0.000000000000000000 ) ) ;
#15899=CARTESIAN_POINT ( 'NONE',  ( -2.085542519210945728E-15, 14.53124999658601624, 11.35316468750000141 ) ) ;
#15901=CARTESIAN_POINT ( 'NONE',  ( 2.485281374238247132, 292.6875000000001137, -6.000000000000325961 ) ) ;
#15905=CARTESIAN_POINT ( 'NONE',  ( 5.676582343750001591, 11.61458332991935016, -9.832129032723420536 ) ) ;
#15907=CARTESIAN_POINT ( 'NONE',  ( -5.676582343749998039, 127.4479166632526983, -9.832129032723420536 ) ) ;
#15908=CARTESIAN_POINT ( 'NONE',  ( -5.000000000000005329, 105.2083333265053824, 8.660254037844387298 ) ) ;
#15912=CARTESIAN_POINT ( 'NONE',  ( 6.123233995736767268E-16, 183.1249999931720538, -10.00000000000000178 ) ) ;
#15913=CARTESIAN_POINT ( 'NONE',  ( -1.836970198721029983E-15, 5.624999993172032475, 10.00000000000000178 ) ) ;
#15914=ORIENTED_EDGE ( 'NONE', *, *, #5400, .T. ) ;
#15915=CARTESIAN_POINT ( 'NONE',  ( 11.35316468749999963, 1.302083329919349941, -3.042071309553165293 ) ) ;
#15916=CARTESIAN_POINT ( 'NONE',  ( -4.721056650415998313, 289.7343750017069510, 4.721056650416000089 ) ) ;
#15917=DIRECTION ( 'NONE',  ( -0.000000000000000000, 1.000000000000000000, -0.000000000000000000 ) ) ;
#15919=FACE_OUTER_BOUND ( 'NONE', #23526, .T. ) ;
#15925=CARTESIAN_POINT ( 'NONE',  ( -8.311093377946836114, 157.9687499965860411, -8.311093377946837890 ) ) ;
#15929=CARTESIAN_POINT ( 'NONE',  ( -8.311093377946841443, 79.21874999658601268, 8.311093377946830785 ) ) ;
#15941=VECTOR ( 'NONE', #38781, 1000.000000000000114 ) ;
#15943=CARTESIAN_POINT ( 'NONE',  ( 7.320508075688766603, 109.3750000000000000, 7.320508075688770155 ) ) ;
#15952=EDGE_CURVE ( 'NONE', #68916, #28711, #67015, .T. ) ;
#15957=CARTESIAN_POINT ( 'NONE',  ( 1.102182119232618108E-15, 299.2500000000000000, 6.000000000000001776 ) ) ;
#15963=CARTESIAN_POINT ( 'NONE',  ( -7.320508075688778149, 83.12499999999998579, 7.320508075688769267 ) ) ;
#15965=CARTESIAN_POINT ( 'NONE',  ( -6.000000000000000888, 291.0625000000000000, 2.485281374238575758 ) ) ;
#15967=VERTEX_POINT ( 'NONE', #35336 ) ;
#15972=CARTESIAN_POINT ( 'NONE',  ( 2.679491924311228956, 57.91666665983870388, -10.00000000000000000 ) ) ;
#15975=CARTESIAN_POINT ( 'NONE',  ( -10.00000000000003908, 77.29166666666669983, -2.679491924311240947 ) ) ;
#15976=CARTESIAN_POINT ( 'NONE',  ( 4.999999999999993783, 194.1666666666666856, 8.660254037844390851 ) ) ;
#15979=CARTESIAN_POINT ( 'NONE',  ( 8.311093377946837890, 161.7187499965860411, -8.311093377946837890 ) ) ;
#15982=CARTESIAN_POINT ( 'NONE',  ( -3.673940397442060854E-16, 292.7500000000000000, -6.000000000000001776 ) ) ;
#15986=CARTESIAN_POINT ( 'NONE',  ( -3.042071309553164404, 22.55208332991935194, -11.35316468749999963 ) ) ;
#15988=FACE_OUTER_BOUND ( 'NONE', #9944, .T. ) ;
#15992=( BOUNDED_CURVE ( )  B_SPLINE_CURVE ( 2, ( #68560, #39887, #62891, #11223, #65110, #53445, #24390, #19094, #12333, #7786, #64021, #47758, #19460 ),
 .UNSPECIFIED., .F., .F. ) 
 B_SPLINE_CURVE_WITH_KNOTS ( ( 3, 2, 2, 2, 2, 2, 3 ),
 ( 2.496284451484902078, 2.501517587813307131, 2.506750724141712183, 2.511983860470117236, 2.517216996798521844, 2.522450133126926897, 2.527683269455331949 ),
 .UNSPECIFIED. ) 
 CURVE ( )  GEOMETRIC_REPRESENTATION_ITEM ( )  RATIONAL_B_SPLINE_CURVE ( ( 1.000000000000129452, 0.9659258262889388602, 1.000000000000000000, 0.9659258262890683122, 1.000000000000000000, 0.9659258262890683122, 1.000000000000000000, 0.9659258262890683122, 1.000000000000000000, 0.9659258262890683122, 1.000000000000000000, 0.9659258262892875813, 0.9999999999997807310 ) ) 
 REPRESENTATION_ITEM ( '' )  );
#15993=CARTESIAN_POINT ( 'NONE',  ( -4.999999999999998224, 58.54166665983870388, -8.660254037844389075 ) ) ;
#16001=CARTESIAN_POINT ( 'NONE',  ( 7.320508075688778149, 30.62500000000000711, -7.320508075688778149 ) ) ;
#16006=CARTESIAN_POINT ( 'NONE',  ( 11.35316468750000141, 135.7812499965860411, 0.000000000000000000 ) ) ;
#16015=( BOUNDED_CURVE ( )  B_SPLINE_CURVE ( 2, ( #924, #59725, #12943, #6933, #42729, #41988, #29943, #59360, #24271, #47282, #70308, #8034, #35980 ),
 .UNSPECIFIED., .F., .T. ) 
 B_SPLINE_CURVE_WITH_KNOTS ( ( 3, 2, 2, 2, 2, 2, 3 ),
 ( 0.04709510635581609650, 0.05232794973517845838, 0.05756079311454082026, 0.06279363649390318214, 0.06802647987326554402, 0.07325932325262790590, 0.07849216663199026778 ),
 .UNSPECIFIED. ) 
 CURVE ( )  GEOMETRIC_REPRESENTATION_ITEM ( )  RATIONAL_B_SPLINE_CURVE ( ( 1.000000000000000000, 0.9659258262890683122, 1.000000000000000000, 0.9659258262890683122, 1.000000000000000000, 0.9659258262890683122, 1.000000000000000000, 0.9659258262890683122, 1.000000000000000000, 0.9659258262890683122, 1.000000000000000000, 0.9659258262893161140, 0.9999999999997521982 ) ) 
 REPRESENTATION_ITEM ( '' )  );
#16018=CARTESIAN_POINT ( 'NONE',  ( -11.35316468750000141, 118.8020833299193413, 3.042071309553159963 ) ) ;
#16022=CARTESIAN_POINT ( 'NONE',  ( 5.676582343749993598, 40.26041666325268409, 9.832129032723422313 ) ) ;
#16028=CARTESIAN_POINT ( 'NONE',  ( -4.088227598258586603E-16, 290.2031250017069510, -6.676582343750001591 ) ) ;
#16029=FACE_OUTER_BOUND ( 'NONE', #56315, .T. ) ;
#16031=ADVANCED_FACE ( 'NONE', ( #70392 ), #12303, .T. ) ;
#16033=CARTESIAN_POINT ( 'NONE',  ( 5.676582343749993598, 155.2604166632526983, 9.832129032723422313 ) ) ;
#16048=CARTESIAN_POINT ( 'NONE',  ( -10.00000000000000355, 47.70833333333333570, 2.679491924311223183 ) ) ;
#16050=CARTESIAN_POINT ( 'NONE',  ( -5.999999999999999112, 291.1250000034140157, 2.485281374238575314 ) ) ;
#16052=CARTESIAN_POINT ( 'NONE',  ( 7.320508075688770155, 34.37500000000000711, 7.320508075688773708 ) ) ;
#16057=CARTESIAN_POINT ( 'NONE',  ( -2.679491924311235174, 10.41666665983869855, 10.00000000000000000 ) ) ;
#16061=CARTESIAN_POINT ( 'NONE',  ( 2.679491924311228956, 151.0416666666666856, -10.00000000000000000 ) ) ;
#16065=CARTESIAN_POINT ( 'NONE',  ( 3.042071309553167069, 127.1354166632526699, -11.35316468749999785 ) ) ;
#16075=CARTESIAN_POINT ( 'NONE',  ( -2.085542519210945728E-15, 204.8437499965860411, 11.35316468750000141 ) ) ;
#16081=CARTESIAN_POINT ( 'NONE',  ( 3.042071309553159519, 94.73958332991934128, 11.35316468750000141 ) ) ;
#16087=CARTESIAN_POINT ( 'NONE',  ( 6.951808397369818766E-16, 107.0312499965860269, -11.35316468750000141 ) ) ;
#16091=CARTESIAN_POINT ( 'NONE',  ( -7.320508075689014404, 21.87500000000019540, -7.320508075689014404 ) ) ;
#16095=CARTESIAN_POINT ( 'NONE',  ( 11.35316468749999963, 85.98958332991938391, -3.042071309553165293 ) ) ;
#16100=CARTESIAN_POINT ( 'NONE',  ( 10.00000000000000178, 177.0833333265053966, -2.679491924311226736 ) ) ;
#16101=CARTESIAN_POINT ( 'NONE',  ( 11.35316468749999785, 80.88541666325268409, 3.042071309553174174 ) ) ;
#16102=CARTESIAN_POINT ( 'NONE',  ( -4.721056650415999201, 291.3281250017069510, -4.721056650415999201 ) ) ;
#16105=CARTESIAN_POINT ( 'NONE',  ( 11.35316468749999963, 215.9895833299192986, -3.042071309553165293 ) ) ;
#16110=CARTESIAN_POINT ( 'NONE',  ( 5.676582343749993598, 209.9479166632526983, 9.832129032723422313 ) ) ;
#16112=CARTESIAN_POINT ( 'NONE',  ( 6.123233995736767268E-16, 98.12499999317203958, -10.00000000000000178 ) ) ;
#16114=CARTESIAN_POINT ( 'NONE',  ( 6.951808397369818766E-16, 197.3437499965860127, -11.35316468750000141 ) ) ;
#16121=CARTESIAN_POINT ( 'NONE',  ( 8.660254037844385522, 19.58333333333333570, 5.000000000000005329 ) ) ;
#16140=CARTESIAN_POINT ( 'NONE',  ( -9.832129032723420536, 89.01041666325268409, 5.676582343749997150 ) ) ;
#16145=CARTESIAN_POINT ( 'NONE',  ( -4.721056650415999201, 288.4843750017070079, -4.721056650415999201 ) ) ;
#16155=CARTESIAN_POINT ( 'NONE',  ( -2.085542519210945728E-15, 164.8437499965860127, 11.35316468750000141 ) ) ;
#16158=DIRECTION ( 'NONE',  ( 0.000000000000000000, 0.000000000000000000, 1.000000000000000000 ) ) ;
#16162=CARTESIAN_POINT ( 'NONE',  ( -9.832129032723420536, 53.69791666325268409, 5.676582343749997150 ) ) ;
#16164=CARTESIAN_POINT ( 'NONE',  ( 2.679491924311222739, 15.83333332650536640, 10.00000000000000355 ) ) ;
#16167=CARTESIAN_POINT ( 'NONE',  ( 8.660254037844389075, 142.2916666598386826, -5.000000000000000000 ) ) ;
#16169=CARTESIAN_POINT ( 'NONE',  ( -11.35316468750000141, 63.28124999658601979, -1.390361679473963753E-15 ) ) ;
#16175=CARTESIAN_POINT ( 'NONE',  ( 3.042071309553159519, 44.73958332991934839, 11.35316468750000141 ) ) ;
#16177=CARTESIAN_POINT ( 'NONE',  ( 8.660254037844383745, 204.5833333333333428, 5.000000000000004441 ) ) ;
#16178=CARTESIAN_POINT ( 'NONE',  ( 3.042071309553159519, 179.7395833299193555, 11.35316468750000141 ) ) ;
#16180=CARTESIAN_POINT ( 'NONE',  ( 7.320508075688774596, 142.4999999931720538, -7.320508075688774596 ) ) ;
#16184=CARTESIAN_POINT ( 'NONE',  ( -11.35316468750000141, 38.80208332991934839, 3.042071309553159963 ) ) ;
#16186=CARTESIAN_POINT ( 'NONE',  ( 11.35316468749999963, 170.9895833299193839, -3.042071309553165293 ) ) ;
#16187=EDGE_LOOP ( 'NONE', ( #3304, #59648, #45719, #9192 ) ) ;
#16191=CARTESIAN_POINT ( 'NONE',  ( 6.123233995736767268E-16, 218.1249999931720538, -10.00000000000000178 ) ) ;
#16193=CARTESIAN_POINT ( 'NONE',  ( 3.042071309553167513, 161.8229166632527267, -11.35316468749999785 ) ) ;
#16203=CARTESIAN_POINT ( 'NONE',  ( 11.35316468750000141, 116.0937499965860127, 0.000000000000000000 ) ) ;
#16204=CARTESIAN_POINT ( 'NONE',  ( 6.123233995736767268E-16, 13.12499999317203425, -10.00000000000000178 ) ) ;
#16230=EDGE_LOOP ( 'NONE', ( #19490, #50449, #38582, #39353 ) ) ;
#16237=CARTESIAN_POINT ( 'NONE',  ( -10.00000000000000888, 127.7083333333333570, 2.679491924311224960 ) ) ;
#16238=CARTESIAN_POINT ( 'NONE',  ( 10.00000000000000178, 125.2083333333333428, -2.679491924311226736 ) ) ;
#16240=CARTESIAN_POINT ( 'NONE',  ( 3.084418934648133437, 225.9999999999999716, 9.520615687278169759 ) ) ;
#16251=CARTESIAN_POINT ( 'NONE',  ( -8.660254037844387298, 213.9583333265053682, -5.000000000000004441 ) ) ;
#16253=CARTESIAN_POINT ( 'NONE',  ( -3.042071309553173730, 14.32291666325268231, 11.35316468749999785 ) ) ;
#16255=CARTESIAN_POINT ( 'NONE',  ( -5.676582343749998039, 202.7604166632526983, -9.832129032723420536 ) ) ;
#16263=CARTESIAN_POINT ( 'NONE',  ( -8.311093377946841443, 3.906249996586016682, 8.311093377946830785 ) ) ;
#16265=CARTESIAN_POINT ( 'NONE',  ( 1.102182119232618108E-15, 292.2500000000000000, 6.000000000000001776 ) ) ;
#16269=CARTESIAN_POINT ( 'NONE',  ( 9.832129032723420536, 1.197916663252682756, -5.676582343749999815 ) ) ;
#16271=CARTESIAN_POINT ( 'NONE',  ( -8.311093377946841443, 138.9062499965859843, 8.311093377946830785 ) ) ;
#16272=CARTESIAN_POINT ( 'NONE',  ( 8.660254037844389075, 107.2916666598387110, -5.000000000000000000 ) ) ;
#16277=VERTEX_POINT ( 'NONE', #38669 ) ;
#16279=CARTESIAN_POINT ( 'NONE',  ( -6.676582343750003368, 290.5468750017071216, -2.765530957081996810 ) ) ;
#16285=AXIS2_PLACEMENT_3D ( 'NONE', #59994, #15453, #8311 ) ;
#16292=CARTESIAN_POINT ( 'NONE',  ( 11.35316468749999785, 80.88541666325269830, 3.042071309553174174 ) ) ;
#16293=ORIENTED_EDGE ( 'NONE', *, *, #3790, .T. ) ;
#16296=ORIENTED_EDGE ( 'NONE', *, *, #63430, .T. ) ;
#16298=CARTESIAN_POINT ( 'NONE',  ( 1.567784982238203817E-13, 113.7500000000000284, 10.00000000000000533 ) ) ;
#16299=CARTESIAN_POINT ( 'NONE',  ( 5.000000000000001776, 67.70833332650536818, -8.660254037844389075 ) ) ;
#16306=DIRECTION ( 'NONE',  ( 0.000000000000000000, 0.000000000000000000, 1.000000000000000000 ) ) ;
#16314=EDGE_CURVE ( 'NONE', #26730, #42029, #72228, .T. ) ;
#16317=VERTEX_POINT ( 'NONE', #72989 ) ;
#16325=CARTESIAN_POINT ( 'NONE',  ( 8.660254037844389075, 80.41666666666667140, -5.000000000000000000 ) ) ;
#16327=CARTESIAN_POINT ( 'NONE',  ( 2.485281374238575314, 291.3125000000000000, 6.000000000000000888 ) ) ;
#16329=EDGE_LOOP ( 'NONE', ( #45604, #30, #51130, #54134 ) ) ;
#16337=CARTESIAN_POINT ( 'NONE',  ( -1.836970198721029983E-15, 198.7500000000000000, 10.00000000000000178 ) ) ;
#16339=LINE ( 'NONE', #26548, #7860 ) ;
#16341=CARTESIAN_POINT ( 'NONE',  ( -11.35316468749999785, 163.3854166632526983, -3.042071309553167513 ) ) ;
#16345=CARTESIAN_POINT ( 'NONE',  ( -4.242640687119285658, 297.1875000034139589, 4.242640687119287435 ) ) ;
#16347=CARTESIAN_POINT ( 'NONE',  ( -9.832129032723420536, 19.01041666325268409, 5.676582343749997150 ) ) ;
#16353=CARTESIAN_POINT ( 'NONE',  ( -10.00000000000000000, 64.16666665983869677, -2.679491924311229845 ) ) ;
#16356=CARTESIAN_POINT ( 'NONE',  ( 5.000000000000104805, 214.1666666666667993, 8.660254037844582697 ) ) ;
#16360=ORIENTED_EDGE ( 'NONE', *, *, #21030, .T. ) ;
#16361=EDGE_CURVE ( 'NONE', #8939, #12433, #32881, .T. ) ;
#16364=CARTESIAN_POINT ( 'NONE',  ( -10.00000000000001599, 162.7083333333333712, 2.679491924311226292 ) ) ;
#16366=CARTESIAN_POINT ( 'NONE',  ( -8.311093377946836114, 137.6562499965859558, -8.311093377946837890 ) ) ;
#16379=CARTESIAN_POINT ( 'NONE',  ( 11.35316468749999963, 131.3020833299193555, -3.042071309553165293 ) ) ;
#16383=CARTESIAN_POINT ( 'NONE',  ( 9.832129032723416984, 35.67708332991935549, 5.676582343750006032 ) ) ;
#16384=ORIENTED_EDGE ( 'NONE', *, *, #12959, .T. ) ;
#16385=LINE ( 'NONE', #33783, #41662 ) ;
#16390=CARTESIAN_POINT ( 'NONE',  ( -4.242640687119285658, 298.1875000034139589, 4.242640687119287435 ) ) ;
#16392=CARTESIAN_POINT ( 'NONE',  ( 8.660254037844389075, 112.2916666598387110, -5.000000000000000000 ) ) ;
#16394=CARTESIAN_POINT ( 'NONE',  ( -8.311093377946836114, 152.9687499965859558, -8.311093377946837890 ) ) ;
#16409=ORIENTED_EDGE ( 'NONE', *, *, #2542, .F. ) ;
#16412=CARTESIAN_POINT ( 'NONE',  ( -8.660254037844390851, 209.7916666598387110, 4.999999999999998224 ) ) ;
#16414=CARTESIAN_POINT ( 'NONE',  ( -10.00000000000000355, 37.70833333333333570, 2.679491924311223183 ) ) ;
#16421=ORIENTED_EDGE ( 'NONE', *, *, #22684, .F. ) ;
#16425=CARTESIAN_POINT ( 'NONE',  ( 1.102182119232618108E-15, 287.3125000034140157, 6.000000000000001776 ) ) ;
#16428=CARTESIAN_POINT ( 'NONE',  ( 5.000000000000001776, 160.8333333333333428, -8.660254037844389075 ) ) ;
#16432=CARTESIAN_POINT ( 'NONE',  ( 8.311093377946837890, 121.7187499965860411, -8.311093377946837890 ) ) ;
#16433=CARTESIAN_POINT ( 'NONE',  ( -2.143145793903030439E-12, 53.74999999999984368, 9.999999999999998224 ) ) ;
#16443=( BOUNDED_CURVE ( )  B_SPLINE_CURVE ( 2, ( #42645, #60370, #8318 ),
 .UNSPECIFIED., .F., .F. ) 
 B_SPLINE_CURVE_WITH_KNOTS ( ( 3, 3 ),
 ( 0.9728260869565217295, 0.9744508335588618619 ),
 .UNSPECIFIED. ) 
 CURVE ( )  GEOMETRIC_REPRESENTATION_ITEM ( )  RATIONAL_B_SPLINE_CURVE ( ( 1.000000000000000000, 0.9694402323236602781, 0.9936961387326025408 ) ) 
 REPRESENTATION_ITEM ( '' )  );
#16445=CARTESIAN_POINT ( 'NONE',  ( 6.951808397369818766E-16, 202.3437499965860127, -11.35316468750000141 ) ) ;
#16451=CARTESIAN_POINT ( 'NONE',  ( 1.425702245604163669E-12, 48.75000000000012079, 10.00000000000000178 ) ) ;
#16452=CARTESIAN_POINT ( 'NONE',  ( 3.042071309553159519, 89.73958332991935549, 11.35316468750000141 ) ) ;
#16459=CARTESIAN_POINT ( 'NONE',  ( 9.832129032723420536, 101.1979166632526841, -5.676582343749999815 ) ) ;
#16461=CARTESIAN_POINT ( 'NONE',  ( 10.00000000000000178, 206.8749999931720538, 0.000000000000000000 ) ) ;
#16463=CARTESIAN_POINT ( 'NONE',  ( 5.000000000000001776, 217.7083333265053682, -8.660254037844389075 ) ) ;
#16467=CARTESIAN_POINT ( 'NONE',  ( -11.35316468749999785, 103.0729166632526841, -3.042071309553167957 ) ) ;
#16472=CARTESIAN_POINT ( 'NONE',  ( 7.320508075688771044, 181.2499999931720254, 7.320508075688775484 ) ) ;
#16475=CARTESIAN_POINT ( 'NONE',  ( -11.35316468750000141, 68.59374999658601268, -1.390361679473963753E-15 ) ) ;
#16476=CARTESIAN_POINT ( 'NONE',  ( -6.676582343750003368, 288.3906250017069510, -2.765530957081996810 ) ) ;
#16480=CARTESIAN_POINT ( 'NONE',  ( 9.832129032723420536, 1.510416663252683422, -5.676582343749999815 ) ) ;
#16485=CARTESIAN_POINT ( 'NONE',  ( 8.311093377946834337, 205.1562499965859843, 8.311093377946839666 ) ) ;
#16488=CARTESIAN_POINT ( 'NONE',  ( -6.676582343750003368, 296.3906250017069510, -2.765530957081996810 ) ) ;
#16490=CARTESIAN_POINT ( 'NONE',  ( -8.311093377946841443, 199.2187499965860411, 8.311093377946834337 ) ) ;
#16493=CIRCLE ( 'NONE', #36968, 10.00000000000000178 ) ;
#16497=CARTESIAN_POINT ( 'NONE',  ( -8.660254037844387298, 17.08333333333333570, -5.000000000000004441 ) ) ;
#16512=VECTOR ( 'NONE', #14842, 1000.000000000000000 ) ;
#16518=CARTESIAN_POINT ( 'NONE',  ( 3.042071309553159519, 90.05208332991932707, 11.35316468750000141 ) ) ;
#16519=CARTESIAN_POINT ( 'NONE',  ( 1.102182119232618108E-15, 297.2500000000000000, 6.000000000000001776 ) ) ;
#16523=CARTESIAN_POINT ( 'NONE',  ( 4.721056650415999201, 289.2343750017069510, -4.721056650415999201 ) ) ;
#16526=CARTESIAN_POINT ( 'NONE',  ( -8.311093377946841443, 198.9062499965860695, 8.311093377946830785 ) ) ;
#16531=CARTESIAN_POINT ( 'NONE',  ( 6.951808397369818766E-16, 172.3437499965860127, -11.35316468750000141 ) ) ;
#16534=CARTESIAN_POINT ( 'NONE',  ( -7.320508075688768379, 206.8750000000000000, -7.320508075688769267 ) ) ;
#16537=CARTESIAN_POINT ( 'NONE',  ( -8.311093377946841443, 48.90624999658601268, 8.311093377946830785 ) ) ;
#16544=DIRECTION ( 'NONE',  ( -0.000000000000000000, 1.000000000000000000, -0.000000000000000000 ) ) ;
#16546=CARTESIAN_POINT ( 'NONE',  ( -8.311093377946836114, 62.65624999658601268, -8.311093377946837890 ) ) ;
#16552=CARTESIAN_POINT ( 'NONE',  ( -3.042071309553163960, 42.23958332991934128, -11.35316468749999963 ) ) ;
#16555=CARTESIAN_POINT ( 'NONE',  ( -8.311093377946836114, 177.6562499965859843, -8.311093377946837890 ) ) ;
#16556=CARTESIAN_POINT ( 'NONE',  ( 8.660254037844389075, 137.2916666598387110, -5.000000000000000000 ) ) ;
#16559=LINE ( 'NONE', #15448, #64112 ) ;
#16560=CARTESIAN_POINT ( 'NONE',  ( 11.35316468750000141, 41.09374999658601979, 0.000000000000000000 ) ) ;
#16561=CARTESIAN_POINT ( 'NONE',  ( 4.242640687119285658, 295.6875000034139589, -4.242640687119286547 ) ) ;
#16562=CARTESIAN_POINT ( 'NONE',  ( 5.676582343750001591, 181.6145833299193555, -9.832129032723420536 ) ) ;
#16569=CARTESIAN_POINT ( 'NONE',  ( 8.311093377946837890, 166.4062499965860127, -8.311093377946837890 ) ) ;
#16578=CARTESIAN_POINT ( 'NONE',  ( 11.35316468750000141, 111.0937499965860127, 0.000000000000000000 ) ) ;
#16579=CARTESIAN_POINT ( 'NONE',  ( -1.836970198721029983E-15, 10.62499999317203425, 10.00000000000000178 ) ) ;
#16610=CARTESIAN_POINT ( 'NONE',  ( 10.00000000000000000, 119.7916666666666714, 2.679491924311236062 ) ) ;
#16614=CARTESIAN_POINT ( 'NONE',  ( -6.676582343750003368, 289.5468750017069510, -2.765530957081996810 ) ) ;
#16626=CARTESIAN_POINT ( 'NONE',  ( -9.832129032723420536, 18.69791666325268409, 5.676582343749997150 ) ) ;
#16628=CARTESIAN_POINT ( 'NONE',  ( 3.042071309553159519, 210.0520833299193555, 11.35316468750000141 ) ) ;
#16632=DIRECTION ( 'NONE',  ( -0.000000000000000000, 1.000000000000000000, -0.000000000000000000 ) ) ;
#16635=CARTESIAN_POINT ( 'NONE',  ( -11.35316468749999785, 18.07291666325267698, -3.042071309553167513 ) ) ;
#16637=DIRECTION ( 'NONE',  ( -0.000000000000000000, 1.000000000000000000, -0.000000000000000000 ) ) ;
#16642=CARTESIAN_POINT ( 'NONE',  ( 9.832129032723420536, 6.197916663252683200, -5.676582343749999815 ) ) ;
#16644=CARTESIAN_POINT ( 'NONE',  ( 8.311093377946834337, 135.1562499965860411, 8.311093377946839666 ) ) ;
#16645=CARTESIAN_POINT ( 'NONE',  ( -10.00000000000000178, 99.37499999317203958, -1.224646799147353454E-15 ) ) ;
#16649=CARTESIAN_POINT ( 'NONE',  ( 1.224646799147353454E-15, 300.0000000000000000, -10.00000000000000178 ) ) ;
#16653=CARTESIAN_POINT ( 'NONE',  ( -6.676582343750001591, 290.6093750017069510, 0.000000000000000000 ) ) ;
#16659=ORIENTED_EDGE ( 'NONE', *, *, #21321, .T. ) ;
#16662=CARTESIAN_POINT ( 'NONE',  ( 7.320508075688771044, 216.2499999931720538, 7.320508075688775484 ) ) ;
#16665=CARTESIAN_POINT ( 'NONE',  ( -2.085542519210945728E-15, 74.84374999658602690, 11.35316468750000141 ) ) ;
#16666=B_SPLINE_CURVE_WITH_KNOTS ( 'NONE', 5,
 ( #57412, #33660, #74368, #62306, #73631, #27225 ),
 .UNSPECIFIED., .F., .F.,
 ( 6, 6 ),
 ( 0.000000000000000000, 4.840251854566806067 ),
 .UNSPECIFIED. ) ;
#16670=ORIENTED_EDGE ( 'NONE', *, *, #40352, .T. ) ;
#16689=ORIENTED_EDGE ( 'NONE', *, *, #39997, .F. ) ;
#16690=CARTESIAN_POINT ( 'NONE',  ( 0.000000000000000000, 300.0000000000000000, 0.000000000000000000 ) ) ;
#16691=VERTEX_POINT ( 'NONE', #17873 ) ;
#16696=CARTESIAN_POINT ( 'NONE',  ( 2.679491924311228956, 86.04166666666667140, -10.00000000000000000 ) ) ;
#16699=CARTESIAN_POINT ( 'NONE',  ( -4.721056650415998313, 298.7343750017069510, 4.721056650416000089 ) ) ;
#16700=ORIENTED_EDGE ( 'NONE', *, *, #65153, .F. ) ;
#16701=EDGE_CURVE ( 'NONE', #39904, #34004, #36182, .T. ) ;
#16710=CARTESIAN_POINT ( 'NONE',  ( 4.999999999999993783, 204.1666666666666856, 8.660254037844390851 ) ) ;
#16712=CARTESIAN_POINT ( 'NONE',  ( 5.676582343749993598, 165.2604166632526983, 9.832129032723422313 ) ) ;
#16720=CARTESIAN_POINT ( 'NONE',  ( -8.311093377946836114, 27.96874999658601624, -8.311093377946837890 ) ) ;
#16722=EDGE_CURVE ( 'NONE', #10942, #58121, #12149, .T. ) ;
#16725=CARTESIAN_POINT ( 'NONE',  ( 7.320508075688774596, 222.4999999931720254, -7.320508075688774596 ) ) ;
#16729=CARTESIAN_POINT ( 'NONE',  ( 10.00000000000000178, 61.87499999317203958, 0.000000000000000000 ) ) ;
#16732=CARTESIAN_POINT ( 'NONE',  ( 10.00000000000022382, 215.0000000000001421, 0.000000000000000000 ) ) ;
#16741=CARTESIAN_POINT ( 'NONE',  ( 9.832129032723420536, 146.1979166632526983, -5.676582343749999815 ) ) ;
#16747=CARTESIAN_POINT ( 'NONE',  ( 0.000000000000000000, 300.0000000000000000, 0.000000000000000000 ) ) ;
#16753=CARTESIAN_POINT ( 'NONE',  ( -5.676582343750006032, 124.4270833299193555, 9.832129032723418760 ) ) ;
#16758=CARTESIAN_POINT ( 'NONE',  ( 3.042071309553167069, 32.13541666325269119, -11.35316468749999785 ) ) ;
#16760=DIRECTION ( 'NONE',  ( -0.000000000000000000, 1.000000000000000000, -0.000000000000000000 ) ) ;
#16765=CARTESIAN_POINT ( 'NONE',  ( -2.485281374238572649, 298.2500000034139589, 6.000000000000002665 ) ) ;
#16768=CARTESIAN_POINT ( 'NONE',  ( -5.676582343750006032, 154.4270833299193555, 9.832129032723418760 ) ) ;
#16770=VECTOR ( 'NONE', #38071, 1000.000000000000000 ) ;
#16776=VECTOR ( 'NONE', #73248, 1000.000000000000000 ) ;
#16785=CARTESIAN_POINT ( 'NONE',  ( -6.000000000000003553, 298.0000000034140157, -2.485281374238571317 ) ) ;
#16787=CARTESIAN_POINT ( 'NONE',  ( -2.679491924311225848, 36.45833333333333570, -10.00000000000000178 ) ) ;
#16790=CARTESIAN_POINT ( 'NONE',  ( -6.000000000000003553, 299.9374999999999432, -2.485281374238571317 ) ) ;
#16791=CARTESIAN_POINT ( 'NONE',  ( 5.000000000000001776, 197.7083333265053966, -8.660254037844389075 ) ) ;
#16801=CARTESIAN_POINT ( 'NONE',  ( -8.660254037844390851, 167.9166666666666856, 4.999999999999998224 ) ) ;
#16805=CARTESIAN_POINT ( 'NONE',  ( 9.832129032723420536, 121.5104166632526841, -5.676582343749999815 ) ) ;
#16812=CARTESIAN_POINT ( 'NONE',  ( 9.255284998869608870, 224.6865538138296756, 3.831861534692823756 ) ) ;
#16813=CYLINDRICAL_SURFACE ( 'NONE', #54279, 10.00000000000000178 ) ;
#16819=CARTESIAN_POINT ( 'NONE',  ( 8.311093377946834337, 215.4687499965860411, 8.311093377946839666 ) ) ;
#16826=CARTESIAN_POINT ( 'NONE',  ( -11.35316468750000141, 98.28124999658602690, -1.390361679473963753E-15 ) ) ;
#16829=PLANE ( 'NONE',  #269 ) ;
#16833=CARTESIAN_POINT ( 'NONE',  ( -5.676582343749998039, 97.44791666325269830, -9.832129032723420536 ) ) ;
#16834=ORIENTED_EDGE ( 'NONE', *, *, #32959, .T. ) ;
#16838=CARTESIAN_POINT ( 'NONE',  ( 2.679491924311222739, 220.8333333265053966, 10.00000000000000355 ) ) ;
#16842=CARTESIAN_POINT ( 'NONE',  ( -8.311093377946841443, 93.90624999658599847, 8.311093377946834337 ) ) ;
#16845=CARTESIAN_POINT ( 'NONE',  ( 5.000000000000038192, 174.1666666666666856, 8.660254037844467234 ) ) ;
#16847=CARTESIAN_POINT ( 'NONE',  ( 8.660254037844385522, 186.4583333265053682, 5.000000000000005329 ) ) ;
#16851=CARTESIAN_POINT ( 'NONE',  ( -9.832129032723420536, 84.01041666325268409, 5.676582343749997150 ) ) ;
#16852=CARTESIAN_POINT ( 'NONE',  ( -6.676582343750001591, 291.4531250017069510, 0.000000000000000000 ) ) ;
#16855=CARTESIAN_POINT ( 'NONE',  ( 6.951808397369818766E-16, 217.0312499965860411, -11.35316468750000141 ) ) ;
#16857=CARTESIAN_POINT ( 'NONE',  ( -10.00000000000000000, 69.16666665983868256, -2.679491924311229845 ) ) ;
#16860=CARTESIAN_POINT ( 'NONE',  ( 5.676582343749993598, 214.9479166632526983, 9.832129032723422313 ) ) ;
#16862=CARTESIAN_POINT ( 'NONE',  ( -2.679491924311137030, 158.5416666666667425, 10.00000000000026823 ) ) ;
#16863=CARTESIAN_POINT ( 'NONE',  ( -4.721056650415998313, 298.5781250017069510, 4.721056650416000089 ) ) ;
#16864=VERTEX_POINT ( 'NONE', #32554 ) ;
#16865=CARTESIAN_POINT ( 'NONE',  ( 6.951808397369818766E-16, 207.3437499965860411, -11.35316468750000141 ) ) ;
#16874=EDGE_CURVE ( 'NONE', #3720, #9276, #45928, .T. ) ;
#16876=CARTESIAN_POINT ( 'NONE',  ( -7.320508075688778149, 18.12500000000000355, 7.320508075688769267 ) ) ;
#16877=AXIS2_PLACEMENT_3D ( 'NONE', #3086, #14757, #37418 ) ;
#16880=ORIENTED_EDGE ( 'NONE', *, *, #56330, .F. ) ;
#16887=CARTESIAN_POINT ( 'NONE',  ( 10.00000000000000178, 17.08333332650536818, -2.679491924311226736 ) ) ;
#16889=CARTESIAN_POINT ( 'NONE',  ( -1.377000000000000002, 255.7199999999997715, 5.684444333912885838 ) ) ;
#16900=CARTESIAN_POINT ( 'NONE',  ( -9.832129032723418760, 83.17708332991935549, -5.676582343750004256 ) ) ;
#16901=DIRECTION ( 'NONE',  ( -0.000000000000000000, 1.000000000000000000, -0.000000000000000000 ) ) ;
#16908=DIRECTION ( 'NONE',  ( 0.000000000000000000, 0.000000000000000000, 1.000000000000000000 ) ) ;
#16910=CARTESIAN_POINT ( 'NONE',  ( 5.676582343749993598, 194.9479166632526983, 9.832129032723422313 ) ) ;
#16916=CARTESIAN_POINT ( 'NONE',  ( 9.832129032723420536, 161.5104166632526983, -5.676582343749999815 ) ) ;
#16919=CARTESIAN_POINT ( 'NONE',  ( -2.679491924311077522, 206.4583333333333144, -10.00000000000007816 ) ) ;
#16920=CARTESIAN_POINT ( 'NONE',  ( -7.320508075688778149, 89.99999999317203958, 7.320508075688769267 ) ) ;
#16924=CARTESIAN_POINT ( 'NONE',  ( 9.832129032723420536, 51.19791666325268409, -5.676582343749999815 ) ) ;
#16930=CARTESIAN_POINT ( 'NONE',  ( -11.35316468749999785, 68.07291666325266988, -3.042071309553167513 ) ) ;
#16936=CARTESIAN_POINT ( 'NONE',  ( 11.35316468750000141, 65.78124999658602690, 0.000000000000000000 ) ) ;
#16938=CARTESIAN_POINT ( 'NONE',  ( -8.660254037844390851, 14.79166665983870210, 4.999999999999998224 ) ) ;
#16939=CARTESIAN_POINT ( 'NONE',  ( 5.676582343750001591, 171.6145833299193555, -9.832129032723420536 ) ) ;
#16941=CARTESIAN_POINT ( 'NONE',  ( -2.679491924311235618, 145.4166666598386826, 10.00000000000000000 ) ) ;
#16944=CARTESIAN_POINT ( 'NONE',  ( -2.085542519210945728E-15, 49.84374999658601268, 11.35316468750000141 ) ) ;
#16945=DIRECTION ( 'NONE',  ( -0.000000000000000000, 1.000000000000000000, -0.000000000000000000 ) ) ;
#16946=CARTESIAN_POINT ( 'NONE',  ( 3.042071309553167069, 181.8229166632526983, -11.35316468749999785 ) ) ;
#16953=CARTESIAN_POINT ( 'NONE',  ( -9.832129032723420536, 168.6979166632526983, 5.676582343749997150 ) ) ;
#16957=ADVANCED_FACE ( 'NONE', ( #40063 ), #44980, .T. ) ;
#16963=CARTESIAN_POINT ( 'NONE',  ( -5.676582343749998039, 112.7604166632526841, -9.832129032723420536 ) ) ;
#16983=( BOUNDED_CURVE ( )  B_SPLINE_CURVE ( 2, ( #56356, #5790, #68406, #28419, #51426, #67673, #74438, #22746, #40110, #57485, #51802, #15972, #40857 ),
 .UNSPECIFIED., .F., .F. ) 
 B_SPLINE_CURVE_WITH_KNOTS ( ( 3, 2, 2, 2, 2, 2, 3 ),
 ( 0.2336956521739130821, 0.2355072463768116131, 0.2373188405797101719, 0.2391304347826087029, 0.2409420289855072339, 0.2427536231884057927, 0.2445652173913043514 ),
 .UNSPECIFIED. ) 
 CURVE ( )  GEOMETRIC_REPRESENTATION_ITEM ( )  RATIONAL_B_SPLINE_CURVE ( ( 0.9999999999999994449, 0.9659258262890688673, 1.000000000000000000, 0.9659258262890683122, 1.000000000000000000, 0.9659258262890683122, 1.000000000000000000, 0.9659258262890683122, 1.000000000000000000, 0.9659258262890683122, 1.000000000000000000, 0.9659258262890683122, 1.000000000000000000 ) ) 
 REPRESENTATION_ITEM ( '' )  );
#16992=CARTESIAN_POINT ( 'NONE',  ( 5.000000000000001776, 120.8333333333333286, -8.660254037844389075 ) ) ;
#16994=CARTESIAN_POINT ( 'NONE',  ( -2.765530957081998586, 288.7968750017069510, 6.676582343750001591 ) ) ;
#17006=CARTESIAN_POINT ( 'NONE',  ( 6.123233995736767268E-16, 53.12499999317203958, -10.00000000000000178 ) ) ;
#17008=CARTESIAN_POINT ( 'NONE',  ( 5.676582343749993598, 14.94791666325268409, 9.832129032723422313 ) ) ;
#17010=CARTESIAN_POINT ( 'NONE',  ( 8.311093377946837890, 201.7187499965860411, -8.311093377946837890 ) ) ;
#17014=CARTESIAN_POINT ( 'NONE',  ( -8.660254037844529407, 42.08333333333342097, -5.000000000000087041 ) ) ;
#17018=CARTESIAN_POINT ( 'NONE',  ( -11.35316468749999785, 28.07291666325268054, -3.042071309553167513 ) ) ;
#17024=CARTESIAN_POINT ( 'NONE',  ( 9.832129032723416984, 15.36458332991935016, 5.676582343750006032 ) ) ;
#17026=CARTESIAN_POINT ( 'NONE',  ( 3.042071309553159519, 139.7395833299193555, 11.35316468750000141 ) ) ;
#17027=CARTESIAN_POINT ( 'NONE',  ( 2.679491924311222739, 95.83333332650535397, 10.00000000000000355 ) ) ;
#17035=DIRECTION ( 'NONE',  ( 0.000000000000000000, 0.000000000000000000, 1.000000000000000000 ) ) ;
#17036=CARTESIAN_POINT ( 'NONE',  ( -6.676582343750000703, 297.5156250017070079, 2.765530957082001251 ) ) ;
#17037=CARTESIAN_POINT ( 'NONE',  ( -9.832129032723418760, 122.8645833299193555, -5.676582343750004256 ) ) ;
#17050=CARTESIAN_POINT ( 'NONE',  ( 3.042071309553167069, 77.13541666325266988, -11.35316468749999785 ) ) ;
#17075=CARTESIAN_POINT ( 'NONE',  ( -2.485281374238227592, 292.1875000000000568, 6.000000000000345501 ) ) ;
#17081=CARTESIAN_POINT ( 'NONE',  ( -5.000000000000005329, 83.33333333333334281, 8.660254037844387298 ) ) ;
#17083=CARTESIAN_POINT ( 'NONE',  ( 6.000000000000001776, 289.5000000000000000, -7.347880794884121708E-16 ) ) ;
#17091=CARTESIAN_POINT ( 'NONE',  ( 0.000000000000000000, 300.0000000000000000, 0.000000000000000000 ) ) ;
#17093=CARTESIAN_POINT ( 'NONE',  ( 7.320508075688774596, 200.6250000000000000, -7.320508075688774596 ) ) ;
#17095=CARTESIAN_POINT ( 'NONE',  ( -8.311093377946841443, 174.2187499965860127, 8.311093377946830785 ) ) ;
#17101=CARTESIAN_POINT ( 'NONE',  ( 3.042071309553167069, 32.13541666325269119, -11.35316468749999785 ) ) ;
#17111=CARTESIAN_POINT ( 'NONE',  ( -2.679491924311225848, 63.33333332650536818, -10.00000000000000178 ) ) ;
#17117=CARTESIAN_POINT ( 'NONE',  ( 2.679491924311228956, 102.9166666598386826, -10.00000000000000000 ) ) ;
#17119=ORIENTED_EDGE ( 'NONE', *, *, #48588, .F. ) ;
#17123=CARTESIAN_POINT ( 'NONE',  ( 11.35316468749999785, 140.5729166632526983, 3.042071309553174174 ) ) ;
#17135=CARTESIAN_POINT ( 'NONE',  ( -9.832129032723418760, 133.1770833299193555, -5.676582343750004256 ) ) ;
#17139=CARTESIAN_POINT ( 'NONE',  ( -3.042071309553173730, 34.63541666325269119, 11.35316468749999785 ) ) ;
#17147=ADVANCED_FACE ( 'NONE', ( #42273 ), #30223, .T. ) ;
#17149=CARTESIAN_POINT ( 'NONE',  ( -6.000000000000001776, 297.0625000034140157, 0.000000000000000000 ) ) ;
#17154=CARTESIAN_POINT ( 'NONE',  ( -2.085542519210945728E-15, 154.8437499965860127, 11.35316468750000141 ) ) ;
#17170=CARTESIAN_POINT ( 'NONE',  ( 8.660254037844389075, 35.41666666666666430, -5.000000000000000000 ) ) ;
#17178=VECTOR ( 'NONE', #7929, 1000.000000000000000 ) ;
#17180=CARTESIAN_POINT ( 'NONE',  ( -2.679491924311226292, 8.333333326505366401, -10.00000000000000178 ) ) ;
#17184=CARTESIAN_POINT ( 'NONE',  ( -4.999999999999998224, 161.6666666666666856, -8.660254037844389075 ) ) ;
#17188=CARTESIAN_POINT ( 'NONE',  ( 9.832129032723416984, 125.6770833299193697, 5.676582343750006032 ) ) ;
#17198=DIRECTION ( 'NONE',  ( 0.000000000000000000, 0.000000000000000000, 1.000000000000000000 ) ) ;
#17201=CARTESIAN_POINT ( 'NONE',  ( -3.042071309553164404, 222.5520833299192986, -11.35316468749999963 ) ) ;
#17207=CARTESIAN_POINT ( 'NONE',  ( -11.35316468750000141, 108.4895833299193413, 3.042071309553159963 ) ) ;
#17212=CARTESIAN_POINT ( 'NONE',  ( -1.966770576099810657E-11, 61.25000000000153477, -9.999999999999998224 ) ) ;
#17214=CARTESIAN_POINT ( 'NONE',  ( -5.676582343750006032, 99.11458332991935549, 9.832129032723418760 ) ) ;
#17219=CARTESIAN_POINT ( 'NONE',  ( -5.000000000000005329, 225.2083333265053966, 8.660254037844387298 ) ) ;
#17222=CARTESIAN_POINT ( 'NONE',  ( 8.311093377946834337, 100.1562499965860127, 8.311093377946839666 ) ) ;
#17227=CARTESIAN_POINT ( 'NONE',  ( -10.00000000000000355, 194.5833333265053966, 2.679491924311223183 ) ) ;
#17230=CARTESIAN_POINT ( 'NONE',  ( -8.311093377946836114, 87.96874999658602690, -8.311093377946837890 ) ) ;
#17231=CARTESIAN_POINT ( 'NONE',  ( -4.721056650415998313, 289.5781250017069510, 4.721056650416000089 ) ) ;
#17234=CARTESIAN_POINT ( 'NONE',  ( 9.832129032723420536, 221.1979166632526983, -5.676582343749999815 ) ) ;
#17235=( BOUNDED_CURVE ( )  B_SPLINE_CURVE ( 2, ( #39027, #44313, #67327, #49215, #72224, #56381, #62395, #27695, #44685, #10722, #15624, #38664, #50704 ),
 .UNSPECIFIED., .F., .F. ) 
 B_SPLINE_CURVE_WITH_KNOTS ( ( 3, 2, 2, 2, 2, 2, 3 ),
 ( 2.056685274044849354, 2.061918634596133781, 2.067151995147418209, 2.072385355698702636, 2.077618716249987063, 2.082852076801271934, 2.088085437352556362 ),
 .UNSPECIFIED. ) 
 CURVE ( )  GEOMETRIC_REPRESENTATION_ITEM ( )  RATIONAL_B_SPLINE_CURVE ( ( 0.9999999999999895639, 0.9659258262890787483, 1.000000000000000000, 0.9659258262890683122, 1.000000000000000000, 0.9659258262890683122, 1.000000000000000000, 0.9659258262890683122, 1.000000000000000000, 0.9659258262890683122, 1.000000000000000000, 0.9659258262893356539, 0.9999999999997326583 ) ) 
 REPRESENTATION_ITEM ( '' )  );
#17238=CARTESIAN_POINT ( 'NONE',  ( 4.242640687119287435, 291.3750000000000000, 4.242640687119285658 ) ) ;
#17239=CARTESIAN_POINT ( 'NONE',  ( -2.085542519210945728E-15, 219.5312499965860411, 11.35316468750000141 ) ) ;
#17242=CARTESIAN_POINT ( 'NONE',  ( -6.676582343750001591, 295.4531250017069510, 0.000000000000000000 ) ) ;
#17245=CARTESIAN_POINT ( 'NONE',  ( -3.042071309553163960, 207.5520833299193271, -11.35316468749999963 ) ) ;
#17250=VECTOR ( 'NONE', #54362, 1000.000000000000000 ) ;
#17254=CARTESIAN_POINT ( 'NONE',  ( -5.000000000000005329, 33.33333333333333570, 8.660254037844387298 ) ) ;
#17265=CARTESIAN_POINT ( 'NONE',  ( 7.320508075688774596, 152.4999999931720538, -7.320508075688774596 ) ) ;
#17266=CARTESIAN_POINT ( 'NONE',  ( 1.226468279477575784E-15, 294.7031250017069510, 6.676582343750001591 ) ) ;
#17269=CARTESIAN_POINT ( 'NONE',  ( -4.242640687119285658, 289.1875000034139589, 4.242640687119287435 ) ) ;
#17278=CARTESIAN_POINT ( 'NONE',  ( 11.35316468749999963, 86.30208332991936970, -3.042071309553165293 ) ) ;
#17279=CARTESIAN_POINT ( 'NONE',  ( -3.673940397442060854E-16, 294.8125000034140157, -6.000000000000001776 ) ) ;
#17283=CARTESIAN_POINT ( 'NONE',  ( 4.999999999999995559, 69.16666666666667140, 8.660254037844392627 ) ) ;
#17284=ORIENTED_EDGE ( 'NONE', *, *, #3458, .T. ) ;
#17287=CARTESIAN_POINT ( 'NONE',  ( -11.35316468750000141, 203.2812499965860411, -1.390361679473963753E-15 ) ) ;
#17291=CARTESIAN_POINT ( 'NONE',  ( 6.951808397369818766E-16, 177.3437499965860411, -11.35316468750000141 ) ) ;
#17299=CARTESIAN_POINT ( 'NONE',  ( -2.085542519210945728E-15, 59.53124999658601979, 11.35316468750000141 ) ) ;
#17304=CARTESIAN_POINT ( 'NONE',  ( 11.35316468749999785, 65.57291666325269830, 3.042071309553174174 ) ) ;
#17309=CARTESIAN_POINT ( 'NONE',  ( 6.951808397369818766E-16, 57.03124999658601268, -11.35316468750000141 ) ) ;
#17312=CARTESIAN_POINT ( 'NONE',  ( 6.123233995736767268E-16, 13.12499999317203425, -10.00000000000000178 ) ) ;
#17313=CARTESIAN_POINT ( 'NONE',  ( -2.679491924311225848, 153.3333333265053682, -10.00000000000000178 ) ) ;
#17316=CARTESIAN_POINT ( 'NONE',  ( 11.35316468750000141, 51.09374999658601268, 0.000000000000000000 ) ) ;
#17319=CARTESIAN_POINT ( 'NONE',  ( 5.676582343750001591, 186.6145833299193839, -9.832129032723420536 ) ) ;
#17320=VERTEX_POINT ( 'NONE', #50824 ) ;
#17324=CARTESIAN_POINT ( 'NONE',  ( -5.676582343750006032, 179.1145833299193555, 9.832129032723418760 ) ) ;
#17330=CARTESIAN_POINT ( 'NONE',  ( -11.35316468750000141, 163.8020833299193555, 3.042071309553159963 ) ) ;
#17331=( BOUNDED_CURVE ( )  B_SPLINE_CURVE ( 2, ( #52828, #30551, #1160, #24868, #12454, #18122, #47887, #19583, #64517 ),
 .UNSPECIFIED., .F., .F. ) 
 B_SPLINE_CURVE_WITH_KNOTS ( ( 3, 2, 2, 2, 3 ),
 ( 0.6874999999999982236, 0.6979166666666648533, 0.7083333333333317050, 0.7187499999999983347, 0.7291666666666649643 ),
 .UNSPECIFIED. ) 
 CURVE ( )  GEOMETRIC_REPRESENTATION_ITEM ( )  RATIONAL_B_SPLINE_CURVE ( ( 1.000000000000012879, 0.9238795325112737489, 1.000000000000000000, 0.9238795325112867385, 1.000000000000000000, 0.9238795325112867385, 1.000000000000000000, 0.9238795325112989509, 0.9999999999999877875 ) ) 
 REPRESENTATION_ITEM ( '' )  );
#17334=CARTESIAN_POINT ( 'NONE',  ( -11.35316468750000141, 133.5937499965860127, -1.390361679473963753E-15 ) ) ;
#17341=EDGE_CURVE ( 'NONE', #65897, #24662, #20290, .T. ) ;
#17365=CARTESIAN_POINT ( 'NONE',  ( 1.226468279477575784E-15, 298.8593750017070079, 6.676582343750001591 ) ) ;
#17366=CARTESIAN_POINT ( 'NONE',  ( 2.679491924311222739, 128.9583333333333428, 10.00000000000000355 ) ) ;
#17368=CARTESIAN_POINT ( 'NONE',  ( -6.676582343750001591, 287.6093750017069510, 0.000000000000000000 ) ) ;
#17377=CARTESIAN_POINT ( 'NONE',  ( -6.676582343750001591, 299.5312500017070079, 0.000000000000000000 ) ) ;
#17381=CARTESIAN_POINT ( 'NONE',  ( -3.673940397442060854E-16, 291.8125000034140157, -6.000000000000001776 ) ) ;
#17383=CARTESIAN_POINT ( 'NONE',  ( 9.832129032723420536, 21.19791666325268409, -5.676582343749999815 ) ) ;
#17385=CARTESIAN_POINT ( 'NONE',  ( -5.676582343750006032, 224.4270833299193555, 9.832129032723418760 ) ) ;
#17386=CARTESIAN_POINT ( 'NONE',  ( 6.123233995736767268E-16, 218.1249999931720538, -10.00000000000000178 ) ) ;
#17388=CARTESIAN_POINT ( 'NONE',  ( -5.000000000000087930, 43.33333333333343518, 8.660254037844529407 ) ) ;
#17391=CARTESIAN_POINT ( 'NONE',  ( 3.042071309553159519, 19.73958332991934483, 11.35316468750000141 ) ) ;
#17394=CARTESIAN_POINT ( 'NONE',  ( -10.00000000000001066, 152.7083333333333428, 2.679491924311225404 ) ) ;
#17397=CARTESIAN_POINT ( 'NONE',  ( -2.085542519210945728E-15, 24.53124999658601624, 11.35316468750000141 ) ) ;
#17399=EDGE_CURVE ( 'NONE', #63756, #32479, #17434, .T. ) ;
#17400=CARTESIAN_POINT ( 'NONE',  ( 9.832129032723416984, 130.3645833299193555, 5.676582343750006032 ) ) ;
#17401=CARTESIAN_POINT ( 'NONE',  ( -8.660254037844390851, 104.7916666598386968, 4.999999999999998224 ) ) ;
#17407=CARTESIAN_POINT ( 'NONE',  ( -5.676582343749998039, 12.76041666325268409, -9.832129032723420536 ) ) ;
#17409=CARTESIAN_POINT ( 'NONE',  ( -10.00000000000000000, 154.1666666598387110, -2.679491924311229845 ) ) ;
#17410=CARTESIAN_POINT ( 'NONE',  ( 6.676582343750003368, 298.0156250017070079, -2.765530957081997254 ) ) ;
#17411=CARTESIAN_POINT ( 'NONE',  ( -11.35316468750000141, 143.4895833299193839, 3.042071309553159963 ) ) ;
#17421=CARTESIAN_POINT ( 'NONE',  ( 6.951808397369818766E-16, 87.34374999658602690, -11.35316468750000141 ) ) ;
#17434=( BOUNDED_CURVE ( )  B_SPLINE_CURVE ( 2, ( #59008, #41276, #36723, #47656, #7681, #19727, #52597, #65008, #70318 ),
 .UNSPECIFIED., .F., .F. ) 
 B_SPLINE_CURVE_WITH_KNOTS ( ( 3, 2, 2, 2, 3 ),
 ( 0.02083333333333103887, 0.03124999999999771363, 0.04166666666666438146, 0.05208333333333105969, 0.06249999999999773792 ),
 .UNSPECIFIED. ) 
 CURVE ( )  GEOMETRIC_REPRESENTATION_ITEM ( )  RATIONAL_B_SPLINE_CURVE ( ( 1.000000000000016653, 0.9238795325112698631, 1.000000000000000000, 0.9238795325112867385, 1.000000000000000000, 0.9238795325112867385, 1.000000000000000000, 0.9238795325113032808, 0.9999999999999834577 ) ) 
 REPRESENTATION_ITEM ( '' )  );
#17437=( BOUNDED_CURVE ( )  B_SPLINE_CURVE ( 2, ( #60209, #25501, #48514, #71520, #64768, #66245, #19844, #60585, #42851, #65868, #13071, #31549, #1421 ),
 .UNSPECIFIED., .F., .T. ) 
 B_SPLINE_CURVE_WITH_KNOTS ( ( 3, 2, 2, 2, 2, 2, 3 ),
 ( 2.150888710979840468, 2.156121240787547411, 2.161353770595253909, 2.166586300402960852, 2.171818830210667794, 2.177051360018374293, 2.182283889826081236 ),
 .UNSPECIFIED. ) 
 CURVE ( )  GEOMETRIC_REPRESENTATION_ITEM ( )  RATIONAL_B_SPLINE_CURVE ( ( 0.9999999999999978906, 0.9659258262890704216, 1.000000000000000000, 0.9659258262890683122, 1.000000000000000000, 0.9659258262890683122, 1.000000000000000000, 0.9659258262890683122, 1.000000000000000000, 0.9659258262890683122, 1.000000000000000000, 0.9659258262891539104, 0.9999999999999144018 ) ) 
 REPRESENTATION_ITEM ( '' )  );
#17454=CARTESIAN_POINT ( 'NONE',  ( -10.00000000000000000, 77.29166666666665719, -2.679491924311229845 ) ) ;
#17456=CARTESIAN_POINT ( 'NONE',  ( 8.311093377946834337, 65.46874999658601268, 8.311093377946839666 ) ) ;
#17457=CARTESIAN_POINT ( 'NONE',  ( -6.000000000000003553, 288.9375000000000000, -2.485281374238571317 ) ) ;
#17463=CARTESIAN_POINT ( 'NONE',  ( 1.102182119232618108E-15, 288.2500000000000000, 6.000000000000001776 ) ) ;
#17467=DIRECTION ( 'NONE',  ( -0.000000000000000000, 1.000000000000000000, -0.000000000000000000 ) ) ;
#17469=CARTESIAN_POINT ( 'NONE',  ( -10.00000000000000000, 207.2916666666666856, -2.679491924311229845 ) ) ;
#17471=CARTESIAN_POINT ( 'NONE',  ( -11.35316468750000141, 178.5937499965860411, -1.390361679473963753E-15 ) ) ;
#17472=CARTESIAN_POINT ( 'NONE',  ( -10.00000000000000355, 37.70833333333333570, 2.679491924311223183 ) ) ;
#17473=CARTESIAN_POINT ( 'NONE',  ( 10.00000000000000178, 177.0833333265053966, -2.679491924311226736 ) ) ;
#17478=CARTESIAN_POINT ( 'NONE',  ( 8.311093377946834337, 30.46874999658601979, 8.311093377946839666 ) ) ;
#17488=CARTESIAN_POINT ( 'NONE',  ( -8.660254037844390851, 64.79166665983871098, 4.999999999999998224 ) ) ;
#17495=CARTESIAN_POINT ( 'NONE',  ( 6.123233995736767268E-16, 103.1249999931720396, -10.00000000000000178 ) ) ;
#17496=ORIENTED_EDGE ( 'NONE', *, *, #41976, .F. ) ;
#17497=ORIENTED_EDGE ( 'NONE', *, *, #8504, .T. ) ;
#17499=CARTESIAN_POINT ( 'NONE',  ( -6.676582343750001591, 298.6093750017069510, 0.000000000000000000 ) ) ;
#17501=CARTESIAN_POINT ( 'NONE',  ( 10.00000000000000000, 41.66666665983870388, 2.679491924311235618 ) ) ;
#17502=CARTESIAN_POINT ( 'NONE',  ( -2.085542519210945728E-15, 149.5312499965860411, 11.35316468750000141 ) ) ;
#17503=CARTESIAN_POINT ( 'NONE',  ( -3.673940397442060854E-16, 297.7500000000000000, -6.000000000000001776 ) ) ;
#17512=CARTESIAN_POINT ( 'NONE',  ( -5.676582343749998039, 122.7604166632526841, -9.832129032723420536 ) ) ;
#17516=CARTESIAN_POINT ( 'NONE',  ( 5.676582343749993598, 30.26041666325268409, 9.832129032723422313 ) ) ;
#17518=CARTESIAN_POINT ( 'NONE',  ( 2.679491924311185880, 35.83333332650536107, 10.00000000000002487 ) ) ;
#17523=CARTESIAN_POINT ( 'NONE',  ( 2.485281374238571317, 297.7500000034140157, -6.000000000000003553 ) ) ;
#17527=CARTESIAN_POINT ( 'NONE',  ( 6.951808397369818766E-16, 152.3437499965860411, -11.35316468750000141 ) ) ;
#17532=ORIENTED_EDGE ( 'NONE', *, *, #59025, .T. ) ;
#17544=CARTESIAN_POINT ( 'NONE',  ( -5.000000000000005329, 210.2083333265053682, 8.660254037844387298 ) ) ;
#17546=CARTESIAN_POINT ( 'NONE',  ( -2.679491924311225848, 46.45833333333334281, -10.00000000000000178 ) ) ;
#17550=CARTESIAN_POINT ( 'NONE',  ( -5.000000000000005329, 35.20833332650536818, 8.660254037844387298 ) ) ;
#17560=CARTESIAN_POINT ( 'NONE',  ( 10.00000000000000178, 155.0000000000000000, 0.000000000000000000 ) ) ;
#17564=CARTESIAN_POINT ( 'NONE',  ( -5.676582343749998039, 122.7604166632526841, -9.832129032723420536 ) ) ;
#17569=CARTESIAN_POINT ( 'NONE',  ( 4.242640687119287435, 298.3750000000000000, 4.242640687119285658 ) ) ;
#17570=VERTEX_POINT ( 'NONE', #10360 ) ;
#17577=CARTESIAN_POINT ( 'NONE',  ( 7.320508075688771044, 16.24999999317203248, 7.320508075688775484 ) ) ;
#17584=CARTESIAN_POINT ( 'NONE',  ( 5.676582343749993598, 109.9479166632526983, 9.832129032723422313 ) ) ;
#17588=CARTESIAN_POINT ( 'NONE',  ( 10.00000000000016165, 40.20833333333342807, -2.679491924311269813 ) ) ;
#17590=CARTESIAN_POINT ( 'NONE',  ( -8.311093377946836114, 107.6562499965860127, -8.311093377946837890 ) ) ;
#17592=LINE ( 'NONE', #35340, #59654 ) ;
#17594=CARTESIAN_POINT ( 'NONE',  ( 2.679491924311222739, 215.8333333265053682, 10.00000000000000355 ) ) ;
#17597=CARTESIAN_POINT ( 'NONE',  ( 6.123233995736767268E-16, 143.1249999931720538, -10.00000000000000178 ) ) ;
#17598=CARTESIAN_POINT ( 'NONE',  ( 3.042071309553159519, 94.73958332991934128, 11.35316468750000141 ) ) ;
#17604=CARTESIAN_POINT ( 'NONE',  ( 8.660254037844385522, 201.4583333265053682, 5.000000000000005329 ) ) ;
#17607=CARTESIAN_POINT ( 'NONE',  ( -11.35316468749999785, 93.38541666325268409, -3.042071309553167957 ) ) ;
#17608=CARTESIAN_POINT ( 'NONE',  ( -6.676582343750001591, 288.4531250017069510, 0.000000000000000000 ) ) ;
#17611=CARTESIAN_POINT ( 'NONE',  ( 8.311093377946837890, 226.4062499965860411, -8.311093377946837890 ) ) ;
#17612=ORIENTED_EDGE ( 'NONE', *, *, #68094, .F. ) ;
#17615=CARTESIAN_POINT ( 'NONE',  ( -11.35316468750000141, 223.2812499965860127, -1.390361679473963753E-15 ) ) ;
#17616=CARTESIAN_POINT ( 'NONE',  ( 8.660254037844389075, 47.29166665983870388, -5.000000000000000000 ) ) ;
#17617=CYLINDRICAL_SURFACE ( 'NONE', #18567, 10.00000000000000178 ) ;
#17618=CARTESIAN_POINT ( 'NONE',  ( -4.088227598258586603E-16, 295.2031250017069510, -6.676582343750001591 ) ) ;
#17621=CARTESIAN_POINT ( 'NONE',  ( -3.042071309553173730, 209.6354166632526699, 11.35316468749999785 ) ) ;
#17629=CARTESIAN_POINT ( 'NONE',  ( -2.679491924311225848, 21.45833333333333925, -10.00000000000000178 ) ) ;
#17634=DIRECTION ( 'NONE',  ( -0.8660254037844696828, 0.4999999999999462097, -0.000000000000000000 ) ) ;
#17635=ADVANCED_FACE ( 'NONE', ( #29202 ), #40577, .F. ) ;
#17639=CARTESIAN_POINT ( 'NONE',  ( 8.660254037844385522, 151.4583333265053682, 5.000000000000005329 ) ) ;
#17640=CARTESIAN_POINT ( 'NONE',  ( -4.721056650415998313, 296.5781250017069510, 4.721056650416000089 ) ) ;
#17649=CARTESIAN_POINT ( 'NONE',  ( 11.35316468750000141, 86.09374999658601268, 0.000000000000000000 ) ) ;
#17654=CARTESIAN_POINT ( 'NONE',  ( 10.00000000000000355, 70.20833333333331439, -2.679491924311227180 ) ) ;
#17658=CARTESIAN_POINT ( 'NONE',  ( -8.660254037844387298, 178.9583333265053682, -5.000000000000004441 ) ) ;
#17659=CARTESIAN_POINT ( 'NONE',  ( -2.085542519210945728E-15, 204.5312499965860411, 11.35316468750000141 ) ) ;
#17665=CARTESIAN_POINT ( 'NONE',  ( -11.35316468750000141, 178.8020833299193271, 3.042071309553159963 ) ) ;
#17669=CARTESIAN_POINT ( 'NONE',  ( 6.123233995736767268E-16, 88.12499999317203958, -10.00000000000000178 ) ) ;
#17673=CARTESIAN_POINT ( 'NONE',  ( -5.676582343750006032, 74.11458332991935549, 9.832129032723418760 ) ) ;
#17675=( BOUNDED_CURVE ( )  B_SPLINE_CURVE ( 2, ( #66774, #44143, #24268, #67156, #26388, #35977, #7301, #19992, #1652, #43000, #58996, #37741, #14328 ),
 .UNSPECIFIED., .F., .F. ) 
 B_SPLINE_CURVE_WITH_KNOTS ( ( 3, 2, 2, 2, 2, 2, 3 ),
 ( 0.2040931733865910258, 0.2093271569598113002, 0.2145611405330315191, 0.2197951241062517935, 0.2250291076794720402, 0.2302630912526922591, 0.2354970748259125335 ),
 .UNSPECIFIED. ) 
 CURVE ( )  GEOMETRIC_REPRESENTATION_ITEM ( )  RATIONAL_B_SPLINE_CURVE ( ( 0.9999999999999992228, 0.9659258262890690894, 1.000000000000000000, 0.9659258262890683122, 1.000000000000000000, 0.9659258262890683122, 1.000000000000000000, 0.9659258262890683122, 1.000000000000000000, 0.9659258262890683122, 1.000000000000000000, 0.9659258262891544655, 0.9999999999999138467 ) ) 
 REPRESENTATION_ITEM ( '' )  );
#17679=CARTESIAN_POINT ( 'NONE',  ( -11.35316468750000141, 68.28124999658602690, -1.390361679473963753E-15 ) ) ;
#17684=CARTESIAN_POINT ( 'NONE',  ( 11.35316468749999785, 65.57291666325268409, 3.042071309553174174 ) ) ;
#17688=CARTESIAN_POINT ( 'NONE',  ( -10.00000000000000178, 154.3749999931720254, -1.224646799147353454E-15 ) ) ;
#17690=CARTESIAN_POINT ( 'NONE',  ( -1.836970198721029983E-15, 55.62499999317203958, 10.00000000000000178 ) ) ;
#17691=CARTESIAN_POINT ( 'NONE',  ( 6.951808397369818766E-16, 42.34374999658601979, -11.35316468750000141 ) ) ;
#17693=CARTESIAN_POINT ( 'NONE',  ( 8.311093377946834337, 185.1562499965860411, 8.311093377946839666 ) ) ;
#17696=CARTESIAN_POINT ( 'NONE',  ( 10.00000000000000178, 161.8749999931720254, 0.000000000000000000 ) ) ;
#17698=CARTESIAN_POINT ( 'NONE',  ( 8.311093377946834337, 180.1562499965860127, 8.311093377946839666 ) ) ;
#17706=CARTESIAN_POINT ( 'NONE',  ( 11.35316468749999785, 165.8854166632526130, 3.042071309553174174 ) ) ;
#17709=CARTESIAN_POINT ( 'NONE',  ( 9.832129032723420536, 126.5104166632526841, -5.676582343749999815 ) ) ;
#17710=CARTESIAN_POINT ( 'NONE',  ( 0.000000000000000000, 300.0000000000000000, 10.00000000000000178 ) ) ;
#17723=CARTESIAN_POINT ( 'NONE',  ( 0.000000000000000000, 300.0000000000000000, 0.000000000000000000 ) ) ;
#17738=CARTESIAN_POINT ( 'NONE',  ( -2.765530957081998142, 298.7968750017070079, 6.676582343750000703 ) ) ;
#17739=CARTESIAN_POINT ( 'NONE',  ( 5.000000000000001776, 135.8333333333333428, -8.660254037844389075 ) ) ;
#17741=CARTESIAN_POINT ( 'NONE',  ( 0.7835476670742943517, 225.9999999999999716, 9.977056579405376269 ) ) ;
#17753=DIRECTION ( 'NONE',  ( -0.000000000000000000, 1.000000000000000000, -0.000000000000000000 ) ) ;
#17758=CARTESIAN_POINT ( 'NONE',  ( 8.311093377946837890, 26.40624999658601268, -8.311093377946837890 ) ) ;
#17760=CARTESIAN_POINT ( 'NONE',  ( -8.311093377946836114, 217.9687499965860127, -8.311093377946837890 ) ) ;
#17766=CARTESIAN_POINT ( 'NONE',  ( -2.085542519210945728E-15, 24.53124999658601624, 11.35316468750000141 ) ) ;
#17772=CARTESIAN_POINT ( 'NONE',  ( -3.042071309553173730, 19.32291666325268409, 11.35316468749999785 ) ) ;
#17775=CARTESIAN_POINT ( 'NONE',  ( -2.085542519210945728E-15, 139.5312499965860411, 11.35316468750000141 ) ) ;
#17778=CARTESIAN_POINT ( 'NONE',  ( -2.679491924311235618, 110.4166666598387110, 10.00000000000000000 ) ) ;
#17780=CARTESIAN_POINT ( 'NONE',  ( 2.679491924311075302, 170.8333333265053398, 10.00000000000008704 ) ) ;
#17783=VERTEX_POINT ( 'NONE', #47015 ) ;
#17784=CARTESIAN_POINT ( 'NONE',  ( -9.832129032723420536, 14.01041666325268409, 5.676582343749997150 ) ) ;
#17787=CARTESIAN_POINT ( 'NONE',  ( -4.721056650415999201, 296.3281250017069510, -4.721056650415999201 ) ) ;
#17788=CARTESIAN_POINT ( 'NONE',  ( 11.35316468749999785, 135.5729166632526983, 3.042071309553174174 ) ) ;
#17789=DIRECTION ( 'NONE',  ( 0.000000000000000000, 0.000000000000000000, 1.000000000000000000 ) ) ;
#17799=CARTESIAN_POINT ( 'NONE',  ( 9.832129032723416984, 95.67708332991935549, 5.676582343750006032 ) ) ;
#17821=AXIS2_PLACEMENT_3D ( 'NONE', #71471, #29650, #25451 ) ;
#17826=EDGE_CURVE ( 'NONE', #3534, #45065, #48272, .T. ) ;
#17827=VERTEX_POINT ( 'NONE', #25006 ) ;
#17833=CARTESIAN_POINT ( 'NONE',  ( 6.123233995736767268E-16, 96.25000000000000000, -10.00000000000000178 ) ) ;
#17835=CARTESIAN_POINT ( 'NONE',  ( 5.676582343749993598, 55.26041666325268409, 9.832129032723422313 ) ) ;
#17836=CARTESIAN_POINT ( 'NONE',  ( 4.242640687119287435, 288.3750000000000000, 4.242640687119285658 ) ) ;
#17841=CARTESIAN_POINT ( 'NONE',  ( 10.00000000000001243, 85.00000000000000000, 0.000000000000000000 ) ) ;
#17846=CARTESIAN_POINT ( 'NONE',  ( -5.000000000000005329, 198.3333333333333428, 8.660254037844387298 ) ) ;
#17848=CARTESIAN_POINT ( 'NONE',  ( 8.311093377946834337, 185.4687499965860127, 8.311093377946839666 ) ) ;
#17854=CARTESIAN_POINT ( 'NONE',  ( -11.35316468750000141, 38.80208332991934839, 3.042071309553159963 ) ) ;
#17857=VECTOR ( 'NONE', #23395, 1000.000000000000000 ) ;
#17860=CARTESIAN_POINT ( 'NONE',  ( -4.999999999999987566, 101.6666666666666572, -8.660254037844371311 ) ) ;
#17863=CARTESIAN_POINT ( 'NONE',  ( -8.660254037844390851, 74.79166665983871098, 4.999999999999998224 ) ) ;
#17870=EDGE_LOOP ( 'NONE', ( #1340, #28682, #11487, #28078 ) ) ;
#17871=CARTESIAN_POINT ( 'NONE',  ( 1.881637226502129035E-11, 6.249999999998538058, -10.00000000000000178 ) ) ;
#17872=CARTESIAN_POINT ( 'NONE',  ( 4.721056650415999201, 299.2343750017069510, -4.721056650415999201 ) ) ;
#17873=CARTESIAN_POINT ( 'NONE',  ( 1.102182119232618108E-15, 290.3125000034140157, 6.000000000000001776 ) ) ;
#17874=CARTESIAN_POINT ( 'NONE',  ( -2.679491924311529161, 88.54166666666665719, 9.999999999999831246 ) ) ;
#17875=CARTESIAN_POINT ( 'NONE',  ( -9.832129032723418760, 157.8645833299193839, -5.676582343750004256 ) ) ;
#17876=CARTESIAN_POINT ( 'NONE',  ( 7.320508075688760385, 104.3750000000000000, 7.320508075688763938 ) ) ;
#17887=CARTESIAN_POINT ( 'NONE',  ( -3.042071309553163960, 127.5520833299193555, -11.35316468749999963 ) ) ;
#17891=CARTESIAN_POINT ( 'NONE',  ( -2.085542519210945728E-15, 54.84374999658601979, 11.35316468750000141 ) ) ;
#17895=( BOUNDED_CURVE ( )  B_SPLINE_CURVE ( 2, ( #63678, #57672, #68599, #34294, #22192, #33924, #68976, #21817, #45216, #74637, #33548, #44848, #56551 ),
 .UNSPECIFIED., .F., .F. ) 
 B_SPLINE_CURVE_WITH_KNOTS ( ( 3, 2, 2, 2, 2, 2, 3 ),
 ( 0.3206521739130435145, 0.3224637681159420732, 0.3242753623188406320, 0.3260869565217391353, 0.3278985507246376940, 0.3297101449275362528, 0.3315217391304347561 ),
 .UNSPECIFIED. ) 
 CURVE ( )  GEOMETRIC_REPRESENTATION_ITEM ( )  RATIONAL_B_SPLINE_CURVE ( ( 0.9999999999999990008, 0.9659258262890693114, 1.000000000000000000, 0.9659258262890683122, 1.000000000000000000, 0.9659258262890683122, 1.000000000000000000, 0.9659258262890683122, 1.000000000000000000, 0.9659258262890683122, 1.000000000000000000, 0.9659258262890683122, 1.000000000000000000 ) ) 
 REPRESENTATION_ITEM ( '' )  );
#17900=CARTESIAN_POINT ( 'NONE',  ( -2.485281374238572649, 295.2500000034139589, 6.000000000000002665 ) ) ;
#17911=ADVANCED_FACE ( 'NONE', ( #22704, #4630 ), #50635, .T. ) ;
#17924=CARTESIAN_POINT ( 'NONE',  ( 8.660254037844389075, 50.41666666666667140, -5.000000000000000000 ) ) ;
#17928=CARTESIAN_POINT ( 'NONE',  ( -6.000000000000001776, 299.0000000000000000, 0.000000000000000000 ) ) ;
#17930=CARTESIAN_POINT ( 'NONE',  ( 6.123233995736767268E-16, 198.1249999931720538, -10.00000000000000178 ) ) ;
#17938=CARTESIAN_POINT ( 'NONE',  ( 10.00000000000000000, 164.7916666666666572, 2.679491924311236062 ) ) ;
#17942=CARTESIAN_POINT ( 'NONE',  ( 8.311093377946834337, 135.4687499965860411, 8.311093377946839666 ) ) ;
#17943=CARTESIAN_POINT ( 'NONE',  ( 1.102182119232618108E-15, 294.3125000034140157, 6.000000000000001776 ) ) ;
#17949=CARTESIAN_POINT ( 'NONE',  ( -9.832129032723418760, 3.177083329919349719, -5.676582343750004256 ) ) ;
#17953=CARTESIAN_POINT ( 'NONE',  ( 2.679491924311222739, 20.83333332650536462, 10.00000000000000355 ) ) ;
#17959=CARTESIAN_POINT ( 'NONE',  ( 8.311093377946837890, 111.4062499965860269, -8.311093377946837890 ) ) ;
#17965=CARTESIAN_POINT ( 'NONE',  ( 8.311093377946834337, 115.1562499965859985, 8.311093377946839666 ) ) ;
#17966=ORIENTED_EDGE ( 'NONE', *, *, #23867, .T. ) ;
#17969=CARTESIAN_POINT ( 'NONE',  ( -10.00000000000000178, 219.3749999931720538, -1.224646799147353454E-15 ) ) ;
#17973=CARTESIAN_POINT ( 'NONE',  ( 9.832129032723416984, 100.3645833299193697, 5.676582343750006032 ) ) ;
#17978=CARTESIAN_POINT ( 'NONE',  ( -10.00000000000000178, 189.3749999931720254, -1.224646799147353454E-15 ) ) ;
#17980=DIRECTION ( 'NONE',  ( -0.000000000000000000, 1.000000000000000000, -0.000000000000000000 ) ) ;
#17982=CARTESIAN_POINT ( 'NONE',  ( 3.042071309553159519, 95.05208332991935549, 11.35316468750000141 ) ) ;
#17986=CARTESIAN_POINT ( 'NONE',  ( -8.311093377946836114, 2.968749996586016238, -8.311093377946837890 ) ) ;
#17990=CARTESIAN_POINT ( 'NONE',  ( 9.832129032723416984, 220.3645833299193839, 5.676582343750006032 ) ) ;
#17992=CARTESIAN_POINT ( 'NONE',  ( 5.000000000000001776, 47.70833332650536818, -8.660254037844389075 ) ) ;
#17993=CARTESIAN_POINT ( 'NONE',  ( -8.660254037844390851, 99.79166665983871098, 4.999999999999998224 ) ) ;
#17994=CARTESIAN_POINT ( 'NONE',  ( 6.676582343750001591, 294.9531250017069510, -8.176455196517173205E-16 ) ) ;
#17997=CARTESIAN_POINT ( 'NONE',  ( 3.042071309553159519, 215.0520833299193555, 11.35316468750000141 ) ) ;
#18004=VERTEX_POINT ( 'NONE', #74022 ) ;
#18009=CARTESIAN_POINT ( 'NONE',  ( -10.00000000000000355, 22.70833333333333215, 2.679491924311223183 ) ) ;
#18019=CARTESIAN_POINT ( 'NONE',  ( 1.226468279477575784E-15, 296.7031250017070079, 6.676582343750001591 ) ) ;
#18029=CARTESIAN_POINT ( 'NONE',  ( -11.35316468750000141, 98.59374999658601268, -1.390361679473963753E-15 ) ) ;
#18034=CARTESIAN_POINT ( 'NONE',  ( 6.123233995736767268E-16, 56.25000000000000000, -10.00000000000000178 ) ) ;
#18038=MANIFOLD_SOLID_BREP ( 'Cut-Extrude1', #33445 ) ;
#18040=CARTESIAN_POINT ( 'NONE',  ( -9.832129032723418760, 217.8645833299193839, -5.676582343750004256 ) ) ;
#18044=CARTESIAN_POINT ( 'NONE',  ( 6.951808397369818766E-16, 187.3437499965860127, -11.35316468750000141 ) ) ;
#18047=CARTESIAN_POINT ( 'NONE',  ( -2.679491924311234730, 108.5416666666666714, 9.999999999999996447 ) ) ;
#18051=CARTESIAN_POINT ( 'NONE',  ( -11.35316468750000141, 63.28124999658601979, -1.390361679473963753E-15 ) ) ;
#18057=CARTESIAN_POINT ( 'NONE',  ( 3.042071309553167069, 76.82291666325269830, -11.35316468749999785 ) ) ;
#18062=CARTESIAN_POINT ( 'NONE',  ( 9.832129032723416984, 55.36458332991934839, 5.676582343750006032 ) ) ;
#18064=CARTESIAN_POINT ( 'NONE',  ( -2.679491924311217410, 13.33333332650536640, -10.00000000000000711 ) ) ;
#18065=CARTESIAN_POINT ( 'NONE',  ( 8.660254037844389075, 152.2916666598387110, -5.000000000000000000 ) ) ;
#18068=CARTESIAN_POINT ( 'NONE',  ( 8.311093377946834337, 45.46874999658601979, 8.311093377946839666 ) ) ;
#18070=CARTESIAN_POINT ( 'NONE',  ( -11.35316468750000141, 183.4895833299193839, 3.042071309553159963 ) ) ;
#18071=ORIENTED_EDGE ( 'NONE', *, *, #44909, .T. ) ;
#18076=CARTESIAN_POINT ( 'NONE',  ( 9.832129032723416984, 185.3645833299193555, 5.676582343750006032 ) ) ;
#18082=CARTESIAN_POINT ( 'NONE',  ( -9.832129032723418760, 163.1770833299193839, -5.676582343750004256 ) ) ;
#18085=CARTESIAN_POINT ( 'NONE',  ( -5.676582343749998039, 127.7604166632526841, -9.832129032723420536 ) ) ;
#18093=( BOUNDED_CURVE ( )  B_SPLINE_CURVE ( 2, ( #1973, #58960, #24232, #12907, #41597, #6161, #47980, #35575, #516, #69905, #58232, #6531, #63864 ),
 .UNSPECIFIED., .F., .F. ) 
 B_SPLINE_CURVE_WITH_KNOTS ( ( 3, 2, 2, 2, 2, 2, 3 ),
 ( 0.4402173913043478382, 0.4420289855072463969, 0.4438405797101449002, 0.4456521739130434590, 0.4474637681159420177, 0.4492753623188405765, 0.4510869565217391353 ),
 .UNSPECIFIED. ) 
 CURVE ( )  GEOMETRIC_REPRESENTATION_ITEM ( )  RATIONAL_B_SPLINE_CURVE ( ( 1.000000000000000000, 0.9659258262890683122, 1.000000000000000000, 0.9659258262890683122, 1.000000000000000000, 0.9659258262890683122, 1.000000000000000000, 0.9659258262890683122, 1.000000000000000000, 0.9659258262890683122, 1.000000000000000000, 0.9659258262890683122, 1.000000000000000000 ) ) 
 REPRESENTATION_ITEM ( '' )  );
#18107=CARTESIAN_POINT ( 'NONE',  ( -8.660254037844545394, 157.0833333333334565, -5.000000000000096811 ) ) ;
#18117=CARTESIAN_POINT ( 'NONE',  ( -2.765530957081996810, 298.4218750017068942, -6.676582343750002480 ) ) ;
#18118=CARTESIAN_POINT ( 'NONE',  ( 8.660254037844385522, 129.5833333333333144, 5.000000000000005329 ) ) ;
#18122=CARTESIAN_POINT ( 'NONE',  ( 6.000000000000003553, 290.5000000034140726, 2.485281374238571317 ) ) ;
#18135=CARTESIAN_POINT ( 'NONE',  ( 3.042071309553167069, 31.82291666325268054, -11.35316468749999785 ) ) ;
#18136=CARTESIAN_POINT ( 'NONE',  ( 2.679491924311317330, 26.04166666666685259, -10.00000000000032863 ) ) ;
#18137=CARTESIAN_POINT ( 'NONE',  ( -11.35316468749999785, 218.3854166632526415, -3.042071309553167513 ) ) ;
#18144=CARTESIAN_POINT ( 'NONE',  ( -9.832129032723418760, 22.86458332991934839, -5.676582343750004256 ) ) ;
#18148=DIRECTION ( 'NONE',  ( -0.000000000000000000, 1.000000000000000000, -0.000000000000000000 ) ) ;
#18150=CARTESIAN_POINT ( 'NONE',  ( 6.951808397369818766E-16, 17.03124999658601624, -11.35316468750000141 ) ) ;
#18152=CARTESIAN_POINT ( 'NONE',  ( 9.832129032723416984, 145.3645833299193555, 5.676582343750006032 ) ) ;
#18153=CARTESIAN_POINT ( 'NONE',  ( -2.679491924311225848, 113.3333333265053682, -10.00000000000000178 ) ) ;
#18157=ORIENTED_EDGE ( 'NONE', *, *, #39189, .F. ) ;
#18158=CARTESIAN_POINT ( 'NONE',  ( 3.042071309553159519, 15.05208332991935194, 11.35316468750000141 ) ) ;
#18161=CARTESIAN_POINT ( 'NONE',  ( -6.676582343750001591, 297.4531250017069510, 0.000000000000000000 ) ) ;
#18163=CARTESIAN_POINT ( 'NONE',  ( 9.832129032723420536, 146.1979166632526983, -5.676582343749999815 ) ) ;
#18174=CARTESIAN_POINT ( 'NONE',  ( 3.042071309553159519, 85.05208332991934128, 11.35316468750000141 ) ) ;
#18193=ADVANCED_FACE ( 'NONE', ( #52141 ), #46467, .T. ) ;
#18207=CARTESIAN_POINT ( 'NONE',  ( -10.00000000000000178, 97.50000000000000000, -1.224646799147353454E-15 ) ) ;
#18209=CARTESIAN_POINT ( 'NONE',  ( 9.832129032723420536, 56.51041666325268409, -5.676582343749999815 ) ) ;
#18210=CARTESIAN_POINT ( 'NONE',  ( -2.485281374238571761, 289.8125000000000000, -6.000000000000003553 ) ) ;
#18211=EDGE_LOOP ( 'NONE', ( #19624, #21443, #8502, #60721 ) ) ;
#18212=( BOUNDED_CURVE ( )  B_SPLINE_CURVE ( 2, ( #21347, #55327, #14929, #16050, #3262, #56071, #4018, #27008, #49652 ),
 .UNSPECIFIED., .F., .F. ) 
 B_SPLINE_CURVE_WITH_KNOTS ( ( 3, 2, 2, 2, 3 ),
 ( 0.6458333333333314830, 0.6562499999999981126, 0.6666666666666647423, 0.6770833333333315940, 0.6874999999999982236 ),
 .UNSPECIFIED. ) 
 CURVE ( )  GEOMETRIC_REPRESENTATION_ITEM ( )  RATIONAL_B_SPLINE_CURVE ( ( 1.000000000000013767, 0.9238795325112729717, 1.000000000000000000, 0.9238795325112867385, 1.000000000000000000, 0.9238795325112867385, 1.000000000000000000, 0.9238795325112997281, 0.9999999999999870104 ) ) 
 REPRESENTATION_ITEM ( '' )  );
#18214=EDGE_CURVE ( 'NONE', #44928, #27622, #27564, .T. ) ;
#18217=CARTESIAN_POINT ( 'NONE',  ( 10.00000000000001066, 85.20833333333337123, -2.679491924311228956 ) ) ;
#18221=CARTESIAN_POINT ( 'NONE',  ( 8.660254037844385522, 219.5833333333333428, 5.000000000000005329 ) ) ;
#18223=CARTESIAN_POINT ( 'NONE',  ( 5.676582343750001591, 186.9270833299193555, -9.832129032723420536 ) ) ;
#18230=CARTESIAN_POINT ( 'NONE',  ( 9.832129032723416984, 30.67708332991935194, 5.676582343750006032 ) ) ;
#18233=CARTESIAN_POINT ( 'NONE',  ( 2.679491924311184103, 11.04166666666667140, -10.00000000000002487 ) ) ;
#18235=CARTESIAN_POINT ( 'NONE',  ( -2.679491924311226292, 58.33333332650537528, -10.00000000000000178 ) ) ;
#18237=CARTESIAN_POINT ( 'NONE',  ( 10.00000000000000178, 76.87499999317203958, 0.000000000000000000 ) ) ;
#18240=CARTESIAN_POINT ( 'NONE',  ( 1.567784982238203817E-13, 73.75000000000002842, 10.00000000000000533 ) ) ;
#18241=CARTESIAN_POINT ( 'NONE',  ( 6.123233995736767268E-16, 48.12499999317203958, -10.00000000000000178 ) ) ;
#18243=ORIENTED_EDGE ( 'NONE', *, *, #39807, .F. ) ;
#18245=CARTESIAN_POINT ( 'NONE',  ( -2.765530957081998586, 296.7968750017070079, 6.676582343750001591 ) ) ;
#18248=CARTESIAN_POINT ( 'NONE',  ( 8.311093377946834337, 160.1562499965860411, 8.311093377946839666 ) ) ;
#18256=AXIS2_PLACEMENT_3D ( 'NONE', #56975, #39614, #38872 ) ;
#18258=CARTESIAN_POINT ( 'NONE',  ( 3.042071309553167513, 142.1354166632526415, -11.35316468749999785 ) ) ;
#18260=CARTESIAN_POINT ( 'NONE',  ( -4.242640687119286547, 290.8750000000000000, -4.242640687119286547 ) ) ;
#18262=EDGE_CURVE ( 'NONE', #42176, #2370, #13960, .T. ) ;
#18263=CARTESIAN_POINT ( 'NONE',  ( 11.35316468749999963, 51.30208332991936260, -3.042071309553165293 ) ) ;
#18265=DIRECTION ( 'NONE',  ( 0.000000000000000000, 0.000000000000000000, 1.000000000000000000 ) ) ;
#18268=AXIS2_PLACEMENT_3D ( 'NONE', #45319, #16632, #4974 ) ;
#18270=CARTESIAN_POINT ( 'NONE',  ( -3.673940397442060854E-16, 293.8125000034140157, -6.000000000000001776 ) ) ;
#18281=ORIENTED_EDGE ( 'NONE', *, *, #58228, .F. ) ;
#18293=CARTESIAN_POINT ( 'NONE',  ( 6.123233995736767268E-16, 43.12499999317203248, -10.00000000000000178 ) ) ;
#18294=CARTESIAN_POINT ( 'NONE',  ( 2.679491924311228956, 61.04166666666665719, -10.00000000000000000 ) ) ;
#18296=CARTESIAN_POINT ( 'NONE',  ( 4.242640687119285658, 299.6250000000000000, -4.242640687119286547 ) ) ;
#18297=DIRECTION ( 'NONE',  ( -0.000000000000000000, 1.000000000000000000, -0.000000000000000000 ) ) ;
#18299=VERTEX_POINT ( 'NONE', #66037 ) ;
#18304=CARTESIAN_POINT ( 'NONE',  ( 8.660254037844371311, 89.58333333333332860, 4.999999999999997335 ) ) ;
#18308=DIRECTION ( 'NONE',  ( 0.8660254037844389297, 0.4999999999999994449, -0.000000000000000000 ) ) ;
#18309=CARTESIAN_POINT ( 'NONE',  ( -2.679491924311225848, 176.4583333333333428, -10.00000000000000178 ) ) ;
#18313=CARTESIAN_POINT ( 'NONE',  ( 6.951808397369818766E-16, 137.3437499965860127, -11.35316468750000141 ) ) ;
#18324=CARTESIAN_POINT ( 'NONE',  ( -8.660254037844390851, 34.79166665983870388, 4.999999999999998224 ) ) ;
#18333=CARTESIAN_POINT ( 'NONE',  ( 2.250000000000000444, 283.9999999999998863, 5.427273995025124975 ) ) ;
#18334=CARTESIAN_POINT ( 'NONE',  ( -3.220591000267885917, 225.9999999999999432, 9.489952148308894664 ) ) ;
#18338=CARTESIAN_POINT ( 'NONE',  ( 6.951808397369818766E-16, 112.0312499965860269, -11.35316468750000141 ) ) ;
#18342=CARTESIAN_POINT ( 'NONE',  ( 7.347880794884121708E-16, 300.0000000000000000, -6.000000000000001776 ) ) ;
#18345=CARTESIAN_POINT ( 'NONE',  ( -4.999999999999997335, 181.6666666666666856, -8.660254037844387298 ) ) ;
#18346=CARTESIAN_POINT ( 'NONE',  ( -5.676582343749998039, 107.4479166632526983, -9.832129032723420536 ) ) ;
#18350=CARTESIAN_POINT ( 'NONE',  ( 4.999999999999996447, 49.16666666666667140, 8.660254037844394404 ) ) ;
#18353=CARTESIAN_POINT ( 'NONE',  ( 6.123233995736767268E-16, 198.1249999931720538, -10.00000000000000178 ) ) ;
#18356=CARTESIAN_POINT ( 'NONE',  ( -5.676582343749998039, 82.76041666325268409, -9.832129032723420536 ) ) ;
#18360=CARTESIAN_POINT ( 'NONE',  ( 11.35316468750000141, 6.093749996586017126, 0.000000000000000000 ) ) ;
#18364=CARTESIAN_POINT ( 'NONE',  ( -8.311093377946841443, 223.9062499965860411, 8.311093377946834337 ) ) ;
#18366=CYLINDRICAL_SURFACE ( 'NONE', #45870, 10.00000000000000178 ) ;
#18368=CARTESIAN_POINT ( 'NONE',  ( -2.765530957081998586, 294.6406250017069510, 6.676582343750001591 ) ) ;
#18371=CARTESIAN_POINT ( 'NONE',  ( 11.35316468750000141, 206.0937499965860411, 0.000000000000000000 ) ) ;
#18380=CARTESIAN_POINT ( 'NONE',  ( 8.660254037844385522, 29.58333333333333570, 5.000000000000005329 ) ) ;
#18386=CARTESIAN_POINT ( 'NONE',  ( -6.338291171875001240, 287.2578125025604550, 0.000000000000000000 ) ) ;
#18390=CARTESIAN_POINT ( 'NONE',  ( -0.4590000000000000746, 255.7199999999997715, 5.818583442785218551 ) ) ;
#18391=CARTESIAN_POINT ( 'NONE',  ( -6.676582343750002480, 296.3906250017069510, -2.765530957081996810 ) ) ;
#18394=VERTEX_POINT ( 'NONE', #20759 ) ;
#18398=ORIENTED_EDGE ( 'NONE', *, *, #41437, .T. ) ;
#18400=CARTESIAN_POINT ( 'NONE',  ( -11.35316468749999785, 98.38541666325268409, -3.042071309553167513 ) ) ;
#18401=CYLINDRICAL_SURFACE ( 'NONE', #69776, 15.99999999999998579 ) ;
#18409=CARTESIAN_POINT ( 'NONE',  ( 5.676582343749993598, 209.9479166632526983, 9.832129032723422313 ) ) ;
#18415=CARTESIAN_POINT ( 'NONE',  ( -11.35316468749999785, 178.3854166632526983, -3.042071309553167513 ) ) ;
#18422=CARTESIAN_POINT ( 'NONE',  ( -2.085542519210945728E-15, 69.53124999658602690, 11.35316468750000141 ) ) ;
#18428=CARTESIAN_POINT ( 'NONE',  ( -3.042071309553164404, 77.23958332991935549, -11.35316468749999963 ) ) ;
#18433=CARTESIAN_POINT ( 'NONE',  ( -9.832129032723420536, 63.69791666325269830, 5.676582343749997150 ) ) ;
#18435=ADVANCED_FACE ( 'NONE', ( #67171 ), #26796, .T. ) ;
#18438=CARTESIAN_POINT ( 'NONE',  ( -2.679491924311235618, 150.4166666598387110, 10.00000000000000000 ) ) ;
#18440=CARTESIAN_POINT ( 'NONE',  ( 4.999999999999998224, 19.16666666666667140, 8.660254037844396180 ) ) ;
#18441=CARTESIAN_POINT ( 'NONE',  ( 11.35316468749999785, 45.88541666325267698, 3.042071309553174174 ) ) ;
#18443=CARTESIAN_POINT ( 'NONE',  ( -5.676582343750006032, 199.1145833299193555, 9.832129032723418760 ) ) ;
#18449=CARTESIAN_POINT ( 'NONE',  ( 11.35316468750000141, 175.7812499965860411, 0.000000000000000000 ) ) ;
#18455=CARTESIAN_POINT ( 'NONE',  ( 5.676582343750001591, 161.9270833299193555, -9.832129032723420536 ) ) ;
#18458=CARTESIAN_POINT ( 'NONE',  ( -3.042071309553173730, 129.6354166632526415, 11.35316468749999785 ) ) ;
#18479=VERTEX_POINT ( 'NONE', #67909 ) ;
#18488=CARTESIAN_POINT ( 'NONE',  ( -1.836970198721029983E-15, 133.7500000000000000, 10.00000000000000178 ) ) ;
#18489=AXIS2_PLACEMENT_3D ( 'NONE', #46792, #17753, #52101 ) ;
#18499=CYLINDRICAL_SURFACE ( 'NONE', #18489, 10.00000000000000178 ) ;
#18504=CARTESIAN_POINT ( 'NONE',  ( -11.35316468750000141, 33.28124999658601979, -1.390361679473963753E-15 ) ) ;
#18506=CARTESIAN_POINT ( 'NONE',  ( -8.311093377946841443, 219.2187499965859843, 8.311093377946830785 ) ) ;
#18509=DIRECTION ( 'NONE',  ( 0.000000000000000000, 0.000000000000000000, 1.000000000000000000 ) ) ;
#18510=ORIENTED_EDGE ( 'NONE', *, *, #47743, .F. ) ;
#18514=CARTESIAN_POINT ( 'NONE',  ( 3.042071309553159519, 34.73958332991934839, 11.35316468750000141 ) ) ;
#18518=DIRECTION ( 'NONE',  ( -0.000000000000000000, 1.000000000000000000, -0.000000000000000000 ) ) ;
#18520=CARTESIAN_POINT ( 'NONE',  ( -3.042071309553173730, 14.32291666325268231, 11.35316468749999785 ) ) ;
#18522=CARTESIAN_POINT ( 'NONE',  ( 5.676582343749993598, 149.9479166632526983, 9.832129032723422313 ) ) ;
#18523=CARTESIAN_POINT ( 'NONE',  ( 8.660254037844385522, 116.4583333265053824, 5.000000000000005329 ) ) ;
#18529=CARTESIAN_POINT ( 'NONE',  ( -11.35316468750000141, 8.593749996586016238, -1.390361679473963753E-15 ) ) ;
#18531=DIRECTION ( 'NONE',  ( 0.000000000000000000, 0.000000000000000000, 1.000000000000000000 ) ) ;
#18532=CARTESIAN_POINT ( 'NONE',  ( -6.676582343750003368, 299.3906250017069510, -2.765530957081996810 ) ) ;
#18534=CARTESIAN_POINT ( 'NONE',  ( -9.832129032723420536, 133.6979166632526983, 5.676582343749997150 ) ) ;
#18542=CARTESIAN_POINT ( 'NONE',  ( -7.320508075688773708, 203.7499999931720538, -7.320508075688774596 ) ) ;
#18544=CARTESIAN_POINT ( 'NONE',  ( 9.832129032723416984, 90.67708332991934128, 5.676582343750006032 ) ) ;
#18556=LINE ( 'NONE', #52521, #19744 ) ;
#18563=FACE_OUTER_BOUND ( 'NONE', #57439, .T. ) ;
#18564=( NAMED_UNIT ( * ) SI_UNIT ( $, .STERADIAN. ) SOLID_ANGLE_UNIT ( ) );
#18567=AXIS2_PLACEMENT_3D ( 'NONE', #4826, #46288, #33882 ) ;
#18572=CARTESIAN_POINT ( 'NONE',  ( -9.999999999999987566, 97.29166666666667140, -2.679491924311226736 ) ) ;
#18576=CARTESIAN_POINT ( 'NONE',  ( 8.660254037844385522, 89.58333333333332860, 5.000000000000005329 ) ) ;
#18577=ADVANCED_FACE ( 'NONE', ( #56227 ), #21133, .T. ) ;
#18579=CARTESIAN_POINT ( 'NONE',  ( -11.35316468749999785, 58.38541666325268409, -3.042071309553167513 ) ) ;
#18580=CARTESIAN_POINT ( 'NONE',  ( 1.226468279477575784E-15, 294.8593750017070079, 6.676582343750001591 ) ) ;
#18582=CARTESIAN_POINT ( 'NONE',  ( -10.00000000000000178, 144.3749999931720538, -1.224646799147353454E-15 ) ) ;
#18585=CARTESIAN_POINT ( 'NONE',  ( -1.744157829248402118E-12, 86.25000000000015632, -10.00000000000000533 ) ) ;
#18590=CARTESIAN_POINT ( 'NONE',  ( 2.679491924311228956, 211.0416666666666572, -10.00000000000000000 ) ) ;
#18592=CARTESIAN_POINT ( 'NONE',  ( 11.35316468750000141, 181.0937499965860411, 0.000000000000000000 ) ) ;
#18597=ORIENTED_EDGE ( 'NONE', *, *, #52290, .T. ) ;
#18598=VECTOR ( 'NONE', #39828, 1000.000000000000000 ) ;
#18601=CARTESIAN_POINT ( 'NONE',  ( -5.676582343750006032, 34.42708332991935549, 9.832129032723418760 ) ) ;
#18603=CARTESIAN_POINT ( 'NONE',  ( 4.643183940729320724, 227.0088029853575620, -10.42876187888753847 ) ) ;
#18610=CARTESIAN_POINT ( 'NONE',  ( 10.00000000000000178, 82.08333332650535397, -2.679491924311226736 ) ) ;
#18615=DIRECTION ( 'NONE',  ( -0.000000000000000000, 1.000000000000000000, -0.000000000000000000 ) ) ;
#18618=CARTESIAN_POINT ( 'NONE',  ( -6.676582343750001591, 297.6093750017069510, 0.000000000000000000 ) ) ;
#18621=CARTESIAN_POINT ( 'NONE',  ( 11.35316468749999963, 160.9895833299193839, -3.042071309553165293 ) ) ;
#18623=DIRECTION ( 'NONE',  ( 0.000000000000000000, 0.000000000000000000, 1.000000000000000000 ) ) ;
#18630=VECTOR ( 'NONE', #30528, 1000.000000000000000 ) ;
#18632=CARTESIAN_POINT ( 'NONE',  ( 11.35316468750000141, 141.0937499965860127, 0.000000000000000000 ) ) ;
#18634=CARTESIAN_POINT ( 'NONE',  ( -6.000000000000001776, 291.0000000000000000, 0.000000000000000000 ) ) ;
#18636=CARTESIAN_POINT ( 'NONE',  ( 9.832129032723416984, 50.67708332991935549, 5.676582343750006032 ) ) ;
#18643=CARTESIAN_POINT ( 'NONE',  ( -6.000000000000003553, 292.0000000034139589, -2.485281374238571317 ) ) ;
#18655=( BOUNDED_CURVE ( )  B_SPLINE_CURVE ( 2, ( #60949, #44348, #22060, #39062, #4735, #4360, #33052, #3611, #26607 ),
 .UNSPECIFIED., .F., .F. ) 
 B_SPLINE_CURVE_WITH_KNOTS ( ( 3, 2, 2, 2, 3 ),
 ( 0.2291666666666645480, 0.2395833333333312609, 0.2499999999999979183, 0.2604166666666646313, 0.2708333333333312609 ),
 .UNSPECIFIED. ) 
 CURVE ( )  GEOMETRIC_REPRESENTATION_ITEM ( )  RATIONAL_B_SPLINE_CURVE ( ( 1.000000000000015321, 0.9238795325112713064, 1.000000000000000000, 0.9238795325112867385, 1.000000000000000000, 0.9238795325112867385, 1.000000000000000000, 0.9238795325113017265, 0.9999999999999850120 ) ) 
 REPRESENTATION_ITEM ( '' )  );
#18658=CARTESIAN_POINT ( 'NONE',  ( 0.000000000000000000, 300.0000000000000000, 10.00000000000000178 ) ) ;
#18660=VERTEX_POINT ( 'NONE', #69769 ) ;
#18664=DIRECTION ( 'NONE',  ( -0.000000000000000000, 1.000000000000000000, -0.000000000000000000 ) ) ;
#18666=CARTESIAN_POINT ( 'NONE',  ( 5.000000000000001776, 50.83333333333333570, -8.660254037844389075 ) ) ;
#18668=CARTESIAN_POINT ( 'NONE',  ( 1.102182119232618108E-15, 297.2500000000000000, 6.000000000000001776 ) ) ;
#18682=CARTESIAN_POINT ( 'NONE',  ( -1.836970198721029983E-15, 173.7500000000000284, 10.00000000000000178 ) ) ;
#18683=CARTESIAN_POINT ( 'NONE',  ( 4.242640687119287435, 297.4375000034140157, 4.242640687119285658 ) ) ;
#18686=CARTESIAN_POINT ( 'NONE',  ( 9.832129032723420536, 146.5104166632526699, -5.676582343749999815 ) ) ;
#18687=CARTESIAN_POINT ( 'NONE',  ( 4.242640687119285658, 294.6875000034139589, -4.242640687119286547 ) ) ;
#18693=CARTESIAN_POINT ( 'NONE',  ( 3.090148520752590944, 225.9998984954551418, -9.510618362637927703 ) ) ;
#18698=CARTESIAN_POINT ( 'NONE',  ( -10.00000000000000355, 34.58333332650536107, 2.679491924311223183 ) ) ;
#18704=CARTESIAN_POINT ( 'NONE',  ( -1.836970198721029983E-15, 5.624999993172032475, 10.00000000000000178 ) ) ;
#18707=CARTESIAN_POINT ( 'NONE',  ( -10.00000000000005329, 62.50000000000002842, -1.224646799147359765E-15 ) ) ;
#18709=CARTESIAN_POINT ( 'NONE',  ( 5.676582343750001591, 116.6145833299193697, -9.832129032723420536 ) ) ;
#18713=LINE ( 'NONE', #18342, #21218 ) ;
#18715=CARTESIAN_POINT ( 'NONE',  ( 1.102182119232618108E-15, 294.3125000034140157, 6.000000000000001776 ) ) ;
#18716=CARTESIAN_POINT ( 'NONE',  ( 2.080949416610004210, 225.9999999999999716, -9.795045780231548704 ) ) ;
#18717=CARTESIAN_POINT ( 'NONE',  ( -11.35316468750000141, 113.2812499965860269, -1.390361679473963753E-15 ) ) ;
#18721=CARTESIAN_POINT ( 'NONE',  ( -5.000000000000005329, 195.2083333265053966, 8.660254037844387298 ) ) ;
#18725=CARTESIAN_POINT ( 'NONE',  ( 9.832129032723416984, 95.67708332991935549, 5.676582343750006032 ) ) ;
#18730=CARTESIAN_POINT ( 'NONE',  ( -11.35316468750000141, 8.802083329919348387, 3.042071309553159963 ) ) ;
#18738=CARTESIAN_POINT ( 'NONE',  ( 4.721056650416000089, 292.8281250017069510, 4.721056650415999201 ) ) ;
#18741=CARTESIAN_POINT ( 'NONE',  ( -9.832129032723418760, 218.1770833299193555, -5.676582343750004256 ) ) ;
#18749=CARTESIAN_POINT ( 'NONE',  ( -7.320508075688773708, 31.87500000000000000, -7.320508075688774596 ) ) ;
#18759=CARTESIAN_POINT ( 'NONE',  ( 1.226468279477575784E-15, 297.7031250017070079, 6.676582343750001591 ) ) ;
#18772=CARTESIAN_POINT ( 'NONE',  ( -3.042071309553173730, 99.63541666325268409, 11.35316468749999785 ) ) ;
#18778=ORIENTED_EDGE ( 'NONE', *, *, #12385, .T. ) ;
#18780=DIRECTION ( 'NONE',  ( -0.000000000000000000, 1.000000000000000000, -0.000000000000000000 ) ) ;
#18782=CARTESIAN_POINT ( 'NONE',  ( -11.35316468750000141, 213.2812499965860411, -1.390361679473963753E-15 ) ) ;
#18787=CARTESIAN_POINT ( 'NONE',  ( 3.042071309553167069, 182.1354166632526699, -11.35316468749999785 ) ) ;
#18794=CARTESIAN_POINT ( 'NONE',  ( -8.311093377946841443, 63.90624999658601979, 8.311093377946830785 ) ) ;
#18801=CARTESIAN_POINT ( 'NONE',  ( -5.676582343750006032, 79.11458332991935549, 9.832129032723418760 ) ) ;
#18806=CARTESIAN_POINT ( 'NONE',  ( -9.832129032723420536, 68.69791666325268409, 5.676582343749997150 ) ) ;
#18808=CARTESIAN_POINT ( 'NONE',  ( 5.000000000000001776, 130.8333333333333428, -8.660254037844389075 ) ) ;
#18809=CARTESIAN_POINT ( 'NONE',  ( 8.660254037844385522, 161.4583333265053966, 5.000000000000005329 ) ) ;
#18812=CARTESIAN_POINT ( 'NONE',  ( 8.311093377946837890, 56.71874999658601979, -8.311093377946837890 ) ) ;
#18814=CARTESIAN_POINT ( 'NONE',  ( -11.35316468750000141, 198.4895833299193555, 3.042071309553159963 ) ) ;
#18815=ORIENTED_EDGE ( 'NONE', *, *, #51126, .F. ) ;
#18819=CARTESIAN_POINT ( 'NONE',  ( -1.836970198721029983E-15, 120.6249999931720396, 10.00000000000000178 ) ) ;
#18821=CARTESIAN_POINT ( 'NONE',  ( -2.085542519210945728E-15, 199.5312499965860411, 11.35316468750000141 ) ) ;
#18822=CARTESIAN_POINT ( 'NONE',  ( 0.000000000000000000, 300.0000000000000000, 0.000000000000000000 ) ) ;
#18824=CARTESIAN_POINT ( 'NONE',  ( -8.660254037844390851, 189.7916666598387110, 4.999999999999998224 ) ) ;
#18826=CARTESIAN_POINT ( 'NONE',  ( 3.042071309553167513, 172.1354166632526983, -11.35316468749999785 ) ) ;
#18854=CARTESIAN_POINT ( 'NONE',  ( -2.765530957081996810, 296.4218750017069510, -6.676582343750002480 ) ) ;
#18855=CARTESIAN_POINT ( 'NONE',  ( -7.320508075688778149, 128.1250000000000000, 7.320508075688769267 ) ) ;
#18871=CARTESIAN_POINT ( 'NONE',  ( 5.676582343749993598, 29.94791666325268409, 9.832129032723422313 ) ) ;
#18873=CARTESIAN_POINT ( 'NONE',  ( 11.35316468750000141, 226.0937499965860127, 0.000000000000000000 ) ) ;
#18879=CARTESIAN_POINT ( 'NONE',  ( -5.676582343750006032, 29.11458332991935194, 9.832129032723418760 ) ) ;
#18883=CARTESIAN_POINT ( 'NONE',  ( -7.320508075688784366, 153.1250000000000000, 7.320508075688776373 ) ) ;
#18886=CARTESIAN_POINT ( 'NONE',  ( -5.676582343749998039, 37.44791666325267698, -9.832129032723420536 ) ) ;
#18888=CARTESIAN_POINT ( 'NONE',  ( 8.311093377946834337, 150.1562499965859843, 8.311093377946839666 ) ) ;
#18890=CARTESIAN_POINT ( 'NONE',  ( 5.000000000000001776, 117.7083333265053824, -8.660254037844389075 ) ) ;
#18892=CARTESIAN_POINT ( 'NONE',  ( 7.320508075688771044, 171.2499999931719969, 7.320508075688775484 ) ) ;
#18894=ORIENTED_EDGE ( 'NONE', *, *, #58712, .T. ) ;
#18895=CARTESIAN_POINT ( 'NONE',  ( 11.35316468750000141, 6.093749996586017126, 0.000000000000000000 ) ) ;
#18899=CARTESIAN_POINT ( 'NONE',  ( -3.042071309553163960, 137.2395833299193271, -11.35316468749999963 ) ) ;
#18906=VECTOR ( 'NONE', #47115, 1000.000000000000000 ) ;
#18907=CARTESIAN_POINT ( 'NONE',  ( 3.153939666463620179E-13, 118.7500000000000426, 9.999999999999998224 ) ) ;
#18909=CARTESIAN_POINT ( 'NONE',  ( -11.35316468750000141, 83.59374999658601268, -1.390361679473963753E-15 ) ) ;
#18924=ORIENTED_EDGE ( 'NONE', *, *, #61971, .F. ) ;
#18932=CARTESIAN_POINT ( 'NONE',  ( 7.320508075688771044, 121.2499999931720254, 7.320508075688775484 ) ) ;
#18935=ORIENTED_EDGE ( 'NONE', *, *, #30328, .F. ) ;
#18941=CARTESIAN_POINT ( 'NONE',  ( 5.000000000000001776, 90.83333333333332860, -8.660254037844389075 ) ) ;
#18943=CARTESIAN_POINT ( 'NONE',  ( 4.721056650416000089, 295.9843750017070079, 4.721056650415999201 ) ) ;
#18945=ORIENTED_EDGE ( 'NONE', *, *, #2585, .F. ) ;
#18946=AXIS2_PLACEMENT_3D ( 'NONE', #71336, #65316, #53642 ) ;
#18947=CARTESIAN_POINT ( 'NONE',  ( -8.660254037844387298, 173.9583333265053682, -5.000000000000004441 ) ) ;
#18950=CARTESIAN_POINT ( 'NONE',  ( -8.660254037844390851, 52.08333333333333570, -5.000000000000005329 ) ) ;
#18955=CARTESIAN_POINT ( 'NONE',  ( -4.999999999999998224, 211.6666666666666572, -8.660254037844389075 ) ) ;
#18957=CARTESIAN_POINT ( 'NONE',  ( 9.832129032723416984, 175.6770833299193555, 5.676582343750006032 ) ) ;
#18958=CARTESIAN_POINT ( 'NONE',  ( 7.320508075688771044, 191.2499999931720538, 7.320508075688775484 ) ) ;
#18965=CARTESIAN_POINT ( 'NONE',  ( 6.951808397369818766E-16, 52.34374999658601979, -11.35316468750000141 ) ) ;
#18967=CARTESIAN_POINT ( 'NONE',  ( 9.832129032723416984, 215.6770833299193555, 5.676582343750006032 ) ) ;
#18969=CARTESIAN_POINT ( 'NONE',  ( 10.00000000000000178, 10.20833333333333570, -2.679491924311227180 ) ) ;
#18973=CARTESIAN_POINT ( 'NONE',  ( 2.679491924311222739, 70.83333332650536818, 10.00000000000000355 ) ) ;
#18981=( BOUNDED_CURVE ( )  B_SPLINE_CURVE ( 2, ( #52535, #58947, #63476, #24590, #64951, #18572, #36297, #58217, #41582, #69891, #29894, #46869, #24219 ),
 .UNSPECIFIED., .F., .F. ) 
 B_SPLINE_CURVE_WITH_KNOTS ( ( 3, 2, 2, 2, 2, 2, 3 ),
 ( 1.208890027026519931, 1.214123945856841358, 1.219357864687163007, 1.224591783517484433, 1.229825702347806082, 1.235059621178127509, 1.240293540008449158 ),
 .UNSPECIFIED. ) 
 CURVE ( )  GEOMETRIC_REPRESENTATION_ITEM ( )  RATIONAL_B_SPLINE_CURVE ( ( 1.000000000000000000, 0.9659258262890683122, 1.000000000000000000, 0.9659258262890683122, 1.000000000000000000, 0.9659258262890683122, 1.000000000000000000, 0.9659258262890683122, 1.000000000000000000, 0.9659258262890683122, 1.000000000000000000, 0.9659258262889941493, 1.000000000000074163 ) ) 
 REPRESENTATION_ITEM ( '' )  );
#18982=CARTESIAN_POINT ( 'NONE',  ( 6.676582343750004256, 292.0468750017070079, 2.765530957081995478 ) ) ;
#18984=CARTESIAN_POINT ( 'NONE',  ( -3.042071309553173730, 154.3229166632527267, 11.35316468749999785 ) ) ;
#18989=ORIENTED_EDGE ( 'NONE', *, *, #37951, .F. ) ;
#18992=CARTESIAN_POINT ( 'NONE',  ( -3.042071309553163960, 142.5520833299193271, -11.35316468749999963 ) ) ;
#18994=CARTESIAN_POINT ( 'NONE',  ( 1.102182119232618108E-15, 291.2500000000000000, 6.000000000000001776 ) ) ;
#18996=CARTESIAN_POINT ( 'NONE',  ( -3.042071309553173730, 54.63541666325268409, 11.35316468749999785 ) ) ;
#19003=CARTESIAN_POINT ( 'NONE',  ( 6.000000000000003553, 292.5000000034140157, 2.485281374238571317 ) ) ;
#19009=CARTESIAN_POINT ( 'NONE',  ( -10.00000000000000000, 64.16666665983869677, -2.679491924311229845 ) ) ;
#19021=ORIENTED_EDGE ( 'NONE', *, *, #70566, .F. ) ;
#19027=CARTESIAN_POINT ( 'NONE',  ( -1.836970198721029983E-15, 58.75000000000000711, 10.00000000000000178 ) ) ;
#19029=CARTESIAN_POINT ( 'NONE',  ( 6.000000000000001776, 296.5000000000000000, -7.347880794884121708E-16 ) ) ;
#19042=CARTESIAN_POINT ( 'NONE',  ( 7.320508075688771044, 179.3750000000000284, 7.320508075688775484 ) ) ;
#19045=CARTESIAN_POINT ( 'NONE',  ( 9.832129032723420536, 136.5104166632526983, -5.676582343749999815 ) ) ;
#19047=CARTESIAN_POINT ( 'NONE',  ( 8.660254037844389075, 27.29166665983870033, -5.000000000000000000 ) ) ;
#19049=CARTESIAN_POINT ( 'NONE',  ( -1.836970198721029983E-15, 105.6249999931720396, 10.00000000000000178 ) ) ;
#19053=CARTESIAN_POINT ( 'NONE',  ( -9.832129032723418760, 13.17708332991935194, -5.676582343750004256 ) ) ;
#19059=CARTESIAN_POINT ( 'NONE',  ( 7.320508075688771044, 36.24999999317202537, 7.320508075688775484 ) ) ;
#19069=CARTESIAN_POINT ( 'NONE',  ( -11.35316468750000141, 113.4895833299193413, 3.042071309553159963 ) ) ;
#19077=CARTESIAN_POINT ( 'NONE',  ( 3.042071309553159519, 114.7395833299193413, 11.35316468750000141 ) ) ;
#19081=CARTESIAN_POINT ( 'NONE',  ( 2.679491924311222739, 210.8333333265053682, 10.00000000000000355 ) ) ;
#19084=CARTESIAN_POINT ( 'NONE',  ( 11.35316468749999785, 95.88541666325268409, 3.042071309553174174 ) ) ;
#19088=CARTESIAN_POINT ( 'NONE',  ( -11.35316468750000141, 8.593749996586016238, -1.390361679473963753E-15 ) ) ;
#19094=CARTESIAN_POINT ( 'NONE',  ( 10.00000000000000178, 200.2083333333333144, -2.679491924311226736 ) ) ;
#19095=CARTESIAN_POINT ( 'NONE',  ( 1.226468279477575784E-15, 292.7031250017069510, 6.676582343750001591 ) ) ;
#19097=CARTESIAN_POINT ( 'NONE',  ( -3.042071309553173730, 224.6354166632526983, 11.35316468749999785 ) ) ;
#19116=CARTESIAN_POINT ( 'NONE',  ( 0.4589999999999999636, 284.2799999999998590, 5.818583442781865678 ) ) ;
#19117=CARTESIAN_POINT ( 'NONE',  ( 2.765530957081996366, 294.1406250017069510, -6.676582343750002480 ) ) ;
#19129=CARTESIAN_POINT ( 'NONE',  ( -8.311093377946836114, 97.96874999658599847, -8.311093377946837890 ) ) ;
#19137=CARTESIAN_POINT ( 'NONE',  ( 1.224646799147353454E-15, 300.0000000000000000, -10.00000000000000178 ) ) ;
#19138=CARTESIAN_POINT ( 'NONE',  ( -9.832129032723420536, 208.6979166632526983, 5.676582343749997150 ) ) ;
#19143=CARTESIAN_POINT ( 'NONE',  ( 11.35316468749999963, 196.3020833299193271, -3.042071309553165293 ) ) ;
#19150=CARTESIAN_POINT ( 'NONE',  ( -11.35316468750000141, 73.48958332991932707, 3.042071309553159963 ) ) ;
#19154=CARTESIAN_POINT ( 'NONE',  ( -8.660254037844412167, 47.91666666666668561, 5.000000000000011546 ) ) ;
#19156=CARTESIAN_POINT ( 'NONE',  ( -11.35316468749999785, 78.07291666325269830, -3.042071309553167513 ) ) ;
#19164=CARTESIAN_POINT ( 'NONE',  ( 3.042071309553159519, 74.73958332991934128, 11.35316468750000141 ) ) ;
#19167=CARTESIAN_POINT ( 'NONE',  ( 2.679491924311228956, 167.9166666598387110, -10.00000000000000000 ) ) ;
#19170=CARTESIAN_POINT ( 'NONE',  ( 5.676582343750001591, 66.92708332991935549, -9.832129032723420536 ) ) ;
#19172=CARTESIAN_POINT ( 'NONE',  ( 11.35316468750000141, 190.7812499965860127, 0.000000000000000000 ) ) ;
#19176=CARTESIAN_POINT ( 'NONE',  ( 6.123233995736767268E-16, 163.1249999931720254, -10.00000000000000178 ) ) ;
#19178=CARTESIAN_POINT ( 'NONE',  ( 11.35316468750000141, 190.7812499965860127, 0.000000000000000000 ) ) ;
#19183=ORIENTED_EDGE ( 'NONE', *, *, #45455, .F. ) ;
#19185=CARTESIAN_POINT ( 'NONE',  ( 11.35316468750000141, 186.0937499965860411, 0.000000000000000000 ) ) ;
#19187=( BOUNDED_CURVE ( )  B_SPLINE_CURVE ( 2, ( #1117, #46737, #65191, #30138, #7867, #53154, #17696, #69761, #59552, #40714, #1488, #29405, #19176 ),
 .UNSPECIFIED., .F., .F. ) 
 B_SPLINE_CURVE_WITH_KNOTS ( ( 3, 2, 2, 2, 2, 2, 3 ),
 ( 0.6902173913043477826, 0.6920289855072463414, 0.6938405797101449002, 0.6956521739130434590, 0.6974637681159420177, 0.6992753623188405765, 0.7010869565217391353 ),
 .UNSPECIFIED. ) 
 CURVE ( )  GEOMETRIC_REPRESENTATION_ITEM ( )  RATIONAL_B_SPLINE_CURVE ( ( 1.000000000000000000, 0.9659258262890683122, 1.000000000000000000, 0.9659258262890683122, 1.000000000000000000, 0.9659258262890683122, 1.000000000000000000, 0.9659258262890683122, 1.000000000000000000, 0.9659258262890683122, 1.000000000000000000, 0.9659258262890683122, 1.000000000000000000 ) ) 
 REPRESENTATION_ITEM ( '' )  );
#19192=CARTESIAN_POINT ( 'NONE',  ( 10.00000000000000178, 0.2083333333333333703, -2.679491924311226736 ) ) ;
#19199=EDGE_LOOP ( 'NONE', ( #72347, #53166, #74559, #29773 ) ) ;
#19202=CARTESIAN_POINT ( 'NONE',  ( 2.679491924310949180, 181.0416666666667425, -10.00000000000022204 ) ) ;
#19205=VERTEX_POINT ( 'NONE', #74355 ) ;
#19213=CARTESIAN_POINT ( 'NONE',  ( -7.320508075688778149, 114.9999999931720254, 7.320508075688769267 ) ) ;
#19217=CARTESIAN_POINT ( 'NONE',  ( 6.676582343750002480, 293.1718750017071216, -2.765530957081997254 ) ) ;
#19218=CARTESIAN_POINT ( 'NONE',  ( 8.660254037844389075, 150.4166666666666572, -5.000000000000000000 ) ) ;
#19226=FACE_OUTER_BOUND ( 'NONE', #32801, .T. ) ;
#19233=CARTESIAN_POINT ( 'NONE',  ( 5.676582343749993598, 34.94791666325268409, 9.832129032723422313 ) ) ;
#19235=CARTESIAN_POINT ( 'NONE',  ( -2.679491924311225848, 8.333333326505366401, -10.00000000000000178 ) ) ;
#19239=CARTESIAN_POINT ( 'NONE',  ( 11.35316468749999963, 40.98958332991935549, -3.042071309553165293 ) ) ;
#19242=CARTESIAN_POINT ( 'NONE',  ( -2.485281374238979879, 298.8125000000000000, -5.999999999999594991 ) ) ;
#19243=CARTESIAN_POINT ( 'NONE',  ( -3.673940397442060854E-16, 290.7500000000000000, -6.000000000000001776 ) ) ;
#19245=CARTESIAN_POINT ( 'NONE',  ( 8.311093377946837890, 36.40624999658601979, -8.311093377946837890 ) ) ;
#19247=CARTESIAN_POINT ( 'NONE',  ( -5.676582343749998039, 152.4479166632526983, -9.832129032723420536 ) ) ;
#19249=CARTESIAN_POINT ( 'NONE',  ( -10.00000000000000355, 109.5833333265053540, 2.679491924311223183 ) ) ;
#19255=CARTESIAN_POINT ( 'NONE',  ( -9.832129032723420536, 24.01041666325268409, 5.676582343749997150 ) ) ;
#19257=CARTESIAN_POINT ( 'NONE',  ( 8.660254037844373087, 104.5833333333333286, 4.999999999999998224 ) ) ;
#19260=CARTESIAN_POINT ( 'NONE',  ( 3.042071309553167513, 151.8229166632526699, -11.35316468749999785 ) ) ;
#19263=AXIS2_PLACEMENT_3D ( 'NONE', #41694, #65804, #53022 ) ;
#19266=ORIENTED_EDGE ( 'NONE', *, *, #53219, .F. ) ;
#19267=ADVANCED_FACE ( 'NONE', ( #22665 ), #45684, .T. ) ;
#19270=CARTESIAN_POINT ( 'NONE',  ( -9.832129032723420536, 99.01041666325269830, 5.676582343749997150 ) ) ;
#19272=EDGE_CURVE ( 'NONE', #23374, #5520, #62815, .T. ) ;
#19287=( BOUNDED_CURVE ( )  B_SPLINE_CURVE ( 2, ( #2524, #60977, #27018, #25516, #9298, #71913, #33083, #37978, #9681, #26257, #14567, #37603, #48528 ),
 .UNSPECIFIED., .F., .F. ) 
 B_SPLINE_CURVE_WITH_KNOTS ( ( 3, 2, 2, 2, 2, 2, 3 ),
 ( 0.7119565217391303769, 0.7137681159420288246, 0.7155797101449273834, 0.7173913043478259421, 0.7192028985507246119, 0.7210144927536231707, 0.7228260869565217295 ),
 .UNSPECIFIED. ) 
 CURVE ( )  GEOMETRIC_REPRESENTATION_ITEM ( )  RATIONAL_B_SPLINE_CURVE ( ( 1.000000000000001998, 0.9659258262890662028, 1.000000000000000000, 0.9659258262890683122, 1.000000000000000000, 0.9659258262890683122, 1.000000000000000000, 0.9659258262890683122, 1.000000000000000000, 0.9659258262890683122, 1.000000000000000000, 0.9659258262890683122, 1.000000000000000000 ) ) 
 REPRESENTATION_ITEM ( '' )  );
#19292=CARTESIAN_POINT ( 'NONE',  ( 10.00000000000000000, 121.6666666598386968, 2.679491924311235618 ) ) ;
#19303=CARTESIAN_POINT ( 'NONE',  ( 2.679491924311222739, 93.95833333333334281, 10.00000000000000355 ) ) ;
#19305=CARTESIAN_POINT ( 'NONE',  ( 2.765530957081996366, 295.2968750017069510, -6.676582343750003368 ) ) ;
#19314=CARTESIAN_POINT ( 'NONE',  ( 10.00000000000000178, 215.0000000000000284, 0.000000000000000000 ) ) ;
#19316=CARTESIAN_POINT ( 'NONE',  ( -5.676582343750006032, 189.4270833299193555, 9.832129032723418760 ) ) ;
#19324=CARTESIAN_POINT ( 'NONE',  ( -9.832129032723420536, 54.01041666325268409, 5.676582343749997150 ) ) ;
#19326=CARTESIAN_POINT ( 'NONE',  ( 8.311093377946834337, 220.4687499965859843, 8.311093377946839666 ) ) ;
#19330=CARTESIAN_POINT ( 'NONE',  ( -7.320508075688773708, 58.74999999317203248, -7.320508075688774596 ) ) ;
#19332=CARTESIAN_POINT ( 'NONE',  ( -3.042071309553164404, 107.2395833299193413, -11.35316468749999963 ) ) ;
#19335=CARTESIAN_POINT ( 'NONE',  ( -8.660254037844387298, 73.95833332650536818, -5.000000000000004441 ) ) ;
#19338=CARTESIAN_POINT ( 'NONE',  ( -2.679491924316527385, 71.45833333333379755, -9.999999999996944666 ) ) ;
#19342=CARTESIAN_POINT ( 'NONE',  ( -4.721056650415999201, 294.4843750017070079, -4.721056650415999201 ) ) ;
#19343=CARTESIAN_POINT ( 'NONE',  ( -7.320508075688787919, 143.1250000000000284, 7.320508075688779925 ) ) ;
#19344=CARTESIAN_POINT ( 'NONE',  ( -11.35316468750000141, 163.4895833299193271, 3.042071309553159963 ) ) ;
#19345=CARTESIAN_POINT ( 'NONE',  ( 10.00000000000000178, 2.083333326505365957, -2.679491924311226736 ) ) ;
#19353=CARTESIAN_POINT ( 'NONE',  ( 3.042071309553159519, 140.0520833299193271, 11.35316468750000141 ) ) ;
#19357=CARTESIAN_POINT ( 'NONE',  ( 8.311093377946837890, 51.71874999658601979, -8.311093377946837890 ) ) ;
#19358=ORIENTED_EDGE ( 'NONE', *, *, #41587, .T. ) ;
#19363=CARTESIAN_POINT ( 'NONE',  ( 4.242640687119287435, 291.4375000034140157, 4.242640687119285658 ) ) ;
#19364=VECTOR ( 'NONE', #9044, 1000.000000000000000 ) ;
#19371=ORIENTED_EDGE ( 'NONE', *, *, #26526, .F. ) ;
#19378=CYLINDRICAL_SURFACE ( 'NONE', #38064, 10.00000000000000178 ) ;
#19382=ORIENTED_EDGE ( 'NONE', *, *, #30261, .T. ) ;
#19386=CARTESIAN_POINT ( 'NONE',  ( 7.320508075688771044, 49.37500000000000000, 7.320508075688775484 ) ) ;
#19388=CARTESIAN_POINT ( 'NONE',  ( 4.242640687119287435, 297.3750000000000000, 4.242640687119285658 ) ) ;
#19395=CARTESIAN_POINT ( 'NONE',  ( -10.00000000000000355, 74.58333332650535397, 2.679491924311223183 ) ) ;
#19400=CARTESIAN_POINT ( 'NONE',  ( -4.999999999999998224, 176.6666666666666572, -8.660254037844389075 ) ) ;
#19404=CARTESIAN_POINT ( 'NONE',  ( 11.35316468749999785, 145.8854166632526983, 3.042071309553174174 ) ) ;
#19406=LINE ( 'NONE', #36043, #73488 ) ;
#19411=CARTESIAN_POINT ( 'NONE',  ( -9.832129032723420536, 4.010416663252683200, 5.676582343749997150 ) ) ;
#19418=CARTESIAN_POINT ( 'NONE',  ( -10.00000000000000355, 39.58333332650536107, 2.679491924311223183 ) ) ;
#19425=CARTESIAN_POINT ( 'NONE',  ( 8.660254037844389075, 7.291666659838699438, -5.000000000000000000 ) ) ;
#19429=CARTESIAN_POINT ( 'NONE',  ( -7.320508075688818117, 63.12500000000004263, 7.320508075688810123 ) ) ;
#19431=CARTESIAN_POINT ( 'NONE',  ( 11.35316468749999963, 115.9895833299193555, -3.042071309553165293 ) ) ;
#19438=CYLINDRICAL_SURFACE ( 'NONE', #73937, 10.00000000000000178 ) ;
#19440=CARTESIAN_POINT ( 'NONE',  ( -5.676582343750006032, 109.1145833299193555, 9.832129032723418760 ) ) ;
#19442=CARTESIAN_POINT ( 'NONE',  ( 10.00000000000000711, 50.00000000000000711, 0.000000000000000000 ) ) ;
#19445=CARTESIAN_POINT ( 'NONE',  ( 8.660254037844389075, 212.2916666598387110, -5.000000000000000000 ) ) ;
#19446=DIRECTION ( 'NONE',  ( -0.000000000000000000, 1.000000000000000000, -0.000000000000000000 ) ) ;
#19448=CARTESIAN_POINT ( 'NONE',  ( 6.951808397369818766E-16, 107.3437499965860269, -11.35316468750000141 ) ) ;
#19452=CARTESIAN_POINT ( 'NONE',  ( -11.35316468750000141, 13.59374999658601801, -1.390361679473963753E-15 ) ) ;
#19460=CARTESIAN_POINT ( 'NONE',  ( 2.220677790255211837E-11, 201.2499999999982663, -9.999999999999998224 ) ) ;
#19461=CARTESIAN_POINT ( 'NONE',  ( 2.765530957082001251, 291.7656250017069510, 6.676582343750000703 ) ) ;
#19463=CARTESIAN_POINT ( 'NONE',  ( 10.00000000000000178, 127.0833333265053682, -2.679491924311226736 ) ) ;
#19464=CARTESIAN_POINT ( 'NONE',  ( 8.311093377946834337, 215.4687499965860127, 8.311093377946839666 ) ) ;
#19469=VERTEX_POINT ( 'NONE', #41514 ) ;
#19470=CARTESIAN_POINT ( 'NONE',  ( -1.836970198721029983E-15, 85.62499999317203958, 10.00000000000000178 ) ) ;
#19479=FACE_OUTER_BOUND ( 'NONE', #30673, .T. ) ;
#19481=CARTESIAN_POINT ( 'NONE',  ( -1.377000000000000002, 267.1439999999997212, 5.668132533233856130 ) ) ;
#19482=CARTESIAN_POINT ( 'NONE',  ( -6.676582343750001591, 294.4531250017069510, 0.000000000000000000 ) ) ;
#19485=VERTEX_POINT ( 'NONE', #52107 ) ;
#19490=ORIENTED_EDGE ( 'NONE', *, *, #56011, .F. ) ;
#19493=CARTESIAN_POINT ( 'NONE',  ( 5.676582343750001591, 106.9270833299193413, -9.832129032723420536 ) ) ;
#19498=CARTESIAN_POINT ( 'NONE',  ( 0.000000000000000000, 300.0000000000000000, 0.000000000000000000 ) ) ;
#19503=CARTESIAN_POINT ( 'NONE',  ( 9.832129032723416984, 215.3645833299193555, 5.676582343750006032 ) ) ;
#19507=CARTESIAN_POINT ( 'NONE',  ( -8.311093377946841443, 194.2187499965859843, 8.311093377946830785 ) ) ;
#19513=CARTESIAN_POINT ( 'NONE',  ( 9.832129032723420536, 76.19791666325269830, -5.676582343749999815 ) ) ;
#19519=CARTESIAN_POINT ( 'NONE',  ( 6.951808397369818766E-16, 82.03124999658602690, -11.35316468750000141 ) ) ;
#19526=CARTESIAN_POINT ( 'NONE',  ( -9.832129032723418760, 77.86458332991935549, -5.676582343750004256 ) ) ;
#19529=( BOUNDED_CURVE ( )  B_SPLINE_CURVE ( 2, ( #74468, #51834, #68072, #5447, #29201, #74099, #27698, #46168, #45420, #46542, #69186, #62765, #5821 ),
 .UNSPECIFIED., .F., .F. ) 
 B_SPLINE_CURVE_WITH_KNOTS ( ( 3, 2, 2, 2, 2, 2, 3 ),
 ( 2.464888983165918646, 2.470121561219082551, 2.475354139272246456, 2.480586717325410362, 2.485819295378574267, 2.491051873431738617, 2.496284451484902078 ),
 .UNSPECIFIED. ) 
 CURVE ( )  GEOMETRIC_REPRESENTATION_ITEM ( )  RATIONAL_B_SPLINE_CURVE ( ( 1.000000000000100142, 0.9659258262889679481, 1.000000000000000000, 0.9659258262890682012, 1.000000000000000000, 0.9659258262890682012, 1.000000000000000000, 0.9659258262890682012, 1.000000000000000000, 0.9659258262890682012, 1.000000000000000000, 0.9659258262891976532, 0.9999999999998705480 ) ) 
 REPRESENTATION_ITEM ( '' )  );
#19530=CARTESIAN_POINT ( 'NONE',  ( -8.660254037844387298, 168.9583333265053682, -5.000000000000004441 ) ) ;
#19534=CARTESIAN_POINT ( 'NONE',  ( 5.676582343750001591, 61.92708332991934839, -9.832129032723420536 ) ) ;
#19536=CARTESIAN_POINT ( 'NONE',  ( -3.042071309553173730, 189.3229166632526699, 11.35316468749999785 ) ) ;
#19542=CARTESIAN_POINT ( 'NONE',  ( 6.951808397369818766E-16, 187.0312499965860127, -11.35316468750000141 ) ) ;
#19546=EDGE_CURVE ( 'NONE', #4267, #60284, #73402, .T. ) ;
#19548=CARTESIAN_POINT ( 'NONE',  ( 3.042071309553159519, 185.0520833299193555, 11.35316468750000141 ) ) ;
#19554=EDGE_CURVE ( 'NONE', #65462, #15764, #27131, .T. ) ;
#19557=CARTESIAN_POINT ( 'NONE',  ( 0.000000000000000000, 300.0000000000000000, 0.000000000000000000 ) ) ;
#19566=CYLINDRICAL_SURFACE ( 'NONE', #27754, 6.000000000000001776 ) ;
#19569=ORIENTED_EDGE ( 'NONE', *, *, #36559, .T. ) ;
#19579=CARTESIAN_POINT ( 'NONE',  ( -2.765530957081996810, 295.4218750017069510, -6.676582343750002480 ) ) ;
#19580=CARTESIAN_POINT ( 'NONE',  ( -5.000000000000005329, 143.3333333333333428, 8.660254037844387298 ) ) ;
#19582=CARTESIAN_POINT ( 'NONE',  ( -8.660254037844390851, 164.7916666598387110, 4.999999999999998224 ) ) ;
#19583=CARTESIAN_POINT ( 'NONE',  ( 2.485281374238878627, 290.3750000034138452, 5.999999999999694467 ) ) ;
#19592=CARTESIAN_POINT ( 'NONE',  ( -7.320508075688773708, 131.8750000000000284, -7.320508075688774596 ) ) ;
#19597=CARTESIAN_POINT ( 'NONE',  ( 11.35316468750000141, 35.78124999658601979, 0.000000000000000000 ) ) ;
#19598=EDGE_CURVE ( 'NONE', #27032, #45065, #2261, .T. ) ;
#19600=CARTESIAN_POINT ( 'NONE',  ( 8.660254037844385522, 11.45833332650536640, 5.000000000000005329 ) ) ;
#19602=CARTESIAN_POINT ( 'NONE',  ( 9.999999999999996447, 185.0000000000000284, 0.000000000000000000 ) ) ;
#19607=CARTESIAN_POINT ( 'NONE',  ( 11.35316468749999785, 35.57291666325267698, 3.042071309553174174 ) ) ;
#19613=CARTESIAN_POINT ( 'NONE',  ( 3.042071309553167513, 36.82291666325267698, -11.35316468749999785 ) ) ;
#19615=CARTESIAN_POINT ( 'NONE',  ( -5.676582343749998039, 142.4479166632526699, -9.832129032723420536 ) ) ;
#19617=CARTESIAN_POINT ( 'NONE',  ( -7.320508075688773708, 123.7499999931720396, -7.320508075688774596 ) ) ;
#19622=CARTESIAN_POINT ( 'NONE',  ( 6.951808397369818766E-16, 17.34374999658601624, -11.35316468750000141 ) ) ;
#19624=ORIENTED_EDGE ( 'NONE', *, *, #37503, .F. ) ;
#19628=CARTESIAN_POINT ( 'NONE',  ( -11.35316468750000141, 153.4895833299193555, 3.042071309553159963 ) ) ;
#19637=CARTESIAN_POINT ( 'NONE',  ( -9.832129032723418760, 108.1770833299193555, -5.676582343750004256 ) ) ;
#19640=( BOUNDED_CURVE ( )  B_SPLINE_CURVE ( 2, ( #43180, #66196, #14500, #43553, #3962, #66948, #14876, #20918, #33380, #73722, #26951, #66567, #49969 ),
 .UNSPECIFIED., .F., .F. ) 
 B_SPLINE_CURVE_WITH_KNOTS ( ( 3, 2, 2, 2, 2, 2, 3 ),
 ( 1.993888113706278942, 1.999121869590356759, 2.004355625474434799, 2.009589381358512838, 2.014823137242590434, 2.020056893126668474, 2.025290649010746513 ),
 .UNSPECIFIED. ) 
 CURVE ( )  GEOMETRIC_REPRESENTATION_ITEM ( )  RATIONAL_B_SPLINE_CURVE ( ( 0.9999999999999978906, 0.9659258262890703106, 1.000000000000000000, 0.9659258262890682012, 1.000000000000000000, 0.9659258262890682012, 1.000000000000000000, 0.9659258262890682012, 1.000000000000000000, 0.9659258262890682012, 1.000000000000000000, 0.9659258262890682012, 1.000000000000000000 ) ) 
 REPRESENTATION_ITEM ( '' )  );
#19654=VECTOR ( 'NONE', #60593, 1000.000000000000000 ) ;
#19657=CARTESIAN_POINT ( 'NONE',  ( -2.679491924311078410, 223.3333333265053113, -10.00000000000008527 ) ) ;
#19671=CARTESIAN_POINT ( 'NONE',  ( -4.999999999999998224, 111.6666666666666714, -8.660254037844389075 ) ) ;
#19673=CARTESIAN_POINT ( 'NONE',  ( 6.676582343750004256, 295.0468750017069510, 2.765530957081995478 ) ) ;
#19685=CARTESIAN_POINT ( 'NONE',  ( -10.00000000000000355, 222.7083333333333428, 2.679491924311223183 ) ) ;
#19688=CARTESIAN_POINT ( 'NONE',  ( -5.676582343749998039, 197.7604166632526983, -9.832129032723420536 ) ) ;
#19689=CARTESIAN_POINT ( 'NONE',  ( 2.679491924311222739, 190.8333333265053682, 10.00000000000000355 ) ) ;
#19691=CARTESIAN_POINT ( 'NONE',  ( 0.000000000000000000, 300.0000000000000000, 6.000000000000001776 ) ) ;
#19695=CARTESIAN_POINT ( 'NONE',  ( -3.042071309553173730, 49.63541666325267698, 11.35316468749999785 ) ) ;
#19703=CARTESIAN_POINT ( 'NONE',  ( -3.042071309553164404, 112.2395833299193697, -11.35316468749999963 ) ) ;
#19704=CARTESIAN_POINT ( 'NONE',  ( 8.660254037844385522, 91.45833332650536818, 5.000000000000005329 ) ) ;
#19707=CARTESIAN_POINT ( 'NONE',  ( -7.320508075688778149, 71.87500000000001421, -7.320508075688779037 ) ) ;
#19710=CARTESIAN_POINT ( 'NONE',  ( -7.535050054895622296, 225.9999999999999716, 6.607029887625837539 ) ) ;
#19713=CARTESIAN_POINT ( 'NONE',  ( -6.676582343750003368, 294.5468750017069510, -2.765530957081996810 ) ) ;
#19716=CARTESIAN_POINT ( 'NONE',  ( -11.35316468749999785, 173.0729166632526983, -3.042071309553167513 ) ) ;
#19725=CARTESIAN_POINT ( 'NONE',  ( -8.311093377946836114, 137.9687499965860127, -8.311093377946837890 ) ) ;
#19727=CARTESIAN_POINT ( 'NONE',  ( 6.000000000000003553, 298.5000000034139589, 2.485281374238571317 ) ) ;
#19729=CARTESIAN_POINT ( 'NONE',  ( -5.676582343749998039, 62.76041666325269119, -9.832129032723420536 ) ) ;
#19730=ORIENTED_EDGE ( 'NONE', *, *, #48588, .T. ) ;
#19731=CARTESIAN_POINT ( 'NONE',  ( -2.679491924311236950, 28.54166666666667140, 10.00000000000000711 ) ) ;
#19737=CARTESIAN_POINT ( 'NONE',  ( -6.000000000000001776, 292.0625000034140157, 0.000000000000000000 ) ) ;
#19744=VECTOR ( 'NONE', #7975, 1000.000000000000000 ) ;
#19747=ORIENTED_EDGE ( 'NONE', *, *, #51917, .T. ) ;
#19762=CARTESIAN_POINT ( 'NONE',  ( -10.00000000000000000, 62.29166666666666430, -2.679491924311229845 ) ) ;
#19765=CARTESIAN_POINT ( 'NONE',  ( 6.000000000000001776, 295.5000000000000000, -7.347880794884121708E-16 ) ) ;
#19775=CARTESIAN_POINT ( 'NONE',  ( 7.320508075688774596, 170.6250000000000284, -7.320508075688774596 ) ) ;
#19776=DIRECTION ( 'NONE',  ( 0.000000000000000000, 0.000000000000000000, -1.000000000000000000 ) ) ;
#19778=CARTESIAN_POINT ( 'NONE',  ( 11.35316468749999963, 156.3020833299192986, -3.042071309553165293 ) ) ;
#19783=CARTESIAN_POINT ( 'NONE',  ( -5.000000000000000000, 166.6666666666666856, -8.660254037844390851 ) ) ;
#19785=CARTESIAN_POINT ( 'NONE',  ( -5.676582343750006032, 9.427083329919350163, 9.832129032723418760 ) ) ;
#19788=CARTESIAN_POINT ( 'NONE',  ( -6.338495502905945601E-13, 181.2500000000000853, -10.00000000000000533 ) ) ;
#19791=CARTESIAN_POINT ( 'NONE',  ( -8.660254037844390851, 49.79166665983870388, 4.999999999999998224 ) ) ;
#19803=CARTESIAN_POINT ( 'NONE',  ( 5.676582343750001591, 126.6145833299193697, -9.832129032723420536 ) ) ;
#19810=CARTESIAN_POINT ( 'NONE',  ( 10.00000000000002665, 45.00000000000001421, 0.000000000000000000 ) ) ;
#19811=CARTESIAN_POINT ( 'NONE',  ( -9.832129032723418760, 112.8645833299193555, -5.676582343750004256 ) ) ;
#19813=CARTESIAN_POINT ( 'NONE',  ( 7.320508075688774596, 82.49999999317202537, -7.320508075688774596 ) ) ;
#19814=ORIENTED_EDGE ( 'NONE', *, *, #9203, .F. ) ;
#19817=CARTESIAN_POINT ( 'NONE',  ( -9.832129032723418760, 108.1770833299193555, -5.676582343750004256 ) ) ;
#19821=CARTESIAN_POINT ( 'NONE',  ( 3.042071309553159519, 20.05208332991934839, 11.35316468750000141 ) ) ;
#19823=CARTESIAN_POINT ( 'NONE',  ( -1.836970198721029983E-15, 180.6249999931720538, 10.00000000000000178 ) ) ;
#19830=CARTESIAN_POINT ( 'NONE',  ( -4.721056650415999201, 293.3281250017069510, -4.721056650415999201 ) ) ;
#19832=CARTESIAN_POINT ( 'NONE',  ( -9.832129032723420536, 224.0104166632526983, 5.676582343749997150 ) ) ;
#19833=CARTESIAN_POINT ( 'NONE',  ( 9.832129032723416984, 130.6770833299193555, 5.676582343750006032 ) ) ;
#19840=VECTOR ( 'NONE', #52744, 1000.000000000000000 ) ;
#19843=VECTOR ( 'NONE', #42870, 1000.000000000000000 ) ;
#19844=CARTESIAN_POINT ( 'NONE',  ( -10.00000000000009948, 172.5000000000000568, -1.224646799147365089E-15 ) ) ;
#19846=EDGE_LOOP ( 'NONE', ( #41043, #7298, #56281, #5645 ) ) ;
#19855=CARTESIAN_POINT ( 'NONE',  ( -6.676582343750001591, 292.4531250017069510, 0.000000000000000000 ) ) ;
#19863=VERTEX_POINT ( 'NONE', #4506 ) ;
#19866=CARTESIAN_POINT ( 'NONE',  ( 11.35316468750000141, 111.0937499965860127, 0.000000000000000000 ) ) ;
#19867=CARTESIAN_POINT ( 'NONE',  ( -2.679491924312698004, 121.4583333333334707, -9.999999999999149125 ) ) ;
#19872=ORIENTED_EDGE ( 'NONE', *, *, #63430, .F. ) ;
#19875=CARTESIAN_POINT ( 'NONE',  ( 9.832129032723416984, 225.3645833299193839, 5.676582343750006032 ) ) ;
#19879=CARTESIAN_POINT ( 'NONE',  ( -5.676582343750006032, 199.4270833299193555, 9.832129032723418760 ) ) ;
#19886=CARTESIAN_POINT ( 'NONE',  ( 9.832129032723420536, 86.19791666325268409, -5.676582343749999815 ) ) ;
#19892=CARTESIAN_POINT ( 'NONE',  ( 11.35316468750000141, 90.78124999658602690, 0.000000000000000000 ) ) ;
#19899=CARTESIAN_POINT ( 'NONE',  ( -5.676582343749998039, 72.44791666325268409, -9.832129032723420536 ) ) ;
#19903=CARTESIAN_POINT ( 'NONE',  ( -5.000000000000005329, 175.2083333265053682, 8.660254037844387298 ) ) ;
#19907=CARTESIAN_POINT ( 'NONE',  ( -5.676582343749998039, 67.76041666325268409, -9.832129032723420536 ) ) ;
#19908=CARTESIAN_POINT ( 'NONE',  ( -4.088227598258586603E-16, 294.2031250017069510, -6.676582343750001591 ) ) ;
#19910=CARTESIAN_POINT ( 'NONE',  ( 3.042071309553159519, 199.7395833299193555, 11.35316468750000141 ) ) ;
#19915=CARTESIAN_POINT ( 'NONE',  ( 9.832129032723420536, 196.1979166632526983, -5.676582343749999815 ) ) ;
#19919=VERTEX_POINT ( 'NONE', #22207 ) ;
#19920=CARTESIAN_POINT ( 'NONE',  ( -8.311093377946841443, 184.2187499965860127, 8.311093377946834337 ) ) ;
#19922=CARTESIAN_POINT ( 'NONE',  ( -9.999999999999994671, 92.50000000000001421, -1.224646799147352665E-15 ) ) ;
#19926=CARTESIAN_POINT ( 'NONE',  ( -1.836970198721029983E-15, 3.750000000000000444, 10.00000000000000178 ) ) ;
#19939=ORIENTED_EDGE ( 'NONE', *, *, #30497, .T. ) ;
#19944=ORIENTED_EDGE ( 'NONE', *, *, #51126, .T. ) ;
#19947=CARTESIAN_POINT ( 'NONE',  ( 9.832129032723420536, 61.51041666325268409, -5.676582343749999815 ) ) ;
#19948=CARTESIAN_POINT ( 'NONE',  ( 6.123233995736767268E-16, 113.1249999931720396, -10.00000000000000178 ) ) ;
#19952=CARTESIAN_POINT ( 'NONE',  ( 2.765530957081996366, 294.2968750017070079, -6.676582343750002480 ) ) ;
#19953=CARTESIAN_POINT ( 'NONE',  ( -7.320508075688773708, 141.8750000000000000, -7.320508075688774596 ) ) ;
#19966=CARTESIAN_POINT ( 'NONE',  ( 6.123233995736767268E-16, 131.2500000000000000, -10.00000000000000178 ) ) ;
#19971=CARTESIAN_POINT ( 'NONE',  ( 11.35316468749999785, 35.57291666325267698, 3.042071309553174174 ) ) ;
#19973=CARTESIAN_POINT ( 'NONE',  ( -5.000000000000005329, 15.20833332650536640, 8.660254037844387298 ) ) ;
#19977=CARTESIAN_POINT ( 'NONE',  ( 9.832129032723416984, 45.36458332991934839, 5.676582343750006032 ) ) ;
#19980=CARTESIAN_POINT ( 'NONE',  ( -6.000000000000001776, 299.0000000000000000, 0.000000000000000000 ) ) ;
#19983=CARTESIAN_POINT ( 'NONE',  ( -11.35316468749999785, 28.07291666325268054, -3.042071309553167957 ) ) ;
#19985=CARTESIAN_POINT ( 'NONE',  ( -5.676582343749998039, 157.4479166632526983, -9.832129032723420536 ) ) ;
#19986=CARTESIAN_POINT ( 'NONE',  ( -8.660254037844387298, 128.9583333265053966, -5.000000000000004441 ) ) ;
#19990=CARTESIAN_POINT ( 'NONE',  ( -4.242640687119285658, 289.1249999999999432, 4.242640687119287435 ) ) ;
#19991=CARTESIAN_POINT ( 'NONE',  ( -11.35316468749999785, 23.38541666325268054, -3.042071309553167957 ) ) ;
#19992=CARTESIAN_POINT ( 'NONE',  ( -10.00000000000001243, 17.70833333333333925, 2.679491924311226292 ) ) ;
#19998=CARTESIAN_POINT ( 'NONE',  ( -9.832129032723418760, 157.8645833299193839, -5.676582343750004256 ) ) ;
#20007=CARTESIAN_POINT ( 'NONE',  ( 11.35316468749999785, 105.8854166632526983, 3.042071309553174174 ) ) ;
#20009=ORIENTED_EDGE ( 'NONE', *, *, #8639, .T. ) ;
#20027=CARTESIAN_POINT ( 'NONE',  ( 4.721056650416000089, 298.8281250017069510, 4.721056650415999201 ) ) ;
#20036=CARTESIAN_POINT ( 'NONE',  ( -2.679491924311235618, 108.5416666666666714, 10.00000000000000000 ) ) ;
#20038=CARTESIAN_POINT ( 'NONE',  ( -4.721056650415999201, 295.4843750017070079, -4.721056650415999201 ) ) ;
#20049=CARTESIAN_POINT ( 'NONE',  ( -4.999999999999998224, 221.6666666666666856, -8.660254037844389075 ) ) ;
#20052=CARTESIAN_POINT ( 'NONE',  ( -8.311093377946841443, 199.2187499965860411, 8.311093377946830785 ) ) ;
#20057=ORIENTED_EDGE ( 'NONE', *, *, #39510, .T. ) ;
#20059=CARTESIAN_POINT ( 'NONE',  ( -8.311093377946836114, 47.96874999658601268, -8.311093377946837890 ) ) ;
#20063=FACE_OUTER_BOUND ( 'NONE', #19199, .T. ) ;
#20067=CARTESIAN_POINT ( 'NONE',  ( 5.676582343749993598, 124.9479166632526983, 9.832129032723422313 ) ) ;
#20069=CARTESIAN_POINT ( 'NONE',  ( -7.320508075688773708, 83.74999999317203958, -7.320508075688774596 ) ) ;
#20070=ADVANCED_FACE ( 'NONE', ( #58796 ), #7106, .T. ) ;
#20076=ORIENTED_EDGE ( 'NONE', *, *, #52505, .T. ) ;
#20080=( BOUNDED_CURVE ( )  B_SPLINE_CURVE ( 2, ( #6083, #73994, #40777, #40413, #17014, #63785, #69082, #63043, #57779, #5711, #17388, #63410, #35138 ),
 .UNSPECIFIED., .F., .F. ) 
 B_SPLINE_CURVE_WITH_KNOTS ( ( 3, 2, 2, 2, 2, 2, 3 ),
 ( 0.5180902627193306742, 0.5233241472621503743, 0.5285580318049700743, 0.5337919163477896634, 0.5390258008906093634, 0.5442596854334290635, 0.5494935699762487635 ),
 .UNSPECIFIED. ) 
 CURVE ( )  GEOMETRIC_REPRESENTATION_ITEM ( )  RATIONAL_B_SPLINE_CURVE ( ( 1.000000000000308642, 0.9659258262887597812, 1.000000000000000000, 0.9659258262890683122, 1.000000000000000000, 0.9659258262890683122, 1.000000000000000000, 0.9659258262890683122, 1.000000000000000000, 0.9659258262890683122, 1.000000000000000000, 0.9659258262890683122, 1.000000000000000000 ) ) 
 REPRESENTATION_ITEM ( '' )  );
#20081=CARTESIAN_POINT ( 'NONE',  ( -2.765530957081998586, 293.7968750017069510, 6.676582343750001591 ) ) ;
#20083=CARTESIAN_POINT ( 'NONE',  ( -2.085542519210945728E-15, 164.5312499965860127, 11.35316468750000141 ) ) ;
#20084=CARTESIAN_POINT ( 'NONE',  ( 6.123233995736767268E-16, 168.1249999931720538, -10.00000000000000178 ) ) ;
#20086=CARTESIAN_POINT ( 'NONE',  ( -10.00000000000004619, 192.7083333333333428, 2.679491924311234730 ) ) ;
#20091=CARTESIAN_POINT ( 'NONE',  ( 8.311093377946834337, 155.4687499965859843, 8.311093377946839666 ) ) ;
#20095=CARTESIAN_POINT ( 'NONE',  ( -8.311093377946841443, 69.21874999658602690, 8.311093377946830785 ) ) ;
#20100=VERTEX_POINT ( 'NONE', #64450 ) ;
#20104=CARTESIAN_POINT ( 'NONE',  ( -4.242640687119285658, 289.1875000034139589, 4.242640687119287435 ) ) ;
#20112=DIRECTION ( 'NONE',  ( 0.000000000000000000, 0.000000000000000000, -1.000000000000000000 ) ) ;
#20114=ORIENTED_EDGE ( 'NONE', *, *, #60670, .T. ) ;
#20127=CARTESIAN_POINT ( 'NONE',  ( 6.000000000000003553, 296.5625000000000000, -2.485281374238571761 ) ) ;
#20129=CARTESIAN_POINT ( 'NONE',  ( -7.320508075688773708, 71.87500000000001421, -7.320508075688774596 ) ) ;
#20131=CARTESIAN_POINT ( 'NONE',  ( -2.485281374238571761, 294.8124999999999432, -6.000000000000003553 ) ) ;
#20142=CARTESIAN_POINT ( 'NONE',  ( 10.00000000000000178, 185.0000000000000284, 0.000000000000000000 ) ) ;
#20145=CARTESIAN_POINT ( 'NONE',  ( -5.676582343749998039, 157.7604166632526983, -9.832129032723420536 ) ) ;
#20152=CARTESIAN_POINT ( 'NONE',  ( 8.311093377946834337, 10.46874999658601624, 8.311093377946839666 ) ) ;
#20157=CARTESIAN_POINT ( 'NONE',  ( 2.679491924311222739, 50.83333332650537528, 10.00000000000000355 ) ) ;
#20163=CYLINDRICAL_SURFACE ( 'NONE', #61892, 6.000000000000001776 ) ;
#20168=CARTESIAN_POINT ( 'NONE',  ( -3.042071309553173730, 134.3229166632526983, 11.35316468749999785 ) ) ;
#20175=CARTESIAN_POINT ( 'NONE',  ( 3.042071309553167513, 126.8229166632526841, -11.35316468749999785 ) ) ;
#20179=AXIS2_PLACEMENT_3D ( 'NONE', #69916, #64247, #13282 ) ;
#20182=CARTESIAN_POINT ( 'NONE',  ( -11.35316468750000141, 103.8020833299193413, 3.042071309553159963 ) ) ;
#20186=CARTESIAN_POINT ( 'NONE',  ( -8.311093377946841443, 29.21874999658601979, 8.311093377946830785 ) ) ;
#20193=CARTESIAN_POINT ( 'NONE',  ( -4.088227598258586603E-16, 289.2031250017069510, -6.676582343750001591 ) ) ;
#20195=CARTESIAN_POINT ( 'NONE',  ( 11.35316468749999963, 216.3020833299193555, -3.042071309553165293 ) ) ;
#20198=CARTESIAN_POINT ( 'NONE',  ( 8.311093377946837890, 146.7187499965860411, -8.311093377946837890 ) ) ;
#20215=CARTESIAN_POINT ( 'NONE',  ( 11.35316468749999963, 190.9895833299193271, -3.042071309553165293 ) ) ;
#20219=CARTESIAN_POINT ( 'NONE',  ( -6.676582343749999815, 292.5156250017070079, 2.765530957082001251 ) ) ;
#20222=ORIENTED_EDGE ( 'NONE', *, *, #22513, .F. ) ;
#20229=EDGE_LOOP ( 'NONE', ( #32381, #26182, #19944, #21706 ) ) ;
#20232=CARTESIAN_POINT ( 'NONE',  ( -5.676582343749998039, 117.7604166632526841, -9.832129032723420536 ) ) ;
#20244=CARTESIAN_POINT ( 'NONE',  ( 11.35316468749999785, 190.8854166632526983, 3.042071309553174174 ) ) ;
#20250=CYLINDRICAL_SURFACE ( 'NONE', #43557, 10.00000000000000178 ) ;
#20251=CARTESIAN_POINT ( 'NONE',  ( -5.676582343749998039, 77.44791666325269830, -9.832129032723420536 ) ) ;
#20254=CARTESIAN_POINT ( 'NONE',  ( 2.696524195522682164E-11, 156.2499999999978968, -10.00000000000000178 ) ) ;
#20256=CARTESIAN_POINT ( 'NONE',  ( 3.042071309553167069, 86.82291666325265567, -11.35316468749999785 ) ) ;
#20260=CARTESIAN_POINT ( 'NONE',  ( 11.35316468750000141, 0.7812499965860163487, 0.000000000000000000 ) ) ;
#20263=CARTESIAN_POINT ( 'NONE',  ( 3.042071309553167513, 71.82291666325268409, -11.35316468749999785 ) ) ;
#20265=CARTESIAN_POINT ( 'NONE',  ( 7.320508075688771044, 129.3750000000000284, 7.320508075688775484 ) ) ;
#20267=EDGE_CURVE ( 'NONE', #42156, #39904, #42552, .T. ) ;
#20268=CARTESIAN_POINT ( 'NONE',  ( -4.999999999999998224, 173.5416666598387110, -8.660254037844389075 ) ) ;
#20272=CARTESIAN_POINT ( 'NONE',  ( 3.042071309553159519, 65.05208332991934128, 11.35316468750000141 ) ) ;
#20273=CARTESIAN_POINT ( 'NONE',  ( 6.676582343750004256, 294.8906250017069510, 2.765530957081995478 ) ) ;
#20275=CARTESIAN_POINT ( 'NONE',  ( -3.042071309553164404, 207.2395833299193555, -11.35316468749999963 ) ) ;
#20278=LINE ( 'NONE', #43301, #58138 ) ;
#20281=CARTESIAN_POINT ( 'NONE',  ( -5.676582343750006032, 194.1145833299193839, 9.832129032723418760 ) ) ;
#20287=CARTESIAN_POINT ( 'NONE',  ( -9.832129032723418760, 183.1770833299193555, -5.676582343750004256 ) ) ;
#20290=( BOUNDED_CURVE ( )  B_SPLINE_CURVE ( 2, ( #18994, #48026, #48398, #29584, #18634, #8044, #18260, #35620, #12951 ),
 .UNSPECIFIED., .F., .F. ) 
 B_SPLINE_CURVE_WITH_KNOTS ( ( 3, 2, 2, 2, 3 ),
 ( 0.7291666666666649643, 0.7395833333333317050, 0.7499999999999983347, 0.7604166666666649643, 0.7708333333333317050 ),
 .UNSPECIFIED. ) 
 CURVE ( )  GEOMETRIC_REPRESENTATION_ITEM ( )  RATIONAL_B_SPLINE_CURVE ( ( 1.000000000000012212, 0.9238795325112745260, 1.000000000000000000, 0.9238795325112867385, 1.000000000000000000, 0.9238795325112867385, 1.000000000000000000, 0.9238795325112989509, 0.9999999999999877875 ) ) 
 REPRESENTATION_ITEM ( '' )  );
#20291=CARTESIAN_POINT ( 'NONE',  ( -8.660254037844381969, 92.08333333333332860, -5.000000000000000888 ) ) ;
#20296=DIRECTION ( 'NONE',  ( -0.000000000000000000, 1.000000000000000000, -0.000000000000000000 ) ) ;
#20304=CARTESIAN_POINT ( 'NONE',  ( -10.00000000000011724, 82.50000000000007105, -1.224646799147367456E-15 ) ) ;
#20308=ORIENTED_EDGE ( 'NONE', *, *, #8504, .F. ) ;
#20315=CARTESIAN_POINT ( 'NONE',  ( 9.832129032723416984, 70.67708332991935549, 5.676582343750006032 ) ) ;
#20320=CARTESIAN_POINT ( 'NONE',  ( -2.765530957081996810, 294.4218750017069510, -6.676582343750002480 ) ) ;
#20321=CARTESIAN_POINT ( 'NONE',  ( 2.679491924311228956, 146.0416666666666288, -10.00000000000000000 ) ) ;
#20322=AXIS2_PLACEMENT_3D ( 'NONE', #22613, #45634, #35811 ) ;
#20333=CARTESIAN_POINT ( 'NONE',  ( -1.836970198721029983E-15, 20.62499999317203603, 10.00000000000000178 ) ) ;
#20338=CARTESIAN_POINT ( 'NONE',  ( 3.042071309553167069, 36.82291666325268409, -11.35316468749999785 ) ) ;
#20340=CARTESIAN_POINT ( 'NONE',  ( -2.679491924311225848, 3.333333326505365513, -10.00000000000000178 ) ) ;
#20344=CARTESIAN_POINT ( 'NONE',  ( 0.000000000000000000, 300.0000000000000000, 10.00000000000000178 ) ) ;
#20345=CARTESIAN_POINT ( 'NONE',  ( -11.35316468750000141, 53.48958332991935549, 3.042071309553159963 ) ) ;
#20351=CARTESIAN_POINT ( 'NONE',  ( -11.35316468749999785, 33.07291666325268409, -3.042071309553167957 ) ) ;
#20354=CARTESIAN_POINT ( 'NONE',  ( 6.951808397369818766E-16, 162.0312499965860127, -11.35316468750000141 ) ) ;
#20356=CARTESIAN_POINT ( 'NONE',  ( 10.00000000000000000, 131.6666666598386541, 2.679491924311236062 ) ) ;
#20360=CARTESIAN_POINT ( 'NONE',  ( -8.311093377946836114, 22.96874999658601979, -8.311093377946837890 ) ) ;
#20362=ORIENTED_EDGE ( 'NONE', *, *, #47390, .T. ) ;
#20367=CARTESIAN_POINT ( 'NONE',  ( -2.085542519210945728E-15, 159.5312499965860127, 11.35316468750000141 ) ) ;
#20377=CARTESIAN_POINT ( 'NONE',  ( 7.347880794884121708E-16, 300.0000000000000000, -6.000000000000001776 ) ) ;
#20379=CARTESIAN_POINT ( 'NONE',  ( 9.832129032723420536, 96.51041666325268409, -5.676582343749999815 ) ) ;
#20389=( BOUNDED_CURVE ( )  B_SPLINE_CURVE ( 2, ( #36861, #31569, #54593, #32327, #25148 ),
 .UNSPECIFIED., .F., .F. ) 
 B_SPLINE_CURVE_WITH_KNOTS ( ( 3, 2, 3 ),
 ( 0.000000000000000000, 0.01041666666666551944, 0.02083333333333103887 ),
 .UNSPECIFIED. ) 
 CURVE ( )  GEOMETRIC_REPRESENTATION_ITEM ( )  RATIONAL_B_SPLINE_CURVE ( ( 1.000000000000000000, 0.9238795325112867385, 1.000000000000000000, 0.9238795325113035029, 0.9999999999999832356 ) ) 
 REPRESENTATION_ITEM ( '' )  );
#20392=CARTESIAN_POINT ( 'NONE',  ( -10.00000000000000000, 159.1666666598386541, -2.679491924311229845 ) ) ;
#20400=( BOUNDED_CURVE ( )  B_SPLINE_CURVE ( 2, ( #44485, #55440, #20715, #32429, #59963, #38460, #8281, #36957, #67498, #61083, #2632, #48634, #20333 ),
 .UNSPECIFIED., .F., .F. ) 
 B_SPLINE_CURVE_WITH_KNOTS ( ( 3, 2, 2, 2, 2, 2, 3 ),
 ( 0.07065217391304347283, 0.07246376811594203160, 0.07427536231884057649, 0.07608695652173913526, 0.07789855072463768015, 0.07971014492753622505, 0.08152173913043478382 ),
 .UNSPECIFIED. ) 
 CURVE ( )  GEOMETRIC_REPRESENTATION_ITEM ( )  RATIONAL_B_SPLINE_CURVE ( ( 1.000000000000000000, 0.9659258262890683122, 1.000000000000000000, 0.9659258262890683122, 1.000000000000000000, 0.9659258262890683122, 1.000000000000000000, 0.9659258262890683122, 1.000000000000000000, 0.9659258262890683122, 1.000000000000000000, 0.9659258262890683122, 1.000000000000000000 ) ) 
 REPRESENTATION_ITEM ( '' )  );
#20412=CARTESIAN_POINT ( 'NONE',  ( 8.660254037844389075, 110.4166666666666714, -5.000000000000000000 ) ) ;
#20414=CARTESIAN_POINT ( 'NONE',  ( 6.676582343750004256, 294.0468750017070079, 2.765530957081995478 ) ) ;
#20426=CARTESIAN_POINT ( 'NONE',  ( -1.836970198721029983E-15, 223.7500000000000000, 10.00000000000000178 ) ) ;
#20428=CARTESIAN_POINT ( 'NONE',  ( -11.35316468749999785, 193.3854166632526415, -3.042071309553167513 ) ) ;
#20437=CARTESIAN_POINT ( 'NONE',  ( 11.35316468750000141, 10.78124999658601624, 0.000000000000000000 ) ) ;
#20445=CARTESIAN_POINT ( 'NONE',  ( 11.35316468749999963, 115.9895833299193555, -3.042071309553165293 ) ) ;
#20446=CARTESIAN_POINT ( 'NONE',  ( -10.00000000000000000, 84.16666665983869677, -2.679491924311229845 ) ) ;
#20449=CARTESIAN_POINT ( 'NONE',  ( -8.660254037844387298, 198.9583333265053682, -5.000000000000004441 ) ) ;
#20450=EDGE_LOOP ( 'NONE', ( #13073, #40002, #63217, #23757 ) ) ;
#20451=CARTESIAN_POINT ( 'NONE',  ( -5.010062319353657756, 225.9999999999999716, -8.679233769287526101 ) ) ;
#20452=CARTESIAN_POINT ( 'NONE',  ( 6.676582343750003368, 295.1718750017070079, -2.765530957081997254 ) ) ;
#20455=CARTESIAN_POINT ( 'NONE',  ( 9.832129032723416984, 175.3645833299193555, 5.676582343750006032 ) ) ;
#20461=CARTESIAN_POINT ( 'NONE',  ( 11.35316468749999963, 161.3020833299193555, -3.042071309553165293 ) ) ;
#20465=CARTESIAN_POINT ( 'NONE',  ( 5.676582343750001591, 56.92708332991935549, -9.832129032723420536 ) ) ;
#20466=VERTEX_POINT ( 'NONE', #55698 ) ;
#20471=CARTESIAN_POINT ( 'NONE',  ( 1.102182119232618108E-15, 290.3125000034140157, 6.000000000000001776 ) ) ;
#20472=CARTESIAN_POINT ( 'NONE',  ( 7.320508075688774596, 67.49999999317201116, -7.320508075688774596 ) ) ;
#20495=DIRECTION ( 'NONE',  ( 0.000000000000000000, 0.000000000000000000, 1.000000000000000000 ) ) ;
#20499=CARTESIAN_POINT ( 'NONE',  ( 8.660254037844385522, 69.58333333333334281, 5.000000000000005329 ) ) ;
#20501=CARTESIAN_POINT ( 'NONE',  ( 6.000000000000003553, 291.4375000000000568, 2.485281374238571317 ) ) ;
#20513=CARTESIAN_POINT ( 'NONE',  ( 10.00000000000000178, 190.0000000000000000, 0.000000000000000000 ) ) ;
#20517=CARTESIAN_POINT ( 'NONE',  ( -3.042071309553164404, 157.5520833299193555, -11.35316468749999963 ) ) ;
#20522=DIRECTION ( 'NONE',  ( -0.000000000000000000, 1.000000000000000000, -0.000000000000000000 ) ) ;
#20524=ORIENTED_EDGE ( 'NONE', *, *, #43571, .F. ) ;
#20525=CARTESIAN_POINT ( 'NONE',  ( 8.311093377946837890, 16.71874999658601268, -8.311093377946837890 ) ) ;
#20527=EDGE_CURVE ( 'NONE', #32479, #31223, #50269, .T. ) ;
#20530=FACE_OUTER_BOUND ( 'NONE', #35831, .T. ) ;
#20532=VECTOR ( 'NONE', #54313, 1000.000000000000000 ) ;
#20533=CARTESIAN_POINT ( 'NONE',  ( -8.660254037844387298, 43.95833332650536818, -5.000000000000004441 ) ) ;
#20536=CARTESIAN_POINT ( 'NONE',  ( 1.110124581937998163E-11, 98.75000000000088107, 10.00000000000000533 ) ) ;
#20546=CARTESIAN_POINT ( 'NONE',  ( 9.832129032723416984, 125.3645833299193413, 5.676582343750006032 ) ) ;
#20549=AXIS2_PLACEMENT_3D ( 'NONE', #37194, #36091, #54927 ) ;
#20551=DIRECTION ( 'NONE',  ( 0.000000000000000000, -0.000000000000000000, -1.000000000000000000 ) ) ;
#20553=CARTESIAN_POINT ( 'NONE',  ( -1.836970198721029983E-15, 155.6249999931720254, 10.00000000000000178 ) ) ;
#20555=CARTESIAN_POINT ( 'NONE',  ( 11.35316468750000141, 125.7812499965860127, 0.000000000000000000 ) ) ;
#20557=ORIENTED_EDGE ( 'NONE', *, *, #49032, .F. ) ;
#20558=ADVANCED_FACE ( 'NONE', ( #57178 ), #73404, .T. ) ;
#20559=CARTESIAN_POINT ( 'NONE',  ( -1.836970198721029983E-15, 50.62499999317203248, 10.00000000000000178 ) ) ;
#20561=CARTESIAN_POINT ( 'NONE',  ( -3.042071309553173730, 114.6354166632526983, 11.35316468749999785 ) ) ;
#20565=CARTESIAN_POINT ( 'NONE',  ( 8.311093377946837890, 21.71874999658601268, -8.311093377946837890 ) ) ;
#20573=CARTESIAN_POINT ( 'NONE',  ( -3.673940397442060854E-16, 298.8125000034140157, -6.000000000000001776 ) ) ;
#20576=VECTOR ( 'NONE', #37990, 1000.000000000000000 ) ;
#20578=CARTESIAN_POINT ( 'NONE',  ( 11.35316468750000141, 146.0937499965860411, 0.000000000000000000 ) ) ;
#20580=EDGE_CURVE ( 'NONE', #51233, #45113, #6430, .T. ) ;
#20592=CYLINDRICAL_SURFACE ( 'NONE', #27050, 6.000000000000001776 ) ;
#20593=CARTESIAN_POINT ( 'NONE',  ( 8.311093377946837890, 181.4062499965860411, -8.311093377946837890 ) ) ;
#20597=CARTESIAN_POINT ( 'NONE',  ( -6.676582343750002480, 291.3906250017070079, -2.765530957081996810 ) ) ;
#20603=MECHANICAL_DESIGN_GEOMETRIC_PRESENTATION_REPRESENTATION('',(#53162),#39967);
#20608=DIRECTION ( 'NONE',  ( -0.000000000000000000, 1.000000000000000000, -0.000000000000000000 ) ) ;
#20611=CARTESIAN_POINT ( 'NONE',  ( -11.35316468750000141, 108.8020833299193555, 3.042071309553159963 ) ) ;
#20626=CARTESIAN_POINT ( 'NONE',  ( -5.676582343749998039, 192.7604166632526983, -9.832129032723420536 ) ) ;
#20628=CARTESIAN_POINT ( 'NONE',  ( 4.951454888531130472, 225.9999999999999716, 8.768144228917044813 ) ) ;
#20633=CARTESIAN_POINT ( 'NONE',  ( 5.676582343750001591, 76.61458332991935549, -9.832129032723420536 ) ) ;
#20634=ORIENTED_EDGE ( 'NONE', *, *, #49676, .T. ) ;
#20638=CARTESIAN_POINT ( 'NONE',  ( 10.00000000000016165, 40.00000000000009948, 0.000000000000000000 ) ) ;
#20641=CARTESIAN_POINT ( 'NONE',  ( 6.951808397369818766E-16, 87.03124999658602690, -11.35316468750000141 ) ) ;
#20649=CARTESIAN_POINT ( 'NONE',  ( 3.042071309553159519, 89.73958332991935549, 11.35316468750000141 ) ) ;
#20652=CARTESIAN_POINT ( 'NONE',  ( -10.00000000000000000, 169.1666666598387110, -2.679491924311229845 ) ) ;
#20655=CARTESIAN_POINT ( 'NONE',  ( 6.951808397369818766E-16, 77.34374999658601268, -11.35316468750000141 ) ) ;
#20656=CARTESIAN_POINT ( 'NONE',  ( 6.676582343750003368, 293.0156250017070079, -2.765530957081997254 ) ) ;
#20658=CARTESIAN_POINT ( 'NONE',  ( 8.311093377946834337, 215.1562499965860127, 8.311093377946839666 ) ) ;
#20660=CARTESIAN_POINT ( 'NONE',  ( 11.35316468750000141, 1.093749996586016682, 0.000000000000000000 ) ) ;
#20664=CARTESIAN_POINT ( 'NONE',  ( -9.832129032723418760, 202.8645833299193555, -5.676582343750004256 ) ) ;
#20669=CARTESIAN_POINT ( 'NONE',  ( 3.042071309553167513, 182.1354166632526699, -11.35316468749999785 ) ) ;
#20675=APPLICATION_CONTEXT ( 'automotive_design' ) ;
#20676=CARTESIAN_POINT ( 'NONE',  ( -4.999999999999998224, 6.666666666666666963, -8.660254037844389075 ) ) ;
#20683=ORIENTED_EDGE ( 'NONE', *, *, #70313, .T. ) ;
#20686=CARTESIAN_POINT ( 'NONE',  ( -7.320508075688858085, 81.87500000000008527, -7.320508075688859861 ) ) ;
#20698=CARTESIAN_POINT ( 'NONE',  ( -2.085542519210945728E-15, 74.84374999658602690, 11.35316468750000141 ) ) ;
#20703=CARTESIAN_POINT ( 'NONE',  ( 2.765530957082001251, 295.9218750017069510, 6.676582343749999815 ) ) ;
#20711=AXIS2_PLACEMENT_3D ( 'NONE', #52757, #52390, #58430 ) ;
#20715=CARTESIAN_POINT ( 'NONE',  ( -4.999999999999998224, 18.54166665983870033, -8.660254037844389075 ) ) ;
#20720=CARTESIAN_POINT ( 'NONE',  ( 9.832129032723416984, 40.36458332991934839, 5.676582343750006032 ) ) ;
#20722=CARTESIAN_POINT ( 'NONE',  ( 7.320508075688774596, 2.499999993172032031, -7.320508075688774596 ) ) ;
#20725=CARTESIAN_POINT ( 'NONE',  ( 10.00000000000000000, 141.6666666598387110, 2.679491924311235618 ) ) ;
#20727=CARTESIAN_POINT ( 'NONE',  ( -11.35316468750000141, 48.28124999658601268, -1.390361679473963753E-15 ) ) ;
#20733=CARTESIAN_POINT ( 'NONE',  ( -3.042071309553163960, 47.23958332991934839, -11.35316468749999963 ) ) ;
#20736=CARTESIAN_POINT ( 'NONE',  ( 11.35316468750000141, 160.7812499965860127, 0.000000000000000000 ) ) ;
#20737=CARTESIAN_POINT ( 'NONE',  ( -8.660254037844387298, 123.9583333265053682, -5.000000000000004441 ) ) ;
#20742=CARTESIAN_POINT ( 'NONE',  ( -8.311093377946836114, 17.96874999658601624, -8.311093377946837890 ) ) ;
#20750=CARTESIAN_POINT ( 'NONE',  ( 5.676582343749993598, 149.9479166632526983, 9.832129032723422313 ) ) ;
#20759=CARTESIAN_POINT ( 'NONE',  ( -1.836970198721029983E-15, 155.6249999931720254, 10.00000000000000178 ) ) ;
#20760=CARTESIAN_POINT ( 'NONE',  ( 8.311093377946837890, 106.7187499965860269, -8.311093377946837890 ) ) ;
#20771=CARTESIAN_POINT ( 'NONE',  ( -5.000000000000005329, 160.2083333265053966, 8.660254037844387298 ) ) ;
#20784=ORIENTED_EDGE ( 'NONE', *, *, #38615, .F. ) ;
#20785=ORIENTED_EDGE ( 'NONE', *, *, #24459, .F. ) ;
#20787=CARTESIAN_POINT ( 'NONE',  ( 10.00000000000000178, 124.7916666666666572, 2.679491924311236062 ) ) ;
#20791=CARTESIAN_POINT ( 'NONE',  ( 10.00000000000007638, 59.79166666666671404, 2.679491924311256490 ) ) ;
#20792=CARTESIAN_POINT ( 'NONE',  ( 2.679491924311222739, 103.9583333333333144, 10.00000000000000355 ) ) ;
#20797=CARTESIAN_POINT ( 'NONE',  ( -6.676582343750000703, 291.6718750017069510, 2.765530957082001251 ) ) ;
#20809=CARTESIAN_POINT ( 'NONE',  ( 9.832129032723420536, 1.197916663252682978, -5.676582343749999815 ) ) ;
#20811=CARTESIAN_POINT ( 'NONE',  ( -3.042071309553173730, 199.6354166632526699, 11.35316468749999785 ) ) ;
#20812=CARTESIAN_POINT ( 'NONE',  ( -8.660254037844390851, 134.7916666598387110, 4.999999999999998224 ) ) ;
#20815=DIRECTION ( 'NONE',  ( 0.000000000000000000, 0.000000000000000000, 1.000000000000000000 ) ) ;
#20819=CARTESIAN_POINT ( 'NONE',  ( 6.951808397369818766E-16, 12.03124999658601801, -11.35316468750000141 ) ) ;
#20828=CARTESIAN_POINT ( 'NONE',  ( 5.676582343750001591, 121.6145833299193555, -9.832129032723420536 ) ) ;
#20829=CARTESIAN_POINT ( 'NONE',  ( -7.320508075688778149, 84.99999999317203958, 7.320508075688769267 ) ) ;
#20833=CARTESIAN_POINT ( 'NONE',  ( 4.999999999999997335, 144.1666666666666572, 8.660254037844396180 ) ) ;
#20836=CARTESIAN_POINT ( 'NONE',  ( 4.721056650416000089, 287.9843750017070079, 4.721056650415999201 ) ) ;
#20840=CARTESIAN_POINT ( 'NONE',  ( 10.00000000000000178, 207.0833333265053966, -2.679491924311226736 ) ) ;
#20843=ORIENTED_EDGE ( 'NONE', *, *, #35143, .F. ) ;
#20844=( BOUNDED_CURVE ( )  B_SPLINE_CURVE ( 2, ( #23201, #39808, #5124, #5864, #28860, #51881, #57174, #62812, #5490, #63560, #46213, #45462, #41302 ),
 .UNSPECIFIED., .F., .F. ) 
 B_SPLINE_CURVE_WITH_KNOTS ( ( 3, 2, 2, 2, 2, 2, 3 ),
 ( 0.7064942623220252793, 0.7117267818841473970, 0.7169593014462694036, 0.7221918210083915213, 0.7274243405705135279, 0.7326568601326356456, 0.7378893796947577632 ),
 .UNSPECIFIED. ) 
 CURVE ( )  GEOMETRIC_REPRESENTATION_ITEM ( )  RATIONAL_B_SPLINE_CURVE ( ( 1.000000000000000000, 0.9659258262890683122, 1.000000000000000000, 0.9659258262890683122, 1.000000000000000000, 0.9659258262890683122, 1.000000000000000000, 0.9659258262890683122, 1.000000000000000000, 0.9659258262890683122, 1.000000000000000000, 0.9659258262891518010, 0.9999999999999165112 ) ) 
 REPRESENTATION_ITEM ( '' )  );
#20846=CARTESIAN_POINT ( 'NONE',  ( 9.832129032723416984, 155.6770833299193555, 5.676582343750006032 ) ) ;
#20847=CARTESIAN_POINT ( 'NONE',  ( -8.660254037844392627, 217.9166666666666856, 5.000000000000000000 ) ) ;
#20850=CARTESIAN_POINT ( 'NONE',  ( -5.676582343750006032, 64.42708332991935549, 9.832129032723418760 ) ) ;
#20856=CARTESIAN_POINT ( 'NONE',  ( 2.485281374238571317, 289.7500000034140157, -6.000000000000003553 ) ) ;
#20880=CARTESIAN_POINT ( 'NONE',  ( 2.679491924311228956, 66.04166666666667140, -10.00000000000000000 ) ) ;
#20883=CARTESIAN_POINT ( 'NONE',  ( 4.242640687119285658, 292.6249999999999432, -4.242640687119286547 ) ) ;
#20891=CARTESIAN_POINT ( 'NONE',  ( -3.673940397442060854E-16, 290.8125000034140157, -6.000000000000001776 ) ) ;
#20894=CARTESIAN_POINT ( 'NONE',  ( -10.00000000000000355, 187.7083333333332860, 2.679491924311223183 ) ) ;
#20895=DIRECTION ( 'NONE',  ( -0.000000000000000000, 1.000000000000000000, -0.000000000000000000 ) ) ;
#20897=CARTESIAN_POINT ( 'NONE',  ( -9.832129032723420536, 149.0104166632526699, 5.676582343749997150 ) ) ;
#20902=LINE ( 'NONE', #43924, #38693 ) ;
#20905=CARTESIAN_POINT ( 'NONE',  ( -8.311093377946836114, 22.96874999658601624, -8.311093377946837890 ) ) ;
#20907=CARTESIAN_POINT ( 'NONE',  ( 7.320508075688774596, 97.49999999317203958, -7.320508075688774596 ) ) ;
#20910=CARTESIAN_POINT ( 'NONE',  ( -2.249999999999998668, 255.9999999999999432, 7.677076266392048431 ) ) ;
#20912=CARTESIAN_POINT ( 'NONE',  ( 10.00000000000000178, 47.08333332650536107, -2.679491924311226736 ) ) ;
#20915=CARTESIAN_POINT ( 'NONE',  ( 7.320508075688758609, 99.37499999999997158, 7.320508075688762162 ) ) ;
#20918=CARTESIAN_POINT ( 'NONE',  ( 10.00000000000002132, 160.2083333333333712, -2.679491924311232953 ) ) ;
#20920=ORIENTED_EDGE ( 'NONE', *, *, #38495, .F. ) ;
#20921=CARTESIAN_POINT ( 'NONE',  ( 2.679491924332284114, 31.04166666666478491, -9.999999999987847943 ) ) ;
#20923=CARTESIAN_POINT ( 'NONE',  ( 3.042071309553167069, 131.8229166632526983, -11.35316468749999785 ) ) ;
#20929=FACE_OUTER_BOUND ( 'NONE', #38219, .T. ) ;
#20930=CARTESIAN_POINT ( 'NONE',  ( -1.836970198721029983E-15, 210.6249999931720538, 10.00000000000000178 ) ) ;
#20931=CARTESIAN_POINT ( 'NONE',  ( -8.311093377946841443, 128.9062499965860411, 8.311093377946834337 ) ) ;
#20932=CARTESIAN_POINT ( 'NONE',  ( -1.836970198721029983E-15, 125.6249999931720254, 10.00000000000000178 ) ) ;
#20934=CARTESIAN_POINT ( 'NONE',  ( 1.224646799147353454E-15, 300.0000000000000000, -10.00000000000000178 ) ) ;
#20937=CARTESIAN_POINT ( 'NONE',  ( 3.042071309553167513, 112.1354166632526699, -11.35316468749999785 ) ) ;
#20941=CARTESIAN_POINT ( 'NONE',  ( -11.35316468750000141, 23.80208332991934839, 3.042071309553159963 ) ) ;
#20943=DIRECTION ( 'NONE',  ( 0.000000000000000000, 0.000000000000000000, 1.000000000000000000 ) ) ;
#20948=CARTESIAN_POINT ( 'NONE',  ( 6.000000000000003553, 298.5000000034140157, 2.485281374238571317 ) ) ;
#20949=DIRECTION ( 'NONE',  ( -0.000000000000000000, 1.000000000000000000, -0.000000000000000000 ) ) ;
#20951=ORIENTED_EDGE ( 'NONE', *, *, #18262, .F. ) ;
#20952=CARTESIAN_POINT ( 'NONE',  ( 8.311093377946834337, 145.4687499965860411, 8.311093377946839666 ) ) ;
#20954=( BOUNDED_CURVE ( )  B_SPLINE_CURVE ( 2, ( #34867, #533, #23513, #14961, #40876, #25354, #1272, #53314, #35231, #65358, #31025, #29924, #58607 ),
 .UNSPECIFIED., .F., .F. ) 
 B_SPLINE_CURVE_WITH_KNOTS ( ( 3, 2, 2, 2, 2, 2, 3 ),
 ( 0.5271739130434782705, 0.5289855072463768293, 0.5307971014492753881, 0.5326086956521739468, 0.5344202898550725056, 0.5362318840579710644, 0.5380434782608695121 ),
 .UNSPECIFIED. ) 
 CURVE ( )  GEOMETRIC_REPRESENTATION_ITEM ( )  RATIONAL_B_SPLINE_CURVE ( ( 1.000000000000000000, 0.9659258262890683122, 1.000000000000000000, 0.9659258262890683122, 1.000000000000000000, 0.9659258262890683122, 1.000000000000000000, 0.9659258262890683122, 1.000000000000000000, 0.9659258262890683122, 1.000000000000000000, 0.9659258262890683122, 1.000000000000000000 ) ) 
 REPRESENTATION_ITEM ( '' )  );
#20968=CARTESIAN_POINT ( 'NONE',  ( 8.311093377946834337, 180.1562499965859843, 8.311093377946839666 ) ) ;
#20971=CARTESIAN_POINT ( 'NONE',  ( -2.765530957081996810, 290.2656250017069510, -6.676582343750002480 ) ) ;
#20973=CARTESIAN_POINT ( 'NONE',  ( -7.320508075688776373, 66.87500000000000000, -7.320508075688777261 ) ) ;
#20986=CARTESIAN_POINT ( 'NONE',  ( -11.35316468750000141, 113.8020833299193555, 3.042071309553159963 ) ) ;
#20987=CARTESIAN_POINT ( 'NONE',  ( 8.660254037844385522, 211.4583333265053682, 5.000000000000005329 ) ) ;
#20991=CARTESIAN_POINT ( 'NONE',  ( 6.000000000000001776, 298.5000000000000000, -7.347880794884121708E-16 ) ) ;
#20993=CARTESIAN_POINT ( 'NONE',  ( -6.362988438888832046E-13, 223.7499999999999147, 9.999999999999998224 ) ) ;
#20998=CARTESIAN_POINT ( 'NONE',  ( -3.042071309553173730, 209.6354166632526415, 11.35316468749999785 ) ) ;
#21000=DIRECTION ( 'NONE',  ( -0.000000000000000000, 1.000000000000000000, -0.000000000000000000 ) ) ;
#21004=CARTESIAN_POINT ( 'NONE',  ( 7.320508075688770155, 185.6249999999999716, -7.320508075688770155 ) ) ;
#21006=CARTESIAN_POINT ( 'NONE',  ( 11.35316468749999785, 100.5729166632526699, 3.042071309553174174 ) ) ;
#21014=CARTESIAN_POINT ( 'NONE',  ( -3.042071309553173730, 84.32291666325268409, 11.35316468749999785 ) ) ;
#21022=CARTESIAN_POINT ( 'NONE',  ( -11.35316468749999785, 83.07291666325268409, -3.042071309553167957 ) ) ;
#21026=CARTESIAN_POINT ( 'NONE',  ( -2.679491924311235618, 185.4166666598386826, 10.00000000000000000 ) ) ;
#21028=CARTESIAN_POINT ( 'NONE',  ( 9.832129032723420536, 71.51041666325268409, -5.676582343749999815 ) ) ;
#21029=CARTESIAN_POINT ( 'NONE',  ( 6.676582343750004256, 293.8906250017069510, 2.765530957081995478 ) ) ;
#21030=EDGE_CURVE ( 'NONE', #2370, #70895, #47837, .T. ) ;
#21032=CARTESIAN_POINT ( 'NONE',  ( -5.676582343750006032, 204.1145833299193555, 9.832129032723418760 ) ) ;
#21034=CARTESIAN_POINT ( 'NONE',  ( -5.000000000000005329, 70.20833332650538239, 8.660254037844387298 ) ) ;
#21038=CARTESIAN_POINT ( 'NONE',  ( 8.311093377946837890, 206.4062499965860127, -8.311093377946837890 ) ) ;
#21043=CARTESIAN_POINT ( 'NONE',  ( -9.832129032723418760, 198.1770833299193555, -5.676582343750004256 ) ) ;
#21049=EDGE_CURVE ( 'NONE', #53778, #3815, #71808, .T. ) ;
#21052=CARTESIAN_POINT ( 'NONE',  ( -5.000000000000005329, 13.33333333333333393, 8.660254037844387298 ) ) ;
#21073=EDGE_LOOP ( 'NONE', ( #5878, #15451, #52600, #19183 ) ) ;
#21075=CARTESIAN_POINT ( 'NONE',  ( -11.35316468750000141, 73.80208332991935549, 3.042071309553159963 ) ) ;
#21080=CARTESIAN_POINT ( 'NONE',  ( 6.676582343750001591, 289.1093750017069510, -8.176455196517173205E-16 ) ) ;
#21090=CARTESIAN_POINT ( 'NONE',  ( 8.311093377946834337, 165.4687499965859843, 8.311093377946839666 ) ) ;
#21093=CARTESIAN_POINT ( 'NONE',  ( -6.000000000000003553, 293.0000000034139589, -2.485281374238571317 ) ) ;
#21098=CARTESIAN_POINT ( 'NONE',  ( -9.832129032723418760, 47.86458332991935549, -5.676582343750004256 ) ) ;
#21101=CARTESIAN_POINT ( 'NONE',  ( 10.00000000000000000, 26.66666665983870033, 2.679491924311236062 ) ) ;
#21104=CARTESIAN_POINT ( 'NONE',  ( 7.320508075688771044, 141.2499999931720254, 7.320508075688775484 ) ) ;
#21105=CARTESIAN_POINT ( 'NONE',  ( -8.660254037844390851, 169.7916666598387110, 4.999999999999998224 ) ) ;
#21106=CARTESIAN_POINT ( 'NONE',  ( 5.676582343750001591, 46.61458332991934839, -9.832129032723420536 ) ) ;
#21112=CARTESIAN_POINT ( 'NONE',  ( 8.311093377946837890, 46.40624999658601268, -8.311093377946837890 ) ) ;
#21114=CARTESIAN_POINT ( 'NONE',  ( 3.178432602446558121E-13, 206.2500000000000000, -10.00000000000000533 ) ) ;
#21115=CARTESIAN_POINT ( 'NONE',  ( 11.35316468750000141, 165.7812499965860411, 0.000000000000000000 ) ) ;
#21116=CARTESIAN_POINT ( 'NONE',  ( -10.00000000000000355, 139.5833333265053966, 2.679491924311223183 ) ) ;
#21119=CARTESIAN_POINT ( 'NONE',  ( -8.311093377946836114, 37.96874999658601979, -8.311093377946837890 ) ) ;
#21126=CARTESIAN_POINT ( 'NONE',  ( 3.042071309553167513, 171.8229166632526983, -11.35316468749999785 ) ) ;
#21131=ORIENTED_EDGE ( 'NONE', *, *, #40215, .T. ) ;
#21133=CYLINDRICAL_SURFACE ( 'NONE', #35184, 10.00000000000000178 ) ;
#21134=CARTESIAN_POINT ( 'NONE',  ( 11.35316468749999963, 116.3020833299193413, -3.042071309553165293 ) ) ;
#21145=VECTOR ( 'NONE', #61339, 1000.000000000000000 ) ;
#21155=CARTESIAN_POINT ( 'NONE',  ( 2.765530957082001251, 298.7656250017070079, 6.676582343749999815 ) ) ;
#21158=( BOUNDED_CURVE ( )  B_SPLINE_CURVE ( 2, ( #15743, #10845, #39146, #32756, #61785, #62887, #17238, #67817, #11220 ),
 .UNSPECIFIED., .F., .F. ) 
 B_SPLINE_CURVE_WITH_KNOTS ( ( 3, 2, 2, 2, 3 ),
 ( 0.6874999999999982236, 0.6979166666666648533, 0.7083333333333317050, 0.7187499999999983347, 0.7291666666666649643 ),
 .UNSPECIFIED. ) 
 CURVE ( )  GEOMETRIC_REPRESENTATION_ITEM ( )  RATIONAL_B_SPLINE_CURVE ( ( 1.000000000000012879, 0.9238795325112737489, 1.000000000000000000, 0.9238795325112867385, 1.000000000000000000, 0.9238795325112867385, 1.000000000000000000, 0.9238795325112989509, 0.9999999999999877875 ) ) 
 REPRESENTATION_ITEM ( '' )  );
#21165=CARTESIAN_POINT ( 'NONE',  ( -1.269107444400135093E-11, 58.74999999999901945, 10.00000000000000178 ) ) ;
#21166=CARTESIAN_POINT ( 'NONE',  ( 8.660254037844385522, 109.5833333333333428, 5.000000000000005329 ) ) ;
#21168=CARTESIAN_POINT ( 'NONE',  ( 4.721056650415999201, 292.2343750017069510, -4.721056650415999201 ) ) ;
#21171=DIRECTION ( 'NONE',  ( -0.000000000000000000, 1.000000000000000000, -0.000000000000000000 ) ) ;
#21181=CARTESIAN_POINT ( 'NONE',  ( -10.00000000000000000, 222.2916666666667140, -2.679491924311229845 ) ) ;
#21182=( BOUNDED_CURVE ( )  B_SPLINE_CURVE ( 2, ( #60589, #54204, #65874, #36477, #7806, #36849, #59493, #37217, #30808, #53831, #60215, #8539, #15300 ),
 .UNSPECIFIED., .F., .F. ) 
 B_SPLINE_CURVE_WITH_KNOTS ( ( 3, 2, 2, 2, 2, 2, 3 ),
 ( 0.1141304347826086890, 0.1159420289855072478, 0.1177536231884057927, 0.1195652173913043514, 0.1213768115942028963, 0.1231884057971014551, 0.1250000000000000000 ),
 .UNSPECIFIED. ) 
 CURVE ( )  GEOMETRIC_REPRESENTATION_ITEM ( )  RATIONAL_B_SPLINE_CURVE ( ( 1.000000000000000000, 0.9659258262890683122, 1.000000000000000000, 0.9659258262890683122, 1.000000000000000000, 0.9659258262890683122, 1.000000000000000000, 0.9659258262890683122, 1.000000000000000000, 0.9659258262890683122, 1.000000000000000000, 0.9659258262890683122, 1.000000000000000000 ) ) 
 REPRESENTATION_ITEM ( '' )  );
#21184=CARTESIAN_POINT ( 'NONE',  ( -3.042071309553164404, 207.5520833299193555, -11.35316468749999963 ) ) ;
#21185=CARTESIAN_POINT ( 'NONE',  ( 6.951808397369818766E-16, 2.031249996586016238, -11.35316468750000141 ) ) ;
#21187=CARTESIAN_POINT ( 'NONE',  ( 4.242640687119285658, 290.6249999999999432, -4.242640687119286547 ) ) ;
#21190=ORIENTED_EDGE ( 'NONE', *, *, #25514, .F. ) ;
#21192=CARTESIAN_POINT ( 'NONE',  ( -5.676582343749998039, 12.44791666325268409, -9.832129032723420536 ) ) ;
#21198=CARTESIAN_POINT ( 'NONE',  ( 5.676582343749993598, 9.947916663252682312, 9.832129032723422313 ) ) ;
#21200=CARTESIAN_POINT ( 'NONE',  ( -9.832129032723418760, 122.8645833299193555, -5.676582343750004256 ) ) ;
#21201=CARTESIAN_POINT ( 'NONE',  ( -7.320508075688773708, 93.74999999317202537, -7.320508075688774596 ) ) ;
#21207=VERTEX_POINT ( 'NONE', #74428 ) ;
#21209=CARTESIAN_POINT ( 'NONE',  ( 2.765530957081996366, 290.2968750017069510, -6.676582343750003368 ) ) ;
#21213=CARTESIAN_POINT ( 'NONE',  ( 7.320508075688774596, 207.4999999931720538, -7.320508075688774596 ) ) ;
#21218=VECTOR ( 'NONE', #47733, 1000.000000000000000 ) ;
#21219=CARTESIAN_POINT ( 'NONE',  ( 5.676582343750001591, 156.9270833299193555, -9.832129032723420536 ) ) ;
#21224=CARTESIAN_POINT ( 'NONE',  ( -3.042071309553164404, 57.55208332991936260, -11.35316468749999963 ) ) ;
#21228=VERTEX_POINT ( 'NONE', #11430 ) ;
#21231=CARTESIAN_POINT ( 'NONE',  ( 2.485281374238575314, 290.3750000034139589, 6.000000000000000888 ) ) ;
#21254=CARTESIAN_POINT ( 'NONE',  ( -8.660254037844390851, 62.91666666666667851, 4.999999999999998224 ) ) ;
#21256=CARTESIAN_POINT ( 'NONE',  ( 1.102182119232618108E-15, 291.2500000000000000, 6.000000000000001776 ) ) ;
#21266=CARTESIAN_POINT ( 'NONE',  ( -8.660254037844421049, 77.91666666666668561, 5.000000000000016875 ) ) ;
#21267=CARTESIAN_POINT ( 'NONE',  ( -10.00000000000000000, 187.2916666666666572, -2.679491924311229845 ) ) ;
#21270=CARTESIAN_POINT ( 'NONE',  ( -5.676582343749998039, 152.7604166632526983, -9.832129032723420536 ) ) ;
#21276=ORIENTED_EDGE ( 'NONE', *, *, #74065, .F. ) ;
#21277=CARTESIAN_POINT ( 'NONE',  ( 5.676582343750001591, 21.92708332991935194, -9.832129032723420536 ) ) ;
#21283=( BOUNDED_CURVE ( )  B_SPLINE_CURVE ( 2, ( #26043, #72074, #14357, #31728, #54750, #20392, #26419, #38140, #47950, #25304, #20771, #43790, #7603 ),
 .UNSPECIFIED., .F., .F. ) 
 B_SPLINE_CURVE_WITH_KNOTS ( ( 3, 2, 2, 2, 2, 2, 3 ),
 ( 0.6793478260869565410, 0.6811594202898550998, 0.6829710144927536586, 0.6847826086956522174, 0.6865942028985507761, 0.6884057971014492239, 0.6902173913043477826 ),
 .UNSPECIFIED. ) 
 CURVE ( )  GEOMETRIC_REPRESENTATION_ITEM ( )  RATIONAL_B_SPLINE_CURVE ( ( 1.000000000000000000, 0.9659258262890683122, 1.000000000000000000, 0.9659258262890683122, 1.000000000000000000, 0.9659258262890683122, 1.000000000000000000, 0.9659258262890683122, 1.000000000000000000, 0.9659258262890683122, 1.000000000000000000, 0.9659258262890683122, 1.000000000000000000 ) ) 
 REPRESENTATION_ITEM ( '' )  );
#21284=CARTESIAN_POINT ( 'NONE',  ( 10.00000000000000178, 46.87499999317203958, 0.000000000000000000 ) ) ;
#21287=CARTESIAN_POINT ( 'NONE',  ( 4.999999999999991118, 54.16666666666666430, 8.660254037844389075 ) ) ;
#21289=CARTESIAN_POINT ( 'NONE',  ( 1.102182119232618108E-15, 291.3125000034140157, 6.000000000000001776 ) ) ;
#21293=CARTESIAN_POINT ( 'NONE',  ( -2.679491924311529605, 223.5416666666666288, 9.999999999999831246 ) ) ;
#21297=CARTESIAN_POINT ( 'NONE',  ( 11.35316468749999963, 145.9895833299193839, -3.042071309553165293 ) ) ;
#21305=CARTESIAN_POINT ( 'NONE',  ( 9.832129032723420536, 131.1979166632526983, -5.676582343749999815 ) ) ;
#21306=CARTESIAN_POINT ( 'NONE',  ( 11.35316468749999963, 55.98958332991934128, -3.042071309553165293 ) ) ;
#21310=CARTESIAN_POINT ( 'NONE',  ( -7.320508075688778149, 24.99999999317203603, 7.320508075688769267 ) ) ;
#21312=CARTESIAN_POINT ( 'NONE',  ( -5.676582343750006032, 109.4270833299193555, 9.832129032723418760 ) ) ;
#21316=CARTESIAN_POINT ( 'NONE',  ( 11.35316468749999963, 26.30208332991934839, -3.042071309553165293 ) ) ;
#21321=EDGE_CURVE ( 'NONE', #38928, #52317, #18981, .T. ) ;
#21325=CARTESIAN_POINT ( 'NONE',  ( -6.676582343750003368, 288.3906250017069510, -2.765530957081996810 ) ) ;
#21326=DIRECTION ( 'NONE',  ( -0.000000000000000000, 1.000000000000000000, -0.000000000000000000 ) ) ;
#21330=CARTESIAN_POINT ( 'NONE',  ( -9.832129032723418760, 148.1770833299193555, -5.676582343750004256 ) ) ;
#21345=CARTESIAN_POINT ( 'NONE',  ( 8.311093377946834337, 190.1562499965860127, 8.311093377946839666 ) ) ;
#21347=CARTESIAN_POINT ( 'NONE',  ( 1.102182119232618108E-15, 291.3125000034140157, 6.000000000000001776 ) ) ;
#21348=CARTESIAN_POINT ( 'NONE',  ( 7.320508075688774596, 132.4999999931720254, -7.320508075688774596 ) ) ;
#21356=ORIENTED_EDGE ( 'NONE', *, *, #1586, .F. ) ;
#21359=CARTESIAN_POINT ( 'NONE',  ( -9.832129032723418760, 118.1770833299193555, -5.676582343750004256 ) ) ;
#21366=CARTESIAN_POINT ( 'NONE',  ( 0.5935108062425623610, 223.7964224127544242, 9.986736671522551845 ) ) ;
#21367=CARTESIAN_POINT ( 'NONE',  ( 3.042071309553159519, 224.7395833299193555, 11.35316468750000141 ) ) ;
#21370=CARTESIAN_POINT ( 'NONE',  ( -2.085542519210945728E-15, 209.8437499965860411, 11.35316468750000141 ) ) ;
#21378=CARTESIAN_POINT ( 'NONE',  ( 9.832129032723420536, 101.1979166632526841, -5.676582343749999815 ) ) ;
#21385=CARTESIAN_POINT ( 'NONE',  ( 8.311093377946834337, 90.15624999658604111, 8.311093377946839666 ) ) ;
#21388=CARTESIAN_POINT ( 'NONE',  ( -1.836970198721029983E-15, 205.6249999931720538, 10.00000000000000178 ) ) ;
#21394=CARTESIAN_POINT ( 'NONE',  ( -9.832129032723418760, 82.86458332991935549, -5.676582343750004256 ) ) ;
#21398=CARTESIAN_POINT ( 'NONE',  ( -8.660254037844387298, 178.9583333265053682, -5.000000000000004441 ) ) ;
#21400=CARTESIAN_POINT ( 'NONE',  ( -5.676582343749998039, 77.76041666325268409, -9.832129032723420536 ) ) ;
#21401=CARTESIAN_POINT ( 'NONE',  ( -6.676582343750000703, 293.5156250017070647, 2.765530957082001251 ) ) ;
#21404=CARTESIAN_POINT ( 'NONE',  ( -9.832129032723420536, 213.6979166632526983, 5.676582343749997150 ) ) ;
#21406=CARTESIAN_POINT ( 'NONE',  ( 1.102182119232618108E-15, 289.3125000034140157, 6.000000000000001776 ) ) ;
#21409=CARTESIAN_POINT ( 'NONE',  ( 6.123233995736767268E-16, 23.12499999317203603, -10.00000000000000178 ) ) ;
#21410=CARTESIAN_POINT ( 'NONE',  ( -9.832129032723418760, 207.8645833299193555, -5.676582343750004256 ) ) ;
#21415=CARTESIAN_POINT ( 'NONE',  ( 11.35316468749999785, 190.8854166632526983, 3.042071309553174174 ) ) ;
#21423=CARTESIAN_POINT ( 'NONE',  ( 8.660254037844385522, 14.58333333333333393, 5.000000000000005329 ) ) ;
#21440=EDGE_CURVE ( 'NONE', #38706, #28551, #60847, .T. ) ;
#21442=EDGE_LOOP ( 'NONE', ( #44234, #9588, #42027, #49169 ) ) ;
#21443=ORIENTED_EDGE ( 'NONE', *, *, #12046, .T. ) ;
#21445=CARTESIAN_POINT ( 'NONE',  ( 5.676582343750001591, 76.92708332991935549, -9.832129032723420536 ) ) ;
#21446=CARTESIAN_POINT ( 'NONE',  ( 0.000000000000000000, 300.0000000000000000, 10.00000000000000178 ) ) ;
#21450=CARTESIAN_POINT ( 'NONE',  ( 6.676582343750002480, 292.1718750017070079, -2.765530957081997254 ) ) ;
#21460=CARTESIAN_POINT ( 'NONE',  ( -11.35316468750000141, 168.5937499965860127, -1.390361679473963753E-15 ) ) ;
#21468=CARTESIAN_POINT ( 'NONE',  ( -11.35316468749999785, 53.07291666325267698, -3.042071309553167513 ) ) ;
#21471=CARTESIAN_POINT ( 'NONE',  ( 10.00000000000000178, 21.87499999317203248, 0.000000000000000000 ) ) ;
#21472=VERTEX_POINT ( 'NONE', #9489 ) ;
#21475=CARTESIAN_POINT ( 'NONE',  ( -11.35316468749999785, 48.07291666325268409, -3.042071309553167513 ) ) ;
#21482=CARTESIAN_POINT ( 'NONE',  ( -11.35316468750000141, 48.48958332991934839, 3.042071309553159963 ) ) ;
#21486=CARTESIAN_POINT ( 'NONE',  ( -11.35316468750000141, 168.2812499965860411, -1.390361679473963753E-15 ) ) ;
#21488=CARTESIAN_POINT ( 'NONE',  ( -8.660254037844390851, 144.7916666598387110, 4.999999999999998224 ) ) ;
#21491=CARTESIAN_POINT ( 'NONE',  ( 3.042071309553167513, 32.13541666325269119, -11.35316468749999785 ) ) ;
#21493=CARTESIAN_POINT ( 'NONE',  ( 4.242640687119287435, 295.4375000034140157, 4.242640687119285658 ) ) ;
#21495=CARTESIAN_POINT ( 'NONE',  ( 0.000000000000000000, 300.0000000000000000, 0.000000000000000000 ) ) ;
#21498=CARTESIAN_POINT ( 'NONE',  ( -7.320508075688783478, 8.125000000000003553, 7.320508075688775484 ) ) ;
#21499=CARTESIAN_POINT ( 'NONE',  ( -8.311093377946841443, 168.9062499965860411, 8.311093377946834337 ) ) ;
#21509=CARTESIAN_POINT ( 'NONE',  ( -5.676582343750006032, 119.4270833299193555, 9.832129032723418760 ) ) ;
#21511=ORIENTED_EDGE ( 'NONE', *, *, #16722, .T. ) ;
#21512=ORIENTED_EDGE ( 'NONE', *, *, #28829, .F. ) ;
#21534=CARTESIAN_POINT ( 'NONE',  ( 6.000000000000001776, 288.5000000000000000, -7.347880794884121708E-16 ) ) ;
#21539=CARTESIAN_POINT ( 'NONE',  ( 2.679491924311228956, 126.0416666666666572, -10.00000000000000000 ) ) ;
#21541=CARTESIAN_POINT ( 'NONE',  ( 2.765530957082001251, 292.9218750017069510, 6.676582343750000703 ) ) ;
#21553=CARTESIAN_POINT ( 'NONE',  ( -5.000000000000005329, 95.20833332650536818, 8.660254037844387298 ) ) ;
#21554=CARTESIAN_POINT ( 'NONE',  ( 6.951808397369818766E-16, 17.03124999658601624, -11.35316468750000141 ) ) ;
#21556=CARTESIAN_POINT ( 'NONE',  ( 9.832129032723420536, 201.5104166632526983, -5.676582343749999815 ) ) ;
#21564=CARTESIAN_POINT ( 'NONE',  ( -11.35316468749999785, 8.072916663252682312, -3.042071309553167513 ) ) ;
#21567=CYLINDRICAL_SURFACE ( 'NONE', #38272, 10.00000000000000178 ) ;
#21569=CARTESIAN_POINT ( 'NONE',  ( 8.311093377946834337, 10.15624999658601801, 8.311093377946839666 ) ) ;
#21572=CARTESIAN_POINT ( 'NONE',  ( 9.832129032723416984, 125.3645833299193413, 5.676582343750006032 ) ) ;
#21573=CARTESIAN_POINT ( 'NONE',  ( -2.679491924311235618, 100.4166666598386684, 10.00000000000000000 ) ) ;
#21580=CARTESIAN_POINT ( 'NONE',  ( 2.765530957081996366, 288.2968750017070647, -6.676582343750003368 ) ) ;
#21583=CARTESIAN_POINT ( 'NONE',  ( 1.224646799147353454E-15, 300.0000000000000000, -10.00000000000000178 ) ) ;
#21588=CARTESIAN_POINT ( 'NONE',  ( 7.320508075688774596, 157.4999999931720254, -7.320508075688774596 ) ) ;
#21589=CARTESIAN_POINT ( 'NONE',  ( 11.35316468750000141, 156.0937499965860127, 0.000000000000000000 ) ) ;
#21593=CARTESIAN_POINT ( 'NONE',  ( 5.676582343749993598, 70.26041666325268409, 9.832129032723422313 ) ) ;
#21599=CARTESIAN_POINT ( 'NONE',  ( -7.320508075688773708, 108.7499999931720254, -7.320508075688774596 ) ) ;
#21604=PRODUCT_DEFINITION_SHAPE ( 'NONE', 'NONE',  #49627 ) ;
#21609=ORIENTED_EDGE ( 'NONE', *, *, #71978, .F. ) ;
#21625=CARTESIAN_POINT ( 'NONE',  ( -10.00000000000000000, 82.29166666666665719, -2.679491924311229845 ) ) ;
#21627=CARTESIAN_POINT ( 'NONE',  ( 2.485281374238571317, 293.6875000000000000, -6.000000000000003553 ) ) ;
#21638=CARTESIAN_POINT ( 'NONE',  ( -10.00000000000003908, 77.50000000000002842, -1.224646799147357990E-15 ) ) ;
#21639=CARTESIAN_POINT ( 'NONE',  ( 4.999999999999993783, 184.1666666666666856, 8.660254037844390851 ) ) ;
#21642=CARTESIAN_POINT ( 'NONE',  ( 11.35316468749999963, 166.3020833299193271, -3.042071309553165293 ) ) ;
#21648=CARTESIAN_POINT ( 'NONE',  ( 3.042071309553159519, 30.05208332991934839, 11.35316468750000141 ) ) ;
#21655=CARTESIAN_POINT ( 'NONE',  ( -10.00000000000000178, 59.37499999317203248, -1.224646799147353454E-15 ) ) ;
#21658=CARTESIAN_POINT ( 'NONE',  ( 4.999999999999985789, 99.16666666666668561, 8.660254037844380193 ) ) ;
#21667=CARTESIAN_POINT ( 'NONE',  ( 3.042071309553167069, 141.8229166632526983, -11.35316468749999785 ) ) ;
#21669=FACE_OUTER_BOUND ( 'NONE', #13698, .T. ) ;
#21679=CARTESIAN_POINT ( 'NONE',  ( 3.042071309553159519, 120.0520833299193555, 11.35316468750000141 ) ) ;
#21683=CARTESIAN_POINT ( 'NONE',  ( 8.311093377946837890, 36.71874999658601979, -8.311093377946837890 ) ) ;
#21688=VECTOR ( 'NONE', #26590, 1000.000000000000000 ) ;
#21691=CARTESIAN_POINT ( 'NONE',  ( 1.226468279477575784E-15, 290.7031250017069510, 6.676582343750001591 ) ) ;
#21695=CARTESIAN_POINT ( 'NONE',  ( 9.832129032723420536, 146.5104166632526699, -5.676582343749999815 ) ) ;
#21706=ORIENTED_EDGE ( 'NONE', *, *, #53851, .F. ) ;
#21708=CARTESIAN_POINT ( 'NONE',  ( -6.000000000000001776, 298.0625000034140157, 0.000000000000000000 ) ) ;
#21710=CARTESIAN_POINT ( 'NONE',  ( -5.676582343750006032, 189.1145833299193839, 9.832129032723418760 ) ) ;
#21712=CARTESIAN_POINT ( 'NONE',  ( 4.242640687119287435, 295.3750000000000000, 4.242640687119285658 ) ) ;
#21713=CARTESIAN_POINT ( 'NONE',  ( 6.676582343750002480, 288.0156250017069510, -2.765530957081997254 ) ) ;
#21714=CARTESIAN_POINT ( 'NONE',  ( 8.660254037844481445, 79.58333333333339965, 5.000000000000061284 ) ) ;
#21715=( BOUNDED_CURVE ( )  B_SPLINE_CURVE ( 2, ( #46966, #57950, #52272, #48069, #18304, #64327, #58316, #36396, #24325, #59410, #608, #70363, #30364 ),
 .UNSPECIFIED., .F., .T. ) 
 B_SPLINE_CURVE_WITH_KNOTS ( ( 3, 2, 2, 2, 2, 2, 3 ),
 ( 1.114692740994780884, 1.119926170633683604, 1.125159600272586102, 1.130393029911488822, 1.135626459550391321, 1.140859889189293819, 1.146093318828196539 ),
 .UNSPECIFIED. ) 
 CURVE ( )  GEOMETRIC_REPRESENTATION_ITEM ( )  RATIONAL_B_SPLINE_CURVE ( ( 1.000000000000003997, 0.9659258262890639823, 0.9999999999999998890, 0.9659258262890682012, 0.9999999999999998890, 0.9659258262890682012, 0.9999999999999998890, 0.9659258262890682012, 0.9999999999999998890, 0.9659258262890682012, 0.9999999999999998890, 0.9659258262890682012, 0.9999999999999998890 ) ) 
 REPRESENTATION_ITEM ( '' )  );
#21720=CARTESIAN_POINT ( 'NONE',  ( -7.320508075688773708, 8.749999993172030699, -7.320508075688774596 ) ) ;
#21724=CARTESIAN_POINT ( 'NONE',  ( -7.320508075688778149, 148.1249999999999716, 7.320508075688769267 ) ) ;
#21728=CARTESIAN_POINT ( 'NONE',  ( 9.832129032723420536, 126.5104166632526841, -5.676582343749999815 ) ) ;
#21732=LINE ( 'NONE', #73796, #20576 ) ;
#21735=EDGE_CURVE ( 'NONE', #19469, #23110, #31990, .T. ) ;
#21739=( BOUNDED_CURVE ( )  B_SPLINE_CURVE ( 2, ( #16579, #51673, #10201, #39616, #23005, #69032, #28292, #62243, #10947, #51299, #39244, #63357, #16204 ),
 .UNSPECIFIED., .F., .F. ) 
 B_SPLINE_CURVE_WITH_KNOTS ( ( 3, 2, 2, 2, 2, 2, 3 ),
 ( 0.03804347826086956763, 0.03985507246376811252, 0.04166666666666666435, 0.04347826086956521618, 0.04528985507246376108, 0.04710144927536231291, 0.04891304347826086474 ),
 .UNSPECIFIED. ) 
 CURVE ( )  GEOMETRIC_REPRESENTATION_ITEM ( )  RATIONAL_B_SPLINE_CURVE ( ( 1.000000000000000000, 0.9659258262890683122, 1.000000000000000000, 0.9659258262890683122, 1.000000000000000000, 0.9659258262890683122, 1.000000000000000000, 0.9659258262890683122, 1.000000000000000000, 0.9659258262890683122, 1.000000000000000000, 0.9659258262890684232, 0.9999999999999998890 ) ) 
 REPRESENTATION_ITEM ( '' )  );
#21741=CARTESIAN_POINT ( 'NONE',  ( 3.042071309553167069, 212.1354166632526983, -11.35316468749999785 ) ) ;
#21748=CARTESIAN_POINT ( 'NONE',  ( 6.951808397369818766E-16, 92.03124999658602690, -11.35316468750000141 ) ) ;
#21754=CARTESIAN_POINT ( 'NONE',  ( 9.832129032723420536, 106.1979166632526983, -5.676582343749999815 ) ) ;
#21758=CARTESIAN_POINT ( 'NONE',  ( -5.000000000000163425, 21.66666666666685970, -8.660254037844673292 ) ) ;
#21762=CARTESIAN_POINT ( 'NONE',  ( -3.042071309553163960, 82.23958332991935549, -11.35316468749999963 ) ) ;
#21767=AXIS2_PLACEMENT_3D ( 'NONE', #9310, #44015, #39104 ) ;
#21768=CARTESIAN_POINT ( 'NONE',  ( -10.00000000000000178, 179.3749999931720538, -1.224646799147353454E-15 ) ) ;
#21770=CARTESIAN_POINT ( 'NONE',  ( 11.35316468750000141, 76.09374999658602690, 0.000000000000000000 ) ) ;
#21771=CARTESIAN_POINT ( 'NONE',  ( 4.721056650415999201, 289.0781250017069510, -4.721056650415999201 ) ) ;
#21773=CARTESIAN_POINT ( 'NONE',  ( 5.676582343749993598, 209.9479166632526983, 9.832129032723422313 ) ) ;
#21776=DIRECTION ( 'NONE',  ( 0.000000000000000000, 0.000000000000000000, 1.000000000000000000 ) ) ;
#21778=CARTESIAN_POINT ( 'NONE',  ( 5.676582343750001591, 206.6145833299193555, -9.832129032723420536 ) ) ;
#21781=CARTESIAN_POINT ( 'NONE',  ( -5.676582343750006032, 199.4270833299193555, 9.832129032723418760 ) ) ;
#21788=CARTESIAN_POINT ( 'NONE',  ( 7.320508075688771044, 19.37499999999999289, 7.320508075688775484 ) ) ;
#21796=ORIENTED_EDGE ( 'NONE', *, *, #27499, .T. ) ;
#21803=ORIENTED_EDGE ( 'NONE', *, *, #4986, .F. ) ;
#21806=ORIENTED_EDGE ( 'NONE', *, *, #42196, .F. ) ;
#21809=CARTESIAN_POINT ( 'NONE',  ( 5.676582343749993598, 70.26041666325268409, 9.832129032723422313 ) ) ;
#21814=CARTESIAN_POINT ( 'NONE',  ( -6.676582343750002480, 288.5468750017070079, -2.765530957081996810 ) ) ;
#21815=AXIS2_PLACEMENT_3D ( 'NONE', #23127, #69530, #45391 ) ;
#21817=CARTESIAN_POINT ( 'NONE',  ( 10.00000000000000178, 77.08333332650536818, -2.679491924311226736 ) ) ;
#21824=CARTESIAN_POINT ( 'NONE',  ( 11.35316468749999963, 171.3020833299193555, -3.042071309553165293 ) ) ;
#21827=CARTESIAN_POINT ( 'NONE',  ( 0.000000000000000000, 284.0000000000000000, 0.000000000000000000 ) ) ;
#21832=CARTESIAN_POINT ( 'NONE',  ( 8.311093377946837890, 61.40624999658602690, -8.311093377946837890 ) ) ;
#21835=CARTESIAN_POINT ( 'NONE',  ( -7.320508075688773708, 28.74999999317203248, -7.320508075688774596 ) ) ;
#21839=CARTESIAN_POINT ( 'NONE',  ( -8.660254037844387298, 168.9583333265053682, -5.000000000000004441 ) ) ;
#21840=CARTESIAN_POINT ( 'NONE',  ( 9.832129032723420536, 66.19791666325268409, -5.676582343749999815 ) ) ;
#21846=CARTESIAN_POINT ( 'NONE',  ( 8.311093377946834337, 40.15624999658601268, 8.311093377946839666 ) ) ;
#21850=CARTESIAN_POINT ( 'NONE',  ( 9.832129032723416984, 170.3645833299193555, 5.676582343750006032 ) ) ;
#21851=EDGE_CURVE ( 'NONE', #62422, #27943, #32503, .T. ) ;
#21852=CARTESIAN_POINT ( 'NONE',  ( -2.679491924311225848, 143.3333333265053398, -10.00000000000000178 ) ) ;
#21856=CARTESIAN_POINT ( 'NONE',  ( 11.35316468750000141, 31.09374999658601979, 0.000000000000000000 ) ) ;
#21857=CARTESIAN_POINT ( 'NONE',  ( -5.000000000000005329, 80.20833332650536818, 8.660254037844387298 ) ) ;
#21858=CARTESIAN_POINT ( 'NONE',  ( 5.676582343749993598, 174.9479166632526699, 9.832129032723422313 ) ) ;
#21860=DIRECTION ( 'NONE',  ( 0.000000000000000000, 0.000000000000000000, 1.000000000000000000 ) ) ;
#21865=CARTESIAN_POINT ( 'NONE',  ( -9.832129032723418760, 172.8645833299193555, -5.676582343750004256 ) ) ;
#21867=EDGE_CURVE ( 'NONE', #69413, #10358, #63383, .T. ) ;
#21876=CARTESIAN_POINT ( 'NONE',  ( 8.311093377946834337, 120.4687499965860269, 8.311093377946839666 ) ) ;
#21896=LINE ( 'NONE', #15492, #10663 ) ;
#21906=CARTESIAN_POINT ( 'NONE',  ( 6.123233995736767268E-16, 116.2500000000000000, -10.00000000000000178 ) ) ;
#21908=CARTESIAN_POINT ( 'NONE',  ( 2.765530957081996366, 292.2968750017070647, -6.676582343750003368 ) ) ;
#21922=CARTESIAN_POINT ( 'NONE',  ( 11.35316468750000141, 15.78124999658601979, 0.000000000000000000 ) ) ;
#21924=CARTESIAN_POINT ( 'NONE',  ( 5.676582343749993598, 205.2604166632526983, 9.832129032723422313 ) ) ;
#21925=CARTESIAN_POINT ( 'NONE',  ( -5.000000000000005329, 135.2083333265053682, 8.660254037844387298 ) ) ;
#21932=CARTESIAN_POINT ( 'NONE',  ( 5.676582343750001591, 6.614583329919350163, -9.832129032723420536 ) ) ;
#21934=CARTESIAN_POINT ( 'NONE',  ( -3.673940397442060854E-16, 292.7500000000000000, -6.000000000000001776 ) ) ;
#21938=CARTESIAN_POINT ( 'NONE',  ( -9.832129032723418760, 7.864583329919350163, -5.676582343750004256 ) ) ;
#21941=CARTESIAN_POINT ( 'NONE',  ( 6.951808397369818766E-16, 137.0312499965860411, -11.35316468750000141 ) ) ;
#21943=CARTESIAN_POINT ( 'NONE',  ( -7.320508075688773708, 98.74999999317205379, -7.320508075688774596 ) ) ;
#21945=CARTESIAN_POINT ( 'NONE',  ( -10.00000000000000000, 4.166666659838700326, -2.679491924311229845 ) ) ;
#21949=CARTESIAN_POINT ( 'NONE',  ( 8.311093377946837890, 1.718749996586016682, -8.311093377946837890 ) ) ;
#21951=CARTESIAN_POINT ( 'NONE',  ( 4.721056650416000089, 289.9843750017070079, 4.721056650415999201 ) ) ;
#21960=CARTESIAN_POINT ( 'NONE',  ( 10.00000000000000178, 216.8749999931720538, 0.000000000000000000 ) ) ;
#21961=CARTESIAN_POINT ( 'NONE',  ( -8.311093377946841443, 174.2187499965860127, 8.311093377946834337 ) ) ;
#21965=CARTESIAN_POINT ( 'NONE',  ( 3.042071309553159519, 75.05208332991935549, 11.35316468750000141 ) ) ;
#21972=CARTESIAN_POINT ( 'NONE',  ( 10.00000000000000178, 66.87499999317203958, 0.000000000000000000 ) ) ;
#21976=VECTOR ( 'NONE', #10925, 1000.000000000000000 ) ;
#21991=EDGE_LOOP ( 'NONE', ( #46541, #60120, #11438, #57057 ) ) ;
#21992=ADVANCED_FACE ( 'NONE', ( #25881 ), #31938, .T. ) ;
#21993=DIRECTION ( 'NONE',  ( -0.000000000000000000, 1.000000000000000000, -0.000000000000000000 ) ) ;
#21999=CARTESIAN_POINT ( 'NONE',  ( -5.000000000000005329, 78.33333333333334281, 8.660254037844387298 ) ) ;
#22001=CARTESIAN_POINT ( 'NONE',  ( -2.485281374238572649, 292.1875000000000000, 6.000000000000002665 ) ) ;
#22003=EDGE_LOOP ( 'NONE', ( #23836, #65566, #61966 ) ) ;
#22011=EDGE_CURVE ( 'NONE', #43617, #59649, #16493, .T. ) ;
#22012=CARTESIAN_POINT ( 'NONE',  ( 5.000000000000001776, 205.8333333333333428, -8.660254037844389075 ) ) ;
#22015=CARTESIAN_POINT ( 'NONE',  ( 8.311093377946834337, 170.4687499965860127, 8.311093377946839666 ) ) ;
#22016=CARTESIAN_POINT ( 'NONE',  ( -5.000000000000116351, 213.3333333333334849, 8.660254037844579145 ) ) ;
#22018=CARTESIAN_POINT ( 'NONE',  ( 0.000000000000000000, 300.0000000000000000, 0.000000000000000000 ) ) ;
#22019=DIRECTION ( 'NONE',  ( -0.000000000000000000, 1.000000000000000000, -0.000000000000000000 ) ) ;
#22021=CARTESIAN_POINT ( 'NONE',  ( 11.35316468749999785, 20.88541666325268764, 3.042071309553174174 ) ) ;
#22027=CARTESIAN_POINT ( 'NONE',  ( -10.00000000000000000, 59.16666665983869677, -2.679491924311229845 ) ) ;
#22037=CARTESIAN_POINT ( 'NONE',  ( -8.311093377946836114, 147.6562499965860411, -8.311093377946837890 ) ) ;
#22048=CARTESIAN_POINT ( 'NONE',  ( 11.35316468749999785, 110.8854166632526699, 3.042071309553174174 ) ) ;
#22051=( BOUNDED_CURVE ( )  B_SPLINE_CURVE ( 2, ( #28443, #68429, #16356, #23151, #62393, #33752, #16732, #39758, #40511, #58256, #69555, #541, #6557 ),
 .UNSPECIFIED., .F., .F. ) 
 B_SPLINE_CURVE_WITH_KNOTS ( ( 3, 2, 2, 2, 2, 2, 3 ),
 ( 2.684688080663935494, 2.689920760420000612, 2.695153440176065729, 2.700386119932130846, 2.705618799688195963, 2.710851479444261081, 2.716084159200326198 ),
 .UNSPECIFIED. ) 
 CURVE ( )  GEOMETRIC_REPRESENTATION_ITEM ( )  RATIONAL_B_SPLINE_CURVE ( ( 1.000000000000077272, 0.9659258262889910407, 1.000000000000000000, 0.9659258262890683122, 1.000000000000000000, 0.9659258262890683122, 1.000000000000000000, 0.9659258262890683122, 1.000000000000000000, 0.9659258262890683122, 1.000000000000000000, 0.9659258262890725311, 0.9999999999999957812 ) ) 
 REPRESENTATION_ITEM ( '' )  );
#22053=CARTESIAN_POINT ( 'NONE',  ( 3.042071309553159519, 40.05208332991935549, 11.35316468750000141 ) ) ;
#22059=CARTESIAN_POINT ( 'NONE',  ( 6.000000000000003553, 294.6250000034140157, -2.485281374238571761 ) ) ;
#22060=CARTESIAN_POINT ( 'NONE',  ( -4.242640687119285658, 297.1250000000000000, 4.242640687119287435 ) ) ;
#22064=CARTESIAN_POINT ( 'NONE',  ( -11.35316468750000141, 153.8020833299192986, 3.042071309553159963 ) ) ;
#22082=CARTESIAN_POINT ( 'NONE',  ( 2.679491924311228956, 36.04166666666666430, -10.00000000000000000 ) ) ;
#22086=CARTESIAN_POINT ( 'NONE',  ( 1.226468279477575784E-15, 287.7031250017069510, 6.676582343750001591 ) ) ;
#22087=CARTESIAN_POINT ( 'NONE',  ( -1.604524386212670052E-13, 78.75000000000000000, 10.00000000000000178 ) ) ;
#22095=CARTESIAN_POINT ( 'NONE',  ( 0.000000000000000000, 300.0000000000000000, 10.00000000000000178 ) ) ;
#22096=CARTESIAN_POINT ( 'NONE',  ( 4.999999999999993783, 164.1666666666666856, 8.660254037844390851 ) ) ;
#22097=DIRECTION ( 'NONE',  ( 0.000000000000000000, 0.000000000000000000, 1.000000000000000000 ) ) ;
#22098=DIRECTION ( 'NONE',  ( -0.000000000000000000, 1.000000000000000000, -0.000000000000000000 ) ) ;
#22100=CARTESIAN_POINT ( 'NONE',  ( -3.042071309553164404, 132.5520833299193555, -11.35316468749999963 ) ) ;
#22101=CARTESIAN_POINT ( 'NONE',  ( -4.242640687119285658, 296.1250000000000000, 4.242640687119287435 ) ) ;
#22105=CARTESIAN_POINT ( 'NONE',  ( -3.673940397442060854E-16, 298.7500000000000000, -6.000000000000001776 ) ) ;
#22112=CARTESIAN_POINT ( 'NONE',  ( 3.042071309553167069, 207.1354166632526415, -11.35316468749999785 ) ) ;
#22118=CARTESIAN_POINT ( 'NONE',  ( -3.042071309553173730, 94.32291666325266988, 11.35316468749999785 ) ) ;
#22125=CARTESIAN_POINT ( 'NONE',  ( -11.35316468749999785, 98.07291666325269830, -3.042071309553167513 ) ) ;
#22129=CARTESIAN_POINT ( 'NONE',  ( 2.679491924311228956, 222.9166666598386826, -10.00000000000000000 ) ) ;
#22132=CARTESIAN_POINT ( 'NONE',  ( 6.951808397369818766E-16, 92.03124999658602690, -11.35316468750000141 ) ) ;
#22137=CARTESIAN_POINT ( 'NONE',  ( -5.000000000000005329, 180.2083333265053682, 8.660254037844387298 ) ) ;
#22140=CARTESIAN_POINT ( 'NONE',  ( 9.832129032723420536, 81.51041666325268409, -5.676582343749999815 ) ) ;
#22141=CARTESIAN_POINT ( 'NONE',  ( 6.676582343750003368, 290.0156250017069510, -2.765530957081997254 ) ) ;
#22143=CARTESIAN_POINT ( 'NONE',  ( 9.832129032723420536, 226.1979166632526983, -5.676582343749999815 ) ) ;
#22148=CARTESIAN_POINT ( 'NONE',  ( 3.042071309553159519, 204.7395833299193555, 11.35316468750000141 ) ) ;
#22152=CARTESIAN_POINT ( 'NONE',  ( -4.088227598258586603E-16, 296.2031250017070079, -6.676582343750001591 ) ) ;
#22154=CARTESIAN_POINT ( 'NONE',  ( 5.676582343749993598, 190.2604166632526983, 9.832129032723422313 ) ) ;
#22162=( BOUNDED_CURVE ( )  B_SPLINE_CURVE ( 2, ( #12109, #6468, #29471, #35874, #52481, #58891, #41525, #23805, #69832 ),
 .UNSPECIFIED., .F., .F. ) 
 B_SPLINE_CURVE_WITH_KNOTS ( ( 3, 2, 2, 2, 3 ),
 ( 0.3124999999999979461, 0.3229166666666646313, 0.3333333333333312609, 0.3437499999999979461, 0.3541666666666646313 ),
 .UNSPECIFIED. ) 
 CURVE ( )  GEOMETRIC_REPRESENTATION_ITEM ( )  RATIONAL_B_SPLINE_CURVE ( ( 1.000000000000015099, 0.9238795325112717505, 1.000000000000000000, 0.9238795325112867385, 1.000000000000000000, 0.9238795325112867385, 1.000000000000000000, 0.9238795325113017265, 0.9999999999999850120 ) ) 
 REPRESENTATION_ITEM ( '' )  );
#22163=CARTESIAN_POINT ( 'NONE',  ( 2.679491924311222739, 18.95833333333333215, 10.00000000000000355 ) ) ;
#22185=CARTESIAN_POINT ( 'NONE',  ( 11.35316468749999785, 90.88541666325266988, 3.042071309553174174 ) ) ;
#22190=CARTESIAN_POINT ( 'NONE',  ( -4.721056650415998313, 290.7343750017069510, 4.721056650416000089 ) ) ;
#22192=CARTESIAN_POINT ( 'NONE',  ( 8.660254037844385522, 76.45833332650536818, 5.000000000000005329 ) ) ;
#22193=LINE ( 'NONE', #64436, #45607 ) ;
#22194=CARTESIAN_POINT ( 'NONE',  ( 8.311093377946834337, 195.1562499965860411, 8.311093377946839666 ) ) ;
#22199=CARTESIAN_POINT ( 'NONE',  ( -11.35316468750000141, 163.5937499965860127, -1.390361679473963753E-15 ) ) ;
#22206=CARTESIAN_POINT ( 'NONE',  ( 8.311093377946834337, 50.15624999658601979, 8.311093377946839666 ) ) ;
#22207=CARTESIAN_POINT ( 'NONE',  ( -6.676582343750001591, 299.4531250017069510, 0.000000000000000000 ) ) ;
#22211=CARTESIAN_POINT ( 'NONE',  ( -7.320508075688773708, 168.7499999931720822, -7.320508075688774596 ) ) ;
#22212=CARTESIAN_POINT ( 'NONE',  ( -9.832129032723420536, 58.69791666325268409, 5.676582343749997150 ) ) ;
#22218=CARTESIAN_POINT ( 'NONE',  ( 6.951808397369818766E-16, 42.03124999658601268, -11.35316468750000141 ) ) ;
#22221=CARTESIAN_POINT ( 'NONE',  ( 3.042071309553167069, 171.8229166632526983, -11.35316468749999785 ) ) ;
#22222=CARTESIAN_POINT ( 'NONE',  ( 2.679491924311222739, 140.8333333265053682, 10.00000000000000355 ) ) ;
#22226=CARTESIAN_POINT ( 'NONE',  ( 3.042071309553159519, 35.05208332991935549, 11.35316468750000141 ) ) ;
#22228=CARTESIAN_POINT ( 'NONE',  ( -5.676582343749998039, 187.4479166632526983, -9.832129032723420536 ) ) ;
#22229=EDGE_LOOP ( 'NONE', ( #69243, #57568, #48401, #50386 ) ) ;
#22235=CARTESIAN_POINT ( 'NONE',  ( -5.676582343749998039, 162.4479166632526983, -9.832129032723420536 ) ) ;
#22241=CARTESIAN_POINT ( 'NONE',  ( -2.085542519210945728E-15, 119.8437499965860269, 11.35316468750000141 ) ) ;
#22277=CARTESIAN_POINT ( 'NONE',  ( 10.00000000000000178, 115.0000000000000000, 0.000000000000000000 ) ) ;
#22279=CARTESIAN_POINT ( 'NONE',  ( -2.765530957081996810, 289.4218750017069510, -6.676582343750003368 ) ) ;
#22289=CARTESIAN_POINT ( 'NONE',  ( -7.320508075688778149, 214.9999999931720822, 7.320508075688769267 ) ) ;
#22291=CARTESIAN_POINT ( 'NONE',  ( -9.832129032723418760, 17.86458332991935194, -5.676582343750004256 ) ) ;
#22292=CARTESIAN_POINT ( 'NONE',  ( 5.676582343749993598, 210.2604166632526699, 9.832129032723422313 ) ) ;
#22299=CARTESIAN_POINT ( 'NONE',  ( 5.676582343749993598, 24.94791666325268764, 9.832129032723422313 ) ) ;
#22301=CARTESIAN_POINT ( 'NONE',  ( 7.320508075688774596, 210.6249999999999716, -7.320508075688774596 ) ) ;
#22305=CARTESIAN_POINT ( 'NONE',  ( 9.832129032723416984, 5.364583329919349275, 5.676582343750006032 ) ) ;
#22307=CARTESIAN_POINT ( 'NONE',  ( -8.311093377946836114, 132.6562499965860411, -8.311093377946837890 ) ) ;
#22308=CARTESIAN_POINT ( 'NONE',  ( 10.00000000000000178, 107.0833333265053540, -2.679491924311226736 ) ) ;
#22315=CARTESIAN_POINT ( 'NONE',  ( -4.088227598258586603E-16, 291.3593750017070079, -6.676582343750001591 ) ) ;
#22322=ORIENTED_EDGE ( 'NONE', *, *, #43318, .F. ) ;
#22323=VECTOR ( 'NONE', #39007, 1000.000000000000000 ) ;
#22327=CARTESIAN_POINT ( 'NONE',  ( -8.311093377946836114, 77.96874999658598426, -8.311093377946837890 ) ) ;
#22338=ADVANCED_FACE ( 'NONE', ( #62458 ), #39459, .T. ) ;
#22350=ORIENTED_EDGE ( 'NONE', *, *, #15012, .T. ) ;
#22352=FACE_OUTER_BOUND ( 'NONE', #21442, .T. ) ;
#22359=CARTESIAN_POINT ( 'NONE',  ( 2.679491924311228956, 81.04166666666668561, -10.00000000000000000 ) ) ;
#22361=CARTESIAN_POINT ( 'NONE',  ( 6.676582343750004256, 299.0468750017069510, 2.765530957081995478 ) ) ;
#22368=DIRECTION ( 'NONE',  ( -0.000000000000000000, 1.000000000000000000, -0.000000000000000000 ) ) ;
#22369=CYLINDRICAL_SURFACE ( 'NONE', #21815, 10.00000000000000178 ) ;
#22371=EDGE_CURVE ( 'NONE', #38699, #49698, #32436, .T. ) ;
#22373=CARTESIAN_POINT ( 'NONE',  ( 10.00000000000000000, 199.7916666666666288, 2.679491924311236062 ) ) ;
#22375=CARTESIAN_POINT ( 'NONE',  ( -5.676582343750006032, 169.4270833299193555, 9.832129032723418760 ) ) ;
#22378=FACE_OUTER_BOUND ( 'NONE', #41173, .T. ) ;
#22380=VERTEX_POINT ( 'NONE', #5507 ) ;
#22382=CARTESIAN_POINT ( 'NONE',  ( -5.676582343750006032, 24.42708332991935194, 9.832129032723418760 ) ) ;
#22390=CARTESIAN_POINT ( 'NONE',  ( -2.679491924311235618, 60.41666665983869677, 10.00000000000000000 ) ) ;
#22402=CARTESIAN_POINT ( 'NONE',  ( -11.35316468750000141, 148.4895833299193555, 3.042071309553159963 ) ) ;
#22408=FACE_OUTER_BOUND ( 'NONE', #63935, .T. ) ;
#22412=ORIENTED_EDGE ( 'NONE', *, *, #60759, .F. ) ;
#22416=CARTESIAN_POINT ( 'NONE',  ( 5.676582343750001591, 121.9270833299193413, -9.832129032723420536 ) ) ;
#22421=CARTESIAN_POINT ( 'NONE',  ( 11.35316468749999963, 41.30208332991936260, -3.042071309553165293 ) ) ;
#22428=CARTESIAN_POINT ( 'NONE',  ( -6.000000000000001776, 295.0625000034140157, 0.000000000000000000 ) ) ;
#22432=CARTESIAN_POINT ( 'NONE',  ( -11.35316468750000141, 158.8020833299193555, 3.042071309553159963 ) ) ;
#22449=CARTESIAN_POINT ( 'NONE',  ( -10.00000000000000000, 42.29166666666667140, -2.679491924311229845 ) ) ;
#22452=CARTESIAN_POINT ( 'NONE',  ( 2.765530957082001251, 287.7656250017069510, 6.676582343749999815 ) ) ;
#22453=CARTESIAN_POINT ( 'NONE',  ( 0.000000000000000000, 300.0000000000000000, 0.000000000000000000 ) ) ;
#22458=CARTESIAN_POINT ( 'NONE',  ( -10.00000000000000355, 9.583333326505364624, 2.679491924311223183 ) ) ;
#22459=DIRECTION ( 'NONE',  ( 0.000000000000000000, 0.000000000000000000, 1.000000000000000000 ) ) ;
#22462=CARTESIAN_POINT ( 'NONE',  ( -10.00000000000000178, 167.5000000000000000, -1.224646799147353454E-15 ) ) ;
#22466=CARTESIAN_POINT ( 'NONE',  ( 11.35316468749999785, 125.8854166632526983, 3.042071309553174174 ) ) ;
#22478=CARTESIAN_POINT ( 'NONE',  ( 6.951808397369818766E-16, 207.3437499965860411, -11.35316468750000141 ) ) ;
#22484=CARTESIAN_POINT ( 'NONE',  ( 0.000000000000000000, 300.0000000000000000, 10.00000000000000178 ) ) ;
#22485=CARTESIAN_POINT ( 'NONE',  ( 9.832129032723420536, 96.19791666325269830, -5.676582343749999815 ) ) ;
#22486=VERTEX_POINT ( 'NONE', #41320 ) ;
#22487=( BOUNDED_CURVE ( )  B_SPLINE_CURVE ( 2, ( #20536, #3959, #21658, #20915, #9232, #43550, #4327, #66564, #32254, #55272, #66945, #27316, #4700 ),
 .UNSPECIFIED., .F., .F. ) 
 B_SPLINE_CURVE_WITH_KNOTS ( ( 3, 2, 2, 2, 2, 2, 3 ),
 ( 1.240293540008449158, 1.245526234162428691, 1.250758928316408003, 1.255991622470387314, 1.261224316624366848, 1.266457010778346159, 1.271689704932325693 ),
 .UNSPECIFIED. ) 
 CURVE ( )  GEOMETRIC_REPRESENTATION_ITEM ( )  RATIONAL_B_SPLINE_CURVE ( ( 0.9999999999999257261, 0.9659258262891424751, 0.9999999999999998890, 0.9659258262890683122, 0.9999999999999998890, 0.9659258262890683122, 0.9999999999999998890, 0.9659258262890683122, 0.9999999999999998890, 0.9659258262890683122, 0.9999999999999998890, 0.9659258262890683122, 0.9999999999999998890 ) ) 
 REPRESENTATION_ITEM ( '' )  );
#22492=CARTESIAN_POINT ( 'NONE',  ( 3.042071309553167069, 106.8229166632526699, -11.35316468749999785 ) ) ;
#22496=CARTESIAN_POINT ( 'NONE',  ( 10.00000000000000000, 216.6666666598387110, 2.679491924311236062 ) ) ;
#22500=CARTESIAN_POINT ( 'NONE',  ( -3.042071309553173730, 99.32291666325271251, 11.35316468749999785 ) ) ;
#22503=EDGE_CURVE ( 'NONE', #23374, #33509, #69383, .T. ) ;
#22504=CARTESIAN_POINT ( 'NONE',  ( 4.999999999999993783, 169.1666666666666856, 8.660254037844390851 ) ) ;
#22506=CARTESIAN_POINT ( 'NONE',  ( 10.00000000000000178, 187.0833333265053398, -2.679491924311226736 ) ) ;
#22509=CARTESIAN_POINT ( 'NONE',  ( 8.311093377946834337, 85.46874999658599847, 8.311093377946839666 ) ) ;
#22510=CARTESIAN_POINT ( 'NONE',  ( 4.721056650415999201, 288.0781250017069510, -4.721056650415999201 ) ) ;
#22513=EDGE_CURVE ( 'NONE', #62806, #23203, #68309, .T. ) ;
#22514=CARTESIAN_POINT ( 'NONE',  ( -11.35316468750000141, 218.2812499965860411, -1.390361679473963753E-15 ) ) ;
#22515=( BOUNDED_CURVE ( )  B_SPLINE_CURVE ( 2, ( #40495, #45778, #52196, #23506, #897, #46522, #63501, #68054, #35224, #69541, #5800, #11823, #11455 ),
 .UNSPECIFIED., .F., .F. ) 
 B_SPLINE_CURVE_WITH_KNOTS ( ( 3, 2, 2, 2, 2, 2, 3 ),
 ( 0.3641304347826087029, 0.3659420289855072617, 0.3677536231884058204, 0.3695652173913043237, 0.3713768115942028825, 0.3731884057971014412, 0.3750000000000000000 ),
 .UNSPECIFIED. ) 
 CURVE ( )  GEOMETRIC_REPRESENTATION_ITEM ( )  RATIONAL_B_SPLINE_CURVE ( ( 1.000000000000000000, 0.9659258262890683122, 1.000000000000000000, 0.9659258262890683122, 1.000000000000000000, 0.9659258262890683122, 1.000000000000000000, 0.9659258262890683122, 1.000000000000000000, 0.9659258262890683122, 1.000000000000000000, 0.9659258262890683122, 1.000000000000000000 ) ) 
 REPRESENTATION_ITEM ( '' )  );
#22517=CARTESIAN_POINT ( 'NONE',  ( -8.660254037844387298, 68.95833332650536818, -5.000000000000004441 ) ) ;
#22520=CARTESIAN_POINT ( 'NONE',  ( 8.311093377946834337, 225.1562499965860411, 8.311093377946839666 ) ) ;
#22523=CARTESIAN_POINT ( 'NONE',  ( 4.721056650416000089, 295.8281250017069510, 4.721056650415999201 ) ) ;
#22525=CARTESIAN_POINT ( 'NONE',  ( 11.35316468750000141, 196.0937499965860127, 0.000000000000000000 ) ) ;
#22535=CARTESIAN_POINT ( 'NONE',  ( 5.000000000000001776, 20.83333333333333570, -8.660254037844389075 ) ) ;
#22543=CARTESIAN_POINT ( 'NONE',  ( 1.102182119232618108E-15, 291.2500000000000000, 6.000000000000001776 ) ) ;
#22551=VECTOR ( 'NONE', #12798, 1000.000000000000000 ) ;
#22558=CARTESIAN_POINT ( 'NONE',  ( -9.832129032723420536, 94.01041666325268409, 5.676582343749997150 ) ) ;
#22563=CARTESIAN_POINT ( 'NONE',  ( -6.676582343749999815, 290.6718750017070079, 2.765530957082001251 ) ) ;
#22565=FACE_OUTER_BOUND ( 'NONE', #3705, .T. ) ;
#22566=CARTESIAN_POINT ( 'NONE',  ( -11.35316468749999785, 198.0729166632526983, -3.042071309553167513 ) ) ;
#22567=EDGE_CURVE ( 'NONE', #12039, #61682, #39697, .T. ) ;
#22573=CARTESIAN_POINT ( 'NONE',  ( 8.311093377946834337, 170.4687499965860127, 8.311093377946839666 ) ) ;
#22580=CARTESIAN_POINT ( 'NONE',  ( -3.042071309553164404, 52.23958332991934128, -11.35316468749999963 ) ) ;
#22583=ORIENTED_EDGE ( 'NONE', *, *, #39625, .T. ) ;
#22587=CARTESIAN_POINT ( 'NONE',  ( -3.042071309553164404, 67.23958332991935549, -11.35316468749999963 ) ) ;
#22591=CARTESIAN_POINT ( 'NONE',  ( -2.679491924311272477, 11.45833333333333925, -9.999999999999976907 ) ) ;
#22593=CARTESIAN_POINT ( 'NONE',  ( -3.042071309553173730, 64.32291666325269830, 11.35316468749999785 ) ) ;
#22596=CARTESIAN_POINT ( 'NONE',  ( 5.676582343749993598, 169.9479166632526983, 9.832129032723422313 ) ) ;
#22597=CARTESIAN_POINT ( 'NONE',  ( 6.123233995736767268E-16, 143.1249999931720538, -10.00000000000000178 ) ) ;
#22600=CARTESIAN_POINT ( 'NONE',  ( -3.042071309553163960, 32.55208332991934128, -11.35316468749999963 ) ) ;
#22602=CARTESIAN_POINT ( 'NONE',  ( 3.042071309553159519, 179.7395833299193555, 11.35316468750000141 ) ) ;
#22609=CARTESIAN_POINT ( 'NONE',  ( -3.042071309553163960, 162.2395833299192986, -11.35316468749999963 ) ) ;
#22613=CARTESIAN_POINT ( 'NONE',  ( 0.000000000000000000, 300.0000000000000000, 0.000000000000000000 ) ) ;
#22619=CARTESIAN_POINT ( 'NONE',  ( 9.832129032723420536, 121.5104166632526841, -5.676582343749999815 ) ) ;
#22620=CARTESIAN_POINT ( 'NONE',  ( 0.4499999999999975131, 255.9999999999997726, 5.815339556497987061 ) ) ;
#22639=ORIENTED_EDGE ( 'NONE', *, *, #58814, .T. ) ;
#22646=CARTESIAN_POINT ( 'NONE',  ( 0.000000000000000000, 0.000000000000000000, 0.000000000000000000 ) ) ;
#22648=CARTESIAN_POINT ( 'NONE',  ( -10.00000000000000355, 122.7083333333333144, 2.679491924311223183 ) ) ;
#22664=CARTESIAN_POINT ( 'NONE',  ( -8.311093377946841443, 13.90624999658601801, 8.311093377946830785 ) ) ;
#22665=FACE_OUTER_BOUND ( 'NONE', #55847, .T. ) ;
#22666=CARTESIAN_POINT ( 'NONE',  ( -11.35316468750000141, 203.8020833299193839, 3.042071309553159963 ) ) ;
#22668=DIRECTION ( 'NONE',  ( -0.000000000000000000, 1.000000000000000000, -0.000000000000000000 ) ) ;
#22675=CARTESIAN_POINT ( 'NONE',  ( -8.311093377946841443, 23.90624999658601979, 8.311093377946830785 ) ) ;
#22681=CARTESIAN_POINT ( 'NONE',  ( 11.35316468749999963, 0.9895833299193492749, -3.042071309553165293 ) ) ;
#22683=CARTESIAN_POINT ( 'NONE',  ( 8.311093377946837890, 136.4062499965859558, -8.311093377946837890 ) ) ;
#22684=EDGE_CURVE ( 'NONE', #22486, #28203, #29628, .T. ) ;
#22685=CARTESIAN_POINT ( 'NONE',  ( 5.000000000000001776, 97.70833332650536818, -8.660254037844389075 ) ) ;
#22692=CYLINDRICAL_SURFACE ( 'NONE', #45016, 10.00000000000000178 ) ;
#22693=CARTESIAN_POINT ( 'NONE',  ( 6.676582343750001591, 295.9531250017069510, -8.176455196517173205E-16 ) ) ;
#22694=CARTESIAN_POINT ( 'NONE',  ( -3.042071309553163960, 132.2395833299193555, -11.35316468749999963 ) ) ;
#22704=FACE_OUTER_BOUND ( 'NONE', #27353, .T. ) ;
#22706=CARTESIAN_POINT ( 'NONE',  ( 11.35316468749999963, 76.30208332991935549, -3.042071309553165293 ) ) ;
#22712=CARTESIAN_POINT ( 'NONE',  ( 7.320508075688773708, 115.6249999999999858, -7.320508075688773708 ) ) ;
#22731=CARTESIAN_POINT ( 'NONE',  ( -6.000000000000001776, 292.0000000000000000, 0.000000000000000000 ) ) ;
#22737=CARTESIAN_POINT ( 'NONE',  ( 10.00000000000000178, 75.20833333333334281, -2.679491924311226736 ) ) ;
#22740=CARTESIAN_POINT ( 'NONE',  ( -4.721056650415999201, 299.4843750017070079, -4.721056650415999201 ) ) ;
#22746=CARTESIAN_POINT ( 'NONE',  ( 10.00000000000000178, 57.08333332650536107, -2.679491924311226736 ) ) ;
#22749=CARTESIAN_POINT ( 'NONE',  ( -4.999999999999998224, 206.6666666666666856, -8.660254037844389075 ) ) ;
#22751=CARTESIAN_POINT ( 'NONE',  ( -3.042071309553164404, 172.5520833299193555, -11.35316468749999963 ) ) ;
#22752=CARTESIAN_POINT ( 'NONE',  ( -1.522892193876115035E-11, 103.7499999999988205, 10.00000000000000178 ) ) ;
#22759=CARTESIAN_POINT ( 'NONE',  ( -3.042071309553164404, 42.55208332991933418, -11.35316468749999963 ) ) ;
#22767=CARTESIAN_POINT ( 'NONE',  ( -7.320508075688773708, 58.74999999317203958, -7.320508075688774596 ) ) ;
#22772=CARTESIAN_POINT ( 'NONE',  ( 10.00000000000000178, 101.8749999931720396, 0.000000000000000000 ) ) ;
#22773=ORIENTED_EDGE ( 'NONE', *, *, #67540, .T. ) ;
#22779=CARTESIAN_POINT ( 'NONE',  ( -11.35316468750000141, 138.2812499965860411, -1.390361679473963753E-15 ) ) ;
#22792=CARTESIAN_POINT ( 'NONE',  ( -8.311093377946841443, 124.2187499965860127, 8.311093377946834337 ) ) ;
#22796=CARTESIAN_POINT ( 'NONE',  ( 8.311093377946837890, 31.71874999658601624, -8.311093377946837890 ) ) ;
#22799=CARTESIAN_POINT ( 'NONE',  ( -5.000000000000005329, 195.2083333265053966, 8.660254037844387298 ) ) ;
#22804=CARTESIAN_POINT ( 'NONE',  ( 6.000000000000003553, 295.5000000034140157, 2.485281374238571317 ) ) ;
#22807=CARTESIAN_POINT ( 'NONE',  ( -8.311093377946841443, 154.2187499965859843, 8.311093377946830785 ) ) ;
#22809=AXIS2_PLACEMENT_3D ( 'NONE', #24902, #47184, #6476 ) ;
#22827=CARTESIAN_POINT ( 'NONE',  ( -3.673940397442060854E-16, 296.7500000000000000, -6.000000000000001776 ) ) ;
#22828=CARTESIAN_POINT ( 'NONE',  ( 8.660254037844389075, 40.41666666666667140, -5.000000000000000000 ) ) ;
#22831=CARTESIAN_POINT ( 'NONE',  ( 6.000000000000003553, 298.5625000000000568, -2.485281374238571761 ) ) ;
#22833=CARTESIAN_POINT ( 'NONE',  ( 3.410844894484189267E-12, 36.24999999999974420, -10.00000000000000178 ) ) ;
#22834=CARTESIAN_POINT ( 'NONE',  ( 8.660254037844385522, 196.4583333265053966, 5.000000000000005329 ) ) ;
#22841=CARTESIAN_POINT ( 'NONE',  ( 0.000000000000000000, 300.0000000000000000, 0.000000000000000000 ) ) ;
#22843=CARTESIAN_POINT ( 'NONE',  ( -7.320508075688773708, 138.7499999931720254, -7.320508075688774596 ) ) ;
#22845=CARTESIAN_POINT ( 'NONE',  ( -1.836970198721029983E-15, 158.7500000000000000, 10.00000000000000178 ) ) ;
#22849=CARTESIAN_POINT ( 'NONE',  ( 6.951808397369818766E-16, 132.3437499965860127, -11.35316468750000141 ) ) ;
#22858=CARTESIAN_POINT ( 'NONE',  ( 2.679491924311103723, 193.9583333333333997, 10.00000000000019362 ) ) ;
#22862=CARTESIAN_POINT ( 'NONE',  ( 3.042071309553159519, 225.0520833299193555, 11.35316468750000141 ) ) ;
#22870=CARTESIAN_POINT ( 'NONE',  ( -9.832129032723418760, 102.8645833299193697, -5.676582343750004256 ) ) ;
#22877=CARTESIAN_POINT ( 'NONE',  ( -11.35316468750000141, 103.2812499965860269, -1.390361679473963753E-15 ) ) ;
#22882=CARTESIAN_POINT ( 'NONE',  ( 4.999999999999993783, 226.0416666598387110, 8.660254037844390851 ) ) ;
#22886=CARTESIAN_POINT ( 'NONE',  ( 6.951808397369818766E-16, 97.03124999658602690, -11.35316468750000141 ) ) ;
#22891=CARTESIAN_POINT ( 'NONE',  ( 10.00000000000000178, 201.8749999931720538, 0.000000000000000000 ) ) ;
#22895=CARTESIAN_POINT ( 'NONE',  ( 5.676582343750001591, 91.92708332991935549, -9.832129032723420536 ) ) ;
#22896=CARTESIAN_POINT ( 'NONE',  ( -6.676582343750001591, 290.4531250017069510, 0.000000000000000000 ) ) ;
#22899=CARTESIAN_POINT ( 'NONE',  ( -3.042071309553164404, 222.2395833299193555, -11.35316468749999963 ) ) ;
#22902=CYLINDRICAL_SURFACE ( 'NONE', #8726, 10.00000000000000178 ) ;
#22904=CARTESIAN_POINT ( 'NONE',  ( -3.042071309553163960, 217.2395833299193271, -11.35316468749999963 ) ) ;
#22906=CARTESIAN_POINT ( 'NONE',  ( -8.660254037844548947, 157.9166666666667993, 5.000000000000091482 ) ) ;
#22907=CARTESIAN_POINT ( 'NONE',  ( 6.676582343750004256, 295.8906250017069510, 2.765530957081995478 ) ) ;
#22910=CARTESIAN_POINT ( 'NONE',  ( -2.085542519210945728E-15, 209.8437499965860411, 11.35316468750000141 ) ) ;
#22918=CARTESIAN_POINT ( 'NONE',  ( -5.000000000000005329, 28.33333333333333570, 8.660254037844387298 ) ) ;
#22931=CARTESIAN_POINT ( 'NONE',  ( 6.676582343750003368, 296.8906250017069510, 2.765530957081995478 ) ) ;
#22945=CARTESIAN_POINT ( 'NONE',  ( 9.832129032723420536, 86.51041666325268409, -5.676582343749999815 ) ) ;
#22950=CARTESIAN_POINT ( 'NONE',  ( -1.538508811358849613E-11, 71.25000000000120792, -10.00000000000000178 ) ) ;
#22955=CARTESIAN_POINT ( 'NONE',  ( -5.676582343750006032, 194.1145833299193839, 9.832129032723418760 ) ) ;
#22959=CARTESIAN_POINT ( 'NONE',  ( -3.042071309553164404, 182.5520833299193271, -11.35316468749999963 ) ) ;
#22963=CARTESIAN_POINT ( 'NONE',  ( -4.999999999999996447, 106.6666666666666714, -8.660254037844383745 ) ) ;
#22966=B_SPLINE_CURVE_WITH_KNOTS ( 'NONE', 1,
 ( #72348, #20660 ),
 .UNSPECIFIED., .F., .F.,
 ( 2, 2 ),
 ( 0.000000000000000000, 1.000000000000000000 ),
 .UNSPECIFIED. ) ;
#22968=CARTESIAN_POINT ( 'NONE',  ( 11.35316468749999785, 55.57291666325267698, 3.042071309553174174 ) ) ;
#22975=CARTESIAN_POINT ( 'NONE',  ( 11.35316468749999963, 55.98958332991934128, -3.042071309553165293 ) ) ;
#22980=CARTESIAN_POINT ( 'NONE',  ( -8.311093377946841443, 58.90624999658600558, 8.311093377946834337 ) ) ;
#22983=CARTESIAN_POINT ( 'NONE',  ( 8.311093377946834337, 175.1562499965860127, 8.311093377946839666 ) ) ;
#22985=CARTESIAN_POINT ( 'NONE',  ( 10.00000000000000000, 161.6666666598386826, 2.679491924311236062 ) ) ;
#22988=CARTESIAN_POINT ( 'NONE',  ( -3.042071309553173730, 49.63541666325268409, 11.35316468749999785 ) ) ;
#22990=CARTESIAN_POINT ( 'NONE',  ( -8.311093377946836114, 177.6562499965859843, -8.311093377946837890 ) ) ;
#22995=CARTESIAN_POINT ( 'NONE',  ( 11.35316468750000141, 180.7812499965860411, 0.000000000000000000 ) ) ;
#23001=AXIS2_PLACEMENT_3D ( 'NONE', #13025, #36062, #30027 ) ;
#23004=CARTESIAN_POINT ( 'NONE',  ( -11.35316468750000141, 123.5937499965860269, -1.390361679473963753E-15 ) ) ;
#23005=CARTESIAN_POINT ( 'NONE',  ( 8.660254037844385522, 11.45833332650536640, 5.000000000000005329 ) ) ;
#23010=EDGE_CURVE ( 'NONE', #23294, #21472, #4675, .T. ) ;
#23020=EDGE_CURVE ( 'NONE', #17783, #32479, #5051, .T. ) ;
#23025=EDGE_CURVE ( 'NONE', #15471, #70797, #46138, .T. ) ;
#23032=CARTESIAN_POINT ( 'NONE',  ( -6.676582343749999815, 298.6718750017070079, 2.765530957082001251 ) ) ;
#23033=CARTESIAN_POINT ( 'NONE',  ( -8.660254037844390851, 122.9166666666666714, 4.999999999999998224 ) ) ;
#23035=CARTESIAN_POINT ( 'NONE',  ( 6.676582343750001591, 288.1093750017069510, -8.176455196517173205E-16 ) ) ;
#23045=CARTESIAN_POINT ( 'NONE',  ( 5.000000000000001776, 52.70833332650536818, -8.660254037844389075 ) ) ;
#23047=CARTESIAN_POINT ( 'NONE',  ( -3.042071309553173730, 9.322916663252685865, 11.35316468749999785 ) ) ;
#23049=CARTESIAN_POINT ( 'NONE',  ( -11.35316468750000141, 218.5937499965860411, -1.390361679473963753E-15 ) ) ;
#23056=CARTESIAN_POINT ( 'NONE',  ( 11.35316468750000141, 15.78124999658601624, 0.000000000000000000 ) ) ;
#23062=CARTESIAN_POINT ( 'NONE',  ( 9.832129032723420536, 16.19791666325268054, -5.676582343749999815 ) ) ;
#23065=CARTESIAN_POINT ( 'NONE',  ( 3.042071309553159519, 129.7395833299193555, 11.35316468750000141 ) ) ;
#23066=CARTESIAN_POINT ( 'NONE',  ( -7.320508075688773708, 103.7499999931720396, -7.320508075688774596 ) ) ;
#23072=CARTESIAN_POINT ( 'NONE',  ( -11.35316468749999785, 8.385416663252684089, -3.042071309553167957 ) ) ;
#23074=CARTESIAN_POINT ( 'NONE',  ( -6.676582343750001591, 296.4531250017069510, 0.000000000000000000 ) ) ;
#23075=CARTESIAN_POINT ( 'NONE',  ( -8.311093377946841443, 138.9062499965859843, 8.311093377946834337 ) ) ;
#23085=CARTESIAN_POINT ( 'NONE',  ( 9.832129032723416984, 80.67708332991935549, 5.676582343750006032 ) ) ;
#23093=VECTOR ( 'NONE', #14118, 1000.000000000000000 ) ;
#23110=VERTEX_POINT ( 'NONE', #17463 ) ;
#23116=CARTESIAN_POINT ( 'NONE',  ( 7.320508075688771044, 84.37499999999998579, 7.320508075688775484 ) ) ;
#23119=CARTESIAN_POINT ( 'NONE',  ( 6.951808397369818766E-16, 62.34374999658602690, -11.35316468750000141 ) ) ;
#23120=CARTESIAN_POINT ( 'NONE',  ( 4.242640687119285658, 289.6249999999999432, -4.242640687119286547 ) ) ;
#23121=EDGE_CURVE ( 'NONE', #24215, #28711, #34104, .T. ) ;
#23127=CARTESIAN_POINT ( 'NONE',  ( 0.000000000000000000, 300.0000000000000000, 0.000000000000000000 ) ) ;
#23131=CARTESIAN_POINT ( 'NONE',  ( -8.660254037844390851, 202.9166666666666856, 4.999999999999998224 ) ) ;
#23133=CARTESIAN_POINT ( 'NONE',  ( 11.35316468749999785, 165.8854166632526415, 3.042071309553174174 ) ) ;
#23134=CARTESIAN_POINT ( 'NONE',  ( -9.999999999999998224, 37.50000000000000711, -1.224646799147353059E-15 ) ) ;
#23135=CARTESIAN_POINT ( 'NONE',  ( 4.999999999999993783, 176.0416666598387110, 8.660254037844390851 ) ) ;
#23140=CARTESIAN_POINT ( 'NONE',  ( 9.832129032723420536, 41.51041666325268409, -5.676582343749999815 ) ) ;
#23148=CARTESIAN_POINT ( 'NONE',  ( 7.320508075688774596, 62.49999999317202537, -7.320508075688774596 ) ) ;
#23151=CARTESIAN_POINT ( 'NONE',  ( 7.320508075688934468, 214.3750000000000853, 7.320508075688938909 ) ) ;
#23154=ORIENTED_EDGE ( 'NONE', *, *, #2363, .F. ) ;
#23157=CARTESIAN_POINT ( 'NONE',  ( -4.088227598258586603E-16, 299.3593750017070079, -6.676582343750001591 ) ) ;
#23160=CARTESIAN_POINT ( 'NONE',  ( 9.832129032723416984, 150.3645833299193555, 5.676582343750006032 ) ) ;
#23165=CARTESIAN_POINT ( 'NONE',  ( -3.673940397442060854E-16, 297.8125000034140157, -6.000000000000001776 ) ) ;
#23171=CARTESIAN_POINT ( 'NONE',  ( -11.35316468750000141, 133.5937499965860127, -1.390361679473963753E-15 ) ) ;
#23175=CARTESIAN_POINT ( 'NONE',  ( -2.085542519210945728E-15, 29.84374999658601624, 11.35316468750000141 ) ) ;
#23178=CARTESIAN_POINT ( 'NONE',  ( 5.000000000000001776, 37.70833332650536818, -8.660254037844389075 ) ) ;
#23185=CARTESIAN_POINT ( 'NONE',  ( 6.000000000000001776, 295.5625000034140157, -7.347880794884121708E-16 ) ) ;
#23190=CARTESIAN_POINT ( 'NONE',  ( -3.042071309553173730, 149.6354166632526983, 11.35316468749999785 ) ) ;
#23193=CARTESIAN_POINT ( 'NONE',  ( -3.673940397442060854E-16, 298.8125000034140157, -6.000000000000001776 ) ) ;
#23196=EDGE_CURVE ( 'NONE', #19863, #71793, #16983, .T. ) ;
#23200=EDGE_CURVE ( 'NONE', #37587, #12265, #10839, .T. ) ;
#23201=CARTESIAN_POINT ( 'NONE',  ( 6.123233995736767268E-16, 56.25000000000000000, -10.00000000000000178 ) ) ;
#23203=VERTEX_POINT ( 'NONE', #24601 ) ;
#23206=CARTESIAN_POINT ( 'NONE',  ( -10.00000000000000178, 209.3749999931720538, -1.224646799147353454E-15 ) ) ;
#23207=CARTESIAN_POINT ( 'NONE',  ( -10.00000000000000178, 44.37499999317203248, -1.224646799147353454E-15 ) ) ;
#23208=CARTESIAN_POINT ( 'NONE',  ( -10.00000000000000355, 42.70833333333333570, 2.679491924311223183 ) ) ;
#23211=CARTESIAN_POINT ( 'NONE',  ( 6.000000000000003553, 299.5625000000000000, -2.485281374238571761 ) ) ;
#23212=EDGE_CURVE ( 'NONE', #9014, #47712, #18093, .T. ) ;
#23219=CARTESIAN_POINT ( 'NONE',  ( -5.000000000000005329, 10.20833332650536640, 8.660254037844387298 ) ) ;
#23221=CARTESIAN_POINT ( 'NONE',  ( 1.491046635511791134E-11, 146.2499999999988631, -9.999999999999998224 ) ) ;
#23222=CARTESIAN_POINT ( 'NONE',  ( -8.660254037844387298, 162.0833333333333712, -5.000000000000004441 ) ) ;
#23226=CARTESIAN_POINT ( 'NONE',  ( 3.042071309553167069, 122.1354166632526841, -11.35316468749999785 ) ) ;
#23239=CARTESIAN_POINT ( 'NONE',  ( 10.00000000000000000, 16.66666665983870033, 2.679491924311236062 ) ) ;
#23246=CARTESIAN_POINT ( 'NONE',  ( 11.35316468750000141, 110.7812499965860269, 0.000000000000000000 ) ) ;
#23250=CARTESIAN_POINT ( 'NONE',  ( 2.752039609470550924E-11, 41.24999999999786127, -9.999999999999998224 ) ) ;
#23252=CARTESIAN_POINT ( 'NONE',  ( -11.35316468750000141, 108.2812499965860269, -1.390361679473963753E-15 ) ) ;
#23256=CARTESIAN_POINT ( 'NONE',  ( 10.00000000000000178, 226.8749999931720254, 0.000000000000000000 ) ) ;
#23260=CARTESIAN_POINT ( 'NONE',  ( -5.676582343749998039, 102.4479166632526841, -9.832129032723420536 ) ) ;
#23263=CARTESIAN_POINT ( 'NONE',  ( 8.660254037844389075, 170.4166666666666856, -5.000000000000000000 ) ) ;
#23265=CARTESIAN_POINT ( 'NONE',  ( 10.00000000000000000, 196.6666666598386826, 2.679491924311236062 ) ) ;
#23268=CARTESIAN_POINT ( 'NONE',  ( 11.35316468749999963, 91.30208332991932707, -3.042071309553165293 ) ) ;
#23269=CARTESIAN_POINT ( 'NONE',  ( 4.721056650415999201, 291.0781250017069510, -4.721056650415999201 ) ) ;
#23272=CARTESIAN_POINT ( 'NONE',  ( 5.676582343750001591, 226.6145833299193839, -9.832129032723420536 ) ) ;
#23276=CARTESIAN_POINT ( 'NONE',  ( 11.35316468749999963, 220.9895833299193555, -3.042071309553165293 ) ) ;
#23278=CARTESIAN_POINT ( 'NONE',  ( 6.676582343750004256, 294.8906250017069510, 2.765530957081995478 ) ) ;
#23281=CARTESIAN_POINT ( 'NONE',  ( 11.35316468749999785, 205.8854166632526699, 3.042071309553174174 ) ) ;
#23286=ORIENTED_EDGE ( 'NONE', *, *, #6738, .T. ) ;
#23289=CARTESIAN_POINT ( 'NONE',  ( -10.00000000000000178, 32.50000000000000000, -1.224646799147353454E-15 ) ) ;
#23294=VERTEX_POINT ( 'NONE', #64237 ) ;
#23301=CARTESIAN_POINT ( 'NONE',  ( -2.765530957081998142, 296.6406250017069510, 6.676582343750000703 ) ) ;
#23306=EDGE_CURVE ( 'NONE', #71352, #53888, #46510, .T. ) ;
#23313=CARTESIAN_POINT ( 'NONE',  ( 11.35316468750000141, 91.09374999658602690, 0.000000000000000000 ) ) ;
#23314=CARTESIAN_POINT ( 'NONE',  ( 0.000000000000000000, 300.0000000000000000, 0.000000000000000000 ) ) ;
#23318=CARTESIAN_POINT ( 'NONE',  ( 6.676582343750001591, 288.1093750017069510, -8.176455196517173205E-16 ) ) ;
#23322=CARTESIAN_POINT ( 'NONE',  ( -8.311093377946836114, 202.6562499965860127, -8.311093377946837890 ) ) ;
#23326=CARTESIAN_POINT ( 'NONE',  ( 11.35316468749999963, 186.3020833299193555, -3.042071309553165293 ) ) ;
#23334=CARTESIAN_POINT ( 'NONE',  ( 6.951808397369818766E-16, 62.03124999658601979, -11.35316468750000141 ) ) ;
#23335=EDGE_CURVE ( 'NONE', #5410, #54290, #36834, .T. ) ;
#23342=CARTESIAN_POINT ( 'NONE',  ( -11.35316468750000141, 68.48958332991935549, 3.042071309553159963 ) ) ;
#23347=CARTESIAN_POINT ( 'NONE',  ( -8.311093377946841443, 63.90624999658601979, 8.311093377946834337 ) ) ;
#23350=CARTESIAN_POINT ( 'NONE',  ( 5.000000000000001776, 152.7083333265053682, -8.660254037844389075 ) ) ;
#23352=CARTESIAN_POINT ( 'NONE',  ( -8.660254037844390851, 54.79166665983869677, 4.999999999999998224 ) ) ;
#23353=CARTESIAN_POINT ( 'NONE',  ( 11.35316468750000141, 46.09374999658602690, 0.000000000000000000 ) ) ;
#23355=CARTESIAN_POINT ( 'NONE',  ( 5.676582343749993598, 179.9479166632526983, 9.832129032723422313 ) ) ;
#23360=CARTESIAN_POINT ( 'NONE',  ( -8.311093377946836114, 177.6562499965859843, -8.311093377946837890 ) ) ;
#23366=ORIENTED_EDGE ( 'NONE', *, *, #71978, .T. ) ;
#23367=EDGE_CURVE ( 'NONE', #60693, #38468, #37421, .T. ) ;
#23368=CARTESIAN_POINT ( 'NONE',  ( -11.35316468749999785, 168.3854166632526699, -3.042071309553167957 ) ) ;
#23371=CARTESIAN_POINT ( 'NONE',  ( 6.951808397369818766E-16, 132.3437499965860127, -11.35316468750000141 ) ) ;
#23374=VERTEX_POINT ( 'NONE', #66077 ) ;
#23395=DIRECTION ( 'NONE',  ( -0.000000000000000000, 1.000000000000000000, -0.000000000000000000 ) ) ;
#23398=CARTESIAN_POINT ( 'NONE',  ( -2.485281374238875962, 289.8750000034139020, -5.999999999999697131 ) ) ;
#23400=CARTESIAN_POINT ( 'NONE',  ( -6.676582343750001591, 299.6093750017069510, 0.000000000000000000 ) ) ;
#23401=CARTESIAN_POINT ( 'NONE',  ( 8.660254037844385522, 139.5833333333333428, 5.000000000000005329 ) ) ;
#23403=CARTESIAN_POINT ( 'NONE',  ( 4.721056650416000089, 289.9843750017070079, 4.721056650415999201 ) ) ;
#23418=CARTESIAN_POINT ( 'NONE',  ( -11.35316468749999785, 33.07291666325268409, -3.042071309553167513 ) ) ;
#23420=CARTESIAN_POINT ( 'NONE',  ( 5.676582343750001591, 226.9270833299193839, -9.832129032723420536 ) ) ;
#23421=CARTESIAN_POINT ( 'NONE',  ( -10.00000000000000178, 219.3749999931720538, -1.224646799147353454E-15 ) ) ;
#23426=CARTESIAN_POINT ( 'NONE',  ( 9.832129032723416984, 25.36458332991935194, 5.676582343750006032 ) ) ;
#23432=CARTESIAN_POINT ( 'NONE',  ( -11.35316468750000141, 13.48958332991935194, 3.042071309553159963 ) ) ;
#23434=CARTESIAN_POINT ( 'NONE',  ( 11.35316468749999963, 130.9895833299193555, -3.042071309553165293 ) ) ;
#23435=CARTESIAN_POINT ( 'NONE',  ( 8.660254037844389075, 112.2916666598387110, -5.000000000000000000 ) ) ;
#23441=CARTESIAN_POINT ( 'NONE',  ( -11.35316468749999785, 13.38541666325268409, -3.042071309553167957 ) ) ;
#23443=CARTESIAN_POINT ( 'NONE',  ( 2.765530957081996366, 297.1406250017070079, -6.676582343750003368 ) ) ;
#23444=CARTESIAN_POINT ( 'NONE',  ( 5.676582343749993598, 134.9479166632526983, 9.832129032723422313 ) ) ;
#23447=AXIS2_PLACEMENT_3D ( 'NONE', #52275, #53386, #69249 ) ;
#23454=CARTESIAN_POINT ( 'NONE',  ( 2.679491924310934969, 217.9166666598387962, -10.00000000000017053 ) ) ;
#23456=CARTESIAN_POINT ( 'NONE',  ( -3.042071309553164404, 87.55208332991936970, -11.35316468749999963 ) ) ;
#23487=CARTESIAN_POINT ( 'NONE',  ( 10.00000000000000000, 89.79166666666665719, 2.679491924311236062 ) ) ;
#23489=CARTESIAN_POINT ( 'NONE',  ( 3.042071309553167069, 67.13541666325266988, -11.35316468749999785 ) ) ;
#23490=CARTESIAN_POINT ( 'NONE',  ( -4.242640687119285658, 290.1249999999999432, 4.242640687119287435 ) ) ;
#23493=CARTESIAN_POINT ( 'NONE',  ( 6.000000000000003553, 294.4375000000000000, 2.485281374238571317 ) ) ;
#23501=CARTESIAN_POINT ( 'NONE',  ( 10.00000000000000178, 195.0000000000000000, 0.000000000000000000 ) ) ;
#23503=CARTESIAN_POINT ( 'NONE',  ( -3.042071309553173730, 184.6354166632526983, 11.35316468749999785 ) ) ;
#23506=CARTESIAN_POINT ( 'NONE',  ( 7.320508075688771044, 86.24999999317203958, 7.320508075688775484 ) ) ;
#23507=VERTEX_POINT ( 'NONE', #31005 ) ;
#23509=CARTESIAN_POINT ( 'NONE',  ( -9.832129032723420536, 39.01041666325268409, 5.676582343749997150 ) ) ;
#23513=CARTESIAN_POINT ( 'NONE',  ( -4.999999999999998224, 123.5416666598387110, -8.660254037844389075 ) ) ;
#23514=CYLINDRICAL_SURFACE ( 'NONE', #40050, 15.99999999999998579 ) ;
#23518=EDGE_CURVE ( 'NONE', #30885, #10942, #28228, .T. ) ;
#23519=CARTESIAN_POINT ( 'NONE',  ( 10.00000000000000000, 76.66666665983871098, 2.679491924311236062 ) ) ;
#23526=EDGE_LOOP ( 'NONE', ( #52427, #27200, #42982, #8321 ) ) ;
#23529=CARTESIAN_POINT ( 'NONE',  ( 2.765530957081996366, 297.2968750017070079, -6.676582343750003368 ) ) ;
#23531=CARTESIAN_POINT ( 'NONE',  ( 5.000000000000001776, 42.70833332650536818, -8.660254037844389075 ) ) ;
#23532=CARTESIAN_POINT ( 'NONE',  ( 8.311093377946834337, 150.1562499965859843, 8.311093377946839666 ) ) ;
#23536=DIRECTION ( 'NONE',  ( -0.000000000000000000, 1.000000000000000000, -0.000000000000000000 ) ) ;
#23543=CARTESIAN_POINT ( 'NONE',  ( 8.311093377946837890, 126.7187499965860269, -8.311093377946837890 ) ) ;
#23547=CARTESIAN_POINT ( 'NONE',  ( 5.676582343750001591, 51.92708332991935549, -9.832129032723420536 ) ) ;
#23554=CARTESIAN_POINT ( 'NONE',  ( 4.242640687119285658, 296.6875000034139589, -4.242640687119286547 ) ) ;
#23563=ORIENTED_EDGE ( 'NONE', *, *, #21440, .F. ) ;
#23577=CARTESIAN_POINT ( 'NONE',  ( -8.660254037844390851, 44.79166665983870388, 4.999999999999998224 ) ) ;
#23578=CARTESIAN_POINT ( 'NONE',  ( -2.679491924311225848, 41.45833333333332149, -10.00000000000000178 ) ) ;
#23581=CARTESIAN_POINT ( 'NONE',  ( 6.000000000000003553, 299.4375000000000000, 2.485281374238571317 ) ) ;
#23582=CARTESIAN_POINT ( 'NONE',  ( -8.660254037844387298, 33.95833332650536818, -5.000000000000004441 ) ) ;
#23592=CARTESIAN_POINT ( 'NONE',  ( 10.00000000000000178, 155.2083333333333712, -2.679491924311226736 ) ) ;
#23596=CARTESIAN_POINT ( 'NONE',  ( 5.676582343750001591, 141.9270833299193555, -9.832129032723420536 ) ) ;
#23602=ORIENTED_EDGE ( 'NONE', *, *, #74221, .T. ) ;
#23609=CARTESIAN_POINT ( 'NONE',  ( -8.660254037844390851, 19.79166665983870033, 4.999999999999998224 ) ) ;
#23616=CARTESIAN_POINT ( 'NONE',  ( -3.042071309553173730, 109.3229166632526983, 11.35316468749999785 ) ) ;
#23617=ORIENTED_EDGE ( 'NONE', *, *, #12959, .F. ) ;
#23618=( BOUNDED_CURVE ( )  B_SPLINE_CURVE ( 2, ( #14159, #25480, #36822, #7782, #43209, #48497, #60567, #30787, #31151, #65849, #37192, #71133, #31530 ),
 .UNSPECIFIED., .F., .F. ) 
 B_SPLINE_CURVE_WITH_KNOTS ( ( 3, 2, 2, 2, 2, 2, 3 ),
 ( 0.4945652173913043237, 0.4963768115942028825, 0.4981884057971014412, 0.5000000000000000000, 0.5018115942028985588, 0.5036231884057971175, 0.5054347826086956763 ),
 .UNSPECIFIED. ) 
 CURVE ( )  GEOMETRIC_REPRESENTATION_ITEM ( )  RATIONAL_B_SPLINE_CURVE ( ( 1.000000000000000000, 0.9659258262890683122, 1.000000000000000000, 0.9659258262890683122, 1.000000000000000000, 0.9659258262890683122, 1.000000000000000000, 0.9659258262890683122, 1.000000000000000000, 0.9659258262890683122, 1.000000000000000000, 0.9659258262890683122, 1.000000000000000000 ) ) 
 REPRESENTATION_ITEM ( '' )  );
#23623=CARTESIAN_POINT ( 'NONE',  ( -11.35316468749999785, 118.0729166632526983, -3.042071309553167513 ) ) ;
#23624=VERTEX_POINT ( 'NONE', #68795 ) ;
#23629=CARTESIAN_POINT ( 'NONE',  ( -10.00000000000000178, 224.3749999931720254, -1.224646799147353454E-15 ) ) ;
#23633=CARTESIAN_POINT ( 'NONE',  ( -9.832129032723418760, 102.8645833299193697, -5.676582343750004256 ) ) ;
#23637=CARTESIAN_POINT ( 'NONE',  ( 5.000000000000046185, 175.8333333333333997, -8.660254037844465458 ) ) ;
#23640=CARTESIAN_POINT ( 'NONE',  ( 8.660254037844385522, 191.4583333265053966, 5.000000000000005329 ) ) ;
#23643=CARTESIAN_POINT ( 'NONE',  ( -3.042071309553173730, 94.63541666325268409, 11.35316468749999785 ) ) ;
#23647=CARTESIAN_POINT ( 'NONE',  ( -8.311093377946841443, 14.21874999658601979, 8.311093377946830785 ) ) ;
#23651=CARTESIAN_POINT ( 'NONE',  ( 9.832129032723416984, 215.3645833299193555, 5.676582343750006032 ) ) ;
#23654=CARTESIAN_POINT ( 'NONE',  ( -2.679491924311152573, 98.33333332650535397, -10.00000000000004619 ) ) ;
#23655=CARTESIAN_POINT ( 'NONE',  ( -6.676582343750000703, 298.5156250017070079, 2.765530957082001251 ) ) ;
#23659=CARTESIAN_POINT ( 'NONE',  ( -11.35316468749999785, 213.3854166632526983, -3.042071309553167957 ) ) ;
#23667=CARTESIAN_POINT ( 'NONE',  ( 4.999999999999993783, 34.16666666666667140, 8.660254037844390851 ) ) ;
#23677=CARTESIAN_POINT ( 'NONE',  ( 4.721056650416000089, 296.8281250017069510, 4.721056650415999201 ) ) ;
#23685=CARTESIAN_POINT ( 'NONE',  ( -9.832129032723420536, 84.01041666325268409, 5.676582343749997150 ) ) ;
#23695=CARTESIAN_POINT ( 'NONE',  ( 11.35316468750000141, 205.7812499965860411, 0.000000000000000000 ) ) ;
#23700=CARTESIAN_POINT ( 'NONE',  ( -2.085542519210945728E-15, 184.8437499965860411, 11.35316468750000141 ) ) ;
#23702=CARTESIAN_POINT ( 'NONE',  ( -10.00000000000000355, 89.58333332650535397, 2.679491924311223183 ) ) ;
#23707=CARTESIAN_POINT ( 'NONE',  ( 11.35316468750000141, 70.78124999658602690, 0.000000000000000000 ) ) ;
#23713=CARTESIAN_POINT ( 'NONE',  ( -3.042071309553173730, 69.32291666325268409, 11.35316468749999785 ) ) ;
#23718=CARTESIAN_POINT ( 'NONE',  ( -11.35316468750000141, 58.48958332991933418, 3.042071309553159963 ) ) ;
#23723=CARTESIAN_POINT ( 'NONE',  ( 7.320508075688771044, 151.2499999931720538, 7.320508075688775484 ) ) ;
#23725=CARTESIAN_POINT ( 'NONE',  ( -10.00000000000000178, 54.37499999317203958, -1.224646799147353454E-15 ) ) ;
#23726=CARTESIAN_POINT ( 'NONE',  ( 11.35316468749999963, 51.30208332991935549, -3.042071309553165293 ) ) ;
#23728=CARTESIAN_POINT ( 'NONE',  ( -3.042071309553173730, 184.3229166632526983, 11.35316468749999785 ) ) ;
#23734=CARTESIAN_POINT ( 'NONE',  ( 11.35316468749999963, 175.9895833299193555, -3.042071309553165293 ) ) ;
#23740=ADVANCED_FACE ( 'NONE', ( #67409 ), #62751, .T. ) ;
#23742=CARTESIAN_POINT ( 'NONE',  ( -2.085542519210945728E-15, 169.8437499965860127, 11.35316468750000141 ) ) ;
#23746=CARTESIAN_POINT ( 'NONE',  ( -3.042071309553173730, 124.6354166632526699, 11.35316468749999785 ) ) ;
#23757=ORIENTED_EDGE ( 'NONE', *, *, #68039, .F. ) ;
#23771=VECTOR ( 'NONE', #70993, 1000.000000000000000 ) ;
#23774=CARTESIAN_POINT ( 'NONE',  ( -6.676582343749999815, 296.6718750017069510, 2.765530957082001251 ) ) ;
#23775=CARTESIAN_POINT ( 'NONE',  ( -4.999999999999998224, 136.6666666666666856, -8.660254037844389075 ) ) ;
#23777=CARTESIAN_POINT ( 'NONE',  ( 4.529167459315944555, 225.9997407208379911, 8.915528146188176351 ) ) ;
#23793=CARTESIAN_POINT ( 'NONE',  ( 9.832129032723420536, 31.19791666325268409, -5.676582343749999815 ) ) ;
#23796=CARTESIAN_POINT ( 'NONE',  ( -5.676582343749998039, 222.7604166632526983, -9.832129032723420536 ) ) ;
#23802=CARTESIAN_POINT ( 'NONE',  ( -5.676582343749998039, 17.44791666325268409, -9.832129032723420536 ) ) ;
#23805=CARTESIAN_POINT ( 'NONE',  ( -2.485281374238947016, 294.8750000034140726, -5.999999999999626965 ) ) ;
#23808=CARTESIAN_POINT ( 'NONE',  ( -2.085542519210945728E-15, 19.53124999658601979, 11.35316468750000141 ) ) ;
#23810=CARTESIAN_POINT ( 'NONE',  ( -8.311093377946841443, 143.9062499965860127, 8.311093377946830785 ) ) ;
#23812=EDGE_CURVE ( 'NONE', #31972, #29110, #20954, .T. ) ;
#23813=CARTESIAN_POINT ( 'NONE',  ( 6.123233995736767268E-16, 113.1249999931720396, -10.00000000000000178 ) ) ;
#23818=CARTESIAN_POINT ( 'NONE',  ( -5.676582343749998039, 7.760416663252684089, -9.832129032723420536 ) ) ;
#23820=CARTESIAN_POINT ( 'NONE',  ( 1.102182119232618108E-15, 289.2500000000000000, 6.000000000000001776 ) ) ;
#23821=CARTESIAN_POINT ( 'NONE',  ( -2.765530957081996810, 298.2656250017068942, -6.676582343750003368 ) ) ;
#23822=CARTESIAN_POINT ( 'NONE',  ( 11.35316468750000141, 145.7812499965860411, 0.000000000000000000 ) ) ;
#23831=CARTESIAN_POINT ( 'NONE',  ( -5.676582343750006032, 84.42708332991935549, 9.832129032723418760 ) ) ;
#23836=ORIENTED_EDGE ( 'NONE', *, *, #59025, .F. ) ;
#23863=CARTESIAN_POINT ( 'NONE',  ( -2.679491924311225848, 96.45833333333331439, -10.00000000000000178 ) ) ;
#23865=CARTESIAN_POINT ( 'NONE',  ( -5.676582343749998039, 67.76041666325268409, -9.832129032723420536 ) ) ;
#23866=CARTESIAN_POINT ( 'NONE',  ( -6.676582343750000703, 298.6718750017070079, 2.765530957082001251 ) ) ;
#23867=EDGE_CURVE ( 'NONE', #12154, #15376, #70117, .T. ) ;
#23868=VERTEX_POINT ( 'NONE', #7286 ) ;
#23877=CARTESIAN_POINT ( 'NONE',  ( -10.00000000000000178, 217.5000000000000284, -1.224646799147353454E-15 ) ) ;
#23880=CARTESIAN_POINT ( 'NONE',  ( 3.042071309553167069, 187.1354166632526983, -11.35316468749999785 ) ) ;
#23883=CYLINDRICAL_SURFACE ( 'NONE', #20179, 10.00000000000000178 ) ;
#23887=CARTESIAN_POINT ( 'NONE',  ( 3.042071309553167069, 42.13541666325267698, -11.35316468749999785 ) ) ;
#23894=CARTESIAN_POINT ( 'NONE',  ( 8.660254037844385522, 71.45833332650538239, 5.000000000000005329 ) ) ;
#23903=CARTESIAN_POINT ( 'NONE',  ( -4.088227598258586603E-16, 296.3593750017070079, -6.676582343750001591 ) ) ;
#23905=CARTESIAN_POINT ( 'NONE',  ( 8.311093377946837890, 156.4062499965860411, -8.311093377946837890 ) ) ;
#23915=CARTESIAN_POINT ( 'NONE',  ( 11.35316468750000141, 126.0937499965860127, 0.000000000000000000 ) ) ;
#23919=CARTESIAN_POINT ( 'NONE',  ( -8.311093377946836114, 47.96874999658601268, -8.311093377946837890 ) ) ;
#23921=FACE_OUTER_BOUND ( 'NONE', #34260, .T. ) ;
#23925=CARTESIAN_POINT ( 'NONE',  ( 6.000000000000001776, 293.5625000034140157, -7.347880794884121708E-16 ) ) ;
#23949=CARTESIAN_POINT ( 'NONE',  ( 10.00000000000000178, 60.20833333333333570, -2.679491924311226736 ) ) ;
#23960=CARTESIAN_POINT ( 'NONE',  ( -7.320508075688773708, 73.74999999317202537, -7.320508075688774596 ) ) ;
#23961=CARTESIAN_POINT ( 'NONE',  ( -7.320508075688778149, 148.1250000000000000, 7.320508075688770155 ) ) ;
#23962=CARTESIAN_POINT ( 'NONE',  ( 7.320508075688774596, 202.4999999931720538, -7.320508075688774596 ) ) ;
#23963=CARTESIAN_POINT ( 'NONE',  ( 7.320508075688774596, 175.6249999999999716, -7.320508075688774596 ) ) ;
#23966=CARTESIAN_POINT ( 'NONE',  ( 3.042071309553159519, 145.0520833299193555, 11.35316468750000141 ) ) ;
#23967=FACE_OUTER_BOUND ( 'NONE', #28429, .T. ) ;
#23973=CARTESIAN_POINT ( 'NONE',  ( 3.655473550591499698, 225.9517612578558783, -9.326890965111893195 ) ) ;
#23977=CARTESIAN_POINT ( 'NONE',  ( 7.320508075688774596, 37.49999999317203248, -7.320508075688774596 ) ) ;
#23984=CARTESIAN_POINT ( 'NONE',  ( -1.836970198721029983E-15, 28.75000000000000000, 10.00000000000000178 ) ) ;
#23985=CARTESIAN_POINT ( 'NONE',  ( -0.6568112349274827233, 225.9999999999999716, 10.00000000000000178 ) ) ;
#23988=CARTESIAN_POINT ( 'NONE',  ( -3.042071309553173730, 114.3229166632526841, 11.35316468749999785 ) ) ;
#23989=VERTEX_POINT ( 'NONE', #8386 ) ;
#23992=CARTESIAN_POINT ( 'NONE',  ( 8.660254037844389075, 227.2916666598387110, -5.000000000000000000 ) ) ;
#23996=CARTESIAN_POINT ( 'NONE',  ( -9.832129032723420536, 93.69791666325269830, 5.676582343749997150 ) ) ;
#23999=CARTESIAN_POINT ( 'NONE',  ( 10.00000000000000178, 170.2083333333333428, -2.679491924311226736 ) ) ;
#24001=CARTESIAN_POINT ( 'NONE',  ( -1.836970198721029983E-15, 195.6249999931720254, 10.00000000000000178 ) ) ;
#24005=CARTESIAN_POINT ( 'NONE',  ( 3.042071309553167513, 92.13541666325266988, -11.35316468749999785 ) ) ;
#24009=CARTESIAN_POINT ( 'NONE',  ( -9.832129032723418760, 8.177083329919350163, -5.676582343750004256 ) ) ;
#24011=CARTESIAN_POINT ( 'NONE',  ( -5.000000000000009770, 138.3333333333333712, 8.660254037844394404 ) ) ;
#24013=CARTESIAN_POINT ( 'NONE',  ( -9.832129032723418760, 217.8645833299193839, -5.676582343750004256 ) ) ;
#24016=CARTESIAN_POINT ( 'NONE',  ( -1.836970198721029983E-15, 150.6249999931720538, 10.00000000000000178 ) ) ;
#24017=CARTESIAN_POINT ( 'NONE',  ( -4.721056650415998313, 292.5781250017069510, 4.721056650416000089 ) ) ;
#24020=CARTESIAN_POINT ( 'NONE',  ( -8.311093377946836114, 202.9687499965860411, -8.311093377946837890 ) ) ;
#24028=CARTESIAN_POINT ( 'NONE',  ( 5.000000000000001776, 30.83333333333333570, -8.660254037844389075 ) ) ;
#24031=( BOUNDED_CURVE ( )  B_SPLINE_CURVE ( 2, ( #60052, #19689, #43069, #18958, #42698, #8756, #66085, #14395, #65347, #55165, #8006, #25343, #41962 ),
 .UNSPECIFIED., .F., .F. ) 
 B_SPLINE_CURVE_WITH_KNOTS ( ( 3, 2, 2, 2, 2, 2, 3 ),
 ( 0.8206521739130434590, 0.8224637681159420177, 0.8242753623188405765, 0.8260869565217391353, 0.8278985507246376940, 0.8297101449275362528, 0.8315217391304348116 ),
 .UNSPECIFIED. ) 
 CURVE ( )  GEOMETRIC_REPRESENTATION_ITEM ( )  RATIONAL_B_SPLINE_CURVE ( ( 1.000000000000000000, 0.9659258262890683122, 1.000000000000000000, 0.9659258262890683122, 1.000000000000000000, 0.9659258262890683122, 1.000000000000000000, 0.9659258262890683122, 1.000000000000000000, 0.9659258262890683122, 1.000000000000000000, 0.9659258262890683122, 1.000000000000000000 ) ) 
 REPRESENTATION_ITEM ( '' )  );
#24032=ORIENTED_EDGE ( 'NONE', *, *, #18262, .T. ) ;
#24035=EDGE_CURVE ( 'NONE', #29411, #27622, #37064, .T. ) ;
#24039=CARTESIAN_POINT ( 'NONE',  ( -2.765530957081998142, 295.6406250017068942, 6.676582343750000703 ) ) ;
#24048=CARTESIAN_POINT ( 'NONE',  ( -9.832129032723420536, 99.01041666325269830, 5.676582343749997150 ) ) ;
#24058=CARTESIAN_POINT ( 'NONE',  ( 9.832129032723416984, 210.3645833299193555, 5.676582343750006032 ) ) ;
#24062=CARTESIAN_POINT ( 'NONE',  ( -11.35316468750000141, 183.5937499965860411, -1.390361679473963753E-15 ) ) ;
#24069=CARTESIAN_POINT ( 'NONE',  ( 11.35316468749999785, 70.57291666325269830, 3.042071309553174174 ) ) ;
#24073=CARTESIAN_POINT ( 'NONE',  ( -7.320508075688796801, 48.12500000000000711, 7.320508075688789695 ) ) ;
#24075=CARTESIAN_POINT ( 'NONE',  ( 9.832129032723420536, 81.19791666325269830, -5.676582343749999815 ) ) ;
#24080=CARTESIAN_POINT ( 'NONE',  ( -11.35316468749999785, 63.07291666325268409, -3.042071309553167957 ) ) ;
#24084=CARTESIAN_POINT ( 'NONE',  ( 2.679491924311222739, 150.8333333265053682, 10.00000000000000355 ) ) ;
#24086=CARTESIAN_POINT ( 'NONE',  ( 7.320508075688777261, 19.37500000000000000, 7.320508075688779925 ) ) ;
#24087=CARTESIAN_POINT ( 'NONE',  ( -9.832129032723418760, 53.17708332991935549, -5.676582343750004256 ) ) ;
#24089=CARTESIAN_POINT ( 'NONE',  ( 8.311093377946834337, 195.1562499965860411, 8.311093377946839666 ) ) ;
#24095=CARTESIAN_POINT ( 'NONE',  ( 3.042071309553167513, 176.8229166632526699, -11.35316468749999785 ) ) ;
#24100=CARTESIAN_POINT ( 'NONE',  ( -11.35316468749999785, 173.3854166632526983, -3.042071309553167957 ) ) ;
#24101=VECTOR ( 'NONE', #50674, 1000.000000000000000 ) ;
#24103=CARTESIAN_POINT ( 'NONE',  ( -9.832129032723420536, 134.0104166632526983, 5.676582343749997150 ) ) ;
#24113=CARTESIAN_POINT ( 'NONE',  ( -2.679491924311088624, 188.5416666666666856, 10.00000000000008704 ) ) ;
#24114=EDGE_CURVE ( 'NONE', #56133, #3444, #3110, .T. ) ;
#24116=CARTESIAN_POINT ( 'NONE',  ( -8.660254037844438812, 177.9166666666666856, 5.000000000000024869 ) ) ;
#24131=FACE_OUTER_BOUND ( 'NONE', #28371, .T. ) ;
#24133=CARTESIAN_POINT ( 'NONE',  ( 4.721056650415999201, 297.2343750017069510, -4.721056650415999201 ) ) ;
#24134=CARTESIAN_POINT ( 'NONE',  ( -5.000000000000005329, 133.3333333333333428, 8.660254037844387298 ) ) ;
#24149=CARTESIAN_POINT ( 'NONE',  ( 4.999999999999993783, 51.04166665983870388, 8.660254037844390851 ) ) ;
#24151=CARTESIAN_POINT ( 'NONE',  ( -3.042071309553164404, 32.23958332991936260, -11.35316468749999963 ) ) ;
#24152=CARTESIAN_POINT ( 'NONE',  ( 10.00000000000032863, 24.79166666666685614, 2.679491924311323547 ) ) ;
#24153=CARTESIAN_POINT ( 'NONE',  ( -8.311093377946841443, 224.2187499965860411, 8.311093377946830785 ) ) ;
#24161=CARTESIAN_POINT ( 'NONE',  ( -3.042071309553173730, 29.32291666325268764, 11.35316468749999785 ) ) ;
#24167=CARTESIAN_POINT ( 'NONE',  ( -5.676582343750006032, 14.11458332991935016, 9.832129032723418760 ) ) ;
#24169=CARTESIAN_POINT ( 'NONE',  ( 3.042071309553159519, 149.7395833299192986, 11.35316468750000141 ) ) ;
#24171=CARTESIAN_POINT ( 'NONE',  ( 8.660254037844389075, 122.2916666598387110, -5.000000000000000000 ) ) ;
#24174=CARTESIAN_POINT ( 'NONE',  ( 6.123233995736767268E-16, 173.1249999931720538, -10.00000000000000178 ) ) ;
#24177=CARTESIAN_POINT ( 'NONE',  ( 6.951808397369818766E-16, 7.343749996586017126, -11.35316468750000141 ) ) ;
#24179=DIRECTION ( 'NONE',  ( -0.000000000000000000, 1.000000000000000000, -0.000000000000000000 ) ) ;
#24180=CARTESIAN_POINT ( 'NONE',  ( 6.676582343750001591, 296.9531250017069510, -8.176455196517173205E-16 ) ) ;
#24182=CARTESIAN_POINT ( 'NONE',  ( -3.042071309553163960, 142.2395833299193839, -11.35316468749999963 ) ) ;
#24190=CARTESIAN_POINT ( 'NONE',  ( -10.00000000000000355, 204.5833333265053966, 2.679491924311223183 ) ) ;
#24192=CARTESIAN_POINT ( 'NONE',  ( -2.085542519210945728E-15, 89.84374999658602690, 11.35316468750000141 ) ) ;
#24195=ORIENTED_EDGE ( 'NONE', *, *, #51625, .F. ) ;
#24202=ADVANCED_FACE ( 'NONE', ( #20063 ), #9525, .T. ) ;
#24211=FACE_OUTER_BOUND ( 'NONE', #70595, .T. ) ;
#24215=VERTEX_POINT ( 'NONE', #38571 ) ;
#24219=CARTESIAN_POINT ( 'NONE',  ( 1.110124581937998163E-11, 98.75000000000088107, 10.00000000000000533 ) ) ;
#24223=CARTESIAN_POINT ( 'NONE',  ( 10.00000000000000178, 100.0000000000000000, 0.000000000000000000 ) ) ;
#24225=CARTESIAN_POINT ( 'NONE',  ( -5.676582343749998039, 62.76041666325269119, -9.832129032723420536 ) ) ;
#24226=CARTESIAN_POINT ( 'NONE',  ( 6.676582343750001591, 295.1093750017069510, -8.176455196517173205E-16 ) ) ;
#24232=CARTESIAN_POINT ( 'NONE',  ( -4.999999999999998224, 103.5416666598386968, -8.660254037844389075 ) ) ;
#24235=CARTESIAN_POINT ( 'NONE',  ( -4.242640687119286547, 292.8750000000000000, -4.242640687119286547 ) ) ;
#24237=CARTESIAN_POINT ( 'NONE',  ( -10.00000000000000355, 217.7083333333333428, 2.679491924311223183 ) ) ;
#24240=CARTESIAN_POINT ( 'NONE',  ( 11.35316468750000141, 176.0937499965860411, 0.000000000000000000 ) ) ;
#24248=CARTESIAN_POINT ( 'NONE',  ( 11.35316468750000141, 41.09374999658601979, 0.000000000000000000 ) ) ;
#24250=CARTESIAN_POINT ( 'NONE',  ( 5.676582343750001591, 226.9270833299193839, -9.832129032723420536 ) ) ;
#24252=CARTESIAN_POINT ( 'NONE',  ( 5.000000000000002665, 10.83333333333333570, -8.660254037844389075 ) ) ;
#24256=CARTESIAN_POINT ( 'NONE',  ( -5.000000000000005329, 75.20833332650536818, 8.660254037844387298 ) ) ;
#24260=DIRECTION ( 'NONE',  ( -0.000000000000000000, 1.000000000000000000, -0.000000000000000000 ) ) ;
#24266=CARTESIAN_POINT ( 'NONE',  ( -2.765530957081996810, 299.4218750017070079, -6.676582343750003368 ) ) ;
#24268=CARTESIAN_POINT ( 'NONE',  ( -5.000000000000002665, 16.66666666666667140, -8.660254037844394404 ) ) ;
#24269=CARTESIAN_POINT ( 'NONE',  ( 3.042071309553159519, 149.7395833299192986, 11.35316468750000141 ) ) ;
#24271=CARTESIAN_POINT ( 'NONE',  ( 8.660254037844389075, 5.416666666666666963, -5.000000000000000888 ) ) ;
#24279=CARTESIAN_POINT ( 'NONE',  ( -9.832129032723418760, 143.1770833299193555, -5.676582343750004256 ) ) ;
#24284=CARTESIAN_POINT ( 'NONE',  ( -9.832129032723418760, 48.17708332991934839, -5.676582343750004256 ) ) ;
#24286=CARTESIAN_POINT ( 'NONE',  ( -10.00000000000001066, 27.70833333333333570, 2.679491924311224960 ) ) ;
#24290=EDGE_CURVE ( 'NONE', #48426, #67846, #16666, .T. ) ;
#24292=CARTESIAN_POINT ( 'NONE',  ( -6.000000000000001776, 291.0625000034140157, 0.000000000000000000 ) ) ;
#24308=DIRECTION ( 'NONE',  ( 0.000000000000000000, 0.000000000000000000, 1.000000000000000000 ) ) ;
#24317=CARTESIAN_POINT ( 'NONE',  ( -2.679491924311235618, 48.54166666666665719, 10.00000000000000000 ) ) ;
#24319=CARTESIAN_POINT ( 'NONE',  ( -6.000000000000001776, 295.0000000000000000, 0.000000000000000000 ) ) ;
#24325=CARTESIAN_POINT ( 'NONE',  ( 8.660254037844374864, 90.41666666666665719, -4.999999999999992006 ) ) ;
#24330=CARTESIAN_POINT ( 'NONE',  ( -4.999999999999998224, 171.6666666666666856, -8.660254037844389075 ) ) ;
#24331=FACE_OUTER_BOUND ( 'NONE', #1936, .T. ) ;
#24332=ADVANCED_FACE ( 'NONE', ( #50241 ), #21567, .T. ) ;
#24335=CARTESIAN_POINT ( 'NONE',  ( -8.311093377946836114, 142.9687499965859843, -8.311093377946837890 ) ) ;
#24339=CARTESIAN_POINT ( 'NONE',  ( 4.999999999999993783, 106.0416666598387110, 8.660254037844390851 ) ) ;
#24343=CARTESIAN_POINT ( 'NONE',  ( 9.832129032723420536, 1.510416663252683422, -5.676582343749999815 ) ) ;
#24348=CARTESIAN_POINT ( 'NONE',  ( 6.123233995736767268E-16, 33.12499999317203248, -10.00000000000000178 ) ) ;
#24360=AXIS2_PLACEMENT_3D ( 'NONE', #66772, #32834, #38856 ) ;
#24361=CARTESIAN_POINT ( 'NONE',  ( 11.35316468750000141, 110.7812499965860269, 0.000000000000000000 ) ) ;
#24365=CARTESIAN_POINT ( 'NONE',  ( 10.00000000000000178, 227.0833333265053682, -2.679491924311226736 ) ) ;
#24369=CARTESIAN_POINT ( 'NONE',  ( -3.042071309553173730, 109.3229166632526983, 11.35316468749999785 ) ) ;
#24372=CARTESIAN_POINT ( 'NONE',  ( 7.320508075688778149, 50.62500000000000000, -7.320508075688778149 ) ) ;
#24376=CARTESIAN_POINT ( 'NONE',  ( -8.660254037844390851, 199.7916666598387110, 4.999999999999998224 ) ) ;
#24379=CARTESIAN_POINT ( 'NONE',  ( 11.35316468749999963, 96.30208332991935549, -3.042071309553165293 ) ) ;
#24383=CARTESIAN_POINT ( 'NONE',  ( -11.35316468749999785, 8.385416663252684089, -3.042071309553167513 ) ) ;
#24390=CARTESIAN_POINT ( 'NONE',  ( 10.00000000000000178, 200.0000000000000000, 0.000000000000000000 ) ) ;
#24391=CARTESIAN_POINT ( 'NONE',  ( -6.676582343750001591, 293.4531250017069510, 0.000000000000000000 ) ) ;
#24392=CARTESIAN_POINT ( 'NONE',  ( -2.679491924311235174, 120.4166666598386826, 10.00000000000000000 ) ) ;
#24393=CARTESIAN_POINT ( 'NONE',  ( -8.311093377946841443, 204.2187499965859843, 8.311093377946834337 ) ) ;
#24395=( BOUNDED_CURVE ( )  B_SPLINE_CURVE ( 2, ( #65823, #42069, #65458, #31505, #53040, #54152, #65077, #41713, #7387 ),
 .UNSPECIFIED., .F., .F. ) 
 B_SPLINE_CURVE_WITH_KNOTS ( ( 3, 2, 2, 2, 3 ),
 ( 0.5208333333333314830, 0.5312499999999981126, 0.5416666666666647423, 0.5520833333333314830, 0.5624999999999981126 ),
 .UNSPECIFIED. ) 
 CURVE ( )  GEOMETRIC_REPRESENTATION_ITEM ( )  RATIONAL_B_SPLINE_CURVE ( ( 1.000000000000013767, 0.9238795325112729717, 1.000000000000000000, 0.9238795325112867385, 1.000000000000000000, 0.9238795325112867385, 1.000000000000000000, 0.9238795325113005052, 0.9999999999999862332 ) ) 
 REPRESENTATION_ITEM ( '' )  );
#24403=CARTESIAN_POINT ( 'NONE',  ( 7.320508075688771044, 29.37500000000000000, 7.320508075688775484 ) ) ;
#24414=CARTESIAN_POINT ( 'NONE',  ( 4.721056650415999201, 295.0781250017069510, -4.721056650415999201 ) ) ;
#24423=CARTESIAN_POINT ( 'NONE',  ( 6.951808397369818766E-16, 97.34374999658601268, -11.35316468750000141 ) ) ;
#24432=CARTESIAN_POINT ( 'NONE',  ( -8.660254037844390851, 179.7916666598387110, 4.999999999999998224 ) ) ;
#24433=CARTESIAN_POINT ( 'NONE',  ( -11.35316468749999785, 208.0729166632526983, -3.042071309553167513 ) ) ;
#24437=CARTESIAN_POINT ( 'NONE',  ( 11.35316468749999785, 175.8854166632527267, 3.042071309553174174 ) ) ;
#24439=CARTESIAN_POINT ( 'NONE',  ( 0.000000000000000000, 300.0000000000000000, 10.00000000000000178 ) ) ;
#24444=CARTESIAN_POINT ( 'NONE',  ( 9.832129032723420536, 66.19791666325268409, -5.676582343749999815 ) ) ;
#24450=CARTESIAN_POINT ( 'NONE',  ( -2.085542519210945728E-15, 74.53124999658602690, 11.35316468750000141 ) ) ;
#24455=CARTESIAN_POINT ( 'NONE',  ( -3.042071309553173730, 69.32291666325268409, 11.35316468749999785 ) ) ;
#24459=EDGE_CURVE ( 'NONE', #26622, #48555, #55197, .T. ) ;
#24460=CARTESIAN_POINT ( 'NONE',  ( 4.999999999999993783, 161.0416666598387110, 8.660254037844390851 ) ) ;
#24462=FACE_OUTER_BOUND ( 'NONE', #8761, .T. ) ;
#24463=CARTESIAN_POINT ( 'NONE',  ( 11.35316468749999963, 66.30208332991935549, -3.042071309553165293 ) ) ;
#24465=CARTESIAN_POINT ( 'NONE',  ( 8.311093377946834337, 190.1562499965860127, 8.311093377946839666 ) ) ;
#24471=CARTESIAN_POINT ( 'NONE',  ( -11.35316468750000141, 173.4895833299193839, 3.042071309553159963 ) ) ;
#24476=CARTESIAN_POINT ( 'NONE',  ( 0.000000000000000000, 300.0000000000000000, 0.000000000000000000 ) ) ;
#24478=CARTESIAN_POINT ( 'NONE',  ( -2.085542519210945728E-15, 174.8437499965860411, 11.35316468750000141 ) ) ;
#24481=CARTESIAN_POINT ( 'NONE',  ( 7.128595191980942047, 226.0000000000000000, -7.835617972993563995 ) ) ;
#24487=( BOUNDED_CURVE ( )  B_SPLINE_CURVE ( 2, ( #42702, #14019, #3475, #31771, #54790, #38564, #49866, #66089, #37433 ),
 .UNSPECIFIED., .F., .F. ) 
 B_SPLINE_CURVE_WITH_KNOTS ( ( 3, 2, 2, 2, 3 ),
 ( 0.1874999999999978351, 0.1979166666666645202, 0.2083333333333312054, 0.2187499999999978906, 0.2291666666666645480 ),
 .UNSPECIFIED. ) 
 CURVE ( )  GEOMETRIC_REPRESENTATION_ITEM ( )  RATIONAL_B_SPLINE_CURVE ( ( 1.000000000000015765, 0.9238795325112709733, 1.000000000000000000, 0.9238795325112867385, 1.000000000000000000, 0.9238795325112867385, 1.000000000000000000, 0.9238795325113021706, 0.9999999999999845679 ) ) 
 REPRESENTATION_ITEM ( '' )  );
#24492=ORIENTED_EDGE ( 'NONE', *, *, #23867, .F. ) ;
#24495=CARTESIAN_POINT ( 'NONE',  ( 2.250000000000000000, 300.0000000000000000, 7.677076266392047543 ) ) ;
#24505=CARTESIAN_POINT ( 'NONE',  ( -4.999999999999998224, 113.5416666598387110, -8.660254037844389075 ) ) ;
#24509=CARTESIAN_POINT ( 'NONE',  ( -2.679491924309764350, 128.5416666666667993, 10.00000000000085620 ) ) ;
#24510=CARTESIAN_POINT ( 'NONE',  ( -7.320508075688778149, 133.1249999999999716, 7.320508075688769267 ) ) ;
#24524=CARTESIAN_POINT ( 'NONE',  ( 9.832129032723420536, 26.19791666325268409, -5.676582343749999815 ) ) ;
#24526=CARTESIAN_POINT ( 'NONE',  ( -11.35316468749999785, 223.3854166632526699, -3.042071309553167513 ) ) ;
#24530=CARTESIAN_POINT ( 'NONE',  ( -4.999999999999998224, 128.5416666598387110, -8.660254037844389075 ) ) ;
#24532=CARTESIAN_POINT ( 'NONE',  ( -11.35316468749999785, 38.07291666325268409, -3.042071309553167513 ) ) ;
#24536=CARTESIAN_POINT ( 'NONE',  ( 0.000000000000000000, 300.0000000000000000, 0.000000000000000000 ) ) ;
#24538=CARTESIAN_POINT ( 'NONE',  ( -11.35316468750000141, 23.28124999658601979, -1.390361679473963753E-15 ) ) ;
#24540=CARTESIAN_POINT ( 'NONE',  ( 8.311093377946837890, 151.4062499965859843, -8.311093377946837890 ) ) ;
#24541=CARTESIAN_POINT ( 'NONE',  ( -7.320508075688778149, 109.9999999931720396, 7.320508075688769267 ) ) ;
#24548=CARTESIAN_POINT ( 'NONE',  ( 6.951808397369818766E-16, 2.343749996586016682, -11.35316468750000141 ) ) ;
#24550=CARTESIAN_POINT ( 'NONE',  ( -3.673940397442060854E-16, 289.7500000000000000, -6.000000000000001776 ) ) ;
#24551=DIRECTION ( 'NONE',  ( -0.000000000000000000, 1.000000000000000000, -0.000000000000000000 ) ) ;
#24552=CARTESIAN_POINT ( 'NONE',  ( 11.35316468750000141, 135.7812499965860411, 0.000000000000000000 ) ) ;
#24562=CARTESIAN_POINT ( 'NONE',  ( -11.35316468750000141, 88.80208332991935549, 3.042071309553159963 ) ) ;
#24583=CARTESIAN_POINT ( 'NONE',  ( -8.660254037844675068, 22.91666666666685970, 5.000000000000163425 ) ) ;
#24590=CARTESIAN_POINT ( 'NONE',  ( -7.320508075688764826, 96.87499999999997158, -7.320508075688765715 ) ) ;
#24594=CARTESIAN_POINT ( 'NONE',  ( -7.320508075688778149, 88.12500000000001421, 7.320508075688769267 ) ) ;
#24596=CARTESIAN_POINT ( 'NONE',  ( -2.765530957081998586, 294.7968750017069510, 6.676582343750001591 ) ) ;
#24598=DIRECTION ( 'NONE',  ( -0.000000000000000000, 1.000000000000000000, -0.000000000000000000 ) ) ;
#24601=CARTESIAN_POINT ( 'NONE',  ( 0.000000000000000000, 237.9999999999999716, 15.99999999999998579 ) ) ;
#24605=CARTESIAN_POINT ( 'NONE',  ( -4.999999999999998224, 216.6666666666666856, -8.660254037844389075 ) ) ;
#24607=CARTESIAN_POINT ( 'NONE',  ( -3.042071309553164404, 182.5520833299193271, -11.35316468749999963 ) ) ;
#24615=CARTESIAN_POINT ( 'NONE',  ( 5.676582343749993598, 45.26041666325268409, 9.832129032723422313 ) ) ;
#24617=CARTESIAN_POINT ( 'NONE',  ( -11.35316468750000141, 218.8020833299193271, 3.042071309553159963 ) ) ;
#24619=CARTESIAN_POINT ( 'NONE',  ( 10.00000000000000000, 9.791666666666667851, 2.679491924311236062 ) ) ;
#24623=CARTESIAN_POINT ( 'NONE',  ( -10.00000000000000355, 74.58333332650533976, 2.679491924311223183 ) ) ;
#24631=CARTESIAN_POINT ( 'NONE',  ( 2.765530957081996366, 298.2968750017069510, -6.676582343750003368 ) ) ;
#24634=CARTESIAN_POINT ( 'NONE',  ( 3.042071309553167069, 161.8229166632526983, -11.35316468749999785 ) ) ;
#24640=EDGE_CURVE ( 'NONE', #40340, #38960, #1907, .T. ) ;
#24643=CARTESIAN_POINT ( 'NONE',  ( 3.042071309553167513, 147.1354166632526983, -11.35316468749999785 ) ) ;
#24647=CARTESIAN_POINT ( 'NONE',  ( 8.311093377946834337, 45.46874999658601268, 8.311093377946839666 ) ) ;
#24653=CARTESIAN_POINT ( 'NONE',  ( 2.485281374238571317, 291.7500000034140726, -6.000000000000003553 ) ) ;
#24658=EDGE_CURVE ( 'NONE', #61990, #48362, #47544, .T. ) ;
#24660=CARTESIAN_POINT ( 'NONE',  ( -1.538508811358849613E-11, 71.25000000000120792, -10.00000000000000178 ) ) ;
#24662=VERTEX_POINT ( 'NONE', #19243 ) ;
#24668=EDGE_CURVE ( 'NONE', #19863, #51786, #63791, .T. ) ;
#24671=VERTEX_POINT ( 'NONE', #13571 ) ;
#24677=CARTESIAN_POINT ( 'NONE',  ( 10.00000000000000000, 54.79166666666665719, 2.679491924311236062 ) ) ;
#24679=CARTESIAN_POINT ( 'NONE',  ( -6.000000000000003553, 297.9375000000000000, -2.485281374238571317 ) ) ;
#24691=CARTESIAN_POINT ( 'NONE',  ( 7.320508075688771044, 174.3749999999999716, 7.320508075688775484 ) ) ;
#24692=CARTESIAN_POINT ( 'NONE',  ( 2.250000000000000000, 300.0000000000000000, 7.677076266392047543 ) ) ;
#24695=CARTESIAN_POINT ( 'NONE',  ( 6.951808397369818766E-16, 147.3437499965860411, -11.35316468750000141 ) ) ;
#24703=CARTESIAN_POINT ( 'NONE',  ( -11.35316468750000141, 3.802083329919349275, 3.042071309553159963 ) ) ;
#24708=CARTESIAN_POINT ( 'NONE',  ( 10.00000000000000178, 32.08333332650536107, -2.679491924311226736 ) ) ;
#24716=ADVANCED_FACE ( 'NONE', ( #29840 ), #70209, .T. ) ;
#24720=CARTESIAN_POINT ( 'NONE',  ( -11.35316468750000141, 113.2812499965860269, -1.390361679473963753E-15 ) ) ;
#24726=CYLINDRICAL_SURFACE ( 'NONE', #28105, 10.00000000000000178 ) ;
#24727=CARTESIAN_POINT ( 'NONE',  ( 0.5249639094239428871, 225.9999999999999716, -9.999968502165486939 ) ) ;
#24728=CARTESIAN_POINT ( 'NONE',  ( 11.35316468750000141, 110.7812499965860269, 0.000000000000000000 ) ) ;
#24730=CARTESIAN_POINT ( 'NONE',  ( 10.00000000000000178, 81.87499999317203958, 0.000000000000000000 ) ) ;
#24733=CARTESIAN_POINT ( 'NONE',  ( 6.123233995736767268E-16, 208.1249999931720538, -10.00000000000000178 ) ) ;
#24736=CARTESIAN_POINT ( 'NONE',  ( -9.832129032723420536, 99.01041666325269830, 5.676582343749997150 ) ) ;
#24740=CARTESIAN_POINT ( 'NONE',  ( -3.042071309553173730, 9.635416663252682312, 11.35316468749999785 ) ) ;
#24742=CYLINDRICAL_SURFACE ( 'NONE', #42835, 6.000000000000001776 ) ;
#24748=CARTESIAN_POINT ( 'NONE',  ( 2.765530957081996366, 291.1406250017069510, -6.676582343750003368 ) ) ;
#24749=AXIS2_PLACEMENT_3D ( 'NONE', #15080, #2658, #37362 ) ;
#24751=CARTESIAN_POINT ( 'NONE',  ( -11.35316468749999785, 223.3854166632526699, -3.042071309553167957 ) ) ;
#24754=VECTOR ( 'NONE', #8436, 1000.000000000000000 ) ;
#24769=CARTESIAN_POINT ( 'NONE',  ( 1.377000000000000002, 267.1439999999997212, 5.668134320359001777 ) ) ;
#24770=CARTESIAN_POINT ( 'NONE',  ( -6.676582343750001591, 291.4531250017069510, 0.000000000000000000 ) ) ;
#24777=ORIENTED_EDGE ( 'NONE', *, *, #16701, .T. ) ;
#24779=CARTESIAN_POINT ( 'NONE',  ( 9.832129032723416984, 105.6770833299193413, 5.676582343750006032 ) ) ;
#24780=CARTESIAN_POINT ( 'NONE',  ( -7.320508075688771932, 121.8750000000000142, -7.320508075688772820 ) ) ;
#24790=CARTESIAN_POINT ( 'NONE',  ( -8.311093377946841443, 218.9062499965860127, 8.311093377946830785 ) ) ;
#24795=CARTESIAN_POINT ( 'NONE',  ( -3.042071309553173730, 194.6354166632526415, 11.35316468749999785 ) ) ;
#24801=CARTESIAN_POINT ( 'NONE',  ( 3.042071309553167069, 71.82291666325269830, -11.35316468749999785 ) ) ;
#24806=CARTESIAN_POINT ( 'NONE',  ( -7.320508075688792360, 46.87500000000001421, -7.320508075688793248 ) ) ;
#24808=CARTESIAN_POINT ( 'NONE',  ( -9.832129032723420536, 78.69791666325269830, 5.676582343749997150 ) ) ;
#24815=CARTESIAN_POINT ( 'NONE',  ( -3.042071309553163960, 72.23958332991935549, -11.35316468749999963 ) ) ;
#24817=CARTESIAN_POINT ( 'NONE',  ( 10.00000000000000000, 129.7916666666666572, 2.679491924311235618 ) ) ;
#24820=CARTESIAN_POINT ( 'NONE',  ( -4.999999999999998224, 163.5416666598387110, -8.660254037844389075 ) ) ;
#24823=CARTESIAN_POINT ( 'NONE',  ( 11.35316468750000141, 56.09374999658601979, 0.000000000000000000 ) ) ;
#24825=CARTESIAN_POINT ( 'NONE',  ( 5.676582343750001591, 201.6145833299193555, -9.832129032723420536 ) ) ;
#24830=CARTESIAN_POINT ( 'NONE',  ( -5.676582343749998039, 197.4479166632526983, -9.832129032723420536 ) ) ;
#24835=CARTESIAN_POINT ( 'NONE',  ( -11.35316468750000141, 178.8020833299193555, 3.042071309553159963 ) ) ;
#24840=CARTESIAN_POINT ( 'NONE',  ( 8.660254037844385522, 4.583333333333333037, 5.000000000000005329 ) ) ;
#24842=DIRECTION ( 'NONE',  ( -0.000000000000000000, 1.000000000000000000, -0.000000000000000000 ) ) ;
#24845=CARTESIAN_POINT ( 'NONE',  ( -10.00000000000000711, 187.7083333333333144, 2.679491924311224071 ) ) ;
#24854=CARTESIAN_POINT ( 'NONE',  ( -5.000000000000091482, 156.6666666666667993, -8.660254037844547170 ) ) ;
#24860=CARTESIAN_POINT ( 'NONE',  ( 10.00000000000000000, 91.66666665983869677, 2.679491924311235618 ) ) ;
#24864=CARTESIAN_POINT ( 'NONE',  ( 4.721056650415999201, 293.2343750017069510, -4.721056650415999201 ) ) ;
#24865=CARTESIAN_POINT ( 'NONE',  ( 10.00000000000000000, 139.7916666666666572, 2.679491924311236062 ) ) ;
#24868=CARTESIAN_POINT ( 'NONE',  ( 6.000000000000003553, 290.6250000034140157, -2.485281374238571761 ) ) ;
#24878=CARTESIAN_POINT ( 'NONE',  ( 1.102182119232618108E-15, 288.3125000034140157, 6.000000000000001776 ) ) ;
#24881=CARTESIAN_POINT ( 'NONE',  ( -11.35316468750000141, 28.48958332991934839, 3.042071309553159963 ) ) ;
#24883=CARTESIAN_POINT ( 'NONE',  ( -2.679491924311235618, 5.416666659838698550, 10.00000000000000000 ) ) ;
#24890=CARTESIAN_POINT ( 'NONE',  ( 3.042071309553167069, 41.82291666325269119, -11.35316468749999785 ) ) ;
#24894=CARTESIAN_POINT ( 'NONE',  ( -8.660254037844392627, 152.0833333333333712, -5.000000000000007994 ) ) ;
#24897=CARTESIAN_POINT ( 'NONE',  ( -3.042071309553163960, 32.23958332991934839, -11.35316468749999963 ) ) ;
#24899=CARTESIAN_POINT ( 'NONE',  ( 11.35316468749999963, 150.9895833299193271, -3.042071309553165293 ) ) ;
#24900=CARTESIAN_POINT ( 'NONE',  ( 4.999999999999993783, 111.0416666598387110, 8.660254037844390851 ) ) ;
#24902=CARTESIAN_POINT ( 'NONE',  ( 0.000000000000000000, 300.0000000000000000, 0.000000000000000000 ) ) ;
#24905=CARTESIAN_POINT ( 'NONE',  ( 8.311093377946834337, 15.46874999658601624, 8.311093377946839666 ) ) ;
#24906=( BOUNDED_CURVE ( )  B_SPLINE_CURVE ( 2, ( #70404, #47380, #54539, #14144, #65837, #25468, #24730, #65471, #2845, #19813, #30041, #7769, #71121 ),
 .UNSPECIFIED., .F., .F. ) 
 B_SPLINE_CURVE_WITH_KNOTS ( ( 3, 2, 2, 2, 2, 2, 3 ),
 ( 0.3423913043478260532, 0.3442028985507245564, 0.3460144927536231152, 0.3478260869565217295, 0.3496376811594202882, 0.3514492753623188470, 0.3532608695652174058 ),
 .UNSPECIFIED. ) 
 CURVE ( )  GEOMETRIC_REPRESENTATION_ITEM ( )  RATIONAL_B_SPLINE_CURVE ( ( 1.000000000000001110, 0.9659258262890673130, 1.000000000000000000, 0.9659258262890683122, 1.000000000000000000, 0.9659258262890683122, 1.000000000000000000, 0.9659258262890683122, 1.000000000000000000, 0.9659258262890683122, 1.000000000000000000, 0.9659258262890683122, 1.000000000000000000 ) ) 
 REPRESENTATION_ITEM ( '' )  );
#24909=CARTESIAN_POINT ( 'NONE',  ( 2.485281374238266672, 289.6875000000000568, -6.000000000000306422 ) ) ;
#24911=CARTESIAN_POINT ( 'NONE',  ( 6.951808397369818766E-16, 157.0312499965860127, -11.35316468750000141 ) ) ;
#24921=CARTESIAN_POINT ( 'NONE',  ( -11.35316468750000141, 98.80208332991932707, 3.042071309553159963 ) ) ;
#24937=ORIENTED_EDGE ( 'NONE', *, *, #48129, .T. ) ;
#24943=SHAPE_REPRESENTATION_RELATIONSHIP ( 'NONE' , 'NONE' ,  #43124, #52625 ) ;
#24948=ORIENTED_EDGE ( 'NONE', *, *, #52826, .T. ) ;
#24955=CARTESIAN_POINT ( 'NONE',  ( -10.00000000000000355, 97.70833333333331439, 2.679491924311223183 ) ) ;
#24959=CARTESIAN_POINT ( 'NONE',  ( -6.676582343750000703, 295.6718750017070079, 2.765530957082001251 ) ) ;
#24962=CARTESIAN_POINT ( 'NONE',  ( -1.836970198721029983E-15, 145.6249999931720538, 10.00000000000000178 ) ) ;
#24969=CARTESIAN_POINT ( 'NONE',  ( -10.00000000000000178, 212.5000000000000284, -1.224646799147353454E-15 ) ) ;
#24971=CARTESIAN_POINT ( 'NONE',  ( 3.042071309553159519, 180.0520833299193271, 11.35316468750000141 ) ) ;
#24978=CARTESIAN_POINT ( 'NONE',  ( -11.35316468750000141, 53.59374999658601979, -1.390361679473963753E-15 ) ) ;
#24980=CARTESIAN_POINT ( 'NONE',  ( 5.676582343749993598, 215.2604166632526983, 9.832129032723422313 ) ) ;
#24983=CARTESIAN_POINT ( 'NONE',  ( -1.836970198721029983E-15, 8.750000000000000000, 10.00000000000000178 ) ) ;
#24985=CARTESIAN_POINT ( 'NONE',  ( -1.836970198721029983E-15, 60.62499999317203958, 10.00000000000000178 ) ) ;
#24987=CARTESIAN_POINT ( 'NONE',  ( -11.35316468749999785, 108.0729166632526699, -3.042071309553167513 ) ) ;
#24988=CARTESIAN_POINT ( 'NONE',  ( -10.00000000000000178, 69.37499999317203958, -1.224646799147353454E-15 ) ) ;
#24994=ORIENTED_EDGE ( 'NONE', *, *, #33989, .F. ) ;
#24995=CARTESIAN_POINT ( 'NONE',  ( -4.721056650415999201, 295.4843750017070079, -4.721056650415999201 ) ) ;
#24997=CARTESIAN_POINT ( 'NONE',  ( 8.311093377946834337, 165.1562499965860127, 8.311093377946839666 ) ) ;
#25005=CARTESIAN_POINT ( 'NONE',  ( 8.311093377946834337, 135.4687499965860411, 8.311093377946839666 ) ) ;
#25006=CARTESIAN_POINT ( 'NONE',  ( 1.102182119232618108E-15, 297.3125000034140157, 6.000000000000001776 ) ) ;
#25009=CARTESIAN_POINT ( 'NONE',  ( -9.832129032723420536, 54.01041666325268409, 5.676582343749997150 ) ) ;
#25015=CARTESIAN_POINT ( 'NONE',  ( 6.000000000000001776, 291.5625000034140157, -7.347880794884121708E-16 ) ) ;
#25020=VECTOR ( 'NONE', #20522, 1000.000000000000000 ) ;
#25024=ORIENTED_EDGE ( 'NONE', *, *, #11973, .T. ) ;
#25039=CARTESIAN_POINT ( 'NONE',  ( 4.999999999999993783, 49.16666666666667140, 8.660254037844390851 ) ) ;
#25040=EDGE_CURVE ( 'NONE', #15376, #32224, #39254, .T. ) ;
#25042=CARTESIAN_POINT ( 'NONE',  ( 1.102182119232618108E-15, 295.2500000000000000, 6.000000000000001776 ) ) ;
#25045=CARTESIAN_POINT ( 'NONE',  ( 6.123233995736767268E-16, 78.12499999317202537, -10.00000000000000178 ) ) ;
#25049=CARTESIAN_POINT ( 'NONE',  ( -7.320508075688778149, 74.99999999317202537, 7.320508075688769267 ) ) ;
#25053=CARTESIAN_POINT ( 'NONE',  ( -2.679491924311235618, 168.5416666666666856, 10.00000000000000000 ) ) ;
#25057=CARTESIAN_POINT ( 'NONE',  ( 8.311093377946837890, 146.7187499965860411, -8.311093377946837890 ) ) ;
#25058=PLANE ( 'NONE',  #30044 ) ;
#25065=CARTESIAN_POINT ( 'NONE',  ( -2.085542519210945728E-15, 4.843749996586016238, 11.35316468750000141 ) ) ;
#25073=CARTESIAN_POINT ( 'NONE',  ( -4.999999999999998224, 38.54166665983869677, -8.660254037844389075 ) ) ;
#25080=ORIENTED_EDGE ( 'NONE', *, *, #9436, .F. ) ;
#25081=CARTESIAN_POINT ( 'NONE',  ( 10.00000000000000355, 29.79166666666667140, 2.679491924311236950 ) ) ;
#25085=CARTESIAN_POINT ( 'NONE',  ( 11.35316468749999963, 120.9895833299193413, -3.042071309553165293 ) ) ;
#25094=CARTESIAN_POINT ( 'NONE',  ( -5.676582343750006032, 119.1145833299193697, 9.832129032723418760 ) ) ;
#25098=CARTESIAN_POINT ( 'NONE',  ( -1.836970198721029983E-15, 210.6249999931720538, 10.00000000000000178 ) ) ;
#25102=CARTESIAN_POINT ( 'NONE',  ( -2.085542519210945728E-15, 104.8437499965860269, 11.35316468750000141 ) ) ;
#25106=CARTESIAN_POINT ( 'NONE',  ( -8.311093377946836114, 12.96874999658601446, -8.311093377946837890 ) ) ;
#25113=CARTESIAN_POINT ( 'NONE',  ( 6.123233995736767268E-16, 148.1249999931720538, -10.00000000000000178 ) ) ;
#25114=CARTESIAN_POINT ( 'NONE',  ( -4.721056650415998313, 293.5781250017069510, 4.721056650416000089 ) ) ;
#25116=CARTESIAN_POINT ( 'NONE',  ( -9.832129032723418760, 223.1770833299193555, -5.676582343750004256 ) ) ;
#25136=CARTESIAN_POINT ( 'NONE',  ( 2.295000000000000373, 272.8559999999997672, 5.415579320911188432 ) ) ;
#25137=CARTESIAN_POINT ( 'NONE',  ( 2.765530957081996366, 292.1406250017070647, -6.676582343750002480 ) ) ;
#25148=CARTESIAN_POINT ( 'NONE',  ( -3.673940397442060854E-16, 298.8125000034140157, -6.000000000000001776 ) ) ;
#25150=CARTESIAN_POINT ( 'NONE',  ( -3.042071309553164404, 97.55208332991932707, -11.35316468749999963 ) ) ;
#25159=CARTESIAN_POINT ( 'NONE',  ( -3.042071309553173730, 214.3229166632526983, 11.35316468749999785 ) ) ;
#25164=CARTESIAN_POINT ( 'NONE',  ( -9.832129032723418760, 188.1770833299193555, -5.676582343750004256 ) ) ;
#25170=CARTESIAN_POINT ( 'NONE',  ( 3.042071309553167069, 86.82291666325265567, -11.35316468749999785 ) ) ;
#25178=CARTESIAN_POINT ( 'NONE',  ( 9.832129032723420536, 76.19791666325269830, -5.676582343749999815 ) ) ;
#25181=AXIS2_PLACEMENT_3D ( 'NONE', #29788, #24842, #52798 ) ;
#25186=CARTESIAN_POINT ( 'NONE',  ( -9.832129032723418760, 67.86458332991935549, -5.676582343750004256 ) ) ;
#25189=CARTESIAN_POINT ( 'NONE',  ( 5.000000000000001776, 172.7083333265053682, -8.660254037844389075 ) ) ;
#25192=CARTESIAN_POINT ( 'NONE',  ( 9.832129032723420536, 61.51041666325268409, -5.676582343749999815 ) ) ;
#25195=CARTESIAN_POINT ( 'NONE',  ( -5.676582343750006032, 189.1145833299193839, 9.832129032723418760 ) ) ;
#25196=ORIENTED_EDGE ( 'NONE', *, *, #51847, .F. ) ;
#25201=CARTESIAN_POINT ( 'NONE',  ( -5.676582343750006032, 189.1145833299193839, 9.832129032723418760 ) ) ;
#25206=CARTESIAN_POINT ( 'NONE',  ( 11.35316468750000141, 176.0937499965860411, 0.000000000000000000 ) ) ;
#25208=CARTESIAN_POINT ( 'NONE',  ( 4.796365593505123037, 226.0000000000000284, -9.057459967333279849 ) ) ;
#25212=CARTESIAN_POINT ( 'NONE',  ( 7.320508075688774596, 5.624999999999999112, -7.320508075688774596 ) ) ;
#25236=CARTESIAN_POINT ( 'NONE',  ( 1.226468279477575784E-15, 292.8593750017070079, 6.676582343750001591 ) ) ;
#25237=CARTESIAN_POINT ( 'NONE',  ( 2.679491924311222739, 153.9583333333333428, 10.00000000000000355 ) ) ;
#25239=CARTESIAN_POINT ( 'NONE',  ( -10.00000000000000178, 164.3749999931720254, -1.224646799147353454E-15 ) ) ;
#25254=CARTESIAN_POINT ( 'NONE',  ( -11.35316468750000141, 48.28124999658601979, -1.390361679473963753E-15 ) ) ;
#25256=CARTESIAN_POINT ( 'NONE',  ( 5.000000000000001776, 2.708333326505365957, -8.660254037844389075 ) ) ;
#25258=CARTESIAN_POINT ( 'NONE',  ( 9.999999999999992895, 184.7916666666666572, 2.679491924311234285 ) ) ;
#25262=CARTESIAN_POINT ( 'NONE',  ( -8.311093377946841443, 38.90624999658599847, 8.311093377946830785 ) ) ;
#25268=CARTESIAN_POINT ( 'NONE',  ( 9.832129032723420536, 31.19791666325268409, -5.676582343749999815 ) ) ;
#25270=CARTESIAN_POINT ( 'NONE',  ( -8.311093377946836114, 142.6562499965860127, -8.311093377946837890 ) ) ;
#25272=CARTESIAN_POINT ( 'NONE',  ( -2.679491924311225848, 123.3333333265053540, -10.00000000000000178 ) ) ;
#25276=CARTESIAN_POINT ( 'NONE',  ( 0.000000000000000000, 300.0000000000000000, 6.000000000000001776 ) ) ;
#25277=CARTESIAN_POINT ( 'NONE',  ( 6.951808397369818766E-16, 27.34374999658601979, -11.35316468750000141 ) ) ;
#25279=FACE_OUTER_BOUND ( 'NONE', #32273, .T. ) ;
#25282=CARTESIAN_POINT ( 'NONE',  ( 9.832129032723420536, 151.1979166632526983, -5.676582343749999815 ) ) ;
#25291=CARTESIAN_POINT ( 'NONE',  ( -10.00000000000000178, 204.3749999931720538, -1.224646799147353454E-15 ) ) ;
#25292=CARTESIAN_POINT ( 'NONE',  ( 1.102182119232618108E-15, 292.3125000034140157, 6.000000000000001776 ) ) ;
#25293=CARTESIAN_POINT ( 'NONE',  ( 3.042071309553167069, 107.1354166632526983, -11.35316468749999785 ) ) ;
#25304=CARTESIAN_POINT ( 'NONE',  ( -7.320508075688778149, 159.9999999931720254, 7.320508075688769267 ) ) ;
#25312=CARTESIAN_POINT ( 'NONE',  ( -10.00000000000033396, 22.70833333333352044, 2.679491924311311557 ) ) ;
#25318=ORIENTED_EDGE ( 'NONE', *, *, #66420, .F. ) ;
#25326=CARTESIAN_POINT ( 'NONE',  ( -2.679491924311225848, 101.4583333333333428, -10.00000000000000178 ) ) ;
#25329=CARTESIAN_POINT ( 'NONE',  ( 1.226468279477575784E-15, 295.8593750017070079, 6.676582343750001591 ) ) ;
#25340=CARTESIAN_POINT ( 'NONE',  ( 2.679491924311222739, 218.9583333333333428, 10.00000000000000355 ) ) ;
#25342=CARTESIAN_POINT ( 'NONE',  ( 8.311093377946834337, 190.4687499965860411, 8.311093377946839666 ) ) ;
#25343=CARTESIAN_POINT ( 'NONE',  ( 2.679491924311228956, 192.9166666598387110, -10.00000000000000000 ) ) ;
#25350=CARTESIAN_POINT ( 'NONE',  ( -9.832129032723420536, 49.01041666325269119, 5.676582343749997150 ) ) ;
#25352=CARTESIAN_POINT ( 'NONE',  ( -8.311093377946841443, 224.2187499965860411, 8.311093377946830785 ) ) ;
#25354=CARTESIAN_POINT ( 'NONE',  ( -10.00000000000000000, 124.1666666598387110, -2.679491924311229845 ) ) ;
#25359=CARTESIAN_POINT ( 'NONE',  ( 9.832129032723420536, 111.1979166632526983, -5.676582343749999815 ) ) ;
#25360=CARTESIAN_POINT ( 'NONE',  ( -10.00000000000000178, 84.37499999317203958, -1.224646799147353454E-15 ) ) ;
#25368=CARTESIAN_POINT ( 'NONE',  ( -6.676582343750003368, 295.5468750017069510, -2.765530957081996810 ) ) ;
#25370=CARTESIAN_POINT ( 'NONE',  ( -9.832129032723418760, 172.8645833299193555, -5.676582343750004256 ) ) ;
#25379=CARTESIAN_POINT ( 'NONE',  ( 8.311093377946834337, 140.4687499965859843, 8.311093377946839666 ) ) ;
#25383=CARTESIAN_POINT ( 'NONE',  ( 3.042071309553167069, 67.13541666325266988, -11.35316468749999785 ) ) ;
#25392=CARTESIAN_POINT ( 'NONE',  ( -6.000000000000003553, 294.0000000034140726, -2.485281374238571317 ) ) ;
#25408=CARTESIAN_POINT ( 'NONE',  ( -2.485281374238927032, 294.8125000000000000, -5.999999999999647393 ) ) ;
#25415=CARTESIAN_POINT ( 'NONE',  ( 2.679491924311222739, 58.95833333333332149, 10.00000000000000355 ) ) ;
#25418=CARTESIAN_POINT ( 'NONE',  ( 4.242640687119287435, 296.3750000000000000, 4.242640687119285658 ) ) ;
#25421=ORIENTED_EDGE ( 'NONE', *, *, #7633, .F. ) ;
#25428=CARTESIAN_POINT ( 'NONE',  ( -10.00000000000000355, 177.7083333333333428, 2.679491924311223183 ) ) ;
#25432=CARTESIAN_POINT ( 'NONE',  ( -5.676582343750006032, 154.4270833299193555, 9.832129032723418760 ) ) ;
#25436=CARTESIAN_POINT ( 'NONE',  ( -6.000000000000001776, 294.0000000000000000, 0.000000000000000000 ) ) ;
#25438=CARTESIAN_POINT ( 'NONE',  ( 11.35316468749999785, 15.88541666325268586, 3.042071309553174174 ) ) ;
#25445=CARTESIAN_POINT ( 'NONE',  ( 10.00000000000000178, 37.08333332650536107, -2.679491924311226736 ) ) ;
#25451=DIRECTION ( 'NONE',  ( 0.000000000000000000, 0.000000000000000000, 1.000000000000000000 ) ) ;
#25452=DIRECTION ( 'NONE',  ( -0.000000000000000000, 1.000000000000000000, -0.000000000000000000 ) ) ;
#25458=CARTESIAN_POINT ( 'NONE',  ( 6.951808397369818766E-16, 132.0312499965860127, -11.35316468750000141 ) ) ;
#25459=ORIENTED_EDGE ( 'NONE', *, *, #14309, .T. ) ;
#25460=CARTESIAN_POINT ( 'NONE',  ( 3.090148520752590944, 225.9998984954551418, -9.510618362637927703 ) ) ;
#25466=CARTESIAN_POINT ( 'NONE',  ( -5.676582343749998039, 112.4479166632526983, -9.832129032723420536 ) ) ;
#25468=CARTESIAN_POINT ( 'NONE',  ( 10.00000000000000000, 81.66666665983869677, 2.679491924311235618 ) ) ;
#25472=CARTESIAN_POINT ( 'NONE',  ( 11.35316468750000141, 106.0937499965860269, 0.000000000000000000 ) ) ;
#25476=CARTESIAN_POINT ( 'NONE',  ( -3.042071309553173730, 19.63541666325268764, 11.35316468749999785 ) ) ;
#25477=ORIENTED_EDGE ( 'NONE', *, *, #9942, .F. ) ;
#25480=CARTESIAN_POINT ( 'NONE',  ( 2.679491924311222739, 115.8333333265053682, 10.00000000000000355 ) ) ;
#25485=CARTESIAN_POINT ( 'NONE',  ( -8.660254037844390851, 149.7916666598387110, 4.999999999999998224 ) ) ;
#25486=CARTESIAN_POINT ( 'NONE',  ( -6.676582343750003368, 294.3906250017070079, -2.765530957081996810 ) ) ;
#25488=CARTESIAN_POINT ( 'NONE',  ( 9.832129032723416984, 220.6770833299193555, 5.676582343750006032 ) ) ;
#25489=ADVANCED_FACE ( 'NONE', ( #29672 ), #36446, .T. ) ;
#25490=CARTESIAN_POINT ( 'NONE',  ( -8.311093377946841443, 134.2187499965860411, 8.311093377946830785 ) ) ;
#25501=CARTESIAN_POINT ( 'NONE',  ( -2.679491924311399043, 171.4583333333333428, -10.00000000000001421 ) ) ;
#25503=ORIENTED_EDGE ( 'NONE', *, *, #61971, .T. ) ;
#25508=CARTESIAN_POINT ( 'NONE',  ( 1.377000000000000002, 255.7199999999997715, 5.684453117602858541 ) ) ;
#25509=CARTESIAN_POINT ( 'NONE',  ( 4.721056650415999201, 294.0781250017069510, -4.721056650415999201 ) ) ;
#25514=EDGE_CURVE ( 'NONE', #9276, #22486, #64822, .T. ) ;
#25516=CARTESIAN_POINT ( 'NONE',  ( 7.320508075688771044, 166.2499999931720538, 7.320508075688775484 ) ) ;
#25520=CARTESIAN_POINT ( 'NONE',  ( -6.000000000000001776, 287.5312500017070079, 0.000000000000000000 ) ) ;
#25522=CARTESIAN_POINT ( 'NONE',  ( 5.676582343749993598, 100.2604166632526841, 9.832129032723422313 ) ) ;
#25528=ORIENTED_EDGE ( 'NONE', *, *, #54111, .T. ) ;
#25530=CARTESIAN_POINT ( 'NONE',  ( -9.832129032723420536, 213.6979166632526983, 5.676582343749997150 ) ) ;
#25534=CARTESIAN_POINT ( 'NONE',  ( 8.311093377946834337, 190.4687499965860411, 8.311093377946839666 ) ) ;
#25541=CARTESIAN_POINT ( 'NONE',  ( -9.832129032723418760, 77.86458332991935549, -5.676582343750004256 ) ) ;
#25544=CARTESIAN_POINT ( 'NONE',  ( -1.836970198721029983E-15, 105.6249999931720396, 10.00000000000000178 ) ) ;
#25547=CARTESIAN_POINT ( 'NONE',  ( 9.832129032723420536, 86.19791666325268409, -5.676582343749999815 ) ) ;
#25552=CARTESIAN_POINT ( 'NONE',  ( 10.00000000000003375, 75.20833333333334281, -2.679491924311235618 ) ) ;
#25554=CARTESIAN_POINT ( 'NONE',  ( -9.832129032723420536, 73.69791666325268409, 5.676582343749997150 ) ) ;
#25557=CARTESIAN_POINT ( 'NONE',  ( -10.00000000000000355, 164.5833333265053682, 2.679491924311223183 ) ) ;
#25561=CARTESIAN_POINT ( 'NONE',  ( -3.042071309553163960, 67.55208332991935549, -11.35316468749999963 ) ) ;
#25562=CARTESIAN_POINT ( 'NONE',  ( -6.676582343750000703, 295.5156250017070079, 2.765530957082001251 ) ) ;
#25564=CARTESIAN_POINT ( 'NONE',  ( -8.311093377946836114, 197.6562499965860695, -8.311093377946837890 ) ) ;
#25570=CARTESIAN_POINT ( 'NONE',  ( 9.832129032723416984, 195.3645833299193839, 5.676582343750006032 ) ) ;
#25575=CARTESIAN_POINT ( 'NONE',  ( -11.35316468750000141, 178.5937499965860411, -1.390361679473963753E-15 ) ) ;
#25578=( BOUNDED_CURVE ( )  B_SPLINE_CURVE ( 2, ( #32058, #4145, #38469, #21104, #72414, #20725, #49395, #33567, #16167, #61094, #56197, #55078, #50150 ),
 .UNSPECIFIED., .F., .F. ) 
 B_SPLINE_CURVE_WITH_KNOTS ( ( 3, 2, 2, 2, 2, 2, 3 ),
 ( 0.6032608695652174058, 0.6050724637681159646, 0.6068840579710145233, 0.6086956521739130821, 0.6105072463768117519, 0.6123188405797103107, 0.6141304347826087584 ),
 .UNSPECIFIED. ) 
 CURVE ( )  GEOMETRIC_REPRESENTATION_ITEM ( )  RATIONAL_B_SPLINE_CURVE ( ( 1.000000000000000000, 0.9659258262890683122, 1.000000000000000000, 0.9659258262890683122, 1.000000000000000000, 0.9659258262890683122, 1.000000000000000000, 0.9659258262890683122, 1.000000000000000000, 0.9659258262890683122, 1.000000000000000000, 0.9659258262890662028, 1.000000000000001998 ) ) 
 REPRESENTATION_ITEM ( '' )  );
#25579=CARTESIAN_POINT ( 'NONE',  ( 3.178432602446558121E-13, 136.2499999999999716, -10.00000000000000533 ) ) ;
#25580=( BOUNDED_CURVE ( )  B_SPLINE_CURVE ( 2, ( #14741, #66816, #71710, #60776, #9483, #9102, #55135, #49832, #32498, #72850, #20027, #21155, #43040, #66059, #67193, #14366, #29348, #64416, #70444, #12714, #6343, #69706, #29713, #35746, #63663, #35022, #58035, #40285, #18759, #64775, #46315, #52355, #693, #11987, #28965, #6705, #57278, #34275, #35387, #41037, #1431, #22931, #23677, #46682, #18019, #23301, #17640, #69329, #64044, #18391, #28590, #70084, #57655, #5961, #12354, #58400, #52726, #41403, #58763, #1060, #40659, #24039, #47049, #41767, #5593, #63286, #7073, #30079, #53097, #51601, #24414, #47419, #74616, #45943, #323, #68956, #17266, #11613, #34650, #51984, #19482, #36482, #60594, #7809, #65878, #19117, #25509, #14184, #31182, #59859, #3263, #36852, #48893, #72284, #48522, #30811, #43238, #8919, #66253, #71906, #59496, #42122, #8172, #26251, #70803, #71528, #48152, #42497, #37221, #53835, #65134, #20219, #19855, #36113, #2143, #65512, #31931, #25137, #13445, #37595, #71162, #1785, #13807, #54207, #2516, #42859, #60219, #54953, #24770, #20597, #43612, #8544, #53467, #31557, #54581, #2886, #25874, #14559, #49269, #13078, #59135, #7443, #30451, #47782, #51138, #15304, #38723, #20971, #28125, #43995, #62088, #33076, #72669, #27009, #56072, #33438, #61720, #15681, #56812, #67005, #3633, #9674, #4381, #38341, #10410, #61348, #56438, #33814, #10777, #14930, #37972, #26631, #32695, #73777, #60971, #50022, #4758, #27750, #10040, #27374, #50394, #55703, #73409, #21713, #4019, #49653, #74148, #22452, #22086, #50762, #5132, #66625, #44742 ),
 .UNSPECIFIED., .F., .F. ) 
 B_SPLINE_CURVE_WITH_KNOTS ( ( 3, 2, 2, 2, 2, 2, 2, 2, 2, 2, 2, 2, 2, 2, 2, 2, 2, 2, 2, 2, 2, 2, 2, 2, 2, 2, 2, 2, 2, 2, 2, 2, 2, 2, 2, 2, 2, 2, 2, 2, 2, 2, 2, 2, 2, 2, 2, 2, 2, 2, 2, 2, 2, 2, 2, 2, 2, 2, 2, 2, 2, 2, 2, 2, 2, 2, 2, 2, 2, 2, 2, 2, 2, 2, 2, 2, 2, 2, 2, 2, 2, 2, 2, 2, 2, 2, 2, 2, 2, 2, 2, 2, 2, 2, 2, 2, 3 ),
 ( 0.000000000000000000, 0.01041666666666666609, 0.02083333333333333218, 0.03125000000000000000, 0.04166666666666666435, 0.05208333333333333565, 0.06250000000000000000, 0.07291666666666667129, 0.08333333333333332871, 0.09375000000000000000, 0.1041666666666666713, 0.1145833333333333287, 0.1250000000000000000, 0.1354166666666666574, 0.1458333333333333426, 0.1562500000000000000, 0.1666666666666666574, 0.1770833333333333426, 0.1875000000000000000, 0.1979166666666666574, 0.2083333333333333426, 0.2187500000000000000, 0.2291666666666666574, 0.2395833333333333426, 0.2500000000000000000, 0.2604166666666666852, 0.2708333333333333148, 0.2812500000000000000, 0.2916666666666666852, 0.3020833333333333148, 0.3125000000000000000, 0.3229166666666666852, 0.3333333333333333148, 0.3437500000000000000, 0.3541666666666666852, 0.3645833333333333148, 0.3750000000000000000, 0.3854166666666666852, 0.3958333333333333148, 0.4062500000000000000, 0.4166666666666666852, 0.4270833333333333148, 0.4375000000000000000, 0.4479166666666666852, 0.4583333333333333148, 0.4687500000000000000, 0.4791666666666666852, 0.4895833333333333148, 0.5000000000000000000, 0.5104166666666666297, 0.5208333333333333703, 0.5312500000000000000, 0.5416666666666666297, 0.5520833333333333703, 0.5625000000000000000, 0.5729166666666666297, 0.5833333333333333703, 0.5937500000000000000, 0.6041666666666666297, 0.6145833333333333703, 0.6250000000000000000, 0.6354166666666666297, 0.6458333333333333703, 0.6562500000000000000, 0.6666666666666666297, 0.6770833333333333703, 0.6875000000000000000, 0.6979166666666666297, 0.7083333333333333703, 0.7187500000000000000, 0.7291666666666666297, 0.7395833333333333703, 0.7500000000000000000, 0.7604166666666666297, 0.7708333333333333703, 0.7812500000000000000, 0.7916666666666666297, 0.8020833333333333703, 0.8125000000000000000, 0.8229166666666666297, 0.8333333333333333703, 0.8437500000000000000, 0.8541666666666666297, 0.8645833333333333703, 0.8750000000000000000, 0.8854166666666666297, 0.8958333333333333703, 0.9062500000000000000, 0.9166666666666666297, 0.9270833333333333703, 0.9375000000000000000, 0.9479166666666666297, 0.9583333333333333703, 0.9687500000000000000, 0.9791666666666666297, 0.9895833333333333703, 1.000000000000000000 ),
 .UNSPECIFIED. ) 
 CURVE ( )  GEOMETRIC_REPRESENTATION_ITEM ( )  RATIONAL_B_SPLINE_CURVE ( ( 1.000000000000000000, 0.9238795325112867385, 1.000000000000000000, 0.9238795325112867385, 1.000000000000000000, 0.9238795325112867385, 1.000000000000000000, 0.9238795325112867385, 1.000000000000000000, 0.9238795325112867385, 1.000000000000000000, 0.9238795325112867385, 1.000000000000000000, 0.9238795325112867385, 1.000000000000000000, 0.9238795325112867385, 1.000000000000000000, 0.9238795325112867385, 1.000000000000000000, 0.9238795325112867385, 1.000000000000000000, 0.9238795325112867385, 1.000000000000000000, 0.9238795325112867385, 1.000000000000000000, 0.9238795325112867385, 1.000000000000000000, 0.9238795325112867385, 1.000000000000000000, 0.9238795325112867385, 1.000000000000000000, 0.9238795325112867385, 1.000000000000000000, 0.9238795325112867385, 1.000000000000000000, 0.9238795325112867385, 1.000000000000000000, 0.9238795325112867385, 1.000000000000000000, 0.9238795325112867385, 1.000000000000000000, 0.9238795325112867385, 1.000000000000000000, 0.9238795325112867385, 1.000000000000000000, 0.9238795325112867385, 1.000000000000000000, 0.9238795325112867385, 1.000000000000000000, 0.9238795325112867385, 1.000000000000000000, 0.9238795325112867385, 1.000000000000000000, 0.9238795325112867385, 1.000000000000000000, 0.9238795325112867385, 1.000000000000000000, 0.9238795325112867385, 1.000000000000000000, 0.9238795325112867385, 1.000000000000000000, 0.9238795325112867385, 1.000000000000000000, 0.9238795325112867385, 1.000000000000000000, 0.9238795325112867385, 1.000000000000000000, 0.9238795325112867385, 1.000000000000000000, 0.9238795325112867385, 1.000000000000000000, 0.9238795325112867385, 1.000000000000000000, 0.9238795325112867385, 1.000000000000000000, 0.9238795325112867385, 1.000000000000000000, 0.9238795325112867385, 1.000000000000000000, 0.9238795325112867385, 1.000000000000000000, 0.9238795325112867385, 1.000000000000000000, 0.9238795325112867385, 1.000000000000000000, 0.9238795325112867385, 1.000000000000000000, 0.9238795325112867385, 1.000000000000000000, 0.9238795325112867385, 1.000000000000000000, 0.9238795325112867385, 1.000000000000000000, 0.9238795325112867385, 1.000000000000000000, 0.9238795325112867385, 1.000000000000000000, 0.9238795325112867385, 1.000000000000000000, 0.9238795325112867385, 1.000000000000000000, 0.9238795325112867385, 1.000000000000000000, 0.9238795325112867385, 1.000000000000000000, 0.9238795325112867385, 1.000000000000000000, 0.9238795325112867385, 1.000000000000000000, 0.9238795325112867385, 1.000000000000000000, 0.9238795325112867385, 1.000000000000000000, 0.9238795325112867385, 1.000000000000000000, 0.9238795325112867385, 1.000000000000000000, 0.9238795325112867385, 1.000000000000000000, 0.9238795325112867385, 1.000000000000000000, 0.9238795325112867385, 1.000000000000000000, 0.9238795325112867385, 1.000000000000000000, 0.9238795325112867385, 1.000000000000000000, 0.9238795325112867385, 1.000000000000000000, 0.9238795325112867385, 1.000000000000000000, 0.9238795325112867385, 1.000000000000000000, 0.9238795325112867385, 1.000000000000000000, 0.9238795325112867385, 1.000000000000000000, 0.9238795325112867385, 1.000000000000000000, 0.9238795325112867385, 1.000000000000000000, 0.9238795325112867385, 1.000000000000000000, 0.9238795325112867385, 1.000000000000000000, 0.9238795325112867385, 1.000000000000000000, 0.9238795325112867385, 1.000000000000000000, 0.9238795325112867385, 1.000000000000000000, 0.9238795325112867385, 1.000000000000000000, 0.9238795325112867385, 1.000000000000000000, 0.9238795325112867385, 1.000000000000000000, 0.9238795325112867385, 1.000000000000000000, 0.9238795325112867385, 1.000000000000000000, 0.9238795325112867385, 1.000000000000000000, 0.9238795325112867385, 1.000000000000000000, 0.9238795325112867385, 1.000000000000000000, 0.9238795325112867385, 1.000000000000000000, 0.9238795325112867385, 1.000000000000000000, 0.9238795325112867385, 1.000000000000000000, 0.9238795325112867385, 1.000000000000000000, 0.9238795325112867385, 1.000000000000000000, 0.9238795325112867385, 1.000000000000000000, 0.9238795325112867385, 1.000000000000000000, 0.9238795325112867385, 1.000000000000000000, 0.9238795325112867385, 1.000000000000000000, 0.9238795325112867385, 1.000000000000000000, 0.9238795325112867385, 1.000000000000000000, 0.9238795325112867385, 1.000000000000000000, 0.9238795325112867385, 1.000000000000000000 ) ) 
 REPRESENTATION_ITEM ( '' )  );
#25584=CARTESIAN_POINT ( 'NONE',  ( -2.679491924311235618, 3.541666666666666963, 10.00000000000000000 ) ) ;
#25586=EDGE_CURVE ( 'NONE', #51233, #17320, #65839, .T. ) ;
#25592=CARTESIAN_POINT ( 'NONE',  ( 4.242640687119287435, 293.4375000034140157, 4.242640687119285658 ) ) ;
#25605=CARTESIAN_POINT ( 'NONE',  ( -5.676582343750006032, 64.42708332991935549, 9.832129032723418760 ) ) ;
#25610=CARTESIAN_POINT ( 'NONE',  ( -2.765530957081996810, 292.4218750017069510, -6.676582343750002480 ) ) ;
#25611=CARTESIAN_POINT ( 'NONE',  ( -2.679491924311235618, 143.5416666666666856, 10.00000000000000000 ) ) ;
#25626=CARTESIAN_POINT ( 'NONE',  ( 6.951808397369818766E-16, 42.03124999658601268, -11.35316468750000141 ) ) ;
#25628=CARTESIAN_POINT ( 'NONE',  ( -10.00000000000000355, 14.58333332650536462, 2.679491924311223183 ) ) ;
#25630=EDGE_CURVE ( 'NONE', #2022, #16864, #55665, .T. ) ;
#25633=CARTESIAN_POINT ( 'NONE',  ( 8.311093377946837890, 36.40624999658601979, -8.311093377946837890 ) ) ;
#25639=CARTESIAN_POINT ( 'NONE',  ( -9.832129032723420536, 28.69791666325268409, 5.676582343749997150 ) ) ;
#25641=EDGE_CURVE ( 'NONE', #46122, #28343, #46952, .T. ) ;
#25642=CARTESIAN_POINT ( 'NONE',  ( -8.311093377946836114, 162.6562499965859843, -8.311093377946837890 ) ) ;
#25643=CARTESIAN_POINT ( 'NONE',  ( 8.660254037844385522, 131.4583333265053682, 5.000000000000005329 ) ) ;
#25647=CARTESIAN_POINT ( 'NONE',  ( 9.832129032723420536, 21.51041666325268409, -5.676582343749999815 ) ) ;
#25654=CARTESIAN_POINT ( 'NONE',  ( -5.676582343749998039, 157.4479166632526983, -9.832129032723420536 ) ) ;
#25663=CARTESIAN_POINT ( 'NONE',  ( 8.311093377946837890, 101.7187499965860269, -8.311093377946837890 ) ) ;
#25681=CARTESIAN_POINT ( 'NONE',  ( -7.320508075689018845, 23.12500000000019540, 7.320508075689011740 ) ) ;
#25682=( BOUNDED_CURVE ( )  B_SPLINE_CURVE ( 2, ( #38270, #48452, #14112, #61274, #9603, #32622, #55630, #3946, #49954, #8467, #31487, #54510, #33365 ),
 .UNSPECIFIED., .F., .F. ) 
 B_SPLINE_CURVE_WITH_KNOTS ( ( 3, 2, 2, 2, 2, 2, 3 ),
 ( 0.3532608695652174058, 0.3550724637681159646, 0.3568840579710144678, 0.3586956521739130266, 0.3605072463768115854, 0.3623188405797101441, 0.3641304347826087029 ),
 .UNSPECIFIED. ) 
 CURVE ( )  GEOMETRIC_REPRESENTATION_ITEM ( )  RATIONAL_B_SPLINE_CURVE ( ( 1.000000000000000000, 0.9659258262890683122, 1.000000000000000000, 0.9659258262890683122, 1.000000000000000000, 0.9659258262890683122, 1.000000000000000000, 0.9659258262890683122, 1.000000000000000000, 0.9659258262890683122, 1.000000000000000000, 0.9659258262890683122, 1.000000000000000000 ) ) 
 REPRESENTATION_ITEM ( '' )  );
#25693=CARTESIAN_POINT ( 'NONE',  ( 3.153939666463669656E-13, 33.75000000000002842, 9.999999999999998224 ) ) ;
#25694=CARTESIAN_POINT ( 'NONE',  ( 8.660254037844385522, 114.5833333333333428, 5.000000000000005329 ) ) ;
#25696=CARTESIAN_POINT ( 'NONE',  ( -4.721056650415999201, 296.4843750017070079, -4.721056650415999201 ) ) ;
#25698=CARTESIAN_POINT ( 'NONE',  ( 7.320508075688800353, 189.3750000000000568, 7.320508075688803906 ) ) ;
#25707=CARTESIAN_POINT ( 'NONE',  ( 3.042071309553167069, 1.822916663252682978, -11.35316468749999785 ) ) ;
#25709=CARTESIAN_POINT ( 'NONE',  ( 5.676582343749993598, 195.2604166632526983, 9.832129032723422313 ) ) ;
#25717=CARTESIAN_POINT ( 'NONE',  ( 11.35316468749999963, 51.30208332991936260, -3.042071309553165293 ) ) ;
#25725=CARTESIAN_POINT ( 'NONE',  ( 3.042071309553167069, 121.8229166632526841, -11.35316468749999785 ) ) ;
#25726=CARTESIAN_POINT ( 'NONE',  ( -10.00000000000000178, 94.37499999317203958, -1.224646799147353454E-15 ) ) ;
#25730=CARTESIAN_POINT ( 'NONE',  ( 6.123233995736767268E-16, 161.2500000000000000, -10.00000000000000178 ) ) ;
#25732=CARTESIAN_POINT ( 'NONE',  ( -7.535105736103198559, 226.0000000000000000, -6.607085568838196643 ) ) ;
#25735=CARTESIAN_POINT ( 'NONE',  ( -4.088227598258586603E-16, 293.3593750017070079, -6.676582343750001591 ) ) ;
#25738=CARTESIAN_POINT ( 'NONE',  ( 9.832129032723420536, 171.1979166632526983, -5.676582343749999815 ) ) ;
#25744=VERTEX_POINT ( 'NONE', #20559 ) ;
#25747=CARTESIAN_POINT ( 'NONE',  ( 9.832129032723420536, 151.5104166632526699, -5.676582343749999815 ) ) ;
#25751=CARTESIAN_POINT ( 'NONE',  ( 9.832129032723416984, 65.67708332991935549, 5.676582343750006032 ) ) ;
#25756=ORIENTED_EDGE ( 'NONE', *, *, #23367, .F. ) ;
#25758=CARTESIAN_POINT ( 'NONE',  ( 1.102182119232618108E-15, 287.3125000034140157, 6.000000000000001776 ) ) ;
#25767=ORIENTED_EDGE ( 'NONE', *, *, #41913, .F. ) ;
#25772=CARTESIAN_POINT ( 'NONE',  ( -6.000000000000001776, 295.0000000000000000, 0.000000000000000000 ) ) ;
#25782=CARTESIAN_POINT ( 'NONE',  ( -2.679491924311225848, 61.45833333333332860, -10.00000000000000178 ) ) ;
#25785=CARTESIAN_POINT ( 'NONE',  ( -4.242640687119285658, 295.1249999999999432, 4.242640687119287435 ) ) ;
#25787=CARTESIAN_POINT ( 'NONE',  ( 10.00000000000000178, 0.9374999965860164597, 0.000000000000000000 ) ) ;
#25788=VERTEX_POINT ( 'NONE', #9253 ) ;
#25796=CARTESIAN_POINT ( 'NONE',  ( 1.224646799147353454E-15, 300.0000000000000000, -10.00000000000000178 ) ) ;
#25797=CARTESIAN_POINT ( 'NONE',  ( -8.660254037844390851, 187.9166666666666856, 4.999999999999998224 ) ) ;
#25801=CARTESIAN_POINT ( 'NONE',  ( 11.35316468750000141, 161.0937499965860127, 0.000000000000000000 ) ) ;
#25806=CARTESIAN_POINT ( 'NONE',  ( -2.485281374238916374, 293.8125000000000000, -5.999999999999657163 ) ) ;
#25809=CARTESIAN_POINT ( 'NONE',  ( -5.676582343750006032, 4.427083329919350163, 9.832129032723418760 ) ) ;
#25814=CARTESIAN_POINT ( 'NONE',  ( 10.00000000000000000, 51.66666665983870388, 2.679491924311236062 ) ) ;
#25825=CARTESIAN_POINT ( 'NONE',  ( -2.085542519210945728E-15, 134.5312499965860411, 11.35316468750000141 ) ) ;
#25829=DIRECTION ( 'NONE',  ( 0.000000000000000000, -1.000000000000000000, 0.000000000000000000 ) ) ;
#25833=CARTESIAN_POINT ( 'NONE',  ( -11.35316468749999785, 108.0729166632526699, -3.042071309553167957 ) ) ;
#25839=CARTESIAN_POINT ( 'NONE',  ( 9.832129032723416984, 100.6770833299193555, 5.676582343750006032 ) ) ;
#25843=CARTESIAN_POINT ( 'NONE',  ( 9.832129032723416984, 25.67708332991935194, 5.676582343750006032 ) ) ;
#25844=ORIENTED_EDGE ( 'NONE', *, *, #28662, .F. ) ;
#25848=CIRCLE ( 'NONE', #33116, 8.000000000000003553 ) ;
#25851=CARTESIAN_POINT ( 'NONE',  ( -6.676582343750001591, 289.4531250017069510, 0.000000000000000000 ) ) ;
#25853=CARTESIAN_POINT ( 'NONE',  ( 11.35316468750000141, 216.0937499965860411, 0.000000000000000000 ) ) ;
#25854=CARTESIAN_POINT ( 'NONE',  ( 3.042071309553167069, 142.1354166632526415, -11.35316468749999785 ) ) ;
#25871=CARTESIAN_POINT ( 'NONE',  ( -3.042071309553173730, 189.3229166632526699, 11.35316468749999785 ) ) ;
#25874=CARTESIAN_POINT ( 'NONE',  ( 6.676582343750001591, 290.9531250017069510, -8.176455196517173205E-16 ) ) ;
#25881=FACE_OUTER_BOUND ( 'NONE', #47351, .T. ) ;
#25884=LINE ( 'NONE', #65145, #28311 ) ;
#25886=CARTESIAN_POINT ( 'NONE',  ( 11.35316468749999963, 111.3020833299193271, -3.042071309553165293 ) ) ;
#25895=DIRECTION ( 'NONE',  ( -0.000000000000000000, 1.000000000000000000, -0.000000000000000000 ) ) ;
#25896=CARTESIAN_POINT ( 'NONE',  ( -2.085542519210945728E-15, 224.5312499965860127, 11.35316468750000141 ) ) ;
#25902=CARTESIAN_POINT ( 'NONE',  ( -5.676582343750006032, 189.4270833299193555, 9.832129032723418760 ) ) ;
#25909=CARTESIAN_POINT ( 'NONE',  ( 11.35316468749999785, 75.57291666325269830, 3.042071309553174174 ) ) ;
#25910=ORIENTED_EDGE ( 'NONE', *, *, #53918, .T. ) ;
#25914=CARTESIAN_POINT ( 'NONE',  ( 6.123233995736767268E-16, 153.1249999931720538, -10.00000000000000178 ) ) ;
#25915=CARTESIAN_POINT ( 'NONE',  ( 8.311093377946837890, 86.40624999658601268, -8.311093377946837890 ) ) ;
#25922=CARTESIAN_POINT ( 'NONE',  ( -3.042071309553173730, 79.32291666325269830, 11.35316468749999785 ) ) ;
#25927=CARTESIAN_POINT ( 'NONE',  ( -8.660254037844390851, 169.7916666598387110, 4.999999999999998224 ) ) ;
#25931=CARTESIAN_POINT ( 'NONE',  ( 9.832129032723416984, 65.67708332991935549, 5.676582343750006032 ) ) ;
#25932=CARTESIAN_POINT ( 'NONE',  ( 1.226468279477575784E-15, 291.7031250017069510, 6.676582343750001591 ) ) ;
#25934=CARTESIAN_POINT ( 'NONE',  ( -5.676582343749998039, 212.4479166632526983, -9.832129032723420536 ) ) ;
#25940=CARTESIAN_POINT ( 'NONE',  ( 11.35316468749999963, 190.9895833299193271, -3.042071309553165293 ) ) ;
#25945=CARTESIAN_POINT ( 'NONE',  ( -5.676582343749998039, 187.7604166632526983, -9.832129032723420536 ) ) ;
#25959=DIRECTION ( 'NONE',  ( -0.000000000000000000, 1.000000000000000000, -0.000000000000000000 ) ) ;
#25968=CARTESIAN_POINT ( 'NONE',  ( -11.35316468749999785, 78.38541666325266988, -3.042071309553167513 ) ) ;
#25972=CARTESIAN_POINT ( 'NONE',  ( -6.676582343749999815, 295.6718750017070079, 2.765530957082001251 ) ) ;
#25973=CARTESIAN_POINT ( 'NONE',  ( 8.660254037844389075, 145.4166666666666572, -5.000000000000000000 ) ) ;
#25983=CARTESIAN_POINT ( 'NONE',  ( -6.000000000000001776, 293.0625000034140157, 0.000000000000000000 ) ) ;
#25990=CARTESIAN_POINT ( 'NONE',  ( 11.35316468749999963, 45.98958332991934839, -3.042071309553165293 ) ) ;
#25992=CARTESIAN_POINT ( 'NONE',  ( 4.999999999999993783, 6.041666659838699438, 8.660254037844390851 ) ) ;
#25996=CARTESIAN_POINT ( 'NONE',  ( 5.676582343749993598, 49.94791666325268409, 9.832129032723422313 ) ) ;
#26002=CARTESIAN_POINT ( 'NONE',  ( 11.35316468749999785, 30.57291666325268409, 3.042071309553174174 ) ) ;
#26006=CARTESIAN_POINT ( 'NONE',  ( 5.676582343750001591, 161.6145833299193839, -9.832129032723420536 ) ) ;
#26008=CARTESIAN_POINT ( 'NONE',  ( -8.660254037844390851, 134.7916666598387110, 4.999999999999998224 ) ) ;
#26011=CARTESIAN_POINT ( 'NONE',  ( -6.000000000000001776, 289.0000000000000000, 0.000000000000000000 ) ) ;
#26012=CARTESIAN_POINT ( 'NONE',  ( 3.042071309553159519, 20.05208332991934839, 11.35316468750000141 ) ) ;
#26020=CARTESIAN_POINT ( 'NONE',  ( 5.676582343749993598, 154.9479166632526983, 9.832129032723422313 ) ) ;
#26025=AXIS2_PLACEMENT_3D ( 'NONE', #4727, #16760, #28094 ) ;
#26031=CARTESIAN_POINT ( 'NONE',  ( -5.999999999999999112, 292.1250000034140157, 2.485281374238575314 ) ) ;
#26032=CARTESIAN_POINT ( 'NONE',  ( -11.35316468750000141, 103.5937499965860269, -1.390361679473963753E-15 ) ) ;
#26034=CARTESIAN_POINT ( 'NONE',  ( 8.660254037844394404, 15.41666666666667140, -5.000000000000004441 ) ) ;
#26035=ORIENTED_EDGE ( 'NONE', *, *, #39415, .F. ) ;
#26043=CARTESIAN_POINT ( 'NONE',  ( 6.123233995736767268E-16, 158.1249999931720254, -10.00000000000000178 ) ) ;
#26057=ORIENTED_EDGE ( 'NONE', *, *, #27468, .T. ) ;
#26063=CARTESIAN_POINT ( 'NONE',  ( -5.000000000000003553, 33.33333333333333570, 8.660254037844383745 ) ) ;
#26064=CARTESIAN_POINT ( 'NONE',  ( -8.660254037844387298, 102.0833333333333428, -5.000000000000004441 ) ) ;
#26066=CARTESIAN_POINT ( 'NONE',  ( 2.765530957081996366, 291.2968750017069510, -6.676582343750003368 ) ) ;
#26074=CARTESIAN_POINT ( 'NONE',  ( 1.224646799147353454E-15, 300.0000000000000000, -10.00000000000000178 ) ) ;
#26075=DIRECTION ( 'NONE',  ( -0.000000000000000000, 1.000000000000000000, -0.000000000000000000 ) ) ;
#26079=CARTESIAN_POINT ( 'NONE',  ( 11.35316468749999963, 0.9895833299193496080, -3.042071309553165293 ) ) ;
#26082=CARTESIAN_POINT ( 'NONE',  ( -9.832129032723418760, 198.1770833299193555, -5.676582343750004256 ) ) ;
#26089=ORIENTED_EDGE ( 'NONE', *, *, #35040, .T. ) ;
#26091=CARTESIAN_POINT ( 'NONE',  ( -8.311093377946841443, 8.906249996586018014, 8.311093377946830785 ) ) ;
#26096=CARTESIAN_POINT ( 'NONE',  ( -1.183492779173324630E-13, 16.25000000000001066, -10.00000000000000178 ) ) ;
#26098=CARTESIAN_POINT ( 'NONE',  ( 8.311093377946837890, 126.4062499965860269, -8.311093377946837890 ) ) ;
#26101=CARTESIAN_POINT ( 'NONE',  ( 5.000000000000001776, 92.70833332650536818, -8.660254037844389075 ) ) ;
#26105=CARTESIAN_POINT ( 'NONE',  ( -2.679491924311226292, 38.33333332650536818, -10.00000000000000178 ) ) ;
#26106=ORIENTED_EDGE ( 'NONE', *, *, #1479, .T. ) ;
#26107=CARTESIAN_POINT ( 'NONE',  ( -8.987711252924967198, 225.9999999999998863, 4.433107781483233367 ) ) ;
#26108=CARTESIAN_POINT ( 'NONE',  ( -6.676582343750001591, 293.6093750017069510, 0.000000000000000000 ) ) ;
#26109=CARTESIAN_POINT ( 'NONE',  ( 8.660254037844385522, 186.4583333265053682, 5.000000000000005329 ) ) ;
#26111=CARTESIAN_POINT ( 'NONE',  ( 8.311093377946834337, 170.1562499965860127, 8.311093377946839666 ) ) ;
#26119=CARTESIAN_POINT ( 'NONE',  ( -8.311093377946841443, 159.2187499965860411, 8.311093377946834337 ) ) ;
#26123=CARTESIAN_POINT ( 'NONE',  ( 3.042071309553159519, 60.05208332991934128, 11.35316468750000141 ) ) ;
#26131=CARTESIAN_POINT ( 'NONE',  ( 4.242640687119287435, 287.4375000034140157, 4.242640687119285658 ) ) ;
#26158=CARTESIAN_POINT ( 'NONE',  ( 2.679491924311228956, 71.04166666666664298, -10.00000000000000000 ) ) ;
#26160=CARTESIAN_POINT ( 'NONE',  ( -3.673940397442060854E-16, 293.7500000000000000, -6.000000000000001776 ) ) ;
#26171=CARTESIAN_POINT ( 'NONE',  ( -2.679491924311235618, 188.5416666666666572, 10.00000000000000000 ) ) ;
#26174=CARTESIAN_POINT ( 'NONE',  ( -11.35316468750000141, 148.5937499965860411, -1.390361679473963753E-15 ) ) ;
#26182=ORIENTED_EDGE ( 'NONE', *, *, #51396, .T. ) ;
#26183=CARTESIAN_POINT ( 'NONE',  ( 11.35316468749999963, 16.30208332991935194, -3.042071309553165293 ) ) ;
#26189=CARTESIAN_POINT ( 'NONE',  ( -7.320508075688778149, 54.99999999317203958, 7.320508075688769267 ) ) ;
#26192=CARTESIAN_POINT ( 'NONE',  ( 8.660254037844397956, 220.4166666666666856, -5.000000000000006217 ) ) ;
#26200=CARTESIAN_POINT ( 'NONE',  ( 11.35316468749999963, 130.9895833299193555, -3.042071309553165293 ) ) ;
#26208=CARTESIAN_POINT ( 'NONE',  ( -9.832129032723418760, 127.8645833299193697, -5.676582343750004256 ) ) ;
#26209=CARTESIAN_POINT ( 'NONE',  ( 2.679491924311228956, 147.9166666598387110, -10.00000000000000000 ) ) ;
#26213=CARTESIAN_POINT ( 'NONE',  ( -11.35316468749999785, 118.3854166632526699, -3.042071309553167957 ) ) ;
#26217=CARTESIAN_POINT ( 'NONE',  ( 6.951808397369818766E-16, 27.34374999658601979, -11.35316468750000141 ) ) ;
#26219=CARTESIAN_POINT ( 'NONE',  ( 8.660254037844389075, 182.2916666598387110, -5.000000000000000000 ) ) ;
#26224=CARTESIAN_POINT ( 'NONE',  ( -2.765530957081996810, 290.2656250017068942, -6.676582343750003368 ) ) ;
#26226=CARTESIAN_POINT ( 'NONE',  ( 11.35316468749999785, 215.8854166632526983, 3.042071309553174174 ) ) ;
#26229=CARTESIAN_POINT ( 'NONE',  ( -5.676582343749998039, 142.7604166632526699, -9.832129032723420536 ) ) ;
#26234=DIRECTION ( 'NONE',  ( -0.000000000000000000, 1.000000000000000000, -0.000000000000000000 ) ) ;
#26247=CARTESIAN_POINT ( 'NONE',  ( 8.311093377946837890, 191.4062499965860127, -8.311093377946837890 ) ) ;
#26250=CARTESIAN_POINT ( 'NONE',  ( 1.224646799147353454E-15, 300.0000000000000000, -10.00000000000000178 ) ) ;
#26251=CARTESIAN_POINT ( 'NONE',  ( 6.676582343750002480, 293.0156250017069510, -2.765530957081997254 ) ) ;
#26253=CARTESIAN_POINT ( 'NONE',  ( 2.679491924305479333, 93.95833333333280279, 10.00000000000330935 ) ) ;
#26257=CARTESIAN_POINT ( 'NONE',  ( 7.320508075688774596, 167.4999999931720538, -7.320508075688774596 ) ) ;
#26263=CARTESIAN_POINT ( 'NONE',  ( -9.832129032723418760, 108.1770833299193555, -5.676582343750004256 ) ) ;
#26271=CARTESIAN_POINT ( 'NONE',  ( -8.311093377946841443, 223.9062499965860411, 8.311093377946830785 ) ) ;
#26275=CARTESIAN_POINT ( 'NONE',  ( -8.311093377946841443, 199.2187499965860411, 8.311093377946830785 ) ) ;
#26282=CARTESIAN_POINT ( 'NONE',  ( -2.085542519210945728E-15, 84.53124999658602690, 11.35316468750000141 ) ) ;
#26287=CARTESIAN_POINT ( 'NONE',  ( 8.660254037844522301, 39.58333333333343518, 5.000000000000085265 ) ) ;
#26289=CARTESIAN_POINT ( 'NONE',  ( 3.042071309553159519, 94.73958332991934128, 11.35316468750000141 ) ) ;
#26290=ORIENTED_EDGE ( 'NONE', *, *, #32572, .T. ) ;
#26297=CARTESIAN_POINT ( 'NONE',  ( -2.085542519210945728E-15, 89.53124999658602690, 11.35316468750000141 ) ) ;
#26300=CARTESIAN_POINT ( 'NONE',  ( -7.320508075688773708, 173.7499999931720254, -7.320508075688774596 ) ) ;
#26304=CARTESIAN_POINT ( 'NONE',  ( -8.311093377946841443, 69.21874999658601268, 8.311093377946834337 ) ) ;
#26305=CARTESIAN_POINT ( 'NONE',  ( -4.721056650415999201, 293.3281250017069510, -4.721056650415999201 ) ) ;
#26307=CARTESIAN_POINT ( 'NONE',  ( -11.35316468749999785, 213.0729166632527267, -3.042071309553167513 ) ) ;
#26313=CARTESIAN_POINT ( 'NONE',  ( 3.042071309553159519, 189.7395833299193271, 11.35316468750000141 ) ) ;
#26314=DIRECTION ( 'NONE',  ( -0.000000000000000000, 1.000000000000000000, -0.000000000000000000 ) ) ;
#26319=CARTESIAN_POINT ( 'NONE',  ( -11.35316468749999785, 188.3854166632526983, -3.042071309553167957 ) ) ;
#26327=CARTESIAN_POINT ( 'NONE',  ( -8.660254037844387298, 2.083333333333333481, -5.000000000000004441 ) ) ;
#26341=ORIENTED_EDGE ( 'NONE', *, *, #70464, .F. ) ;
#26344=ORIENTED_EDGE ( 'NONE', *, *, #53851, .T. ) ;
#26347=CARTESIAN_POINT ( 'NONE',  ( 8.311093377946834337, 70.46874999658599847, 8.311093377946839666 ) ) ;
#26352=CARTESIAN_POINT ( 'NONE',  ( -4.721056650415999201, 295.4843750017070079, -4.721056650415999201 ) ) ;
#26368=CARTESIAN_POINT ( 'NONE',  ( -11.35316468749999785, 38.07291666325269119, -3.042071309553167513 ) ) ;
#26370=CARTESIAN_POINT ( 'NONE',  ( -2.679491924311225848, 13.33333332650536640, -10.00000000000000178 ) ) ;
#26373=CARTESIAN_POINT ( 'NONE',  ( 3.042071309553167069, 46.82291666325267698, -11.35316468749999785 ) ) ;
#26376=CARTESIAN_POINT ( 'NONE',  ( -5.999999999999999112, 299.0625000000000000, 2.485281374238575314 ) ) ;
#26379=CARTESIAN_POINT ( 'NONE',  ( 3.042071309553159519, 39.73958332991934128, 11.35316468750000141 ) ) ;
#26382=CARTESIAN_POINT ( 'NONE',  ( -3.042071309553164404, 167.2395833299193839, -11.35316468749999963 ) ) ;
#26383=CARTESIAN_POINT ( 'NONE',  ( -10.00000000000000000, 124.1666666598387110, -2.679491924311229845 ) ) ;
#26385=ORIENTED_EDGE ( 'NONE', *, *, #52826, .F. ) ;
#26387=CARTESIAN_POINT ( 'NONE',  ( 3.042071309553167513, 22.13541666325268409, -11.35316468749999785 ) ) ;
#26388=CARTESIAN_POINT ( 'NONE',  ( -8.660254037844392627, 17.08333333333334281, -5.000000000000008882 ) ) ;
#26394=CARTESIAN_POINT ( 'NONE',  ( -8.311093377946841443, 153.9062499965860411, 8.311093377946834337 ) ) ;
#26405=CARTESIAN_POINT ( 'NONE',  ( 9.832129032723420536, 101.5104166632526841, -5.676582343749999815 ) ) ;
#26419=CARTESIAN_POINT ( 'NONE',  ( -10.00000000000000178, 159.3749999931720254, -1.224646799147353454E-15 ) ) ;
#26423=ORIENTED_EDGE ( 'NONE', *, *, #43571, .T. ) ;
#26425=ADVANCED_FACE ( 'NONE', ( #10939 ), #56972, .T. ) ;
#26429=CARTESIAN_POINT ( 'NONE',  ( -1.836970198721029983E-15, 70.62499999317203958, 10.00000000000000178 ) ) ;
#26440=CARTESIAN_POINT ( 'NONE',  ( 7.320508075688771044, 104.3750000000000000, 7.320508075688775484 ) ) ;
#26441=ADVANCED_FACE ( 'NONE', ( #48587 ), #2209, .T. ) ;
#26443=CARTESIAN_POINT ( 'NONE',  ( 6.676582343750001591, 291.1093750017069510, -8.176455196517173205E-16 ) ) ;
#26455=CARTESIAN_POINT ( 'NONE',  ( -7.320508075688773708, 213.7499999931720254, -7.320508075688774596 ) ) ;
#26456=CARTESIAN_POINT ( 'NONE',  ( 9.832129032723420536, 6.197916663252683200, -5.676582343749999815 ) ) ;
#26459=CARTESIAN_POINT ( 'NONE',  ( 9.832129032723420536, 196.5104166632526983, -5.676582343749999815 ) ) ;
#26463=CARTESIAN_POINT ( 'NONE',  ( 0.000000000000000000, 300.0000000000000000, 0.000000000000000000 ) ) ;
#26468=CARTESIAN_POINT ( 'NONE',  ( -2.085542519210945728E-15, 9.531249996586018014, 11.35316468750000141 ) ) ;
#26472=CARTESIAN_POINT ( 'NONE',  ( -6.676582343750001591, 287.5312500017070079, 0.000000000000000000 ) ) ;
#26476=CARTESIAN_POINT ( 'NONE',  ( -8.311093377946841443, 118.9062499965860269, 8.311093377946830785 ) ) ;
#26477=CARTESIAN_POINT ( 'NONE',  ( -2.679491924311235618, 95.41666665983868256, 10.00000000000000000 ) ) ;
#26483=CARTESIAN_POINT ( 'NONE',  ( -5.010106067795776497, 225.9999999999999716, 8.679299243466562785 ) ) ;
#26484=CARTESIAN_POINT ( 'NONE',  ( -2.765530957081996810, 294.4218750017069510, -6.676582343750003368 ) ) ;
#26487=CARTESIAN_POINT ( 'NONE',  ( 3.042071309553159519, 169.7395833299193839, 11.35316468750000141 ) ) ;
#26489=CARTESIAN_POINT ( 'NONE',  ( 10.00000000000000178, 206.8749999931720538, 0.000000000000000000 ) ) ;
#26490=CARTESIAN_POINT ( 'NONE',  ( -5.000000000000026645, 193.3333333333333712, 8.660254037844424602 ) ) ;
#26495=CARTESIAN_POINT ( 'NONE',  ( 5.676582343749993598, 155.2604166632526983, 9.832129032723422313 ) ) ;
#26500=CARTESIAN_POINT ( 'NONE',  ( -2.085542519210945728E-15, 59.84374999658602690, 11.35316468750000141 ) ) ;
#26504=ORIENTED_EDGE ( 'NONE', *, *, #45031, .F. ) ;
#26506=CARTESIAN_POINT ( 'NONE',  ( -4.242640687119286547, 288.9375000034140157, -4.242640687119286547 ) ) ;
#26513=CARTESIAN_POINT ( 'NONE',  ( -3.673940397442060854E-16, 294.7500000000000000, -6.000000000000001776 ) ) ;
#26516=AXIS2_PLACEMENT_3D ( 'NONE', #54515, #37530, #38277 ) ;
#26518=AXIS2_PLACEMENT_3D ( 'NONE', #66655, #37999, #60997 ) ;
#26526=EDGE_CURVE ( 'NONE', #58121, #15471, #29126, .T. ) ;
#26533=CARTESIAN_POINT ( 'NONE',  ( -8.660254037844387298, 67.08333333333334281, -5.000000000000004441 ) ) ;
#26535=CARTESIAN_POINT ( 'NONE',  ( -6.000000000000000888, 292.0625000000000000, 2.485281374238575758 ) ) ;
#26546=DIRECTION ( 'NONE',  ( -0.000000000000000000, 1.000000000000000000, -0.000000000000000000 ) ) ;
#26547=CARTESIAN_POINT ( 'NONE',  ( -7.320508075688778149, 183.1250000000000284, 7.320508075688769267 ) ) ;
#26548=CARTESIAN_POINT ( 'NONE',  ( 0.000000000000000000, 300.0000000000000000, 10.00000000000000178 ) ) ;
#26550=CARTESIAN_POINT ( 'NONE',  ( 3.042071309553167069, 157.1354166632526983, -11.35316468749999785 ) ) ;
#26558=CARTESIAN_POINT ( 'NONE',  ( 8.311093377946834337, 20.46874999658601624, 8.311093377946839666 ) ) ;
#26559=CARTESIAN_POINT ( 'NONE',  ( 10.00000000000000178, 96.87499999317203958, 0.000000000000000000 ) ) ;
#26561=CARTESIAN_POINT ( 'NONE',  ( 5.000000000000001776, 32.70833332650536107, -8.660254037844389075 ) ) ;
#26566=CARTESIAN_POINT ( 'NONE',  ( 8.660254037844389075, 47.29166665983870388, -5.000000000000000000 ) ) ;
#26569=DIRECTION ( 'NONE',  ( -0.000000000000000000, 1.000000000000000000, -0.000000000000000000 ) ) ;
#26575=CARTESIAN_POINT ( 'NONE',  ( -8.660254037844390851, 222.9166666666666856, 4.999999999999998224 ) ) ;
#26576=CARTESIAN_POINT ( 'NONE',  ( 1.224646799147353454E-15, 300.0000000000000000, -10.00000000000000178 ) ) ;
#26579=CARTESIAN_POINT ( 'NONE',  ( -3.042071309553164404, 132.2395833299193555, -11.35316468749999963 ) ) ;
#26580=ORIENTED_EDGE ( 'NONE', *, *, #72251, .T. ) ;
#26586=CARTESIAN_POINT ( 'NONE',  ( -4.999999999999998224, 153.5416666598387110, -8.660254037844389075 ) ) ;
#26588=CARTESIAN_POINT ( 'NONE',  ( 11.35316468749999785, 130.5729166632526983, 3.042071309553174174 ) ) ;
#26590=DIRECTION ( 'NONE',  ( -0.000000000000000000, 1.000000000000000000, -0.000000000000000000 ) ) ;
#26595=CARTESIAN_POINT ( 'NONE',  ( 8.311093377946834337, 115.4687499965860127, 8.311093377946839666 ) ) ;
#26600=CARTESIAN_POINT ( 'NONE',  ( 5.676582343750001591, 21.92708332991935194, -9.832129032723420536 ) ) ;
#26606=CARTESIAN_POINT ( 'NONE',  ( 4.242640687119285658, 298.6875000034139589, -4.242640687119286547 ) ) ;
#26607=CARTESIAN_POINT ( 'NONE',  ( -3.673940397442060854E-16, 296.7500000000000000, -6.000000000000001776 ) ) ;
#26610=CARTESIAN_POINT ( 'NONE',  ( -8.311093377946836114, 142.9687499965859843, -8.311093377946837890 ) ) ;
#26613=EDGE_CURVE ( 'NONE', #55859, #3208, #61412, .T. ) ;
#26622=VERTEX_POINT ( 'NONE', #33508 ) ;
#26627=CARTESIAN_POINT ( 'NONE',  ( -9.832129032723418760, 192.8645833299193839, -5.676582343750004256 ) ) ;
#26631=CARTESIAN_POINT ( 'NONE',  ( 2.765530957082001251, 288.7656250017069510, 6.676582343749999815 ) ) ;
#26632=CARTESIAN_POINT ( 'NONE',  ( 9.498558403365325509E-13, 68.75000000000008527, 10.00000000000000178 ) ) ;
#26639=DIRECTION ( 'NONE',  ( 0.000000000000000000, 0.000000000000000000, 1.000000000000000000 ) ) ;
#26643=CARTESIAN_POINT ( 'NONE',  ( 0.000000000000000000, 300.0000000000000000, 10.00000000000000178 ) ) ;
#26645=CARTESIAN_POINT ( 'NONE',  ( -5.676582343750006032, 114.4270833299193555, 9.832129032723418760 ) ) ;
#26651=CARTESIAN_POINT ( 'NONE',  ( 4.242640687119285658, 298.6250000000000000, -4.242640687119286547 ) ) ;
#26654=CARTESIAN_POINT ( 'NONE',  ( 8.311093377946834337, 220.1562499965860127, 8.311093377946839666 ) ) ;
#26656=ADVANCED_FACE ( 'NONE', ( #66697 ), #67449, .T. ) ;
#26659=CARTESIAN_POINT ( 'NONE',  ( -5.676582343749998039, 212.7604166632526699, -9.832129032723420536 ) ) ;
#26666=CARTESIAN_POINT ( 'NONE',  ( 9.832129032723416984, 85.36458332991936970, 5.676582343750006032 ) ) ;
#26673=CARTESIAN_POINT ( 'NONE',  ( 5.676582343750001591, 91.61458332991935549, -9.832129032723420536 ) ) ;
#26675=CARTESIAN_POINT ( 'NONE',  ( 2.679491924311075302, 205.8333333265053682, 10.00000000000008704 ) ) ;
#26681=CARTESIAN_POINT ( 'NONE',  ( 9.832129032723420536, 86.19791666325268409, -5.676582343749999815 ) ) ;
#26686=CARTESIAN_POINT ( 'NONE',  ( -10.00000000000000355, 179.5833333265053966, 2.679491924311223183 ) ) ;
#26687=CARTESIAN_POINT ( 'NONE',  ( 2.485281374238175189, 296.7500000034139589, -6.000000000000396128 ) ) ;
#26688=CARTESIAN_POINT ( 'NONE',  ( -2.085542519210945728E-15, 74.84374999658602690, 11.35316468750000141 ) ) ;
#26689=CARTESIAN_POINT ( 'NONE',  ( -4.721056650415999201, 294.3281250017069510, -4.721056650415999201 ) ) ;
#26693=CARTESIAN_POINT ( 'NONE',  ( 5.676582343749993598, 204.9479166632526983, 9.832129032723422313 ) ) ;
#26699=CARTESIAN_POINT ( 'NONE',  ( 9.832129032723420536, 201.1979166632526983, -5.676582343749999815 ) ) ;
#26700=CARTESIAN_POINT ( 'NONE',  ( 6.123233995736767268E-16, 193.1249999931720254, -10.00000000000000178 ) ) ;
#26702=CARTESIAN_POINT ( 'NONE',  ( -6.676582343750003368, 299.3906250017069510, -2.765530957081996810 ) ) ;
#26705=CARTESIAN_POINT ( 'NONE',  ( -5.676582343750006032, 194.4270833299193839, 9.832129032723418760 ) ) ;
#26710=VERTEX_POINT ( 'NONE', #16112 ) ;
#26712=CARTESIAN_POINT ( 'NONE',  ( -1.836970198721029983E-15, 13.75000000000000000, 10.00000000000000178 ) ) ;
#26718=CARTESIAN_POINT ( 'NONE',  ( -1.836970198721029983E-15, 185.6249999931720538, 10.00000000000000178 ) ) ;
#26729=EDGE_LOOP ( 'NONE', ( #20076, #49715, #74391, #43399 ) ) ;
#26730=VERTEX_POINT ( 'NONE', #4449 ) ;
#26732=CARTESIAN_POINT ( 'NONE',  ( 11.35316468749999963, 81.30208332991935549, -3.042071309553165293 ) ) ;
#26735=CYLINDRICAL_SURFACE ( 'NONE', #40923, 10.00000000000000178 ) ;
#26737=CARTESIAN_POINT ( 'NONE',  ( 2.765530957081996366, 290.2968750017069510, -6.676582343750002480 ) ) ;
#26741=ADVANCED_FACE ( 'NONE', ( #27440 ), #28665, .F. ) ;
#26748=CARTESIAN_POINT ( 'NONE',  ( -2.085542519210945728E-15, 169.8437499965860127, 11.35316468750000141 ) ) ;
#26751=CARTESIAN_POINT ( 'NONE',  ( -3.673940397442060854E-16, 292.8125000034140157, -6.000000000000001776 ) ) ;
#26757=CARTESIAN_POINT ( 'NONE',  ( 3.042071309553167069, 46.82291666325267698, -11.35316468749999785 ) ) ;
#26759=CARTESIAN_POINT ( 'NONE',  ( -2.679491924311225848, 23.33333332650536818, -10.00000000000000178 ) ) ;
#26763=CARTESIAN_POINT ( 'NONE',  ( -10.00000000000000178, 169.3749999931720538, -1.224646799147353454E-15 ) ) ;
#26764=EDGE_CURVE ( 'NONE', #2022, #73747, #51807, .T. ) ;
#26765=CARTESIAN_POINT ( 'NONE',  ( -11.35316468750000141, 43.28124999658601268, -1.390361679473963753E-15 ) ) ;
#26768=CARTESIAN_POINT ( 'NONE',  ( -2.485281374238159646, 299.1875000000000000, 6.000000000000414779 ) ) ;
#26771=CARTESIAN_POINT ( 'NONE',  ( 8.311093377946834337, 50.15624999658601268, 8.311093377946839666 ) ) ;
#26773=CARTESIAN_POINT ( 'NONE',  ( 4.999999999999992895, 204.1666666666666856, 8.660254037844390851 ) ) ;
#26774=CARTESIAN_POINT ( 'NONE',  ( 11.35316468749999785, 165.5729166632526415, 3.042071309553174174 ) ) ;
#26775=CARTESIAN_POINT ( 'NONE',  ( 7.320508075688771044, 131.2499999931720254, 7.320508075688775484 ) ) ;
#26776=AXIS2_PLACEMENT_3D ( 'NONE', #3612, #10390, #73388 ) ;
#26779=CARTESIAN_POINT ( 'NONE',  ( 8.311093377946837890, 41.71874999658601979, -8.311093377946837890 ) ) ;
#26781=ORIENTED_EDGE ( 'NONE', *, *, #27397, .T. ) ;
#26786=CARTESIAN_POINT ( 'NONE',  ( 3.042071309553167513, 166.8229166632526983, -11.35316468749999785 ) ) ;
#26791=EDGE_CURVE ( 'NONE', #9554, #40886, #67247, .T. ) ;
#26796=CYLINDRICAL_SURFACE ( 'NONE', #18256, 6.000000000000001776 ) ;
#26797=CARTESIAN_POINT ( 'NONE',  ( -11.35316468749999785, 118.3854166632526557, -3.042071309553167513 ) ) ;
#26800=VERTEX_POINT ( 'NONE', #34814 ) ;
#26824=CARTESIAN_POINT ( 'NONE',  ( -3.673940397442060854E-16, 288.7500000000000000, -6.000000000000001776 ) ) ;
#26828=CARTESIAN_POINT ( 'NONE',  ( 5.000000000000001776, 110.8333333333333428, -8.660254037844389075 ) ) ;
#26831=CARTESIAN_POINT ( 'NONE',  ( 4.721056650416000089, 293.9843750017070079, 4.721056650415999201 ) ) ;
#26834=CARTESIAN_POINT ( 'NONE',  ( 1.224646799147353454E-15, 300.0000000000000000, -10.00000000000000178 ) ) ;
#26839=CARTESIAN_POINT ( 'NONE',  ( 0.000000000000000000, 255.9999999999999432, 0.000000000000000000 ) ) ;
#26844=CARTESIAN_POINT ( 'NONE',  ( 9.832129032723416984, 5.364583329919349275, 5.676582343750006032 ) ) ;
#26846=CARTESIAN_POINT ( 'NONE',  ( 11.35316468749999963, 201.3020833299193839, -3.042071309553165293 ) ) ;
#26847=CARTESIAN_POINT ( 'NONE',  ( 11.35316468750000141, 0.7812499965860162376, 0.000000000000000000 ) ) ;
#26852=VERTEX_POINT ( 'NONE', #45729 ) ;
#26855=CARTESIAN_POINT ( 'NONE',  ( 9.832129032723420536, 11.19791666325268409, -5.676582343749999815 ) ) ;
#26859=DIRECTION ( 'NONE',  ( 0.000000000000000000, 0.000000000000000000, 1.000000000000000000 ) ) ;
#26861=CARTESIAN_POINT ( 'NONE',  ( -3.042071309553173730, 9.322916663252684089, 11.35316468749999785 ) ) ;
#26863=CARTESIAN_POINT ( 'NONE',  ( 9.832129032723416984, 115.3645833299193555, 5.676582343750006032 ) ) ;
#26865=CARTESIAN_POINT ( 'NONE',  ( 10.00000000000000178, 91.87499999317203958, 0.000000000000000000 ) ) ;
#26869=CARTESIAN_POINT ( 'NONE',  ( 2.679491924311224516, 143.9583333333333428, 10.00000000000000888 ) ) ;
#26871=CARTESIAN_POINT ( 'NONE',  ( -8.660254037844390851, 117.0833333333333570, -5.000000000000007105 ) ) ;
#26872=CARTESIAN_POINT ( 'NONE',  ( 6.676582343750001591, 290.1093750017069510, -8.176455196517173205E-16 ) ) ;
#26876=CARTESIAN_POINT ( 'NONE',  ( -2.679491924311235618, 210.4166666598386826, 10.00000000000000000 ) ) ;
#26879=ORIENTED_EDGE ( 'NONE', *, *, #56984, .F. ) ;
#26881=CARTESIAN_POINT ( 'NONE',  ( -3.042071309553173730, 159.6354166632526699, 11.35316468749999785 ) ) ;
#26884=CARTESIAN_POINT ( 'NONE',  ( 6.951808397369818766E-16, 57.34374999658601979, -11.35316468750000141 ) ) ;
#26889=VECTOR ( 'NONE', #5110, 1000.000000000000000 ) ;
#26891=CARTESIAN_POINT ( 'NONE',  ( -2.485281374238571761, 289.8750000034139589, -6.000000000000003553 ) ) ;
#26901=VERTEX_POINT ( 'NONE', #40452 ) ;
#26909=ORIENTED_EDGE ( 'NONE', *, *, #66787, .F. ) ;
#26917=CARTESIAN_POINT ( 'NONE',  ( -7.320508075688773708, 61.87500000000000000, -7.320508075688774596 ) ) ;
#26920=CARTESIAN_POINT ( 'NONE',  ( -6.000000000000000888, 293.0625000000000000, 2.485281374238575758 ) ) ;
#26928=CARTESIAN_POINT ( 'NONE',  ( 7.320508075688774596, 185.6249999999999716, -7.320508075688774596 ) ) ;
#26931=CARTESIAN_POINT ( 'NONE',  ( 6.951808397369818766E-16, 157.3437499965860127, -11.35316468750000141 ) ) ;
#26938=CARTESIAN_POINT ( 'NONE',  ( 9.832129032723416984, 25.67708332991935194, 5.676582343750006032 ) ) ;
#26945=CARTESIAN_POINT ( 'NONE',  ( 10.00000000000000178, 51.87499999317203248, 0.000000000000000000 ) ) ;
#26948=CARTESIAN_POINT ( 'NONE',  ( 2.679491924310263951, 53.95833333333325044, 10.00000000000055067 ) ) ;
#26951=CARTESIAN_POINT ( 'NONE',  ( 5.000000000000010658, 160.8333333333333428, -8.660254037844403285 ) ) ;
#26958=CARTESIAN_POINT ( 'NONE',  ( 11.35316468749999963, 125.9895833299193271, -3.042071309553165293 ) ) ;
#26965=CARTESIAN_POINT ( 'NONE',  ( 3.042071309553167513, 121.8229166632526841, -11.35316468749999785 ) ) ;
#26973=CARTESIAN_POINT ( 'NONE',  ( -5.676582343749998039, 112.7604166632526841, -9.832129032723420536 ) ) ;
#26978=CARTESIAN_POINT ( 'NONE',  ( 3.042071309553167069, 17.13541666325268409, -11.35316468749999785 ) ) ;
#26979=ORIENTED_EDGE ( 'NONE', *, *, #7189, .F. ) ;
#26984=CARTESIAN_POINT ( 'NONE',  ( -2.765530957081996810, 289.2656250017069510, -6.676582343750003368 ) ) ;
#26985=DIRECTION ( 'NONE',  ( 0.000000000000000000, 0.000000000000000000, 1.000000000000000000 ) ) ;
#26987=EDGE_LOOP ( 'NONE', ( #25196, #65036, #57167, #17119 ) ) ;
#26988=CARTESIAN_POINT ( 'NONE',  ( 5.676582343749993598, 140.2604166632526983, 9.832129032723422313 ) ) ;
#27006=CARTESIAN_POINT ( 'NONE',  ( -11.35316468749999785, 188.0729166632526983, -3.042071309553167513 ) ) ;
#27008=CARTESIAN_POINT ( 'NONE',  ( -2.485281374238895502, 290.8750000034139589, -5.999999999999677591 ) ) ;
#27009=CARTESIAN_POINT ( 'NONE',  ( 6.676582343750003368, 289.8906250017069510, 2.765530957081995478 ) ) ;
#27011=CARTESIAN_POINT ( 'NONE',  ( 2.250000000000000000, 284.0000000000000000, 7.677076266392047543 ) ) ;
#27012=CARTESIAN_POINT ( 'NONE',  ( -2.679491924310867912, 68.54166666666671404, 10.00000000000021494 ) ) ;
#27018=CARTESIAN_POINT ( 'NONE',  ( 4.999999999999993783, 166.0416666598387110, 8.660254037844390851 ) ) ;
#27026=CARTESIAN_POINT ( 'NONE',  ( -8.311093377946836114, 117.9687499965860127, -8.311093377946837890 ) ) ;
#27027=CARTESIAN_POINT ( 'NONE',  ( 10.00000000000000000, 211.6666666598386826, 2.679491924311235618 ) ) ;
#27032=VERTEX_POINT ( 'NONE', #65301 ) ;
#27034=CARTESIAN_POINT ( 'NONE',  ( 2.485281374238286656, 287.7500000034141294, -6.000000000000285105 ) ) ;
#27037=CARTESIAN_POINT ( 'NONE',  ( 9.832129032723420536, 201.5104166632526983, -5.676582343749999815 ) ) ;
#27039=CARTESIAN_POINT ( 'NONE',  ( 10.54825475571325022, 225.9999999999999716, 3.425896574385907112 ) ) ;
#27045=CARTESIAN_POINT ( 'NONE',  ( 11.35316468750000141, 100.7812499965860269, 0.000000000000000000 ) ) ;
#27046=ORIENTED_EDGE ( 'NONE', *, *, #33346, .T. ) ;
#27050=AXIS2_PLACEMENT_3D ( 'NONE', #43608, #13804, #48149 ) ;
#27052=CARTESIAN_POINT ( 'NONE',  ( 11.35316468749999785, 95.57291666325269830, 3.042071309553174174 ) ) ;
#27060=CARTESIAN_POINT ( 'NONE',  ( 9.832129032723416984, 90.36458332991935549, 5.676582343750006032 ) ) ;
#27064=CARTESIAN_POINT ( 'NONE',  ( 2.679491924311228956, 187.9166666598387394, -10.00000000000000000 ) ) ;
#27067=CARTESIAN_POINT ( 'NONE',  ( -11.35316468749999785, 78.38541666325266988, -3.042071309553167957 ) ) ;
#27068=CARTESIAN_POINT ( 'NONE',  ( -2.765530957081998586, 293.6406250017069510, 6.676582343750001591 ) ) ;
#27070=CARTESIAN_POINT ( 'NONE',  ( 8.311093377946837890, 211.4062499965860411, -8.311093377946837890 ) ) ;
#27076=CARTESIAN_POINT ( 'NONE',  ( -8.311093377946841443, 203.9062499965859843, 8.311093377946834337 ) ) ;
#27078=CARTESIAN_POINT ( 'NONE',  ( 7.347880794884121708E-16, 300.0000000000000000, -6.000000000000001776 ) ) ;
#27080=CARTESIAN_POINT ( 'NONE',  ( 5.676582343749993598, 200.2604166632526983, 9.832129032723422313 ) ) ;
#27087=CARTESIAN_POINT ( 'NONE',  ( 4.999999999999993783, 9.166666666666666075, 8.660254037844390851 ) ) ;
#27104=ORIENTED_EDGE ( 'NONE', *, *, #12372, .F. ) ;
#27108=CARTESIAN_POINT ( 'NONE',  ( -9.832129032723420536, 69.01041666325268409, 5.676582343749997150 ) ) ;
#27113=CARTESIAN_POINT ( 'NONE',  ( -2.765530957081998142, 288.7968750017069510, 6.676582343750000703 ) ) ;
#27119=VERTEX_POINT ( 'NONE', #57359 ) ;
#27122=CARTESIAN_POINT ( 'NONE',  ( -11.35316468749999785, 163.3854166632526983, -3.042071309553167513 ) ) ;
#27130=CARTESIAN_POINT ( 'NONE',  ( 9.832129032723416984, 50.36458332991934839, 5.676582343750006032 ) ) ;
#27131=( BOUNDED_CURVE ( )  B_SPLINE_CURVE ( 2, ( #55073, #65628, #43738, #2639, #59608, #60719, #31681, #7921, #48273, #48642, #13559, #31298, #14304 ),
 .UNSPECIFIED., .F., .F. ) 
 B_SPLINE_CURVE_WITH_KNOTS ( ( 3, 2, 2, 2, 2, 2, 3 ),
 ( 1.868286558610450454, 1.873520558097138355, 1.878754557583826035, 1.883988557070513936, 1.889222556557201838, 1.894456556043889517, 1.899690555530577418 ),
 .UNSPECIFIED. ) 
 CURVE ( )  GEOMETRIC_REPRESENTATION_ITEM ( )  RATIONAL_B_SPLINE_CURVE ( ( 1.000000000000194289, 0.9659258262888741342, 1.000000000000000000, 0.9659258262890683122, 1.000000000000000000, 0.9659258262890683122, 1.000000000000000000, 0.9659258262890683122, 1.000000000000000000, 0.9659258262890683122, 1.000000000000000000, 0.9659258262890912938, 0.9999999999999770184 ) ) 
 REPRESENTATION_ITEM ( '' )  );
#27133=CARTESIAN_POINT ( 'NONE',  ( 10.00000000000000178, 27.08333332650536462, -2.679491924311226736 ) ) ;
#27137=CARTESIAN_POINT ( 'NONE',  ( 8.311093377946837890, 51.40624999658601979, -8.311093377946837890 ) ) ;
#27142=CARTESIAN_POINT ( 'NONE',  ( 9.832129032723416984, 40.36458332991934839, 5.676582343750006032 ) ) ;
#27145=CARTESIAN_POINT ( 'NONE',  ( -9.832129032723420536, 158.6979166632526983, 5.676582343749997150 ) ) ;
#27146=CARTESIAN_POINT ( 'NONE',  ( 10.00000000000000178, 141.8749999931720538, 0.000000000000000000 ) ) ;
#27149=CARTESIAN_POINT ( 'NONE',  ( 5.676582343750001591, 36.92708332991935549, -9.832129032723420536 ) ) ;
#27155=CARTESIAN_POINT ( 'NONE',  ( -5.000000000000001776, 6.666666666666670515, -8.660254037844392627 ) ) ;
#27156=CARTESIAN_POINT ( 'NONE',  ( 5.676582343750001591, 171.6145833299193555, -9.832129032723420536 ) ) ;
#27165=CARTESIAN_POINT ( 'NONE',  ( -9.832129032723418760, 113.1770833299193555, -5.676582343750004256 ) ) ;
#27186=CARTESIAN_POINT ( 'NONE',  ( 6.123233995736767268E-16, 73.12499999317203958, -10.00000000000000178 ) ) ;
#27188=ORIENTED_EDGE ( 'NONE', *, *, #28115, .F. ) ;
#27196=CARTESIAN_POINT ( 'NONE',  ( 5.000000000000001776, 125.8333333333333570, -8.660254037844389075 ) ) ;
#27198=CARTESIAN_POINT ( 'NONE',  ( 6.676582343750003368, 290.1718750017070079, -2.765530957081997254 ) ) ;
#27200=ORIENTED_EDGE ( 'NONE', *, *, #25586, .T. ) ;
#27210=LINE ( 'NONE', #50972, #16776 ) ;
#27211=CARTESIAN_POINT ( 'NONE',  ( -11.35316468750000141, 8.489583329919350163, 3.042071309553159963 ) ) ;
#27213=CARTESIAN_POINT ( 'NONE',  ( 6.951808397369818766E-16, 202.3437499965860127, -11.35316468750000141 ) ) ;
#27214=CARTESIAN_POINT ( 'NONE',  ( -2.679491924311235174, 135.4166666598387110, 10.00000000000000000 ) ) ;
#27221=CARTESIAN_POINT ( 'NONE',  ( -5.676582343750006032, 14.11458332991935016, 9.832129032723418760 ) ) ;
#27225=CARTESIAN_POINT ( 'NONE',  ( -2.249999999999998224, 283.9999999998748308, 5.427273999917394676 ) ) ;
#27227=CARTESIAN_POINT ( 'NONE',  ( -8.311093377946841443, 3.906249996586016682, 8.311093377946834337 ) ) ;
#27229=CARTESIAN_POINT ( 'NONE',  ( 11.35316468750000141, 120.7812499965860269, 0.000000000000000000 ) ) ;
#27230=CARTESIAN_POINT ( 'NONE',  ( 8.660254037844389075, 97.29166665983871098, -5.000000000000000000 ) ) ;
#27237=CARTESIAN_POINT ( 'NONE',  ( 8.248616681371277227E-12, 116.2499999999993747, -10.00000000000000178 ) ) ;
#27238=CARTESIAN_POINT ( 'NONE',  ( 2.765530957082001251, 290.9218750017070647, 6.676582343750000703 ) ) ;
#27249=CARTESIAN_POINT ( 'NONE',  ( -2.085542519210945728E-15, 159.8437499965860127, 11.35316468750000141 ) ) ;
#27250=( NAMED_UNIT ( * ) PLANE_ANGLE_UNIT ( ) SI_UNIT ( $, .RADIAN. ) );
#27253=CARTESIAN_POINT ( 'NONE',  ( -11.35316468749999785, 78.38541666325266988, -3.042071309553167513 ) ) ;
#27259=CARTESIAN_POINT ( 'NONE',  ( -4.242640687119286547, 287.9375000034140157, -4.242640687119286547 ) ) ;
#27277=ORIENTED_EDGE ( 'NONE', *, *, #4737, .T. ) ;
#27284=CARTESIAN_POINT ( 'NONE',  ( 10.00000000000000000, 74.79166666666667140, 2.679491924311236062 ) ) ;
#27286=CARTESIAN_POINT ( 'NONE',  ( 2.485281374238571317, 292.6875000000001137, -6.000000000000003553 ) ) ;
#27298=CARTESIAN_POINT ( 'NONE',  ( -2.679491924311235618, 193.5416666666666856, 10.00000000000000000 ) ) ;
#27301=CARTESIAN_POINT ( 'NONE',  ( 6.951808397369818766E-16, 172.3437499965860127, -11.35316468750000141 ) ) ;
#27303=CARTESIAN_POINT ( 'NONE',  ( 5.000000000000086153, 154.1666666666667993, 8.660254037844548947 ) ) ;
#27304=CYLINDRICAL_SURFACE ( 'NONE', #35880, 10.00000000000000178 ) ;
#27307=CARTESIAN_POINT ( 'NONE',  ( 9.832129032723420536, 21.51041666325268409, -5.676582343749999815 ) ) ;
#27313=CARTESIAN_POINT ( 'NONE',  ( -8.660254037844390851, 44.79166665983870388, 4.999999999999998224 ) ) ;
#27316=CARTESIAN_POINT ( 'NONE',  ( 2.679491924311225404, 101.0416666666666714, -9.999999999999982236 ) ) ;
#27326=CARTESIAN_POINT ( 'NONE',  ( 6.951808397369818766E-16, 137.0312499965860411, -11.35316468750000141 ) ) ;
#27338=CARTESIAN_POINT ( 'NONE',  ( 9.832129032723420536, 111.5104166632526841, -5.676582343749999815 ) ) ;
#27343=CARTESIAN_POINT ( 'NONE',  ( 9.832129032723420536, 36.51041666325267698, -5.676582343749999815 ) ) ;
#27348=ADVANCED_FACE ( 'NONE', ( #12423 ), #6780, .T. ) ;
#27351=CARTESIAN_POINT ( 'NONE',  ( 6.000000000000001776, 298.5625000034140157, -7.347880794884121708E-16 ) ) ;
#27353=EDGE_LOOP ( 'NONE', ( #36920, #1500 ) ) ;
#27354=CARTESIAN_POINT ( 'NONE',  ( -11.35316468750000141, 148.8020833299193555, 3.042071309553159963 ) ) ;
#27371=CARTESIAN_POINT ( 'NONE',  ( 8.311093377946834337, 185.1562499965860411, 8.311093377946839666 ) ) ;
#27373=CARTESIAN_POINT ( 'NONE',  ( 4.242640687119285658, 295.6249999999999432, -4.242640687119286547 ) ) ;
#27374=CARTESIAN_POINT ( 'NONE',  ( -2.765530957081996810, 288.2656250017069510, -6.676582343750002480 ) ) ;
#27376=CARTESIAN_POINT ( 'NONE',  ( -8.660254037844390851, 67.91666666666668561, 5.000000000000000000 ) ) ;
#27382=CARTESIAN_POINT ( 'NONE',  ( -8.660254037844387298, 8.958333326505366401, -5.000000000000004441 ) ) ;
#27386=CARTESIAN_POINT ( 'NONE',  ( -1.836970198721029983E-15, 143.7500000000000284, 10.00000000000000178 ) ) ;
#27388=LINE ( 'NONE', #26643, #64466 ) ;
#27390=CARTESIAN_POINT ( 'NONE',  ( 3.042071309553159519, 125.0520833299193555, 11.35316468750000141 ) ) ;
#27397=EDGE_CURVE ( 'NONE', #59649, #23374, #4745, .T. ) ;
#27398=CARTESIAN_POINT ( 'NONE',  ( 7.285275666675271822, 225.6005920617279799, -6.856447244518973250 ) ) ;
#27404=CARTESIAN_POINT ( 'NONE',  ( 9.832129032723416984, 205.6770833299193555, 5.676582343750006032 ) ) ;
#27410=CARTESIAN_POINT ( 'NONE',  ( 3.042071309553167069, 101.8229166632526699, -11.35316468749999785 ) ) ;
#27416=CARTESIAN_POINT ( 'NONE',  ( -9.832129032723420536, 98.69791666325269830, 5.676582343749997150 ) ) ;
#27420=CARTESIAN_POINT ( 'NONE',  ( 1.102182119232618108E-15, 287.3125000034140157, 6.000000000000001776 ) ) ;
#27424=CARTESIAN_POINT ( 'NONE',  ( 5.676582343750001591, 91.61458332991935549, -9.832129032723420536 ) ) ;
#27428=CARTESIAN_POINT ( 'NONE',  ( -7.320508075688773708, 183.7499999931719969, -7.320508075688774596 ) ) ;
#27430=CARTESIAN_POINT ( 'NONE',  ( 9.832129032723420536, 76.51041666325268409, -5.676582343749999815 ) ) ;
#27431=CARTESIAN_POINT ( 'NONE',  ( 6.676582343750003368, 291.0156250017069510, -2.765530957081997254 ) ) ;
#27433=CARTESIAN_POINT ( 'NONE',  ( 8.311093377946837890, 206.4062499965860127, -8.311093377946837890 ) ) ;
#27438=CARTESIAN_POINT ( 'NONE',  ( 11.35316468749999963, 205.9895833299193555, -3.042071309553165293 ) ) ;
#27440=FACE_OUTER_BOUND ( 'NONE', #63802, .T. ) ;
#27442=VECTOR ( 'NONE', #35148, 1000.000000000000000 ) ;
#27443=CARTESIAN_POINT ( 'NONE',  ( -3.042071309553173730, 194.6354166632526415, 11.35316468749999785 ) ) ;
#27451=CARTESIAN_POINT ( 'NONE',  ( 4.999999999999993783, 19.16666666666666785, 8.660254037844390851 ) ) ;
#27468=EDGE_CURVE ( 'NONE', #66396, #9485, #27210, .T. ) ;
#27472=EDGE_CURVE ( 'NONE', #28745, #27032, #5114, .T. ) ;
#27475=CARTESIAN_POINT ( 'NONE',  ( -3.042071309553164404, 77.55208332991932707, -11.35316468749999963 ) ) ;
#27480=CARTESIAN_POINT ( 'NONE',  ( 4.721056650416000089, 288.9843750017070079, 4.721056650415999201 ) ) ;
#27486=ORIENTED_EDGE ( 'NONE', *, *, #33369, .F. ) ;
#27490=CARTESIAN_POINT ( 'NONE',  ( 11.35316468749999785, 170.8854166632526983, 3.042071309553174174 ) ) ;
#27491=DIRECTION ( 'NONE',  ( -0.000000000000000000, 1.000000000000000000, -0.000000000000000000 ) ) ;
#27494=DIRECTION ( 'NONE',  ( -0.000000000000000000, 1.000000000000000000, -0.000000000000000000 ) ) ;
#27498=CARTESIAN_POINT ( 'NONE',  ( 5.676582343750001591, 56.61458332991934839, -9.832129032723420536 ) ) ;
#27499=EDGE_CURVE ( 'NONE', #60229, #49815, #12786, .T. ) ;
#27501=CARTESIAN_POINT ( 'NONE',  ( 7.320508075688774596, 27.49999999317203248, -7.320508075688774596 ) ) ;
#27503=EDGE_LOOP ( 'NONE', ( #16421, #52903, #48927, #22639, #43043, #25318, #58936, #4415, #10484 ) ) ;
#27505=CARTESIAN_POINT ( 'NONE',  ( -10.00000000000000000, 169.1666666598387394, -2.679491924311229845 ) ) ;
#27506=CARTESIAN_POINT ( 'NONE',  ( -8.311093377946841443, 48.90624999658600558, 8.311093377946830785 ) ) ;
#27507=AXIS2_PLACEMENT_3D ( 'NONE', #33879, #68927, #63259 ) ;
#27513=CARTESIAN_POINT ( 'NONE',  ( -8.311093377946836114, 52.65624999658601268, -8.311093377946837890 ) ) ;
#27515=CARTESIAN_POINT ( 'NONE',  ( 7.320508075688769267, 204.3750000000000284, 7.320508075688773708 ) ) ;
#27516=CARTESIAN_POINT ( 'NONE',  ( -9.832129032723420536, 178.6979166632526983, 5.676582343749997150 ) ) ;
#27517=AXIS2_PLACEMENT_3D ( 'NONE', #26839, #26075, #31759 ) ;
#27518=CARTESIAN_POINT ( 'NONE',  ( 4.999999999999993783, 141.0416666598387110, 8.660254037844390851 ) ) ;
#27521=CARTESIAN_POINT ( 'NONE',  ( -9.832129032723420536, 39.01041666325268409, 5.676582343749997150 ) ) ;
#27529=CARTESIAN_POINT ( 'NONE',  ( -8.311093377946836114, 162.6562499965860127, -8.311093377946837890 ) ) ;
#27538=CARTESIAN_POINT ( 'NONE',  ( 6.951808397369818766E-16, 122.3437499965860269, -11.35316468750000141 ) ) ;
#27564=( BOUNDED_CURVE ( )  B_SPLINE_CURVE ( 2, ( #25292, #49432, #48679, #26031, #55113, #8702, #31334, #49052, #47935 ),
 .UNSPECIFIED., .F., .F. ) 
 B_SPLINE_CURVE_WITH_KNOTS ( ( 3, 2, 2, 2, 3 ),
 ( 0.5624999999999981126, 0.5729166666666647423, 0.5833333333333314830, 0.5937499999999982236, 0.6041666666666648533 ),
 .UNSPECIFIED. ) 
 CURVE ( )  GEOMETRIC_REPRESENTATION_ITEM ( )  RATIONAL_B_SPLINE_CURVE ( ( 1.000000000000013767, 0.9238795325112729717, 1.000000000000000000, 0.9238795325112867385, 1.000000000000000000, 0.9238795325112867385, 1.000000000000000000, 0.9238795325112997281, 0.9999999999999870104 ) ) 
 REPRESENTATION_ITEM ( '' )  );
#27573=CARTESIAN_POINT ( 'NONE',  ( -7.320508075688778149, 123.1250000000000000, 7.320508075688769267 ) ) ;
#27575=CARTESIAN_POINT ( 'NONE',  ( -4.088227598258586603E-16, 291.3593750017070079, -6.676582343750001591 ) ) ;
#27586=CARTESIAN_POINT ( 'NONE',  ( -4.999999999999998224, 213.5416666598387110, -8.660254037844389075 ) ) ;
#27587=CARTESIAN_POINT ( 'NONE',  ( -11.35316468750000141, 13.48958332991935016, 3.042071309553159963 ) ) ;
#27589=CARTESIAN_POINT ( 'NONE',  ( -3.042071309553173730, 204.6354166632526699, 11.35316468749999785 ) ) ;
#27593=CARTESIAN_POINT ( 'NONE',  ( 0.000000000000000000, 300.0000000000000000, 0.000000000000000000 ) ) ;
#27594=ORIENTED_EDGE ( 'NONE', *, *, #33607, .F. ) ;
#27596=CARTESIAN_POINT ( 'NONE',  ( 8.311093377946834337, 5.156249996586015349, 8.311093377946839666 ) ) ;
#27600=DIRECTION ( 'NONE',  ( -0.000000000000000000, 1.000000000000000000, -0.000000000000000000 ) ) ;
#27602=CARTESIAN_POINT ( 'NONE',  ( -9.832129032723418760, 12.86458332991935194, -5.676582343750004256 ) ) ;
#27604=CARTESIAN_POINT ( 'NONE',  ( 9.832129032723420536, 131.1979166632526983, -5.676582343749999815 ) ) ;
#27605=EDGE_CURVE ( 'NONE', #25744, #27119, #43651, .T. ) ;
#27607=CARTESIAN_POINT ( 'NONE',  ( 7.320508075688774596, 102.4999999931720112, -7.320508075688774596 ) ) ;
#27609=CARTESIAN_POINT ( 'NONE',  ( -10.00000000000000355, 4.583333326505365513, 2.679491924311223183 ) ) ;
#27612=EDGE_LOOP ( 'NONE', ( #25459, #61523, #32456, #73197 ) ) ;
#27613=CARTESIAN_POINT ( 'NONE',  ( 11.35316468750000141, 1.093749996586016682, 0.000000000000000000 ) ) ;
#27615=CARTESIAN_POINT ( 'NONE',  ( 6.676582343750001591, 288.1093750017069510, -8.176455196517173205E-16 ) ) ;
#27616=DIRECTION ( 'NONE',  ( 0.000000000000000000, 0.000000000000000000, 1.000000000000000000 ) ) ;
#27622=VERTEX_POINT ( 'NONE', #17381 ) ;
#27624=CARTESIAN_POINT ( 'NONE',  ( 10.00000000000000000, 216.6666666598387110, 2.679491924311235618 ) ) ;
#27625=CARTESIAN_POINT ( 'NONE',  ( -11.35316468750000141, 168.8020833299193271, 3.042071309553159963 ) ) ;
#27629=CARTESIAN_POINT ( 'NONE',  ( 6.951808397369818766E-16, 77.34374999658601268, -11.35316468750000141 ) ) ;
#27634=EDGE_LOOP ( 'NONE', ( #68752, #70524, #37461, #6479 ) ) ;
#27645=EDGE_LOOP ( 'NONE', ( #25756, #48810, #64505, #43197 ) ) ;
#27653=ORIENTED_EDGE ( 'NONE', *, *, #67296, .F. ) ;
#27661=CARTESIAN_POINT ( 'NONE',  ( -4.999999999999998224, 81.66666666666667140, -8.660254037844389075 ) ) ;
#27665=CARTESIAN_POINT ( 'NONE',  ( -4.242640687119285658, 294.1249999999999432, 4.242640687119287435 ) ) ;
#27668=CARTESIAN_POINT ( 'NONE',  ( 0.000000000000000000, 300.0000000000000000, 10.00000000000000178 ) ) ;
#27675=CARTESIAN_POINT ( 'NONE',  ( 5.000000000000001776, 200.8333333333333428, -8.660254037844389075 ) ) ;
#27678=CARTESIAN_POINT ( 'NONE',  ( 11.35316468750000141, 166.0937499965860127, 0.000000000000000000 ) ) ;
#27683=CARTESIAN_POINT ( 'NONE',  ( 11.27292232226671054, 225.9999999999999432, 1.347431162485829281 ) ) ;
#27685=CARTESIAN_POINT ( 'NONE',  ( -3.042071309553164404, 27.55208332991935194, -11.35316468749999963 ) ) ;
#27689=( BOUNDED_CURVE ( )  B_SPLINE_CURVE ( 2, ( #254, #22858, #40593, #7005, #34953, #57968, #40968, #34582, #52288, #12649, #57587, #62846, #35323 ),
 .UNSPECIFIED., .F., .F. ) 
 B_SPLINE_CURVE_WITH_KNOTS ( ( 3, 2, 2, 2, 2, 2, 3 ),
 ( 2.433485766383421289, 2.438719635847170775, 2.443953505310920260, 2.449187374774670189, 2.454421244238419675, 2.459655113702169160, 2.464888983165918646 ),
 .UNSPECIFIED. ) 
 CURVE ( )  GEOMETRIC_REPRESENTATION_ITEM ( )  RATIONAL_B_SPLINE_CURVE ( ( 1.000000000000001998, 0.9659258262890662028, 1.000000000000000000, 0.9659258262890683122, 1.000000000000000000, 0.9659258262890683122, 1.000000000000000000, 0.9659258262890683122, 1.000000000000000000, 0.9659258262890683122, 1.000000000000000000, 0.9659258262891685654, 0.9999999999998997469 ) ) 
 REPRESENTATION_ITEM ( '' )  );
#27690=CARTESIAN_POINT ( 'NONE',  ( -8.660254037844390851, 59.79166665983870388, 4.999999999999998224 ) ) ;
#27695=CARTESIAN_POINT ( 'NONE',  ( 10.00000000000000000, 165.2083333333333712, -2.679491924311226736 ) ) ;
#27698=CARTESIAN_POINT ( 'NONE',  ( -10.00000000000011013, 197.5000000000000568, -1.224646799147366470E-15 ) ) ;
#27702=CARTESIAN_POINT ( 'NONE',  ( 9.832129032723420536, 141.1979166632526699, -5.676582343749999815 ) ) ;
#27716=CARTESIAN_POINT ( 'NONE',  ( -11.35316468750000141, 118.5937499965860269, -1.390361679473963753E-15 ) ) ;
#27720=CARTESIAN_POINT ( 'NONE',  ( 9.832129032723416984, 40.67708332991935549, 5.676582343750006032 ) ) ;
#27728=CARTESIAN_POINT ( 'NONE',  ( -2.485281374238572649, 297.2500000034140157, 6.000000000000002665 ) ) ;
#27730=CARTESIAN_POINT ( 'NONE',  ( 4.999999999999993783, 111.0416666598387110, 8.660254037844390851 ) ) ;
#27732=CARTESIAN_POINT ( 'NONE',  ( 8.311093377946837890, 156.7187499965860127, -8.311093377946837890 ) ) ;
#27739=AXIS2_PLACEMENT_3D ( 'NONE', #11934, #57981, #6286 ) ;
#27743=VERTEX_POINT ( 'NONE', #12201 ) ;
#27747=CARTESIAN_POINT ( 'NONE',  ( 10.00000000000000178, 35.00000000000000000, 0.000000000000000000 ) ) ;
#27750=CARTESIAN_POINT ( 'NONE',  ( -6.676582343750002480, 288.3906250017070079, -2.765530957081996810 ) ) ;
#27751=CARTESIAN_POINT ( 'NONE',  ( 7.320508075688772820, 35.62500000000000711, -7.320508075688772820 ) ) ;
#27754=AXIS2_PLACEMENT_3D ( 'NONE', #52805, #42205, #65595 ) ;
#27761=CARTESIAN_POINT ( 'NONE',  ( -10.00000000000000355, 152.7083333333333428, 2.679491924311223183 ) ) ;
#27765=CARTESIAN_POINT ( 'NONE',  ( -8.311093377946836114, 127.9687499965860269, -8.311093377946837890 ) ) ;
#27766=CARTESIAN_POINT ( 'NONE',  ( 2.679491924311228956, 212.9166666598386826, -10.00000000000000000 ) ) ;
#27768=AXIS2_PLACEMENT_3D ( 'NONE', #3012, #72028, #47906 ) ;
#27774=AXIS2_PLACEMENT_3D ( 'NONE', #67410, #21000, #8947 ) ;
#27775=CARTESIAN_POINT ( 'NONE',  ( 5.563815795553805899, 224.2175593924927739, 8.329924368427569448 ) ) ;
#27778=CARTESIAN_POINT ( 'NONE',  ( 8.311093377946837890, 201.7187499965860411, -8.311093377946837890 ) ) ;
#27785=CARTESIAN_POINT ( 'NONE',  ( 5.676582343749993598, 99.94791666325268409, 9.832129032723422313 ) ) ;
#27790=CARTESIAN_POINT ( 'NONE',  ( 7.320508075688890059, 40.62500000000008527, -7.320508075688890059 ) ) ;
#27792=CARTESIAN_POINT ( 'NONE',  ( -9.832129032723420536, 108.6979166632526983, 5.676582343749997150 ) ) ;
#27795=ADVANCED_FACE ( 'NONE', ( #29564 ), #1283, .T. ) ;
#27797=LINE ( 'NONE', #43283, #9318 ) ;
#27801=CARTESIAN_POINT ( 'NONE',  ( -11.35316468750000141, 83.28124999658602690, -1.390361679473963753E-15 ) ) ;
#27808=CARTESIAN_POINT ( 'NONE',  ( -5.000000000000005329, 185.2083333265053682, 8.660254037844387298 ) ) ;
#27811=CARTESIAN_POINT ( 'NONE',  ( -11.35316468749999785, 73.38541666325268409, -3.042071309553167957 ) ) ;
#27812=CARTESIAN_POINT ( 'NONE',  ( 2.765530957082001251, 288.7656250017068942, 6.676582343750000703 ) ) ;
#27815=CARTESIAN_POINT ( 'NONE',  ( -11.35316468750000141, 218.4895833299193271, 3.042071309553159963 ) ) ;
#27821=CARTESIAN_POINT ( 'NONE',  ( -2.085542519210945728E-15, 204.5312499965860411, 11.35316468750000141 ) ) ;
#27825=CARTESIAN_POINT ( 'NONE',  ( 6.676582343750001591, 298.9531250017069510, -8.176455196517173205E-16 ) ) ;
#27826=EDGE_CURVE ( 'NONE', #26800, #25744, #61048, .T. ) ;
#27828=CARTESIAN_POINT ( 'NONE',  ( 3.042071309553159519, 200.0520833299193555, 11.35316468750000141 ) ) ;
#27834=CARTESIAN_POINT ( 'NONE',  ( 2.679491924311222739, 13.95833333333333393, 10.00000000000000355 ) ) ;
#27836=AXIS2_PLACEMENT_3D ( 'NONE', #39694, #67259, #28005 ) ;
#27843=EDGE_LOOP ( 'NONE', ( #27277, #65551, #5399, #36341 ) ) ;
#27853=ORIENTED_EDGE ( 'NONE', *, *, #5374, .F. ) ;
#27856=CARTESIAN_POINT ( 'NONE',  ( 3.042071309553167069, 87.13541666325268409, -11.35316468749999785 ) ) ;
#27861=CARTESIAN_POINT ( 'NONE',  ( 1.226468279477575784E-15, 289.8593750017070079, 6.676582343750001591 ) ) ;
#27864=CARTESIAN_POINT ( 'NONE',  ( 9.832129032723420536, 196.1979166632526983, -5.676582343749999815 ) ) ;
#27869=CARTESIAN_POINT ( 'NONE',  ( 9.832129032723420536, 171.5104166632526983, -5.676582343749999815 ) ) ;
#27872=CARTESIAN_POINT ( 'NONE',  ( -2.664923566518097392E-11, 208.7499999999979252, 10.00000000000000178 ) ) ;
#27876=CARTESIAN_POINT ( 'NONE',  ( 5.676582343750001591, 61.61458332991935549, -9.832129032723420536 ) ) ;
#27882=CARTESIAN_POINT ( 'NONE',  ( 3.042071309553159519, 64.73958332991935549, 11.35316468750000141 ) ) ;
#27887=CARTESIAN_POINT ( 'NONE',  ( -8.660254037844390851, 12.91666666666666963, 4.999999999999998224 ) ) ;
#27889=CARTESIAN_POINT ( 'NONE',  ( 8.311093377946837890, 51.40624999658601268, -8.311093377946837890 ) ) ;
#27892=CARTESIAN_POINT ( 'NONE',  ( -8.311093377946841443, 168.9062499965860411, 8.311093377946830785 ) ) ;
#27893=EDGE_CURVE ( 'NONE', #70895, #58068, #48040, .T. ) ;
#27894=CARTESIAN_POINT ( 'NONE',  ( 7.320508075688774596, 137.4999999931720254, -7.320508075688774596 ) ) ;
#27898=CARTESIAN_POINT ( 'NONE',  ( 9.832129032723420536, 31.51041666325268764, -5.676582343749999815 ) ) ;
#27900=CARTESIAN_POINT ( 'NONE',  ( 8.311093377946837890, 181.4062499965860411, -8.311093377946837890 ) ) ;
#27907=CARTESIAN_POINT ( 'NONE',  ( 11.35316468749999963, 160.9895833299193555, -3.042071309553165293 ) ) ;
#27915=( BOUNDED_CURVE ( )  B_SPLINE_CURVE ( 2, ( #3535, #9943, #14458, #43509, #43895, #72180, #3921, #60868, #15957 ),
 .UNSPECIFIED., .F., .F. ) 
 B_SPLINE_CURVE_WITH_KNOTS ( ( 3, 2, 2, 2, 3 ),
 ( 0.02083333333333103887, 0.03124999999999771363, 0.04166666666666438146, 0.05208333333333105969, 0.06249999999999773792 ),
 .UNSPECIFIED. ) 
 CURVE ( )  GEOMETRIC_REPRESENTATION_ITEM ( )  RATIONAL_B_SPLINE_CURVE ( ( 1.000000000000016653, 0.9238795325112698631, 1.000000000000000000, 0.9238795325112867385, 1.000000000000000000, 0.9238795325112867385, 1.000000000000000000, 0.9238795325113032808, 0.9999999999999834577 ) ) 
 REPRESENTATION_ITEM ( '' )  );
#27918=CARTESIAN_POINT ( 'NONE',  ( 9.832129032723416984, 120.6770833299193555, 5.676582343750006032 ) ) ;
#27943=VERTEX_POINT ( 'NONE', #39591 ) ;
#27946=CARTESIAN_POINT ( 'NONE',  ( 1.102182119232618108E-15, 288.2500000000000000, 6.000000000000001776 ) ) ;
#27953=CARTESIAN_POINT ( 'NONE',  ( -10.00000000000000355, 127.7083333333333570, 2.679491924311223183 ) ) ;
#27964=CARTESIAN_POINT ( 'NONE',  ( -2.250000000000000000, 274.6666666666666288, 5.427076266392048431 ) ) ;
#27967=CARTESIAN_POINT ( 'NONE',  ( -8.660254037844387298, 93.95833332650536818, -5.000000000000004441 ) ) ;
#27969=CARTESIAN_POINT ( 'NONE',  ( 11.35316468750000141, 10.78124999658601624, 0.000000000000000000 ) ) ;
#27972=CARTESIAN_POINT ( 'NONE',  ( 11.35316468749999785, 210.8854166632526983, 3.042071309553174174 ) ) ;
#27973=CARTESIAN_POINT ( 'NONE',  ( 6.123233995736767268E-16, 133.1249999931720254, -10.00000000000000178 ) ) ;
#27974=CARTESIAN_POINT ( 'NONE',  ( -10.00000000000000000, 219.1666666598387110, -2.679491924311229845 ) ) ;
#27979=CARTESIAN_POINT ( 'NONE',  ( -9.832129032723420536, 18.69791666325268409, 5.676582343749997150 ) ) ;
#27981=CARTESIAN_POINT ( 'NONE',  ( 10.00000000000000000, 209.7916666666666856, 2.679491924311236062 ) ) ;
#27985=CARTESIAN_POINT ( 'NONE',  ( -9.832129032723420536, 3.697916663252683200, 5.676582343749997150 ) ) ;
#27988=CARTESIAN_POINT ( 'NONE',  ( -2.085542519210945728E-15, 134.5312499965860411, 11.35316468750000141 ) ) ;
#27989=CARTESIAN_POINT ( 'NONE',  ( -2.679491924311225848, 98.33333332650538239, -10.00000000000000178 ) ) ;
#27996=CARTESIAN_POINT ( 'NONE',  ( 6.676582343750004256, 290.0468750017070079, 2.765530957081995478 ) ) ;
#28005=DIRECTION ( 'NONE',  ( 0.000000000000000000, 0.000000000000000000, 1.000000000000000000 ) ) ;
#28007=CARTESIAN_POINT ( 'NONE',  ( -11.35316468750000141, 73.80208332991935549, 3.042071309553159963 ) ) ;
#28011=ORIENTED_EDGE ( 'NONE', *, *, #47224, .F. ) ;
#28031=ORIENTED_EDGE ( 'NONE', *, *, #43390, .F. ) ;
#28038=CARTESIAN_POINT ( 'NONE',  ( 8.660254037844389075, 75.41666666666667140, -5.000000000000000000 ) ) ;
#28040=CARTESIAN_POINT ( 'NONE',  ( -6.676582343750003368, 299.5468750017069510, -2.765530957081996810 ) ) ;
#28041=ADVANCED_FACE ( 'NONE', ( #14065 ), #11292, .T. ) ;
#28050=CARTESIAN_POINT ( 'NONE',  ( -8.660254037844387298, 202.0833333333333428, -5.000000000000004441 ) ) ;
#28053=CARTESIAN_POINT ( 'NONE',  ( -5.676582343749998039, 172.7604166632526983, -9.832129032723420536 ) ) ;
#28058=ORIENTED_EDGE ( 'NONE', *, *, #35388, .F. ) ;
#28059=CARTESIAN_POINT ( 'NONE',  ( 3.042071309553167069, 27.13541666325268409, -11.35316468749999785 ) ) ;
#28066=CARTESIAN_POINT ( 'NONE',  ( 6.123233995736767268E-16, 58.12499999317203248, -10.00000000000000178 ) ) ;
#28075=CARTESIAN_POINT ( 'NONE',  ( -2.679491924311961704, 86.45833333333341386, -9.999999999999579003 ) ) ;
#28077=CARTESIAN_POINT ( 'NONE',  ( 5.676582343750001591, 146.6145833299193555, -9.832129032723420536 ) ) ;
#28078=ORIENTED_EDGE ( 'NONE', *, *, #54865, .F. ) ;
#28088=CARTESIAN_POINT ( 'NONE',  ( -5.676582343749998039, 132.7604166632526983, -9.832129032723420536 ) ) ;
#28092=CARTESIAN_POINT ( 'NONE',  ( 6.951808397369818766E-16, 42.34374999658601979, -11.35316468750000141 ) ) ;
#28094=DIRECTION ( 'NONE',  ( 0.000000000000000000, 0.000000000000000000, 1.000000000000000000 ) ) ;
#28095=CARTESIAN_POINT ( 'NONE',  ( -2.679491924311235174, 195.4166666598387394, 10.00000000000000000 ) ) ;
#28099=CARTESIAN_POINT ( 'NONE',  ( 1.102182119232618108E-15, 295.3125000034140157, 6.000000000000001776 ) ) ;
#28102=CARTESIAN_POINT ( 'NONE',  ( -9.832129032723418760, 158.1770833299193555, -5.676582343750004256 ) ) ;
#28105=AXIS2_PLACEMENT_3D ( 'NONE', #36805, #71859, #37174 ) ;
#28115=EDGE_CURVE ( 'NONE', #69413, #73838, #66790, .T. ) ;
#28121=CARTESIAN_POINT ( 'NONE',  ( -7.320508075688778149, 43.12500000000000000, 7.320508075688769267 ) ) ;
#28125=CARTESIAN_POINT ( 'NONE',  ( -4.088227598258586603E-16, 290.2031250017069510, -6.676582343750001591 ) ) ;
#28126=CARTESIAN_POINT ( 'NONE',  ( 9.999999999999998224, 34.79166666666667140, 2.679491924311235174 ) ) ;
#28132=CARTESIAN_POINT ( 'NONE',  ( 6.123233995736767268E-16, 8.124999993172032475, -10.00000000000000178 ) ) ;
#28136=CARTESIAN_POINT ( 'NONE',  ( 8.660254037844385522, 164.5833333333333428, 5.000000000000005329 ) ) ;
#28137=CARTESIAN_POINT ( 'NONE',  ( -2.485281374238990093, 299.8124999999999432, -5.999999999999583444 ) ) ;
#28140=CARTESIAN_POINT ( 'NONE',  ( -11.35316468749999785, 133.3854166632526699, -3.042071309553167513 ) ) ;
#28146=ORIENTED_EDGE ( 'NONE', *, *, #5394, .F. ) ;
#28147=CARTESIAN_POINT ( 'NONE',  ( 9.015042500306268636, 224.6398387169884074, 4.368317829918140660 ) ) ;
#28152=CARTESIAN_POINT ( 'NONE',  ( 11.35316468749999963, 211.3020833299193839, -3.042071309553165293 ) ) ;
#28160=DIRECTION ( 'NONE',  ( -0.000000000000000000, 1.000000000000000000, -0.000000000000000000 ) ) ;
#28161=CARTESIAN_POINT ( 'NONE',  ( 5.676582343749993598, 89.94791666325269830, 9.832129032723422313 ) ) ;
#28167=CARTESIAN_POINT ( 'NONE',  ( -8.311093377946836114, 102.6562499965860269, -8.311093377946837890 ) ) ;
#28171=CARTESIAN_POINT ( 'NONE',  ( -10.00000000000000355, 224.5833333265053398, 2.679491924311223183 ) ) ;
#28175=CARTESIAN_POINT ( 'NONE',  ( 8.311093377946834337, 105.1562499965860269, 8.311093377946839666 ) ) ;
#28178=DIRECTION ( 'NONE',  ( -0.000000000000000000, 1.000000000000000000, -0.000000000000000000 ) ) ;
#28180=CARTESIAN_POINT ( 'NONE',  ( -10.00000000000000178, 184.3749999931720538, -1.224646799147353454E-15 ) ) ;
#28183=CARTESIAN_POINT ( 'NONE',  ( 9.832129032723416984, 90.67708332991934128, 5.676582343750006032 ) ) ;
#28184=CARTESIAN_POINT ( 'NONE',  ( 6.676582343750004256, 288.8906250017070079, 2.765530957081995478 ) ) ;
#28188=CARTESIAN_POINT ( 'NONE',  ( 11.35316468750000141, 225.7812499965860127, 0.000000000000000000 ) ) ;
#28190=CARTESIAN_POINT ( 'NONE',  ( -4.999999999999998224, 68.54166665983869677, -8.660254037844389075 ) ) ;
#28193=CARTESIAN_POINT ( 'NONE',  ( -11.35316468750000141, 208.2812499965860411, -1.390361679473963753E-15 ) ) ;
#28195=CARTESIAN_POINT ( 'NONE',  ( -10.00000000000000355, 99.58333332650536818, 2.679491924311223183 ) ) ;
#28196=CARTESIAN_POINT ( 'NONE',  ( 1.226468279477575784E-15, 297.7031250017070079, 6.676582343750001591 ) ) ;
#28198=CARTESIAN_POINT ( 'NONE',  ( -8.311093377946841443, 189.2187499965860411, 8.311093377946834337 ) ) ;
#28203=VERTEX_POINT ( 'NONE', #6010 ) ;
#28207=CARTESIAN_POINT ( 'NONE',  ( -10.00000000000000355, 12.70833333333333570, 2.679491924311223183 ) ) ;
#28218=CARTESIAN_POINT ( 'NONE',  ( -1.836970198721029983E-15, 150.6249999931720538, 10.00000000000000178 ) ) ;
#28228=( BOUNDED_CURVE ( )  B_SPLINE_CURVE ( 2, ( #2340, #43822, #38171, #14760, #7999, #8365, #60044, #55155, #43061, #37800, #60421, #60795, #49475 ),
 .UNSPECIFIED., .F., .F. ) 
 B_SPLINE_CURVE_WITH_KNOTS ( ( 3, 2, 2, 2, 2, 2, 3 ),
 ( 0.7880434782608697342, 0.7898550724637682929, 0.7916666666666668517, 0.7934782608695654105, 0.7952898550724638582, 0.7971014492753624170, 0.7989130434782609758 ),
 .UNSPECIFIED. ) 
 CURVE ( )  GEOMETRIC_REPRESENTATION_ITEM ( )  RATIONAL_B_SPLINE_CURVE ( ( 0.9999999999999957812, 0.9659258262890725311, 1.000000000000000000, 0.9659258262890683122, 1.000000000000000000, 0.9659258262890683122, 1.000000000000000000, 0.9659258262890683122, 1.000000000000000000, 0.9659258262890683122, 1.000000000000000000, 0.9659258262890662028, 1.000000000000001998 ) ) 
 REPRESENTATION_ITEM ( '' )  );
#28231=CARTESIAN_POINT ( 'NONE',  ( -5.676582343749998039, 92.76041666325268409, -9.832129032723420536 ) ) ;
#28236=CARTESIAN_POINT ( 'NONE',  ( 2.765530957082001251, 290.9218750017070647, 6.676582343749999815 ) ) ;
#28239=CARTESIAN_POINT ( 'NONE',  ( 4.529167459315944555, 225.9997407208379911, 8.915528146188176351 ) ) ;
#28240=EDGE_CURVE ( 'NONE', #23989, #46215, #53354, .T. ) ;
#28241=CARTESIAN_POINT ( 'NONE',  ( 3.042071309553167069, 201.8229166632526415, -11.35316468749999785 ) ) ;
#28246=CARTESIAN_POINT ( 'NONE',  ( 5.676582343749993598, 170.2604166632526983, 9.832129032723422313 ) ) ;
#28253=CARTESIAN_POINT ( 'NONE',  ( 3.042071309553159519, 49.73958332991935549, 11.35316468750000141 ) ) ;
#28259=CARTESIAN_POINT ( 'NONE',  ( -10.00000000000000355, 169.5833333265053398, 2.679491924311223183 ) ) ;
#28260=CARTESIAN_POINT ( 'NONE',  ( 11.35316468749999963, 65.98958332991936970, -3.042071309553165293 ) ) ;
#28264=CARTESIAN_POINT ( 'NONE',  ( -10.00000000000000355, 12.70833333333333570, 2.679491924311223183 ) ) ;
#28266=CARTESIAN_POINT ( 'NONE',  ( -9.832129032723420536, 58.69791666325268409, 5.676582343749997150 ) ) ;
#28269=CARTESIAN_POINT ( 'NONE',  ( 5.676582343750001591, 176.6145833299193555, -9.832129032723420536 ) ) ;
#28271=CARTESIAN_POINT ( 'NONE',  ( 10.00000000000000000, 141.6666666598387110, 2.679491924311236062 ) ) ;
#28275=CARTESIAN_POINT ( 'NONE',  ( 9.832129032723416984, 30.67708332991935194, 5.676582343750006032 ) ) ;
#28277=CARTESIAN_POINT ( 'NONE',  ( -11.35316468750000141, 188.4895833299193555, 3.042071309553159963 ) ) ;
#28284=CARTESIAN_POINT ( 'NONE',  ( -11.35316468750000141, 168.4895833299193555, 3.042071309553159963 ) ) ;
#28291=CARTESIAN_POINT ( 'NONE',  ( 11.35316468749999785, 115.8854166632526841, 3.042071309553174174 ) ) ;
#28292=CARTESIAN_POINT ( 'NONE',  ( 10.00000000000000178, 11.87499999317203248, 0.000000000000000000 ) ) ;
#28309=CARTESIAN_POINT ( 'NONE',  ( 4.242640687119287435, 293.3750000000000000, 4.242640687119285658 ) ) ;
#28311=VECTOR ( 'NONE', #48903, 1000.000000000000000 ) ;
#28322=CARTESIAN_POINT ( 'NONE',  ( -5.000000000000005329, 123.3333333333333428, 8.660254037844387298 ) ) ;
#28324=CARTESIAN_POINT ( 'NONE',  ( 6.676582343750004256, 289.0468750017070079, 2.765530957081995478 ) ) ;
#28337=CARTESIAN_POINT ( 'NONE',  ( 9.832129032723416984, 20.36458332991935194, 5.676582343750006032 ) ) ;
#28338=CARTESIAN_POINT ( 'NONE',  ( -8.311093377946836114, 212.9687499965860411, -8.311093377946837890 ) ) ;
#28340=CARTESIAN_POINT ( 'NONE',  ( -1.836970198721029983E-15, 220.6249999931720538, 10.00000000000000178 ) ) ;
#28343=VERTEX_POINT ( 'NONE', #42168 ) ;
#28346=CARTESIAN_POINT ( 'NONE',  ( -9.832129032723420536, 23.69791666325268409, 5.676582343749997150 ) ) ;
#28351=CARTESIAN_POINT ( 'NONE',  ( -8.311093377946836114, 7.656249996586015349, -8.311093377946837890 ) ) ;
#28354=CARTESIAN_POINT ( 'NONE',  ( 3.042071309553167069, 131.8229166632526983, -11.35316468749999785 ) ) ;
#28355=CARTESIAN_POINT ( 'NONE',  ( 2.679491924311228956, 107.9166666598386826, -10.00000000000000000 ) ) ;
#28362=CARTESIAN_POINT ( 'NONE',  ( -10.00000000000000178, 154.3749999931720254, -1.224646799147353454E-15 ) ) ;
#28363=CARTESIAN_POINT ( 'NONE',  ( -2.765530957081996810, 291.4218750017070079, -6.676582343750003368 ) ) ;
#28364=CARTESIAN_POINT ( 'NONE',  ( 3.042071309553167513, 131.8229166632526983, -11.35316468749999785 ) ) ;
#28371=EDGE_LOOP ( 'NONE', ( #31702, #51160, #36195, #69310 ) ) ;
#28373=CARTESIAN_POINT ( 'NONE',  ( 4.999999999999993783, 216.0416666598387110, 8.660254037844390851 ) ) ;
#28376=CARTESIAN_POINT ( 'NONE',  ( -3.042071309553164404, 72.55208332991934128, -11.35316468749999963 ) ) ;
#28382=CARTESIAN_POINT ( 'NONE',  ( -10.00000000000000355, 109.5833333265053540, 2.679491924311223183 ) ) ;
#28389=CARTESIAN_POINT ( 'NONE',  ( 4.999999999999991118, 109.1666666666666714, 8.660254037844387298 ) ) ;
#28403=CARTESIAN_POINT ( 'NONE',  ( -6.000000000000003553, 291.9374999999999432, -2.485281374238571317 ) ) ;
#28409=CARTESIAN_POINT ( 'NONE',  ( 8.660254037844385522, 79.58333333333334281, 5.000000000000005329 ) ) ;
#28411=CARTESIAN_POINT ( 'NONE',  ( 2.485281374238575314, 288.3125000000000000, 6.000000000000000888 ) ) ;
#28414=CARTESIAN_POINT ( 'NONE',  ( 1.102182119232618108E-15, 294.2500000000000000, 6.000000000000001776 ) ) ;
#28417=CARTESIAN_POINT ( 'NONE',  ( 0.000000000000000000, 284.0000000000000000, 6.000000000000001776 ) ) ;
#28419=CARTESIAN_POINT ( 'NONE',  ( 7.320508075688771044, 56.24999999317203248, 7.320508075688775484 ) ) ;
#28423=CARTESIAN_POINT ( 'NONE',  ( -2.679491924311225848, 206.4583333333333712, -10.00000000000000178 ) ) ;
#28425=CARTESIAN_POINT ( 'NONE',  ( -3.042071309553173730, 164.6354166632526983, 11.35316468749999785 ) ) ;
#28429=EDGE_LOOP ( 'NONE', ( #32914, #28608, #39539, #67195 ) ) ;
#28431=CARTESIAN_POINT ( 'NONE',  ( 11.35316468749999963, 31.30208332991934839, -3.042071309553165293 ) ) ;
#28434=DIRECTION ( 'NONE',  ( -0.000000000000000000, 1.000000000000000000, -0.000000000000000000 ) ) ;
#28439=VECTOR ( 'NONE', #23536, 1000.000000000000000 ) ;
#28440=CARTESIAN_POINT ( 'NONE',  ( 6.123233995736767268E-16, 68.12499999317203958, -10.00000000000000178 ) ) ;
#28443=CARTESIAN_POINT ( 'NONE',  ( -1.173938163346586453E-11, 213.7499999999991189, 10.00000000000000178 ) ) ;
#28445=CARTESIAN_POINT ( 'NONE',  ( 7.320508075688774596, 102.4999999931720254, -7.320508075688774596 ) ) ;
#28452=CARTESIAN_POINT ( 'NONE',  ( -10.00000000000000000, 87.29166666666667140, -2.679491924311229401 ) ) ;
#28453=CARTESIAN_POINT ( 'NONE',  ( 3.042071309553167069, 136.8229166632526699, -11.35316468749999785 ) ) ;
#28464=CARTESIAN_POINT ( 'NONE',  ( 3.042071309553167513, 122.1354166632526841, -11.35316468749999785 ) ) ;
#28468=CARTESIAN_POINT ( 'NONE',  ( 11.35316468749999785, 40.88541666325268409, 3.042071309553174174 ) ) ;
#28476=CARTESIAN_POINT ( 'NONE',  ( -6.000000000000003553, 297.0000000034139589, -2.485281374238571317 ) ) ;
#28480=CARTESIAN_POINT ( 'NONE',  ( 11.35316468749999785, 150.8854166632527267, 3.042071309553174174 ) ) ;
#28486=ORIENTED_EDGE ( 'NONE', *, *, #9662, .T. ) ;
#28497=CARTESIAN_POINT ( 'NONE',  ( 10.00000000000000178, 45.00000000000000711, 0.000000000000000000 ) ) ;
#28500=CARTESIAN_POINT ( 'NONE',  ( 6.000000000000001776, 298.5000000000000000, -7.347880794884121708E-16 ) ) ;
#28510=CARTESIAN_POINT ( 'NONE',  ( -10.00000000000000355, 157.7083333333333712, 2.679491924311223183 ) ) ;
#28511=CARTESIAN_POINT ( 'NONE',  ( 0.000000000000000000, 300.0000000000000000, 0.000000000000000000 ) ) ;
#28514=CARTESIAN_POINT ( 'NONE',  ( -8.311093377946836114, 122.9687499965860127, -8.311093377946837890 ) ) ;
#28521=CARTESIAN_POINT ( 'NONE',  ( 4.012887317181695224, 224.0794175527780965, 9.164256819418794109 ) ) ;
#28526=CARTESIAN_POINT ( 'NONE',  ( -3.042071309553173730, 219.6354166632526699, 11.35316468749999785 ) ) ;
#28533=CARTESIAN_POINT ( 'NONE',  ( 8.311093377946834337, 100.1562499965860127, 8.311093377946839666 ) ) ;
#28539=CARTESIAN_POINT ( 'NONE',  ( -5.676582343749998039, 102.4479166632526841, -9.832129032723420536 ) ) ;
#28543=CARTESIAN_POINT ( 'NONE',  ( 7.320508075688774596, 222.4999999931719969, -7.320508075688774596 ) ) ;
#28547=CARTESIAN_POINT ( 'NONE',  ( 3.042071309553159519, 99.73958332991935549, 11.35316468750000141 ) ) ;
#28551=VERTEX_POINT ( 'NONE', #44794 ) ;
#28554=CARTESIAN_POINT ( 'NONE',  ( -2.679491924311235618, 200.4166666598386826, 10.00000000000000000 ) ) ;
#28557=CARTESIAN_POINT ( 'NONE',  ( 9.832129032723416984, 85.67708332991935549, 5.676582343750006032 ) ) ;
#28558=CARTESIAN_POINT ( 'NONE',  ( 1.226468279477575784E-15, 289.7031250017069510, 6.676582343750001591 ) ) ;
#28561=CARTESIAN_POINT ( 'NONE',  ( 5.676582343750001591, 216.6145833299193555, -9.832129032723420536 ) ) ;
#28564=LINE ( 'NONE', #50829, #15941 ) ;
#28565=CARTESIAN_POINT ( 'NONE',  ( 11.35316468749999963, 215.9895833299193271, -3.042071309553165293 ) ) ;
#28567=CARTESIAN_POINT ( 'NONE',  ( -2.765530957081996810, 297.2656250017069510, -6.676582343750003368 ) ) ;
#28569=CARTESIAN_POINT ( 'NONE',  ( -5.000000000000005329, 120.2083333265053824, 8.660254037844387298 ) ) ;
#28570=CARTESIAN_POINT ( 'NONE',  ( 11.35316468749999785, 210.8854166632526983, 3.042071309553174174 ) ) ;
#28580=CARTESIAN_POINT ( 'NONE',  ( 4.999999999999993783, 24.16666666666667140, 8.660254037844390851 ) ) ;
#28590=CARTESIAN_POINT ( 'NONE',  ( -4.721056650415999201, 296.3281250017069510, -4.721056650415999201 ) ) ;
#28594=PRODUCT_CONTEXT ( 'NONE', #20675, 'mechanical' ) ;
#28602=CARTESIAN_POINT ( 'NONE',  ( -3.042071309553173730, 89.63541666325268409, 11.35316468749999785 ) ) ;
#28608=ORIENTED_EDGE ( 'NONE', *, *, #67155, .T. ) ;
#28611=CARTESIAN_POINT ( 'NONE',  ( -11.35316468750000141, 203.4895833299193271, 3.042071309553159963 ) ) ;
#28616=CARTESIAN_POINT ( 'NONE',  ( 3.042071309553167069, 177.1354166632527267, -11.35316468749999785 ) ) ;
#28624=CARTESIAN_POINT ( 'NONE',  ( -11.35316468749999785, 58.07291666325269119, -3.042071309553167513 ) ) ;
#28630=CARTESIAN_POINT ( 'NONE',  ( 11.35316468749999963, 60.98958332991934839, -3.042071309553165293 ) ) ;
#28635=CARTESIAN_POINT ( 'NONE',  ( -11.35316468749999785, 53.07291666325266988, -3.042071309553167957 ) ) ;
#28638=CARTESIAN_POINT ( 'NONE',  ( -8.311093377946836114, 172.6562499965860411, -8.311093377946837890 ) ) ;
#28639=CARTESIAN_POINT ( 'NONE',  ( 7.320508075688771044, 141.2499999931720538, 7.320508075688775484 ) ) ;
#28641=CARTESIAN_POINT ( 'NONE',  ( 8.660254037844392627, 20.41666666666667140, -5.000000000000004441 ) ) ;
#28642=CARTESIAN_POINT ( 'NONE',  ( 11.35316468749999785, 50.88541666325269119, 3.042071309553174174 ) ) ;
#28643=CARTESIAN_POINT ( 'NONE',  ( -10.00000000000000000, 79.16666665983871098, -2.679491924311229845 ) ) ;
#28644=CARTESIAN_POINT ( 'NONE',  ( 11.35316468750000141, 175.7812499965860411, 0.000000000000000000 ) ) ;
#28650=CARTESIAN_POINT ( 'NONE',  ( 3.042071309553167513, 181.8229166632526983, -11.35316468749999785 ) ) ;
#28656=AXIS2_PLACEMENT_3D ( 'NONE', #26463, #49487, #20815 ) ;
#28658=CARTESIAN_POINT ( 'NONE',  ( 5.676582343749993598, 125.2604166632526841, 9.832129032723422313 ) ) ;
#28659=ORIENTED_EDGE ( 'NONE', *, *, #53389, .F. ) ;
#28662=EDGE_CURVE ( 'NONE', #52532, #33382, #68763, .T. ) ;
#28665=( BOUNDED_SURFACE ( )  B_SPLINE_SURFACE ( 1, 2, ( 
 ( #55395, #26702, #49722, #9738, #4827, #72738, #44807, #10477, #27825, #50834, #43306, #58015, #64022, #62892, #16863, #23655, #51962, #39888, #29687, #33883, #6684, #57254, #69307, #51207, #12334, #40262, #62522, #46289, #28196, #56883, #35367, #29324, #34624, #45179, #68192, #28567, #11224, #39525, #52334, #63636, #5567, #45542, #10849, #34253, #51575, #46662, #74594, #73845, #671, #16488, #34998, #11967, #22152, #57630, #5199, #74218, #58379, #22907, #22523, #6320, #45919, #68561, #69681, #68931, #17242, #63263, #11589, #5944, #17618, #28943, #299, #40636, #17994, #23278, #41012, #36093, #53811, #18368, #48132, #12691, #70060, #25486, #47024, #36460, #70782, #53446, #30060, #53072, #7051, #65853, #48500, #71506, #59836, #59111, #25114, #13055, #24391, #52703, #19830, #30791, #47399, #31155, #42834, #59474, #2120, #14163, #18738, #7787, #19095, #8518, #24017, #70422, #37196, #41746, #42100, #64756, #13423, #35725, #1037, #41382, #8150, #71138, #54187, #19461, #2493, #65111, #60196, #1407, #64394, #7419, #58741, #30426, #1767, #24748, #47759, #42473, #65490, #13782, #36826, #66230, #21691, #49630, #49998, #32670, #48871, #15655, #3610, #26224, #16028, #71879, #55680, #60571, #50368, #3995, #72645, #9650, #38318, #2863, #44717, #32288, #25851, #66602, #54929, #26984, #20193, #67732, #39061, #9266, #73385, #62062, #31535, #43212, #61324, #44346, #38696, #37572, #73015, #21325, #8895, #67356, #61697, #14532, #60946, #10019, #33051, #31908, #43970, #3238, #56050, #15281, #43587, #49244, #55302 ),
 ( #4359, #54556, #66979, #72260, #20573, #14908, #26606, #37947, #27351, #20948, #68101, #34906, #5474, #16765, #16390, #69587, #68836, #5850, #51484, #74495, #51866, #17523, #39429, #57541, #68465, #11502, #50739, #28843, #45086, #27728, #57914, #4734, #17149, #28476, #11135, #62428, #10754, #33791, #23554, #6223, #29226, #40539, #39792, #207, #45448, #56788, #10387, #52239, #63176, #5109, #63545, #573, #40171, #34535, #46566, #51114, #23185, #22804, #40913, #56413, #28099, #17900, #74126, #45825, #22428, #46196, #62796, #33413, #73753, #11870, #69211, #22059, #34158, #57158, #1673, #31057, #64295, #6587, #47303, #69962, #2395, #25392, #6950, #54085, #18270, #2029, #13326, #29594, #23925, #48407, #7324, #7690, #65017, #52605, #48035, #35999, #58644, #41285, #41651, #59379, #59016, #70685, #30329, #36363, #30697, #19003, #70328, #12602, #943, #35271, #47663, #58284, #19737, #18643, #42009, #46934, #53715, #24653, #35629, #52975, #25015, #29962, #19363, #42377, #8054, #71044, #63924, #1309, #24292, #64661, #12234, #12961, #53348, #65394, #13691, #36733, #59744, #71413, #9173, #21231, #20471, #9921, #61601, #4269, #54465, #49530, #55582, #26891, #48779, #20856, #9559, #71786, #43874, #32574, #37100, #72161, #66890, #61230, #20104, #55211, #8422, #3897, #26506, #54837, #43116, #43491, #32953, #37856, #49907, #3147, #66135, #2772, #60853, #55959, #8805, #14440, #37474, #15196, #27259, #44257, #72921, #50277, #31816, #60475, #67268, #38225, #26131, #73297, #25758, #42746, #49150, #15563, #66503 ) ),
 .UNSPECIFIED., .F., .F., .F. ) 
 B_SPLINE_SURFACE_WITH_KNOTS ( ( 2, 2 ),
 ( 3, 2, 2, 2, 2, 2, 2, 2, 2, 2, 2, 2, 2, 2, 2, 2, 2, 2, 2, 2, 2, 2, 2, 2, 2, 2, 2, 2, 2, 2, 2, 2, 2, 2, 2, 2, 2, 2, 2, 2, 2, 2, 2, 2, 2, 2, 2, 2, 2, 2, 2, 2, 2, 2, 2, 2, 2, 2, 2, 2, 2, 2, 2, 2, 2, 2, 2, 2, 2, 2, 2, 2, 2, 2, 2, 2, 2, 2, 2, 2, 2, 2, 2, 2, 2, 2, 2, 2, 2, 2, 2, 2, 2, 2, 2, 2, 3 ),
 ( 0.000000000000000000, 1.000000000000000000 ),
 ( 0.000000000000000000, 0.01041666666666666609, 0.02083333333333333218, 0.03125000000000000000, 0.04166666666666666435, 0.05208333333333333565, 0.06250000000000000000, 0.07291666666666667129, 0.08333333333333332871, 0.09375000000000000000, 0.1041666666666666713, 0.1145833333333333287, 0.1250000000000000000, 0.1354166666666666574, 0.1458333333333333426, 0.1562500000000000000, 0.1666666666666666574, 0.1770833333333333426, 0.1875000000000000000, 0.1979166666666666574, 0.2083333333333333426, 0.2187500000000000000, 0.2291666666666666574, 0.2395833333333333426, 0.2500000000000000000, 0.2604166666666666852, 0.2708333333333333148, 0.2812500000000000000, 0.2916666666666666852, 0.3020833333333333148, 0.3125000000000000000, 0.3229166666666666852, 0.3333333333333333148, 0.3437500000000000000, 0.3541666666666666852, 0.3645833333333333148, 0.3750000000000000000, 0.3854166666666666852, 0.3958333333333333148, 0.4062500000000000000, 0.4166666666666666852, 0.4270833333333333148, 0.4375000000000000000, 0.4479166666666666852, 0.4583333333333333148, 0.4687500000000000000, 0.4791666666666666852, 0.4895833333333333148, 0.5000000000000000000, 0.5104166666666666297, 0.5208333333333333703, 0.5312500000000000000, 0.5416666666666666297, 0.5520833333333333703, 0.5625000000000000000, 0.5729166666666666297, 0.5833333333333333703, 0.5937500000000000000, 0.6041666666666666297, 0.6145833333333333703, 0.6250000000000000000, 0.6354166666666666297, 0.6458333333333333703, 0.6562500000000000000, 0.6666666666666666297, 0.6770833333333333703, 0.6875000000000000000, 0.6979166666666666297, 0.7083333333333333703, 0.7187500000000000000, 0.7291666666666666297, 0.7395833333333333703, 0.7500000000000000000, 0.7604166666666666297, 0.7708333333333333703, 0.7812500000000000000, 0.7916666666666666297, 0.8020833333333333703, 0.8125000000000000000, 0.8229166666666666297, 0.8333333333333333703, 0.8437500000000000000, 0.8541666666666666297, 0.8645833333333333703, 0.8750000000000000000, 0.8854166666666666297, 0.8958333333333333703, 0.9062500000000000000, 0.9166666666666666297, 0.9270833333333333703, 0.9375000000000000000, 0.9479166666666666297, 0.9583333333333333703, 0.9687500000000000000, 0.9791666666666666297, 0.9895833333333333703, 1.000000000000000000 ),
 .UNSPECIFIED. ) 
 GEOMETRIC_REPRESENTATION_ITEM ( )  RATIONAL_B_SPLINE_SURFACE ( (
 ( 1.000000000000000000, 0.9238795325112867385, 1.000000000000000000, 0.9238795325112867385, 1.000000000000000000, 0.9238795325112867385, 1.000000000000000000, 0.9238795325112867385, 1.000000000000000000, 0.9238795325112867385, 1.000000000000000000, 0.9238795325112867385, 1.000000000000000000, 0.9238795325112867385, 1.000000000000000000, 0.9238795325112867385, 1.000000000000000000, 0.9238795325112867385, 1.000000000000000000, 0.9238795325112867385, 1.000000000000000000, 0.9238795325112867385, 1.000000000000000000, 0.9238795325112867385, 1.000000000000000000, 0.9238795325112867385, 1.000000000000000000, 0.9238795325112867385, 1.000000000000000000, 0.9238795325112867385, 1.000000000000000000, 0.9238795325112867385, 1.000000000000000000, 0.9238795325112867385, 1.000000000000000000, 0.9238795325112867385, 1.000000000000000000, 0.9238795325112867385, 1.000000000000000000, 0.9238795325112867385, 1.000000000000000000, 0.9238795325112867385, 1.000000000000000000, 0.9238795325112867385, 1.000000000000000000, 0.9238795325112867385, 1.000000000000000000, 0.9238795325112867385, 1.000000000000000000, 0.9238795325112867385, 1.000000000000000000, 0.9238795325112867385, 1.000000000000000000, 0.9238795325112867385, 1.000000000000000000, 0.9238795325112867385, 1.000000000000000000, 0.9238795325112867385, 1.000000000000000000, 0.9238795325112867385, 1.000000000000000000, 0.9238795325112867385, 1.000000000000000000, 0.9238795325112867385, 1.000000000000000000, 0.9238795325112867385, 1.000000000000000000, 0.9238795325112867385, 1.000000000000000000, 0.9238795325112867385, 1.000000000000000000, 0.9238795325112867385, 1.000000000000000000, 0.9238795325112867385, 1.000000000000000000, 0.9238795325112867385, 1.000000000000000000, 0.9238795325112867385, 1.000000000000000000, 0.9238795325112867385, 1.000000000000000000, 0.9238795325112867385, 1.000000000000000000, 0.9238795325112867385, 1.000000000000000000, 0.9238795325112867385, 1.000000000000000000, 0.9238795325112867385, 1.000000000000000000, 0.9238795325112867385, 1.000000000000000000, 0.9238795325112867385, 1.000000000000000000, 0.9238795325112867385, 1.000000000000000000, 0.9238795325112867385, 1.000000000000000000, 0.9238795325112867385, 1.000000000000000000, 0.9238795325112867385, 1.000000000000000000, 0.9238795325112867385, 1.000000000000000000, 0.9238795325112867385, 1.000000000000000000, 0.9238795325112867385, 1.000000000000000000, 0.9238795325112867385, 1.000000000000000000, 0.9238795325112867385, 1.000000000000000000, 0.9238795325112867385, 1.000000000000000000, 0.9238795325112867385, 1.000000000000000000, 0.9238795325112867385, 1.000000000000000000, 0.9238795325112867385, 1.000000000000000000, 0.9238795325112867385, 1.000000000000000000, 0.9238795325112867385, 1.000000000000000000, 0.9238795325112867385, 1.000000000000000000, 0.9238795325112867385, 1.000000000000000000, 0.9238795325112867385, 1.000000000000000000, 0.9238795325112867385, 1.000000000000000000, 0.9238795325112867385, 1.000000000000000000, 0.9238795325112867385, 1.000000000000000000, 0.9238795325112867385, 1.000000000000000000, 0.9238795325112867385, 1.000000000000000000, 0.9238795325112867385, 1.000000000000000000, 0.9238795325112867385, 1.000000000000000000, 0.9238795325112867385, 1.000000000000000000, 0.9238795325112867385, 1.000000000000000000, 0.9238795325112867385, 1.000000000000000000, 0.9238795325112867385, 1.000000000000000000, 0.9238795325112867385, 1.000000000000000000, 0.9238795325112867385, 1.000000000000000000, 0.9238795325112867385, 1.000000000000000000, 0.9238795325112867385, 1.000000000000000000, 0.9238795325112867385, 1.000000000000000000, 0.9238795325112867385, 1.000000000000000000, 0.9238795325112867385, 1.000000000000000000, 0.9238795325112867385, 1.000000000000000000, 0.9238795325112867385, 1.000000000000000000, 0.9238795325112867385, 1.000000000000000000, 0.9238795325112867385, 1.000000000000000000, 0.9238795325112867385, 1.000000000000000000, 0.9238795325112867385, 1.000000000000000000, 0.9238795325112867385, 1.000000000000000000, 0.9238795325112867385, 1.000000000000000000, 0.9238795325112867385, 1.000000000000000000, 0.9238795325112867385, 1.000000000000000000, 0.9238795325112867385, 1.000000000000000000, 0.9238795325112867385, 1.000000000000000000, 0.9238795325112867385, 1.000000000000000000, 0.9238795325112867385, 1.000000000000000000),
 ( 1.000000000000000000, 0.9238795325112867385, 1.000000000000000000, 0.9238795325112867385, 1.000000000000000000, 0.9238795325112867385, 1.000000000000000000, 0.9238795325112867385, 1.000000000000000000, 0.9238795325112867385, 1.000000000000000000, 0.9238795325112867385, 1.000000000000000000, 0.9238795325112867385, 1.000000000000000000, 0.9238795325112867385, 1.000000000000000000, 0.9238795325112867385, 1.000000000000000000, 0.9238795325112867385, 1.000000000000000000, 0.9238795325112867385, 1.000000000000000000, 0.9238795325112867385, 1.000000000000000000, 0.9238795325112867385, 1.000000000000000000, 0.9238795325112867385, 1.000000000000000000, 0.9238795325112867385, 1.000000000000000000, 0.9238795325112867385, 1.000000000000000000, 0.9238795325112867385, 1.000000000000000000, 0.9238795325112867385, 1.000000000000000000, 0.9238795325112867385, 1.000000000000000000, 0.9238795325112867385, 1.000000000000000000, 0.9238795325112867385, 1.000000000000000000, 0.9238795325112867385, 1.000000000000000000, 0.9238795325112867385, 1.000000000000000000, 0.9238795325112867385, 1.000000000000000000, 0.9238795325112867385, 1.000000000000000000, 0.9238795325112867385, 1.000000000000000000, 0.9238795325112867385, 1.000000000000000000, 0.9238795325112867385, 1.000000000000000000, 0.9238795325112867385, 1.000000000000000000, 0.9238795325112867385, 1.000000000000000000, 0.9238795325112867385, 1.000000000000000000, 0.9238795325112867385, 1.000000000000000000, 0.9238795325112867385, 1.000000000000000000, 0.9238795325112867385, 1.000000000000000000, 0.9238795325112867385, 1.000000000000000000, 0.9238795325112867385, 1.000000000000000000, 0.9238795325112867385, 1.000000000000000000, 0.9238795325112867385, 1.000000000000000000, 0.9238795325112867385, 1.000000000000000000, 0.9238795325112867385, 1.000000000000000000, 0.9238795325112867385, 1.000000000000000000, 0.9238795325112867385, 1.000000000000000000, 0.9238795325112867385, 1.000000000000000000, 0.9238795325112867385, 1.000000000000000000, 0.9238795325112867385, 1.000000000000000000, 0.9238795325112867385, 1.000000000000000000, 0.9238795325112867385, 1.000000000000000000, 0.9238795325112867385, 1.000000000000000000, 0.9238795325112867385, 1.000000000000000000, 0.9238795325112867385, 1.000000000000000000, 0.9238795325112867385, 1.000000000000000000, 0.9238795325112867385, 1.000000000000000000, 0.9238795325112867385, 1.000000000000000000, 0.9238795325112867385, 1.000000000000000000, 0.9238795325112867385, 1.000000000000000000, 0.9238795325112867385, 1.000000000000000000, 0.9238795325112867385, 1.000000000000000000, 0.9238795325112867385, 1.000000000000000000, 0.9238795325112867385, 1.000000000000000000, 0.9238795325112867385, 1.000000000000000000, 0.9238795325112867385, 1.000000000000000000, 0.9238795325112867385, 1.000000000000000000, 0.9238795325112867385, 1.000000000000000000, 0.9238795325112867385, 1.000000000000000000, 0.9238795325112867385, 1.000000000000000000, 0.9238795325112867385, 1.000000000000000000, 0.9238795325112867385, 1.000000000000000000, 0.9238795325112867385, 1.000000000000000000, 0.9238795325112867385, 1.000000000000000000, 0.9238795325112867385, 1.000000000000000000, 0.9238795325112867385, 1.000000000000000000, 0.9238795325112867385, 1.000000000000000000, 0.9238795325112867385, 1.000000000000000000, 0.9238795325112867385, 1.000000000000000000, 0.9238795325112867385, 1.000000000000000000, 0.9238795325112867385, 1.000000000000000000, 0.9238795325112867385, 1.000000000000000000, 0.9238795325112867385, 1.000000000000000000, 0.9238795325112867385, 1.000000000000000000, 0.9238795325112867385, 1.000000000000000000, 0.9238795325112867385, 1.000000000000000000, 0.9238795325112867385, 1.000000000000000000, 0.9238795325112867385, 1.000000000000000000, 0.9238795325112867385, 1.000000000000000000, 0.9238795325112867385, 1.000000000000000000, 0.9238795325112867385, 1.000000000000000000, 0.9238795325112867385, 1.000000000000000000, 0.9238795325112867385, 1.000000000000000000, 0.9238795325112867385, 1.000000000000000000, 0.9238795325112867385, 1.000000000000000000, 0.9238795325112867385, 1.000000000000000000, 0.9238795325112867385, 1.000000000000000000, 0.9238795325112867385, 1.000000000000000000, 0.9238795325112867385, 1.000000000000000000, 0.9238795325112867385, 1.000000000000000000, 0.9238795325112867385, 1.000000000000000000) ) ) 
 REPRESENTATION_ITEM ( '' )  SURFACE ( )  );
#28682=ORIENTED_EDGE ( 'NONE', *, *, #39801, .T. ) ;
#28688=CARTESIAN_POINT ( 'NONE',  ( 2.765530957082001251, 298.9218750017070647, 6.676582343749999815 ) ) ;
#28689=CARTESIAN_POINT ( 'NONE',  ( 10.00000000000000178, 120.0000000000000142, 0.000000000000000000 ) ) ;
#28692=CARTESIAN_POINT ( 'NONE',  ( -4.721056650415999201, 288.4843750017070079, -4.721056650415999201 ) ) ;
#28704=CARTESIAN_POINT ( 'NONE',  ( -8.311093377946841443, 18.90624999658601624, 8.311093377946830785 ) ) ;
#28706=CARTESIAN_POINT ( 'NONE',  ( 5.676582343749993598, 215.2604166632526983, 9.832129032723422313 ) ) ;
#28708=CARTESIAN_POINT ( 'NONE',  ( -5.000000000000005329, 220.2083333265053966, 8.660254037844387298 ) ) ;
#28710=CYLINDRICAL_SURFACE ( 'NONE', #18268, 10.00000000000000178 ) ;
#28711=VERTEX_POINT ( 'NONE', #11948 ) ;
#28714=CARTESIAN_POINT ( 'NONE',  ( 6.951808397369818766E-16, 22.03124999658601624, -11.35316468750000141 ) ) ;
#28718=CARTESIAN_POINT ( 'NONE',  ( 0.000000000000000000, 300.0000000000000000, 0.000000000000000000 ) ) ;
#28720=CARTESIAN_POINT ( 'NONE',  ( -3.042071309553163960, 22.23958332991935194, -11.35316468749999963 ) ) ;
#28722=CARTESIAN_POINT ( 'NONE',  ( -9.832129032723418760, 132.8645833299193555, -5.676582343750004256 ) ) ;
#28723=CARTESIAN_POINT ( 'NONE',  ( 10.00000000000000000, 106.6666666598387110, 2.679491924311236062 ) ) ;
#28725=CARTESIAN_POINT ( 'NONE',  ( -7.320508075688773708, 3.749999993172032475, -7.320508075688774596 ) ) ;
#28729=CARTESIAN_POINT ( 'NONE',  ( 11.35316468750000141, 11.09374999658601624, 0.000000000000000000 ) ) ;
#28731=CARTESIAN_POINT ( 'NONE',  ( -6.676582343750000703, 296.5156250017069510, 2.765530957082001251 ) ) ;
#28732=CARTESIAN_POINT ( 'NONE',  ( 9.832129032723416984, 145.3645833299193555, 5.676582343750006032 ) ) ;
#28735=EDGE_CURVE ( 'NONE', #28855, #47954, #30646, .T. ) ;
#28739=EDGE_CURVE ( 'NONE', #47641, #23624, #6666, .T. ) ;
#28744=CARTESIAN_POINT ( 'NONE',  ( 5.676582343750001591, 71.92708332991934128, -9.832129032723420536 ) ) ;
#28745=VERTEX_POINT ( 'NONE', #34235 ) ;
#28748=VERTEX_POINT ( 'NONE', #57236 ) ;
#28751=CARTESIAN_POINT ( 'NONE',  ( -10.00000000000000178, 109.3749999931720396, -1.224646799147353454E-15 ) ) ;
#28777=CARTESIAN_POINT ( 'NONE',  ( -8.660254037844390851, 77.91666666666667140, 4.999999999999998224 ) ) ;
#28779=CARTESIAN_POINT ( 'NONE',  ( -9.832129032723418760, 58.17708332991936260, -5.676582343750004256 ) ) ;
#28780=CARTESIAN_POINT ( 'NONE',  ( 4.242640687119287435, 290.3750000000000000, 4.242640687119285658 ) ) ;
#28792=CARTESIAN_POINT ( 'NONE',  ( -10.00000000000000000, 202.2916666666666572, -2.679491924311229845 ) ) ;
#28794=CARTESIAN_POINT ( 'NONE',  ( -5.676582343749998039, 162.7604166632526983, -9.832129032723420536 ) ) ;
#28796=DIRECTION ( 'NONE',  ( -0.000000000000000000, 1.000000000000000000, -0.000000000000000000 ) ) ;
#28800=CARTESIAN_POINT ( 'NONE',  ( 11.35316468749999785, 35.88541666325268409, 3.042071309553174174 ) ) ;
#28805=DIRECTION ( 'NONE',  ( -0.000000000000000000, 1.000000000000000000, -0.000000000000000000 ) ) ;
#28808=CARTESIAN_POINT ( 'NONE',  ( -2.679491924311225848, 58.33333332650537528, -10.00000000000000178 ) ) ;
#28811=CARTESIAN_POINT ( 'NONE',  ( 2.966170491840901068E-11, 66.24999999999768363, -9.999999999999998224 ) ) ;
#28815=ORIENTED_EDGE ( 'NONE', *, *, #55588, .T. ) ;
#28818=CARTESIAN_POINT ( 'NONE',  ( 4.721056650415999201, 298.2343750017069510, -4.721056650415999201 ) ) ;
#28821=CARTESIAN_POINT ( 'NONE',  ( 9.832129032723420536, 136.1979166632526983, -5.676582343749999815 ) ) ;
#28828=EDGE_LOOP ( 'NONE', ( #12919, #11756, #71429, #7233 ) ) ;
#28829=EDGE_CURVE ( 'NONE', #38870, #31834, #24906, .T. ) ;
#28832=CARTESIAN_POINT ( 'NONE',  ( -5.676582343750006032, 134.4270833299193555, 9.832129032723418760 ) ) ;
#28836=CARTESIAN_POINT ( 'NONE',  ( 5.676582343750001591, 31.92708332991935194, -9.832129032723420536 ) ) ;
#28837=ORIENTED_EDGE ( 'NONE', *, *, #25641, .F. ) ;
#28843=CARTESIAN_POINT ( 'NONE',  ( 2.485281374238575314, 297.3750000034139589, 6.000000000000000888 ) ) ;
#28847=CARTESIAN_POINT ( 'NONE',  ( -3.042071309553164404, 157.5520833299193555, -11.35316468749999963 ) ) ;
#28849=EDGE_CURVE ( 'NONE', #8118, #5410, #1791, .T. ) ;
#28855=VERTEX_POINT ( 'NONE', #13038 ) ;
#28860=CARTESIAN_POINT ( 'NONE',  ( -8.660254037844454800, 57.08333333333337833, -5.000000000000044409 ) ) ;
#28865=CARTESIAN_POINT ( 'NONE',  ( -4.242640687119285658, 298.1875000034139589, 4.242640687119287435 ) ) ;
#28866=CARTESIAN_POINT ( 'NONE',  ( -5.000000000000005329, 45.20833332650536818, 8.660254037844387298 ) ) ;
#28867=CARTESIAN_POINT ( 'NONE',  ( -8.660254037844390851, 42.91666666666667140, 4.999999999999998224 ) ) ;
#28872=CARTESIAN_POINT ( 'NONE',  ( 2.679491924311222739, 195.8333333265053682, 10.00000000000000355 ) ) ;
#28880=( BOUNDED_CURVE ( )  B_SPLINE_CURVE ( 2, ( #21934, #15901, #38932, #10261, #11005, #62303, #33287, #44964, #16265 ),
 .UNSPECIFIED., .F., .F. ) 
 B_SPLINE_CURVE_WITH_KNOTS ( ( 3, 2, 2, 2, 3 ),
 ( 0.6041666666666648533, 0.6145833333333315940, 0.6249999999999982236, 0.6354166666666647423, 0.6458333333333314830 ),
 .UNSPECIFIED. ) 
 CURVE ( )  GEOMETRIC_REPRESENTATION_ITEM ( )  RATIONAL_B_SPLINE_CURVE ( ( 1.000000000000012879, 0.9238795325112737489, 1.000000000000000000, 0.9238795325112867385, 1.000000000000000000, 0.9238795325112867385, 1.000000000000000000, 0.9238795325113005052, 0.9999999999999862332 ) ) 
 REPRESENTATION_ITEM ( '' )  );
#28881=CARTESIAN_POINT ( 'NONE',  ( -10.00000000000000355, 139.5833333265053682, 2.679491924311223183 ) ) ;
#28882=CARTESIAN_POINT ( 'NONE',  ( -4.999999999999998224, 156.6666666666666856, -8.660254037844389075 ) ) ;
#28886=CARTESIAN_POINT ( 'NONE',  ( -2.085542519210945728E-15, 129.8437499965860127, 11.35316468750000141 ) ) ;
#28887=CARTESIAN_POINT ( 'NONE',  ( -5.999999999999999112, 294.1250000034140157, 2.485281374238575314 ) ) ;
#28891=CARTESIAN_POINT ( 'NONE',  ( 2.485281374238974994, 298.3124999999999432, 5.999999999999600320 ) ) ;
#28892=EDGE_CURVE ( 'NONE', #48188, #13863, #11932, .T. ) ;
#28900=CARTESIAN_POINT ( 'NONE',  ( 4.999999999999993783, 21.04166665983870033, 8.660254037844390851 ) ) ;
#28907=CARTESIAN_POINT ( 'NONE',  ( -3.042071309553173730, 114.3229166632526841, 11.35316468749999785 ) ) ;
#28911=DIRECTION ( 'NONE',  ( -0.000000000000000000, 1.000000000000000000, -0.000000000000000000 ) ) ;
#28915=CARTESIAN_POINT ( 'NONE',  ( 5.676582343749993598, 104.9479166632526841, 9.832129032723422313 ) ) ;
#28920=CARTESIAN_POINT ( 'NONE',  ( 4.999999999999993783, 221.0416666598387110, 8.660254037844390851 ) ) ;
#28924=CARTESIAN_POINT ( 'NONE',  ( 8.311093377946837890, 101.4062499965860127, -8.311093377946837890 ) ) ;
#28927=CARTESIAN_POINT ( 'NONE',  ( 2.679491924311081963, 171.0416666666666572, -10.00000000000008349 ) ) ;
#28929=CARTESIAN_POINT ( 'NONE',  ( -1.836970198721029983E-15, 200.6249999931720538, 10.00000000000000178 ) ) ;
#28932=CARTESIAN_POINT ( 'NONE',  ( -9.832129032723420536, 89.01041666325268409, 5.676582343749997150 ) ) ;
#28933=CARTESIAN_POINT ( 'NONE',  ( 2.765530957082001251, 289.7656250017069510, 6.676582343750000703 ) ) ;
#28936=CARTESIAN_POINT ( 'NONE',  ( 11.35316468750000141, 1.093749996586016682, 0.000000000000000000 ) ) ;
#28940=CARTESIAN_POINT ( 'NONE',  ( -8.311093377946841443, 213.9062499965860411, 8.311093377946834337 ) ) ;
#28943=CARTESIAN_POINT ( 'NONE',  ( 2.765530957081996366, 295.1406250017069510, -6.676582343750003368 ) ) ;
#28946=CARTESIAN_POINT ( 'NONE',  ( 5.676582343750001591, 201.9270833299193555, -9.832129032723420536 ) ) ;
#28953=CARTESIAN_POINT ( 'NONE',  ( -10.00000000000000178, 22.50000000000000355, -1.224646799147353454E-15 ) ) ;
#28962=CARTESIAN_POINT ( 'NONE',  ( 0.000000000000000000, 300.0000000000000000, 0.000000000000000000 ) ) ;
#28965=CARTESIAN_POINT ( 'NONE',  ( -4.721056650415999201, 297.3281250017069510, -4.721056650415999201 ) ) ;
#28974=DIRECTION ( 'NONE',  ( -0.000000000000000000, 1.000000000000000000, -0.000000000000000000 ) ) ;
#28975=CARTESIAN_POINT ( 'NONE',  ( 6.951808397369818766E-16, 82.34374999658601268, -11.35316468750000141 ) ) ;
#28986=CARTESIAN_POINT ( 'NONE',  ( 3.042071309553159519, 194.7395833299193555, 11.35316468750000141 ) ) ;
#28990=CARTESIAN_POINT ( 'NONE',  ( 8.311093377946834337, 185.4687499965860127, 8.311093377946839666 ) ) ;
#28994=CARTESIAN_POINT ( 'NONE',  ( 1.592277918221149080E-13, 106.2500000000000142, -10.00000000000000178 ) ) ;
#28998=CARTESIAN_POINT ( 'NONE',  ( -9.832129032723420536, 63.69791666325269830, 5.676582343749997150 ) ) ;
#29001=ORIENTED_EDGE ( 'NONE', *, *, #58712, .F. ) ;
#29004=CARTESIAN_POINT ( 'NONE',  ( 3.042071309553167069, 66.82291666325266988, -11.35316468749999785 ) ) ;
#29009=CARTESIAN_POINT ( 'NONE',  ( -2.085542519210945728E-15, 64.53124999658602690, 11.35316468750000141 ) ) ;
#29014=CARTESIAN_POINT ( 'NONE',  ( -8.660254037844390851, 154.7916666598387110, 4.999999999999998224 ) ) ;
#29016=CARTESIAN_POINT ( 'NONE',  ( 8.660254037844390851, 19.58333333333333925, 5.000000000000009770 ) ) ;
#29017=CARTESIAN_POINT ( 'NONE',  ( 3.042071309553159519, 45.05208332991934839, 11.35316468750000141 ) ) ;
#29019=CARTESIAN_POINT ( 'NONE',  ( -9.832129032723420536, 178.6979166632526983, 5.676582343749997150 ) ) ;
#29025=CARTESIAN_POINT ( 'NONE',  ( -3.042071309553163960, 177.2395833299193555, -11.35316468749999963 ) ) ;
#29032=CARTESIAN_POINT ( 'NONE',  ( -5.676582343749998039, 167.7604166632526983, -9.832129032723420536 ) ) ;
#29035=CARTESIAN_POINT ( 'NONE',  ( 9.832129032723416984, 135.6770833299193555, 5.676582343750006032 ) ) ;
#29038=ORIENTED_EDGE ( 'NONE', *, *, #73766, .F. ) ;
#29067=CARTESIAN_POINT ( 'NONE',  ( -6.676582343750001591, 297.6093750017069510, 0.000000000000000000 ) ) ;
#29068=CARTESIAN_POINT ( 'NONE',  ( 2.679491924311228956, 136.0416666666666572, -10.00000000000000000 ) ) ;
#29069=EDGE_CURVE ( 'NONE', #13964, #42156, #72628, .T. ) ;
#29071=CARTESIAN_POINT ( 'NONE',  ( 2.765530957082001251, 287.9218750017069510, 6.676582343750000703 ) ) ;
#29086=CARTESIAN_POINT ( 'NONE',  ( -11.35316468749999785, 18.07291666325267698, -3.042071309553167513 ) ) ;
#29088=CARTESIAN_POINT ( 'NONE',  ( 3.042071309553159519, 225.0520833299193555, 11.35316468750000141 ) ) ;
#29095=CARTESIAN_POINT ( 'NONE',  ( 8.311093377946834337, 25.15624999658601268, 8.311093377946839666 ) ) ;
#29102=CARTESIAN_POINT ( 'NONE',  ( 8.311093377946837890, 16.40624999658601624, -8.311093377946837890 ) ) ;
#29104=CARTESIAN_POINT ( 'NONE',  ( -3.042071309553173730, 139.3229166632526699, 11.35316468749999785 ) ) ;
#29105=CARTESIAN_POINT ( 'NONE',  ( -2.679491924311235618, 120.4166666598386826, 10.00000000000000000 ) ) ;
#29107=CARTESIAN_POINT ( 'NONE',  ( 0.000000000000000000, 300.0000000000000000, 0.000000000000000000 ) ) ;
#29110=VERTEX_POINT ( 'NONE', #20932 ) ;
#29111=CARTESIAN_POINT ( 'NONE',  ( -11.35316468750000141, 8.802083329919348387, 3.042071309553159963 ) ) ;
#29112=CARTESIAN_POINT ( 'NONE',  ( -8.660254037844390851, 154.7916666598387110, 4.999999999999998224 ) ) ;
#29113=CARTESIAN_POINT ( 'NONE',  ( -6.676582343750001591, 299.4531250017069510, 0.000000000000000000 ) ) ;
#29114=CARTESIAN_POINT ( 'NONE',  ( -11.35316468750000141, 143.2812499965860411, -1.390361679473963753E-15 ) ) ;
#29125=CARTESIAN_POINT ( 'NONE',  ( 5.676582343749993598, 95.26041666325268409, 9.832129032723422313 ) ) ;
#29126=( BOUNDED_CURVE ( )  B_SPLINE_CURVE ( 2, ( #41827, #53159, #47850, #70505, #48960, #71971, #59195, #31624, #18824, #54274, #65574, #1493, #13140 ),
 .UNSPECIFIED., .F., .F. ) 
 B_SPLINE_CURVE_WITH_KNOTS ( ( 3, 2, 2, 2, 2, 2, 3 ),
 ( 0.8097826086956521063, 0.8115942028985506651, 0.8134057971014491129, 0.8152173913043476716, 0.8170289855072463414, 0.8188405797101449002, 0.8206521739130434590 ),
 .UNSPECIFIED. ) 
 CURVE ( )  GEOMETRIC_REPRESENTATION_ITEM ( )  RATIONAL_B_SPLINE_CURVE ( ( 1.000000000000001998, 0.9659258262890662028, 1.000000000000000000, 0.9659258262890683122, 1.000000000000000000, 0.9659258262890683122, 1.000000000000000000, 0.9659258262890683122, 1.000000000000000000, 0.9659258262890683122, 1.000000000000000000, 0.9659258262890683122, 1.000000000000000000 ) ) 
 REPRESENTATION_ITEM ( '' )  );
#29131=ORIENTED_EDGE ( 'NONE', *, *, #57299, .F. ) ;
#29152=ORIENTED_EDGE ( 'NONE', *, *, #14822, .F. ) ;
#29158=CARTESIAN_POINT ( 'NONE',  ( 4.999999999999993783, 99.16666666666667140, 8.660254037844390851 ) ) ;
#29163=CARTESIAN_POINT ( 'NONE',  ( 9.832129032723420536, 66.51041666325268409, -5.676582343749999815 ) ) ;
#29164=CARTESIAN_POINT ( 'NONE',  ( -2.765530957081996810, 299.4218750017070079, -6.676582343750003368 ) ) ;
#29170=CARTESIAN_POINT ( 'NONE',  ( 4.999999999999999112, 84.16666666666668561, 8.660254037844399733 ) ) ;
#29175=CARTESIAN_POINT ( 'NONE',  ( -10.00000000000000355, 207.7083333333333712, 2.679491924311223183 ) ) ;
#29177=CARTESIAN_POINT ( 'NONE',  ( 5.676582343750001591, 181.9270833299193555, -9.832129032723420536 ) ) ;
#29184=CARTESIAN_POINT ( 'NONE',  ( -5.676582343750006032, 39.42708332991935549, 9.832129032723418760 ) ) ;
#29189=CARTESIAN_POINT ( 'NONE',  ( 5.000000000000001776, 222.7083333265053966, -8.660254037844389075 ) ) ;
#29192=CARTESIAN_POINT ( 'NONE',  ( 4.999999999999993783, 61.04166665983870388, 8.660254037844390851 ) ) ;
#29201=CARTESIAN_POINT ( 'NONE',  ( -8.660254037844477892, 197.0833333333333997, -5.000000000000058620 ) ) ;
#29202=FACE_OUTER_BOUND ( 'NONE', #57086, .T. ) ;
#29204=CARTESIAN_POINT ( 'NONE',  ( 8.660254037844385522, 41.45833332650536818, 5.000000000000005329 ) ) ;
#29205=CARTESIAN_POINT ( 'NONE',  ( 11.35316468750000141, 150.7812499965860411, 0.000000000000000000 ) ) ;
#29212=VERTEX_POINT ( 'NONE', #74540 ) ;
#29215=CARTESIAN_POINT ( 'NONE',  ( -3.042071309553173730, 124.6354166632526699, 11.35316468749999785 ) ) ;
#29219=CARTESIAN_POINT ( 'NONE',  ( -11.35316468749999785, 43.38541666325269119, -3.042071309553167513 ) ) ;
#29226=CARTESIAN_POINT ( 'NONE',  ( 6.000000000000001776, 296.5625000034140157, -7.347880794884121708E-16 ) ) ;
#29245=EDGE_LOOP ( 'NONE', ( #59928, #4175, #63786, #67134 ) ) ;
#29249=CARTESIAN_POINT ( 'NONE',  ( -10.00000000000000000, 44.16666665983870388, -2.679491924311229845 ) ) ;
#29250=CARTESIAN_POINT ( 'NONE',  ( -7.320508075688778149, 38.12499999999999289, 7.320508075688769267 ) ) ;
#29253=CARTESIAN_POINT ( 'NONE',  ( -4.999999999999998224, 33.54166665983870388, -8.660254037844389075 ) ) ;
#29263=CARTESIAN_POINT ( 'NONE',  ( -10.00000000000000178, 139.3749999931720538, -1.224646799147353454E-15 ) ) ;
#29264=CARTESIAN_POINT ( 'NONE',  ( 8.660254037844389075, 160.4166666666666856, -5.000000000000000000 ) ) ;
#29268=CARTESIAN_POINT ( 'NONE',  ( 5.676582343749993598, 135.2604166632526983, 9.832129032723422313 ) ) ;
#29282=CARTESIAN_POINT ( 'NONE',  ( 6.123233995736767268E-16, 28.12499999317203603, -10.00000000000000178 ) ) ;
#29288=FACE_OUTER_BOUND ( 'NONE', #55696, .T. ) ;
#29289=CARTESIAN_POINT ( 'NONE',  ( 11.35316468749999785, 105.5729166632526983, 3.042071309553174174 ) ) ;
#29295=CARTESIAN_POINT ( 'NONE',  ( -9.832129032723418760, 117.8645833299193697, -5.676582343750004256 ) ) ;
#29299=CARTESIAN_POINT ( 'NONE',  ( 5.000000000000001776, 222.7083333265053966, -8.660254037844389075 ) ) ;
#29302=CARTESIAN_POINT ( 'NONE',  ( -7.320508075688776373, 183.1250000000000000, 7.320508075688768379 ) ) ;
#29303=CARTESIAN_POINT ( 'NONE',  ( 9.832129032723416984, 95.36458332991935549, 5.676582343750006032 ) ) ;
#29306=CARTESIAN_POINT ( 'NONE',  ( -2.222453528114265639E-12, 168.7499999999998295, 10.00000000000000178 ) ) ;
#29309=CARTESIAN_POINT ( 'NONE',  ( -4.999999999999998224, 193.5416666598387110, -8.660254037844389075 ) ) ;
#29310=EDGE_CURVE ( 'NONE', #28343, #62422, #4222, .T. ) ;
#29312=CARTESIAN_POINT ( 'NONE',  ( -11.35316468750000141, 88.59374999658602690, -1.390361679473963753E-15 ) ) ;
#29316=CARTESIAN_POINT ( 'NONE',  ( -3.042071309553173730, 219.3229166632526699, 11.35316468749999785 ) ) ;
#29320=CARTESIAN_POINT ( 'NONE',  ( -2.085542519210945728E-15, 224.5312499965860127, 11.35316468750000141 ) ) ;
#29323=CARTESIAN_POINT ( 'NONE',  ( 3.153939666463620179E-13, 158.7500000000000284, 9.999999999999998224 ) ) ;
#29324=CARTESIAN_POINT ( 'NONE',  ( -6.676582343750000703, 297.5156250017070079, 2.765530957082001251 ) ) ;
#29327=CARTESIAN_POINT ( 'NONE',  ( -5.676582343750006032, 214.4270833299193555, 9.832129032723418760 ) ) ;
#29335=ADVANCED_FACE ( 'NONE', ( #2070 ), #37142, .T. ) ;
#29336=CARTESIAN_POINT ( 'NONE',  ( -2.679491924311225848, 31.45833333333333925, -10.00000000000000178 ) ) ;
#29341=AXIS2_PLACEMENT_3D ( 'NONE', #31941, #20608, #37982 ) ;
#29344=LINE ( 'NONE', #18386, #66735 ) ;
#29348=CARTESIAN_POINT ( 'NONE',  ( -6.676582343750001591, 298.4531250017069510, 0.000000000000000000 ) ) ;
#29360=CARTESIAN_POINT ( 'NONE',  ( 9.832129032723420536, 81.51041666325268409, -5.676582343749999815 ) ) ;
#29369=CARTESIAN_POINT ( 'NONE',  ( 11.35316468749999785, 205.5729166632526699, 3.042071309553174174 ) ) ;
#29374=CARTESIAN_POINT ( 'NONE',  ( 5.676582343749993598, 185.2604166632526983, 9.832129032723422313 ) ) ;
#29381=CARTESIAN_POINT ( 'NONE',  ( 11.35316468750000141, 65.78124999658602690, 0.000000000000000000 ) ) ;
#29386=VECTOR ( 'NONE', #63891, 1000.000000000000000 ) ;
#29388=CARTESIAN_POINT ( 'NONE',  ( -11.35316468749999785, 58.07291666325268409, -3.042071309553167513 ) ) ;
#29393=CARTESIAN_POINT ( 'NONE',  ( 11.35316468749999785, 55.57291666325267698, 3.042071309553174174 ) ) ;
#29396=CARTESIAN_POINT ( 'NONE',  ( -7.320508075688778149, 159.9999999931720254, 7.320508075688769267 ) ) ;
#29399=CARTESIAN_POINT ( 'NONE',  ( -2.085542519210945728E-15, 44.84374999658602690, 11.35316468750000141 ) ) ;
#29401=CARTESIAN_POINT ( 'NONE',  ( 9.832129032723420536, 186.1979166632526983, -5.676582343749999815 ) ) ;
#29405=CARTESIAN_POINT ( 'NONE',  ( 2.679491924311228956, 162.9166666598387110, -10.00000000000000000 ) ) ;
#29407=CARTESIAN_POINT ( 'NONE',  ( -8.311093377946841443, 173.9062499965860127, 8.311093377946834337 ) ) ;
#29411=VERTEX_POINT ( 'NONE', #53394 ) ;
#29412=CARTESIAN_POINT ( 'NONE',  ( -5.676582343749998039, 162.7604166632526983, -9.832129032723420536 ) ) ;
#29414=CARTESIAN_POINT ( 'NONE',  ( 8.311093377946834337, 130.4687499965860127, 8.311093377946839666 ) ) ;
#29426=CARTESIAN_POINT ( 'NONE',  ( -10.00000000000005684, 177.7083333333333712, 2.679491924311237838 ) ) ;
#29441=CARTESIAN_POINT ( 'NONE',  ( 6.676582343750002480, 297.1718750017071216, -2.765530957081997254 ) ) ;
#29442=CARTESIAN_POINT ( 'NONE',  ( 7.320508075688771044, 139.3750000000000000, 7.320508075688775484 ) ) ;
#29444=CARTESIAN_POINT ( 'NONE',  ( 6.676582343750004256, 290.0468750017070079, 2.765530957081995478 ) ) ;
#29455=FACE_OUTER_BOUND ( 'NONE', #44057, .T. ) ;
#29460=CARTESIAN_POINT ( 'NONE',  ( -3.042071309553173730, 29.32291666325268764, 11.35316468749999785 ) ) ;
#29462=CARTESIAN_POINT ( 'NONE',  ( 8.311093377946837890, 226.7187499965860411, -8.311093377946837890 ) ) ;
#29468=CARTESIAN_POINT ( 'NONE',  ( -9.832129032723418760, 17.86458332991935194, -5.676582343750004256 ) ) ;
#29471=CARTESIAN_POINT ( 'NONE',  ( -4.242640687119285658, 295.1875000034139589, 4.242640687119287435 ) ) ;
#29472=CARTESIAN_POINT ( 'NONE',  ( 0.000000000000000000, 300.0000000000000000, 10.00000000000000178 ) ) ;
#29474=CARTESIAN_POINT ( 'NONE',  ( 8.311093377946837890, 21.40624999658601268, -8.311093377946837890 ) ) ;
#29476=CARTESIAN_POINT ( 'NONE',  ( 5.676582343750001591, 151.6145833299193555, -9.832129032723420536 ) ) ;
#29478=CARTESIAN_POINT ( 'NONE',  ( 10.00000000000000178, 122.0833333265053540, -2.679491924311226736 ) ) ;
#29483=CARTESIAN_POINT ( 'NONE',  ( -8.311093377946841443, 14.21874999658601801, 8.311093377946834337 ) ) ;
#29484=ORIENTED_EDGE ( 'NONE', *, *, #43452, .T. ) ;
#29486=CARTESIAN_POINT ( 'NONE',  ( 4.721056650416000089, 297.8281250017069510, 4.721056650415999201 ) ) ;
#29487=CARTESIAN_POINT ( 'NONE',  ( 8.311093377946834337, 135.1562499965860695, 8.311093377946839666 ) ) ;
#29496=CARTESIAN_POINT ( 'NONE',  ( 10.00000000000000533, 120.0000000000000142, 0.000000000000000000 ) ) ;
#29499=CARTESIAN_POINT ( 'NONE',  ( -11.35316468750000141, 93.59374999658602690, -1.390361679473963753E-15 ) ) ;
#29500=ORIENTED_EDGE ( 'NONE', *, *, #63422, .T. ) ;
#29509=EDGE_CURVE ( 'NONE', #48426, #9276, #19406, .T. ) ;
#29518=( NAMED_UNIT ( * ) PLANE_ANGLE_UNIT ( ) SI_UNIT ( $, .RADIAN. ) );
#29529=CARTESIAN_POINT ( 'NONE',  ( 10.00000000000000178, 95.00000000000000000, 0.000000000000000000 ) ) ;
#29531=CARTESIAN_POINT ( 'NONE',  ( -8.311093377946841443, 59.21874999658601979, 8.311093377946830785 ) ) ;
#29532=CARTESIAN_POINT ( 'NONE',  ( -2.765530957081996810, 298.4218750017069510, -6.676582343750003368 ) ) ;
#29533=ORIENTED_EDGE ( 'NONE', *, *, #31063, .T. ) ;
#29540=DIRECTION ( 'NONE',  ( 0.000000000000000000, 0.000000000000000000, 1.000000000000000000 ) ) ;
#29542=CARTESIAN_POINT ( 'NONE',  ( -10.00000000000000000, 217.2916666666667140, -2.679491924311229845 ) ) ;
#29544=CARTESIAN_POINT ( 'NONE',  ( 6.951808397369818766E-16, 182.3437499965860411, -11.35316468750000141 ) ) ;
#29547=CYLINDRICAL_SURFACE ( 'NONE', #12965, 6.000000000000001776 ) ;
#29548=CARTESIAN_POINT ( 'NONE',  ( 0.000000000000000000, 237.9999999999999716, 0.000000000000000000 ) ) ;
#29552=CARTESIAN_POINT ( 'NONE',  ( -9.832129032723420536, 34.01041666325269119, 5.676582343749997150 ) ) ;
#29556=DIRECTION ( 'NONE',  ( -0.000000000000000000, 1.000000000000000000, -0.000000000000000000 ) ) ;
#29557=CARTESIAN_POINT ( 'NONE',  ( 6.123233995736767268E-16, 58.12499999317203248, -10.00000000000000178 ) ) ;
#29560=CARTESIAN_POINT ( 'NONE',  ( 7.320508075688774596, 77.49999999317205379, -7.320508075688774596 ) ) ;
#29563=CARTESIAN_POINT ( 'NONE',  ( 9.999999999999996447, 55.00000000000000000, 0.000000000000000000 ) ) ;
#29564=FACE_OUTER_BOUND ( 'NONE', #35397, .T. ) ;
#29565=CARTESIAN_POINT ( 'NONE',  ( 0.000000000000000000, 300.0000000000000000, 10.00000000000000178 ) ) ;
#29570=CARTESIAN_POINT ( 'NONE',  ( 2.765530957082001251, 297.9218750017069510, 6.676582343750000703 ) ) ;
#29573=CARTESIAN_POINT ( 'NONE',  ( -5.676582343750006032, 149.1145833299193555, 9.832129032723418760 ) ) ;
#29582=CARTESIAN_POINT ( 'NONE',  ( -11.35316468750000141, 128.8020833299193555, 3.042071309553159963 ) ) ;
#29584=CARTESIAN_POINT ( 'NONE',  ( -5.999999999999999112, 291.0625000000000000, 2.485281374238575314 ) ) ;
#29586=CARTESIAN_POINT ( 'NONE',  ( -3.042071309553164404, 47.55208332991935549, -11.35316468749999963 ) ) ;
#29594=CARTESIAN_POINT ( 'NONE',  ( 6.000000000000003553, 293.6250000034140157, -2.485281374238571761 ) ) ;
#29615=ORIENTED_EDGE ( 'NONE', *, *, #43204, .T. ) ;
#29618=CARTESIAN_POINT ( 'NONE',  ( -10.00000000000000355, 57.70833333333332149, 2.679491924311223183 ) ) ;
#29622=CARTESIAN_POINT ( 'NONE',  ( -6.000000000000001776, 288.0625000034140157, 0.000000000000000000 ) ) ;
#29628=LINE ( 'NONE', #12634, #35807 ) ;
#29631=CARTESIAN_POINT ( 'NONE',  ( -7.320508075688778149, 168.1250000000000284, 7.320508075688769267 ) ) ;
#29635=CARTESIAN_POINT ( 'NONE',  ( -11.35316468750000141, 143.5937499965860411, -1.390361679473963753E-15 ) ) ;
#29642=CARTESIAN_POINT ( 'NONE',  ( 5.239869872917444660, 225.8121258658414092, -8.537502151162962960 ) ) ;
#29645=CARTESIAN_POINT ( 'NONE',  ( 8.660254037844385522, 41.45833332650536818, 5.000000000000005329 ) ) ;
#29650=DIRECTION ( 'NONE',  ( -0.000000000000000000, 1.000000000000000000, -0.000000000000000000 ) ) ;
#29655=CARTESIAN_POINT ( 'NONE',  ( -8.660254037844435260, 62.91666666666670693, 5.000000000000023981 ) ) ;
#29657=CARTESIAN_POINT ( 'NONE',  ( -3.042071309553164404, 117.2395833299193555, -11.35316468749999963 ) ) ;
#29658=ORIENTED_EDGE ( 'NONE', *, *, #21735, .T. ) ;
#29662=CARTESIAN_POINT ( 'NONE',  ( 8.660254037844389075, 217.2916666598387110, -5.000000000000000000 ) ) ;
#29666=CARTESIAN_POINT ( 'NONE',  ( -11.35316468749999785, 98.07291666325269830, -3.042071309553167957 ) ) ;
#29669=CARTESIAN_POINT ( 'NONE',  ( 2.679491924295794192, 176.0416666666681635, -10.00000000000901323 ) ) ;
#29671=CARTESIAN_POINT ( 'NONE',  ( 10.00000000000000000, 191.6666666598387394, 2.679491924311236062 ) ) ;
#29672=FACE_OUTER_BOUND ( 'NONE', #53921, .T. ) ;
#29675=CARTESIAN_POINT ( 'NONE',  ( 11.35316468749999785, 85.88541666325268409, 3.042071309553174174 ) ) ;
#29679=CARTESIAN_POINT ( 'NONE',  ( 3.042071309553159519, 15.05208332991935194, 11.35316468750000141 ) ) ;
#29681=CARTESIAN_POINT ( 'NONE',  ( -10.00000000000001066, 137.2916666666666856, -2.679491924311232953 ) ) ;
#29682=CARTESIAN_POINT ( 'NONE',  ( -11.35316468749999785, 213.0729166632526983, -3.042071309553167957 ) ) ;
#29685=CARTESIAN_POINT ( 'NONE',  ( 10.00000000000000178, 47.08333332650536107, -2.679491924311226736 ) ) ;
#29686=CARTESIAN_POINT ( 'NONE',  ( -7.320508075688778149, 149.9999999931720254, 7.320508075688769267 ) ) ;
#29687=CARTESIAN_POINT ( 'NONE',  ( -4.721056650415999201, 298.3281250017069510, -4.721056650415999201 ) ) ;
#29690=CARTESIAN_POINT ( 'NONE',  ( -5.676582343749998039, 207.7604166632526983, -9.832129032723420536 ) ) ;
#29697=VERTEX_POINT ( 'NONE', #43533 ) ;
#29701=CARTESIAN_POINT ( 'NONE',  ( 10.00000000000000178, 25.20833333333333570, -2.679491924311226736 ) ) ;
#29702=DIRECTION ( 'NONE',  ( -0.000000000000000000, 1.000000000000000000, -0.000000000000000000 ) ) ;
#29713=CARTESIAN_POINT ( 'NONE',  ( 4.721056650415999201, 298.0781250017069510, -4.721056650415999201 ) ) ;
#29715=CARTESIAN_POINT ( 'NONE',  ( -2.485281374238268004, 289.2500000034140726, 6.000000000000304645 ) ) ;
#29716=VERTEX_POINT ( 'NONE', #38268 ) ;
#29722=CARTESIAN_POINT ( 'NONE',  ( 3.042071309553159519, 105.0520833299193271, 11.35316468750000141 ) ) ;
#29730=CARTESIAN_POINT ( 'NONE',  ( -7.320508075688778149, 179.9999999931720254, 7.320508075688769267 ) ) ;
#29731=CARTESIAN_POINT ( 'NONE',  ( -2.085542519210945728E-15, 219.5312499965860411, 11.35316468750000141 ) ) ;
#29735=CARTESIAN_POINT ( 'NONE',  ( -5.676582343749998039, 182.7604166632526699, -9.832129032723420536 ) ) ;
#29741=CARTESIAN_POINT ( 'NONE',  ( -3.042071309553173730, 64.32291666325269830, 11.35316468749999785 ) ) ;
#29747=CARTESIAN_POINT ( 'NONE',  ( -8.311093377946836114, 72.65624999658604111, -8.311093377946837890 ) ) ;
#29752=CARTESIAN_POINT ( 'NONE',  ( -8.311093377946836114, 57.65624999658601268, -8.311093377946837890 ) ) ;
#29754=CARTESIAN_POINT ( 'NONE',  ( -8.660254037844387298, 13.95833332650536818, -5.000000000000004441 ) ) ;
#29755=CARTESIAN_POINT ( 'NONE',  ( 10.00000000000000000, 151.6666666598387110, 2.679491924311236062 ) ) ;
#29758=CARTESIAN_POINT ( 'NONE',  ( -8.311093377946841443, 44.21874999658602690, 8.311093377946834337 ) ) ;
#29761=CARTESIAN_POINT ( 'NONE',  ( 9.832129032723420536, 191.1979166632526983, -5.676582343749999815 ) ) ;
#29767=CARTESIAN_POINT ( 'NONE',  ( 9.832129032723416984, 180.3645833299193555, 5.676582343750006032 ) ) ;
#29773=ORIENTED_EDGE ( 'NONE', *, *, #2401, .F. ) ;
#29774=CARTESIAN_POINT ( 'NONE',  ( -9.832129032723418760, 173.1770833299193555, -5.676582343750004256 ) ) ;
#29777=CARTESIAN_POINT ( 'NONE',  ( 3.042071309553159519, 130.0520833299193555, 11.35316468750000141 ) ) ;
#29778=( BOUNDED_CURVE ( )  B_SPLINE_CURVE ( 2, ( #46906, #10720, #62760, #911, #5441, #57510, #63143, #63515, #39394, #11471, #57880, #69181, #28811 ),
 .UNSPECIFIED., .F., .F. ) 
 B_SPLINE_CURVE_WITH_KNOTS ( ( 3, 2, 2, 2, 2, 2, 3 ),
 ( 0.8006953296466258196, 0.8059278359778203615, 0.8111603423090147924, 0.8163928486402091123, 0.8216253549714036541, 0.8268578613025980850, 0.8320903676337926269 ),
 .UNSPECIFIED. ) 
 CURVE ( )  GEOMETRIC_REPRESENTATION_ITEM ( )  RATIONAL_B_SPLINE_CURVE ( ( 1.000000000000000000, 0.9659258262890684232, 1.000000000000000000, 0.9659258262890684232, 1.000000000000000000, 0.9659258262890684232, 1.000000000000000000, 0.9659258262890684232, 1.000000000000000000, 0.9659258262890684232, 1.000000000000000000, 0.9659258262894588887, 0.9999999999996095346 ) ) 
 REPRESENTATION_ITEM ( '' )  );
#29779=CARTESIAN_POINT ( 'NONE',  ( 10.58424618561840092, 225.9999999999999147, -3.898667594295466277 ) ) ;
#29787=( BOUNDED_CURVE ( )  B_SPLINE_CURVE ( 2, ( #601, #28872, #45474, #74525, #22834, #11528, #57945, #40569, #10780, #11899, #16791, #51892, #17930 ),
 .UNSPECIFIED., .F., .F. ) 
 B_SPLINE_CURVE_WITH_KNOTS ( ( 3, 2, 2, 2, 2, 2, 3 ),
 ( 0.8423913043478260532, 0.8442028985507246119, 0.8460144927536231707, 0.8478260869565217295, 0.8496376811594202882, 0.8514492753623188470, 0.8532608695652174058 ),
 .UNSPECIFIED. ) 
 CURVE ( )  GEOMETRIC_REPRESENTATION_ITEM ( )  RATIONAL_B_SPLINE_CURVE ( ( 1.000000000000000000, 0.9659258262890683122, 1.000000000000000000, 0.9659258262890683122, 1.000000000000000000, 0.9659258262890683122, 1.000000000000000000, 0.9659258262890683122, 1.000000000000000000, 0.9659258262890683122, 1.000000000000000000, 0.9659258262890683122, 1.000000000000000000 ) ) 
 REPRESENTATION_ITEM ( '' )  );
#29788=CARTESIAN_POINT ( 'NONE',  ( 0.000000000000000000, 300.0000000000000000, 0.000000000000000000 ) ) ;
#29791=CARTESIAN_POINT ( 'NONE',  ( 1.269536070779894168E-12, 186.2499999999999147, -10.00000000000000178 ) ) ;
#29795=CARTESIAN_POINT ( 'NONE',  ( -6.338495502905945601E-13, 181.2500000000000853, -10.00000000000000533 ) ) ;
#29802=EDGE_LOOP ( 'NONE', ( #26979, #67400, #29892, #34720 ) ) ;
#29808=CARTESIAN_POINT ( 'NONE',  ( 0.000000000000000000, 300.0000000000000000, 0.000000000000000000 ) ) ;
#29810=CARTESIAN_POINT ( 'NONE',  ( -4.088227598258586603E-16, 296.3593750017070079, -6.676582343750001591 ) ) ;
#29811=CARTESIAN_POINT ( 'NONE',  ( 6.123233995736767268E-16, 141.2500000000000284, -10.00000000000000178 ) ) ;
#29827=CARTESIAN_POINT ( 'NONE',  ( -2.085542519210945728E-15, 24.53124999658601624, 11.35316468750000141 ) ) ;
#29829=CARTESIAN_POINT ( 'NONE',  ( -9.832129032723418760, 223.1770833299193555, -5.676582343750004256 ) ) ;
#29836=CARTESIAN_POINT ( 'NONE',  ( 6.951808397369818766E-16, 37.03124999658601979, -11.35316468750000141 ) ) ;
#29840=FACE_OUTER_BOUND ( 'NONE', #102, .T. ) ;
#29842=CARTESIAN_POINT ( 'NONE',  ( 8.311093377946834337, 20.15624999658601268, 8.311093377946839666 ) ) ;
#29845=CARTESIAN_POINT ( 'NONE',  ( 8.311093377946837890, 146.4062499965860127, -8.311093377946837890 ) ) ;
#29847=CARTESIAN_POINT ( 'NONE',  ( 8.660254037844385522, 121.4583333265053824, 5.000000000000005329 ) ) ;
#29852=CARTESIAN_POINT ( 'NONE',  ( -9.832129032723420536, 9.010416663252684089, 5.676582343749997150 ) ) ;
#29856=CARTESIAN_POINT ( 'NONE',  ( -2.765530957081996810, 297.2656250017069510, -6.676582343750003368 ) ) ;
#29857=CARTESIAN_POINT ( 'NONE',  ( 8.311093377946837890, 136.4062499965859843, -8.311093377946837890 ) ) ;
#29864=DIRECTION ( 'NONE',  ( 0.000000000000000000, 0.000000000000000000, 1.000000000000000000 ) ) ;
#29866=CARTESIAN_POINT ( 'NONE',  ( -2.085542519210945728E-15, 94.84374999658601268, 11.35316468750000141 ) ) ;
#29886=CARTESIAN_POINT ( 'NONE',  ( -7.320508075688778149, 224.9999999931720254, 7.320508075688769267 ) ) ;
#29887=( LENGTH_UNIT ( ) NAMED_UNIT ( * ) SI_UNIT ( .MILLI., .METRE. ) );
#29889=CARTESIAN_POINT ( 'NONE',  ( -1.836970198721029983E-15, 200.6249999931720538, 10.00000000000000178 ) ) ;
#29892=ORIENTED_EDGE ( 'NONE', *, *, #570, .T. ) ;
#29894=CARTESIAN_POINT ( 'NONE',  ( -4.999999999999999112, 98.33333333333332860, 8.660254037844376640 ) ) ;
#29898=CARTESIAN_POINT ( 'NONE',  ( -5.000000000000005329, 98.33333333333334281, 8.660254037844387298 ) ) ;
#29900=CARTESIAN_POINT ( 'NONE',  ( -11.35316468749999785, 63.38541666325269119, -3.042071309553167513 ) ) ;
#29901=CARTESIAN_POINT ( 'NONE',  ( 2.765530957081996366, 296.2968750017070079, -6.676582343750003368 ) ) ;
#29904=CARTESIAN_POINT ( 'NONE',  ( 7.320508075688803018, 190.6250000000000568, -7.320508075688803018 ) ) ;
#29907=DIRECTION ( 'NONE',  ( -0.000000000000000000, 1.000000000000000000, -0.000000000000000000 ) ) ;
#29909=CARTESIAN_POINT ( 'NONE',  ( -5.999999999999999112, 293.0624999999999432, 2.485281374238575314 ) ) ;
#29911=CARTESIAN_POINT ( 'NONE',  ( 10.00000000000000000, 214.7916666666666572, 2.679491924311236062 ) ) ;
#29913=CARTESIAN_POINT ( 'NONE',  ( -8.311093377946841443, 179.2187499965859843, 8.311093377946830785 ) ) ;
#29920=CARTESIAN_POINT ( 'NONE',  ( 8.311093377946837890, 41.71874999658601979, -8.311093377946837890 ) ) ;
#29922=CARTESIAN_POINT ( 'NONE',  ( -2.085542519210945728E-15, 214.8437499965860411, 11.35316468750000141 ) ) ;
#29924=CARTESIAN_POINT ( 'NONE',  ( -2.679491924311235174, 125.4166666598386968, 10.00000000000000000 ) ) ;
#29926=CARTESIAN_POINT ( 'NONE',  ( -7.320508075688762162, 103.1249999999999858, 7.320508075688755056 ) ) ;
#29930=CARTESIAN_POINT ( 'NONE',  ( 10.00000000000000178, 81.87499999317203958, 0.000000000000000000 ) ) ;
#29934=FACE_OUTER_BOUND ( 'NONE', #18211, .T. ) ;
#29937=EDGE_CURVE ( 'NONE', #271, #29212, #50469, .T. ) ;
#29938=CARTESIAN_POINT ( 'NONE',  ( -6.676582343750003368, 296.5468750017069510, -2.765530957081996810 ) ) ;
#29941=CARTESIAN_POINT ( 'NONE',  ( 3.042071309553159519, 154.7395833299193555, 11.35316468750000141 ) ) ;
#29943=CARTESIAN_POINT ( 'NONE',  ( 10.00000000000000355, 5.000000000000000888, 0.000000000000000000 ) ) ;
#29952=CARTESIAN_POINT ( 'NONE',  ( -9.832129032723420536, 144.0104166632526699, 5.676582343749997150 ) ) ;
#29956=CARTESIAN_POINT ( 'NONE',  ( 3.042071309553159519, 50.05208332991935549, 11.35316468750000141 ) ) ;
#29958=CARTESIAN_POINT ( 'NONE',  ( -8.660254037844394404, 27.91666666666667140, 5.000000000000001776 ) ) ;
#29962=CARTESIAN_POINT ( 'NONE',  ( 6.000000000000003553, 291.5000000034140157, 2.485281374238571317 ) ) ;
#29984=CARTESIAN_POINT ( 'NONE',  ( -10.00000000000000178, 52.50000000000000711, -1.224646799147353454E-15 ) ) ;
#30000=CARTESIAN_POINT ( 'NONE',  ( 2.679491924311228956, 202.9166666598387110, -10.00000000000000000 ) ) ;
#30002=CARTESIAN_POINT ( 'NONE',  ( 10.00000000000000178, 175.0000000000000284, 0.000000000000000000 ) ) ;
#30006=CARTESIAN_POINT ( 'NONE',  ( 11.35316468750000141, 146.0937499965860411, 0.000000000000000000 ) ) ;
#30008=CARTESIAN_POINT ( 'NONE',  ( 5.000000000000001776, 27.70833332650536818, -8.660254037844389075 ) ) ;
#30011=CARTESIAN_POINT ( 'NONE',  ( -10.00000000000000533, 167.7083333333333428, 2.679491924311223627 ) ) ;
#30018=CARTESIAN_POINT ( 'NONE',  ( 8.660254037844389075, 37.29166665983869677, -5.000000000000000000 ) ) ;
#30026=CARTESIAN_POINT ( 'NONE',  ( -10.00003937256114028, 225.9999999999999716, 0.6562093533521827782 ) ) ;
#30027=DIRECTION ( 'NONE',  ( 0.000000000000000000, 0.000000000000000000, -1.000000000000000000 ) ) ;
#30029=CARTESIAN_POINT ( 'NONE',  ( -8.311093377946836114, 117.6562499965860269, -8.311093377946837890 ) ) ;
#30033=CARTESIAN_POINT ( 'NONE',  ( 5.000000000000001776, 227.7083333265053966, -8.660254037844389075 ) ) ;
#30037=CARTESIAN_POINT ( 'NONE',  ( 5.676582343750001591, 116.6145833299193697, -9.832129032723420536 ) ) ;
#30041=CARTESIAN_POINT ( 'NONE',  ( 5.000000000000001776, 82.70833332650536818, -8.660254037844389075 ) ) ;
#30043=CARTESIAN_POINT ( 'NONE',  ( -8.660254037844390851, 189.7916666598387110, 4.999999999999998224 ) ) ;
#30044=AXIS2_PLACEMENT_3D ( 'NONE', #46975, #59058, #54129 ) ;
#30047=CARTESIAN_POINT ( 'NONE',  ( 8.311093377946834337, 95.46874999658601268, 8.311093377946839666 ) ) ;
#30048=CARTESIAN_POINT ( 'NONE',  ( -4.721056650415998313, 287.5781250017069510, 4.721056650416000089 ) ) ;
#30051=CARTESIAN_POINT ( 'NONE',  ( 3.042071309553159519, 10.05208332991935016, 11.35316468750000141 ) ) ;
#30060=CARTESIAN_POINT ( 'NONE',  ( 4.721056650415999201, 294.0781250017069510, -4.721056650415999201 ) ) ;
#30062=CARTESIAN_POINT ( 'NONE',  ( -1.836970198721029983E-15, 120.6249999931720396, 10.00000000000000178 ) ) ;
#30063=CARTESIAN_POINT ( 'NONE',  ( 3.042071309553167513, 202.1354166632526983, -11.35316468749999785 ) ) ;
#30070=CARTESIAN_POINT ( 'NONE',  ( 10.00000000000000178, 30.20833333333333570, -2.679491924311226736 ) ) ;
#30078=CARTESIAN_POINT ( 'NONE',  ( -2.295000000000000373, 272.8559999999997672, 5.415577408909600265 ) ) ;
#30079=CARTESIAN_POINT ( 'NONE',  ( -2.765530957081996810, 295.2656250017070079, -6.676582343750002480 ) ) ;
#30081=CARTESIAN_POINT ( 'NONE',  ( 2.679491924311222739, 135.8333333265053682, 10.00000000000000355 ) ) ;
#30089=CARTESIAN_POINT ( 'NONE',  ( 11.35316468749999963, 96.30208332991934128, -3.042071309553165293 ) ) ;
#30090=CARTESIAN_POINT ( 'NONE',  ( -10.00000000000000000, 122.5000000000000284, -1.224646799147353059E-15 ) ) ;
#30101=CARTESIAN_POINT ( 'NONE',  ( -5.676582343749998039, 212.4479166632526983, -9.832129032723420536 ) ) ;
#30106=CARTESIAN_POINT ( 'NONE',  ( -5.676582343750006032, 184.4270833299193555, 9.832129032723418760 ) ) ;
#30113=CARTESIAN_POINT ( 'NONE',  ( 5.676582343750001591, 66.61458332991935549, -9.832129032723420536 ) ) ;
#30117=CARTESIAN_POINT ( 'NONE',  ( -10.00000000000002842, 47.50000000000001421, -1.224646799147356412E-15 ) ) ;
#30119=CARTESIAN_POINT ( 'NONE',  ( 11.35316468750000141, 75.78124999658602690, 0.000000000000000000 ) ) ;
#30124=CARTESIAN_POINT ( 'NONE',  ( -5.676582343749998039, 77.44791666325269830, -9.832129032723420536 ) ) ;
#30129=CARTESIAN_POINT ( 'NONE',  ( -10.00000000000000000, 159.1666666598386541, -2.679491924311229845 ) ) ;
#30131=CARTESIAN_POINT ( 'NONE',  ( 6.123233995736767268E-16, 53.12499999317203958, -10.00000000000000178 ) ) ;
#30132=CARTESIAN_POINT ( 'NONE',  ( 5.676582343750001591, 46.92708332991934839, -9.832129032723420536 ) ) ;
#30134=CARTESIAN_POINT ( 'NONE',  ( -3.042071309553164404, 197.2395833299193555, -11.35316468749999963 ) ) ;
#30138=CARTESIAN_POINT ( 'NONE',  ( 7.320508075688771044, 161.2499999931720538, 7.320508075688775484 ) ) ;
#30140=CARTESIAN_POINT ( 'NONE',  ( 6.951808397369818766E-16, 177.0312499965860411, -11.35316468750000141 ) ) ;
#30145=CARTESIAN_POINT ( 'NONE',  ( -9.832129032723420536, 174.0104166632526983, 5.676582343749997150 ) ) ;
#30168=ORIENTED_EDGE ( 'NONE', *, *, #26613, .F. ) ;
#30170=VERTEX_POINT ( 'NONE', #41708 ) ;
#30176=CARTESIAN_POINT ( 'NONE',  ( -6.676582343750001591, 298.6093750017069510, 0.000000000000000000 ) ) ;
#30177=CARTESIAN_POINT ( 'NONE',  ( 5.000000000000001776, 130.8333333333333428, -8.660254037844389075 ) ) ;
#30189=CARTESIAN_POINT ( 'NONE',  ( -9.999999999999998224, 132.2916666666666572, -2.679491924311230289 ) ) ;
#30194=CARTESIAN_POINT ( 'NONE',  ( -11.35316468750000141, 33.48958332991934128, 3.042071309553159963 ) ) ;
#30196=CARTESIAN_POINT ( 'NONE',  ( 3.042071309553159519, 215.0520833299193555, 11.35316468750000141 ) ) ;
#30197=DIRECTION ( 'NONE',  ( 0.000000000000000000, -0.000000000000000000, -1.000000000000000000 ) ) ;
#30200=CARTESIAN_POINT ( 'NONE',  ( 5.676582343750001591, 36.61458332991934839, -9.832129032723420536 ) ) ;
#30207=CARTESIAN_POINT ( 'NONE',  ( 5.676582343749993598, 19.94791666325268409, 9.832129032723422313 ) ) ;
#30209=CARTESIAN_POINT ( 'NONE',  ( 3.042071309553167069, 146.8229166632527267, -11.35316468749999785 ) ) ;
#30211=CARTESIAN_POINT ( 'NONE',  ( -8.660254037844387298, 113.9583333265053682, -5.000000000000004441 ) ) ;
#30215=ORIENTED_EDGE ( 'NONE', *, *, #64194, .F. ) ;
#30216=CARTESIAN_POINT ( 'NONE',  ( -8.311093377946841443, 9.218749996586016238, 8.311093377946834337 ) ) ;
#30217=( BOUNDED_CURVE ( )  B_SPLINE_CURVE ( 2, ( #73354, #26948, #21287, #15249, #72981, #56379, #29563, #40137, #52574, #6187, #68803, #74094, #40883 ),
 .UNSPECIFIED., .F., .F. ) 
 B_SPLINE_CURVE_WITH_KNOTS ( ( 3, 2, 2, 2, 2, 2, 3 ),
 ( 0.6750949594983258750, 0.6803281766356090721, 0.6855613937728922691, 0.6907946109101755772, 0.6960278280474587742, 0.7012610451847419712, 0.7064942623220252793 ),
 .UNSPECIFIED. ) 
 CURVE ( )  GEOMETRIC_REPRESENTATION_ITEM ( )  RATIONAL_B_SPLINE_CURVE ( ( 1.000000000000013545, 0.9659258262890547675, 1.000000000000000000, 0.9659258262890683122, 1.000000000000000000, 0.9659258262890683122, 1.000000000000000000, 0.9659258262890683122, 1.000000000000000000, 0.9659258262890683122, 1.000000000000000000, 0.9659258262890683122, 1.000000000000000000 ) ) 
 REPRESENTATION_ITEM ( '' )  );
#30218=EDGE_CURVE ( 'NONE', #30602, #26622, #59801, .T. ) ;
#30219=VERTEX_POINT ( 'NONE', #67699 ) ;
#30220=CARTESIAN_POINT ( 'NONE',  ( 2.485281374238858643, 289.3125000000000000, 5.999999999999716671 ) ) ;
#30222=CARTESIAN_POINT ( 'NONE',  ( -9.832129032723418760, 137.8645833299193555, -5.676582343750004256 ) ) ;
#30223=CYLINDRICAL_SURFACE ( 'NONE', #15820, 10.00000000000000178 ) ;
#30228=ORIENTED_EDGE ( 'NONE', *, *, #53092, .T. ) ;
#30230=CYLINDRICAL_SURFACE ( 'NONE', #59426, 10.00000000000000178 ) ;
#30232=CARTESIAN_POINT ( 'NONE',  ( 9.832129032723420536, 86.51041666325268409, -5.676582343749999815 ) ) ;
#30247=ADVANCED_FACE ( 'NONE', ( #38662 ), #8862, .T. ) ;
#30251=VECTOR ( 'NONE', #37166, 1000.000000000000000 ) ;
#30252=EDGE_CURVE ( 'NONE', #36674, #33382, #61288, .T. ) ;
#30261=EDGE_CURVE ( 'NONE', #28748, #46215, #9615, .T. ) ;
#30269=CARTESIAN_POINT ( 'NONE',  ( 2.679491924311228956, 96.04166666666665719, -10.00000000000000000 ) ) ;
#30271=CARTESIAN_POINT ( 'NONE',  ( -4.088227598258586603E-16, 297.3593750017070079, -6.676582343750001591 ) ) ;
#30273=CARTESIAN_POINT ( 'NONE',  ( 0.000000000000000000, 300.0000000000000000, 0.000000000000000000 ) ) ;
#30276=CARTESIAN_POINT ( 'NONE',  ( 7.320508075688779037, 84.37500000000000000, 7.320508075688782590 ) ) ;
#30280=CARTESIAN_POINT ( 'NONE',  ( 2.679491924311222739, 213.9583333333332860, 10.00000000000000355 ) ) ;
#30282=CARTESIAN_POINT ( 'NONE',  ( -9.832129032723420536, 179.0104166632526699, 5.676582343749997150 ) ) ;
#30284=FACE_OUTER_BOUND ( 'NONE', #72986, .T. ) ;
#30290=CARTESIAN_POINT ( 'NONE',  ( 9.832129032723416984, 45.67708332991934839, 5.676582343750006032 ) ) ;
#30292=CARTESIAN_POINT ( 'NONE',  ( 9.832129032723420536, 226.5104166632526983, -5.676582343749999815 ) ) ;
#30299=CARTESIAN_POINT ( 'NONE',  ( 2.679491924311222739, 75.83333332650533976, 10.00000000000000355 ) ) ;
#30302=CARTESIAN_POINT ( 'NONE',  ( -7.320508075688778149, 49.99999999317202537, 7.320508075688769267 ) ) ;
#30306=CARTESIAN_POINT ( 'NONE',  ( -1.836970198721029983E-15, 143.7500000000000284, 10.00000000000000178 ) ) ;
#30308=CARTESIAN_POINT ( 'NONE',  ( -3.042071309553173730, 149.3229166632526699, 11.35316468749999785 ) ) ;
#30309=FACE_OUTER_BOUND ( 'NONE', #63160, .T. ) ;
#30318=CARTESIAN_POINT ( 'NONE',  ( 8.311093377946837890, 146.7187499965860127, -8.311093377946837890 ) ) ;
#30322=CARTESIAN_POINT ( 'NONE',  ( -11.35316468749999785, 53.38541666325267698, -3.042071309553167513 ) ) ;
#30328=EDGE_CURVE ( 'NONE', #45065, #56250, #63930, .T. ) ;
#30329=CARTESIAN_POINT ( 'NONE',  ( 4.242640687119285658, 292.6875000034139589, -4.242640687119286547 ) ) ;
#30330=CARTESIAN_POINT ( 'NONE',  ( 0.000000000000000000, 300.0000000000000000, 0.000000000000000000 ) ) ;
#30348=EDGE_CURVE ( 'NONE', #52317, #3422, #22487, .T. ) ;
#30354=CARTESIAN_POINT ( 'NONE',  ( -8.660254037844390851, 57.91666666666667140, 4.999999999999998224 ) ) ;
#30356=CARTESIAN_POINT ( 'NONE',  ( 4.242640687119287435, 298.3750000000000000, 4.242640687119285658 ) ) ;
#30359=ORIENTED_EDGE ( 'NONE', *, *, #51117, .F. ) ;
#30364=CARTESIAN_POINT ( 'NONE',  ( 6.123233995736767268E-16, 91.25000000000001421, -10.00000000000000178 ) ) ;
#30369=CARTESIAN_POINT ( 'NONE',  ( -1.836970198721029983E-15, 168.7500000000000000, 10.00000000000000178 ) ) ;
#30370=CARTESIAN_POINT ( 'NONE',  ( 4.242640687119285658, 297.6875000034139589, -4.242640687119286547 ) ) ;
#30373=CARTESIAN_POINT ( 'NONE',  ( -8.311093377946841443, 139.2187499965860127, 8.311093377946830785 ) ) ;
#30375=CARTESIAN_POINT ( 'NONE',  ( 7.320508075688774596, 27.49999999317203248, -7.320508075688774596 ) ) ;
#30377=CARTESIAN_POINT ( 'NONE',  ( 8.660254037844389075, 107.2916666598387110, -5.000000000000000000 ) ) ;
#30380=CARTESIAN_POINT ( 'NONE',  ( -8.311093377946836114, 12.96874999658601446, -8.311093377946837890 ) ) ;
#30386=CARTESIAN_POINT ( 'NONE',  ( -7.320508075688773708, 38.74999999317203958, -7.320508075688774596 ) ) ;
#30391=CYLINDRICAL_SURFACE ( 'NONE', #17821, 6.000000000000001776 ) ;
#30395=CARTESIAN_POINT ( 'NONE',  ( -2.679491924311249385, 63.54166666666669983, 10.00000000000005329 ) ) ;
#30398=CARTESIAN_POINT ( 'NONE',  ( 9.832129032723416984, 110.3645833299193555, 5.676582343750006032 ) ) ;
#30406=CARTESIAN_POINT ( 'NONE',  ( 3.042071309553167513, 116.8229166632526841, -11.35316468749999785 ) ) ;
#30408=CARTESIAN_POINT ( 'NONE',  ( 7.320508075688775484, 49.37500000000000000, 7.320508075688779037 ) ) ;
#30410=CARTESIAN_POINT ( 'NONE',  ( 2.679491924311222739, 205.8333333265053966, 10.00000000000000355 ) ) ;
#30413=CARTESIAN_POINT ( 'NONE',  ( -3.042071309553173730, 99.63541666325268409, 11.35316468749999785 ) ) ;
#30417=CARTESIAN_POINT ( 'NONE',  ( 11.35316468749999963, 6.302083329919350163, -3.042071309553165293 ) ) ;
#30419=EDGE_CURVE ( 'NONE', #54290, #5538, #30217, .T. ) ;
#30420=CARTESIAN_POINT ( 'NONE',  ( -7.320508075688779925, 136.8750000000000000, -7.320508075688781702 ) ) ;
#30426=CARTESIAN_POINT ( 'NONE',  ( -2.765530957081996810, 291.2656250017070079, -6.676582343750003368 ) ) ;
#30428=CARTESIAN_POINT ( 'NONE',  ( 8.311093377946834337, 225.4687499965860411, 8.311093377946839666 ) ) ;
#30429=EDGE_CURVE ( 'NONE', #73073, #3534, #22051, .T. ) ;
#30450=CARTESIAN_POINT ( 'NONE',  ( 1.377000000000000002, 284.2799999999998590, 5.684444333912814784 ) ) ;
#30451=CARTESIAN_POINT ( 'NONE',  ( -4.721056650415998313, 290.5781250017069510, 4.721056650416000089 ) ) ;
#30461=CARTESIAN_POINT ( 'NONE',  ( 11.35316468749999785, 105.8854166632526983, 3.042071309553174174 ) ) ;
#30469=CARTESIAN_POINT ( 'NONE',  ( -10.00000000000000000, 179.1666666598387110, -2.679491924311229845 ) ) ;
#30470=CARTESIAN_POINT ( 'NONE',  ( -8.311093377946836114, 217.6562499965860127, -8.311093377946837890 ) ) ;
#30474=CARTESIAN_POINT ( 'NONE',  ( -11.35316468749999785, 188.3854166632526983, -3.042071309553167513 ) ) ;
#30481=CARTESIAN_POINT ( 'NONE',  ( -3.042071309553164404, 72.23958332991935549, -11.35316468749999963 ) ) ;
#30484=VERTEX_POINT ( 'NONE', #74462 ) ;
#30487=CARTESIAN_POINT ( 'NONE',  ( -5.676582343750006032, 74.11458332991935549, 9.832129032723418760 ) ) ;
#30491=CARTESIAN_POINT ( 'NONE',  ( 1.567784982238203817E-13, 73.75000000000002842, 10.00000000000000533 ) ) ;
#30493=CARTESIAN_POINT ( 'NONE',  ( 9.832129032723420536, 71.19791666325268409, -5.676582343749999815 ) ) ;
#30495=CARTESIAN_POINT ( 'NONE',  ( 2.679491924311222739, 160.8333333265053682, 10.00000000000000355 ) ) ;
#30497=EDGE_CURVE ( 'NONE', #28711, #46242, #29778, .T. ) ;
#30499=CARTESIAN_POINT ( 'NONE',  ( -5.676582343750006032, 64.42708332991935549, 9.832129032723418760 ) ) ;
#30501=CARTESIAN_POINT ( 'NONE',  ( 5.676582343749993598, 194.9479166632526983, 9.832129032723422313 ) ) ;
#30508=CARTESIAN_POINT ( 'NONE',  ( 8.311093377946837890, 191.4062499965860127, -8.311093377946837890 ) ) ;
#30513=CARTESIAN_POINT ( 'NONE',  ( -9.832129032723420536, 179.0104166632526699, 5.676582343749997150 ) ) ;
#30515=CARTESIAN_POINT ( 'NONE',  ( 3.527950947924078040, 225.9999999999998295, -9.433590150150084952 ) ) ;
#30526=CARTESIAN_POINT ( 'NONE',  ( -5.000000000000000000, 186.6666666666666856, -8.660254037844390851 ) ) ;
#30528=DIRECTION ( 'NONE',  ( -0.000000000000000000, 1.000000000000000000, -0.000000000000000000 ) ) ;
#30546=CARTESIAN_POINT ( 'NONE',  ( 4.721056650416000089, 293.9843750017070079, 4.721056650415999201 ) ) ;
#30547=CARTESIAN_POINT ( 'NONE',  ( -5.000000000000005329, 128.3333333333333428, 8.660254037844387298 ) ) ;
#30551=CARTESIAN_POINT ( 'NONE',  ( 2.485281374238247132, 290.7500000034139020, -6.000000000000325961 ) ) ;
#30559=CARTESIAN_POINT ( 'NONE',  ( -5.711993833409989278E-12, 133.7499999999995737, 9.999999999999998224 ) ) ;
#30564=CARTESIAN_POINT ( 'NONE',  ( -11.35316468750000141, 23.28124999658601979, -1.390361679473963753E-15 ) ) ;
#30565=CARTESIAN_POINT ( 'NONE',  ( -8.660254037844387298, 13.95833332650536818, -5.000000000000004441 ) ) ;
#30570=CARTESIAN_POINT ( 'NONE',  ( 11.35316468750000141, 30.78124999658601979, 0.000000000000000000 ) ) ;
#30576=CARTESIAN_POINT ( 'NONE',  ( -11.35316468750000141, 33.48958332991934839, 3.042071309553159963 ) ) ;
#30578=CARTESIAN_POINT ( 'NONE',  ( -3.042071309553173730, 149.3229166632526699, 11.35316468749999785 ) ) ;
#30579=CARTESIAN_POINT ( 'NONE',  ( 5.000000000000001776, 112.7083333265053682, -8.660254037844389075 ) ) ;
#30581=CARTESIAN_POINT ( 'NONE',  ( 1.102182119232618108E-15, 296.2500000000000000, 6.000000000000001776 ) ) ;
#30586=CARTESIAN_POINT ( 'NONE',  ( 11.35316468750000141, 26.09374999658601624, 0.000000000000000000 ) ) ;
#30590=CARTESIAN_POINT ( 'NONE',  ( -5.676582343750006032, 154.1145833299193555, 9.832129032723418760 ) ) ;
#30599=CARTESIAN_POINT ( 'NONE',  ( -9.832129032723418760, 93.17708332991935549, -5.676582343750004256 ) ) ;
#30602=VERTEX_POINT ( 'NONE', #6922 ) ;
#30631=CARTESIAN_POINT ( 'NONE',  ( -7.320508075688770155, 31.87500000000000000, -7.320508075688771044 ) ) ;
#30632=CARTESIAN_POINT ( 'NONE',  ( -2.679491924311225848, 91.45833333333332860, -10.00000000000000178 ) ) ;
#30633=EDGE_CURVE ( 'NONE', #64059, #18479, #71605, .T. ) ;
#30636=CARTESIAN_POINT ( 'NONE',  ( -2.765530957081998586, 295.7968750017070079, 6.676582343750001591 ) ) ;
#30637=ORIENTED_EDGE ( 'NONE', *, *, #51034, .F. ) ;
#30642=CARTESIAN_POINT ( 'NONE',  ( -5.000000000000006217, 53.33333333333333570, 8.660254037844390851 ) ) ;
#30646=( BOUNDED_CURVE ( )  B_SPLINE_CURVE ( 2, ( #57614, #11574, #16845, #39872, #62874, #1020, #35349, #12317, #46644, #68915, #23637, #29669, #40995 ),
 .UNSPECIFIED., .F., .F. ) 
 B_SPLINE_CURVE_WITH_KNOTS ( ( 3, 2, 2, 2, 2, 2, 3 ),
 ( 2.182283889826081236, 2.187517731460320913, 2.192751573094560591, 2.197985414728800269, 2.203219256363039502, 2.208453097997279180, 2.213686939631518857 ),
 .UNSPECIFIED. ) 
 CURVE ( )  GEOMETRIC_REPRESENTATION_ITEM ( )  RATIONAL_B_SPLINE_CURVE ( ( 1.000000000000085709, 0.9659258262889827140, 1.000000000000000000, 0.9659258262890683122, 1.000000000000000000, 0.9659258262890683122, 1.000000000000000000, 0.9659258262890683122, 1.000000000000000000, 0.9659258262890683122, 1.000000000000000000, 0.9659258262888490432, 1.000000000000219158 ) ) 
 REPRESENTATION_ITEM ( '' )  );
#30647=CARTESIAN_POINT ( 'NONE',  ( -7.320508075688773708, 211.8749999999999432, -7.320508075688774596 ) ) ;
#30649=CARTESIAN_POINT ( 'NONE',  ( 9.832129032723420536, 176.5104166632526699, -5.676582343749999815 ) ) ;
#30658=CARTESIAN_POINT ( 'NONE',  ( -5.676582343749998039, 47.76041666325269119, -9.832129032723420536 ) ) ;
#30660=CARTESIAN_POINT ( 'NONE',  ( 3.042071309553167069, 217.1354166632526983, -11.35316468749999785 ) ) ;
#30666=CARTESIAN_POINT ( 'NONE',  ( -11.35316468750000141, 103.4895833299193697, 3.042071309553159963 ) ) ;
#30667=CARTESIAN_POINT ( 'NONE',  ( -1.836970198721029983E-15, 80.62499999317203958, 10.00000000000000178 ) ) ;
#30673=EDGE_LOOP ( 'NONE', ( #40934, #9986, #11226, #73364 ) ) ;
#30675=CARTESIAN_POINT ( 'NONE',  ( -4.721056650415998313, 293.7343750017069510, 4.721056650416000089 ) ) ;
#30677=CARTESIAN_POINT ( 'NONE',  ( -11.35316468750000141, 153.2812499965860127, -1.390361679473963753E-15 ) ) ;
#30686=CARTESIAN_POINT ( 'NONE',  ( -9.832129032723418760, 148.1770833299193555, -5.676582343750004256 ) ) ;
#30691=CARTESIAN_POINT ( 'NONE',  ( -9.832129032723418760, 43.17708332991934839, -5.676582343750004256 ) ) ;
#30697=CARTESIAN_POINT ( 'NONE',  ( 6.000000000000001776, 292.5625000034140157, -7.347880794884121708E-16 ) ) ;
#30703=CARTESIAN_POINT ( 'NONE',  ( -10.00000000000000178, 64.37499999317203958, -1.224646799147353454E-15 ) ) ;
#30720=CARTESIAN_POINT ( 'NONE',  ( -2.679491924311225848, 51.45833333333332860, -10.00000000000000178 ) ) ;
#30722=CARTESIAN_POINT ( 'NONE',  ( 4.242640687119285658, 296.6250000000000000, -4.242640687119286547 ) ) ;
#30724=LINE ( 'NONE', #58311, #47858 ) ;
#30735=CARTESIAN_POINT ( 'NONE',  ( -8.660254037844390851, 172.9166666666666856, 4.999999999999998224 ) ) ;
#30739=CARTESIAN_POINT ( 'NONE',  ( 8.311093377946834337, 145.4687499965860411, 8.311093377946839666 ) ) ;
#30740=CARTESIAN_POINT ( 'NONE',  ( 2.485281374238939911, 294.3750000034140157, 5.999999999999634959 ) ) ;
#30745=CARTESIAN_POINT ( 'NONE',  ( -8.311093377946841443, 4.218749996586018014, 8.311093377946830785 ) ) ;
#30747=CARTESIAN_POINT ( 'NONE',  ( -9.999999999999994671, 112.4999999999999858, -1.224646799147352665E-15 ) ) ;
#30751=CARTESIAN_POINT ( 'NONE',  ( -7.320508075688778149, 34.99999999317203958, 7.320508075688769267 ) ) ;
#30762=CARTESIAN_POINT ( 'NONE',  ( 11.35316468750000141, 120.7812499965860269, 0.000000000000000000 ) ) ;
#30769=CARTESIAN_POINT ( 'NONE',  ( -11.35316468750000141, 118.4895833299193697, 3.042071309553159963 ) ) ;
#30771=EDGE_CURVE ( 'NONE', #42176, #68967, #48492, .T. ) ;
#30772=CARTESIAN_POINT ( 'NONE',  ( 5.000000000000004441, 50.83333333333333570, -8.660254037844390851 ) ) ;
#30775=CARTESIAN_POINT ( 'NONE',  ( -4.999999999999998224, 208.5416666598387394, -8.660254037844389075 ) ) ;
#30778=CARTESIAN_POINT ( 'NONE',  ( -5.676582343750006032, 104.4270833299193555, 9.832129032723418760 ) ) ;
#30783=CARTESIAN_POINT ( 'NONE',  ( -8.311093377946836114, 7.968749996586014461, -8.311093377946837890 ) ) ;
#30785=CARTESIAN_POINT ( 'NONE',  ( 4.999999999999993783, 181.0416666598387110, 8.660254037844390851 ) ) ;
#30787=CARTESIAN_POINT ( 'NONE',  ( 10.00000000000000178, 117.0833333265053824, -2.679491924311226736 ) ) ;
#30789=FACE_OUTER_BOUND ( 'NONE', #8535, .T. ) ;
#30791=CARTESIAN_POINT ( 'NONE',  ( -2.765530957081996810, 293.2656250017068942, -6.676582343750003368 ) ) ;
#30793=CARTESIAN_POINT ( 'NONE',  ( 6.951808397369818766E-16, 222.3437499965860127, -11.35316468750000141 ) ) ;
#30795=VECTOR ( 'NONE', #34921, 1000.000000000000000 ) ;
#30806=EDGE_LOOP ( 'NONE', ( #963, #43019, #36253, #19021 ) ) ;
#30808=CARTESIAN_POINT ( 'NONE',  ( -8.660254037844390851, 29.79166665983870388, 4.999999999999998224 ) ) ;
#30810=CARTESIAN_POINT ( 'NONE',  ( -1.377000000000000002, 284.2799999999998590, 5.684453117602865646 ) ) ;
#30811=CARTESIAN_POINT ( 'NONE',  ( -6.676582343749999815, 293.5156250017070079, 2.765530957082001251 ) ) ;
#30822=CARTESIAN_POINT ( 'NONE',  ( 8.311093377946834337, 105.4687499965860127, 8.311093377946839666 ) ) ;
#30830=CARTESIAN_POINT ( 'NONE',  ( 5.676582343750001591, 206.6145833299193555, -9.832129032723420536 ) ) ;
#30836=CARTESIAN_POINT ( 'NONE',  ( 8.311093377946834337, 195.4687499965859843, 8.311093377946839666 ) ) ;
#30843=CARTESIAN_POINT ( 'NONE',  ( 5.676582343750001591, 81.61458332991935549, -9.832129032723420536 ) ) ;
#30846=CARTESIAN_POINT ( 'NONE',  ( 8.660254037844396180, 140.4166666666666572, -5.000000000000004441 ) ) ;
#30851=CARTESIAN_POINT ( 'NONE',  ( -11.35316468750000141, 73.28124999658602690, -1.390361679473963753E-15 ) ) ;
#30858=CARTESIAN_POINT ( 'NONE',  ( 9.832129032723416984, 75.36458332991935549, 5.676582343750006032 ) ) ;
#30863=CARTESIAN_POINT ( 'NONE',  ( 5.000000000000001776, 162.7083333265053966, -8.660254037844389075 ) ) ;
#30866=CARTESIAN_POINT ( 'NONE',  ( -5.676582343749998039, 57.76041666325268409, -9.832129032723420536 ) ) ;
#30869=CARTESIAN_POINT ( 'NONE',  ( 8.311093377946837890, 201.4062499965860127, -8.311093377946837890 ) ) ;
#30870=EDGE_LOOP ( 'NONE', ( #49255, #41638, #73358, #44251, #32077 ) ) ;
#30871=DIRECTION ( 'NONE',  ( -0.000000000000000000, 1.000000000000000000, -0.000000000000000000 ) ) ;
#30873=CARTESIAN_POINT ( 'NONE',  ( 2.679491924311149464, 60.83333332650535397, 10.00000000000004619 ) ) ;
#30875=CARTESIAN_POINT ( 'NONE',  ( -8.311093377946836114, 187.6562499965860411, -8.311093377946837890 ) ) ;
#30880=CARTESIAN_POINT ( 'NONE',  ( -3.042071309553173730, 184.6354166632526983, 11.35316468749999785 ) ) ;
#30885=VERTEX_POINT ( 'NONE', #15912 ) ;
#30887=CARTESIAN_POINT ( 'NONE',  ( 2.679491924311228956, 6.041666666666666075, -10.00000000000000000 ) ) ;
#30896=CARTESIAN_POINT ( 'NONE',  ( 5.000000000000028422, 180.8333333333333997, -8.660254037844435260 ) ) ;
#30909=CARTESIAN_POINT ( 'NONE',  ( -2.765530957081998142, 293.7968750017070079, 6.676582343750000703 ) ) ;
#30910=CARTESIAN_POINT ( 'NONE',  ( -2.679491924311235618, 153.5416666666666856, 10.00000000000000000 ) ) ;
#30925=CARTESIAN_POINT ( 'NONE',  ( 9.832129032723420536, 36.19791666325268409, -5.676582343749999815 ) ) ;
#30927=CARTESIAN_POINT ( 'NONE',  ( -10.00000000000000178, 4.374999993172032475, -1.224646799147353454E-15 ) ) ;
#30931=CARTESIAN_POINT ( 'NONE',  ( -7.320508075688778149, 129.9999999931719969, 7.320508075688769267 ) ) ;
#30934=CARTESIAN_POINT ( 'NONE',  ( 11.35316468749999785, 40.57291666325268409, 3.042071309553174174 ) ) ;
#30941=CARTESIAN_POINT ( 'NONE',  ( -8.311093377946836114, 27.65624999658601979, -8.311093377946837890 ) ) ;
#30943=CARTESIAN_POINT ( 'NONE',  ( -8.311093377946841443, 153.9062499965860127, 8.311093377946830785 ) ) ;
#30944=CARTESIAN_POINT ( 'NONE',  ( -2.679491924311225848, 128.3333333265053682, -10.00000000000000178 ) ) ;
#30949=CARTESIAN_POINT ( 'NONE',  ( -5.999999999999999112, 289.0625000000000000, 2.485281374238575314 ) ) ;
#30950=CARTESIAN_POINT ( 'NONE',  ( 3.042071309553159519, 25.05208332991934839, 11.35316468750000141 ) ) ;
#30952=FACE_OUTER_BOUND ( 'NONE', #37146, .T. ) ;
#30953=CARTESIAN_POINT ( 'NONE',  ( 1.959434878635763554E-15, 237.9999999999999716, -15.99999999999998579 ) ) ;
#30955=CARTESIAN_POINT ( 'NONE',  ( 8.311093377946834337, 155.1562499965860127, 8.311093377946839666 ) ) ;
#30963=AXIS2_PLACEMENT_3D ( 'NONE', #53005, #59405, #12989 ) ;
#30966=CARTESIAN_POINT ( 'NONE',  ( -11.35316468749999785, 103.3854166632526699, -3.042071309553167513 ) ) ;
#30997=CARTESIAN_POINT ( 'NONE',  ( -10.00000000000000000, 112.2916666666666714, -2.679491924311229845 ) ) ;
#31000=CARTESIAN_POINT ( 'NONE',  ( -6.676582343750003368, 296.5468750017069510, -2.765530957081996810 ) ) ;
#31005=CARTESIAN_POINT ( 'NONE',  ( -1.836970198721029983E-15, 40.62499999317203248, 10.00000000000000178 ) ) ;
#31010=CARTESIAN_POINT ( 'NONE',  ( -7.320508075688778149, 213.1249999999999716, 7.320508075688769267 ) ) ;
#31012=CARTESIAN_POINT ( 'NONE',  ( 5.676582343750001591, 196.9270833299193839, -9.832129032723420536 ) ) ;
#31021=CARTESIAN_POINT ( 'NONE',  ( -9.832129032723420536, 44.01041666325268409, 5.676582343749997150 ) ) ;
#31023=CARTESIAN_POINT ( 'NONE',  ( 9.832129032723416984, 220.6770833299193555, 5.676582343750006032 ) ) ;
#31025=CARTESIAN_POINT ( 'NONE',  ( -5.000000000000005329, 125.2083333265053540, 8.660254037844387298 ) ) ;
#31027=CARTESIAN_POINT ( 'NONE',  ( -7.320508075688778149, 59.99999999317203248, 7.320508075688769267 ) ) ;
#31029=CARTESIAN_POINT ( 'NONE',  ( 3.042071309553167069, 111.8229166632526983, -11.35316468749999785 ) ) ;
#31030=ADVANCED_FACE ( 'NONE', ( #73066 ), #54984, .T. ) ;
#31031=CARTESIAN_POINT ( 'NONE',  ( -8.660254037844390851, 89.79166665983869677, 4.999999999999998224 ) ) ;
#31038=CARTESIAN_POINT ( 'NONE',  ( 4.721056650416000089, 294.9843750017070079, 4.721056650415999201 ) ) ;
#31040=CARTESIAN_POINT ( 'NONE',  ( -11.35316468750000141, 168.2812499965860411, -1.390361679473963753E-15 ) ) ;
#31047=CARTESIAN_POINT ( 'NONE',  ( -11.35316468749999785, 143.3854166632526983, -3.042071309553167957 ) ) ;
#31051=CARTESIAN_POINT ( 'NONE',  ( 11.35316468749999963, 61.30208332991934839, -3.042071309553165293 ) ) ;
#31057=CARTESIAN_POINT ( 'NONE',  ( 2.485281374238575314, 294.3750000034139589, 6.000000000000000888 ) ) ;
#31063=EDGE_CURVE ( 'NONE', #34861, #6677, #46134, .T. ) ;
#31064=CARTESIAN_POINT ( 'NONE',  ( -10.00000000000000355, 64.58333332650536818, 2.679491924311223183 ) ) ;
#31078=CARTESIAN_POINT ( 'NONE',  ( -5.000000000000005329, 203.3333333333333428, 8.660254037844387298 ) ) ;
#31081=CARTESIAN_POINT ( 'NONE',  ( 6.123233995736767268E-16, 56.25000000000000000, -10.00000000000000178 ) ) ;
#31083=CARTESIAN_POINT ( 'NONE',  ( -4.242640687119286547, 296.8750000000000000, -4.242640687119286547 ) ) ;
#31091=CARTESIAN_POINT ( 'NONE',  ( 0.000000000000000000, 237.9999999999999716, 0.000000000000000000 ) ) ;
#31095=CARTESIAN_POINT ( 'NONE',  ( 6.123233995736767268E-16, 171.2500000000000000, -10.00000000000000178 ) ) ;
#31099=CARTESIAN_POINT ( 'NONE',  ( -11.35316468749999785, 153.3854166632526699, -3.042071309553167513 ) ) ;
#31104=CARTESIAN_POINT ( 'NONE',  ( -7.320508075688775484, 166.8750000000000284, -7.320508075688776373 ) ) ;
#31107=CARTESIAN_POINT ( 'NONE',  ( 11.35316468749999963, 11.30208332991934839, -3.042071309553165293 ) ) ;
#31109=CARTESIAN_POINT ( 'NONE',  ( 6.123233995736767268E-16, 93.12499999317203958, -10.00000000000000178 ) ) ;
#31116=CARTESIAN_POINT ( 'NONE',  ( -2.679491924311235618, 40.41666665983869677, 10.00000000000000000 ) ) ;
#31121=CARTESIAN_POINT ( 'NONE',  ( 6.000000000000003553, 291.5000000034140157, 2.485281374238571317 ) ) ;
#31122=FACE_OUTER_BOUND ( 'NONE', #16230, .T. ) ;
#31123=EDGE_LOOP ( 'NONE', ( #46403, #11396, #66465, #14831, #7142 ) ) ;
#31126=CARTESIAN_POINT ( 'NONE',  ( 9.832129032723420536, 126.1979166632526983, -5.676582343749999815 ) ) ;
#31134=CARTESIAN_POINT ( 'NONE',  ( -3.042071309553163960, 112.2395833299193555, -11.35316468749999963 ) ) ;
#31136=CARTESIAN_POINT ( 'NONE',  ( 4.999999999999993783, 146.0416666598387110, 8.660254037844390851 ) ) ;
#31138=CARTESIAN_POINT ( 'NONE',  ( -10.00000000000000178, 204.3749999931720538, -1.224646799147353454E-15 ) ) ;
#31142=CARTESIAN_POINT ( 'NONE',  ( 9.832129032723420536, 106.5104166632526841, -5.676582343749999815 ) ) ;
#31147=CARTESIAN_POINT ( 'NONE',  ( 9.832129032723416984, 15.67708332991935016, 5.676582343750006032 ) ) ;
#31149=CARTESIAN_POINT ( 'NONE',  ( 10.00000000000000000, 181.6666666598387110, 2.679491924311235618 ) ) ;
#31151=CARTESIAN_POINT ( 'NONE',  ( 8.660254037844389075, 117.2916666598386968, -5.000000000000000000 ) ) ;
#31155=CARTESIAN_POINT ( 'NONE',  ( 2.765530957081996366, 293.1406250017069510, -6.676582343750003368 ) ) ;
#31159=CARTESIAN_POINT ( 'NONE',  ( 11.35316468749999963, 131.3020833299193555, -3.042071309553165293 ) ) ;
#31163=ADVANCED_FACE ( 'NONE', ( #72315 ), #49684, .T. ) ;
#31175=ORIENTED_EDGE ( 'NONE', *, *, #2505, .F. ) ;
#31181=CARTESIAN_POINT ( 'NONE',  ( 1.377000000000000002, 261.4319999999996753, 5.673913216232851831 ) ) ;
#31182=CARTESIAN_POINT ( 'NONE',  ( 6.676582343750001591, 293.9531250017069510, -8.176455196517173205E-16 ) ) ;
#31195=CARTESIAN_POINT ( 'NONE',  ( -5.676582343749998039, 107.7604166632526841, -9.832129032723420536 ) ) ;
#31203=CARTESIAN_POINT ( 'NONE',  ( -8.311093377946841443, 208.9062499965860411, 8.311093377946830785 ) ) ;
#31204=( BOUNDED_CURVE ( )  B_SPLINE_CURVE ( 2, ( #43630, #32709, #22101, #3277, #61362, #56457, #73424, #61738, #4774 ),
 .UNSPECIFIED., .F., .F. ) 
 B_SPLINE_CURVE_WITH_KNOTS ( ( 3, 2, 2, 2, 3 ),
 ( 0.3124999999999979461, 0.3229166666666646313, 0.3333333333333312609, 0.3437499999999979461, 0.3541666666666646313 ),
 .UNSPECIFIED. ) 
 CURVE ( )  GEOMETRIC_REPRESENTATION_ITEM ( )  RATIONAL_B_SPLINE_CURVE ( ( 1.000000000000015099, 0.9238795325112717505, 1.000000000000000000, 0.9238795325112867385, 1.000000000000000000, 0.9238795325112867385, 1.000000000000000000, 0.9238795325113017265, 0.9999999999999850120 ) ) 
 REPRESENTATION_ITEM ( '' )  );
#31209=CARTESIAN_POINT ( 'NONE',  ( -8.311093377946836114, 192.9687499965859843, -8.311093377946837890 ) ) ;
#31216=CARTESIAN_POINT ( 'NONE',  ( 11.35316468750000141, 85.78124999658602690, 0.000000000000000000 ) ) ;
#31221=CARTESIAN_POINT ( 'NONE',  ( 6.123233995736767268E-16, 108.1249999931720396, -10.00000000000000178 ) ) ;
#31222=CARTESIAN_POINT ( 'NONE',  ( 11.35316468749999963, 85.98958332991936970, -3.042071309553165293 ) ) ;
#31223=VERTEX_POINT ( 'NONE', #23165 ) ;
#31228=CARTESIAN_POINT ( 'NONE',  ( 7.320508075688794136, 74.37500000000004263, 7.320508075688798577 ) ) ;
#31230=CARTESIAN_POINT ( 'NONE',  ( 11.35316468749999963, 75.98958332991935549, -3.042071309553165293 ) ) ;
#31233=CARTESIAN_POINT ( 'NONE',  ( 2.679491924311222739, 165.8333333265053682, 10.00000000000000355 ) ) ;
#31236=CARTESIAN_POINT ( 'NONE',  ( 3.042071309553167513, 67.13541666325268409, -11.35316468749999785 ) ) ;
#31237=CARTESIAN_POINT ( 'NONE',  ( 6.676582343750004256, 291.8906250017069510, 2.765530957081995478 ) ) ;
#31239=CARTESIAN_POINT ( 'NONE',  ( 8.311093377946834337, 200.1562499965860695, 8.311093377946839666 ) ) ;
#31245=CARTESIAN_POINT ( 'NONE',  ( -11.35316468750000141, 193.2812499965860127, -1.390361679473963753E-15 ) ) ;
#31250=CARTESIAN_POINT ( 'NONE',  ( -11.35316468749999785, 183.3854166632526699, -3.042071309553167957 ) ) ;
#31273=EDGE_CURVE ( 'NONE', #32512, #47954, #57141, .T. ) ;
#31276=CARTESIAN_POINT ( 'NONE',  ( 11.35316468749999785, 60.88541666325269119, 3.042071309553174174 ) ) ;
#31281=CARTESIAN_POINT ( 'NONE',  ( -6.676582343750001591, 292.6093750017069510, 0.000000000000000000 ) ) ;
#31282=CARTESIAN_POINT ( 'NONE',  ( -4.999999999999998224, 146.6666666666666572, -8.660254037844389075 ) ) ;
#31291=LINE ( 'NONE', #66367, #9481 ) ;
#31292=CARTESIAN_POINT ( 'NONE',  ( 10.00000000000000533, 135.2083333333333144, -2.679491924311227624 ) ) ;
#31297=CARTESIAN_POINT ( 'NONE',  ( -8.311093377946836114, 42.65624999658600558, -8.311093377946837890 ) ) ;
#31298=CARTESIAN_POINT ( 'NONE',  ( 2.679491924312849882, 151.0416666666665151, -9.999999999999067413 ) ) ;
#31299=CARTESIAN_POINT ( 'NONE',  ( -7.320508075688773708, 8.749999993172030699, -7.320508075688774596 ) ) ;
#31303=CARTESIAN_POINT ( 'NONE',  ( -7.320508075688773708, 128.7499999931720538, -7.320508075688774596 ) ) ;
#31305=CARTESIAN_POINT ( 'NONE',  ( 8.311093377946834337, 35.15624999658601979, 8.311093377946839666 ) ) ;
#31308=CARTESIAN_POINT ( 'NONE',  ( -6.000000000000003553, 298.9374999999999432, -2.485281374238571317 ) ) ;
#31311=CARTESIAN_POINT ( 'NONE',  ( -5.676582343749998039, 27.44791666325268409, -9.832129032723420536 ) ) ;
#31313=CARTESIAN_POINT ( 'NONE',  ( -11.35316468749999785, 158.0729166632526699, -3.042071309553167513 ) ) ;
#31315=CARTESIAN_POINT ( 'NONE',  ( -10.00000000000000355, 124.5833333265053682, 2.679491924311223183 ) ) ;
#31319=CARTESIAN_POINT ( 'NONE',  ( -5.676582343749998039, 17.76041666325268409, -9.832129032723420536 ) ) ;
#31320=( BOUNDED_CURVE ( )  B_SPLINE_CURVE ( 2, ( #41322, #34567, #46232, #63962, #11535, #12273, #6626, #70366, #34940, #23962, #5883, #30000, #40576 ),
 .UNSPECIFIED., .F., .F. ) 
 B_SPLINE_CURVE_WITH_KNOTS ( ( 3, 2, 2, 2, 2, 2, 3 ),
 ( 0.8641304347826086474, 0.8659420289855072062, 0.8677536231884057649, 0.8695652173913043237, 0.8713768115942028825, 0.8731884057971014412, 0.8750000000000000000 ),
 .UNSPECIFIED. ) 
 CURVE ( )  GEOMETRIC_REPRESENTATION_ITEM ( )  RATIONAL_B_SPLINE_CURVE ( ( 1.000000000000000000, 0.9659258262890683122, 1.000000000000000000, 0.9659258262890683122, 1.000000000000000000, 0.9659258262890683122, 1.000000000000000000, 0.9659258262890683122, 1.000000000000000000, 0.9659258262890683122, 1.000000000000000000, 0.9659258262890683122, 1.000000000000000000 ) ) 
 REPRESENTATION_ITEM ( '' )  );
#31325=CARTESIAN_POINT ( 'NONE',  ( -3.042071309553163960, 157.2395833299193555, -11.35316468749999963 ) ) ;
#31334=CARTESIAN_POINT ( 'NONE',  ( -4.242640687119286547, 291.9375000034140157, -4.242640687119286547 ) ) ;
#31335=CARTESIAN_POINT ( 'NONE',  ( 5.676582343749993598, 100.2604166632526841, 9.832129032723422313 ) ) ;
#31357=DIRECTION ( 'NONE',  ( 0.000000000000000000, 0.000000000000000000, 1.000000000000000000 ) ) ;
#31371=CARTESIAN_POINT ( 'NONE',  ( -2.679491924311123263, 33.54166666666668561, 10.00000000000006040 ) ) ;
#31372=CARTESIAN_POINT ( 'NONE',  ( 7.320508075688771044, 114.3750000000000142, 7.320508075688775484 ) ) ;
#31375=CARTESIAN_POINT ( 'NONE',  ( 4.721056650415999201, 294.2343750017069510, -4.721056650415999201 ) ) ;
#31377=EDGE_LOOP ( 'NONE', ( #74248, #22773, #34508, #66884 ) ) ;
#31378=CYLINDRICAL_SURFACE ( 'NONE', #33773, 6.000000000000001776 ) ;
#31386=CARTESIAN_POINT ( 'NONE',  ( 11.35316468750000141, 0.7812499965860163487, 0.000000000000000000 ) ) ;
#31388=CARTESIAN_POINT ( 'NONE',  ( -9.832129032723420536, 194.0104166632526983, 5.676582343749997150 ) ) ;
#31389=LINE ( 'NONE', #31767, #15434 ) ;
#31392=CYLINDRICAL_SURFACE ( 'NONE', #28656, 10.00000000000000178 ) ;
#31396=CARTESIAN_POINT ( 'NONE',  ( -9.832129032723418760, 48.17708332991934839, -5.676582343750004256 ) ) ;
#31404=CARTESIAN_POINT ( 'NONE',  ( 11.35316468750000141, 105.7812499965860269, 0.000000000000000000 ) ) ;
#31405=CARTESIAN_POINT ( 'NONE',  ( 2.679491924311228956, 92.91666665983871098, -10.00000000000000000 ) ) ;
#31411=CARTESIAN_POINT ( 'NONE',  ( -8.679299243466303437, 226.0000000000000000, -5.010106067796166407 ) ) ;
#31413=CARTESIAN_POINT ( 'NONE',  ( 1.226468279477575784E-15, 292.8593750017070079, 6.676582343750001591 ) ) ;
#31416=CARTESIAN_POINT ( 'NONE',  ( 11.35316468749999785, 170.5729166632526983, 3.042071309553174174 ) ) ;
#31421=ORIENTED_EDGE ( 'NONE', *, *, #38912, .F. ) ;
#31422=( BOUNDED_CURVE ( )  B_SPLINE_CURVE ( 2, ( #46110, #67645, #28389, #15943, #39709, #34078, #57827, #34450, #51397, #56326, #11784, #34821, #74039 ),
 .UNSPECIFIED., .F., .F. ) 
 B_SPLINE_CURVE_WITH_KNOTS ( ( 3, 2, 2, 2, 2, 2, 3 ),
 ( 1.365892743354367500, 1.371125127663376464, 1.376357511972385650, 1.381589896281394614, 1.386822280590403800, 1.392054664899412764, 1.397287049208421728 ),
 .UNSPECIFIED. ) 
 CURVE ( )  GEOMETRIC_REPRESENTATION_ITEM ( )  RATIONAL_B_SPLINE_CURVE ( ( 1.000000000000000000, 0.9659258262890684232, 1.000000000000000000, 0.9659258262890684232, 1.000000000000000000, 0.9659258262890684232, 1.000000000000000000, 0.9659258262890684232, 1.000000000000000000, 0.9659258262890684232, 1.000000000000000000, 0.9659258262893064551, 0.9999999999997619682 ) ) 
 REPRESENTATION_ITEM ( '' )  );
#31423=VECTOR ( 'NONE', #65607, 1000.000000000000000 ) ;
#31426=CARTESIAN_POINT ( 'NONE',  ( 11.35316468749999963, 141.3020833299193271, -3.042071309553165293 ) ) ;
#31430=CARTESIAN_POINT ( 'NONE',  ( -8.311093377946841443, 64.21874999658601268, 8.311093377946830785 ) ) ;
#31456=CARTESIAN_POINT ( 'NONE',  ( -5.999999999999999112, 295.0625000000000000, 2.485281374238575314 ) ) ;
#31462=CARTESIAN_POINT ( 'NONE',  ( -10.00000000000000000, 202.2916666666666572, -2.679491924311229845 ) ) ;
#31465=CARTESIAN_POINT ( 'NONE',  ( -7.320508075688778149, 73.12500000000001421, 7.320508075688769267 ) ) ;
#31468=CARTESIAN_POINT ( 'NONE',  ( -2.485281374238571761, 296.8125000000000000, -6.000000000000003553 ) ) ;
#31480=CARTESIAN_POINT ( 'NONE',  ( 8.660254037844385522, 194.5833333333333712, 5.000000000000005329 ) ) ;
#31483=CARTESIAN_POINT ( 'NONE',  ( -11.35316468750000141, 153.5937499965860127, -1.390361679473963753E-15 ) ) ;
#31487=CARTESIAN_POINT ( 'NONE',  ( -5.000000000000005329, 85.20833332650538239, 8.660254037844387298 ) ) ;
#31488=CARTESIAN_POINT ( 'NONE',  ( -5.999999999999999112, 294.0625000000000000, 2.485281374238575314 ) ) ;
#31489=ORIENTED_EDGE ( 'NONE', *, *, #64560, .T. ) ;
#31490=CARTESIAN_POINT ( 'NONE',  ( 3.042071309553159519, 10.05208332991935016, 11.35316468750000141 ) ) ;
#31496=CARTESIAN_POINT ( 'NONE',  ( 2.679491924311228956, 47.91666665983869677, -10.00000000000000000 ) ) ;
#31502=LINE ( 'NONE', #49214, #67273 ) ;
#31505=CARTESIAN_POINT ( 'NONE',  ( 6.000000000000003553, 292.6250000034139589, -2.485281374238571761 ) ) ;
#31506=CARTESIAN_POINT ( 'NONE',  ( -2.679491924311229401, 161.4583333333333712, -10.00000000000001421 ) ) ;
#31508=CARTESIAN_POINT ( 'NONE',  ( -9.832129032723418760, 132.8645833299193555, -5.676582343750004256 ) ) ;
#31512=DIRECTION ( 'NONE',  ( -0.000000000000000000, 1.000000000000000000, -0.000000000000000000 ) ) ;
#31515=CARTESIAN_POINT ( 'NONE',  ( 6.123233995736767268E-16, 46.25000000000000711, -10.00000000000000178 ) ) ;
#31516=CARTESIAN_POINT ( 'NONE',  ( 3.042071309553159519, 109.7395833299193555, 11.35316468750000141 ) ) ;
#31520=CARTESIAN_POINT ( 'NONE',  ( -2.679491924311235174, 25.41666665983869677, 10.00000000000000000 ) ) ;
#31522=CARTESIAN_POINT ( 'NONE',  ( -3.042071309553173730, 104.6354166632526699, 11.35316468749999785 ) ) ;
#31526=CARTESIAN_POINT ( 'NONE',  ( 11.35316468749999963, 16.30208332991935194, -3.042071309553165293 ) ) ;
#31528=CARTESIAN_POINT ( 'NONE',  ( 5.000000000000001776, 182.7083333265053682, -8.660254037844389075 ) ) ;
#31530=CARTESIAN_POINT ( 'NONE',  ( 6.123233995736767268E-16, 118.1249999931720396, -10.00000000000000178 ) ) ;
#31535=CARTESIAN_POINT ( 'NONE',  ( 4.721056650416000089, 288.8281250017069510, 4.721056650415999201 ) ) ;
#31537=CARTESIAN_POINT ( 'NONE',  ( 11.35316468750000141, 221.0937499965860127, 0.000000000000000000 ) ) ;
#31538=CARTESIAN_POINT ( 'NONE',  ( -9.832129032723418760, 138.1770833299193555, -5.676582343750004256 ) ) ;
#31549=CARTESIAN_POINT ( 'NONE',  ( -2.679491924317297435, 173.5416666666662024, 9.999999999996612488 ) ) ;
#31554=CARTESIAN_POINT ( 'NONE',  ( -11.35316468750000141, 183.4895833299193839, 3.042071309553159963 ) ) ;
#31556=CARTESIAN_POINT ( 'NONE',  ( 6.000000000000003553, 295.5625000000000000, -2.485281374238571761 ) ) ;
#31557=CARTESIAN_POINT ( 'NONE',  ( 2.765530957081996366, 291.1406250017069510, -6.676582343750002480 ) ) ;
#31569=CARTESIAN_POINT ( 'NONE',  ( -6.000000000000003553, 299.0000000034139589, -2.485281374238571317 ) ) ;
#31571=CARTESIAN_POINT ( 'NONE',  ( -8.311093377946841443, 119.2187499965860127, 8.311093377946830785 ) ) ;
#31577=ORIENTED_EDGE ( 'NONE', *, *, #3806, .T. ) ;
#31578=VECTOR ( 'NONE', #28911, 1000.000000000000000 ) ;
#31580=CARTESIAN_POINT ( 'NONE',  ( 9.832129032723420536, 226.1979166632526983, -5.676582343749999815 ) ) ;
#31586=CARTESIAN_POINT ( 'NONE',  ( -11.35316468749999785, 198.3854166632526699, -3.042071309553167513 ) ) ;
#31588=CARTESIAN_POINT ( 'NONE',  ( 9.420701371451851713, 225.9999999999999716, 5.314304958673083057 ) ) ;
#31593=CARTESIAN_POINT ( 'NONE',  ( -11.35316468750000141, 88.28124999658602690, -1.390361679473963753E-15 ) ) ;
#31597=CARTESIAN_POINT ( 'NONE',  ( 2.679491924311891093, 38.95833333333347781, 9.999999999999802824 ) ) ;
#31599=CARTESIAN_POINT ( 'NONE',  ( -8.311093377946841443, 88.90624999658602690, 8.311093377946830785 ) ) ;
#31605=CARTESIAN_POINT ( 'NONE',  ( 5.676582343750001591, 71.61458332991935549, -9.832129032723420536 ) ) ;
#31608=CARTESIAN_POINT ( 'NONE',  ( 4.999999999999993783, 171.0416666598387110, 8.660254037844390851 ) ) ;
#31610=VECTOR ( 'NONE', #45022, 1000.000000000000000 ) ;
#31612=CARTESIAN_POINT ( 'NONE',  ( 9.832129032723416984, 55.67708332991935549, 5.676582343750006032 ) ) ;
#31613=CARTESIAN_POINT ( 'NONE',  ( 4.721056650415999201, 294.0781250017069510, -4.721056650415999201 ) ) ;
#31615=CARTESIAN_POINT ( 'NONE',  ( -9.832129032723418760, 207.8645833299193555, -5.676582343750004256 ) ) ;
#31621=CARTESIAN_POINT ( 'NONE',  ( -9.832129032723418760, 197.8645833299193555, -5.676582343750004256 ) ) ;
#31624=CARTESIAN_POINT ( 'NONE',  ( -10.00000000000000355, 189.5833333265053682, 2.679491924311223183 ) ) ;
#31627=CARTESIAN_POINT ( 'NONE',  ( 6.951808397369818766E-16, 187.3437499965860127, -11.35316468750000141 ) ) ;
#31635=CARTESIAN_POINT ( 'NONE',  ( 7.320508075688774596, 0.6250000000000000000, -7.320508075688774596 ) ) ;
#31636=EDGE_CURVE ( 'NONE', #36130, #70797, #34641, .T. ) ;
#31656=CARTESIAN_POINT ( 'NONE',  ( -11.35316468750000141, 78.59374999658601268, -1.390361679473963753E-15 ) ) ;
#31657=CARTESIAN_POINT ( 'NONE',  ( -2.679491924311226292, 113.3333333265053540, -10.00000000000000178 ) ) ;
#31661=CARTESIAN_POINT ( 'NONE',  ( 2.765530957081996366, 292.2968750017070079, -6.676582343750002480 ) ) ;
#31662=CARTESIAN_POINT ( 'NONE',  ( -2.679491924311235618, 148.5416666666666288, 10.00000000000000000 ) ) ;
#31665=B_SPLINE_CURVE_WITH_KNOTS ( 'NONE', 1,
 ( #49572, #38264 ),
 .UNSPECIFIED., .F., .F.,
 ( 2, 2 ),
 ( 0.000000000000000000, 1.000000000000000000 ),
 .UNSPECIFIED. ) ;
#31675=CARTESIAN_POINT ( 'NONE',  ( -1.836970198721029983E-15, 170.6249999931720538, 10.00000000000000178 ) ) ;
#31676=CARTESIAN_POINT ( 'NONE',  ( 2.679491924311377282, 136.0416666666666572, -9.999999999999918288 ) ) ;
#31677=CARTESIAN_POINT ( 'NONE',  ( 2.485281374238266672, 288.7500000034140726, -6.000000000000306422 ) ) ;
#31680=CARTESIAN_POINT ( 'NONE',  ( 5.676582343749993598, 44.94791666325267698, 9.832129032723422313 ) ) ;
#31681=CARTESIAN_POINT ( 'NONE',  ( 10.00000000000000533, 150.0000000000000000, 0.000000000000000000 ) ) ;
#31682=CARTESIAN_POINT ( 'NONE',  ( -4.999999999999998224, 3.541666659838699438, -8.660254037844389075 ) ) ;
#31686=CARTESIAN_POINT ( 'NONE',  ( 8.311093377946837890, 46.40624999658601268, -8.311093377946837890 ) ) ;
#31692=CARTESIAN_POINT ( 'NONE',  ( 3.042071309553167513, 26.82291666325268054, -11.35316468749999785 ) ) ;
#31694=CARTESIAN_POINT ( 'NONE',  ( -10.00000000000000000, 49.16666665983869677, -2.679491924311229845 ) ) ;
#31695=CARTESIAN_POINT ( 'NONE',  ( 3.042071309553159519, 164.7395833299193271, 11.35316468750000141 ) ) ;
#31696=CARTESIAN_POINT ( 'NONE',  ( 5.000000000000001776, 127.7083333265053824, -8.660254037844389075 ) ) ;
#31698=VERTEX_POINT ( 'NONE', #3131 ) ;
#31699=CARTESIAN_POINT ( 'NONE',  ( 4.999999999999993783, 21.04166665983870033, 8.660254037844390851 ) ) ;
#31700=CARTESIAN_POINT ( 'NONE',  ( 6.951808397369818766E-16, 22.34374999658601979, -11.35316468750000141 ) ) ;
#31702=ORIENTED_EDGE ( 'NONE', *, *, #57172, .F. ) ;
#31705=LINE ( 'NONE', #49041, #11253 ) ;
#31707=CARTESIAN_POINT ( 'NONE',  ( -9.832129032723420536, 153.6979166632526983, 5.676582343749997150 ) ) ;
#31717=CARTESIAN_POINT ( 'NONE',  ( 8.311093377946837890, 96.71874999658599847, -8.311093377946837890 ) ) ;
#31728=CARTESIAN_POINT ( 'NONE',  ( -7.320508075688773708, 158.7499999931720254, -7.320508075688774596 ) ) ;
#31750=CARTESIAN_POINT ( 'NONE',  ( -1.836970198721029983E-15, 103.7500000000000142, 10.00000000000000178 ) ) ;
#31752=CARTESIAN_POINT ( 'NONE',  ( -2.765530957081998586, 291.7968750017070079, 6.676582343750001591 ) ) ;
#31754=ORIENTED_EDGE ( 'NONE', *, *, #25040, .T. ) ;
#31759=DIRECTION ( 'NONE',  ( 0.000000000000000000, 0.000000000000000000, 1.000000000000000000 ) ) ;
#31763=CARTESIAN_POINT ( 'NONE',  ( 5.676582343750001591, 6.614583329919350163, -9.832129032723420536 ) ) ;
#31766=CARTESIAN_POINT ( 'NONE',  ( -11.35316468749999785, 188.3854166632526983, -3.042071309553167513 ) ) ;
#31767=CARTESIAN_POINT ( 'NONE',  ( 7.347880794884121708E-16, 300.0000000000000000, -6.000000000000001776 ) ) ;
#31770=FACE_OUTER_BOUND ( 'NONE', #19846, .T. ) ;
#31771=CARTESIAN_POINT ( 'NONE',  ( 6.000000000000003553, 297.5625000000001137, -2.485281374238571761 ) ) ;
#31774=CARTESIAN_POINT ( 'NONE',  ( -8.311093377946836114, 7.656249996586014461, -8.311093377946837890 ) ) ;
#31782=CARTESIAN_POINT ( 'NONE',  ( -11.35316468749999785, 118.0729166632526983, -3.042071309553167513 ) ) ;
#31785=CARTESIAN_POINT ( 'NONE',  ( 6.123233995736767268E-16, 88.12499999317203958, -10.00000000000000178 ) ) ;
#31789=CARTESIAN_POINT ( 'NONE',  ( 8.660254037844390851, 144.5833333333333428, 5.000000000000008882 ) ) ;
#31793=CARTESIAN_POINT ( 'NONE',  ( 4.721056650416000089, 293.9843750017070079, 4.721056650415999201 ) ) ;
#31796=CARTESIAN_POINT ( 'NONE',  ( 3.042071309553159519, 164.7395833299193271, 11.35316468750000141 ) ) ;
#31805=CARTESIAN_POINT ( 'NONE',  ( -9.832129032723420536, 154.0104166632526983, 5.676582343749997150 ) ) ;
#31809=CARTESIAN_POINT ( 'NONE',  ( -8.311093377946836114, 57.96874999658602690, -8.311093377946837890 ) ) ;
#31816=CARTESIAN_POINT ( 'NONE',  ( 4.242640687119285658, 287.6875000034139589, -4.242640687119286547 ) ) ;
#31834=VERTEX_POINT ( 'NONE', #54446 ) ;
#31839=CARTESIAN_POINT ( 'NONE',  ( -7.320508075688778149, 63.12500000000000000, 7.320508075688769267 ) ) ;
#31841=CARTESIAN_POINT ( 'NONE',  ( -2.485281374238572649, 296.1875000000000000, 6.000000000000002665 ) ) ;
#31852=CARTESIAN_POINT ( 'NONE',  ( 2.679491924311228956, 186.0416666666666572, -10.00000000000000000 ) ) ;
#31855=CARTESIAN_POINT ( 'NONE',  ( 11.35316468750000141, 151.0937499965860411, 0.000000000000000000 ) ) ;
#31860=CARTESIAN_POINT ( 'NONE',  ( 1.102182119232618108E-15, 297.3125000034140157, 6.000000000000001776 ) ) ;
#31862=CARTESIAN_POINT ( 'NONE',  ( -11.35316468749999785, 8.385416663252684089, -3.042071309553167513 ) ) ;
#31865=CARTESIAN_POINT ( 'NONE',  ( -3.673940397442060854E-16, 296.7500000000000000, -6.000000000000001776 ) ) ;
#31868=CARTESIAN_POINT ( 'NONE',  ( -4.999999999999998224, 53.54166665983870388, -8.660254037844389075 ) ) ;
#31872=DIRECTION ( 'NONE',  ( 0.000000000000000000, 0.000000000000000000, 1.000000000000000000 ) ) ;
#31880=CARTESIAN_POINT ( 'NONE',  ( 11.35316468749999785, 135.5729166632526983, 3.042071309553174174 ) ) ;
#31890=CARTESIAN_POINT ( 'NONE',  ( 11.35316468749999963, 125.9895833299193271, -3.042071309553165293 ) ) ;
#31891=CARTESIAN_POINT ( 'NONE',  ( 6.123233995736767268E-16, 148.1249999931720538, -10.00000000000000178 ) ) ;
#31896=CARTESIAN_POINT ( 'NONE',  ( 3.042071309553167513, 117.1354166632526699, -11.35316468749999785 ) ) ;
#31900=CARTESIAN_POINT ( 'NONE',  ( -11.35316468750000141, 23.59374999658601979, -1.390361679473963753E-15 ) ) ;
#31901=VERTEX_POINT ( 'NONE', #62323 ) ;
#31905=VECTOR ( 'NONE', #26546, 1000.000000000000000 ) ;
#31908=CARTESIAN_POINT ( 'NONE',  ( 6.676582343750004256, 287.8906250017069510, 2.765530957081995478 ) ) ;
#31911=CARTESIAN_POINT ( 'NONE',  ( 9.832129032723420536, 216.5104166632526983, -5.676582343749999815 ) ) ;
#31913=CARTESIAN_POINT ( 'NONE',  ( 6.951808397369818766E-16, 142.3437499965860411, -11.35316468750000141 ) ) ;
#31927=DIRECTION ( 'NONE',  ( -0.000000000000000000, 1.000000000000000000, -0.000000000000000000 ) ) ;
#31928=CARTESIAN_POINT ( 'NONE',  ( 9.832129032723420536, 186.1979166632526983, -5.676582343749999815 ) ) ;
#31931=CARTESIAN_POINT ( 'NONE',  ( -4.088227598258586603E-16, 292.2031250017069510, -6.676582343750001591 ) ) ;
#31938=CYLINDRICAL_SURFACE ( 'NONE', #8220, 10.00000000000000178 ) ;
#31941=CARTESIAN_POINT ( 'NONE',  ( 0.000000000000000000, 300.0000000000000000, 0.000000000000000000 ) ) ;
#31944=CARTESIAN_POINT ( 'NONE',  ( 6.951808397369818766E-16, 117.3437499965860127, -11.35316468750000141 ) ) ;
#31953=CARTESIAN_POINT ( 'NONE',  ( 3.508290994201011870, 226.7807916744830550, -10.79751095028410290 ) ) ;
#31957=CARTESIAN_POINT ( 'NONE',  ( 9.832129032723420536, 191.5104166632526983, -5.676582343749999815 ) ) ;
#31964=CARTESIAN_POINT ( 'NONE',  ( -5.676582343750006032, 84.11458332991935549, 9.832129032723418760 ) ) ;
#31965=ORIENTED_EDGE ( 'NONE', *, *, #17341, .T. ) ;
#31966=CARTESIAN_POINT ( 'NONE',  ( 2.679491924311084627, 141.0416666666667425, -10.00000000000009592 ) ) ;
#31967=CARTESIAN_POINT ( 'NONE',  ( 1.268984979720182487E-11, 76.24999999999903366, -10.00000000000000178 ) ) ;
#31970=FACE_OUTER_BOUND ( 'NONE', #21991, .T. ) ;
#31971=CARTESIAN_POINT ( 'NONE',  ( -2.085542519210945728E-15, 84.53124999658602690, 11.35316468750000141 ) ) ;
#31972=VERTEX_POINT ( 'NONE', #39886 ) ;
#31980=CARTESIAN_POINT ( 'NONE',  ( 9.832129032723416984, 80.36458332991935549, 5.676582343750006032 ) ) ;
#31984=CARTESIAN_POINT ( 'NONE',  ( 2.679491924311228956, 172.9166666598386826, -10.00000000000000000 ) ) ;
#31988=CARTESIAN_POINT ( 'NONE',  ( -8.311093377946841443, 64.21874999658601268, 8.311093377946834337 ) ) ;
#31989=CARTESIAN_POINT ( 'NONE',  ( 2.765530957082001251, 294.7656250017070079, 6.676582343750000703 ) ) ;
#31990=( BOUNDED_CURVE ( )  B_SPLINE_CURVE ( 2, ( #26824, #38533, #38899, #55515, #21534, #56253, #4570, #4947, #27946 ),
 .UNSPECIFIED., .F., .F. ) 
 B_SPLINE_CURVE_WITH_KNOTS ( ( 3, 2, 2, 2, 3 ),
 ( 0.9374999999999984457, 0.9479166666666650753, 0.9583333333333319271, 0.9687499999999985567, 0.9791666666666651864 ),
 .UNSPECIFIED. ) 
 CURVE ( )  GEOMETRIC_REPRESENTATION_ITEM ( )  RATIONAL_B_SPLINE_CURVE ( ( 1.000000000000011324, 0.9238795325112754142, 1.000000000000000000, 0.9238795325112867385, 1.000000000000000000, 0.9238795325112867385, 1.000000000000000000, 0.9238795325112972856, 0.9999999999999894529 ) ) 
 REPRESENTATION_ITEM ( '' )  );
#31992=CARTESIAN_POINT ( 'NONE',  ( 3.042071309553159519, 209.7395833299193839, 11.35316468750000141 ) ) ;
#31996=CARTESIAN_POINT ( 'NONE',  ( -5.999999999999999112, 288.0625000000000000, 2.485281374238575314 ) ) ;
#31998=CARTESIAN_POINT ( 'NONE',  ( -9.832129032723418760, 187.8645833299193839, -5.676582343750004256 ) ) ;
#32003=EDGE_CURVE ( 'NONE', #18299, #26800, #63036, .T. ) ;
#32005=CARTESIAN_POINT ( 'NONE',  ( 11.35316468750000141, 181.0937499965860411, 0.000000000000000000 ) ) ;
#32011=CARTESIAN_POINT ( 'NONE',  ( 6.123233995736767268E-16, 1.250000000000000000, -10.00000000000000178 ) ) ;
#32018=CARTESIAN_POINT ( 'NONE',  ( 4.242640687119285658, 293.6875000034139589, -4.242640687119286547 ) ) ;
#32030=CARTESIAN_POINT ( 'NONE',  ( 6.951808397369818766E-16, 77.34374999658601268, -11.35316468750000141 ) ) ;
#32035=CARTESIAN_POINT ( 'NONE',  ( 1.226468279477575784E-15, 293.8593750017070079, 6.676582343750001591 ) ) ;
#32046=CARTESIAN_POINT ( 'NONE',  ( 4.242640687119287435, 289.4375000034140157, 4.242640687119285658 ) ) ;
#32052=CARTESIAN_POINT ( 'NONE',  ( -11.35316468749999785, 43.07291666325269119, -3.042071309553167513 ) ) ;
#32055=CARTESIAN_POINT ( 'NONE',  ( 10.00000000000000000, 11.66666665983870033, 2.679491924311236062 ) ) ;
#32058=CARTESIAN_POINT ( 'NONE',  ( -1.836970198721029983E-15, 140.6249999931720538, 10.00000000000000178 ) ) ;
#32060=CARTESIAN_POINT ( 'NONE',  ( -9.832129032723418760, 47.86458332991934839, -5.676582343750004256 ) ) ;
#32066=CARTESIAN_POINT ( 'NONE',  ( 11.35316468749999785, 35.57291666325267698, 3.042071309553174174 ) ) ;
#32069=CARTESIAN_POINT ( 'NONE',  ( -11.35316468750000141, 163.2812499965860127, -1.390361679473963753E-15 ) ) ;
#32070=ADVANCED_FACE ( 'NONE', ( #70058 ), #18366, .T. ) ;
#32071=CARTESIAN_POINT ( 'NONE',  ( -1.836970198721029983E-15, 135.6249999931720538, 10.00000000000000178 ) ) ;
#32074=CARTESIAN_POINT ( 'NONE',  ( 2.679491924311228956, 22.91666665983870033, -10.00000000000000000 ) ) ;
#32075=CARTESIAN_POINT ( 'NONE',  ( 11.35316468749999963, 26.30208332991934839, -3.042071309553165293 ) ) ;
#32077=ORIENTED_EDGE ( 'NONE', *, *, #28739, .F. ) ;
#32078=CYLINDRICAL_SURFACE ( 'NONE', #24749, 10.00000000000000178 ) ;
#32082=CARTESIAN_POINT ( 'NONE',  ( -2.085542519210945728E-15, 149.5312499965860411, 11.35316468750000141 ) ) ;
#32091=DIRECTION ( 'NONE',  ( -0.000000000000000000, -0.000000000000000000, 1.000000000000000000 ) ) ;
#32093=CARTESIAN_POINT ( 'NONE',  ( -2.085542519210945728E-15, 104.8437499965860269, 11.35316468750000141 ) ) ;
#32121=CARTESIAN_POINT ( 'NONE',  ( 8.660254037844390851, 125.4166666666666714, -5.000000000000000888 ) ) ;
#32125=CARTESIAN_POINT ( 'NONE',  ( 8.660254037844451247, 59.58333333333337833, 5.000000000000044409 ) ) ;
#32127=CARTESIAN_POINT ( 'NONE',  ( 6.123233995736767268E-16, 111.2500000000000000, -10.00000000000000178 ) ) ;
#32129=CARTESIAN_POINT ( 'NONE',  ( -2.765530957081996810, 293.4218750017070079, -6.676582343750003368 ) ) ;
#32134=CARTESIAN_POINT ( 'NONE',  ( -5.000000000000005329, 175.2083333265053682, 8.660254037844387298 ) ) ;
#32141=CARTESIAN_POINT ( 'NONE',  ( -5.676582343749998039, 7.447916663252683200, -9.832129032723420536 ) ) ;
#32144=CARTESIAN_POINT ( 'NONE',  ( -5.676582343750006032, 194.4270833299193839, 9.832129032723418760 ) ) ;
#32145=CARTESIAN_POINT ( 'NONE',  ( 6.123233995736767268E-16, 173.1249999931720538, -10.00000000000000178 ) ) ;
#32149=DIRECTION ( 'NONE',  ( -0.000000000000000000, 1.000000000000000000, -0.000000000000000000 ) ) ;
#32152=CARTESIAN_POINT ( 'NONE',  ( 11.35316468749999785, 15.57291666325268409, 3.042071309553174174 ) ) ;
#32160=CARTESIAN_POINT ( 'NONE',  ( 5.676582343750001591, 126.6145833299193697, -9.832129032723420536 ) ) ;
#32162=CARTESIAN_POINT ( 'NONE',  ( -8.660254037844387298, 93.95833332650536818, -5.000000000000004441 ) ) ;
#32166=CARTESIAN_POINT ( 'NONE',  ( -1.836970198721029983E-15, 40.62499999317203248, 10.00000000000000178 ) ) ;
#32169=ADVANCED_FACE ( 'NONE', ( #30789 ), #53444, .T. ) ;
#32170=CARTESIAN_POINT ( 'NONE',  ( 4.721056650416000089, 292.9843750017070079, 4.721056650415999201 ) ) ;
#32171=CARTESIAN_POINT ( 'NONE',  ( 10.00000000000000178, 186.8749999931720538, 0.000000000000000000 ) ) ;
#32173=CARTESIAN_POINT ( 'NONE',  ( 8.311093377946837890, 171.4062499965860127, -8.311093377946837890 ) ) ;
#32180=CARTESIAN_POINT ( 'NONE',  ( 6.951808397369818766E-16, 152.3437499965860411, -11.35316468750000141 ) ) ;
#32184=CARTESIAN_POINT ( 'NONE',  ( 6.951808397369818766E-16, 67.34374999658601268, -11.35316468750000141 ) ) ;
#32189=ORIENTED_EDGE ( 'NONE', *, *, #17826, .T. ) ;
#32192=CARTESIAN_POINT ( 'NONE',  ( -2.679491924311300011, 108.3333333265053682, -9.999999999999959144 ) ) ;
#32214=DIRECTION ( 'NONE',  ( -0.000000000000000000, 1.000000000000000000, -0.000000000000000000 ) ) ;
#32218=CARTESIAN_POINT ( 'NONE',  ( -10.00000000000000178, 62.50000000000000000, -1.224646799147353454E-15 ) ) ;
#32220=CARTESIAN_POINT ( 'NONE',  ( -4.242640687119285658, 293.1249999999999432, 4.242640687119287435 ) ) ;
#32224=VERTEX_POINT ( 'NONE', #2861 ) ;
#32232=CARTESIAN_POINT ( 'NONE',  ( -5.000000000000005329, 183.3333333333333428, 8.660254037844387298 ) ) ;
#32236=CARTESIAN_POINT ( 'NONE',  ( 11.35316468750000141, 156.0937499965860127, 0.000000000000000000 ) ) ;
#32243=AXIS2_PLACEMENT_3D ( 'NONE', #55551, #3864, #26859 ) ;
#32245=CARTESIAN_POINT ( 'NONE',  ( -8.311093377946841443, 19.21874999658601979, 8.311093377946830785 ) ) ;
#32246=CARTESIAN_POINT ( 'NONE',  ( -1.836970198721029983E-15, 95.62499999317203958, 10.00000000000000178 ) ) ;
#32248=CARTESIAN_POINT ( 'NONE',  ( 2.679491924311222739, 30.83333332650536462, 10.00000000000000355 ) ) ;
#32251=CARTESIAN_POINT ( 'NONE',  ( -2.679491924311235618, 50.41666665983868967, 10.00000000000000000 ) ) ;
#32254=CARTESIAN_POINT ( 'NONE',  ( 8.660254037844376640, 100.4166666666666856, -4.999999999999992006 ) ) ;
#32263=CARTESIAN_POINT ( 'NONE',  ( -8.311093377946836114, 132.6562499965860411, -8.311093377946837890 ) ) ;
#32265=CARTESIAN_POINT ( 'NONE',  ( -5.999999999999999112, 298.0625000000000000, 2.485281374238575314 ) ) ;
#32270=CARTESIAN_POINT ( 'NONE',  ( 2.679491924311309337, 46.04166666666667851, -9.999999999999980460 ) ) ;
#32271=CARTESIAN_POINT ( 'NONE',  ( -5.676582343749998039, 127.4479166632526983, -9.832129032723420536 ) ) ;
#32273=EDGE_LOOP ( 'NONE', ( #18157, #26290, #38435, #38974 ) ) ;
#32276=CARTESIAN_POINT ( 'NONE',  ( -4.999999999999998224, 23.54166665983870033, -8.660254037844389075 ) ) ;
#32278=CARTESIAN_POINT ( 'NONE',  ( -8.311093377946836114, 117.9687499965860127, -8.311093377946837890 ) ) ;
#32282=CARTESIAN_POINT ( 'NONE',  ( 9.832129032723420536, 21.51041666325268409, -5.676582343749999815 ) ) ;
#32288=CARTESIAN_POINT ( 'NONE',  ( -6.676582343750000703, 289.5156250017070647, 2.765530957082001251 ) ) ;
#32289=CARTESIAN_POINT ( 'NONE',  ( 7.320508075688774596, 112.4999999931720396, -7.320508075688774596 ) ) ;
#32292=CARTESIAN_POINT ( 'NONE',  ( -2.085542519210945728E-15, 144.8437499965860411, 11.35316468750000141 ) ) ;
#32310=CARTESIAN_POINT ( 'NONE',  ( 9.832129032723416984, 190.3645833299193839, 5.676582343750006032 ) ) ;
#32313=LINE ( 'NONE', #26250, #58264 ) ;
#32323=DIRECTION ( 'NONE',  ( -0.000000000000000000, 1.000000000000000000, -0.000000000000000000 ) ) ;
#32327=CARTESIAN_POINT ( 'NONE',  ( -2.485281374238990093, 298.8750000034140726, -5.999999999999583444 ) ) ;
#32329=CARTESIAN_POINT ( 'NONE',  ( 11.35316468749999963, 121.3020833299193697, -3.042071309553165293 ) ) ;
#32338=CARTESIAN_POINT ( 'NONE',  ( 5.676582343750001591, 226.6145833299193839, -9.832129032723420536 ) ) ;
#32342=CARTESIAN_POINT ( 'NONE',  ( -5.676582343750006032, 209.4270833299193555, 9.832129032723418760 ) ) ;
#32348=CARTESIAN_POINT ( 'NONE',  ( -8.311093377946836114, 82.65624999658602690, -8.311093377946837890 ) ) ;
#32354=CARTESIAN_POINT ( 'NONE',  ( -11.35316468750000141, 88.28124999658602690, -1.390361679473963753E-15 ) ) ;
#32362=CARTESIAN_POINT ( 'NONE',  ( 11.35316468749999785, 85.57291666325268409, 3.042071309553174174 ) ) ;
#32366=CARTESIAN_POINT ( 'NONE',  ( 7.320508075688771044, 176.2499999931720254, 7.320508075688775484 ) ) ;
#32368=CARTESIAN_POINT ( 'NONE',  ( -9.832129032723418760, 73.17708332991934128, -5.676582343750004256 ) ) ;
#32369=CARTESIAN_POINT ( 'NONE',  ( -6.676582343750003368, 293.3906250017069510, -2.765530957081996810 ) ) ;
#32371=CARTESIAN_POINT ( 'NONE',  ( -9.832129032723418760, 202.8645833299193555, -5.676582343750004256 ) ) ;
#32373=CYLINDRICAL_SURFACE ( 'NONE', #45218, 6.000000000000001776 ) ;
#32377=CARTESIAN_POINT ( 'NONE',  ( -9.832129032723420536, 208.6979166632526983, 5.676582343749997150 ) ) ;
#32381=ORIENTED_EDGE ( 'NONE', *, *, #52290, .F. ) ;
#32382=CARTESIAN_POINT ( 'NONE',  ( 11.35316468750000141, 201.0937499965860127, 0.000000000000000000 ) ) ;
#32390=CARTESIAN_POINT ( 'NONE',  ( 10.00000000000000178, 0.000000000000000000, 0.000000000000000000 ) ) ;
#32411=CARTESIAN_POINT ( 'NONE',  ( 11.35316468750000141, 71.09374999658601268, 0.000000000000000000 ) ) ;
#32416=CARTESIAN_POINT ( 'NONE',  ( -6.676582343750002480, 289.5468750017070079, -2.765530957081996810 ) ) ;
#32429=CARTESIAN_POINT ( 'NONE',  ( -7.320508075688773708, 18.74999999317203248, -7.320508075688774596 ) ) ;
#32431=CARTESIAN_POINT ( 'NONE',  ( 10.00000000000000533, 135.0000000000000284, 0.000000000000000000 ) ) ;
#32435=CARTESIAN_POINT ( 'NONE',  ( -5.676582343749998039, 47.44791666325268409, -9.832129032723420536 ) ) ;
#32436=( BOUNDED_CURVE ( )  B_SPLINE_CURVE ( 2, ( #16425, #11533, #74155, #34188, #57192 ),
 .UNSPECIFIED., .F., .F. ) 
 B_SPLINE_CURVE_WITH_KNOTS ( ( 3, 2, 3 ),
 ( 0.9791666666666651864, 0.9895833333333325932, 1.000000000000000000 ),
 .UNSPECIFIED. ) 
 CURVE ( )  GEOMETRIC_REPRESENTATION_ITEM ( )  RATIONAL_B_SPLINE_CURVE ( ( 1.000000000000010436, 0.9238795325112761914, 1.000000000000000000, 0.9238795325112867385, 1.000000000000000000 ) ) 
 REPRESENTATION_ITEM ( '' )  );
#32438=CARTESIAN_POINT ( 'NONE',  ( 8.660254037844385522, 16.45833332650536818, 5.000000000000005329 ) ) ;
#32443=CARTESIAN_POINT ( 'NONE',  ( 11.35316468749999785, 55.57291666325266988, 3.042071309553174174 ) ) ;
#32449=CARTESIAN_POINT ( 'NONE',  ( -8.311093377946841443, 43.90624999658601979, 8.311093377946834337 ) ) ;
#32452=CARTESIAN_POINT ( 'NONE',  ( 3.042071309553167069, 161.8229166632526983, -11.35316468749999785 ) ) ;
#32454=CARTESIAN_POINT ( 'NONE',  ( -10.00000000000000178, 124.3749999931720396, -1.224646799147353454E-15 ) ) ;
#32456=ORIENTED_EDGE ( 'NONE', *, *, #7927, .F. ) ;
#32458=CARTESIAN_POINT ( 'NONE',  ( 8.311093377946834337, 40.46874999658601979, 8.311093377946839666 ) ) ;
#32465=CARTESIAN_POINT ( 'NONE',  ( -5.676582343750006032, 169.1145833299193555, 9.832129032723418760 ) ) ;
#32473=LINE ( 'NONE', #71685, #17250 ) ;
#32475=CARTESIAN_POINT ( 'NONE',  ( 6.951808397369818766E-16, 102.3437499965860127, -11.35316468750000141 ) ) ;
#32479=VERTEX_POINT ( 'NONE', #49996 ) ;
#32498=CARTESIAN_POINT ( 'NONE',  ( 6.676582343750001591, 298.9531250017069510, -8.176455196517173205E-16 ) ) ;
#32503=LINE ( 'NONE', #3827, #46762 ) ;
#32508=CARTESIAN_POINT ( 'NONE',  ( 8.660254037844385522, 104.5833333333333286, 5.000000000000005329 ) ) ;
#32510=CARTESIAN_POINT ( 'NONE',  ( 1.226468279477575784E-15, 293.8593750017070079, 6.676582343750001591 ) ) ;
#32512=VERTEX_POINT ( 'NONE', #32145 ) ;
#32520=CARTESIAN_POINT ( 'NONE',  ( 2.249999999999997335, 255.9999999999998295, 5.427273999917215264 ) ) ;
#32525=CARTESIAN_POINT ( 'NONE',  ( 10.00000000000000178, 225.0000000000000000, 0.000000000000000000 ) ) ;
#32528=CARTESIAN_POINT ( 'NONE',  ( 11.35316468750000141, 201.0937499965860127, 0.000000000000000000 ) ) ;
#32531=CARTESIAN_POINT ( 'NONE',  ( 6.000000000000003553, 290.5625000000000000, -2.485281374238571761 ) ) ;
#32536=CARTESIAN_POINT ( 'NONE',  ( -3.042071309553164404, 7.239583329919349275, -11.35316468749999963 ) ) ;
#32544=CARTESIAN_POINT ( 'NONE',  ( 5.676582343750001591, 116.6145833299193697, -9.832129032723420536 ) ) ;
#32545=CARTESIAN_POINT ( 'NONE',  ( -8.660254037844387298, 88.95833332650536818, -5.000000000000004441 ) ) ;
#32552=CARTESIAN_POINT ( 'NONE',  ( -9.679871326005349275, 225.9999999999998863, 2.594511375997681668 ) ) ;
#32553=CARTESIAN_POINT ( 'NONE',  ( 1.226468279477575784E-15, 289.8593750017070079, 6.676582343750001591 ) ) ;
#32554=CARTESIAN_POINT ( 'NONE',  ( 2.395154805519954641E-11, 111.2499999999981242, -9.999999999999998224 ) ) ;
#32557=CARTESIAN_POINT ( 'NONE',  ( 10.00000000000000000, 206.6666666598387110, 2.679491924311236062 ) ) ;
#32562=CARTESIAN_POINT ( 'NONE',  ( 2.679491924311222739, 155.8333333265053682, 10.00000000000000355 ) ) ;
#32563=CARTESIAN_POINT ( 'NONE',  ( -11.35316468750000141, 148.5937499965860411, -1.390361679473963753E-15 ) ) ;
#32567=CARTESIAN_POINT ( 'NONE',  ( 11.35316468750000141, 66.09374999658601268, 0.000000000000000000 ) ) ;
#32572=EDGE_CURVE ( 'NONE', #7760, #55468, #31389, .T. ) ;
#32574=CARTESIAN_POINT ( 'NONE',  ( 6.000000000000003553, 289.5000000034139589, 2.485281374238571317 ) ) ;
#32580=VECTOR ( 'NONE', #39651, 1000.000000000000000 ) ;
#32581=EDGE_CURVE ( 'NONE', #15471, #9634, #24031, .T. ) ;
#32592=CARTESIAN_POINT ( 'NONE',  ( -6.000000000000001776, 290.0000000000000000, 0.000000000000000000 ) ) ;
#32595=CARTESIAN_POINT ( 'NONE',  ( 0.000000000000000000, 300.0000000000000000, 10.00000000000000178 ) ) ;
#32597=CARTESIAN_POINT ( 'NONE',  ( -2.679491924311234285, 3.541666666666664742, 9.999999999999996447 ) ) ;
#32601=CARTESIAN_POINT ( 'NONE',  ( 10.00000000000000178, 70.20833333333331439, -2.679491924311226736 ) ) ;
#32603=CARTESIAN_POINT ( 'NONE',  ( -2.485281374238572649, 293.1875000000000000, 6.000000000000002665 ) ) ;
#32614=CYLINDRICAL_SURFACE ( 'NONE', #70419, 10.00000000000000178 ) ;
#32615=CARTESIAN_POINT ( 'NONE',  ( -7.320508075688773708, 191.8750000000000284, -7.320508075688774596 ) ) ;
#32616=CARTESIAN_POINT ( 'NONE',  ( 0.000000000000000000, 300.0000000000000000, 10.00000000000000178 ) ) ;
#32618=CARTESIAN_POINT ( 'NONE',  ( -3.042071309553173730, 149.6354166632526983, 11.35316468749999785 ) ) ;
#32619=CARTESIAN_POINT ( 'NONE',  ( -1.836970198721029983E-15, 38.75000000000000000, 10.00000000000000178 ) ) ;
#32621=CARTESIAN_POINT ( 'NONE',  ( 8.660254037844541841, 154.5833333333334565, 5.000000000000096811 ) ) ;
#32622=CARTESIAN_POINT ( 'NONE',  ( -10.00000000000000000, 84.16666665983869677, -2.679491924311229845 ) ) ;
#32625=CARTESIAN_POINT ( 'NONE',  ( -9.832129032723418760, 18.17708332991935194, -5.676582343750004256 ) ) ;
#32628=CARTESIAN_POINT ( 'NONE',  ( 10.00000000000000178, 31.87499999317203248, 0.000000000000000000 ) ) ;
#32632=CARTESIAN_POINT ( 'NONE',  ( 6.123233995736767268E-16, 43.12499999317203248, -10.00000000000000178 ) ) ;
#32637=DIRECTION ( 'NONE',  ( -0.000000000000000000, 1.000000000000000000, -0.000000000000000000 ) ) ;
#32645=CARTESIAN_POINT ( 'NONE',  ( 3.042071309553159519, 124.7395833299193555, 11.35316468750000141 ) ) ;
#32647=CARTESIAN_POINT ( 'NONE',  ( -6.000000000000003553, 297.9375000000000000, -2.485281374238571317 ) ) ;
#32649=PLANE ( 'NONE',  #50133 ) ;
#32652=CARTESIAN_POINT ( 'NONE',  ( -11.35316468750000141, 128.4895833299193555, 3.042071309553159963 ) ) ;
#32658=CARTESIAN_POINT ( 'NONE',  ( -5.676582343750006032, 119.4270833299193555, 9.832129032723418760 ) ) ;
#32663=CARTESIAN_POINT ( 'NONE',  ( 5.676582343750001591, 16.92708332991935194, -9.832129032723420536 ) ) ;
#32670=CARTESIAN_POINT ( 'NONE',  ( -6.676582343750000703, 290.5156250017070079, 2.765530957082001251 ) ) ;
#32671=CARTESIAN_POINT ( 'NONE',  ( 2.679491924311228956, 112.9166666598387110, -10.00000000000000000 ) ) ;
#32675=CARTESIAN_POINT ( 'NONE',  ( -5.676582343749998039, 147.7604166632526699, -9.832129032723420536 ) ) ;
#32679=( BOUNDED_CURVE ( )  B_SPLINE_CURVE ( 2, ( #49125, #26869, #20833, #4247, #31789, #44976, #73273, #44233, #3873, #61204, #37829, #67244, #49883 ),
 .UNSPECIFIED., .F., .F. ) 
 B_SPLINE_CURVE_WITH_KNOTS ( ( 3, 2, 2, 2, 2, 2, 3 ),
 ( 1.805491404681675016, 1.810723803553510036, 1.815956202425345056, 1.821188601297179854, 1.826421000169014874, 1.831653399040849894, 1.836885797912684914 ),
 .UNSPECIFIED. ) 
 CURVE ( )  GEOMETRIC_REPRESENTATION_ITEM ( )  RATIONAL_B_SPLINE_CURVE ( ( 1.000000000000000000, 0.9659258262890683122, 1.000000000000000000, 0.9659258262890683122, 1.000000000000000000, 0.9659258262890683122, 1.000000000000000000, 0.9659258262890683122, 1.000000000000000000, 0.9659258262890683122, 1.000000000000000000, 0.9659258262891664559, 0.9999999999999018563 ) ) 
 REPRESENTATION_ITEM ( '' )  );
#32682=ORIENTED_EDGE ( 'NONE', *, *, #6344, .F. ) ;
#32691=CARTESIAN_POINT ( 'NONE',  ( 11.35316468749999963, 180.9895833299193555, -3.042071309553165293 ) ) ;
#32695=CARTESIAN_POINT ( 'NONE',  ( 1.226468279477575784E-15, 288.7031250017069510, 6.676582343750001591 ) ) ;
#32704=CARTESIAN_POINT ( 'NONE',  ( -10.00000000000000000, 139.1666666598387110, -2.679491924311229845 ) ) ;
#32705=CYLINDRICAL_SURFACE ( 'NONE', #40162, 6.000000000000001776 ) ;
#32708=CARTESIAN_POINT ( 'NONE',  ( -3.042071309553164404, 117.5520833299193413, -11.35316468749999963 ) ) ;
#32709=CARTESIAN_POINT ( 'NONE',  ( -2.485281374238197394, 296.1875000000000000, 6.000000000000376588 ) ) ;
#32716=CARTESIAN_POINT ( 'NONE',  ( 9.692727098607901937, 225.2031118130280731, -2.530001495371571707 ) ) ;
#32720=CARTESIAN_POINT ( 'NONE',  ( -11.35316468750000141, 213.5937499965860411, -1.390361679473963753E-15 ) ) ;
#32722=CARTESIAN_POINT ( 'NONE',  ( 5.355978476798539667, 225.9999999999999716, 8.594851559336273539 ) ) ;
#32728=CARTESIAN_POINT ( 'NONE',  ( 6.951808397369818766E-16, 97.03124999658602690, -11.35316468750000141 ) ) ;
#32734=CARTESIAN_POINT ( 'NONE',  ( -11.35316468750000141, 93.28124999658602690, -1.390361679473963753E-15 ) ) ;
#32741=CARTESIAN_POINT ( 'NONE',  ( -8.311093377946841443, 88.90624999658602690, 8.311093377946834337 ) ) ;
#32747=CARTESIAN_POINT ( 'NONE',  ( 4.999999999999993783, 186.0416666598387110, 8.660254037844390851 ) ) ;
#32749=CARTESIAN_POINT ( 'NONE',  ( -8.311093377946841443, 74.21874999658602690, 8.311093377946834337 ) ) ;
#32750=CARTESIAN_POINT ( 'NONE',  ( 6.676582343750003368, 295.0156250017069510, -2.765530957081997254 ) ) ;
#32752=CARTESIAN_POINT ( 'NONE',  ( -8.311093377946841443, 203.9062499965859843, 8.311093377946830785 ) ) ;
#32756=CARTESIAN_POINT ( 'NONE',  ( 6.000000000000003553, 291.5625000000000000, -2.485281374238571761 ) ) ;
#32758=CARTESIAN_POINT ( 'NONE',  ( -5.676582343750006032, 209.1145833299193555, 9.832129032723418760 ) ) ;
#32762=CARTESIAN_POINT ( 'NONE',  ( 8.311093377946837890, 196.7187499965860127, -8.311093377946837890 ) ) ;
#32770=CARTESIAN_POINT ( 'NONE',  ( 6.123233995736767268E-16, 16.25000000000000000, -10.00000000000000178 ) ) ;
#32781=CARTESIAN_POINT ( 'NONE',  ( -1.836970198721029983E-15, 83.75000000000000000, 10.00000000000000178 ) ) ;
#32791=CARTESIAN_POINT ( 'NONE',  ( 9.832129032723420536, 76.51041666325268409, -5.676582343749999815 ) ) ;
#32796=CARTESIAN_POINT ( 'NONE',  ( -2.765530957081996810, 291.4218750017069510, -6.676582343750002480 ) ) ;
#32801=EDGE_LOOP ( 'NONE', ( #12285, #60964, #35423, #61432 ) ) ;
#32806=CARTESIAN_POINT ( 'NONE',  ( -9.832129032723420536, 174.0104166632526983, 5.676582343749997150 ) ) ;
#32809=CARTESIAN_POINT ( 'NONE',  ( 1.102182119232618108E-15, 289.3125000034140157, 6.000000000000001776 ) ) ;
#32814=CARTESIAN_POINT ( 'NONE',  ( -2.085542519210945728E-15, 54.53124999658602690, 11.35316468750000141 ) ) ;
#32816=CARTESIAN_POINT ( 'NONE',  ( 7.320508075688771044, 26.24999999317203603, 7.320508075688775484 ) ) ;
#32821=CARTESIAN_POINT ( 'NONE',  ( -5.676582343749998039, 47.44791666325268409, -9.832129032723420536 ) ) ;
#32827=CARTESIAN_POINT ( 'NONE',  ( 11.35316468749999963, 40.98958332991934839, -3.042071309553165293 ) ) ;
#32830=CARTESIAN_POINT ( 'NONE',  ( -9.832129032723418760, 167.8645833299193555, -5.676582343750004256 ) ) ;
#32831=CARTESIAN_POINT ( 'NONE',  ( -1.836970198721029983E-15, 140.6249999931720538, 10.00000000000000178 ) ) ;
#32834=DIRECTION ( 'NONE',  ( -0.000000000000000000, 1.000000000000000000, -0.000000000000000000 ) ) ;
#32835=CARTESIAN_POINT ( 'NONE',  ( -2.085542519210945728E-15, 39.84374999658601979, 11.35316468750000141 ) ) ;
#32842=CARTESIAN_POINT ( 'NONE',  ( 11.35316468750000141, 170.7812499965860411, 0.000000000000000000 ) ) ;
#32847=EDGE_CURVE ( 'NONE', #27119, #5538, #73252, .T. ) ;
#32852=AXIS2_PLACEMENT_3D ( 'NONE', #16747, #24551, #7219 ) ;
#32856=CARTESIAN_POINT ( 'NONE',  ( 3.042071309553159519, 115.0520833299193555, 11.35316468750000141 ) ) ;
#32858=CARTESIAN_POINT ( 'NONE',  ( 4.999999999999998224, 14.16666666666667318, 8.660254037844397956 ) ) ;
#32878=CARTESIAN_POINT ( 'NONE',  ( 7.320508075688774596, 72.49999999317203958, -7.320508075688774596 ) ) ;
#32881=( BOUNDED_CURVE ( )  B_SPLINE_CURVE ( 2, ( #43558, #31506, #66573, #39033, #68074, #46170, #34513, #16364, #57517, #11845, #62037, #67706, #51088 ),
 .UNSPECIFIED., .F., .F. ) 
 B_SPLINE_CURVE_WITH_KNOTS ( ( 3, 2, 2, 2, 2, 2, 3 ),
 ( 2.025290649010746513, 2.030523086516430098, 2.035755524022114127, 2.040987961527798156, 2.046220399033481741, 2.051452836539165325, 2.056685274044849354 ),
 .UNSPECIFIED. ) 
 CURVE ( )  GEOMETRIC_REPRESENTATION_ITEM ( )  RATIONAL_B_SPLINE_CURVE ( ( 1.000000000000000000, 0.9659258262890682012, 1.000000000000000000, 0.9659258262890682012, 1.000000000000000000, 0.9659258262890682012, 1.000000000000000000, 0.9659258262890682012, 1.000000000000000000, 0.9659258262890682012, 1.000000000000000000, 0.9659258262890577651, 1.000000000000010436 ) ) 
 REPRESENTATION_ITEM ( '' )  );
#32890=CARTESIAN_POINT ( 'NONE',  ( -5.000000000000005329, 118.3333333333333428, 8.660254037844387298 ) ) ;
#32893=CARTESIAN_POINT ( 'NONE',  ( -6.676582343750001591, 290.6093750017069510, 0.000000000000000000 ) ) ;
#32906=CARTESIAN_POINT ( 'NONE',  ( -10.00000000000000178, 222.5000000000000000, -1.224646799147353454E-15 ) ) ;
#32908=CARTESIAN_POINT ( 'NONE',  ( 11.35316468750000141, 211.0937499965860411, 0.000000000000000000 ) ) ;
#32914=ORIENTED_EDGE ( 'NONE', *, *, #73132, .T. ) ;
#32915=EDGE_CURVE ( 'NONE', #60693, #13964, #67892, .T. ) ;
#32917=CARTESIAN_POINT ( 'NONE',  ( -5.676582343749998039, 7.447916663252683200, -9.832129032723420536 ) ) ;
#32923=CARTESIAN_POINT ( 'NONE',  ( 11.35316468750000141, 0.7812499965860163487, 0.000000000000000000 ) ) ;
#32925=CARTESIAN_POINT ( 'NONE',  ( -8.311093377946836114, 117.6562499965860269, -8.311093377946837890 ) ) ;
#32926=CARTESIAN_POINT ( 'NONE',  ( -10.00000000000000000, 99.16666665983871098, -2.679491924311229845 ) ) ;
#32930=CARTESIAN_POINT ( 'NONE',  ( -7.320508075688773708, 38.74999999317203958, -7.320508075688774596 ) ) ;
#32933=CARTESIAN_POINT ( 'NONE',  ( -4.721056650415998313, 291.7343750017069510, 4.721056650416000089 ) ) ;
#32942=CARTESIAN_POINT ( 'NONE',  ( 8.311093377946837890, 156.7187499965860127, -8.311093377946837890 ) ) ;
#32946=CARTESIAN_POINT ( 'NONE',  ( -9.832129032723418760, 78.17708332991935549, -5.676582343750004256 ) ) ;
#32953=CARTESIAN_POINT ( 'NONE',  ( 4.242640687119285658, 288.6875000034139589, -4.242640687119286547 ) ) ;
#32959=EDGE_CURVE ( 'NONE', #33017, #8939, #39295, .T. ) ;
#32963=DIRECTION ( 'NONE',  ( -0.000000000000000000, 1.000000000000000000, -0.000000000000000000 ) ) ;
#32965=ADVANCED_FACE ( 'NONE', ( #10624 ), #70749, .F. ) ;
#32971=CARTESIAN_POINT ( 'NONE',  ( 1.102182119232618108E-15, 290.2500000000000000, 6.000000000000001776 ) ) ;
#32975=DIRECTION ( 'NONE',  ( -0.000000000000000000, 1.000000000000000000, -0.000000000000000000 ) ) ;
#32977=CARTESIAN_POINT ( 'NONE',  ( -2.679491924317381812, 1.458333333333883930, -9.999999999996445510 ) ) ;
#32981=( BOUNDED_CURVE ( )  B_SPLINE_CURVE ( 2, ( #51282, #56213, #16561, #5643, #39969, #67893, #21493, #62976, #73549 ),
 .UNSPECIFIED., .F., .F. ) 
 B_SPLINE_CURVE_WITH_KNOTS ( ( 3, 2, 2, 2, 3 ),
 ( 0.2708333333333312609, 0.2812499999999979461, 0.2916666666666646313, 0.3020833333333312609, 0.3124999999999979461 ),
 .UNSPECIFIED. ) 
 CURVE ( )  GEOMETRIC_REPRESENTATION_ITEM ( )  RATIONAL_B_SPLINE_CURVE ( ( 1.000000000000015099, 0.9238795325112717505, 1.000000000000000000, 0.9238795325112867385, 1.000000000000000000, 0.9238795325112867385, 1.000000000000000000, 0.9238795325113017265, 0.9999999999999850120 ) ) 
 REPRESENTATION_ITEM ( '' )  );
#32982=CARTESIAN_POINT ( 'NONE',  ( 8.660254037844389075, 70.41666666666667140, -5.000000000000000000 ) ) ;
#32984=CARTESIAN_POINT ( 'NONE',  ( -2.485281374238571761, 293.8124999999999432, -6.000000000000003553 ) ) ;
#32986=ORIENTED_EDGE ( 'NONE', *, *, #23212, .T. ) ;
#32994=CARTESIAN_POINT ( 'NONE',  ( 8.660254037844385522, 189.5833333333333428, 5.000000000000005329 ) ) ;
#32997=CARTESIAN_POINT ( 'NONE',  ( -8.311093377946836114, 167.9687499965859843, -8.311093377946837890 ) ) ;
#33000=CARTESIAN_POINT ( 'NONE',  ( 2.679491924329232777, 153.9583333333350197, 9.999999999989814370 ) ) ;
#33002=ORIENTED_EDGE ( 'NONE', *, *, #67401, .T. ) ;
#33004=CARTESIAN_POINT ( 'NONE',  ( -11.35316468749999785, 18.38541666325267698, -3.042071309553167513 ) ) ;
#33011=CARTESIAN_POINT ( 'NONE',  ( 5.000000000000001776, 47.70833332650536818, -8.660254037844389075 ) ) ;
#33017=VERTEX_POINT ( 'NONE', #4235 ) ;
#33020=CARTESIAN_POINT ( 'NONE',  ( -10.00000000000000000, 222.2916666666666856, -2.679491924311229845 ) ) ;
#33024=CARTESIAN_POINT ( 'NONE',  ( -9.832129032723418760, 137.8645833299193555, -5.676582343750004256 ) ) ;
#33025=ORIENTED_EDGE ( 'NONE', *, *, #10258, .F. ) ;
#33031=CARTESIAN_POINT ( 'NONE',  ( 5.676582343750001591, 131.6145833299193555, -9.832129032723420536 ) ) ;
#33039=CARTESIAN_POINT ( 'NONE',  ( 9.832129032723416984, 120.6770833299193555, 5.676582343750006032 ) ) ;
#33043=CARTESIAN_POINT ( 'NONE',  ( -2.085542519210945728E-15, 19.84374999658601979, 11.35316468750000141 ) ) ;
#33051=CARTESIAN_POINT ( 'NONE',  ( 6.676582343750001591, 287.9531250017069510, -8.176455196517173205E-16 ) ) ;
#33052=CARTESIAN_POINT ( 'NONE',  ( -4.242640687119286547, 296.8750000000000000, -4.242640687119286547 ) ) ;
#33055=CARTESIAN_POINT ( 'NONE',  ( -8.311093377946836114, 137.9687499965860411, -8.311093377946837890 ) ) ;
#33073=CARTESIAN_POINT ( 'NONE',  ( -8.311093377946836114, 187.6562499965860411, -8.311093377946837890 ) ) ;
#33075=CARTESIAN_POINT ( 'NONE',  ( -3.673940397442060854E-16, 295.7500000000000000, -6.000000000000001776 ) ) ;
#33076=CARTESIAN_POINT ( 'NONE',  ( 6.676582343750002480, 290.0156250017069510, -2.765530957081997254 ) ) ;
#33077=CARTESIAN_POINT ( 'NONE',  ( 2.679491924318032403, 81.04166666666614560, -9.999999999996202149 ) ) ;
#33078=CARTESIAN_POINT ( 'NONE',  ( 6.123233995736767268E-16, 96.25000000000000000, -10.00000000000000178 ) ) ;
#33083=CARTESIAN_POINT ( 'NONE',  ( 10.00000000000000178, 166.8749999931720538, 0.000000000000000000 ) ) ;
#33087=CARTESIAN_POINT ( 'NONE',  ( -8.660254037844387298, 142.0833333333333428, -5.000000000000004441 ) ) ;
#33091=CARTESIAN_POINT ( 'NONE',  ( 5.676582343750001591, 116.9270833299193555, -9.832129032723420536 ) ) ;
#33100=CARTESIAN_POINT ( 'NONE',  ( 8.311093377946834337, 225.1562499965860411, 8.311093377946839666 ) ) ;
#33102=CARTESIAN_POINT ( 'NONE',  ( -11.35316468750000141, 203.8020833299193839, 3.042071309553159963 ) ) ;
#33109=CARTESIAN_POINT ( 'NONE',  ( 8.311093377946834337, 95.15624999658601268, 8.311093377946839666 ) ) ;
#33116=AXIS2_PLACEMENT_3D ( 'NONE', #36020, #18664, #5496 ) ;
#33118=CARTESIAN_POINT ( 'NONE',  ( -11.35316468750000141, 98.28124999658602690, -1.390361679473963753E-15 ) ) ;
#33126=CARTESIAN_POINT ( 'NONE',  ( -3.042071309553173730, 89.32291666325268409, 11.35316468749999785 ) ) ;
#33130=CARTESIAN_POINT ( 'NONE',  ( 5.000000000000001776, 187.7083333265053966, -8.660254037844389075 ) ) ;
#33132=CARTESIAN_POINT ( 'NONE',  ( -3.042071309553163960, 72.55208332991934128, -11.35316468749999963 ) ) ;
#33133=CARTESIAN_POINT ( 'NONE',  ( 6.676582343750004256, 287.8906250017069510, 2.765530957081995478 ) ) ;
#33136=CARTESIAN_POINT ( 'NONE',  ( 6.951808397369818766E-16, 207.0312499965860411, -11.35316468750000141 ) ) ;
#33142=CARTESIAN_POINT ( 'NONE',  ( 11.35316468750000141, 210.7812499965860411, 0.000000000000000000 ) ) ;
#33147=CARTESIAN_POINT ( 'NONE',  ( -5.676582343749998039, 192.7604166632526983, -9.832129032723420536 ) ) ;
#33154=CARTESIAN_POINT ( 'NONE',  ( -7.320508075688773708, 16.87500000000000355, -7.320508075688774596 ) ) ;
#33173=CARTESIAN_POINT ( 'NONE',  ( 5.676582343749993598, 80.26041666325268409, 9.832129032723422313 ) ) ;
#33178=CARTESIAN_POINT ( 'NONE',  ( 6.676582343750001591, 290.1093750017069510, -8.176455196517173205E-16 ) ) ;
#33182=EDGE_CURVE ( 'NONE', #30219, #17320, #1371, .T. ) ;
#33188=CARTESIAN_POINT ( 'NONE',  ( -3.042071309553164404, 172.5520833299193555, -11.35316468749999963 ) ) ;
#33191=CARTESIAN_POINT ( 'NONE',  ( -9.999999999999996447, 207.7083333333333428, 2.679491924311221851 ) ) ;
#33196=CARTESIAN_POINT ( 'NONE',  ( 5.676582343749993598, 59.94791666325269119, 9.832129032723422313 ) ) ;
#33198=CARTESIAN_POINT ( 'NONE',  ( 7.320508075688774596, 17.49999999317202892, -7.320508075688774596 ) ) ;
#33203=CARTESIAN_POINT ( 'NONE',  ( 9.832129032723420536, 51.19791666325268409, -5.676582343749999815 ) ) ;
#33207=CARTESIAN_POINT ( 'NONE',  ( -10.00000000000000000, 12.29166666666666963, -2.679491924311229845 ) ) ;
#33209=CARTESIAN_POINT ( 'NONE',  ( 5.676582343750001591, 51.61458332991934839, -9.832129032723420536 ) ) ;
#33211=CARTESIAN_POINT ( 'NONE',  ( -11.35316468750000141, 178.4895833299193555, 3.042071309553159963 ) ) ;
#33212=CARTESIAN_POINT ( 'NONE',  ( 7.320508075688771044, 136.2499999931720538, 7.320508075688775484 ) ) ;
#33215=CARTESIAN_POINT ( 'NONE',  ( 9.832129032723416984, 35.67708332991935549, 5.676582343750006032 ) ) ;
#33222=CARTESIAN_POINT ( 'NONE',  ( -3.042071309553163960, 172.2395833299193839, -11.35316468749999963 ) ) ;
#33230=CARTESIAN_POINT ( 'NONE',  ( 3.042071309553167069, 122.1354166632526841, -11.35316468749999785 ) ) ;
#33259=CARTESIAN_POINT ( 'NONE',  ( 2.679491924311228956, 121.0416666666666714, -10.00000000000000000 ) ) ;
#33262=CARTESIAN_POINT ( 'NONE',  ( 1.226468279477575784E-15, 292.8593750017070079, 6.676582343750001591 ) ) ;
#33264=ORIENTED_EDGE ( 'NONE', *, *, #59152, .F. ) ;
#33270=CARTESIAN_POINT ( 'NONE',  ( 0.000000000000000000, 300.0000000000000000, 10.00000000000000178 ) ) ;
#33275=CARTESIAN_POINT ( 'NONE',  ( 3.042071309553159519, 19.73958332991934483, 11.35316468750000141 ) ) ;
#33277=CARTESIAN_POINT ( 'NONE',  ( -11.35316468749999785, 213.3854166632526983, -3.042071309553167513 ) ) ;
#33278=CARTESIAN_POINT ( 'NONE',  ( -7.320508075688773708, 133.7499999931720538, -7.320508075688774596 ) ) ;
#33279=CARTESIAN_POINT ( 'NONE',  ( -3.673940397442060854E-16, 290.7500000000000000, -6.000000000000001776 ) ) ;
#33284=CARTESIAN_POINT ( 'NONE',  ( 5.676582343749993598, 14.94791666325268409, 9.832129032723422313 ) ) ;
#33287=CARTESIAN_POINT ( 'NONE',  ( 4.242640687119287435, 292.3750000000000000, 4.242640687119285658 ) ) ;
#33292=CARTESIAN_POINT ( 'NONE',  ( -5.676582343749998039, 12.44791666325268409, -9.832129032723420536 ) ) ;
#33294=CARTESIAN_POINT ( 'NONE',  ( -5.676582343749998039, 137.4479166632526983, -9.832129032723420536 ) ) ;
#33295=CARTESIAN_POINT ( 'NONE',  ( -4.999999999999998224, 103.5416666598386968, -8.660254037844389075 ) ) ;
#33301=ORIENTED_EDGE ( 'NONE', *, *, #19598, .T. ) ;
#33303=CARTESIAN_POINT ( 'NONE',  ( 4.721056650415999201, 288.2343750017069510, -4.721056650415999201 ) ) ;
#33312=CARTESIAN_POINT ( 'NONE',  ( 5.676582343749993598, 150.2604166632526699, 9.832129032723422313 ) ) ;
#33316=CARTESIAN_POINT ( 'NONE',  ( 5.676582343749993598, 80.26041666325268409, 9.832129032723422313 ) ) ;
#33340=ORIENTED_EDGE ( 'NONE', *, *, #63422, .F. ) ;
#33345=CARTESIAN_POINT ( 'NONE',  ( 8.660254037844389075, 85.41666666666667140, -5.000000000000000000 ) ) ;
#33346=EDGE_CURVE ( 'NONE', #70231, #6481, #28880, .T. ) ;
#33348=CARTESIAN_POINT ( 'NONE',  ( 6.000000000000001776, 293.5000000000000000, -7.347880794884121708E-16 ) ) ;
#33350=ORIENTED_EDGE ( 'NONE', *, *, #44827, .F. ) ;
#33359=CARTESIAN_POINT ( 'NONE',  ( 6.123233995736767268E-16, 201.2500000000000000, -10.00000000000000178 ) ) ;
#33362=CARTESIAN_POINT ( 'NONE',  ( 3.042071309553159519, 170.0520833299193271, 11.35316468750000141 ) ) ;
#33365=CARTESIAN_POINT ( 'NONE',  ( -1.836970198721029983E-15, 85.62499999317203958, 10.00000000000000178 ) ) ;
#33367=EDGE_LOOP ( 'NONE', ( #57143, #72629, #66569, #8260 ) ) ;
#33368=CARTESIAN_POINT ( 'NONE',  ( -5.676582343750006032, 19.42708332991934839, 9.832129032723418760 ) ) ;
#33369=EDGE_CURVE ( 'NONE', #1466, #64770, #49151, .T. ) ;
#33371=CARTESIAN_POINT ( 'NONE',  ( 0.000000000000000000, 300.0000000000000000, 0.000000000000000000 ) ) ;
#33375=CARTESIAN_POINT ( 'NONE',  ( 10.00000000000000178, 62.08333332650536818, -2.679491924311226736 ) ) ;
#33380=CARTESIAN_POINT ( 'NONE',  ( 8.660254037844403285, 160.4166666666666856, -5.000000000000008882 ) ) ;
#33381=ORIENTED_EDGE ( 'NONE', *, *, #47224, .T. ) ;
#33382=VERTEX_POINT ( 'NONE', #62670 ) ;
#33388=CARTESIAN_POINT ( 'NONE',  ( 8.311093377946837890, 146.4062499965860127, -8.311093377946837890 ) ) ;
#33402=CARTESIAN_POINT ( 'NONE',  ( 9.832129032723420536, 121.5104166632526841, -5.676582343749999815 ) ) ;
#33406=CARTESIAN_POINT ( 'NONE',  ( 11.35316468749999785, 35.88541666325268409, 3.042071309553174174 ) ) ;
#33408=CARTESIAN_POINT ( 'NONE',  ( -1.836970198721029983E-15, 100.6249999931720396, 10.00000000000000178 ) ) ;
#33413=CARTESIAN_POINT ( 'NONE',  ( -2.485281374238571761, 294.8750000034140157, -6.000000000000003553 ) ) ;
#33414=CARTESIAN_POINT ( 'NONE',  ( 2.679491924311296014, 110.8333333265053682, 9.999999999999959144 ) ) ;
#33416=ORIENTED_EDGE ( 'NONE', *, *, #5400, .F. ) ;
#33417=CARTESIAN_POINT ( 'NONE',  ( 11.35316468750000141, 151.0937499965860411, 0.000000000000000000 ) ) ;
#33424=( BOUNDED_CURVE ( )  B_SPLINE_CURVE ( 2, ( #33826, #56823, #5144, #28137, #53388 ),
 .UNSPECIFIED., .F., .F. ) 
 B_SPLINE_CURVE_WITH_KNOTS ( ( 3, 2, 3 ),
 ( 0.000000000000000000, 0.01041666666666551944, 0.02083333333333103887 ),
 .UNSPECIFIED. ) 
 CURVE ( )  GEOMETRIC_REPRESENTATION_ITEM ( )  RATIONAL_B_SPLINE_CURVE ( ( 1.000000000000000000, 0.9238795325112867385, 1.000000000000000000, 0.9238795325113035029, 0.9999999999999832356 ) ) 
 REPRESENTATION_ITEM ( '' )  );
#33435=CARTESIAN_POINT ( 'NONE',  ( -4.999999999999998224, 41.66666666666667140, -8.660254037844389075 ) ) ;
#33438=CARTESIAN_POINT ( 'NONE',  ( 2.765530957082001251, 289.7656250017069510, 6.676582343749999815 ) ) ;
#33439=CARTESIAN_POINT ( 'NONE',  ( 9.999999999999998224, 35.20833333333333570, -2.679491924311226292 ) ) ;
#33445=CLOSED_SHELL ( 'NONE', ( #8476, #11695, #74305, #73855, #55223, #58205, #32169, #72535, #234, #73042, #25489, #28041, #56953, #22338, #72680, #10145, #50815, #72630, #62508, #18435, #13577, #7440, #40641, #41771, #34889, #68339, #43980, #26425, #13662, #62246, #23740, #7793, #35963, #8335, #45321, #39731, #20070, #55131, #5663, #57058, #52253, #71525, #56158, #3351, #40827, #19267, #3910, #72637, #3981, #36375, #61167, #12863, #74006, #47118, #36502, #146, #24202, #17147, #30247, #70526, #21992, #13787, #11738, #49158, #20558, #27348, #42097, #46702, #51844, #36913, #64840, #37767, #57935, #26441, #7543, #62358, #40863, #62034, #32070, #24716, #51003, #49155, #8989, #11684, #31030, #60181, #60088, #49544, #38878, #14232, #31163, #43862, #38805, #59478, #40678, #7576, #59282, #8803, #18577, #18193, #53449, #9577, #71042, #12958, #40441, #39555, #9280, #16957, #55088, #37655, #54670, #2064, #26656, #27795, #40389, #29335, #34101, #14570, #66213, #62363, #72179, #55505, #71253, #36066, #53703, #17911, #24332, #59063, #11716, #12250, #54559, #32965, #13585, #35736, #4236, #64331, #17635, #69309, #26741, #48219, #688, #16031, #52990 ) ) ;
#33451=CARTESIAN_POINT ( 'NONE',  ( -10.00000000000000355, 147.7083333333333144, 2.679491924311223183 ) ) ;
#33455=CARTESIAN_POINT ( 'NONE',  ( -11.35316468749999785, 123.3854166632526699, -3.042071309553167513 ) ) ;
#33456=CARTESIAN_POINT ( 'NONE',  ( 8.660254037844389075, 212.2916666598387110, -5.000000000000000000 ) ) ;
#33462=CARTESIAN_POINT ( 'NONE',  ( 9.992507110355417055, 225.0379066577874880, -0.4855310866818578486 ) ) ;
#33463=FACE_OUTER_BOUND ( 'NONE', #40570, .T. ) ;
#33467=CARTESIAN_POINT ( 'NONE',  ( -11.35316468750000141, 203.5937499965860127, -1.390361679473963753E-15 ) ) ;
#33474=CARTESIAN_POINT ( 'NONE',  ( -5.676582343749998039, 97.44791666325269830, -9.832129032723420536 ) ) ;
#33480=CARTESIAN_POINT ( 'NONE',  ( -3.042071309553164404, 107.2395833299193413, -11.35316468749999963 ) ) ;
#33482=CARTESIAN_POINT ( 'NONE',  ( 7.320508075688774596, 207.4999999931720254, -7.320508075688774596 ) ) ;
#33484=LINE ( 'NONE', #60642, #12903 ) ;
#33488=CARTESIAN_POINT ( 'NONE',  ( 8.311093377946837890, 86.40624999658599847, -8.311093377946837890 ) ) ;
#33492=CARTESIAN_POINT ( 'NONE',  ( -10.00000000000000000, 184.1666666598386826, -2.679491924311229845 ) ) ;
#33495=CARTESIAN_POINT ( 'NONE',  ( 6.000000000000003553, 296.5000000034139589, 2.485281374238571317 ) ) ;
#33496=CARTESIAN_POINT ( 'NONE',  ( -3.042071309553163960, 77.55208332991934128, -11.35316468749999963 ) ) ;
#33497=CARTESIAN_POINT ( 'NONE',  ( -6.676582343750001591, 289.4531250017069510, 0.000000000000000000 ) ) ;
#33500=CARTESIAN_POINT ( 'NONE',  ( 8.311093377946834337, 225.1562499965860411, 8.311093377946839666 ) ) ;
#33505=CARTESIAN_POINT ( 'NONE',  ( 11.35316468749999785, 205.5729166632526699, 3.042071309553174174 ) ) ;
#33507=CARTESIAN_POINT ( 'NONE',  ( -7.320508075688778149, 99.99999999317203958, 7.320508075688769267 ) ) ;
#33508=CARTESIAN_POINT ( 'NONE',  ( -6.000000000000001776, 300.0000000000000000, 0.000000000000000000 ) ) ;
#33509=VERTEX_POINT ( 'NONE', #20260 ) ;
#33511=CARTESIAN_POINT ( 'NONE',  ( -8.311093377946836114, 197.9687499965860411, -8.311093377946837890 ) ) ;
#33520=CARTESIAN_POINT ( 'NONE',  ( 10.00000000000000178, 10.20833333333333393, -2.679491924311226736 ) ) ;
#33523=ORIENTED_EDGE ( 'NONE', *, *, #15952, .T. ) ;
#33542=CARTESIAN_POINT ( 'NONE',  ( -5.676582343750006032, 84.42708332991935549, 9.832129032723418760 ) ) ;
#33547=CARTESIAN_POINT ( 'NONE',  ( -4.088227598258586603E-16, 288.3593750017070079, -6.676582343750001591 ) ) ;
#33548=CARTESIAN_POINT ( 'NONE',  ( 5.000000000000001776, 77.70833332650536818, -8.660254037844389075 ) ) ;
#33550=CARTESIAN_POINT ( 'NONE',  ( 8.311093377946837890, 206.4062499965860127, -8.311093377946837890 ) ) ;
#33555=CARTESIAN_POINT ( 'NONE',  ( -11.35316468750000141, 168.8020833299193271, 3.042071309553159963 ) ) ;
#33558=CARTESIAN_POINT ( 'NONE',  ( 0.000000000000000000, 300.0000000000000000, 0.000000000000000000 ) ) ;
#33562=CARTESIAN_POINT ( 'NONE',  ( -5.676582343750006032, 49.11458332991935549, 9.832129032723418760 ) ) ;
#33567=CARTESIAN_POINT ( 'NONE',  ( 10.00000000000000178, 142.0833333265053966, -2.679491924311226736 ) ) ;
#33568=CARTESIAN_POINT ( 'NONE',  ( -4.999999999999998224, 168.5416666598387110, -8.660254037844389075 ) ) ;
#33569=CARTESIAN_POINT ( 'NONE',  ( 6.951808397369818766E-16, 67.03124999658602690, -11.35316468750000141 ) ) ;
#33573=DIRECTION ( 'NONE',  ( -0.000000000000000000, 1.000000000000000000, -0.000000000000000000 ) ) ;
#33576=CARTESIAN_POINT ( 'NONE',  ( 9.832129032723416984, 50.36458332991934839, 5.676582343750006032 ) ) ;
#33578=CARTESIAN_POINT ( 'NONE',  ( 2.679491924311074857, 203.9583333333333428, 10.00000000000008349 ) ) ;
#33579=CARTESIAN_POINT ( 'NONE',  ( -3.042071309553164404, 177.2395833299193555, -11.35316468749999963 ) ) ;
#33581=CARTESIAN_POINT ( 'NONE',  ( 2.679491924311228956, 142.9166666598386826, -10.00000000000000000 ) ) ;
#33584=CARTESIAN_POINT ( 'NONE',  ( 11.35316468749999963, 31.30208332991934839, -3.042071309553165293 ) ) ;
#33585=CARTESIAN_POINT ( 'NONE',  ( 9.832129032723420536, 181.1979166632526983, -5.676582343749999815 ) ) ;
#33592=CARTESIAN_POINT ( 'NONE',  ( 5.676582343749993598, 159.9479166632526983, 9.832129032723422313 ) ) ;
#33598=ORIENTED_EDGE ( 'NONE', *, *, #59152, .T. ) ;
#33600=CARTESIAN_POINT ( 'NONE',  ( -5.676582343750006032, 114.4270833299193555, 9.832129032723418760 ) ) ;
#33602=ORIENTED_EDGE ( 'NONE', *, *, #68936, .F. ) ;
#33607=EDGE_CURVE ( 'NONE', #61626, #66396, #19187, .T. ) ;
#33619=CARTESIAN_POINT ( 'NONE',  ( 3.178432602446558121E-13, 206.2500000000000000, -10.00000000000000533 ) ) ;
#33623=ORIENTED_EDGE ( 'NONE', *, *, #23010, .T. ) ;
#33630=CARTESIAN_POINT ( 'NONE',  ( 7.320508075688830552, 60.62500000000004974, -7.320508075688830552 ) ) ;
#33632=CARTESIAN_POINT ( 'NONE',  ( -1.836970198721029983E-15, 123.7500000000000142, 10.00000000000000178 ) ) ;
#33636=CARTESIAN_POINT ( 'NONE',  ( 0.000000000000000000, 300.0000000000000000, 6.000000000000001776 ) ) ;
#33647=CARTESIAN_POINT ( 'NONE',  ( -3.042071309553164404, 17.23958332991935194, -11.35316468749999963 ) ) ;
#33648=CARTESIAN_POINT ( 'NONE',  ( 10.00000000000000178, 0.000000000000000000, 0.000000000000000000 ) ) ;
#33649=CARTESIAN_POINT ( 'NONE',  ( -5.676582343750006032, 214.4270833299193555, 9.832129032723418760 ) ) ;
#33651=CARTESIAN_POINT ( 'NONE',  ( -3.190679070438223991E-13, 203.7500000000000000, 10.00000000000000533 ) ) ;
#33656=CARTESIAN_POINT ( 'NONE',  ( -8.311093377946836114, 22.65624999658601979, -8.311093377946837890 ) ) ;
#33660=CARTESIAN_POINT ( 'NONE',  ( 1.349999999999999201, 283.9999999999998863, 5.686520093750307758 ) ) ;
#33662=CARTESIAN_POINT ( 'NONE',  ( 8.311093377946837890, 11.40624999658601624, -8.311093377946837890 ) ) ;
#33665=CARTESIAN_POINT ( 'NONE',  ( 5.676582343750001591, 141.6145833299193555, -9.832129032723420536 ) ) ;
#33667=CARTESIAN_POINT ( 'NONE',  ( 7.320508075688774596, 107.4999999931720254, -7.320508075688774596 ) ) ;
#33676=CARTESIAN_POINT ( 'NONE',  ( 6.676582343750003368, 291.1718750017069510, -2.765530957081997254 ) ) ;
#33686=FACE_OUTER_BOUND ( 'NONE', #68855, .T. ) ;
#33689=CARTESIAN_POINT ( 'NONE',  ( 3.042071309553167069, 82.13541666325269830, -11.35316468749999785 ) ) ;
#33703=DIRECTION ( 'NONE',  ( -0.000000000000000000, 1.000000000000000000, -0.000000000000000000 ) ) ;
#33704=EDGE_LOOP ( 'NONE', ( #44839, #70351, #7532, #45358 ) ) ;
#33721=CARTESIAN_POINT ( 'NONE',  ( -7.320508075688773708, 86.87500000000001421, -7.320508075688774596 ) ) ;
#33724=CARTESIAN_POINT ( 'NONE',  ( 6.000000000000003553, 290.5625000000000568, -2.485281374238571761 ) ) ;
#33734=CARTESIAN_POINT ( 'NONE',  ( -4.999999999999998224, 196.6666666666666856, -8.660254037844389075 ) ) ;
#33736=CARTESIAN_POINT ( 'NONE',  ( 8.311093377946837890, 166.7187499965859843, -8.311093377946837890 ) ) ;
#33741=CARTESIAN_POINT ( 'NONE',  ( -8.311093377946841443, 24.21874999658601979, 8.311093377946830785 ) ) ;
#33749=CARTESIAN_POINT ( 'NONE',  ( 10.00000000000000178, 57.08333332650536107, -2.679491924311226736 ) ) ;
#33752=CARTESIAN_POINT ( 'NONE',  ( 10.00000000000022204, 214.7916666666668277, 2.679491924311295570 ) ) ;
#33762=CARTESIAN_POINT ( 'NONE',  ( -11.35316468749999785, 138.0729166632526699, -3.042071309553167513 ) ) ;
#33772=VERTEX_POINT ( 'NONE', #18819 ) ;
#33773=AXIS2_PLACEMENT_3D ( 'NONE', #30273, #24598, #12904 ) ;
#33776=CARTESIAN_POINT ( 'NONE',  ( -11.35316468749999785, 128.3854166632526699, -3.042071309553167957 ) ) ;
#33780=CARTESIAN_POINT ( 'NONE',  ( -3.042071309553173730, 29.63541666325268054, 11.35316468749999785 ) ) ;
#33782=ORIENTED_EDGE ( 'NONE', *, *, #35551, .F. ) ;
#33783=CARTESIAN_POINT ( 'NONE',  ( 1.224646799147353454E-15, 300.0000000000000000, -10.00000000000000178 ) ) ;
#33784=CARTESIAN_POINT ( 'NONE',  ( -1.836970198721029983E-15, 195.6249999931720254, 10.00000000000000178 ) ) ;
#33788=EDGE_CURVE ( 'NONE', #24215, #71882, #44315, .T. ) ;
#33791=CARTESIAN_POINT ( 'NONE',  ( 2.485281374238571317, 296.7500000034140157, -6.000000000000003553 ) ) ;
#33795=CARTESIAN_POINT ( 'NONE',  ( -5.676582343749998039, 157.7604166632526983, -9.832129032723420536 ) ) ;
#33802=EDGE_CURVE ( 'NONE', #23110, #25788, #37028, .T. ) ;
#33811=CARTESIAN_POINT ( 'NONE',  ( -7.320508075688773708, 41.87499999999999289, -7.320508075688774596 ) ) ;
#33814=CARTESIAN_POINT ( 'NONE',  ( 6.676582343750002480, 289.0156250017070079, -2.765530957081997254 ) ) ;
#33815=CARTESIAN_POINT ( 'NONE',  ( 2.679491924311179218, 78.95833333333339965, 10.00000000000015810 ) ) ;
#33823=CARTESIAN_POINT ( 'NONE',  ( -2.679491924324927776, 148.5416666666654351, 9.999999999992095212 ) ) ;
#33825=CARTESIAN_POINT ( 'NONE',  ( -10.00000000000000178, 162.5000000000000000, -1.224646799147353454E-15 ) ) ;
#33826=CARTESIAN_POINT ( 'NONE',  ( -6.000000000000001776, 300.0000000000000000, 0.000000000000000000 ) ) ;
#33829=CARTESIAN_POINT ( 'NONE',  ( 11.35316468749999963, 131.3020833299193555, -3.042071309553165293 ) ) ;
#33841=CARTESIAN_POINT ( 'NONE',  ( 8.311093377946834337, 210.4687499965859843, 8.311093377946839666 ) ) ;
#33848=CARTESIAN_POINT ( 'NONE',  ( 11.35316468749999785, 95.57291666325269830, 3.042071309553174174 ) ) ;
#33850=FACE_OUTER_BOUND ( 'NONE', #35170, .T. ) ;
#33854=CARTESIAN_POINT ( 'NONE',  ( 11.35316468749999963, 105.9895833299193555, -3.042071309553165293 ) ) ;
#33859=CARTESIAN_POINT ( 'NONE',  ( 6.123233995736767268E-16, 218.1249999931720538, -10.00000000000000178 ) ) ;
#33863=CARTESIAN_POINT ( 'NONE',  ( -8.311093377946841443, 103.9062499965860269, 8.311093377946834337 ) ) ;
#33868=CARTESIAN_POINT ( 'NONE',  ( 4.999999999999993783, 176.0416666598387110, 8.660254037844390851 ) ) ;
#33871=CARTESIAN_POINT ( 'NONE',  ( 6.951808397369818766E-16, 72.34374999658602690, -11.35316468750000141 ) ) ;
#33872=CARTESIAN_POINT ( 'NONE',  ( -6.676582343750003368, 291.3906250017070079, -2.765530957081996810 ) ) ;
#33875=CARTESIAN_POINT ( 'NONE',  ( 3.042071309553167069, 216.8229166632526699, -11.35316468749999785 ) ) ;
#33879=CARTESIAN_POINT ( 'NONE',  ( 0.000000000000000000, 300.0000000000000000, 0.000000000000000000 ) ) ;
#33880=CARTESIAN_POINT ( 'NONE',  ( 5.676582343750001591, 201.6145833299193555, -9.832129032723420536 ) ) ;
#33882=DIRECTION ( 'NONE',  ( 0.000000000000000000, 0.000000000000000000, 1.000000000000000000 ) ) ;
#33883=CARTESIAN_POINT ( 'NONE',  ( -2.765530957081996810, 298.2656250017068942, -6.676582343750003368 ) ) ;
#33884=ORIENTED_EDGE ( 'NONE', *, *, #73450, .T. ) ;
#33885=CARTESIAN_POINT ( 'NONE',  ( 3.042071309553167513, 197.1354166632526415, -11.35316468749999785 ) ) ;
#33889=ORIENTED_EDGE ( 'NONE', *, *, #55182, .T. ) ;
#33894=CARTESIAN_POINT ( 'NONE',  ( -1.836970198721029983E-15, 8.750000000000000000, 10.00000000000000178 ) ) ;
#33904=CARTESIAN_POINT ( 'NONE',  ( 7.320508075688771044, 16.24999999317203248, 7.320508075688775484 ) ) ;
#33910=ORIENTED_EDGE ( 'NONE', *, *, #54111, .F. ) ;
#33917=CARTESIAN_POINT ( 'NONE',  ( 8.311093377946837890, 81.71874999658601268, -8.311093377946837890 ) ) ;
#33922=CARTESIAN_POINT ( 'NONE',  ( -6.676582343749999815, 289.6718750017070079, 2.765530957082001251 ) ) ;
#33924=CARTESIAN_POINT ( 'NONE',  ( 10.00000000000000000, 76.66666665983871098, 2.679491924311235618 ) ) ;
#33926=CARTESIAN_POINT ( 'NONE',  ( 8.311093377946837890, 196.4062499965860411, -8.311093377946837890 ) ) ;
#33928=ORIENTED_EDGE ( 'NONE', *, *, #37843, .F. ) ;
#33931=CARTESIAN_POINT ( 'NONE',  ( -9.832129032723418760, 168.1770833299193555, -5.676582343750004256 ) ) ;
#33935=CARTESIAN_POINT ( 'NONE',  ( -2.679491924311233397, 113.5416666666666714, 9.999999999999992895 ) ) ;
#33938=CARTESIAN_POINT ( 'NONE',  ( -5.676582343749998039, 57.44791666325269119, -9.832129032723420536 ) ) ;
#33944=CARTESIAN_POINT ( 'NONE',  ( -11.35316468749999785, 63.07291666325268409, -3.042071309553167513 ) ) ;
#33951=CARTESIAN_POINT ( 'NONE',  ( 11.35316468749999785, 45.57291666325266988, 3.042071309553174174 ) ) ;
#33955=CARTESIAN_POINT ( 'NONE',  ( 8.311093377946834337, 170.1562499965860127, 8.311093377946839666 ) ) ;
#33956=CARTESIAN_POINT ( 'NONE',  ( 10.00000000000000178, 146.8749999931720538, 0.000000000000000000 ) ) ;
#33960=CARTESIAN_POINT ( 'NONE',  ( -9.832129032723418760, 33.17708332991934839, -5.676582343750004256 ) ) ;
#33963=CARTESIAN_POINT ( 'NONE',  ( -8.311093377946836114, 187.6562499965860411, -8.311093377946837890 ) ) ;
#33970=CARTESIAN_POINT ( 'NONE',  ( -9.832129032723418760, 162.8645833299193839, -5.676582343750004256 ) ) ;
#33979=CARTESIAN_POINT ( 'NONE',  ( 9.832129032723416984, 115.6770833299193555, 5.676582343750006032 ) ) ;
#33980=CARTESIAN_POINT ( 'NONE',  ( 1.349999999999996092, 255.9999999999997726, 5.686528119825783989 ) ) ;
#33989=EDGE_CURVE ( 'NONE', #29411, #65897, #21158, .T. ) ;
#33998=FACE_OUTER_BOUND ( 'NONE', #68590, .T. ) ;
#33999=CARTESIAN_POINT ( 'NONE',  ( 6.000000000000001776, 293.5000000000000000, -7.347880794884121708E-16 ) ) ;
#34004=VERTEX_POINT ( 'NONE', #38782 ) ;
#34012=CARTESIAN_POINT ( 'NONE',  ( 5.000000000000001776, 115.8333333333333428, -8.660254037844389075 ) ) ;
#34021=CARTESIAN_POINT ( 'NONE',  ( -2.250000000000000000, 265.3333333333333144, 5.427076266392048431 ) ) ;
#34026=CARTESIAN_POINT ( 'NONE',  ( 11.35316468750000141, 20.78124999658601624, 0.000000000000000000 ) ) ;
#34028=CARTESIAN_POINT ( 'NONE',  ( -11.35316468750000141, 208.8020833299193555, 3.042071309553159963 ) ) ;
#34029=DIRECTION ( 'NONE',  ( -0.000000000000000000, 1.000000000000000000, -0.000000000000000000 ) ) ;
#34033=ORIENTED_EDGE ( 'NONE', *, *, #64585, .T. ) ;
#34036=CARTESIAN_POINT ( 'NONE',  ( -3.042071309553173730, 19.32291666325268409, 11.35316468749999785 ) ) ;
#34042=CARTESIAN_POINT ( 'NONE',  ( 5.676582343750001591, 6.614583329919350163, -9.832129032723420536 ) ) ;
#34046=CARTESIAN_POINT ( 'NONE',  ( 9.832129032723416984, 140.3645833299193555, 5.676582343750006032 ) ) ;
#34047=CARTESIAN_POINT ( 'NONE',  ( -4.999999999999998224, 108.5416666598387110, -8.660254037844389075 ) ) ;
#34055=DIRECTION ( 'NONE',  ( -0.000000000000000000, 1.000000000000000000, -0.000000000000000000 ) ) ;
#34056=CARTESIAN_POINT ( 'NONE',  ( -2.765530957081998586, 289.7968750017070079, 6.676582343750001591 ) ) ;
#34063=DIRECTION ( 'NONE',  ( 0.000000000000000000, 0.000000000000000000, 1.000000000000000000 ) ) ;
#34066=CARTESIAN_POINT ( 'NONE',  ( -11.35316468749999785, 73.38541666325268409, -3.042071309553167513 ) ) ;
#34072=CARTESIAN_POINT ( 'NONE',  ( -7.320508075688778149, 109.9999999931720396, 7.320508075688769267 ) ) ;
#34078=CARTESIAN_POINT ( 'NONE',  ( 9.999999999999994671, 109.7916666666666572, 2.679491924311234730 ) ) ;
#34095=CARTESIAN_POINT ( 'NONE',  ( 4.999999999999993783, 79.16666666666667140, 8.660254037844390851 ) ) ;
#34097=CARTESIAN_POINT ( 'NONE',  ( -3.673940397442060854E-16, 289.7500000000000000, -6.000000000000001776 ) ) ;
#34099=( BOUNDED_CURVE ( )  B_SPLINE_CURVE ( 2, ( #61969, #4643, #10297, #38226, #50644, #73664, #21972, #43493, #45000, #20472, #16299, #37857, #4270 ),
 .UNSPECIFIED., .F., .F. ) 
 B_SPLINE_CURVE_WITH_KNOTS ( ( 3, 2, 2, 2, 2, 2, 3 ),
 ( 0.2771739130434782705, 0.2789855072463768293, 0.2807971014492753881, 0.2826086956521738913, 0.2844202898550724501, 0.2862318840579710089, 0.2880434782608695676 ),
 .UNSPECIFIED. ) 
 CURVE ( )  GEOMETRIC_REPRESENTATION_ITEM ( )  RATIONAL_B_SPLINE_CURVE ( ( 1.000000000000000000, 0.9659258262890683122, 1.000000000000000000, 0.9659258262890683122, 1.000000000000000000, 0.9659258262890683122, 1.000000000000000000, 0.9659258262890683122, 1.000000000000000000, 0.9659258262890683122, 1.000000000000000000, 0.9659258262890683122, 1.000000000000000000 ) ) 
 REPRESENTATION_ITEM ( '' )  );
#34101=ADVANCED_FACE ( 'NONE', ( #40257 ), #45915, .T. ) ;
#34104=LINE ( 'NONE', #62005, #12940 ) ;
#34107=CARTESIAN_POINT ( 'NONE',  ( 6.123233995736767268E-16, 206.2500000000000284, -10.00000000000000178 ) ) ;
#34109=CARTESIAN_POINT ( 'NONE',  ( 3.042071309553167069, 172.1354166632526983, -11.35316468749999785 ) ) ;
#34110=CARTESIAN_POINT ( 'NONE',  ( -10.00000000000022382, 212.5000000000001705, -1.224646799147380669E-15 ) ) ;
#34113=ORIENTED_EDGE ( 'NONE', *, *, #40263, .T. ) ;
#34115=CARTESIAN_POINT ( 'NONE',  ( -8.311093377946841443, 34.21874999658601979, 8.311093377946830785 ) ) ;
#34123=CARTESIAN_POINT ( 'NONE',  ( 10.00000000000000178, 66.87499999317203958, 0.000000000000000000 ) ) ;
#34134=CARTESIAN_POINT ( 'NONE',  ( -8.660254037844385522, 87.08333333333332860, -5.000000000000004441 ) ) ;
#34136=CARTESIAN_POINT ( 'NONE',  ( 11.35316468750000141, 145.7812499965860411, 0.000000000000000000 ) ) ;
#34137=CARTESIAN_POINT ( 'NONE',  ( 9.999999999999982236, 104.7916666666666572, 2.679491924311231621 ) ) ;
#34139=LINE ( 'NONE', #39770, #28439 ) ;
#34144=ORIENTED_EDGE ( 'NONE', *, *, #72310, .T. ) ;
#34147=CARTESIAN_POINT ( 'NONE',  ( 9.832129032723416984, 125.6770833299193697, 5.676582343750006032 ) ) ;
#34151=CARTESIAN_POINT ( 'NONE',  ( 9.832129032723420536, 31.51041666325268764, -5.676582343749999815 ) ) ;
#34154=CARTESIAN_POINT ( 'NONE',  ( -8.660254037844390851, 194.7916666598387110, 4.999999999999998224 ) ) ;
#34158=CARTESIAN_POINT ( 'NONE',  ( 6.000000000000001776, 294.5625000034140157, -7.347880794884121708E-16 ) ) ;
#34161=CARTESIAN_POINT ( 'NONE',  ( -2.085542519210945728E-15, 159.8437499965860127, 11.35316468750000141 ) ) ;
#34178=CARTESIAN_POINT ( 'NONE',  ( -8.660254037844387298, 37.08333333333333570, -5.000000000000004441 ) ) ;
#34181=CARTESIAN_POINT ( 'NONE',  ( -4.242640687119286547, 298.8750000000000000, -4.242640687119286547 ) ) ;
#34188=CARTESIAN_POINT ( 'NONE',  ( -5.999999999999999112, 287.1250000034140157, 2.485281374238575314 ) ) ;
#34192=CARTESIAN_POINT ( 'NONE',  ( -10.00000000000000355, 162.7083333333333428, 2.679491924311223183 ) ) ;
#34195=CARTESIAN_POINT ( 'NONE',  ( 6.951808397369818766E-16, 122.3437499965860269, -11.35316468750000141 ) ) ;
#34205=FACE_OUTER_BOUND ( 'NONE', #8452, .T. ) ;
#34208=CARTESIAN_POINT ( 'NONE',  ( 8.311093377946837890, 216.7187499965860411, -8.311093377946837890 ) ) ;
#34216=CARTESIAN_POINT ( 'NONE',  ( -11.35316468749999785, 98.07291666325269830, -3.042071309553167513 ) ) ;
#34223=CARTESIAN_POINT ( 'NONE',  ( 11.35316468749999785, 100.5729166632526699, 3.042071309553174174 ) ) ;
#34227=CARTESIAN_POINT ( 'NONE',  ( -8.660254037844390851, 214.7916666598387110, 4.999999999999998224 ) ) ;
#34231=CARTESIAN_POINT ( 'NONE',  ( -3.042071309553173730, 94.32291666325268409, 11.35316468749999785 ) ) ;
#34235=CARTESIAN_POINT ( 'NONE',  ( 6.123233995736767268E-16, 213.1249999931720538, -10.00000000000000178 ) ) ;
#34237=CARTESIAN_POINT ( 'NONE',  ( 10.00000000000000178, 196.8749999931720254, 0.000000000000000000 ) ) ;
#34240=CARTESIAN_POINT ( 'NONE',  ( -9.832129032723418760, 83.17708332991935549, -5.676582343750004256 ) ) ;
#34241=CARTESIAN_POINT ( 'NONE',  ( 2.765530957081996366, 291.1406250017069510, -6.676582343750003368 ) ) ;
#34244=CARTESIAN_POINT ( 'NONE',  ( 5.676582343749993598, 219.9479166632526983, 9.832129032723422313 ) ) ;
#34246=CARTESIAN_POINT ( 'NONE',  ( -8.660254037844390851, 69.79166665983869677, 4.999999999999998224 ) ) ;
#34249=CARTESIAN_POINT ( 'NONE',  ( -11.35316468750000141, 213.4895833299193839, 3.042071309553159963 ) ) ;
#34251=CARTESIAN_POINT ( 'NONE',  ( 10.00000000000000000, 46.66666665983868967, 2.679491924311235618 ) ) ;
#34253=CARTESIAN_POINT ( 'NONE',  ( 2.765530957082001251, 296.7656250017069510, 6.676582343750000703 ) ) ;
#34256=CARTESIAN_POINT ( 'NONE',  ( 6.951808397369818766E-16, 212.3437499965860411, -11.35316468750000141 ) ) ;
#34260=EDGE_LOOP ( 'NONE', ( #39723, #28815, #13284, #34793 ) ) ;
#34263=CARTESIAN_POINT ( 'NONE',  ( -2.679491924311225848, 26.45833333333333215, -10.00000000000000178 ) ) ;
#34275=CARTESIAN_POINT ( 'NONE',  ( 2.765530957081996366, 297.1406250017069510, -6.676582343750002480 ) ) ;
#34284=EDGE_LOOP ( 'NONE', ( #1296, #68070, #36988, #2800 ) ) ;
#34286=CARTESIAN_POINT ( 'NONE',  ( -5.676582343750006032, 94.42708332991935549, 9.832129032723418760 ) ) ;
#34287=CARTESIAN_POINT ( 'NONE',  ( -1.836970198721029983E-15, 220.6249999931720538, 10.00000000000000178 ) ) ;
#34291=CARTESIAN_POINT ( 'NONE',  ( -2.765530957081998142, 287.7968750017070079, 6.676582343750000703 ) ) ;
#34294=CARTESIAN_POINT ( 'NONE',  ( 7.320508075688771044, 76.24999999317203958, 7.320508075688775484 ) ) ;
#34296=CARTESIAN_POINT ( 'NONE',  ( -11.35316468749999785, 203.0729166632526415, -3.042071309553167513 ) ) ;
#34301=CARTESIAN_POINT ( 'NONE',  ( 3.042071309553159519, 165.0520833299193839, 11.35316468750000141 ) ) ;
#34305=CARTESIAN_POINT ( 'NONE',  ( -9.999999999999998224, 107.5000000000000142, -1.224646799147352862E-15 ) ) ;
#34309=CARTESIAN_POINT ( 'NONE',  ( 6.951808397369818766E-16, 52.03124999658602690, -11.35316468750000141 ) ) ;
#34315=CARTESIAN_POINT ( 'NONE',  ( -5.676582343749998039, 62.44791666325268409, -9.832129032723420536 ) ) ;
#34320=CARTESIAN_POINT ( 'NONE',  ( 8.311093377946834337, 55.15624999658601268, 8.311093377946839666 ) ) ;
#34323=CARTESIAN_POINT ( 'NONE',  ( -7.320508075688778149, 14.99999999317203425, 7.320508075688769267 ) ) ;
#34325=CARTESIAN_POINT ( 'NONE',  ( 3.042071309553159519, 169.7395833299193839, 11.35316468750000141 ) ) ;
#34327=CARTESIAN_POINT ( 'NONE',  ( -5.000000000000005329, 145.2083333265053682, 8.660254037844387298 ) ) ;
#34331=CARTESIAN_POINT ( 'NONE',  ( 9.832129032723420536, 51.51041666325269119, -5.676582343749999815 ) ) ;
#34332=CARTESIAN_POINT ( 'NONE',  ( -7.320508075688778149, 79.99999999317203958, 7.320508075688769267 ) ) ;
#34333=CARTESIAN_POINT ( 'NONE',  ( -8.311093377946836114, 182.6562499965860411, -8.311093377946837890 ) ) ;
#34340=CARTESIAN_POINT ( 'NONE',  ( -2.085542519210945728E-15, 184.5312499965860411, 11.35316468750000141 ) ) ;
#34350=CARTESIAN_POINT ( 'NONE',  ( 9.832129032723420536, 111.5104166632526841, -5.676582343749999815 ) ) ;
#34372=EDGE_CURVE ( 'NONE', #31698, #15376, #21896, .T. ) ;
#34380=CARTESIAN_POINT ( 'NONE',  ( 1.681385197618709730E-11, 51.24999999999869971, -10.00000000000000178 ) ) ;
#34381=CARTESIAN_POINT ( 'NONE',  ( -10.00000000000000178, 122.5000000000000142, -1.224646799147353454E-15 ) ) ;
#34383=CARTESIAN_POINT ( 'NONE',  ( 6.676582343750003368, 289.1718750017070647, -2.765530957081997254 ) ) ;
#34396=CARTESIAN_POINT ( 'NONE',  ( 5.676582343749993598, 9.947916663252682312, 9.832129032723422313 ) ) ;
#34398=CARTESIAN_POINT ( 'NONE',  ( -2.085542519210945728E-15, 209.8437499965860411, 11.35316468750000141 ) ) ;
#34400=CARTESIAN_POINT ( 'NONE',  ( -4.999999999999998224, 218.5416666598387110, -8.660254037844389075 ) ) ;
#34405=CARTESIAN_POINT ( 'NONE',  ( -9.832129032723418760, 27.86458332991935194, -5.676582343750004256 ) ) ;
#34411=CARTESIAN_POINT ( 'NONE',  ( -8.311093377946841443, 13.90624999658601801, 8.311093377946834337 ) ) ;
#34413=CARTESIAN_POINT ( 'NONE',  ( 8.311093377946837890, 131.4062499965860411, -8.311093377946837890 ) ) ;
#34415=CARTESIAN_POINT ( 'NONE',  ( 6.123233995736767268E-16, 103.1249999931720396, -10.00000000000000178 ) ) ;
#34417=CARTESIAN_POINT ( 'NONE',  ( -8.660254037844390851, 4.791666659838699438, 4.999999999999998224 ) ) ;
#34421=CARTESIAN_POINT ( 'NONE',  ( 3.042071309553159519, 5.052083329919350163, 11.35316468750000141 ) ) ;
#34424=CARTESIAN_POINT ( 'NONE',  ( -6.676582343750000703, 287.6718750017070079, 2.765530957082001251 ) ) ;
#34425=CARTESIAN_POINT ( 'NONE',  ( -11.35316468749999785, 128.0729166632526699, -3.042071309553167957 ) ) ;
#34434=DIRECTION ( 'NONE',  ( -0.000000000000000000, 1.000000000000000000, -0.000000000000000000 ) ) ;
#34438=CARTESIAN_POINT ( 'NONE',  ( 9.832129032723420536, 71.51041666325268409, -5.676582343749999815 ) ) ;
#34445=CARTESIAN_POINT ( 'NONE',  ( 10.00000000000000178, 115.2083333333333428, -2.679491924311227180 ) ) ;
#34450=CARTESIAN_POINT ( 'NONE',  ( 9.999999999999996447, 110.2083333333333286, -2.679491924311225848 ) ) ;
#34459=DIRECTION ( 'NONE',  ( 1.000000000000000000, 0.000000000000000000, 0.000000000000000000 ) ) ;
#34463=ORIENTED_EDGE ( 'NONE', *, *, #62342, .F. ) ;
#34471=CARTESIAN_POINT ( 'NONE',  ( 2.679491924311222739, 78.95833333333334281, 10.00000000000000355 ) ) ;
#34473=CARTESIAN_POINT ( 'NONE',  ( -6.676582343750001591, 298.6093750017069510, 0.000000000000000000 ) ) ;
#34484=CARTESIAN_POINT ( 'NONE',  ( 10.00000000000000000, 194.7916666666666856, 2.679491924311236062 ) ) ;
#34486=CARTESIAN_POINT ( 'NONE',  ( 6.951808397369818766E-16, 162.3437499965860127, -11.35316468750000141 ) ) ;
#34490=CARTESIAN_POINT ( 'NONE',  ( -4.242640687119286547, 296.9375000034140157, -4.242640687119286547 ) ) ;
#34493=CARTESIAN_POINT ( 'NONE',  ( -8.311093377946841443, 39.21874999658600558, 8.311093377946830785 ) ) ;
#34502=CARTESIAN_POINT ( 'NONE',  ( -4.999999999999998224, 68.54166665983869677, -8.660254037844389075 ) ) ;
#34508=ORIENTED_EDGE ( 'NONE', *, *, #55476, .T. ) ;
#34512=CARTESIAN_POINT ( 'NONE',  ( 2.765530957082001251, 296.9218750017069510, 6.676582343750000703 ) ) ;
#34513=CARTESIAN_POINT ( 'NONE',  ( -10.00000000000001243, 162.5000000000000000, -1.224646799147354637E-15 ) ) ;
#34515=CARTESIAN_POINT ( 'NONE',  ( 9.832129032723416984, 140.3645833299193555, 5.676582343750006032 ) ) ;
#34525=CARTESIAN_POINT ( 'NONE',  ( -9.832129032723418760, 128.1770833299193555, -5.676582343750004256 ) ) ;
#34529=CARTESIAN_POINT ( 'NONE',  ( 8.311093377946834337, 35.46874999658600558, 8.311093377946839666 ) ) ;
#34535=CARTESIAN_POINT ( 'NONE',  ( 2.485281374238571317, 295.7500000034140157, -6.000000000000003553 ) ) ;
#34538=CARTESIAN_POINT ( 'NONE',  ( 5.676582343749993598, 160.2604166632526983, 9.832129032723422313 ) ) ;
#34555=CARTESIAN_POINT ( 'NONE',  ( -2.679491924311226292, 208.3333333265054250, -10.00000000000000178 ) ) ;
#34557=CARTESIAN_POINT ( 'NONE',  ( 8.660254037844385522, 39.58333333333333570, 5.000000000000005329 ) ) ;
#34567=CARTESIAN_POINT ( 'NONE',  ( 2.679491924311222739, 200.8333333265053398, 10.00000000000000355 ) ) ;
#34568=CARTESIAN_POINT ( 'NONE',  ( 2.679491924311222739, 163.9583333333333712, 10.00000000000000355 ) ) ;
#34572=CARTESIAN_POINT ( 'NONE',  ( -2.085542519210945728E-15, 124.8437499965860269, 11.35316468750000141 ) ) ;
#34582=CARTESIAN_POINT ( 'NONE',  ( 10.00000000000010836, 195.2083333333334281, -2.679491924311255602 ) ) ;
#34584=CARTESIAN_POINT ( 'NONE',  ( 10.00000000000000000, 21.66666665983870388, 2.679491924311236062 ) ) ;
#34590=CARTESIAN_POINT ( 'NONE',  ( -11.35316468750000141, 113.2812499965860269, -1.390361679473963753E-15 ) ) ;
#34596=CARTESIAN_POINT ( 'NONE',  ( 11.35316468750000141, 95.78124999658602690, 0.000000000000000000 ) ) ;
#34600=CARTESIAN_POINT ( 'NONE',  ( -10.00000000000000355, 219.5833333265053966, 2.679491924311223183 ) ) ;
#34604=CARTESIAN_POINT ( 'NONE',  ( -11.35316468750000141, 98.28124999658602690, -1.390361679473963753E-15 ) ) ;
#34607=CARTESIAN_POINT ( 'NONE',  ( 8.660254037844385522, 169.5833333333333428, 5.000000000000005329 ) ) ;
#34609=VECTOR ( 'NONE', #67312, 1000.000000000000000 ) ;
#34610=CARTESIAN_POINT ( 'NONE',  ( -8.660254037844387298, 193.9583333265053966, -5.000000000000004441 ) ) ;
#34613=CARTESIAN_POINT ( 'NONE',  ( 3.042071309553167513, 87.13541666325268409, -11.35316468749999785 ) ) ;
#34614=CARTESIAN_POINT ( 'NONE',  ( -6.676582343750000703, 290.5156250017070079, 2.765530957082001251 ) ) ;
#34617=CARTESIAN_POINT ( 'NONE',  ( -11.35316468749999785, 218.0729166632526699, -3.042071309553167513 ) ) ;
#34621=CARTESIAN_POINT ( 'NONE',  ( 6.951808397369818766E-16, 217.0312499965860411, -11.35316468750000141 ) ) ;
#34622=CARTESIAN_POINT ( 'NONE',  ( 6.123233995736767268E-16, 48.12499999317203958, -10.00000000000000178 ) ) ;
#34623=CARTESIAN_POINT ( 'NONE',  ( -10.00000000000018829, 157.5000000000001137, -1.224646799147375936E-15 ) ) ;
#34624=CARTESIAN_POINT ( 'NONE',  ( -6.676582343750001591, 297.4531250017069510, 0.000000000000000000 ) ) ;
#34627=CARTESIAN_POINT ( 'NONE',  ( 9.832129032723420536, 206.5104166632526983, -5.676582343749999815 ) ) ;
#34629=EDGE_CURVE ( 'NONE', #65897, #71712, #9023, .T. ) ;
#34633=AXIS2_PLACEMENT_3D ( 'NONE', #63134, #28434, #51442 ) ;
#34638=CARTESIAN_POINT ( 'NONE',  ( 8.660254037844389075, 25.41666666666666785, -5.000000000000000000 ) ) ;
#34641=( BOUNDED_CURVE ( )  B_SPLINE_CURVE ( 2, ( #13676, #8036, #71394, #71770, #36715, #48390, #66489, #20086, #59727, #42731, #26490, #72906, #2754 ),
 .UNSPECIFIED., .F., .F. ) 
 B_SPLINE_CURVE_WITH_KNOTS ( ( 3, 2, 2, 2, 2, 2, 3 ),
 ( 2.402083059725570013, 2.407316844168545078, 2.412550628611520587, 2.417784413054495651, 2.423018197497470716, 2.428251981940446225, 2.433485766383421289 ),
 .UNSPECIFIED. ) 
 CURVE ( )  GEOMETRIC_REPRESENTATION_ITEM ( )  RATIONAL_B_SPLINE_CURVE ( ( 1.000000000000087708, 0.9659258262889806046, 1.000000000000000000, 0.9659258262890683122, 1.000000000000000000, 0.9659258262890683122, 1.000000000000000000, 0.9659258262890683122, 1.000000000000000000, 0.9659258262890683122, 1.000000000000000000, 0.9659258262890704216, 0.9999999999999978906 ) ) 
 REPRESENTATION_ITEM ( '' )  );
#34650=CARTESIAN_POINT ( 'NONE',  ( -4.721056650415998313, 294.5781250017069510, 4.721056650416000089 ) ) ;
#34662=CARTESIAN_POINT ( 'NONE',  ( 3.042071309553159519, 85.05208332991934128, 11.35316468750000141 ) ) ;
#34670=CARTESIAN_POINT ( 'NONE',  ( -4.999999999999998224, 178.5416666598387110, -8.660254037844389075 ) ) ;
#34671=CARTESIAN_POINT ( 'NONE',  ( -11.35316468750000141, 193.2812499965860127, -1.390361679473963753E-15 ) ) ;
#34675=CARTESIAN_POINT ( 'NONE',  ( -9.832129032723418760, 178.1770833299193555, -5.676582343750004256 ) ) ;
#34678=CARTESIAN_POINT ( 'NONE',  ( -1.836970198721029983E-15, 90.62499999317203958, 10.00000000000000178 ) ) ;
#34682=CARTESIAN_POINT ( 'NONE',  ( -5.676582343749998039, 62.44791666325268409, -9.832129032723420536 ) ) ;
#34687=CARTESIAN_POINT ( 'NONE',  ( 5.676582343749993598, 59.94791666325268409, 9.832129032723422313 ) ) ;
#34692=CARTESIAN_POINT ( 'NONE',  ( 3.042071309553167513, 61.82291666325267698, -11.35316468749999785 ) ) ;
#34696=CARTESIAN_POINT ( 'NONE',  ( -4.999999999999998224, 158.5416666598387110, -8.660254037844389075 ) ) ;
#34699=CARTESIAN_POINT ( 'NONE',  ( -5.676582343749998039, 52.76041666325269119, -9.832129032723420536 ) ) ;
#34701=CARTESIAN_POINT ( 'NONE',  ( 5.676582343750001591, 176.6145833299193555, -9.832129032723420536 ) ) ;
#34702=ORIENTED_EDGE ( 'NONE', *, *, #39790, .F. ) ;
#34706=CARTESIAN_POINT ( 'NONE',  ( -8.311093377946841443, 178.9062499965859843, 8.311093377946834337 ) ) ;
#34708=EDGE_CURVE ( 'NONE', #66396, #34804, #54898, .T. ) ;
#34714=CARTESIAN_POINT ( 'NONE',  ( 9.832129032723420536, 166.5104166632526983, -5.676582343749999815 ) ) ;
#34718=CARTESIAN_POINT ( 'NONE',  ( -11.35316468750000141, 128.5937499965860127, -1.390361679473963753E-15 ) ) ;
#34720=ORIENTED_EDGE ( 'NONE', *, *, #66288, .F. ) ;
#34745=ORIENTED_EDGE ( 'NONE', *, *, #30419, .F. ) ;
#34751=CARTESIAN_POINT ( 'NONE',  ( -2.765530957081998142, 297.7968750017069510, 6.676582343750000703 ) ) ;
#34752=CARTESIAN_POINT ( 'NONE',  ( -5.000000000000005329, 138.3333333333333428, 8.660254037844387298 ) ) ;
#34755=CARTESIAN_POINT ( 'NONE',  ( -6.676582343750000703, 289.6718750017070079, 2.765530957082001251 ) ) ;
#34757=( BOUNDED_CURVE ( )  B_SPLINE_CURVE ( 2, ( #39684, #6107, #26586, #38298, #62684, #17409, #28362, #40431, #29112, #49610, #95, #72237, #20553 ),
 .UNSPECIFIED., .F., .F. ) 
 B_SPLINE_CURVE_WITH_KNOTS ( ( 3, 2, 2, 2, 2, 2, 3 ),
 ( 0.6576086956521739468, 0.6594202898550725056, 0.6612318840579710644, 0.6630434782608695121, 0.6648550724637680709, 0.6666666666666666297, 0.6684782608695651884 ),
 .UNSPECIFIED. ) 
 CURVE ( )  GEOMETRIC_REPRESENTATION_ITEM ( )  RATIONAL_B_SPLINE_CURVE ( ( 1.000000000000000000, 0.9659258262890683122, 1.000000000000000000, 0.9659258262890683122, 1.000000000000000000, 0.9659258262890683122, 1.000000000000000000, 0.9659258262890683122, 1.000000000000000000, 0.9659258262890683122, 1.000000000000000000, 0.9659258262890683122, 1.000000000000000000 ) ) 
 REPRESENTATION_ITEM ( '' )  );
#34771=CARTESIAN_POINT ( 'NONE',  ( 3.042071309553159519, 14.73958332991935016, 11.35316468750000141 ) ) ;
#34773=CARTESIAN_POINT ( 'NONE',  ( 3.042071309553167069, 222.1354166632526699, -11.35316468749999785 ) ) ;
#34774=CARTESIAN_POINT ( 'NONE',  ( -10.00000000000000355, 219.5833333265053682, 2.679491924311223183 ) ) ;
#34779=CARTESIAN_POINT ( 'NONE',  ( 3.042071309553167069, 21.82291666325268054, -11.35316468749999785 ) ) ;
#34785=CARTESIAN_POINT ( 'NONE',  ( 9.832129032723416984, 25.36458332991935194, 5.676582343750006032 ) ) ;
#34787=CARTESIAN_POINT ( 'NONE',  ( -8.311093377946836114, 137.6562499965859558, -8.311093377946837890 ) ) ;
#34788=CARTESIAN_POINT ( 'NONE',  ( -8.660254037844390851, 109.7916666598387110, 4.999999999999998224 ) ) ;
#34793=ORIENTED_EDGE ( 'NONE', *, *, #50379, .F. ) ;
#34794=CARTESIAN_POINT ( 'NONE',  ( 9.832129032723420536, 11.51041666325268409, -5.676582343749999815 ) ) ;
#34796=CARTESIAN_POINT ( 'NONE',  ( 6.676582343750004256, 298.8906250017069510, 2.765530957081995478 ) ) ;
#34797=CARTESIAN_POINT ( 'NONE',  ( -5.676582343750006032, 139.1145833299193555, 9.832129032723418760 ) ) ;
#34801=DIRECTION ( 'NONE',  ( 0.000000000000000000, 0.000000000000000000, 1.000000000000000000 ) ) ;
#34804=VERTEX_POINT ( 'NONE', #38823 ) ;
#34807=CARTESIAN_POINT ( 'NONE',  ( -11.35316468749999785, 88.38541666325268409, -3.042071309553167513 ) ) ;
#34812=ORIENTED_EDGE ( 'NONE', *, *, #54723, .T. ) ;
#34814=CARTESIAN_POINT ( 'NONE',  ( 6.123233995736767268E-16, 48.12499999317203958, -10.00000000000000178 ) ) ;
#34815=VECTOR ( 'NONE', #49375, 1000.000000000000000 ) ;
#34821=CARTESIAN_POINT ( 'NONE',  ( 2.679491924328011532, 111.0416666666651651, -9.999999999990302868 ) ) ;
#34833=ORIENTED_EDGE ( 'NONE', *, *, #51847, .T. ) ;
#34840=CARTESIAN_POINT ( 'NONE',  ( -10.00000000000000355, 87.70833333333334281, 2.679491924311223183 ) ) ;
#34842=CARTESIAN_POINT ( 'NONE',  ( 6.951808397369818766E-16, 57.34374999658601979, -11.35316468750000141 ) ) ;
#34843=CARTESIAN_POINT ( 'NONE',  ( -2.485281374238572649, 288.1875000000000000, 6.000000000000002665 ) ) ;
#34845=CARTESIAN_POINT ( 'NONE',  ( -3.673940397442060854E-16, 294.7500000000000000, -6.000000000000001776 ) ) ;
#34854=CARTESIAN_POINT ( 'NONE',  ( 10.00000000000000178, 200.2083333333333144, -2.679491924311226736 ) ) ;
#34856=CARTESIAN_POINT ( 'NONE',  ( 3.042071309553167069, 177.1354166632527267, -11.35316468749999785 ) ) ;
#34861=VERTEX_POINT ( 'NONE', #28239 ) ;
#34864=CARTESIAN_POINT ( 'NONE',  ( -5.676582343749998039, 37.76041666325267698, -9.832129032723420536 ) ) ;
#34867=CARTESIAN_POINT ( 'NONE',  ( 6.123233995736767268E-16, 123.1249999931720396, -10.00000000000000178 ) ) ;
#34868=CARTESIAN_POINT ( 'NONE',  ( 8.660254037844389075, 222.2916666598387110, -5.000000000000000000 ) ) ;
#34871=CARTESIAN_POINT ( 'NONE',  ( -10.00000000000000355, 64.58333332650536818, 2.679491924311223183 ) ) ;
#34881=CARTESIAN_POINT ( 'NONE',  ( -4.088227598258586603E-16, 298.3593750017070079, -6.676582343750001591 ) ) ;
#34883=CARTESIAN_POINT ( 'NONE',  ( -5.000000000000005329, 88.33333333333332860, 8.660254037844385522 ) ) ;
#34884=CARTESIAN_POINT ( 'NONE',  ( -5.676582343750006032, 159.1145833299193839, 9.832129032723418760 ) ) ;
#34889=ADVANCED_FACE ( 'NONE', ( #22565 ), #45585, .T. ) ;
#34894=CARTESIAN_POINT ( 'NONE',  ( -2.085542519210945728E-15, 134.8437499965860127, 11.35316468750000141 ) ) ;
#34899=CARTESIAN_POINT ( 'NONE',  ( 3.042071309553167069, 47.13541666325268409, -11.35316468749999785 ) ) ;
#34901=CARTESIAN_POINT ( 'NONE',  ( 10.00000000000000000, 36.66666665983869677, 2.679491924311235618 ) ) ;
#34906=CARTESIAN_POINT ( 'NONE',  ( 2.485281374238575314, 298.3750000034140157, 6.000000000000000888 ) ) ;
#34921=DIRECTION ( 'NONE',  ( -0.000000000000000000, 1.000000000000000000, -0.000000000000000000 ) ) ;
#34928=CARTESIAN_POINT ( 'NONE',  ( -7.320508075688773708, 46.87500000000000000, -7.320508075688774596 ) ) ;
#34940=CARTESIAN_POINT ( 'NONE',  ( 8.660254037844389075, 202.2916666598387110, -5.000000000000000000 ) ) ;
#34941=CARTESIAN_POINT ( 'NONE',  ( -10.00000000000000178, 157.5000000000000000, -1.224646799147353454E-15 ) ) ;
#34945=CARTESIAN_POINT ( 'NONE',  ( -3.042071309553164404, 122.5520833299193413, -11.35316468749999963 ) ) ;
#34953=CARTESIAN_POINT ( 'NONE',  ( 8.660254037844477892, 194.5833333333334281, 5.000000000000059508 ) ) ;
#34955=CARTESIAN_POINT ( 'NONE',  ( 6.123233995736767268E-16, 23.12499999317203603, -10.00000000000000178 ) ) ;
#34962=CARTESIAN_POINT ( 'NONE',  ( 6.951808397369818766E-16, 102.0312499965860269, -11.35316468750000141 ) ) ;
#34965=CYLINDRICAL_SURFACE ( 'NONE', #27739, 10.00000000000000178 ) ;
#34966=CARTESIAN_POINT ( 'NONE',  ( 2.679491924333024855, 41.04166666666481689, -9.999999999987601029 ) ) ;
#34968=CARTESIAN_POINT ( 'NONE',  ( 11.35316468749999785, 115.5729166632526841, 3.042071309553174174 ) ) ;
#34973=CARTESIAN_POINT ( 'NONE',  ( -10.00000000000000355, 214.5833333265053682, 2.679491924311223183 ) ) ;
#34976=CARTESIAN_POINT ( 'NONE',  ( -7.320508075688771932, 181.8750000000000000, -7.320508075688772820 ) ) ;
#34977=CARTESIAN_POINT ( 'NONE',  ( -9.832129032723418760, 97.86458332991935549, -5.676582343750004256 ) ) ;
#34980=EDGE_CURVE ( 'NONE', #45507, #19485, #22193, .T. ) ;
#34983=CARTESIAN_POINT ( 'NONE',  ( 7.320508075688774596, 192.4999999931720538, -7.320508075688774596 ) ) ;
#34986=CARTESIAN_POINT ( 'NONE',  ( -3.042071309553163960, 82.55208332991935549, -11.35316468749999963 ) ) ;
#34991=CARTESIAN_POINT ( 'NONE',  ( 5.676582343750001591, 221.6145833299193839, -9.832129032723420536 ) ) ;
#34995=CARTESIAN_POINT ( 'NONE',  ( -8.311093377946836114, 217.6562499965860127, -8.311093377946837890 ) ) ;
#34996=DIRECTION ( 'NONE',  ( 0.000000000000000000, 0.000000000000000000, 1.000000000000000000 ) ) ;
#34998=CARTESIAN_POINT ( 'NONE',  ( -4.721056650415999201, 296.3281250017069510, -4.721056650415999201 ) ) ;
#35001=CARTESIAN_POINT ( 'NONE',  ( -9.832129032723420536, 214.0104166632526699, 5.676582343749997150 ) ) ;
#35010=CARTESIAN_POINT ( 'NONE',  ( 7.320508075688774596, 25.62499999999999645, -7.320508075688774596 ) ) ;
#35022=CARTESIAN_POINT ( 'NONE',  ( 6.676582343750003368, 297.8906250017069510, 2.765530957081995478 ) ) ;
#35030=CARTESIAN_POINT ( 'NONE',  ( -11.35316468750000141, 93.59374999658602690, -1.390361679473963753E-15 ) ) ;
#35035=CARTESIAN_POINT ( 'NONE',  ( 4.721056650416000089, 287.9843750017070079, 4.721056650415999201 ) ) ;
#35039=CARTESIAN_POINT ( 'NONE',  ( 9.832129032723420536, 201.1979166632526983, -5.676582343749999815 ) ) ;
#35040=EDGE_CURVE ( 'NONE', #1694, #15967, #52036, .T. ) ;
#35045=CARTESIAN_POINT ( 'NONE',  ( -8.311093377946836114, 182.9687499965859843, -8.311093377946837890 ) ) ;
#35052=CARTESIAN_POINT ( 'NONE',  ( 8.311093377946834337, 75.15624999658602690, 8.311093377946839666 ) ) ;
#35058=CARTESIAN_POINT ( 'NONE',  ( -8.311093377946841443, 63.90624999658601979, 8.311093377946830785 ) ) ;
#35063=CARTESIAN_POINT ( 'NONE',  ( 8.311093377946834337, 65.15624999658602690, 8.311093377946839666 ) ) ;
#35067=CARTESIAN_POINT ( 'NONE',  ( -5.000000000000005329, 160.2083333265053966, 8.660254037844387298 ) ) ;
#35069=CARTESIAN_POINT ( 'NONE',  ( -5.394762896564973355E-12, 18.74999999999958433, 10.00000000000000178 ) ) ;
#35070=CARTESIAN_POINT ( 'NONE',  ( -8.311093377946836114, 52.96874999658601268, -8.311093377946837890 ) ) ;
#35072=CARTESIAN_POINT ( 'NONE',  ( -8.311093377946841443, 183.9062499965860411, 8.311093377946830785 ) ) ;
#35076=CARTESIAN_POINT ( 'NONE',  ( 4.999999999999993783, 61.04166665983870388, 8.660254037844390851 ) ) ;
#35078=CARTESIAN_POINT ( 'NONE',  ( -11.35316468750000141, 173.2812499965860411, -1.390361679473963753E-15 ) ) ;
#35084=CARTESIAN_POINT ( 'NONE',  ( -3.042071309553173730, 164.6354166632526699, 11.35316468749999785 ) ) ;
#35086=CARTESIAN_POINT ( 'NONE',  ( 8.311093377946837890, 131.7187499965860127, -8.311093377946837890 ) ) ;
#35093=( BOUNDED_CURVE ( )  B_SPLINE_CURVE ( 2, ( #18704, #3207, #8865, #13388, #14128, #36426, #7752, #64724, #19425, #59076, #42067, #8117, #65821 ),
 .UNSPECIFIED., .F., .F. ) 
 B_SPLINE_CURVE_WITH_KNOTS ( ( 3, 2, 2, 2, 2, 2, 3 ),
 ( 0.01630434782608695607, 0.01811594202898550790, 0.01992753623188405626, 0.02173913043478260809, 0.02355072463768115992, 0.02536231884057971175, 0.02717391304347826012 ),
 .UNSPECIFIED. ) 
 CURVE ( )  GEOMETRIC_REPRESENTATION_ITEM ( )  RATIONAL_B_SPLINE_CURVE ( ( 1.000000000000000000, 0.9659258262890683122, 1.000000000000000000, 0.9659258262890683122, 1.000000000000000000, 0.9659258262890683122, 1.000000000000000000, 0.9659258262890683122, 1.000000000000000000, 0.9659258262890683122, 1.000000000000000000, 0.9659258262890683122, 1.000000000000000000 ) ) 
 REPRESENTATION_ITEM ( '' )  );
#35100=CARTESIAN_POINT ( 'NONE',  ( -10.00000000000005507, 177.5000000000000853, -1.224646799147360159E-15 ) ) ;
#35116=CARTESIAN_POINT ( 'NONE',  ( 2.765530957082001251, 296.9218750017069510, 6.676582343749999815 ) ) ;
#35117=CARTESIAN_POINT ( 'NONE',  ( -7.320508075688778149, 138.1250000000000000, 7.320508075688769267 ) ) ;
#35119=CARTESIAN_POINT ( 'NONE',  ( 3.819983998516707224, 225.9999999999999716, 9.249899904189801347 ) ) ;
#35134=CARTESIAN_POINT ( 'NONE',  ( 3.042071309553159519, 24.73958332991934483, 11.35316468750000141 ) ) ;
#35135=CARTESIAN_POINT ( 'NONE',  ( 10.00000000000000178, 1.874999993172032697, 0.000000000000000000 ) ) ;
#35138=CARTESIAN_POINT ( 'NONE',  ( -1.836970198721029983E-15, 43.75000000000000711, 10.00000000000000178 ) ) ;
#35139=AXIS2_PLACEMENT_3D ( 'NONE', #27593, #11368, #74360 ) ;
#35143=EDGE_CURVE ( 'NONE', #5256, #49691, #58783, .T. ) ;
#35144=CARTESIAN_POINT ( 'NONE',  ( -5.676582343749998039, 27.44791666325268409, -9.832129032723420536 ) ) ;
#35148=DIRECTION ( 'NONE',  ( -0.000000000000000000, 1.000000000000000000, -0.000000000000000000 ) ) ;
#35150=CARTESIAN_POINT ( 'NONE',  ( -2.085542519210945728E-15, 14.53124999658601624, 11.35316468750000141 ) ) ;
#35152=CARTESIAN_POINT ( 'NONE',  ( 5.676582343749993598, 154.9479166632526983, 9.832129032723422313 ) ) ;
#35153=CARTESIAN_POINT ( 'NONE',  ( 4.999999999999993783, 121.0416666598386968, 8.660254037844390851 ) ) ;
#35158=CARTESIAN_POINT ( 'NONE',  ( -11.35316468750000141, 13.80208332991934839, 3.042071309553159963 ) ) ;
#35161=CARTESIAN_POINT ( 'NONE',  ( -4.088227598258586603E-16, 297.2031250017070079, -6.676582343750001591 ) ) ;
#35162=CARTESIAN_POINT ( 'NONE',  ( 3.042071309553167513, 141.8229166632526983, -11.35316468749999785 ) ) ;
#35165=AXIS2_PLACEMENT_3D ( 'NONE', #62857, #57220, #68526 ) ;
#35170=EDGE_LOOP ( 'NONE', ( #51017, #30359, #13312, #61863, #42733 ) ) ;
#35172=CARTESIAN_POINT ( 'NONE',  ( 0.000000000000000000, 300.0000000000000000, 0.000000000000000000 ) ) ;
#35173=CARTESIAN_POINT ( 'NONE',  ( 11.35316468749999963, 86.30208332991936970, -3.042071309553165293 ) ) ;
#35184=AXIS2_PLACEMENT_3D ( 'NONE', #38504, #61504, #51297 ) ;
#35188=ORIENTED_EDGE ( 'NONE', *, *, #47390, .F. ) ;
#35204=CARTESIAN_POINT ( 'NONE',  ( 7.320508075688774596, 95.62499999999998579, -7.320508075688774596 ) ) ;
#35208=CARTESIAN_POINT ( 'NONE',  ( 8.311093377946834337, 60.46874999658602690, 8.311093377946839666 ) ) ;
#35209=CARTESIAN_POINT ( 'NONE',  ( -4.088227598258586603E-16, 299.3593750017070079, -6.676582343750001591 ) ) ;
#35212=CARTESIAN_POINT ( 'NONE',  ( 6.000000000000003553, 294.5625000000000000, -2.485281374238571761 ) ) ;
#35218=CARTESIAN_POINT ( 'NONE',  ( -7.320508075688778149, 208.1250000000000000, 7.320508075688769267 ) ) ;
#35220=CARTESIAN_POINT ( 'NONE',  ( -11.35316468749999785, 183.3854166632526699, -3.042071309553167513 ) ) ;
#35224=CARTESIAN_POINT ( 'NONE',  ( 8.660254037844389075, 87.29166665983869677, -5.000000000000000000 ) ) ;
#35228=CARTESIAN_POINT ( 'NONE',  ( -8.311093377946836114, 37.96874999658601979, -8.311093377946837890 ) ) ;
#35231=CARTESIAN_POINT ( 'NONE',  ( -8.660254037844390851, 124.7916666598387110, 4.999999999999998224 ) ) ;
#35234=CARTESIAN_POINT ( 'NONE',  ( -10.00000000000000000, 79.16666665983872520, -2.679491924311229845 ) ) ;
#35240=CARTESIAN_POINT ( 'NONE',  ( -1.836970198721029983E-15, 100.6249999931720396, 10.00000000000000178 ) ) ;
#35241=ORIENTED_EDGE ( 'NONE', *, *, #65946, .T. ) ;
#35242=ORIENTED_EDGE ( 'NONE', *, *, #5446, .F. ) ;
#35243=CARTESIAN_POINT ( 'NONE',  ( -6.000000000000003553, 288.9375000000000000, -2.485281374238571317 ) ) ;
#35244=CARTESIAN_POINT ( 'NONE',  ( 1.226468279477575784E-15, 297.8593750017070079, 6.676582343750001591 ) ) ;
#35246=CARTESIAN_POINT ( 'NONE',  ( 4.999999999999993783, 41.04166665983870388, 8.660254037844390851 ) ) ;
#35247=CARTESIAN_POINT ( 'NONE',  ( -2.085542519210945728E-15, 159.5312499965860127, 11.35316468750000141 ) ) ;
#35258=CARTESIAN_POINT ( 'NONE',  ( 9.832129032723416984, 130.6770833299193555, 5.676582343750006032 ) ) ;
#35263=CARTESIAN_POINT ( 'NONE',  ( 11.35316468749999785, 50.88541666325269119, 3.042071309553174174 ) ) ;
#35264=ORIENTED_EDGE ( 'NONE', *, *, #9748, .F. ) ;
#35271=CARTESIAN_POINT ( 'NONE',  ( -2.485281374238572649, 292.2500000034140726, 6.000000000000002665 ) ) ;
#35293=CARTESIAN_POINT ( 'NONE',  ( 2.679491924311222739, 48.95833333333333570, 10.00000000000000355 ) ) ;
#35296=CARTESIAN_POINT ( 'NONE',  ( -4.242640687119286547, 299.8750000000000000, -4.242640687119286547 ) ) ;
#35297=CARTESIAN_POINT ( 'NONE',  ( -7.320508075688778149, 34.99999999317203248, 7.320508075688769267 ) ) ;
#35305=CARTESIAN_POINT ( 'NONE',  ( -1.836970198721029983E-15, 140.6249999931720538, 10.00000000000000178 ) ) ;
#35308=CARTESIAN_POINT ( 'NONE',  ( 10.00000000000000178, 165.0000000000000000, 0.000000000000000000 ) ) ;
#35311=( BOUNDED_CURVE ( )  B_SPLINE_CURVE ( 2, ( #60920, #9243, #9627, #32265, #49606, #32647, #72993, #46546, #17503 ),
 .UNSPECIFIED., .F., .F. ) 
 B_SPLINE_CURVE_WITH_KNOTS ( ( 3, 2, 2, 2, 3 ),
 ( 0.1458333333333311499, 0.1562499999999978073, 0.1666666666666644647, 0.1770833333333311777, 0.1874999999999978351 ),
 .UNSPECIFIED. ) 
 CURVE ( )  GEOMETRIC_REPRESENTATION_ITEM ( )  RATIONAL_B_SPLINE_CURVE ( ( 1.000000000000015987, 0.9238795325112707513, 1.000000000000000000, 0.9238795325112867385, 1.000000000000000000, 0.9238795325112867385, 1.000000000000000000, 0.9238795325113025037, 0.9999999999999842348 ) ) 
 REPRESENTATION_ITEM ( '' )  );
#35313=CARTESIAN_POINT ( 'NONE',  ( 11.35316468749999963, 136.3020833299193555, -3.042071309553165293 ) ) ;
#35315=CARTESIAN_POINT ( 'NONE',  ( 7.320508075688771044, 26.24999999317203248, 7.320508075688775484 ) ) ;
#35323=CARTESIAN_POINT ( 'NONE',  ( 1.522769729196201526E-11, 196.2499999999988063, -10.00000000000000178 ) ) ;
#35326=CARTESIAN_POINT ( 'NONE',  ( -1.836970198721029983E-15, 40.62499999317203248, 10.00000000000000178 ) ) ;
#35336=CARTESIAN_POINT ( 'NONE',  ( -1.836970198721029983E-15, 180.6249999931720538, 10.00000000000000178 ) ) ;
#35338=CARTESIAN_POINT ( 'NONE',  ( -11.35316468750000141, 118.2812499965860269, -1.390361679473963753E-15 ) ) ;
#35340=CARTESIAN_POINT ( 'NONE',  ( 1.224646799147353454E-15, 300.0000000000000000, -10.00000000000000178 ) ) ;
#35342=CARTESIAN_POINT ( 'NONE',  ( -7.320508075688773708, 218.7499999931720538, -7.320508075688774596 ) ) ;
#35344=CARTESIAN_POINT ( 'NONE',  ( 0.000000000000000000, 300.0000000000000000, 10.00000000000000178 ) ) ;
#35346=CARTESIAN_POINT ( 'NONE',  ( -9.832129032723420536, 98.69791666325269830, 5.676582343749997150 ) ) ;
#35349=CARTESIAN_POINT ( 'NONE',  ( 10.00000000000009059, 175.0000000000000568, 0.000000000000000000 ) ) ;
#35351=CARTESIAN_POINT ( 'NONE',  ( 10.00000000000000178, 192.0833333265053682, -2.679491924311226736 ) ) ;
#35355=CARTESIAN_POINT ( 'NONE',  ( -3.042071309553163960, 92.55208332991935549, -11.35316468749999963 ) ) ;
#35359=CARTESIAN_POINT ( 'NONE',  ( -11.35316468749999785, 3.385416663252682756, -3.042071309553167513 ) ) ;
#35363=CARTESIAN_POINT ( 'NONE',  ( -5.676582343749998039, 222.4479166632526983, -9.832129032723420536 ) ) ;
#35365=CARTESIAN_POINT ( 'NONE',  ( 7.320508075688771044, 46.24999999317203248, 7.320508075688775484 ) ) ;
#35367=CARTESIAN_POINT ( 'NONE',  ( -4.721056650415998313, 297.5781250017069510, 4.721056650416000089 ) ) ;
#35369=CARTESIAN_POINT ( 'NONE',  ( 3.153939666463620179E-13, 118.7500000000000426, 9.999999999999998224 ) ) ;
#35370=CARTESIAN_POINT ( 'NONE',  ( 8.311093377946834337, 210.4687499965859843, 8.311093377946839666 ) ) ;
#35379=CARTESIAN_POINT ( 'NONE',  ( -7.320508075688778149, 23.12500000000000355, 7.320508075688769267 ) ) ;
#35382=ORIENTED_EDGE ( 'NONE', *, *, #42494, .F. ) ;
#35387=CARTESIAN_POINT ( 'NONE',  ( 4.721056650415999201, 297.0781250017069510, -4.721056650415999201 ) ) ;
#35388=EDGE_CURVE ( 'NONE', #31834, #12265, #48542, .T. ) ;
#35392=ORIENTED_EDGE ( 'NONE', *, *, #73132, .F. ) ;
#35397=EDGE_LOOP ( 'NONE', ( #20951, #2334, #68738, #41548 ) ) ;
#35399=CARTESIAN_POINT ( 'NONE',  ( -9.832129032723418760, 98.17708332991935549, -5.676582343750004256 ) ) ;
#35404=CARTESIAN_POINT ( 'NONE',  ( -4.721056650415998313, 287.7343750017069510, 4.721056650416000089 ) ) ;
#35409=CARTESIAN_POINT ( 'NONE',  ( -5.676582343749998039, 207.4479166632527267, -9.832129032723420536 ) ) ;
#35413=CARTESIAN_POINT ( 'NONE',  ( 5.676582343749993598, 180.2604166632526699, 9.832129032723422313 ) ) ;
#35419=CARTESIAN_POINT ( 'NONE',  ( 11.35316468749999963, 65.98958332991936970, -3.042071309553165293 ) ) ;
#35423=ORIENTED_EDGE ( 'NONE', *, *, #48230, .T. ) ;
#35427=CARTESIAN_POINT ( 'NONE',  ( 11.35316468749999963, 75.98958332991935549, -3.042071309553165293 ) ) ;
#35430=CARTESIAN_POINT ( 'NONE',  ( -3.042071309553173730, 54.32291666325268409, 11.35316468749999785 ) ) ;
#35434=CARTESIAN_POINT ( 'NONE',  ( 10.00000000000000178, 151.8749999931720538, 0.000000000000000000 ) ) ;
#35436=CARTESIAN_POINT ( 'NONE',  ( 2.679491924305151596, 18.95833333333278858, 10.00000000000351896 ) ) ;
#35437=CARTESIAN_POINT ( 'NONE',  ( 3.042071309553159519, 55.05208332991934128, 11.35316468750000141 ) ) ;
#35439=CARTESIAN_POINT ( 'NONE',  ( 6.951808397369818766E-16, 197.0312499965860411, -11.35316468750000141 ) ) ;
#35445=CARTESIAN_POINT ( 'NONE',  ( -5.676582343750006032, 174.1145833299193555, 9.832129032723418760 ) ) ;
#35448=VERTEX_POINT ( 'NONE', #14954 ) ;
#35449=CARTESIAN_POINT ( 'NONE',  ( 5.676582343750001591, 171.9270833299193555, -9.832129032723420536 ) ) ;
#35451=CARTESIAN_POINT ( 'NONE',  ( -2.085542519210945728E-15, 124.8437499965860269, 11.35316468750000141 ) ) ;
#35478=CARTESIAN_POINT ( 'NONE',  ( 2.765530957081996366, 298.2968750017070079, -6.676582343750002480 ) ) ;
#35479=CARTESIAN_POINT ( 'NONE',  ( 2.679491924311228956, 141.0416666666666572, -10.00000000000000000 ) ) ;
#35496=CARTESIAN_POINT ( 'NONE',  ( -11.35316468750000141, 28.28124999658601624, -1.390361679473963753E-15 ) ) ;
#35498=CARTESIAN_POINT ( 'NONE',  ( -5.676582343749998039, 217.7604166632526983, -9.832129032723420536 ) ) ;
#35501=DIRECTION ( 'NONE',  ( -0.000000000000000000, 1.000000000000000000, -0.000000000000000000 ) ) ;
#35504=CARTESIAN_POINT ( 'NONE',  ( 9.832129032723420536, 36.19791666325267698, -5.676582343749999815 ) ) ;
#35510=CARTESIAN_POINT ( 'NONE',  ( -9.832129032723420536, 18.69791666325268409, 5.676582343749997150 ) ) ;
#35512=CARTESIAN_POINT ( 'NONE',  ( -8.311093377946836114, 147.6562499965860411, -8.311093377946837890 ) ) ;
#35513=CARTESIAN_POINT ( 'NONE',  ( -4.999999999999998224, 118.5416666598386968, -8.660254037844389075 ) ) ;
#35515=CARTESIAN_POINT ( 'NONE',  ( 5.000000000000001776, 172.7083333265053682, -8.660254037844389075 ) ) ;
#35518=CARTESIAN_POINT ( 'NONE',  ( -11.35316468750000141, 3.802083329919350163, 3.042071309553159963 ) ) ;
#35520=EDGE_LOOP ( 'NONE', ( #35241, #51236, #47298, #13793 ) ) ;
#35522=CARTESIAN_POINT ( 'NONE',  ( 4.721056650415999201, 298.0781250017069510, -4.721056650415999201 ) ) ;
#35524=CARTESIAN_POINT ( 'NONE',  ( -11.35316468750000141, 138.4895833299193555, 3.042071309553159963 ) ) ;
#35534=CARTESIAN_POINT ( 'NONE',  ( -9.832129032723418760, 83.17708332991935549, -5.676582343750004256 ) ) ;
#35546=VECTOR ( 'NONE', #28974, 1000.000000000000000 ) ;
#35550=ORIENTED_EDGE ( 'NONE', *, *, #42627, .T. ) ;
#35551=EDGE_CURVE ( 'NONE', #3815, #72057, #71368, .T. ) ;
#35555=CARTESIAN_POINT ( 'NONE',  ( -1.836970198721029983E-15, 80.62499999317203958, 10.00000000000000178 ) ) ;
#35566=CARTESIAN_POINT ( 'NONE',  ( -8.660254037844390851, 92.91666666666667140, 4.999999999999998224 ) ) ;
#35568=CARTESIAN_POINT ( 'NONE',  ( 3.042071309553167069, 62.13541666325267698, -11.35316468749999785 ) ) ;
#35569=CARTESIAN_POINT ( 'NONE',  ( 6.676582343750003368, 297.1718750017071216, -2.765530957081997254 ) ) ;
#35572=CARTESIAN_POINT ( 'NONE',  ( -2.679491924311226292, 173.3333333265053682, -10.00000000000000178 ) ) ;
#35575=CARTESIAN_POINT ( 'NONE',  ( -10.00000000000000355, 104.5833333265053824, 2.679491924311223183 ) ) ;
#35580=CARTESIAN_POINT ( 'NONE',  ( -1.836970198721029983E-15, 218.7500000000000284, 10.00000000000000178 ) ) ;
#35582=CARTESIAN_POINT ( 'NONE',  ( -5.676582343749998039, 187.7604166632526983, -9.832129032723420536 ) ) ;
#35584=CARTESIAN_POINT ( 'NONE',  ( 7.320508075688771044, 176.2499999931720254, 7.320508075688775484 ) ) ;
#35589=CARTESIAN_POINT ( 'NONE',  ( 3.042071309553167069, 37.13541666325268409, -11.35316468749999785 ) ) ;
#35591=CARTESIAN_POINT ( 'NONE',  ( 8.311093377946837890, 226.7187499965860411, -8.311093377946837890 ) ) ;
#35597=CARTESIAN_POINT ( 'NONE',  ( 2.679491924311228956, 72.91666665983871098, -10.00000000000000000 ) ) ;
#35606=CARTESIAN_POINT ( 'NONE',  ( 4.721056650416000089, 297.9843750017070079, 4.721056650415999201 ) ) ;
#35607=CARTESIAN_POINT ( 'NONE',  ( -3.166186134455097228E-13, 141.2500000000000284, -9.999999999999998224 ) ) ;
#35608=CARTESIAN_POINT ( 'NONE',  ( 8.660254037844389075, 42.29166665983870388, -5.000000000000000000 ) ) ;
#35609=CARTESIAN_POINT ( 'NONE',  ( -11.35316468750000141, 158.2812499965860127, -1.390361679473963753E-15 ) ) ;
#35611=FACE_OUTER_BOUND ( 'NONE', #65650, .T. ) ;
#35617=DIRECTION ( 'NONE',  ( -0.000000000000000000, 1.000000000000000000, -0.000000000000000000 ) ) ;
#35618=CARTESIAN_POINT ( 'NONE',  ( 5.676582343750001591, 146.9270833299193555, -9.832129032723420536 ) ) ;
#35620=CARTESIAN_POINT ( 'NONE',  ( -2.485281374238875962, 290.8125000000000568, -5.999999999999697131 ) ) ;
#35622=CARTESIAN_POINT ( 'NONE',  ( 9.832129032723416984, 45.67708332991934839, 5.676582343750006032 ) ) ;
#35629=CARTESIAN_POINT ( 'NONE',  ( 4.242640687119285658, 291.6875000034139589, -4.242640687119286547 ) ) ;
#35650=EDGE_LOOP ( 'NONE', ( #25024, #71571, #14723, #26035 ) ) ;
#35653=CARTESIAN_POINT ( 'NONE',  ( 2.679491924311228956, 51.04166666666665719, -10.00000000000000000 ) ) ;
#35667=CARTESIAN_POINT ( 'NONE',  ( -1.744157829248402118E-12, 86.25000000000015632, -10.00000000000000533 ) ) ;
#35668=CARTESIAN_POINT ( 'NONE',  ( -1.836970198721029983E-15, 178.7500000000000284, 10.00000000000000178 ) ) ;
#35671=CARTESIAN_POINT ( 'NONE',  ( 11.35316468750000141, 141.0937499965860127, 0.000000000000000000 ) ) ;
#35676=CARTESIAN_POINT ( 'NONE',  ( -8.660254037844389075, 167.0833333333333428, -5.000000000000006217 ) ) ;
#35678=CARTESIAN_POINT ( 'NONE',  ( 5.676582343750001591, 1.927083329919350163, -9.832129032723420536 ) ) ;
#35683=CARTESIAN_POINT ( 'NONE',  ( -5.000000000000005329, 40.20833332650536818, 8.660254037844387298 ) ) ;
#35690=ORIENTED_EDGE ( 'NONE', *, *, #1479, .F. ) ;
#35692=CARTESIAN_POINT ( 'NONE',  ( -2.594694132007996146, 225.9999999999999432, 9.679754673387174435 ) ) ;
#35695=CARTESIAN_POINT ( 'NONE',  ( 3.042071309553159519, 119.7395833299193413, 11.35316468750000141 ) ) ;
#35696=ORIENTED_EDGE ( 'NONE', *, *, #55182, .F. ) ;
#35703=CARTESIAN_POINT ( 'NONE',  ( -8.311093377946841443, 108.9062499965860127, 8.311093377946834337 ) ) ;
#35709=CARTESIAN_POINT ( 'NONE',  ( -10.00000000000000178, 199.3749999931720538, -1.224646799147353454E-15 ) ) ;
#35710=CARTESIAN_POINT ( 'NONE',  ( 0.000000000000000000, 300.0000000000000000, 0.000000000000000000 ) ) ;
#35713=CARTESIAN_POINT ( 'NONE',  ( -3.042071309553163960, 102.5520833299193697, -11.35316468749999963 ) ) ;
#35717=CARTESIAN_POINT ( 'NONE',  ( 5.676582343750001591, 6.927083329919350163, -9.832129032723420536 ) ) ;
#35721=CARTESIAN_POINT ( 'NONE',  ( 8.311093377946834337, 220.1562499965860127, 8.311093377946839666 ) ) ;
#35725=CARTESIAN_POINT ( 'NONE',  ( 2.765530957081996366, 292.1406250017070079, -6.676582343750003368 ) ) ;
#35726=EDGE_LOOP ( 'NONE', ( #51501, #46765, #10314, #2745 ) ) ;
#35728=CARTESIAN_POINT ( 'NONE',  ( 5.676582343749993598, 210.2604166632526699, 9.832129032723422313 ) ) ;
#35735=CARTESIAN_POINT ( 'NONE',  ( 2.679491924311228956, 26.04166666666666430, -10.00000000000000000 ) ) ;
#35736=ADVANCED_FACE ( 'NONE', ( #40591 ), #5758, .F. ) ;
#35741=LINE ( 'NONE', #12349, #69884 ) ;
#35742=( BOUNDED_SURFACE ( )  B_SPLINE_SURFACE ( 1, 2, ( 
 ( #45472, #16790, #35296, #598, #11157, #69988, #18296, #23211, #41312, #23581, #64320, #68488, #12624, #46591, #69612, #40194, #17928, #58310, #34181, #63196, #63952, #74523, #5500, #22831, #28500, #11526, #30356, #59404, #13716, #65788, #71070, #48063, #14466, #24679, #36025, #12987, #65419, #36760, #59773, #13351, #7719, #36389, #19388, #8448, #18668, #60130, #47689, #70711, #8082, #42401, #31083, #31468, #54492, #54113, #30722, #53743, #19029, #2423, #25418, #2054, #59042, #31841, #60503, #2797, #14092, #37505, #8830, #48432, #7349, #53377, #42036, #71435, #19765, #54860, #65042, #42772, #25042, #37127, #25785, #48804, #24319, #71813, #1701, #20131, #43146, #66163, #47330, #70357, #41679, #64688, #38631, #61633, #61254, #39363, #27665, #60876, #9586, #15220, #61999, #32984, #26160, #21627, #3171, #9951, #33348, #44651, #72189, #67292, #9199, #32603, #32220, #26920, #68034, #55238, #55985, #38251, #55612, #27286, #20883, #3544, #38994, #4295, #49178, #43904, #3929, #22001, #66915, #26535, #50670, #49560, #72578, #50303, #49935, #72948, #73324, #10322, #67667, #20501, #44281, #16327, #21256, #62360, #43516, #15965, #15592, #66530, #56349, #73689, #4668, #45027, #10690, #33724, #14840, #37881, #28780, #51797, #51419, #63110, #23490, #41224, #5409, #144, #11071, #18210, #34097, #52179, #23120, #62731, #17083, #46132, #46502, #69150, #5784, #46876, #57093, #68401, #45385, #17457, #40478, #63483, #45761, #40105, #68772, #11805, #40850, #51051, #17836, #28411, #74433, #34843, #57850, #6156, #63858 ),
 ( #64232, #28040, #22740, #29164, #35209, #511, #74062, #69522, #12173, #22361, #56726, #11436, #58226, #5044, #16699, #23866, #34473, #57478, #6525, #29532, #52542, #880, #39730, #69899, #12541, #13999, #64957, #36304, #59322, #41591, #71722, #66071, #47602, #7627, #1967, #13267, #30271, #7994, #58582, #35569, #36673, #42315, #2708, #53288, #1613, #47974, #12900, #54024, #58953, #31000, #25696, #54401, #6890, #29901, #47240, #35936, #42685, #52914, #18943, #2332, #25329, #30636, #53656, #24959, #48344, #70989, #20038, #1249, #64604, #19305, #37038, #71351, #24226, #19673, #59685, #70267, #18580, #24596, #65331, #7261, #65697, #60039, #13635, #41949, #8359, #70625, #31375, #48716, #43054, #20414, #26831, #67205, #32510, #61165, #4578, #38163, #50214, #73601, #49845, #32129, #44565, #10234, #67577, #73235, #37793, #61909, #72488, #21541, #33262, #56261, #15503, #15874, #43431, #9114, #38540, #72863, #49087, #21908, #21168, #66446, #8740, #9496, #55523, #3835, #60789, #31752, #3082, #20797, #44192, #55148, #61541, #3453, #27575, #26066, #44939, #14379, #26443, #49468, #60414, #9864, #43814, #66829, #50583, #54772, #32893, #55895, #15131, #72101, #37415, #4209, #38907, #27198, #14753, #29444, #23403, #40021, #63024, #62646, #74342, #34755, #52455, #16614, #11348, #22279, #793, #45301, #63390, #34383, #73974, #28324, #57383, #57759, #5693, #16994, #58135, #68316, #4955, #56640, #28692, #51705, #52, #57009, #51334, #5322, #23035, #52091, #62279, #29071, #39649, #10979, #46044, #69064, #17368 ) ),
 .UNSPECIFIED., .F., .F., .F. ) 
 B_SPLINE_SURFACE_WITH_KNOTS ( ( 2, 2 ),
 ( 3, 2, 2, 2, 2, 2, 2, 2, 2, 2, 2, 2, 2, 2, 2, 2, 2, 2, 2, 2, 2, 2, 2, 2, 2, 2, 2, 2, 2, 2, 2, 2, 2, 2, 2, 2, 2, 2, 2, 2, 2, 2, 2, 2, 2, 2, 2, 2, 2, 2, 2, 2, 2, 2, 2, 2, 2, 2, 2, 2, 2, 2, 2, 2, 2, 2, 2, 2, 2, 2, 2, 2, 2, 2, 2, 2, 2, 2, 2, 2, 2, 2, 2, 2, 2, 2, 2, 2, 2, 2, 2, 2, 2, 2, 2, 2, 3 ),
 ( 0.000000000000000000, 1.000000000000000000 ),
 ( 0.000000000000000000, 0.01041666666666666609, 0.02083333333333333218, 0.03125000000000000000, 0.04166666666666666435, 0.05208333333333333565, 0.06250000000000000000, 0.07291666666666667129, 0.08333333333333332871, 0.09375000000000000000, 0.1041666666666666713, 0.1145833333333333287, 0.1250000000000000000, 0.1354166666666666574, 0.1458333333333333426, 0.1562500000000000000, 0.1666666666666666574, 0.1770833333333333426, 0.1875000000000000000, 0.1979166666666666574, 0.2083333333333333426, 0.2187500000000000000, 0.2291666666666666574, 0.2395833333333333426, 0.2500000000000000000, 0.2604166666666666852, 0.2708333333333333148, 0.2812500000000000000, 0.2916666666666666852, 0.3020833333333333148, 0.3125000000000000000, 0.3229166666666666852, 0.3333333333333333148, 0.3437500000000000000, 0.3541666666666666852, 0.3645833333333333148, 0.3750000000000000000, 0.3854166666666666852, 0.3958333333333333148, 0.4062500000000000000, 0.4166666666666666852, 0.4270833333333333148, 0.4375000000000000000, 0.4479166666666666852, 0.4583333333333333148, 0.4687500000000000000, 0.4791666666666666852, 0.4895833333333333148, 0.5000000000000000000, 0.5104166666666666297, 0.5208333333333333703, 0.5312500000000000000, 0.5416666666666666297, 0.5520833333333333703, 0.5625000000000000000, 0.5729166666666666297, 0.5833333333333333703, 0.5937500000000000000, 0.6041666666666666297, 0.6145833333333333703, 0.6250000000000000000, 0.6354166666666666297, 0.6458333333333333703, 0.6562500000000000000, 0.6666666666666666297, 0.6770833333333333703, 0.6875000000000000000, 0.6979166666666666297, 0.7083333333333333703, 0.7187500000000000000, 0.7291666666666666297, 0.7395833333333333703, 0.7500000000000000000, 0.7604166666666666297, 0.7708333333333333703, 0.7812500000000000000, 0.7916666666666666297, 0.8020833333333333703, 0.8125000000000000000, 0.8229166666666666297, 0.8333333333333333703, 0.8437500000000000000, 0.8541666666666666297, 0.8645833333333333703, 0.8750000000000000000, 0.8854166666666666297, 0.8958333333333333703, 0.9062500000000000000, 0.9166666666666666297, 0.9270833333333333703, 0.9375000000000000000, 0.9479166666666666297, 0.9583333333333333703, 0.9687500000000000000, 0.9791666666666666297, 0.9895833333333333703, 1.000000000000000000 ),
 .UNSPECIFIED. ) 
 GEOMETRIC_REPRESENTATION_ITEM ( )  RATIONAL_B_SPLINE_SURFACE ( (
 ( 1.000000000000000000, 0.9238795325112867385, 1.000000000000000000, 0.9238795325112867385, 1.000000000000000000, 0.9238795325112867385, 1.000000000000000000, 0.9238795325112867385, 1.000000000000000000, 0.9238795325112867385, 1.000000000000000000, 0.9238795325112867385, 1.000000000000000000, 0.9238795325112867385, 1.000000000000000000, 0.9238795325112867385, 1.000000000000000000, 0.9238795325112867385, 1.000000000000000000, 0.9238795325112867385, 1.000000000000000000, 0.9238795325112867385, 1.000000000000000000, 0.9238795325112867385, 1.000000000000000000, 0.9238795325112867385, 1.000000000000000000, 0.9238795325112867385, 1.000000000000000000, 0.9238795325112867385, 1.000000000000000000, 0.9238795325112867385, 1.000000000000000000, 0.9238795325112867385, 1.000000000000000000, 0.9238795325112867385, 1.000000000000000000, 0.9238795325112867385, 1.000000000000000000, 0.9238795325112867385, 1.000000000000000000, 0.9238795325112867385, 1.000000000000000000, 0.9238795325112867385, 1.000000000000000000, 0.9238795325112867385, 1.000000000000000000, 0.9238795325112867385, 1.000000000000000000, 0.9238795325112867385, 1.000000000000000000, 0.9238795325112867385, 1.000000000000000000, 0.9238795325112867385, 1.000000000000000000, 0.9238795325112867385, 1.000000000000000000, 0.9238795325112867385, 1.000000000000000000, 0.9238795325112867385, 1.000000000000000000, 0.9238795325112867385, 1.000000000000000000, 0.9238795325112867385, 1.000000000000000000, 0.9238795325112867385, 1.000000000000000000, 0.9238795325112867385, 1.000000000000000000, 0.9238795325112867385, 1.000000000000000000, 0.9238795325112867385, 1.000000000000000000, 0.9238795325112867385, 1.000000000000000000, 0.9238795325112867385, 1.000000000000000000, 0.9238795325112867385, 1.000000000000000000, 0.9238795325112867385, 1.000000000000000000, 0.9238795325112867385, 1.000000000000000000, 0.9238795325112867385, 1.000000000000000000, 0.9238795325112867385, 1.000000000000000000, 0.9238795325112867385, 1.000000000000000000, 0.9238795325112867385, 1.000000000000000000, 0.9238795325112867385, 1.000000000000000000, 0.9238795325112867385, 1.000000000000000000, 0.9238795325112867385, 1.000000000000000000, 0.9238795325112867385, 1.000000000000000000, 0.9238795325112867385, 1.000000000000000000, 0.9238795325112867385, 1.000000000000000000, 0.9238795325112867385, 1.000000000000000000, 0.9238795325112867385, 1.000000000000000000, 0.9238795325112867385, 1.000000000000000000, 0.9238795325112867385, 1.000000000000000000, 0.9238795325112867385, 1.000000000000000000, 0.9238795325112867385, 1.000000000000000000, 0.9238795325112867385, 1.000000000000000000, 0.9238795325112867385, 1.000000000000000000, 0.9238795325112867385, 1.000000000000000000, 0.9238795325112867385, 1.000000000000000000, 0.9238795325112867385, 1.000000000000000000, 0.9238795325112867385, 1.000000000000000000, 0.9238795325112867385, 1.000000000000000000, 0.9238795325112867385, 1.000000000000000000, 0.9238795325112867385, 1.000000000000000000, 0.9238795325112867385, 1.000000000000000000, 0.9238795325112867385, 1.000000000000000000, 0.9238795325112867385, 1.000000000000000000, 0.9238795325112867385, 1.000000000000000000, 0.9238795325112867385, 1.000000000000000000, 0.9238795325112867385, 1.000000000000000000, 0.9238795325112867385, 1.000000000000000000, 0.9238795325112867385, 1.000000000000000000, 0.9238795325112867385, 1.000000000000000000, 0.9238795325112867385, 1.000000000000000000, 0.9238795325112867385, 1.000000000000000000, 0.9238795325112867385, 1.000000000000000000, 0.9238795325112867385, 1.000000000000000000, 0.9238795325112867385, 1.000000000000000000, 0.9238795325112867385, 1.000000000000000000, 0.9238795325112867385, 1.000000000000000000, 0.9238795325112867385, 1.000000000000000000, 0.9238795325112867385, 1.000000000000000000, 0.9238795325112867385, 1.000000000000000000, 0.9238795325112867385, 1.000000000000000000, 0.9238795325112867385, 1.000000000000000000, 0.9238795325112867385, 1.000000000000000000, 0.9238795325112867385, 1.000000000000000000, 0.9238795325112867385, 1.000000000000000000, 0.9238795325112867385, 1.000000000000000000, 0.9238795325112867385, 1.000000000000000000, 0.9238795325112867385, 1.000000000000000000, 0.9238795325112867385, 1.000000000000000000, 0.9238795325112867385, 1.000000000000000000, 0.9238795325112867385, 1.000000000000000000),
 ( 1.000000000000000000, 0.9238795325112867385, 1.000000000000000000, 0.9238795325112867385, 1.000000000000000000, 0.9238795325112867385, 1.000000000000000000, 0.9238795325112867385, 1.000000000000000000, 0.9238795325112867385, 1.000000000000000000, 0.9238795325112867385, 1.000000000000000000, 0.9238795325112867385, 1.000000000000000000, 0.9238795325112867385, 1.000000000000000000, 0.9238795325112867385, 1.000000000000000000, 0.9238795325112867385, 1.000000000000000000, 0.9238795325112867385, 1.000000000000000000, 0.9238795325112867385, 1.000000000000000000, 0.9238795325112867385, 1.000000000000000000, 0.9238795325112867385, 1.000000000000000000, 0.9238795325112867385, 1.000000000000000000, 0.9238795325112867385, 1.000000000000000000, 0.9238795325112867385, 1.000000000000000000, 0.9238795325112867385, 1.000000000000000000, 0.9238795325112867385, 1.000000000000000000, 0.9238795325112867385, 1.000000000000000000, 0.9238795325112867385, 1.000000000000000000, 0.9238795325112867385, 1.000000000000000000, 0.9238795325112867385, 1.000000000000000000, 0.9238795325112867385, 1.000000000000000000, 0.9238795325112867385, 1.000000000000000000, 0.9238795325112867385, 1.000000000000000000, 0.9238795325112867385, 1.000000000000000000, 0.9238795325112867385, 1.000000000000000000, 0.9238795325112867385, 1.000000000000000000, 0.9238795325112867385, 1.000000000000000000, 0.9238795325112867385, 1.000000000000000000, 0.9238795325112867385, 1.000000000000000000, 0.9238795325112867385, 1.000000000000000000, 0.9238795325112867385, 1.000000000000000000, 0.9238795325112867385, 1.000000000000000000, 0.9238795325112867385, 1.000000000000000000, 0.9238795325112867385, 1.000000000000000000, 0.9238795325112867385, 1.000000000000000000, 0.9238795325112867385, 1.000000000000000000, 0.9238795325112867385, 1.000000000000000000, 0.9238795325112867385, 1.000000000000000000, 0.9238795325112867385, 1.000000000000000000, 0.9238795325112867385, 1.000000000000000000, 0.9238795325112867385, 1.000000000000000000, 0.9238795325112867385, 1.000000000000000000, 0.9238795325112867385, 1.000000000000000000, 0.9238795325112867385, 1.000000000000000000, 0.9238795325112867385, 1.000000000000000000, 0.9238795325112867385, 1.000000000000000000, 0.9238795325112867385, 1.000000000000000000, 0.9238795325112867385, 1.000000000000000000, 0.9238795325112867385, 1.000000000000000000, 0.9238795325112867385, 1.000000000000000000, 0.9238795325112867385, 1.000000000000000000, 0.9238795325112867385, 1.000000000000000000, 0.9238795325112867385, 1.000000000000000000, 0.9238795325112867385, 1.000000000000000000, 0.9238795325112867385, 1.000000000000000000, 0.9238795325112867385, 1.000000000000000000, 0.9238795325112867385, 1.000000000000000000, 0.9238795325112867385, 1.000000000000000000, 0.9238795325112867385, 1.000000000000000000, 0.9238795325112867385, 1.000000000000000000, 0.9238795325112867385, 1.000000000000000000, 0.9238795325112867385, 1.000000000000000000, 0.9238795325112867385, 1.000000000000000000, 0.9238795325112867385, 1.000000000000000000, 0.9238795325112867385, 1.000000000000000000, 0.9238795325112867385, 1.000000000000000000, 0.9238795325112867385, 1.000000000000000000, 0.9238795325112867385, 1.000000000000000000, 0.9238795325112867385, 1.000000000000000000, 0.9238795325112867385, 1.000000000000000000, 0.9238795325112867385, 1.000000000000000000, 0.9238795325112867385, 1.000000000000000000, 0.9238795325112867385, 1.000000000000000000, 0.9238795325112867385, 1.000000000000000000, 0.9238795325112867385, 1.000000000000000000, 0.9238795325112867385, 1.000000000000000000, 0.9238795325112867385, 1.000000000000000000, 0.9238795325112867385, 1.000000000000000000, 0.9238795325112867385, 1.000000000000000000, 0.9238795325112867385, 1.000000000000000000, 0.9238795325112867385, 1.000000000000000000, 0.9238795325112867385, 1.000000000000000000, 0.9238795325112867385, 1.000000000000000000, 0.9238795325112867385, 1.000000000000000000, 0.9238795325112867385, 1.000000000000000000, 0.9238795325112867385, 1.000000000000000000, 0.9238795325112867385, 1.000000000000000000, 0.9238795325112867385, 1.000000000000000000, 0.9238795325112867385, 1.000000000000000000, 0.9238795325112867385, 1.000000000000000000, 0.9238795325112867385, 1.000000000000000000, 0.9238795325112867385, 1.000000000000000000, 0.9238795325112867385, 1.000000000000000000) ) ) 
 REPRESENTATION_ITEM ( '' )  SURFACE ( )  );
#35746=CARTESIAN_POINT ( 'NONE',  ( 6.676582343750002480, 298.0156250017069510, -2.765530957081997254 ) ) ;
#35758=CARTESIAN_POINT ( 'NONE',  ( -5.676582343749998039, 102.7604166632526841, -9.832129032723420536 ) ) ;
#35759=CARTESIAN_POINT ( 'NONE',  ( -9.999999999999996447, 122.2916666666666856, -2.679491924311229401 ) ) ;
#35766=CARTESIAN_POINT ( 'NONE',  ( -7.320508075688773708, 178.7499999931720254, -7.320508075688774596 ) ) ;
#35767=CARTESIAN_POINT ( 'NONE',  ( -11.35316468750000141, 213.4895833299193839, 3.042071309553159963 ) ) ;
#35773=CARTESIAN_POINT ( 'NONE',  ( -9.832129032723418760, 183.1770833299193555, -5.676582343750004256 ) ) ;
#35775=CARTESIAN_POINT ( 'NONE',  ( -2.485281374238947016, 295.8750000034140726, -5.999999999999626965 ) ) ;
#35780=CARTESIAN_POINT ( 'NONE',  ( -8.311093377946836114, 62.65624999658601268, -8.311093377946837890 ) ) ;
#35787=CARTESIAN_POINT ( 'NONE',  ( -8.311093377946841443, 78.90624999658602690, 8.311093377946830785 ) ) ;
#35792=CARTESIAN_POINT ( 'NONE',  ( 11.35316468749999963, 60.98958332991934839, -3.042071309553165293 ) ) ;
#35795=CARTESIAN_POINT ( 'NONE',  ( 5.000000000000001776, 157.7083333265053966, -8.660254037844389075 ) ) ;
#35798=CARTESIAN_POINT ( 'NONE',  ( 5.676582343749993598, 45.26041666325268409, 9.832129032723422313 ) ) ;
#35800=CARTESIAN_POINT ( 'NONE',  ( 5.676582343750001591, 191.6145833299193839, -9.832129032723420536 ) ) ;
#35806=CARTESIAN_POINT ( 'NONE',  ( 11.35316468749999963, 180.9895833299193555, -3.042071309553165293 ) ) ;
#35807=VECTOR ( 'NONE', #70364, 1000.000000000000000 ) ;
#35811=DIRECTION ( 'NONE',  ( 0.000000000000000000, 0.000000000000000000, 1.000000000000000000 ) ) ;
#35813=EDGE_CURVE ( 'NONE', #61945, #31223, #18713, .T. ) ;
#35814=CARTESIAN_POINT ( 'NONE',  ( -8.311093377946841443, 169.2187499965860127, 8.311093377946834337 ) ) ;
#35817=CARTESIAN_POINT ( 'NONE',  ( 8.482974764195253314, 225.9999999999999432, -6.716101469744629959 ) ) ;
#35831=EDGE_LOOP ( 'NONE', ( #20843, #15254, #29615, #18281 ) ) ;
#35845=CARTESIAN_POINT ( 'NONE',  ( 6.676582343750002480, 298.1718750017070079, -2.765530957081997254 ) ) ;
#35846=CARTESIAN_POINT ( 'NONE',  ( -7.320508075688773708, 136.8750000000000000, -7.320508075688774596 ) ) ;
#35862=CARTESIAN_POINT ( 'NONE',  ( -9.832129032723420536, 23.69791666325268409, 5.676582343749997150 ) ) ;
#35864=CARTESIAN_POINT ( 'NONE',  ( 11.35316468749999785, 220.8854166632526699, 3.042071309553174174 ) ) ;
#35870=CARTESIAN_POINT ( 'NONE',  ( 11.35316468749999785, 30.57291666325268409, 3.042071309553174174 ) ) ;
#35874=CARTESIAN_POINT ( 'NONE',  ( -5.999999999999999112, 295.1250000034140157, 2.485281374238575314 ) ) ;
#35877=CARTESIAN_POINT ( 'NONE',  ( 9.832129032723420536, 21.19791666325268409, -5.676582343749999815 ) ) ;
#35879=CARTESIAN_POINT ( 'NONE',  ( 6.951808397369818766E-16, 147.0312499965860411, -11.35316468750000141 ) ) ;
#35880=AXIS2_PLACEMENT_3D ( 'NONE', #22018, #28796, #45399 ) ;
#35881=CARTESIAN_POINT ( 'NONE',  ( 8.660254037844385522, 111.4583333265053682, 5.000000000000005329 ) ) ;
#35883=FACE_OUTER_BOUND ( 'NONE', #15253, .T. ) ;
#35887=CARTESIAN_POINT ( 'NONE',  ( -5.676582343750006032, 9.427083329919350163, 9.832129032723418760 ) ) ;
#35888=ORIENTED_EDGE ( 'NONE', *, *, #30252, .F. ) ;
#35889=CARTESIAN_POINT ( 'NONE',  ( 0.000000000000000000, 300.0000000000000000, 0.000000000000000000 ) ) ;
#35890=CARTESIAN_POINT ( 'NONE',  ( -6.676582343750001591, 298.4531250017069510, 0.000000000000000000 ) ) ;
#35892=CARTESIAN_POINT ( 'NONE',  ( 8.311093377946834337, 140.1562499965860127, 8.311093377946839666 ) ) ;
#35902=CARTESIAN_POINT ( 'NONE',  ( -3.042071309553164404, 92.55208332991934128, -11.35316468749999963 ) ) ;
#35917=VECTOR ( 'NONE', #34029, 1000.000000000000000 ) ;
#35927=ORIENTED_EDGE ( 'NONE', *, *, #23020, .F. ) ;
#35934=CARTESIAN_POINT ( 'NONE',  ( 10.00000000000000178, 90.00000000000001421, 0.000000000000000000 ) ) ;
#35936=CARTESIAN_POINT ( 'NONE',  ( 6.676582343750003368, 296.1718750017069510, -2.765530957081997254 ) ) ;
#35946=CARTESIAN_POINT ( 'NONE',  ( -10.00000000000000355, 212.7083333333333144, 2.679491924311223183 ) ) ;
#35949=CARTESIAN_POINT ( 'NONE',  ( 9.832129032723420536, 186.5104166632526983, -5.676582343749999815 ) ) ;
#35955=CARTESIAN_POINT ( 'NONE',  ( -8.311093377946841443, 44.21874999658602690, 8.311093377946830785 ) ) ;
#35957=CARTESIAN_POINT ( 'NONE',  ( -5.676582343749998039, 217.7604166632526983, -9.832129032723420536 ) ) ;
#35961=CYLINDRICAL_SURFACE ( 'NONE', #53502, 6.000000000000001776 ) ;
#35963=ADVANCED_FACE ( 'NONE', ( #65087 ), #36436, .T. ) ;
#35966=CARTESIAN_POINT ( 'NONE',  ( 10.00000000000000178, 71.87499999317203958, 0.000000000000000000 ) ) ;
#35969=CARTESIAN_POINT ( 'NONE',  ( -10.00000000000000888, 72.70833333333332860, 2.679491924311224516 ) ) ;
#35975=CARTESIAN_POINT ( 'NONE',  ( 2.765530957082001251, 295.9218750017070079, 6.676582343750000703 ) ) ;
#35976=CARTESIAN_POINT ( 'NONE',  ( -2.679491924311238282, 143.5416666666667140, 10.00000000000001243 ) ) ;
#35977=CARTESIAN_POINT ( 'NONE',  ( -10.00000000000000888, 17.29166666666666430, -2.679491924311232953 ) ) ;
#35978=CARTESIAN_POINT ( 'NONE',  ( 11.35316468750000141, 160.7812499965860127, 0.000000000000000000 ) ) ;
#35980=CARTESIAN_POINT ( 'NONE',  ( 1.881637226502129035E-11, 6.249999999998538058, -10.00000000000000178 ) ) ;
#35989=CARTESIAN_POINT ( 'NONE',  ( 11.35316468749999785, 140.8854166632526699, 3.042071309553174174 ) ) ;
#35993=CARTESIAN_POINT ( 'NONE',  ( -5.676582343750006032, 49.42708332991935549, 9.832129032723418760 ) ) ;
#35994=ORIENTED_EDGE ( 'NONE', *, *, #31273, .F. ) ;
#35999=CARTESIAN_POINT ( 'NONE',  ( -6.000000000000000888, 293.1250000034141294, 2.485281374238575758 ) ) ;
#36005=CARTESIAN_POINT ( 'NONE',  ( -7.320508075688778149, 64.99999999317203958, 7.320508075688769267 ) ) ;
#36016=ORIENTED_EDGE ( 'NONE', *, *, #33346, .F. ) ;
#36020=CARTESIAN_POINT ( 'NONE',  ( 0.000000000000000000, 255.9999999999999432, 0.000000000000000000 ) ) ;
#36022=CARTESIAN_POINT ( 'NONE',  ( 8.660254037844385522, 49.58333333333333570, 5.000000000000005329 ) ) ;
#36025=CARTESIAN_POINT ( 'NONE',  ( -4.242640687119286547, 297.8750000000000000, -4.242640687119286547 ) ) ;
#36026=CARTESIAN_POINT ( 'NONE',  ( 1.102182119232618108E-15, 288.3125000034140157, 6.000000000000001776 ) ) ;
#36037=CARTESIAN_POINT ( 'NONE',  ( 10.00000000000000178, 180.2083333333333144, -2.679491924311226736 ) ) ;
#36041=CARTESIAN_POINT ( 'NONE',  ( -9.832129032723420536, 144.0104166632526699, 5.676582343749997150 ) ) ;
#36043=CARTESIAN_POINT ( 'NONE',  ( 2.250000000000000000, 284.0000000000000000, 7.677076266392047543 ) ) ;
#36053=CARTESIAN_POINT ( 'NONE',  ( -10.00000000000000178, 29.37499999317203248, -1.224646799147353454E-15 ) ) ;
#36060=VERTEX_POINT ( 'NONE', #44696 ) ;
#36062=DIRECTION ( 'NONE',  ( 1.000000000000000000, 0.000000000000000000, 0.000000000000000000 ) ) ;
#36064=CARTESIAN_POINT ( 'NONE',  ( -5.676582343749998039, 117.4479166632526841, -9.832129032723420536 ) ) ;
#36066=ADVANCED_FACE ( 'NONE', ( #43949 ), #32649, .T. ) ;
#36072=CARTESIAN_POINT ( 'NONE',  ( -11.35316468749999785, 113.0729166632526841, -3.042071309553167957 ) ) ;
#36074=ORIENTED_EDGE ( 'NONE', *, *, #56687, .T. ) ;
#36077=CARTESIAN_POINT ( 'NONE',  ( 8.660254037844389075, 207.2916666598387110, -5.000000000000000000 ) ) ;
#36080=CARTESIAN_POINT ( 'NONE',  ( 3.042071309553167513, 97.13541666325268409, -11.35316468749999785 ) ) ;
#36084=CARTESIAN_POINT ( 'NONE',  ( 9.832129032723420536, 11.51041666325268409, -5.676582343749999815 ) ) ;
#36086=CARTESIAN_POINT ( 'NONE',  ( 3.178432602446558121E-13, 136.2499999999999716, -10.00000000000000533 ) ) ;
#36091=DIRECTION ( 'NONE',  ( -0.000000000000000000, 1.000000000000000000, -0.000000000000000000 ) ) ;
#36093=CARTESIAN_POINT ( 'NONE',  ( 2.765530957082001251, 294.7656250017070079, 6.676582343750000703 ) ) ;
#36096=CARTESIAN_POINT ( 'NONE',  ( -5.676582343750006032, 224.4270833299193555, 9.832129032723418760 ) ) ;
#36112=CARTESIAN_POINT ( 'NONE',  ( -1.377000000000000002, 278.5679999999998699, 5.673913216228727130 ) ) ;
#36113=CARTESIAN_POINT ( 'NONE',  ( -6.676582343750002480, 292.3906250017069510, -2.765530957081996810 ) ) ;
#36117=ORIENTED_EDGE ( 'NONE', *, *, #71796, .F. ) ;
#36119=AXIS2_PLACEMENT_3D ( 'NONE', #68013, #32963, #16306 ) ;
#36122=EDGE_LOOP ( 'NONE', ( #38321, #61239, #33301, #67914 ) ) ;
#36124=CARTESIAN_POINT ( 'NONE',  ( 5.676582343749993598, 105.2604166632526841, 9.832129032723422313 ) ) ;
#36125=CARTESIAN_POINT ( 'NONE',  ( -5.000000000000004441, 123.3333333333333712, 8.660254037844383745 ) ) ;
#36130=VERTEX_POINT ( 'NONE', #44325 ) ;
#36135=CARTESIAN_POINT ( 'NONE',  ( 9.832129032723420536, 216.1979166632526983, -5.676582343749999815 ) ) ;
#36139=CARTESIAN_POINT ( 'NONE',  ( 11.35316468749999785, 185.8854166632526983, 3.042071309553174174 ) ) ;
#36146=CARTESIAN_POINT ( 'NONE',  ( 3.042071309553167069, 66.82291666325266988, -11.35316468749999785 ) ) ;
#36150=CARTESIAN_POINT ( 'NONE',  ( -5.000000000000011546, 46.66666666666668561, -8.660254037844410391 ) ) ;
#36152=CARTESIAN_POINT ( 'NONE',  ( -5.676582343749998039, 72.44791666325268409, -9.832129032723420536 ) ) ;
#36158=CARTESIAN_POINT ( 'NONE',  ( -5.676582343750006032, 69.11458332991936970, 9.832129032723418760 ) ) ;
#36160=CARTESIAN_POINT ( 'NONE',  ( 10.00000000000000000, 130.2083333333333428, -2.679491924311226736 ) ) ;
#36161=CARTESIAN_POINT ( 'NONE',  ( -10.00000000000000000, 154.1666666598387394, -2.679491924311229845 ) ) ;
#36164=CARTESIAN_POINT ( 'NONE',  ( 11.35316468750000141, 61.09374999658602690, 0.000000000000000000 ) ) ;
#36166=CARTESIAN_POINT ( 'NONE',  ( 5.676582343749993598, 199.9479166632526983, 9.832129032723422313 ) ) ;
#36172=CARTESIAN_POINT ( 'NONE',  ( 3.042071309553167513, 186.8229166632526983, -11.35316468749999785 ) ) ;
#36178=CARTESIAN_POINT ( 'NONE',  ( 6.951808397369818766E-16, 167.3437499965860127, -11.35316468750000141 ) ) ;
#36182=( BOUNDED_CURVE ( )  B_SPLINE_CURVE ( 2, ( #35607, #58622, #6928, #71025, #52954, #47278, #70304, #64641, #12939, #19343, #47643, #35976, #30306 ),
 .UNSPECIFIED., .F., .F. ) 
 B_SPLINE_CURVE_WITH_KNOTS ( ( 3, 2, 2, 2, 2, 2, 3 ),
 ( 1.774089285059882615, 1.779322971663514608, 1.784556658267146823, 1.789790344870778815, 1.795024031474410808, 1.800257718078043023, 1.805491404681675016 ),
 .UNSPECIFIED. ) 
 CURVE ( )  GEOMETRIC_REPRESENTATION_ITEM ( )  RATIONAL_B_SPLINE_CURVE ( ( 0.9999999999999978906, 0.9659258262890704216, 1.000000000000000000, 0.9659258262890683122, 1.000000000000000000, 0.9659258262890683122, 1.000000000000000000, 0.9659258262890683122, 1.000000000000000000, 0.9659258262890683122, 1.000000000000000000, 0.9659258262890683122, 1.000000000000000000 ) ) 
 REPRESENTATION_ITEM ( '' )  );
#36183=CARTESIAN_POINT ( 'NONE',  ( 5.202883259092580204, 225.9999999999999432, -8.895588268986850622 ) ) ;
#36195=ORIENTED_EDGE ( 'NONE', *, *, #38576, .T. ) ;
#36198=CARTESIAN_POINT ( 'NONE',  ( 8.660254037844435260, 180.4166666666666856, -5.000000000000026645 ) ) ;
#36211=CARTESIAN_POINT ( 'NONE',  ( -6.676582343750002480, 294.5468750017069510, -2.765530957081996810 ) ) ;
#36212=CARTESIAN_POINT ( 'NONE',  ( -2.679491924311235618, 138.5416666666666572, 10.00000000000000000 ) ) ;
#36215=EDGE_CURVE ( 'NONE', #15967, #4343, #34139, .T. ) ;
#36229=CARTESIAN_POINT ( 'NONE',  ( 11.35316468749999963, 30.98958332991935194, -3.042071309553165293 ) ) ;
#36232=CARTESIAN_POINT ( 'NONE',  ( 8.311093377946837890, 216.7187499965860411, -8.311093377946837890 ) ) ;
#36238=CARTESIAN_POINT ( 'NONE',  ( -5.676582343749998039, 32.44791666325268409, -9.832129032723420536 ) ) ;
#36245=CARTESIAN_POINT ( 'NONE',  ( -11.35316468750000141, 38.28124999658601979, -1.390361679473963753E-15 ) ) ;
#36247=CARTESIAN_POINT ( 'NONE',  ( 8.311093377946834337, 145.1562499965860127, 8.311093377946839666 ) ) ;
#36249=CARTESIAN_POINT ( 'NONE',  ( -8.660254037844387298, 118.9583333265053824, -5.000000000000004441 ) ) ;
#36253=ORIENTED_EDGE ( 'NONE', *, *, #54530, .T. ) ;
#36254=CARTESIAN_POINT ( 'NONE',  ( -5.676582343749998039, 22.76041666325268409, -9.832129032723420536 ) ) ;
#36260=CARTESIAN_POINT ( 'NONE',  ( -11.35316468749999785, 133.0729166632526983, -3.042071309553167957 ) ) ;
#36269=CARTESIAN_POINT ( 'NONE',  ( -2.085542519210945728E-15, 84.84374999658601268, 11.35316468750000141 ) ) ;
#36287=CARTESIAN_POINT ( 'NONE',  ( -1.836970198721029983E-15, 123.7500000000000142, 10.00000000000000178 ) ) ;
#36291=CARTESIAN_POINT ( 'NONE',  ( 10.00000000000000178, 121.8749999931720396, 0.000000000000000000 ) ) ;
#36297=CARTESIAN_POINT ( 'NONE',  ( -9.999999999999989342, 97.50000000000000000, -1.224646799147351876E-15 ) ) ;
#36302=CARTESIAN_POINT ( 'NONE',  ( -5.000000000000005329, 93.33333333333334281, 8.660254037844387298 ) ) ;
#36304=CARTESIAN_POINT ( 'NONE',  ( 2.765530957082001251, 297.9218750017069510, 6.676582343750000703 ) ) ;
#36310=CARTESIAN_POINT ( 'NONE',  ( -10.00000000000000711, 52.70833333333334281, 2.679491924311223627 ) ) ;
#36315=CARTESIAN_POINT ( 'NONE',  ( 8.660254037844389075, 210.4166666666666572, -5.000000000000000000 ) ) ;
#36316=EDGE_CURVE ( 'NONE', #16317, #61723, #36738, .T. ) ;
#36318=CARTESIAN_POINT ( 'NONE',  ( -11.35316468750000141, 183.5937499965860411, -1.390361679473963753E-15 ) ) ;
#36326=CARTESIAN_POINT ( 'NONE',  ( -5.676582343749998039, 52.76041666325269119, -9.832129032723420536 ) ) ;
#36328=CARTESIAN_POINT ( 'NONE',  ( -2.085542519210945728E-15, 224.8437499965860127, 11.35316468750000141 ) ) ;
#36332=CARTESIAN_POINT ( 'NONE',  ( -10.00000000000000178, 59.37499999317203248, -1.224646799147353454E-15 ) ) ;
#36334=CARTESIAN_POINT ( 'NONE',  ( -5.676582343750006032, 114.1145833299193555, 9.832129032723418760 ) ) ;
#36335=CARTESIAN_POINT ( 'NONE',  ( -2.679491924311225848, 78.33333332650536818, -10.00000000000000178 ) ) ;
#36341=ORIENTED_EDGE ( 'NONE', *, *, #29069, .F. ) ;
#36342=CARTESIAN_POINT ( 'NONE',  ( 1.226468279477575784E-15, 291.8593750017070079, 6.676582343750001591 ) ) ;
#36344=CARTESIAN_POINT ( 'NONE',  ( 11.35316468750000141, 155.7812499965860127, 0.000000000000000000 ) ) ;
#36353=CARTESIAN_POINT ( 'NONE',  ( 11.35316468749999963, 136.3020833299193555, -3.042071309553165293 ) ) ;
#36357=CARTESIAN_POINT ( 'NONE',  ( 9.832129032723416984, 55.67708332991935549, 5.676582343750006032 ) ) ;
#36363=CARTESIAN_POINT ( 'NONE',  ( 6.000000000000003553, 292.6250000034140157, -2.485281374238571761 ) ) ;
#36364=DIRECTION ( 'NONE',  ( 0.000000000000000000, 0.000000000000000000, 1.000000000000000000 ) ) ;
#36375=ADVANCED_FACE ( 'NONE', ( #30309 ), #2375, .T. ) ;
#36385=CARTESIAN_POINT ( 'NONE',  ( 1.102182119232618108E-15, 296.2500000000000000, 6.000000000000001776 ) ) ;
#36387=CARTESIAN_POINT ( 'NONE',  ( -7.320508075688773708, 51.87499999999999289, -7.320508075688774596 ) ) ;
#36389=CARTESIAN_POINT ( 'NONE',  ( 6.000000000000003553, 297.4374999999999432, 2.485281374238571317 ) ) ;
#36396=CARTESIAN_POINT ( 'NONE',  ( 9.999999999999985789, 90.20833333333331439, -2.679491924311223183 ) ) ;
#36400=FACE_OUTER_BOUND ( 'NONE', #6243, .T. ) ;
#36402=CARTESIAN_POINT ( 'NONE',  ( -10.00000000000000178, 172.5000000000000284, -1.224646799147353454E-15 ) ) ;
#36406=CARTESIAN_POINT ( 'NONE',  ( 6.951808397369818766E-16, 142.3437499965860411, -11.35316468750000141 ) ) ;
#36413=CARTESIAN_POINT ( 'NONE',  ( -11.35316468750000141, 13.80208332991934661, 3.042071309553159963 ) ) ;
#36415=CARTESIAN_POINT ( 'NONE',  ( -2.679491924294440608, 111.4583333333318222, -10.00000000000968470 ) ) ;
#36420=CARTESIAN_POINT ( 'NONE',  ( 5.000000000000001776, 37.70833332650536818, -8.660254037844389075 ) ) ;
#36426=CARTESIAN_POINT ( 'NONE',  ( 10.00000000000000000, 6.666666659838699438, 2.679491924311235618 ) ) ;
#36427=ORIENTED_EDGE ( 'NONE', *, *, #56751, .F. ) ;
#36431=AXIS2_PLACEMENT_3D ( 'NONE', #55843, #38110, #61110 ) ;
#36432=CARTESIAN_POINT ( 'NONE',  ( 11.35316468749999785, 110.5729166632526983, 3.042071309553174174 ) ) ;
#36436=CYLINDRICAL_SURFACE ( 'NONE', #64632, 10.00000000000000178 ) ;
#36440=CARTESIAN_POINT ( 'NONE',  ( -9.832129032723418760, 117.8645833299193697, -5.676582343750004256 ) ) ;
#36445=CARTESIAN_POINT ( 'NONE',  ( 7.320508075688771044, 211.2499999931719969, 7.320508075688775484 ) ) ;
#36446=CYLINDRICAL_SURFACE ( 'NONE', #8162, 6.000000000000001776 ) ;
#36448=CARTESIAN_POINT ( 'NONE',  ( 5.676582343749993598, 100.2604166632526841, 9.832129032723422313 ) ) ;
#36452=CARTESIAN_POINT ( 'NONE',  ( 5.676582343750001591, 11.92708332991935016, -9.832129032723420536 ) ) ;
#36460=CARTESIAN_POINT ( 'NONE',  ( -2.765530957081996810, 294.2656250017069510, -6.676582343750003368 ) ) ;
#36477=CARTESIAN_POINT ( 'NONE',  ( -7.320508075688773708, 28.74999999317203248, -7.320508075688774596 ) ) ;
#36481=CARTESIAN_POINT ( 'NONE',  ( 0.4589999999999999636, 272.8559999999997672, 5.793770692573254166 ) ) ;
#36482=CARTESIAN_POINT ( 'NONE',  ( -6.676582343750002480, 294.3906250017070079, -2.765530957081996810 ) ) ;
#36493=CARTESIAN_POINT ( 'NONE',  ( 8.311093377946834337, 95.46874999658601268, 8.311093377946839666 ) ) ;
#36494=CARTESIAN_POINT ( 'NONE',  ( -4.999999999999997335, 121.6666666666666856, -8.660254037844385522 ) ) ;
#36502=ADVANCED_FACE ( 'NONE', ( #35611 ), #58267, .T. ) ;
#36503=CARTESIAN_POINT ( 'NONE',  ( 6.951808397369818766E-16, 212.0312499965860411, -11.35316468750000141 ) ) ;
#36504=( BOUNDED_CURVE ( )  B_SPLINE_CURVE ( 2, ( #8701, #54737, #9457, #44155, #67170, #15465, #38503, #6322, #11969, #5946, #28569, #24392, #30062 ),
 .UNSPECIFIED., .F., .F. ) 
 B_SPLINE_CURVE_WITH_KNOTS ( ( 3, 2, 2, 2, 2, 2, 3 ),
 ( 0.5054347826086956763, 0.5072463768115942351, 0.5090579710144927938, 0.5108695652173913526, 0.5126811594202898004, 0.5144927536231883591, 0.5163043478260869179 ),
 .UNSPECIFIED. ) 
 CURVE ( )  GEOMETRIC_REPRESENTATION_ITEM ( )  RATIONAL_B_SPLINE_CURVE ( ( 1.000000000000000000, 0.9659258262890683122, 1.000000000000000000, 0.9659258262890683122, 1.000000000000000000, 0.9659258262890683122, 1.000000000000000000, 0.9659258262890683122, 1.000000000000000000, 0.9659258262890683122, 1.000000000000000000, 0.9659258262890683122, 1.000000000000000000 ) ) 
 REPRESENTATION_ITEM ( '' )  );
#36509=CARTESIAN_POINT ( 'NONE',  ( 3.042071309553159519, 190.0520833299193839, 11.35316468750000141 ) ) ;
#36511=LINE ( 'NONE', #24439, #54071 ) ;
#36516=CARTESIAN_POINT ( 'NONE',  ( 3.042071309553159519, 79.73958332991934128, 11.35316468750000141 ) ) ;
#36520=CARTESIAN_POINT ( 'NONE',  ( -2.679491924310542394, 48.54166666666674246, 10.00000000000043165 ) ) ;
#36522=CARTESIAN_POINT ( 'NONE',  ( 5.676582343750001591, 76.61458332991935549, -9.832129032723420536 ) ) ;
#36529=CARTESIAN_POINT ( 'NONE',  ( 11.35316468750000141, 75.78124999658602690, 0.000000000000000000 ) ) ;
#36532=CARTESIAN_POINT ( 'NONE',  ( 4.999999999999993783, 166.0416666598387110, 8.660254037844390851 ) ) ;
#36535=CARTESIAN_POINT ( 'NONE',  ( 5.676582343749993598, 55.26041666325268409, 9.832129032723422313 ) ) ;
#36537=CARTESIAN_POINT ( 'NONE',  ( 3.042071309553167069, 191.8229166632526415, -11.35316468749999785 ) ) ;
#36543=CARTESIAN_POINT ( 'NONE',  ( -9.832129032723420536, 198.6979166632526983, 5.676582343749997150 ) ) ;
#36544=CYLINDRICAL_SURFACE ( 'NONE', #14031, 10.00000000000000178 ) ;
#36548=CARTESIAN_POINT ( 'NONE',  ( 5.676582343749993598, 180.2604166632526699, 9.832129032723422313 ) ) ;
#36550=CARTESIAN_POINT ( 'NONE',  ( 9.371230106042952812, 225.9999999999998863, -5.731621267630282013 ) ) ;
#36559=EDGE_CURVE ( 'NONE', #55260, #48752, #16015, .T. ) ;
#36573=CARTESIAN_POINT ( 'NONE',  ( -1.836970198721029983E-15, 115.6249999931720396, 10.00000000000000178 ) ) ;
#36577=CARTESIAN_POINT ( 'NONE',  ( -2.765530957081998142, 295.7968750017070647, 6.676582343750000703 ) ) ;
#36578=CARTESIAN_POINT ( 'NONE',  ( -5.000000000000005329, 148.3333333333333428, 8.660254037844387298 ) ) ;
#36582=EDGE_CURVE ( 'NONE', #58121, #36130, #14045, .T. ) ;
#36588=DIRECTION ( 'NONE',  ( -0.000000000000000000, 1.000000000000000000, -0.000000000000000000 ) ) ;
#36597=CARTESIAN_POINT ( 'NONE',  ( -9.832129032723418760, 27.86458332991935194, -5.676582343750004256 ) ) ;
#36599=CARTESIAN_POINT ( 'NONE',  ( 6.123233995736767268E-16, 3.124999993172032919, -10.00000000000000178 ) ) ;
#36600=FACE_OUTER_BOUND ( 'NONE', #63128, .T. ) ;
#36601=CARTESIAN_POINT ( 'NONE',  ( 0.000000000000000000, 300.0000000000000000, 6.000000000000001776 ) ) ;
#36605=CARTESIAN_POINT ( 'NONE',  ( -8.311093377946841443, 33.90624999658601979, 8.311093377946830785 ) ) ;
#36611=CARTESIAN_POINT ( 'NONE',  ( 11.35316468750000141, 30.78124999658601979, 0.000000000000000000 ) ) ;
#36613=CARTESIAN_POINT ( 'NONE',  ( -3.042071309553164404, 142.2395833299193839, -11.35316468749999963 ) ) ;
#36614=CARTESIAN_POINT ( 'NONE',  ( -7.320508075688778149, 124.9999999931720538, 7.320508075688769267 ) ) ;
#36617=CARTESIAN_POINT ( 'NONE',  ( 0.000000000000000000, 300.0000000000000000, 10.00000000000000178 ) ) ;
#36622=CARTESIAN_POINT ( 'NONE',  ( -11.35316468750000141, 18.59374999658601979, -1.390361679473963753E-15 ) ) ;
#36624=ORIENTED_EDGE ( 'NONE', *, *, #27468, .F. ) ;
#36628=CARTESIAN_POINT ( 'NONE',  ( -11.35316468750000141, 153.2812499965860127, -1.390361679473963753E-15 ) ) ;
#36635=CARTESIAN_POINT ( 'NONE',  ( 7.320508075688777261, 120.6250000000000284, -7.320508075688777261 ) ) ;
#36637=CARTESIAN_POINT ( 'NONE',  ( -2.085542519210945728E-15, 99.84374999658601268, 11.35316468750000141 ) ) ;
#36671=CARTESIAN_POINT ( 'NONE',  ( 7.320508075688771044, 89.37499999999998579, 7.320508075688775484 ) ) ;
#36673=CARTESIAN_POINT ( 'NONE',  ( 6.676582343750001591, 297.1093750017069510, -8.176455196517173205E-16 ) ) ;
#36674=VERTEX_POINT ( 'NONE', #20084 ) ;
#36675=CARTESIAN_POINT ( 'NONE',  ( 10.00000000000004263, 190.2083333333333428, -2.679491924311237394 ) ) ;
#36683=CARTESIAN_POINT ( 'NONE',  ( -2.679491924311225848, 216.4583333333333144, -10.00000000000000178 ) ) ;
#36686=CARTESIAN_POINT ( 'NONE',  ( 11.35316468750000141, 196.0937499965860127, 0.000000000000000000 ) ) ;
#36694=CARTESIAN_POINT ( 'NONE',  ( -3.042071309553164404, 47.55208332991935549, -11.35316468749999963 ) ) ;
#36696=CARTESIAN_POINT ( 'NONE',  ( -5.676582343750006032, 224.4270833299193555, 9.832129032723418760 ) ) ;
#36702=CARTESIAN_POINT ( 'NONE',  ( -3.042071309553164404, 102.2395833299193697, -11.35316468749999963 ) ) ;
#36703=CARTESIAN_POINT ( 'NONE',  ( -8.660254037844387298, 78.95833332650536818, -5.000000000000004441 ) ) ;
#36710=CARTESIAN_POINT ( 'NONE',  ( -4.088227598258586603E-16, 294.3593750017070079, -6.676582343750001591 ) ) ;
#36712=CARTESIAN_POINT ( 'NONE',  ( 6.951808397369818766E-16, 172.0312499965860411, -11.35316468750000141 ) ) ;
#36715=CARTESIAN_POINT ( 'NONE',  ( -8.660254037844424602, 192.0833333333333428, -5.000000000000025757 ) ) ;
#36721=CARTESIAN_POINT ( 'NONE',  ( 11.35316468749999785, 135.8854166632526699, 3.042071309553174174 ) ) ;
#36723=CARTESIAN_POINT ( 'NONE',  ( 4.242640687119285658, 298.6875000034139589, -4.242640687119286547 ) ) ;
#36725=CARTESIAN_POINT ( 'NONE',  ( -3.042071309553173730, 64.63541666325269830, 11.35316468749999785 ) ) ;
#36733=CARTESIAN_POINT ( 'NONE',  ( 6.000000000000003553, 290.6250000034140157, -2.485281374238571761 ) ) ;
#36738=( BOUNDED_CURVE ( )  B_SPLINE_CURVE ( 2, ( #48015, #19345, #12211, #13308, #41634, #53697, #7303 ),
 .UNSPECIFIED., .F., .F. ) 
 B_SPLINE_CURVE_WITH_KNOTS ( ( 3, 2, 2, 3 ),
 ( 0.000000000000000000, 0.001811594202898550747, 0.003623188405797101493, 0.005434782608695652023 ),
 .UNSPECIFIED. ) 
 CURVE ( )  GEOMETRIC_REPRESENTATION_ITEM ( )  RATIONAL_B_SPLINE_CURVE ( ( 1.000000000000000000, 0.9659258262890683122, 1.000000000000000000, 0.9659258262890683122, 1.000000000000000000, 0.9659258262890683122, 1.000000000000000000 ) ) 
 REPRESENTATION_ITEM ( '' )  );
#36749=CARTESIAN_POINT ( 'NONE',  ( 1.102182119232618108E-15, 295.2500000000000000, 6.000000000000001776 ) ) ;
#36758=CARTESIAN_POINT ( 'NONE',  ( -5.000000000000005329, 58.33333333333333570, 8.660254037844387298 ) ) ;
#36760=CARTESIAN_POINT ( 'NONE',  ( 2.485281374238571317, 297.6875000000000000, -6.000000000000003553 ) ) ;
#36762=LINE ( 'NONE', #55613, #16512 ) ;
#36771=CARTESIAN_POINT ( 'NONE',  ( -10.00000000000000000, 172.2916666666666288, -2.679491924311229845 ) ) ;
#36772=CARTESIAN_POINT ( 'NONE',  ( 1.102182119232618108E-15, 297.3125000034140157, 6.000000000000001776 ) ) ;
#36775=CARTESIAN_POINT ( 'NONE',  ( -8.311093377946836114, 147.9687499965860411, -8.311093377946837890 ) ) ;
#36779=CARTESIAN_POINT ( 'NONE',  ( 10.00000000000000000, 106.6666666598387252, 2.679491924311235618 ) ) ;
#36782=CARTESIAN_POINT ( 'NONE',  ( -11.35316468750000141, 13.59374999658601801, -1.390361679473963753E-15 ) ) ;
#36788=CARTESIAN_POINT ( 'NONE',  ( 6.123233995736767268E-16, 38.12499999317203958, -10.00000000000000178 ) ) ;
#36793=CARTESIAN_POINT ( 'NONE',  ( 6.000000000000003553, 291.6250000034140157, -2.485281374238571761 ) ) ;
#36796=CARTESIAN_POINT ( 'NONE',  ( -5.711993833409989278E-12, 133.7499999999995737, 9.999999999999998224 ) ) ;
#36797=CARTESIAN_POINT ( 'NONE',  ( -5.000000000000031086, 63.33333333333336412, 8.660254037844431707 ) ) ;
#36799=CARTESIAN_POINT ( 'NONE',  ( -11.35316468750000141, 128.4895833299193555, 3.042071309553159963 ) ) ;
#36805=CARTESIAN_POINT ( 'NONE',  ( 0.000000000000000000, 300.0000000000000000, 0.000000000000000000 ) ) ;
#36807=CARTESIAN_POINT ( 'NONE',  ( 5.676582343750001591, 111.6145833299193555, -9.832129032723420536 ) ) ;
#36811=CARTESIAN_POINT ( 'NONE',  ( 2.679491924311228956, 212.9166666598386826, -10.00000000000000000 ) ) ;
#36814=CARTESIAN_POINT ( 'NONE',  ( 11.35316468749999963, 101.3020833299193555, -3.042071309553165293 ) ) ;
#36818=CARTESIAN_POINT ( 'NONE',  ( 8.311093377946834337, 15.46874999658601624, 8.311093377946839666 ) ) ;
#36822=CARTESIAN_POINT ( 'NONE',  ( 4.999999999999993783, 116.0416666598387110, 8.660254037844390851 ) ) ;
#36825=CARTESIAN_POINT ( 'NONE',  ( -10.00000000000000000, 149.1666666598387110, -2.679491924311229845 ) ) ;
#36826=CARTESIAN_POINT ( 'NONE',  ( 4.721056650416000089, 290.8281250017069510, 4.721056650415999201 ) ) ;
#36828=CARTESIAN_POINT ( 'NONE',  ( 10.00000000000000178, 126.8749999931720396, 0.000000000000000000 ) ) ;
#36831=CARTESIAN_POINT ( 'NONE',  ( -8.311093377946841443, 129.2187499965860127, 8.311093377946830785 ) ) ;
#36834=( BOUNDED_CURVE ( )  B_SPLINE_CURVE ( 2, ( #47246, #1620, #70273, #70631, #18950, #41954, #13271, #36310, #59327, #7636, #30642, #42320, #65338 ),
 .UNSPECIFIED., .F., .F. ) 
 B_SPLINE_CURVE_WITH_KNOTS ( ( 3, 2, 2, 2, 2, 2, 3 ),
 ( 0.6436908981619412495, 0.6489249083846719834, 0.6541589186074028284, 0.6593929288301335623, 0.6646269390528642962, 0.6698609492755951411, 0.6750949594983258750 ),
 .UNSPECIFIED. ) 
 CURVE ( )  GEOMETRIC_REPRESENTATION_ITEM ( )  RATIONAL_B_SPLINE_CURVE ( ( 1.000000000000161871, 0.9659258262889065527, 1.000000000000000000, 0.9659258262890684232, 1.000000000000000000, 0.9659258262890684232, 1.000000000000000000, 0.9659258262890684232, 1.000000000000000000, 0.9659258262890684232, 1.000000000000000000, 0.9659258262890819680, 0.9999999999999864553 ) ) 
 REPRESENTATION_ITEM ( '' )  );
#36849=CARTESIAN_POINT ( 'NONE',  ( -10.00000000000000000, 29.16666665983869677, -2.679491924311229845 ) ) ;
#36852=CARTESIAN_POINT ( 'NONE',  ( 2.765530957082001251, 293.7656250017069510, 6.676582343749999815 ) ) ;
#36861=CARTESIAN_POINT ( 'NONE',  ( -6.000000000000001776, 299.0625000034140157, 0.000000000000000000 ) ) ;
#36863=CARTESIAN_POINT ( 'NONE',  ( 6.951808397369818766E-16, 107.3437499965860269, -11.35316468750000141 ) ) ;
#36871=CARTESIAN_POINT ( 'NONE',  ( -9.832129032723420536, 218.6979166632526983, 5.676582343749997150 ) ) ;
#36876=CARTESIAN_POINT ( 'NONE',  ( 6.951808397369818766E-16, 192.3437499965860127, -11.35316468750000141 ) ) ;
#36883=CARTESIAN_POINT ( 'NONE',  ( 9.832129032723416984, 75.36458332991935549, 5.676582343750006032 ) ) ;
#36886=DIRECTION ( 'NONE',  ( 0.000000000000000000, 0.000000000000000000, 1.000000000000000000 ) ) ;
#36887=CARTESIAN_POINT ( 'NONE',  ( 11.35316468750000141, 70.78124999658602690, 0.000000000000000000 ) ) ;
#36894=CARTESIAN_POINT ( 'NONE',  ( -11.35316468749999785, 73.07291666325266988, -3.042071309553167957 ) ) ;
#36900=CARTESIAN_POINT ( 'NONE',  ( 6.123233995736767268E-16, 168.1249999931720538, -10.00000000000000178 ) ) ;
#36903=CARTESIAN_POINT ( 'NONE',  ( -3.042071309553173730, 64.63541666325268409, 11.35316468749999785 ) ) ;
#36905=CARTESIAN_POINT ( 'NONE',  ( 11.35316468749999963, 195.9895833299193555, -3.042071309553165293 ) ) ;
#36911=CARTESIAN_POINT ( 'NONE',  ( -2.085542519210945728E-15, 189.5312499965860127, 11.35316468750000141 ) ) ;
#36912=CARTESIAN_POINT ( 'NONE',  ( -10.00000000000000000, 194.1666666598387110, -2.679491924311229845 ) ) ;
#36913=ADVANCED_FACE ( 'NONE', ( #15919 ), #57805, .T. ) ;
#36916=ORIENTED_EDGE ( 'NONE', *, *, #66420, .T. ) ;
#36917=CARTESIAN_POINT ( 'NONE',  ( 9.832129032723416984, 175.6770833299193555, 5.676582343750006032 ) ) ;
#36920=ORIENTED_EDGE ( 'NONE', *, *, #51862, .T. ) ;
#36942=CARTESIAN_POINT ( 'NONE',  ( -8.311093377946836114, 57.96874999658602690, -8.311093377946837890 ) ) ;
#36947=CARTESIAN_POINT ( 'NONE',  ( -4.721056650415998313, 292.7343750017069510, 4.721056650416000089 ) ) ;
#36948=CARTESIAN_POINT ( 'NONE',  ( 4.999999999999993783, 154.1666666666666856, 8.660254037844390851 ) ) ;
#36949=CARTESIAN_POINT ( 'NONE',  ( -5.000000000000005329, 165.2083333265053682, 8.660254037844387298 ) ) ;
#36957=CARTESIAN_POINT ( 'NONE',  ( -10.00000000000000355, 19.58333332650536462, 2.679491924311223183 ) ) ;
#36959=CARTESIAN_POINT ( 'NONE',  ( 7.320508075688774596, 134.3750000000000000, 7.320508075688778149 ) ) ;
#36960=CARTESIAN_POINT ( 'NONE',  ( 4.242640687119285658, 288.6875000034139589, -4.242640687119286547 ) ) ;
#36963=CARTESIAN_POINT ( 'NONE',  ( -2.085542519210945728E-15, 39.53124999658601268, 11.35316468750000141 ) ) ;
#36965=CARTESIAN_POINT ( 'NONE',  ( 2.679491924311228956, 12.91666665983869677, -10.00000000000000000 ) ) ;
#36968=AXIS2_PLACEMENT_3D ( 'NONE', #15311, #32323, #44005 ) ;
#36972=CARTESIAN_POINT ( 'NONE',  ( -5.676582343750006032, 39.11458332991934839, 9.832129032723418760 ) ) ;
#36974=CARTESIAN_POINT ( 'NONE',  ( 5.676582343750001591, 61.61458332991934839, -9.832129032723420536 ) ) ;
#36976=CARTESIAN_POINT ( 'NONE',  ( 6.123233995736767268E-16, 33.12499999317203248, -10.00000000000000178 ) ) ;
#36979=CARTESIAN_POINT ( 'NONE',  ( -9.832129032723420536, 38.69791666325268409, 5.676582343749997150 ) ) ;
#36981=CARTESIAN_POINT ( 'NONE',  ( 9.832129032723416984, 165.3645833299193555, 5.676582343750006032 ) ) ;
#36983=CARTESIAN_POINT ( 'NONE',  ( 2.679491924311222739, 130.8333333265053398, 10.00000000000000355 ) ) ;
#36987=CARTESIAN_POINT ( 'NONE',  ( -3.042071309553163960, 17.55208332991935194, -11.35316468749999963 ) ) ;
#36988=ORIENTED_EDGE ( 'NONE', *, *, #58759, .F. ) ;
#36991=CARTESIAN_POINT ( 'NONE',  ( 11.35316468750000141, 155.7812499965860127, 0.000000000000000000 ) ) ;
#37004=CARTESIAN_POINT ( 'NONE',  ( 11.35316468749999963, 101.3020833299193555, -3.042071309553165293 ) ) ;
#37006=CARTESIAN_POINT ( 'NONE',  ( -1.903569318090136080E-11, 13.74999999999851852, 10.00000000000000178 ) ) ;
#37028=( BOUNDED_CURVE ( )  B_SPLINE_CURVE ( 2, ( #71220, #8981, #65569, #31996, #14622 ),
 .UNSPECIFIED., .F., .F. ) 
 B_SPLINE_CURVE_WITH_KNOTS ( ( 3, 2, 3 ),
 ( 0.9791666666666651864, 0.9895833333333325932, 1.000000000000000000 ),
 .UNSPECIFIED. ) 
 CURVE ( )  GEOMETRIC_REPRESENTATION_ITEM ( )  RATIONAL_B_SPLINE_CURVE ( ( 1.000000000000010436, 0.9238795325112761914, 1.000000000000000000, 0.9238795325112867385, 1.000000000000000000 ) ) 
 REPRESENTATION_ITEM ( '' )  );
#37035=CARTESIAN_POINT ( 'NONE',  ( -8.660254037844383745, 32.08333333333333570, -5.000000000000002665 ) ) ;
#37036=CARTESIAN_POINT ( 'NONE',  ( 2.679491924311222739, 113.9583333333333428, 10.00000000000000355 ) ) ;
#37038=CARTESIAN_POINT ( 'NONE',  ( 4.721056650415999201, 295.2343750017069510, -4.721056650415999201 ) ) ;
#37040=AXIS2_PLACEMENT_3D ( 'NONE', #72119, #54041, #65714 ) ;
#37041=CARTESIAN_POINT ( 'NONE',  ( -2.679491924311373729, 143.3333333265053966, -9.999999999999916511 ) ) ;
#37048=CARTESIAN_POINT ( 'NONE',  ( -3.042071309553164404, 7.239583329919349275, -11.35316468749999963 ) ) ;
#37049=( BOUNDED_CURVE ( )  B_SPLINE_CURVE ( 2, ( #4041, #27034, #14205, #43258, #67404, #50045, #60617, #15705, #61746 ),
 .UNSPECIFIED., .F., .F. ) 
 B_SPLINE_CURVE_WITH_KNOTS ( ( 3, 2, 2, 2, 3 ),
 ( 0.9374999999999984457, 0.9479166666666650753, 0.9583333333333319271, 0.9687499999999985567, 0.9791666666666651864 ),
 .UNSPECIFIED. ) 
 CURVE ( )  GEOMETRIC_REPRESENTATION_ITEM ( )  RATIONAL_B_SPLINE_CURVE ( ( 1.000000000000011324, 0.9238795325112754142, 1.000000000000000000, 0.9238795325112867385, 1.000000000000000000, 0.9238795325112867385, 1.000000000000000000, 0.9238795325112972856, 0.9999999999999894529 ) ) 
 REPRESENTATION_ITEM ( '' )  );
#37051=CARTESIAN_POINT ( 'NONE',  ( -9.832129032723420536, 199.0104166632526983, 5.676582343749997150 ) ) ;
#37060=CARTESIAN_POINT ( 'NONE',  ( -11.35316468749999785, 48.38541666325268409, -3.042071309553167513 ) ) ;
#37064=LINE ( 'NONE', #67234, #55077 ) ;
#37068=CARTESIAN_POINT ( 'NONE',  ( 6.951808397369818766E-16, 107.0312499965860269, -11.35316468750000141 ) ) ;
#37069=CARTESIAN_POINT ( 'NONE',  ( -5.000000000000005329, 90.20833332650536818, 8.660254037844387298 ) ) ;
#37072=CARTESIAN_POINT ( 'NONE',  ( -5.000000000000000888, 71.66666666666667140, -8.660254037844390851 ) ) ;
#37077=CARTESIAN_POINT ( 'NONE',  ( -6.676582343750001591, 294.6093750017069510, 0.000000000000000000 ) ) ;
#37078=CARTESIAN_POINT ( 'NONE',  ( 8.660254037844389075, 187.2916666598387110, -5.000000000000000000 ) ) ;
#37080=CARTESIAN_POINT ( 'NONE',  ( -9.832129032723420536, 173.6979166632526983, 5.676582343749997150 ) ) ;
#37081=DIRECTION ( 'NONE',  ( -0.000000000000000000, 1.000000000000000000, -0.000000000000000000 ) ) ;
#37090=CARTESIAN_POINT ( 'NONE',  ( 11.35316468749999963, 146.3020833299193555, -3.042071309553165293 ) ) ;
#37093=CARTESIAN_POINT ( 'NONE',  ( -11.35316468750000141, 68.80208332991935549, 3.042071309553159963 ) ) ;
#37100=CARTESIAN_POINT ( 'NONE',  ( 4.242640687119287435, 289.4375000034140157, 4.242640687119285658 ) ) ;
#37116=CARTESIAN_POINT ( 'NONE',  ( -2.485281374238208052, 295.1875000000000568, 6.000000000000366818 ) ) ;
#37121=CARTESIAN_POINT ( 'NONE',  ( -8.660254037844383745, 2.083333333333331261, -5.000000000000001776 ) ) ;
#37125=CARTESIAN_POINT ( 'NONE',  ( -8.660254037844390851, 72.91666666666667140, 4.999999999999998224 ) ) ;
#37127=CARTESIAN_POINT ( 'NONE',  ( -2.485281374238572649, 295.1875000000000000, 6.000000000000002665 ) ) ;
#37138=CARTESIAN_POINT ( 'NONE',  ( 10.00000000000000000, 179.7916666666666856, 2.679491924311236062 ) ) ;
#37140=CARTESIAN_POINT ( 'NONE',  ( -9.832129032723418760, 148.1770833299193555, -5.676582343750004256 ) ) ;
#37142=CYLINDRICAL_SURFACE ( 'NONE', #19263, 10.00000000000000178 ) ;
#37145=CARTESIAN_POINT ( 'NONE',  ( -10.00000000000000533, 167.5000000000000000, -1.224646799147353848E-15 ) ) ;
#37146=EDGE_LOOP ( 'NONE', ( #69280, #16880, #6667, #13825 ) ) ;
#37147=CARTESIAN_POINT ( 'NONE',  ( 3.042071309553159519, 5.052083329919351051, 11.35316468750000141 ) ) ;
#37156=CARTESIAN_POINT ( 'NONE',  ( -5.000000000000005329, 45.20833332650536818, 8.660254037844387298 ) ) ;
#37166=DIRECTION ( 'NONE',  ( -0.000000000000000000, 1.000000000000000000, -0.000000000000000000 ) ) ;
#37168=CARTESIAN_POINT ( 'NONE',  ( 11.35316468750000141, 125.7812499965860127, 0.000000000000000000 ) ) ;
#37174=DIRECTION ( 'NONE',  ( 0.000000000000000000, 0.000000000000000000, 1.000000000000000000 ) ) ;
#37175=CARTESIAN_POINT ( 'NONE',  ( 1.901548650871797615E-12, 218.7500000000001990, 10.00000000000000533 ) ) ;
#37176=CARTESIAN_POINT ( 'NONE',  ( -3.042071309553173730, 119.3229166632526557, 11.35316468749999785 ) ) ;
#37178=CARTESIAN_POINT ( 'NONE',  ( 2.679491924322640273, 51.04166666666564112, -9.999999999993418598 ) ) ;
#37184=CARTESIAN_POINT ( 'NONE',  ( -11.35316468749999785, 108.3854166632526841, -3.042071309553167957 ) ) ;
#37188=CARTESIAN_POINT ( 'NONE',  ( -5.676582343749998039, 27.76041666325268409, -9.832129032723420536 ) ) ;
#37192=CARTESIAN_POINT ( 'NONE',  ( 5.000000000000001776, 117.7083333265053824, -8.660254037844389075 ) ) ;
#37194=CARTESIAN_POINT ( 'NONE',  ( 0.000000000000000000, 300.0000000000000000, 0.000000000000000000 ) ) ;
#37196=CARTESIAN_POINT ( 'NONE',  ( -6.676582343750001591, 292.4531250017069510, 0.000000000000000000 ) ) ;
#37198=CARTESIAN_POINT ( 'NONE',  ( -11.35316468749999785, 218.3854166632526415, -3.042071309553167957 ) ) ;
#37199=CARTESIAN_POINT ( 'NONE',  ( 5.676582343750001591, 141.9270833299193555, -9.832129032723420536 ) ) ;
#37201=EDGE_CURVE ( 'NONE', #413, #34861, #16443, .T. ) ;
#37210=AXIS2_PLACEMENT_3D ( 'NONE', #21827, #11642, #16158 ) ;
#37217=CARTESIAN_POINT ( 'NONE',  ( -10.00000000000000355, 29.58333332650536818, 2.679491924311223183 ) ) ;
#37218=CARTESIAN_POINT ( 'NONE',  ( -3.042071309553164404, 182.2395833299193555, -11.35316468749999963 ) ) ;
#37220=CARTESIAN_POINT ( 'NONE',  ( -0.4590000000000000746, 267.1439999999997212, 5.793770692572753234 ) ) ;
#37221=CARTESIAN_POINT ( 'NONE',  ( 1.226468279477575784E-15, 292.7031250017069510, 6.676582343750001591 ) ) ;
#37234=CARTESIAN_POINT ( 'NONE',  ( -9.832129032723420536, 119.0104166632526841, 5.676582343749997150 ) ) ;
#37235=CARTESIAN_POINT ( 'NONE',  ( 7.320508075688771044, 211.2499999931719969, 7.320508075688775484 ) ) ;
#37239=DIRECTION ( 'NONE',  ( 0.000000000000000000, 0.000000000000000000, 1.000000000000000000 ) ) ;
#37243=CARTESIAN_POINT ( 'NONE',  ( 9.832129032723416984, 220.3645833299193839, 5.676582343750006032 ) ) ;
#37248=CARTESIAN_POINT ( 'NONE',  ( -8.311093377946841443, 189.2187499965860411, 8.311093377946830785 ) ) ;
#37256=CARTESIAN_POINT ( 'NONE',  ( 8.311093377946837890, 86.40624999658601268, -8.311093377946837890 ) ) ;
#37263=CARTESIAN_POINT ( 'NONE',  ( -11.35316468750000141, 83.28124999658602690, -1.390361679473963753E-15 ) ) ;
#37271=CARTESIAN_POINT ( 'NONE',  ( -5.676582343750006032, 74.11458332991935549, 9.832129032723418760 ) ) ;
#37274=CARTESIAN_POINT ( 'NONE',  ( -10.00000000000000000, 164.1666666598387110, -2.679491924311229845 ) ) ;
#37276=DIRECTION ( 'NONE',  ( 0.000000000000000000, 0.000000000000000000, 1.000000000000000000 ) ) ;
#37277=CARTESIAN_POINT ( 'NONE',  ( -8.311093377946836114, 57.96874999658601979, -8.311093377946837890 ) ) ;
#37278=CARTESIAN_POINT ( 'NONE',  ( 2.765530957081996366, 294.1406250017069510, -6.676582343750003368 ) ) ;
#37281=CARTESIAN_POINT ( 'NONE',  ( 3.042071309553167069, 211.8229166632527267, -11.35316468749999785 ) ) ;
#37287=CARTESIAN_POINT ( 'NONE',  ( -8.311093377946836114, 197.6562499965860411, -8.311093377946837890 ) ) ;
#37292=CARTESIAN_POINT ( 'NONE',  ( 5.676582343750001591, 186.9270833299193555, -9.832129032723420536 ) ) ;
#37297=CARTESIAN_POINT ( 'NONE',  ( -8.660254037844387298, 7.083333333333333925, -5.000000000000004441 ) ) ;
#37298=AXIS2_PLACEMENT_3D ( 'NONE', #14856, #61648, #43920 ) ;
#37306=CARTESIAN_POINT ( 'NONE',  ( -8.660254037844490327, 82.91666666666674246, 5.000000000000055955 ) ) ;
#37317=CARTESIAN_POINT ( 'NONE',  ( 6.951808397369818766E-16, 72.34374999658602690, -11.35316468750000141 ) ) ;
#37322=CARTESIAN_POINT ( 'NONE',  ( -2.765530957081996810, 293.4218750017070079, -6.676582343750002480 ) ) ;
#37323=CARTESIAN_POINT ( 'NONE',  ( 4.999999999999993783, 149.1666666666666572, 8.660254037844390851 ) ) ;
#37335=CARTESIAN_POINT ( 'NONE',  ( 8.660254037844390851, 135.4166666666667140, -5.000000000000001776 ) ) ;
#37339=CARTESIAN_POINT ( 'NONE',  ( -5.676582343750006032, 39.11458332991934839, 9.832129032723418760 ) ) ;
#37341=CARTESIAN_POINT ( 'NONE',  ( -8.660254037844390851, 4.791666659838699438, 4.999999999999998224 ) ) ;
#37343=CARTESIAN_POINT ( 'NONE',  ( -2.679491924311226292, 128.3333333265053682, -10.00000000000000178 ) ) ;
#37345=CARTESIAN_POINT ( 'NONE',  ( 5.676582343750001591, 51.61458332991934839, -9.832129032723420536 ) ) ;
#37351=CARTESIAN_POINT ( 'NONE',  ( -8.311093377946841443, 28.90624999658601624, 8.311093377946834337 ) ) ;
#37353=CARTESIAN_POINT ( 'NONE',  ( 9.832129032723416984, 160.3645833299193839, 5.676582343750006032 ) ) ;
#37355=CARTESIAN_POINT ( 'NONE',  ( -4.999999999999998224, 133.5416666598387110, -8.660254037844389075 ) ) ;
#37359=CARTESIAN_POINT ( 'NONE',  ( -11.35316468750000141, 23.59374999658601979, -1.390361679473963753E-15 ) ) ;
#37360=LINE ( 'NONE', #3404, #46109 ) ;
#37362=DIRECTION ( 'NONE',  ( 0.000000000000000000, 0.000000000000000000, 1.000000000000000000 ) ) ;
#37366=CARTESIAN_POINT ( 'NONE',  ( -3.042071309553173730, 149.3229166632526699, 11.35316468749999785 ) ) ;
#37375=CARTESIAN_POINT ( 'NONE',  ( -5.676582343750006032, 109.4270833299193555, 9.832129032723418760 ) ) ;
#37410=CARTESIAN_POINT ( 'NONE',  ( 8.660254037844389075, 105.4166666666666714, -5.000000000000000000 ) ) ;
#37415=CARTESIAN_POINT ( 'NONE',  ( -4.088227598258586603E-16, 290.3593750017070079, -6.676582343750001591 ) ) ;
#37418=DIRECTION ( 'NONE',  ( 0.000000000000000000, 0.000000000000000000, 1.000000000000000000 ) ) ;
#37421=LINE ( 'NONE', #26074, #9286 ) ;
#37426=CARTESIAN_POINT ( 'NONE',  ( -5.676582343749998039, 2.447916663252683200, -9.832129032723420536 ) ) ;
#37428=CARTESIAN_POINT ( 'NONE',  ( -5.676582343750006032, 199.4270833299193555, 9.832129032723418760 ) ) ;
#37433=CARTESIAN_POINT ( 'NONE',  ( 1.102182119232618108E-15, 297.2500000000000000, 6.000000000000001776 ) ) ;
#37441=CARTESIAN_POINT ( 'NONE',  ( -10.00000000000000000, 59.16666665983869677, -2.679491924311229845 ) ) ;
#37444=CARTESIAN_POINT ( 'NONE',  ( -11.35316468750000141, 123.2812499965860269, -1.390361679473963753E-15 ) ) ;
#37445=CARTESIAN_POINT ( 'NONE',  ( 7.320508075688771044, 91.24999999317205379, 7.320508075688775484 ) ) ;
#37448=CARTESIAN_POINT ( 'NONE',  ( -7.320508075688778149, 199.9999999931720254, 7.320508075688769267 ) ) ;
#37449=CARTESIAN_POINT ( 'NONE',  ( 0.000000000000000000, 300.0000000000000000, 0.000000000000000000 ) ) ;
#37453=CARTESIAN_POINT ( 'NONE',  ( -6.676582343750000703, 293.6718750017070079, 2.765530957082001251 ) ) ;
#37456=CARTESIAN_POINT ( 'NONE',  ( -3.042071309553173730, 169.3229166632526699, 11.35316468749999785 ) ) ;
#37461=ORIENTED_EDGE ( 'NONE', *, *, #38615, .T. ) ;
#37462=CARTESIAN_POINT ( 'NONE',  ( -5.676582343749998039, 152.7604166632526983, -9.832129032723420536 ) ) ;
#37466=CARTESIAN_POINT ( 'NONE',  ( 8.311093377946837890, 61.71874999658601979, -8.311093377946837890 ) ) ;
#37471=ORIENTED_EDGE ( 'NONE', *, *, #8997, .T. ) ;
#37474=CARTESIAN_POINT ( 'NONE',  ( -6.000000000000001776, 288.0625000034140157, 0.000000000000000000 ) ) ;
#37484=CIRCLE ( 'NONE', #68833, 10.00000000000000178 ) ;
#37486=EDGE_CURVE ( 'NONE', #42303, #48426, #54159, .T. ) ;
#37494=LINE ( 'NONE', #32595, #71049 ) ;
#37501=CARTESIAN_POINT ( 'NONE',  ( 7.320508075688774596, 70.62500000000000000, -7.320508075688774596 ) ) ;
#37503=EDGE_CURVE ( 'NONE', #53794, #36060, #70868, .T. ) ;
#37505=CARTESIAN_POINT ( 'NONE',  ( -6.000000000000003553, 295.9374999999999432, -2.485281374238571317 ) ) ;
#37517=CARTESIAN_POINT ( 'NONE',  ( 2.679491924311222739, 183.9583333333333428, 10.00000000000000355 ) ) ;
#37520=CARTESIAN_POINT ( 'NONE',  ( 8.311093377946834337, 150.4687499965860127, 8.311093377946839666 ) ) ;
#37526=CARTESIAN_POINT ( 'NONE',  ( 8.311093377946837890, 6.718749996586016238, -8.311093377946837890 ) ) ;
#37529=CARTESIAN_POINT ( 'NONE',  ( 8.660254037844389075, 32.29166665983870388, -5.000000000000000000 ) ) ;
#37530=DIRECTION ( 'NONE',  ( -0.000000000000000000, 1.000000000000000000, -0.000000000000000000 ) ) ;
#37532=CARTESIAN_POINT ( 'NONE',  ( 7.320508075688774596, 42.49999999317203248, -7.320508075688774596 ) ) ;
#37536=CARTESIAN_POINT ( 'NONE',  ( 1.901548650871797615E-12, 218.7500000000001990, 10.00000000000000533 ) ) ;
#37545=CARTESIAN_POINT ( 'NONE',  ( -9.832129032723420536, 133.6979166632526983, 5.676582343749997150 ) ) ;
#37553=CARTESIAN_POINT ( 'NONE',  ( -5.676582343750006032, 124.1145833299193555, 9.832129032723418760 ) ) ;
#37560=CARTESIAN_POINT ( 'NONE',  ( 9.832129032723416984, 115.6770833299193555, 5.676582343750006032 ) ) ;
#37564=CARTESIAN_POINT ( 'NONE',  ( -11.35316468749999785, 23.38541666325268054, -3.042071309553167513 ) ) ;
#37572=CARTESIAN_POINT ( 'NONE',  ( -6.676582343750000703, 288.5156250017069510, 2.765530957082001251 ) ) ;
#37574=CARTESIAN_POINT ( 'NONE',  ( -11.35316468750000141, 218.5937499965860411, -1.390361679473963753E-15 ) ) ;
#37576=CARTESIAN_POINT ( 'NONE',  ( 9.832129032723416984, 145.6770833299193555, 5.676582343750006032 ) ) ;
#37581=ORIENTED_EDGE ( 'NONE', *, *, #39922, .T. ) ;
#37587=VERTEX_POINT ( 'NONE', #52417 ) ;
#37591=CARTESIAN_POINT ( 'NONE',  ( 0.000000000000000000, 300.0000000000000000, 0.000000000000000000 ) ) ;
#37592=CARTESIAN_POINT ( 'NONE',  ( 9.832129032723420536, 181.1979166632526983, -5.676582343749999815 ) ) ;
#37594=DIRECTION ( 'NONE',  ( -0.000000000000000000, 1.000000000000000000, -0.000000000000000000 ) ) ;
#37595=CARTESIAN_POINT ( 'NONE',  ( 6.676582343750002480, 292.0156250017069510, -2.765530957081997254 ) ) ;
#37597=CARTESIAN_POINT ( 'NONE',  ( 2.966170491840901068E-11, 66.24999999999768363, -9.999999999999998224 ) ) ;
#37603=CARTESIAN_POINT ( 'NONE',  ( 2.679491924311228956, 167.9166666598387110, -10.00000000000000000 ) ) ;
#37606=FACE_OUTER_BOUND ( 'NONE', #27843, .T. ) ;
#37609=CARTESIAN_POINT ( 'NONE',  ( -2.085542519210945728E-15, 109.8437499965860269, 11.35316468750000141 ) ) ;
#37610=CARTESIAN_POINT ( 'NONE',  ( 1.224646799147353454E-15, 300.0000000000000000, -10.00000000000000178 ) ) ;
#37625=CARTESIAN_POINT ( 'NONE',  ( 9.832129032723420536, 196.5104166632526983, -5.676582343749999815 ) ) ;
#37627=CARTESIAN_POINT ( 'NONE',  ( 11.16751265488280787, 226.0000000000000000, 1.778318385449065842 ) ) ;
#37632=CARTESIAN_POINT ( 'NONE',  ( -11.35316468749999785, 78.07291666325269830, -3.042071309553167513 ) ) ;
#37635=CARTESIAN_POINT ( 'NONE',  ( -3.166186134455097228E-13, 141.2500000000000284, -9.999999999999998224 ) ) ;
#37640=CARTESIAN_POINT ( 'NONE',  ( -8.311093377946836114, 82.65624999658602690, -8.311093377946837890 ) ) ;
#37644=DIRECTION ( 'NONE',  ( -0.000000000000000000, 1.000000000000000000, -0.000000000000000000 ) ) ;
#37648=CARTESIAN_POINT ( 'NONE',  ( -5.676582343749998039, 92.44791666325269830, -9.832129032723420536 ) ) ;
#37650=CARTESIAN_POINT ( 'NONE',  ( -10.00000000000000355, 169.5833333265053398, 2.679491924311223183 ) ) ;
#37653=CARTESIAN_POINT ( 'NONE',  ( 6.951808397369818766E-16, 62.34374999658602690, -11.35316468750000141 ) ) ;
#37654=CARTESIAN_POINT ( 'NONE',  ( -4.721056650415998313, 293.5781250017069510, 4.721056650416000089 ) ) ;
#37655=ADVANCED_FACE ( 'NONE', ( #58822 ), #69764, .T. ) ;
#37657=CARTESIAN_POINT ( 'NONE',  ( -2.085542519210945728E-15, 204.5312499965860411, 11.35316468750000141 ) ) ;
#37663=CARTESIAN_POINT ( 'NONE',  ( -11.35316468750000141, 198.2812499965860411, -1.390361679473963753E-15 ) ) ;
#37668=CARTESIAN_POINT ( 'NONE',  ( 3.042071309553167513, 187.1354166632526983, -11.35316468749999785 ) ) ;
#37672=ORIENTED_EDGE ( 'NONE', *, *, #537, .F. ) ;
#37677=CARTESIAN_POINT ( 'NONE',  ( -10.00000000000000355, 2.708333333333333481, 2.679491924311223183 ) ) ;
#37696=CARTESIAN_POINT ( 'NONE',  ( -5.676582343750006032, 74.42708332991934128, 9.832129032723418760 ) ) ;
#37699=CARTESIAN_POINT ( 'NONE',  ( 0.000000000000000000, 300.0000000000000000, 0.000000000000000000 ) ) ;
#37701=CARTESIAN_POINT ( 'NONE',  ( -2.765530957081998142, 294.7968750017070079, 6.676582343750000703 ) ) ;
#37703=CARTESIAN_POINT ( 'NONE',  ( -10.00000000000000355, 164.5833333265053682, 2.679491924311223183 ) ) ;
#37713=CARTESIAN_POINT ( 'NONE',  ( 1.567784982238203817E-13, 113.7500000000000284, 10.00000000000000533 ) ) ;
#37715=CARTESIAN_POINT ( 'NONE',  ( 6.000000000000003553, 288.5000000034140157, 2.485281374238571317 ) ) ;
#37718=CARTESIAN_POINT ( 'NONE',  ( 9.832129032723416984, 45.36458332991935549, 5.676582343750006032 ) ) ;
#37722=CARTESIAN_POINT ( 'NONE',  ( -1.836970198721029983E-15, 10.62499999317203425, 10.00000000000000178 ) ) ;
#37726=CARTESIAN_POINT ( 'NONE',  ( 3.042071309553159519, 54.73958332991934839, 11.35316468750000141 ) ) ;
#37732=CARTESIAN_POINT ( 'NONE',  ( -9.832129032723418760, 27.86458332991935194, -5.676582343750004256 ) ) ;
#37735=CARTESIAN_POINT ( 'NONE',  ( -3.042071309553164404, 162.2395833299193271, -11.35316468749999963 ) ) ;
#37736=CARTESIAN_POINT ( 'NONE',  ( 8.660254037844385522, 126.4583333265053540, 5.000000000000005329 ) ) ;
#37739=CARTESIAN_POINT ( 'NONE',  ( 8.660254037844389075, 22.29166665983870033, -5.000000000000000000 ) ) ;
#37740=CARTESIAN_POINT ( 'NONE',  ( 9.832129032723416984, 25.67708332991935194, 5.676582343750006032 ) ) ;
#37741=CARTESIAN_POINT ( 'NONE',  ( -2.679491924317311202, 18.54166666666612073, 9.999999999996500577 ) ) ;
#37747=CARTESIAN_POINT ( 'NONE',  ( -5.676582343749998039, 147.4479166632526983, -9.832129032723420536 ) ) ;
#37755=CARTESIAN_POINT ( 'NONE',  ( 6.123233995736767268E-16, 208.1249999931720538, -10.00000000000000178 ) ) ;
#37758=CARTESIAN_POINT ( 'NONE',  ( 11.35316468749999785, 100.8854166632526841, 3.042071309553174174 ) ) ;
#37760=CARTESIAN_POINT ( 'NONE',  ( 7.320508075688779925, 15.62500000000000355, -7.320508075688779925 ) ) ;
#37767=ADVANCED_FACE ( 'NONE', ( #3327 ), #36544, .T. ) ;
#37786=CARTESIAN_POINT ( 'NONE',  ( 7.320508075688776373, 125.6250000000000142, -7.320508075688776373 ) ) ;
#37791=CARTESIAN_POINT ( 'NONE',  ( 2.679491924311228956, 106.0416666666666856, -10.00000000000000000 ) ) ;
#37793=CARTESIAN_POINT ( 'NONE',  ( 6.676582343750001591, 293.1093750017069510, -8.176455196517173205E-16 ) ) ;
#37800=CARTESIAN_POINT ( 'NONE',  ( -7.320508075688778149, 184.9999999931720254, 7.320508075688769267 ) ) ;
#37804=CARTESIAN_POINT ( 'NONE',  ( -9.832129032723418760, 2.864583329919349719, -5.676582343750004256 ) ) ;
#37806=CARTESIAN_POINT ( 'NONE',  ( -11.35316468750000141, 193.5937499965860127, -1.390361679473963753E-15 ) ) ;
#37811=FACE_OUTER_BOUND ( 'NONE', #3948, .T. ) ;
#37812=ORIENTED_EDGE ( 'NONE', *, *, #19598, .F. ) ;
#37816=CARTESIAN_POINT ( 'NONE',  ( -11.35316468750000141, 8.281249996586016238, -1.390361679473963753E-15 ) ) ;
#37824=CARTESIAN_POINT ( 'NONE',  ( 9.832129032723416984, 120.3645833299193697, 5.676582343750006032 ) ) ;
#37825=CARTESIAN_POINT ( 'NONE',  ( 10.00000000000000178, 86.87499999317203958, 0.000000000000000000 ) ) ;
#37829=CARTESIAN_POINT ( 'NONE',  ( 5.000000000000005329, 145.8333333333333428, -8.660254037844392627 ) ) ;
#37832=CARTESIAN_POINT ( 'NONE',  ( -6.676582343750000703, 292.6718750017069510, 2.765530957082001251 ) ) ;
#37834=CARTESIAN_POINT ( 'NONE',  ( -8.311093377946836114, 172.6562499965860411, -8.311093377946837890 ) ) ;
#37843=EDGE_CURVE ( 'NONE', #9634, #5468, #11182, .T. ) ;
#37845=CARTESIAN_POINT ( 'NONE',  ( -2.085542519210945728E-15, 154.8437499965860127, 11.35316468750000141 ) ) ;
#37849=CARTESIAN_POINT ( 'NONE',  ( 11.35316468749999963, 56.30208332991934839, -3.042071309553165293 ) ) ;
#37850=ORIENTED_EDGE ( 'NONE', *, *, #6344, .T. ) ;
#37856=CARTESIAN_POINT ( 'NONE',  ( 6.000000000000003553, 288.6250000034139589, -2.485281374238571761 ) ) ;
#37857=CARTESIAN_POINT ( 'NONE',  ( 2.679491924311228956, 67.91666665983868256, -10.00000000000000000 ) ) ;
#37862=CARTESIAN_POINT ( 'NONE',  ( -6.676582343750001591, 287.5312500017070079, 0.000000000000000000 ) ) ;
#37878=CARTESIAN_POINT ( 'NONE',  ( 7.320508075688771044, 74.37500000000001421, 7.320508075688775484 ) ) ;
#37879=AXIS2_PLACEMENT_3D ( 'NONE', #42856, #54576, #71901 ) ;
#37881=CARTESIAN_POINT ( 'NONE',  ( 6.000000000000003553, 290.4375000000000000, 2.485281374238571317 ) ) ;
#37883=CARTESIAN_POINT ( 'NONE',  ( -5.000000000000001776, 126.6666666666666714, -8.660254037844392627 ) ) ;
#37892=CARTESIAN_POINT ( 'NONE',  ( 2.679491924311228956, 191.0416666666666572, -10.00000000000000000 ) ) ;
#37895=CARTESIAN_POINT ( 'NONE',  ( 8.311093377946837890, 156.7187499965860127, -8.311093377946837890 ) ) ;
#37898=CARTESIAN_POINT ( 'NONE',  ( 10.00000000000018296, 155.2083333333334565, -2.679491924311276030 ) ) ;
#37903=CARTESIAN_POINT ( 'NONE',  ( 5.676582343749993598, 15.26041666325268409, 9.832129032723422313 ) ) ;
#37909=CARTESIAN_POINT ( 'NONE',  ( -2.679491924311235618, 55.41666665983870388, 10.00000000000000000 ) ) ;
#37916=ORIENTED_EDGE ( 'NONE', *, *, #63354, .T. ) ;
#37921=CARTESIAN_POINT ( 'NONE',  ( -5.676582343750006032, 124.1145833299193555, 9.832129032723418760 ) ) ;
#37922=VERTEX_POINT ( 'NONE', #11131 ) ;
#37926=CYLINDRICAL_SURFACE ( 'NONE', #47384, 8.000000000000003553 ) ;
#37928=CARTESIAN_POINT ( 'NONE',  ( 9.832129032723416984, 130.3645833299193555, 5.676582343750006032 ) ) ;
#37929=CARTESIAN_POINT ( 'NONE',  ( 0.000000000000000000, 300.0000000000000000, 10.00000000000000178 ) ) ;
#37931=CARTESIAN_POINT ( 'NONE',  ( -5.000000000000005329, 25.20833332650536818, 8.660254037844387298 ) ) ;
#37933=CARTESIAN_POINT ( 'NONE',  ( 6.951808397369818766E-16, 117.3437499965860127, -11.35316468750000141 ) ) ;
#37938=CARTESIAN_POINT ( 'NONE',  ( 9.832129032723420536, 26.51041666325268409, -5.676582343749999815 ) ) ;
#37947=CARTESIAN_POINT ( 'NONE',  ( 6.000000000000003553, 298.6250000034140157, -2.485281374238571761 ) ) ;
#37951=EDGE_CURVE ( 'NONE', #32224, #10358, #8745, .T. ) ;
#37952=CARTESIAN_POINT ( 'NONE',  ( 8.311093377946834337, 140.4687499965859843, 8.311093377946839666 ) ) ;
#37961=EDGE_CURVE ( 'NONE', #67735, #42303, #63898, .T. ) ;
#37968=CARTESIAN_POINT ( 'NONE',  ( 0.000000000000000000, 300.0000000000000000, 0.000000000000000000 ) ) ;
#37969=CARTESIAN_POINT ( 'NONE',  ( -11.35316468750000141, 183.2812499965860411, -1.390361679473963753E-15 ) ) ;
#37972=CARTESIAN_POINT ( 'NONE',  ( 4.721056650416000089, 288.8281250017069510, 4.721056650415999201 ) ) ;
#37974=CARTESIAN_POINT ( 'NONE',  ( 9.999999999999996447, 95.00000000000000000, 0.000000000000000000 ) ) ;
#37975=ORIENTED_EDGE ( 'NONE', *, *, #63738, .T. ) ;
#37978=CARTESIAN_POINT ( 'NONE',  ( 10.00000000000000178, 167.0833333265053682, -2.679491924311226736 ) ) ;
#37982=DIRECTION ( 'NONE',  ( 0.000000000000000000, 0.000000000000000000, 1.000000000000000000 ) ) ;
#37985=CARTESIAN_POINT ( 'NONE',  ( 5.676582343749993598, 115.2604166632526983, 9.832129032723422313 ) ) ;
#37986=LINE ( 'NONE', #37610, #7145 ) ;
#37990=DIRECTION ( 'NONE',  ( -0.000000000000000000, 1.000000000000000000, -0.000000000000000000 ) ) ;
#37993=CARTESIAN_POINT ( 'NONE',  ( -9.832129032723418760, 222.8645833299193839, -5.676582343750004256 ) ) ;
#37997=CARTESIAN_POINT ( 'NONE',  ( -8.311093377946841443, 209.2187499965859843, 8.311093377946830785 ) ) ;
#37999=DIRECTION ( 'NONE',  ( -0.000000000000000000, 1.000000000000000000, -0.000000000000000000 ) ) ;
#38004=CARTESIAN_POINT ( 'NONE',  ( -11.35316468750000141, 83.48958332991935549, 3.042071309553159963 ) ) ;
#38010=CARTESIAN_POINT ( 'NONE',  ( 3.042071309553159519, 84.73958332991936970, 11.35316468750000141 ) ) ;
#38017=CARTESIAN_POINT ( 'NONE',  ( 5.676582343749993598, 79.94791666325269830, 9.832129032723422313 ) ) ;
#38022=CARTESIAN_POINT ( 'NONE',  ( -4.999999999999998224, 168.5416666598387110, -8.660254037844389075 ) ) ;
#38025=CARTESIAN_POINT ( 'NONE',  ( 3.042071309553167513, 72.13541666325268409, -11.35316468749999785 ) ) ;
#38026=CARTESIAN_POINT ( 'NONE',  ( -6.676582343750003368, 292.3906250017068942, -2.765530957081996810 ) ) ;
#38028=CARTESIAN_POINT ( 'NONE',  ( -11.35316468750000141, 208.2812499965860411, -1.390361679473963753E-15 ) ) ;
#38034=CARTESIAN_POINT ( 'NONE',  ( 11.35316468750000141, 200.7812499965860411, 0.000000000000000000 ) ) ;
#38039=CARTESIAN_POINT ( 'NONE',  ( -9.832129032723420536, 194.0104166632526983, 5.676582343749997150 ) ) ;
#38042=CARTESIAN_POINT ( 'NONE',  ( -7.320508075688771932, 93.12500000000000000, 7.320508075688763938 ) ) ;
#38045=( BOUNDED_CURVE ( )  B_SPLINE_CURVE ( 2, ( #59324, #42687, #65699, #25698, #1970, #47242, #48719, #36675, #70269, #29904, #59687, #8361, #41594 ),
 .UNSPECIFIED., .F., .F. ) 
 B_SPLINE_CURVE_WITH_KNOTS ( ( 3, 2, 2, 2, 2, 2, 3 ),
 ( 2.370688293668704372, 2.375920754678181979, 2.381153215687659586, 2.386385676697137193, 2.391618137706614799, 2.396850598716092406, 2.402083059725570013 ),
 .UNSPECIFIED. ) 
 CURVE ( )  GEOMETRIC_REPRESENTATION_ITEM ( )  RATIONAL_B_SPLINE_CURVE ( ( 0.9999999999999978906, 0.9659258262890704216, 1.000000000000000000, 0.9659258262890683122, 1.000000000000000000, 0.9659258262890683122, 1.000000000000000000, 0.9659258262890683122, 1.000000000000000000, 0.9659258262890683122, 1.000000000000000000, 0.9659258262891560198, 0.9999999999999122924 ) ) 
 REPRESENTATION_ITEM ( '' )  );
#38046=FACE_OUTER_BOUND ( 'NONE', #29245, .T. ) ;
#38058=CARTESIAN_POINT ( 'NONE',  ( -7.320508075688863414, 83.12500000000005684, 7.320508075688855421 ) ) ;
#38064=AXIS2_PLACEMENT_3D ( 'NONE', #7706, #47680, #24308 ) ;
#38070=CARTESIAN_POINT ( 'NONE',  ( 5.676582343750001591, 71.92708332991934128, -9.832129032723420536 ) ) ;
#38071=DIRECTION ( 'NONE',  ( -0.000000000000000000, 1.000000000000000000, -0.000000000000000000 ) ) ;
#38075=CARTESIAN_POINT ( 'NONE',  ( -4.088227598258586603E-16, 291.3593750017070079, -6.676582343750001591 ) ) ;
#38077=CARTESIAN_POINT ( 'NONE',  ( -4.999999999999998224, 163.5416666598387110, -8.660254037844389075 ) ) ;
#38091=CARTESIAN_POINT ( 'NONE',  ( 6.951808397369818766E-16, 47.03124999658601979, -11.35316468750000141 ) ) ;
#38093=CARTESIAN_POINT ( 'NONE',  ( -10.00000000000000355, 9.583333326505362848, 2.679491924311223183 ) ) ;
#38096=EDGE_CURVE ( 'NONE', #49230, #69413, #21739, .T. ) ;
#38098=CARTESIAN_POINT ( 'NONE',  ( -8.311093377946836114, 42.65624999658600558, -8.311093377946837890 ) ) ;
#38102=CARTESIAN_POINT ( 'NONE',  ( -9.832129032723418760, 47.86458332991934839, -5.676582343750004256 ) ) ;
#38106=CARTESIAN_POINT ( 'NONE',  ( -11.35316468750000141, 158.4895833299193839, 3.042071309553159963 ) ) ;
#38107=CARTESIAN_POINT ( 'NONE',  ( -7.320508075688778149, 129.9999999931719969, 7.320508075688769267 ) ) ;
#38110=DIRECTION ( 'NONE',  ( -0.000000000000000000, 1.000000000000000000, -0.000000000000000000 ) ) ;
#38111=CARTESIAN_POINT ( 'NONE',  ( 11.35316468749999963, 36.30208332991935549, -3.042071309553165293 ) ) ;
#38119=CARTESIAN_POINT ( 'NONE',  ( -5.676582343750006032, 159.1145833299193839, 9.832129032723418760 ) ) ;
#38128=CARTESIAN_POINT ( 'NONE',  ( -3.042071309553173730, 104.6354166632526699, 11.35316468749999785 ) ) ;
#38140=CARTESIAN_POINT ( 'NONE',  ( -10.00000000000000355, 159.5833333265053398, 2.679491924311223183 ) ) ;
#38156=CARTESIAN_POINT ( 'NONE',  ( 10.00000000000000355, 125.2083333333333428, -2.679491924311227180 ) ) ;
#38161=CARTESIAN_POINT ( 'NONE',  ( 7.320508075688774596, 105.6250000000000142, -7.320508075688774596 ) ) ;
#38163=CARTESIAN_POINT ( 'NONE',  ( -6.676582343750000703, 293.6718750017070079, 2.765530957082001251 ) ) ;
#38171=CARTESIAN_POINT ( 'NONE',  ( -4.999999999999998224, 183.5416666598387110, -8.660254037844389075 ) ) ;
#38176=CARTESIAN_POINT ( 'NONE',  ( -8.660254037844390851, 94.79166665983871098, 4.999999999999998224 ) ) ;
#38177=CARTESIAN_POINT ( 'NONE',  ( -2.679491924311235618, 223.5416666666666856, 10.00000000000000000 ) ) ;
#38179=CARTESIAN_POINT ( 'NONE',  ( 11.35316468749999785, 200.8854166632526699, 3.042071309553174174 ) ) ;
#38180=CARTESIAN_POINT ( 'NONE',  ( -10.00000000000000000, 134.1666666598387110, -2.679491924311229845 ) ) ;
#38182=CARTESIAN_POINT ( 'NONE',  ( 1.102182119232618108E-15, 290.2500000000000000, 6.000000000000001776 ) ) ;
#38187=CARTESIAN_POINT ( 'NONE',  ( -3.042071309553173730, 9.322916663252685865, 11.35316468749999785 ) ) ;
#38193=CARTESIAN_POINT ( 'NONE',  ( 8.311093377946837890, 1.406249996586016238, -8.311093377946837890 ) ) ;
#38196=CARTESIAN_POINT ( 'NONE',  ( -11.35316468750000141, 118.2812499965860269, -1.390361679473963753E-15 ) ) ;
#38197=CARTESIAN_POINT ( 'NONE',  ( 10.00000000000000000, 86.66666665983869677, 2.679491924311236062 ) ) ;
#38201=CARTESIAN_POINT ( 'NONE',  ( -2.679491924311235174, 40.41666665983869677, 10.00000000000000000 ) ) ;
#38202=ORIENTED_EDGE ( 'NONE', *, *, #23518, .F. ) ;
#38203=CARTESIAN_POINT ( 'NONE',  ( -8.987638501917114553, 226.0000000000000000, -4.433077647033027091 ) ) ;
#38205=CARTESIAN_POINT ( 'NONE',  ( 2.765530957082001251, 289.9218750017069510, 6.676582343750000703 ) ) ;
#38209=CARTESIAN_POINT ( 'NONE',  ( -8.660254037844390851, 209.7916666598387110, 4.999999999999998224 ) ) ;
#38214=CARTESIAN_POINT ( 'NONE',  ( -11.35316468749999785, 158.3854166632526699, -3.042071309553167957 ) ) ;
#38218=CARTESIAN_POINT ( 'NONE',  ( -11.35316468750000141, 58.80208332991933418, 3.042071309553159963 ) ) ;
#38219=EDGE_LOOP ( 'NONE', ( #65226, #37916, #54524, #45659 ) ) ;
#38225=CARTESIAN_POINT ( 'NONE',  ( 6.000000000000003553, 287.5000000034140157, 2.485281374238571317 ) ) ;
#38226=CARTESIAN_POINT ( 'NONE',  ( 7.320508075688771044, 66.24999999317203958, 7.320508075688775484 ) ) ;
#38245=CARTESIAN_POINT ( 'NONE',  ( -4.999999999999998224, 201.6666666666666856, -8.660254037844389075 ) ) ;
#38249=CARTESIAN_POINT ( 'NONE',  ( 10.00000000000000000, 69.79166666666664298, 2.679491924311236062 ) ) ;
#38251=CARTESIAN_POINT ( 'NONE',  ( -2.485281374238571761, 292.8125000000000000, -6.000000000000003553 ) ) ;
#38254=ORIENTED_EDGE ( 'NONE', *, *, #69377, .F. ) ;
#38263=CARTESIAN_POINT ( 'NONE',  ( 10.00000000000000178, 185.2083333333332860, -2.679491924311226736 ) ) ;
#38264=CARTESIAN_POINT ( 'NONE',  ( 10.00000000000000178, 1.874999993172032697, 0.000000000000000000 ) ) ;
#38266=CARTESIAN_POINT ( 'NONE',  ( 8.311093377946834337, 160.4687499965860127, 8.311093377946839666 ) ) ;
#38268=CARTESIAN_POINT ( 'NONE',  ( 1.102182119232618108E-15, 294.2500000000000000, 6.000000000000001776 ) ) ;
#38270=CARTESIAN_POINT ( 'NONE',  ( 6.123233995736767268E-16, 83.12499999317203958, -10.00000000000000178 ) ) ;
#38272=AXIS2_PLACEMENT_3D ( 'NONE', #28718, #57037, #51733 ) ;
#38274=CARTESIAN_POINT ( 'NONE',  ( -9.832129032723418760, 28.17708332991935194, -5.676582343750004256 ) ) ;
#38276=CARTESIAN_POINT ( 'NONE',  ( 8.660254037844385522, 31.45833332650536818, 5.000000000000005329 ) ) ;
#38277=DIRECTION ( 'NONE',  ( 0.000000000000000000, 0.000000000000000000, 1.000000000000000000 ) ) ;
#38280=CARTESIAN_POINT ( 'NONE',  ( 2.679491924311222739, 45.83333332650537528, 10.00000000000000355 ) ) ;
#38283=DIRECTION ( 'NONE',  ( -0.000000000000000000, 1.000000000000000000, -0.000000000000000000 ) ) ;
#38292=CARTESIAN_POINT ( 'NONE',  ( 8.311093377946834337, 135.1562499965860411, 8.311093377946839666 ) ) ;
#38298=CARTESIAN_POINT ( 'NONE',  ( -7.320508075688773708, 153.7499999931720538, -7.320508075688774596 ) ) ;
#38300=CARTESIAN_POINT ( 'NONE',  ( -11.35316468749999785, 123.0729166632526983, -3.042071309553167957 ) ) ;
#38301=CARTESIAN_POINT ( 'NONE',  ( 8.660254037844389075, 147.2916666598387110, -5.000000000000000000 ) ) ;
#38307=CARTESIAN_POINT ( 'NONE',  ( 6.951808397369818766E-16, 112.3437499965860127, -11.35316468750000141 ) ) ;
#38311=CARTESIAN_POINT ( 'NONE',  ( -9.832129032723418760, 18.17708332991935194, -5.676582343750004256 ) ) ;
#38318=CARTESIAN_POINT ( 'NONE',  ( 1.226468279477575784E-15, 289.7031250017069510, 6.676582343750001591 ) ) ;
#38321=ORIENTED_EDGE ( 'NONE', *, *, #141, .F. ) ;
#38322=CARTESIAN_POINT ( 'NONE',  ( -8.311093377946841443, 144.2187499965860127, 8.311093377946830785 ) ) ;
#38338=CARTESIAN_POINT ( 'NONE',  ( 5.676582343750001591, 186.6145833299193839, -9.832129032723420536 ) ) ;
#38341=CARTESIAN_POINT ( 'NONE',  ( -2.765530957081996810, 289.2656250017069510, -6.676582343750002480 ) ) ;
#38342=LINE ( 'NONE', #27011, #63485 ) ;
#38353=CARTESIAN_POINT ( 'NONE',  ( 11.35316468749999963, 116.3020833299193413, -3.042071309553165293 ) ) ;
#38358=LINE ( 'NONE', #50042, #53118 ) ;
#38360=EDGE_CURVE ( 'NONE', #24671, #39497, #58831, .T. ) ;
#38362=CARTESIAN_POINT ( 'NONE',  ( 10.00943074283379097, 224.9691878336754769, 0.3937656040914069289 ) ) ;
#38365=EDGE_CURVE ( 'NONE', #65401, #72057, #48646, .T. ) ;
#38367=CARTESIAN_POINT ( 'NONE',  ( -9.832129032723418760, 208.1770833299193555, -5.676582343750004256 ) ) ;
#38369=CARTESIAN_POINT ( 'NONE',  ( 11.03609750322952898, 225.9999999999999716, 2.202692091203484637 ) ) ;
#38375=CARTESIAN_POINT ( 'NONE',  ( 5.676582343750001591, 91.61458332991935549, -9.832129032723420536 ) ) ;
#38382=CARTESIAN_POINT ( 'NONE',  ( 3.042071309553167069, 91.82291666325269830, -11.35316468749999785 ) ) ;
#38383=ORIENTED_EDGE ( 'NONE', *, *, #71804, .F. ) ;
#38390=CARTESIAN_POINT ( 'NONE',  ( 11.35316468750000141, 80.78124999658602690, 0.000000000000000000 ) ) ;
#38395=CARTESIAN_POINT ( 'NONE',  ( 6.123233995736767268E-16, 183.1249999931720538, -10.00000000000000178 ) ) ;
#38398=CARTESIAN_POINT ( 'NONE',  ( 3.042071309553159519, 80.05208332991935549, 11.35316468750000141 ) ) ;
#38399=CARTESIAN_POINT ( 'NONE',  ( 2.765530957082001251, 293.7656250017068942, 6.676582343750000703 ) ) ;
#38401=CARTESIAN_POINT ( 'NONE',  ( -8.311093377946836114, 207.6562499965860411, -8.311093377946837890 ) ) ;
#38404=CARTESIAN_POINT ( 'NONE',  ( -2.679491924311235174, 70.41666665983869677, 10.00000000000000000 ) ) ;
#38408=CARTESIAN_POINT ( 'NONE',  ( 9.832129032723416984, 205.3645833299193555, 5.676582343750006032 ) ) ;
#38413=CARTESIAN_POINT ( 'NONE',  ( 5.676582343749993598, 195.2604166632526983, 9.832129032723422313 ) ) ;
#38420=CARTESIAN_POINT ( 'NONE',  ( -2.679491924311235618, 8.541666666666667851, 10.00000000000000000 ) ) ;
#38428=ORIENTED_EDGE ( 'NONE', *, *, #21851, .T. ) ;
#38435=ORIENTED_EDGE ( 'NONE', *, *, #65708, .T. ) ;
#38442=CARTESIAN_POINT ( 'NONE',  ( 11.35316468749999785, 70.88541666325265567, 3.042071309553174174 ) ) ;
#38445=DIRECTION ( 'NONE',  ( -0.000000000000000000, 1.000000000000000000, -0.000000000000000000 ) ) ;
#38447=CARTESIAN_POINT ( 'NONE',  ( 2.765530957081996366, 289.2968750017069510, -6.676582343750002480 ) ) ;
#38457=CARTESIAN_POINT ( 'NONE',  ( 11.35316468749999785, 165.8854166632526415, 3.042071309553174174 ) ) ;
#38458=CARTESIAN_POINT ( 'NONE',  ( 1.269536070779894168E-12, 186.2499999999999147, -10.00000000000000178 ) ) ;
#38460=CARTESIAN_POINT ( 'NONE',  ( -10.00000000000000000, 19.16666665983869322, -2.679491924311229845 ) ) ;
#38464=CARTESIAN_POINT ( 'NONE',  ( 9.832129032723420536, 41.19791666325269119, -5.676582343749999815 ) ) ;
#38466=CARTESIAN_POINT ( 'NONE',  ( -10.00000000000000178, 24.37499999317203603, -1.224646799147353454E-15 ) ) ;
#38468=VERTEX_POINT ( 'NONE', #25579 ) ;
#38469=CARTESIAN_POINT ( 'NONE',  ( 4.999999999999993783, 141.0416666598387110, 8.660254037844390851 ) ) ;
#38471=CARTESIAN_POINT ( 'NONE',  ( 3.042071309553167069, 51.82291666325266988, -11.35316468749999785 ) ) ;
#38477=CARTESIAN_POINT ( 'NONE',  ( -3.042071309553173730, 44.32291666325267698, 11.35316468749999785 ) ) ;
#38480=CARTESIAN_POINT ( 'NONE',  ( 8.311093377946837890, 156.4062499965860411, -8.311093377946837890 ) ) ;
#38482=CARTESIAN_POINT ( 'NONE',  ( -7.320508075688773708, 143.7499999931719969, -7.320508075688774596 ) ) ;
#38484=CYLINDRICAL_SURFACE ( 'NONE', #24360, 10.00000000000000178 ) ;
#38485=CARTESIAN_POINT ( 'NONE',  ( 3.042071309553167513, 37.13541666325267698, -11.35316468749999785 ) ) ;
#38486=CARTESIAN_POINT ( 'NONE',  ( 2.220677790255211837E-11, 201.2499999999982663, -9.999999999999998224 ) ) ;
#38492=CARTESIAN_POINT ( 'NONE',  ( 9.832129032723420536, 166.1979166632526983, -5.676582343749999815 ) ) ;
#38495=EDGE_CURVE ( 'NONE', #52730, #19485, #60294, .T. ) ;
#38503=CARTESIAN_POINT ( 'NONE',  ( -10.00000000000000178, 119.3749999931720396, -1.224646799147353454E-15 ) ) ;
#38504=CARTESIAN_POINT ( 'NONE',  ( 0.000000000000000000, 300.0000000000000000, 0.000000000000000000 ) ) ;
#38505=CARTESIAN_POINT ( 'NONE',  ( -3.042071309553173730, 114.6354166632526983, 11.35316468749999785 ) ) ;
#38527=CARTESIAN_POINT ( 'NONE',  ( 5.000000000000001776, 72.70833332650536818, -8.660254037844389075 ) ) ;
#38533=CARTESIAN_POINT ( 'NONE',  ( 2.485281374238286656, 288.6875000000000568, -6.000000000000285105 ) ) ;
#38538=CARTESIAN_POINT ( 'NONE',  ( -8.660254037844387298, 117.0833333333333428, -5.000000000000004441 ) ) ;
#38540=CARTESIAN_POINT ( 'NONE',  ( -4.721056650415999201, 292.4843750017070079, -4.721056650415999201 ) ) ;
#38551=LINE ( 'NONE', #33270, #45617 ) ;
#38555=CARTESIAN_POINT ( 'NONE',  ( 6.123233995736767268E-16, 93.12499999317203958, -10.00000000000000178 ) ) ;
#38556=CARTESIAN_POINT ( 'NONE',  ( 6.951808397369818766E-16, 7.031249996586016238, -11.35316468750000141 ) ) ;
#38558=CARTESIAN_POINT ( 'NONE',  ( -3.042071309553173730, 209.6354166632526415, 11.35316468749999785 ) ) ;
#38564=CARTESIAN_POINT ( 'NONE',  ( 6.000000000000003553, 297.4374999999999432, 2.485281374238571317 ) ) ;
#38567=CARTESIAN_POINT ( 'NONE',  ( 11.35316468749999785, 5.572916663252682312, 3.042071309553174174 ) ) ;
#38571=CARTESIAN_POINT ( 'NONE',  ( -1.836970198721029983E-15, 60.62499999317203958, 10.00000000000000178 ) ) ;
#38573=CARTESIAN_POINT ( 'NONE',  ( 11.35316468750000141, 10.78124999658601624, 0.000000000000000000 ) ) ;
#38575=CARTESIAN_POINT ( 'NONE',  ( -2.085542519210945728E-15, 119.5312499965860269, 11.35316468750000141 ) ) ;
#38576=EDGE_CURVE ( 'NONE', #5834, #51512, #33484, .T. ) ;
#38577=CARTESIAN_POINT ( 'NONE',  ( 7.320508075688774596, 82.49999999317202537, -7.320508075688774596 ) ) ;
#38582=ORIENTED_EDGE ( 'NONE', *, *, #48129, .F. ) ;
#38583=CARTESIAN_POINT ( 'NONE',  ( 6.676582343750001591, 289.1093750017069510, -8.176455196517173205E-16 ) ) ;
#38591=CARTESIAN_POINT ( 'NONE',  ( 10.00000000000000000, 156.6666666598386826, 2.679491924311235618 ) ) ;
#38592=CARTESIAN_POINT ( 'NONE',  ( 11.35316468749999785, 150.8854166632526983, 3.042071309553174174 ) ) ;
#38594=EDGE_CURVE ( 'NONE', #49230, #32224, #27797, .T. ) ;
#38596=CARTESIAN_POINT ( 'NONE',  ( -5.676582343749998039, 77.76041666325268409, -9.832129032723420536 ) ) ;
#38606=VECTOR ( 'NONE', #55145, 1000.000000000000000 ) ;
#38615=EDGE_CURVE ( 'NONE', #5468, #21228, #49701, .T. ) ;
#38629=CARTESIAN_POINT ( 'NONE',  ( -10.00000000000000178, 67.50000000000000000, -1.224646799147353454E-15 ) ) ;
#38631=CARTESIAN_POINT ( 'NONE',  ( 4.242640687119287435, 294.3750000000000000, 4.242640687119285658 ) ) ;
#38641=CARTESIAN_POINT ( 'NONE',  ( -1.604524386212670052E-13, 78.75000000000000000, 10.00000000000000178 ) ) ;
#38642=CARTESIAN_POINT ( 'NONE',  ( 10.00000000000000000, 189.7916666666666856, 2.679491924311236062 ) ) ;
#38645=CARTESIAN_POINT ( 'NONE',  ( -5.676582343750006032, 164.4270833299193555, 9.832129032723418760 ) ) ;
#38652=CARTESIAN_POINT ( 'NONE',  ( -3.042071309553173730, 19.63541666325268764, 11.35316468749999785 ) ) ;
#38653=CARTESIAN_POINT ( 'NONE',  ( 2.679491924311302675, 97.91666665983869677, -9.999999999999957367 ) ) ;
#38659=CARTESIAN_POINT ( 'NONE',  ( -10.00000000000000178, 54.37499999317203958, -1.224646799147353454E-15 ) ) ;
#38662=FACE_OUTER_BOUND ( 'NONE', #66349, .T. ) ;
#38664=CARTESIAN_POINT ( 'NONE',  ( 2.679491924330074770, 166.0416666666649803, -9.999999999989118038 ) ) ;
#38669=CARTESIAN_POINT ( 'NONE',  ( -1.604524386212670052E-13, 78.75000000000000000, 10.00000000000000178 ) ) ;
#38671=CARTESIAN_POINT ( 'NONE',  ( -8.311093377946841443, 138.9062499965859843, 8.311093377946830785 ) ) ;
#38678=CARTESIAN_POINT ( 'NONE',  ( -8.311093377946836114, 122.6562499965860269, -8.311093377946837890 ) ) ;
#38684=CARTESIAN_POINT ( 'NONE',  ( -3.042071309553163960, 117.5520833299193413, -11.35316468749999963 ) ) ;
#38688=CARTESIAN_POINT ( 'NONE',  ( -5.676582343749998039, 17.76041666325268409, -9.832129032723420536 ) ) ;
#38689=ORIENTED_EDGE ( 'NONE', *, *, #11739, .F. ) ;
#38690=CARTESIAN_POINT ( 'NONE',  ( 1.224646799147353454E-15, 300.0000000000000000, -10.00000000000000178 ) ) ;
#38693=VECTOR ( 'NONE', #22019, 1000.000000000000000 ) ;
#38696=CARTESIAN_POINT ( 'NONE',  ( -4.721056650415998313, 288.5781250017069510, 4.721056650416000089 ) ) ;
#38697=CARTESIAN_POINT ( 'NONE',  ( -1.269107444400135093E-11, 58.74999999999901945, 10.00000000000000178 ) ) ;
#38699=VERTEX_POINT ( 'NONE', #27420 ) ;
#38700=EDGE_CURVE ( 'NONE', #42029, #4267, #8303, .T. ) ;
#38701=CARTESIAN_POINT ( 'NONE',  ( -9.832129032723420536, 149.0104166632526699, 5.676582343749997150 ) ) ;
#38706=VERTEX_POINT ( 'NONE', #36287 ) ;
#38719=CARTESIAN_POINT ( 'NONE',  ( 3.042071309553167069, 181.8229166632526983, -11.35316468749999785 ) ) ;
#38723=CARTESIAN_POINT ( 'NONE',  ( -4.721056650415999201, 290.3281250017069510, -4.721056650415999201 ) ) ;
#38724=DIRECTION ( 'NONE',  ( -0.000000000000000000, 1.000000000000000000, -0.000000000000000000 ) ) ;
#38734=CARTESIAN_POINT ( 'NONE',  ( -10.00000000000000178, 142.5000000000000284, -1.224646799147353454E-15 ) ) ;
#38738=CARTESIAN_POINT ( 'NONE',  ( -11.35316468750000141, 108.5937499965860269, -1.390361679473963753E-15 ) ) ;
#38746=CARTESIAN_POINT ( 'NONE',  ( 2.338768297991025147, 223.9372515351016659, 9.740328430350823297 ) ) ;
#38749=CARTESIAN_POINT ( 'NONE',  ( -11.35316468749999785, 203.3854166632526983, -3.042071309553167513 ) ) ;
#38756=CARTESIAN_POINT ( 'NONE',  ( 11.35316468749999785, 90.57291666325268409, 3.042071309553174174 ) ) ;
#38763=CARTESIAN_POINT ( 'NONE',  ( -8.311093377946841443, 83.90624999658602690, 8.311093377946830785 ) ) ;
#38765=CARTESIAN_POINT ( 'NONE',  ( 10.00000000000000000, 206.6666666598387110, 2.679491924311235618 ) ) ;
#38769=CARTESIAN_POINT ( 'NONE',  ( 6.951808397369818766E-16, 87.03124999658602690, -11.35316468750000141 ) ) ;
#38773=CARTESIAN_POINT ( 'NONE',  ( -4.999999999999998224, 188.5416666598387110, -8.660254037844389075 ) ) ;
#38775=CARTESIAN_POINT ( 'NONE',  ( 5.676582343749993598, 80.26041666325268409, 9.832129032723422313 ) ) ;
#38776=CARTESIAN_POINT ( 'NONE',  ( -2.765530957081998586, 295.6406250017069510, 6.676582343750001591 ) ) ;
#38778=CARTESIAN_POINT ( 'NONE',  ( 5.676582343749993598, 214.9479166632526983, 9.832129032723422313 ) ) ;
#38781=DIRECTION ( 'NONE',  ( 0.8660254037844696828, -0.4999999999999462097, 0.000000000000000000 ) ) ;
#38782=CARTESIAN_POINT ( 'NONE',  ( -1.836970198721029983E-15, 143.7500000000000284, 10.00000000000000178 ) ) ;
#38783=CARTESIAN_POINT ( 'NONE',  ( 5.676582343749993598, 204.9479166632526983, 9.832129032723422313 ) ) ;
#38787=CARTESIAN_POINT ( 'NONE',  ( -11.35316468750000141, 188.8020833299193555, 3.042071309553159963 ) ) ;
#38795=CARTESIAN_POINT ( 'NONE',  ( 2.679491924311222739, 8.958333333333333925, 10.00000000000000355 ) ) ;
#38803=CARTESIAN_POINT ( 'NONE',  ( 10.00000000000000178, 16.87499999317203248, 0.000000000000000000 ) ) ;
#38805=ADVANCED_FACE ( 'NONE', ( #18563 ), #1233, .T. ) ;
#38818=CARTESIAN_POINT ( 'NONE',  ( -3.042071309553173730, 79.63541666325268409, 11.35316468749999785 ) ) ;
#38821=CARTESIAN_POINT ( 'NONE',  ( 4.721056650416000089, 290.9843750017070079, 4.721056650415999201 ) ) ;
#38823=CARTESIAN_POINT ( 'NONE',  ( -1.836970198721029983E-15, 165.6249999931720254, 10.00000000000000178 ) ) ;
#38829=CARTESIAN_POINT ( 'NONE',  ( -3.042071309553164404, 162.5520833299193555, -11.35316468749999963 ) ) ;
#38837=CARTESIAN_POINT ( 'NONE',  ( 9.832129032723420536, 61.19791666325267698, -5.676582343749999815 ) ) ;
#38839=CARTESIAN_POINT ( 'NONE',  ( -7.320508075688773708, 18.74999999317203248, -7.320508075688774596 ) ) ;
#38844=CARTESIAN_POINT ( 'NONE',  ( 5.676582343749993598, 44.94791666325267698, 9.832129032723422313 ) ) ;
#38849=CARTESIAN_POINT ( 'NONE',  ( -9.832129032723420536, 48.69791666325268409, 5.676582343749997150 ) ) ;
#38852=CARTESIAN_POINT ( 'NONE',  ( -9.832129032723418760, 172.8645833299193555, -5.676582343750004256 ) ) ;
#38853=CARTESIAN_POINT ( 'NONE',  ( 8.660254037844389075, 147.2916666598387110, -5.000000000000000000 ) ) ;
#38856=DIRECTION ( 'NONE',  ( 0.000000000000000000, 0.000000000000000000, 1.000000000000000000 ) ) ;
#38857=CARTESIAN_POINT ( 'NONE',  ( -8.311093377946841443, 29.21874999658601624, 8.311093377946834337 ) ) ;
#38858=LINE ( 'NONE', #57333, #21976 ) ;
#38863=CARTESIAN_POINT ( 'NONE',  ( -8.660254037844394404, 7.916666666666672292, 5.000000000000001776 ) ) ;
#38864=CARTESIAN_POINT ( 'NONE',  ( -11.35316468750000141, 163.2812499965860127, -1.390361679473963753E-15 ) ) ;
#38870=VERTEX_POINT ( 'NONE', #35555 ) ;
#38872=DIRECTION ( 'NONE',  ( 0.000000000000000000, 0.000000000000000000, 1.000000000000000000 ) ) ;
#38873=CARTESIAN_POINT ( 'NONE',  ( 8.311093377946837890, 116.7187499965859985, -8.311093377946837890 ) ) ;
#38878=ADVANCED_FACE ( 'NONE', ( #24211 ), #70610, .T. ) ;
#38899=CARTESIAN_POINT ( 'NONE',  ( 4.242640687119285658, 288.6249999999999432, -4.242640687119286547 ) ) ;
#38903=CARTESIAN_POINT ( 'NONE',  ( 8.660254037844454800, 60.41666666666670693, -5.000000000000039080 ) ) ;
#38904=CARTESIAN_POINT ( 'NONE',  ( 2.679491924311228956, 116.0416666666666430, -10.00000000000000000 ) ) ;
#38907=CARTESIAN_POINT ( 'NONE',  ( 4.721056650415999201, 290.2343750017069510, -4.721056650415999201 ) ) ;
#38912=EDGE_CURVE ( 'NONE', #11319, #413, #62157, .T. ) ;
#38916=DIRECTION ( 'NONE',  ( -0.000000000000000000, 1.000000000000000000, -0.000000000000000000 ) ) ;
#38920=CARTESIAN_POINT ( 'NONE',  ( -10.00000000000000178, 94.37499999317203958, -1.224646799147353454E-15 ) ) ;
#38921=CARTESIAN_POINT ( 'NONE',  ( 9.832129032723416984, 10.36458332991935016, 5.676582343750006032 ) ) ;
#38923=CARTESIAN_POINT ( 'NONE',  ( 11.35316468749999963, 206.3020833299193271, -3.042071309553165293 ) ) ;
#38928=VERTEX_POINT ( 'NONE', #14739 ) ;
#38930=CARTESIAN_POINT ( 'NONE',  ( -5.676582343749998039, 2.447916663252682756, -9.832129032723420536 ) ) ;
#38932=CARTESIAN_POINT ( 'NONE',  ( 4.242640687119285658, 292.6249999999999432, -4.242640687119286547 ) ) ;
#38936=CARTESIAN_POINT ( 'NONE',  ( 3.042071309553167513, 11.82291666325268231, -11.35316468749999785 ) ) ;
#38939=CARTESIAN_POINT ( 'NONE',  ( -8.311093377946836114, 127.6562499965860411, -8.311093377946837890 ) ) ;
#38940=CARTESIAN_POINT ( 'NONE',  ( -1.836970198721029983E-15, 105.6249999931720396, 10.00000000000000178 ) ) ;
#38944=CARTESIAN_POINT ( 'NONE',  ( -5.000000000000005329, 40.20833332650536818, 8.660254037844387298 ) ) ;
#38947=CARTESIAN_POINT ( 'NONE',  ( -4.721056650415999201, 290.4843750017070079, -4.721056650415999201 ) ) ;
#38955=CARTESIAN_POINT ( 'NONE',  ( 11.35316468749999963, 151.3020833299193555, -3.042071309553165293 ) ) ;
#38959=CARTESIAN_POINT ( 'NONE',  ( 8.311093377946834337, 80.46874999658601268, 8.311093377946839666 ) ) ;
#38960=VERTEX_POINT ( 'NONE', #66814 ) ;
#38974=ORIENTED_EDGE ( 'NONE', *, *, #41524, .F. ) ;
#38992=CARTESIAN_POINT ( 'NONE',  ( -7.320508075688773708, 81.87500000000000000, -7.320508075688774596 ) ) ;
#38994=CARTESIAN_POINT ( 'NONE',  ( 6.000000000000001776, 292.5000000000000000, -7.347880794884121708E-16 ) ) ;
#39006=CARTESIAN_POINT ( 'NONE',  ( -10.00000000000000178, 187.5000000000000000, -1.224646799147353454E-15 ) ) ;
#39007=DIRECTION ( 'NONE',  ( -0.000000000000000000, 1.000000000000000000, -0.000000000000000000 ) ) ;
#39009=CARTESIAN_POINT ( 'NONE',  ( -8.311093377946836114, 162.9687499965860411, -8.311093377946837890 ) ) ;
#39010=CYLINDRICAL_SURFACE ( 'NONE', #37298, 10.00000000000000178 ) ;
#39012=CARTESIAN_POINT ( 'NONE',  ( 9.498558403365325509E-13, 68.75000000000008527, 10.00000000000000178 ) ) ;
#39013=DIRECTION ( 'NONE',  ( -0.000000000000000000, 1.000000000000000000, -0.000000000000000000 ) ) ;
#39017=CARTESIAN_POINT ( 'NONE',  ( -9.832129032723418760, 23.17708332991934839, -5.676582343750004256 ) ) ;
#39023=CARTESIAN_POINT ( 'NONE',  ( -8.660254037844387298, 58.95833332650537528, -5.000000000000004441 ) ) ;
#39027=CARTESIAN_POINT ( 'NONE',  ( 1.584317714026805320E-12, 163.7500000000001137, 9.999999999999998224 ) ) ;
#39033=CARTESIAN_POINT ( 'NONE',  ( -7.320508075688783478, 161.8750000000000284, -7.320508075688784366 ) ) ;
#39036=CARTESIAN_POINT ( 'NONE',  ( 8.311093377946837890, 136.4062499965859558, -8.311093377946837890 ) ) ;
#39048=CARTESIAN_POINT ( 'NONE',  ( -9.832129032723420536, 109.0104166632526841, 5.676582343749997150 ) ) ;
#39053=CARTESIAN_POINT ( 'NONE',  ( -9.832129032723418760, 38.17708332991935549, -5.676582343750004256 ) ) ;
#39061=CARTESIAN_POINT ( 'NONE',  ( 4.721056650415999201, 289.0781250017069510, -4.721056650415999201 ) ) ;
#39062=CARTESIAN_POINT ( 'NONE',  ( -5.999999999999999112, 297.0624999999999432, 2.485281374238575314 ) ) ;
#39065=CARTESIAN_POINT ( 'NONE',  ( 3.042071309553159519, 155.0520833299192986, 11.35316468750000141 ) ) ;
#39070=ORIENTED_EDGE ( 'NONE', *, *, #54530, .F. ) ;
#39078=CARTESIAN_POINT ( 'NONE',  ( -3.673940397442060854E-16, 297.8125000034140157, -6.000000000000001776 ) ) ;
#39080=CARTESIAN_POINT ( 'NONE',  ( -8.660254037844390851, 47.91666666666667140, 4.999999999999998224 ) ) ;
#39095=CARTESIAN_POINT ( 'NONE',  ( -7.320508075688773708, 151.8750000000000000, -7.320508075688774596 ) ) ;
#39099=CARTESIAN_POINT ( 'NONE',  ( -5.676582343750006032, 129.4270833299193555, 9.832129032723418760 ) ) ;
#39100=CARTESIAN_POINT ( 'NONE',  ( 10.00000000000000178, 211.8749999931720538, 0.000000000000000000 ) ) ;
#39104=DIRECTION ( 'NONE',  ( 0.000000000000000000, 0.000000000000000000, 1.000000000000000000 ) ) ;
#39106=CARTESIAN_POINT ( 'NONE',  ( 1.472960921100393561, 223.8667061704458092, 9.895268813711334488 ) ) ;
#39109=CARTESIAN_POINT ( 'NONE',  ( -3.042071309553173730, 204.6354166632526699, 11.35316468749999785 ) ) ;
#39116=CARTESIAN_POINT ( 'NONE',  ( 11.35316468749999963, 95.98958332991935549, -3.042071309553165293 ) ) ;
#39122=CARTESIAN_POINT ( 'NONE',  ( -9.832129032723418760, 97.86458332991935549, -5.676582343750004256 ) ) ;
#39130=CARTESIAN_POINT ( 'NONE',  ( -11.35316468750000141, 88.28124999658602690, -1.390361679473963753E-15 ) ) ;
#39135=CARTESIAN_POINT ( 'NONE',  ( -7.320508075688773708, 178.7499999931720254, -7.320508075688774596 ) ) ;
#39137=CARTESIAN_POINT ( 'NONE',  ( 6.000000000000001776, 296.5625000034140157, -7.347880794884121708E-16 ) ) ;
#39138=CARTESIAN_POINT ( 'NONE',  ( 11.35316468750000141, 81.09374999658601268, 0.000000000000000000 ) ) ;
#39139=CARTESIAN_POINT ( 'NONE',  ( -4.721056650415999201, 289.3281250017069510, -4.721056650415999201 ) ) ;
#39142=CARTESIAN_POINT ( 'NONE',  ( 3.042071309553159519, 224.7395833299193555, 11.35316468750000141 ) ) ;
#39146=CARTESIAN_POINT ( 'NONE',  ( 4.242640687119285658, 291.6249999999999432, -4.242640687119286547 ) ) ;
#39147=CARTESIAN_POINT ( 'NONE',  ( -11.35316468750000141, 203.4895833299193555, 3.042071309553159963 ) ) ;
#39152=CARTESIAN_POINT ( 'NONE',  ( -3.042071309553173730, 199.6354166632526983, 11.35316468749999785 ) ) ;
#39159=CARTESIAN_POINT ( 'NONE',  ( -2.679491924311225848, 16.45833333333333570, -10.00000000000000178 ) ) ;
#39162=ORIENTED_EDGE ( 'NONE', *, *, #12239, .F. ) ;
#39167=CARTESIAN_POINT ( 'NONE',  ( 10.00000000000000000, 16.66666665983870033, 2.679491924311235618 ) ) ;
#39179=CARTESIAN_POINT ( 'NONE',  ( -3.042071309553164404, 92.55208332991934128, -11.35316468749999963 ) ) ;
#39184=CARTESIAN_POINT ( 'NONE',  ( -2.765530957081998142, 289.7968750017068942, 6.676582343750000703 ) ) ;
#39188=CARTESIAN_POINT ( 'NONE',  ( 11.35316468749999963, 195.9895833299193555, -3.042071309553165293 ) ) ;
#39189=EDGE_CURVE ( 'NONE', #7760, #57671, #8166, .T. ) ;
#39196=CARTESIAN_POINT ( 'NONE',  ( 6.951808397369818766E-16, 167.3437499965860127, -11.35316468750000141 ) ) ;
#39203=CARTESIAN_POINT ( 'NONE',  ( -11.35316468750000141, 53.48958332991935549, 3.042071309553159963 ) ) ;
#39205=CARTESIAN_POINT ( 'NONE',  ( 5.000000000000001776, 27.70833332650536818, -8.660254037844389075 ) ) ;
#39211=CARTESIAN_POINT ( 'NONE',  ( 9.832129032723416984, 65.36458332991935549, 5.676582343750006032 ) ) ;
#39215=CARTESIAN_POINT ( 'NONE',  ( 0.000000000000000000, 300.0000000000000000, 0.000000000000000000 ) ) ;
#39218=CARTESIAN_POINT ( 'NONE',  ( 8.311093377946837890, 41.40624999658601268, -8.311093377946837890 ) ) ;
#39220=CARTESIAN_POINT ( 'NONE',  ( 9.999999999999998224, 205.2083333333333712, -2.679491924311226292 ) ) ;
#39221=CARTESIAN_POINT ( 'NONE',  ( -3.042071309553173730, 174.3229166632526983, 11.35316468749999785 ) ) ;
#39222=CARTESIAN_POINT ( 'NONE',  ( 10.00000000000000178, 136.8749999931720538, 0.000000000000000000 ) ) ;
#39225=CARTESIAN_POINT ( 'NONE',  ( -11.35316468750000141, 33.59374999658601268, -1.390361679473963753E-15 ) ) ;
#39227=CARTESIAN_POINT ( 'NONE',  ( -11.35316468750000141, 163.2812499965860127, -1.390361679473963753E-15 ) ) ;
#39233=CARTESIAN_POINT ( 'NONE',  ( -8.660254037844390851, 7.083333333333338366, -5.000000000000007994 ) ) ;
#39234=CARTESIAN_POINT ( 'NONE',  ( 11.35316468749999785, 160.5729166632526983, 3.042071309553174174 ) ) ;
#39243=CARTESIAN_POINT ( 'NONE',  ( 5.676582343750001591, 121.9270833299193413, -9.832129032723420536 ) ) ;
#39244=CARTESIAN_POINT ( 'NONE',  ( 5.000000000000001776, 12.70833332650536640, -8.660254037844389075 ) ) ;
#39254=( BOUNDED_CURVE ( )  B_SPLINE_CURVE ( 2, ( #72033, #22591, #56947, #62583, #45611, #33207, #61851, #28264, #27887, #10171, #62963, #50156, #39959 ),
 .UNSPECIFIED., .F., .F. ) 
 B_SPLINE_CURVE_WITH_KNOTS ( ( 3, 2, 2, 2, 2, 2, 3 ),
 ( 0.1412976416564819815, 0.1465300236806699186, 0.1517624057048578279, 0.1569947877290457372, 0.1622271697532336743, 0.1674595517774215836, 0.1726919338016095207 ),
 .UNSPECIFIED. ) 
 CURVE ( )  GEOMETRIC_REPRESENTATION_ITEM ( )  RATIONAL_B_SPLINE_CURVE ( ( 0.9999999999999994449, 0.9659258262890690894, 1.000000000000000000, 0.9659258262890684232, 1.000000000000000000, 0.9659258262890684232, 1.000000000000000000, 0.9659258262890684232, 1.000000000000000000, 0.9659258262890684232, 1.000000000000000000, 0.9659258262892563840, 0.9999999999998120392 ) ) 
 REPRESENTATION_ITEM ( '' )  );
#39262=DIRECTION ( 'NONE',  ( -0.000000000000000000, 1.000000000000000000, -0.000000000000000000 ) ) ;
#39274=CARTESIAN_POINT ( 'NONE',  ( -8.660254037844394404, 127.9166666666666856, 5.000000000000001776 ) ) ;
#39275=CARTESIAN_POINT ( 'NONE',  ( -7.320508075688778149, 118.1250000000000000, 7.320508075688769267 ) ) ;
#39291=CARTESIAN_POINT ( 'NONE',  ( 8.311093377946837890, 16.40624999658601268, -8.311093377946837890 ) ) ;
#39294=CARTESIAN_POINT ( 'NONE',  ( -11.35316468749999785, 203.3854166632526983, -3.042071309553167513 ) ) ;
#39295=LINE ( 'NONE', #3851, #35917 ) ;
#39298=CYLINDRICAL_SURFACE ( 'NONE', #35139, 10.00000000000000178 ) ;
#39303=CARTESIAN_POINT ( 'NONE',  ( -5.676582343750006032, 4.114583329919349275, 9.832129032723418760 ) ) ;
#39305=AXIS2_PLACEMENT_3D ( 'NONE', #49993, #72640, #20943 ) ;
#39310=CARTESIAN_POINT ( 'NONE',  ( -11.35316468749999785, 3.072916663252683200, -3.042071309553167957 ) ) ;
#39312=CARTESIAN_POINT ( 'NONE',  ( 11.35316468750000141, 135.7812499965860411, 0.000000000000000000 ) ) ;
#39314=CARTESIAN_POINT ( 'NONE',  ( 8.660254037844385522, 96.45833332650536818, 5.000000000000005329 ) ) ;
#39317=CARTESIAN_POINT ( 'NONE',  ( -8.660254037844387298, 3.958333326505365957, -5.000000000000004441 ) ) ;
#39321=CARTESIAN_POINT ( 'NONE',  ( -6.676582343750000703, 289.6718750017070079, 2.765530957082001251 ) ) ;
#39332=CARTESIAN_POINT ( 'NONE',  ( 8.311093377946837890, 81.71874999658601268, -8.311093377946837890 ) ) ;
#39333=ORIENTED_EDGE ( 'NONE', *, *, #9760, .F. ) ;
#39338=CARTESIAN_POINT ( 'NONE',  ( 7.320508075688771044, 114.3750000000000142, 7.320508075688774596 ) ) ;
#39353=ORIENTED_EDGE ( 'NONE', *, *, #70739, .F. ) ;
#39360=CARTESIAN_POINT ( 'NONE',  ( 10.00000000000000178, 85.20833333333334281, -2.679491924311226736 ) ) ;
#39363=CARTESIAN_POINT ( 'NONE',  ( -2.485281374238572649, 294.1875000000000000, 6.000000000000002665 ) ) ;
#39375=CARTESIAN_POINT ( 'NONE',  ( -7.320508075688773708, 201.8749999999999716, -7.320508075688774596 ) ) ;
#39378=CARTESIAN_POINT ( 'NONE',  ( -2.085542519210945728E-15, 164.8437499965860127, 11.35316468750000141 ) ) ;
#39382=CARTESIAN_POINT ( 'NONE',  ( -3.673940397442060854E-16, 296.8125000034140157, -6.000000000000001776 ) ) ;
#39384=CARTESIAN_POINT ( 'NONE',  ( 11.35316468750000141, 21.09374999658601624, 0.000000000000000000 ) ) ;
#39391=CARTESIAN_POINT ( 'NONE',  ( -10.00000000000000178, 64.37499999317203958, -1.224646799147353454E-15 ) ) ;
#39394=CARTESIAN_POINT ( 'NONE',  ( 8.660254037844433483, 65.41666666666669983, -5.000000000000025757 ) ) ;
#39403=CARTESIAN_POINT ( 'NONE',  ( -3.042071309553173730, 144.3229166632527267, 11.35316468749999785 ) ) ;
#39415=EDGE_CURVE ( 'NONE', #29697, #41900, #41482, .T. ) ;
#39418=CARTESIAN_POINT ( 'NONE',  ( -11.35316468750000141, 128.5937499965860127, -1.390361679473963753E-15 ) ) ;
#39422=CARTESIAN_POINT ( 'NONE',  ( 11.35316468750000141, 41.09374999658601979, 0.000000000000000000 ) ) ;
#39429=CARTESIAN_POINT ( 'NONE',  ( 4.242640687119285658, 297.6875000034139589, -4.242640687119286547 ) ) ;
#39431=CARTESIAN_POINT ( 'NONE',  ( 3.042071309553159519, 150.0520833299193555, 11.35316468750000141 ) ) ;
#39444=CARTESIAN_POINT ( 'NONE',  ( -2.679491924311382611, 210.4166666598386541, 9.999999999999914735 ) ) ;
#39447=CARTESIAN_POINT ( 'NONE',  ( 10.00000000000000178, 40.00000000000000000, 0.000000000000000000 ) ) ;
#39459=CYLINDRICAL_SURFACE ( 'NONE', #4622, 6.000000000000001776 ) ;
#39463=EDGE_CURVE ( 'NONE', #61990, #60693, #65585, .T. ) ;
#39464=CARTESIAN_POINT ( 'NONE',  ( 8.660254037844389075, 165.4166666666666856, -5.000000000000000000 ) ) ;
#39465=CARTESIAN_POINT ( 'NONE',  ( -1.224646799147353454E-15, 225.9999999999999432, 10.00000000000000178 ) ) ;
#39468=CARTESIAN_POINT ( 'NONE',  ( -5.676582343749998039, 127.7604166632526841, -9.832129032723420536 ) ) ;
#39475=CARTESIAN_POINT ( 'NONE',  ( 9.910777348998651703, 225.1079956670950821, -1.365085748358755735 ) ) ;
#39481=CARTESIAN_POINT ( 'NONE',  ( -8.311093377946836114, 207.9687499965859843, -8.311093377946837890 ) ) ;
#39488=CARTESIAN_POINT ( 'NONE',  ( -11.35316468750000141, 93.48958332991934128, 3.042071309553159963 ) ) ;
#39496=CARTESIAN_POINT ( 'NONE',  ( -3.042071309553164404, 102.2395833299193697, -11.35316468749999963 ) ) ;
#39497=VERTEX_POINT ( 'NONE', #3264 ) ;
#39500=CARTESIAN_POINT ( 'NONE',  ( -8.660254037844390851, 219.7916666598387110, 4.999999999999998224 ) ) ;
#39504=CARTESIAN_POINT ( 'NONE',  ( -11.35316468749999785, 93.07291666325268409, -3.042071309553167957 ) ) ;
#39509=CARTESIAN_POINT ( 'NONE',  ( 10.00000000000000178, 181.8749999931720538, 0.000000000000000000 ) ) ;
#39510=EDGE_CURVE ( 'NONE', #9276, #41900, #38342, .T. ) ;
#39513=CARTESIAN_POINT ( 'NONE',  ( -9.832129032723420536, 74.01041666325268409, 5.676582343749997150 ) ) ;
#39514=CARTESIAN_POINT ( 'NONE',  ( 4.721056650415999201, 290.0781250017069510, -4.721056650415999201 ) ) ;
#39517=CARTESIAN_POINT ( 'NONE',  ( 3.042071309553159519, 219.7395833299193271, 11.35316468750000141 ) ) ;
#39522=CARTESIAN_POINT ( 'NONE',  ( -3.042071309553163960, 207.2395833299193839, -11.35316468749999963 ) ) ;
#39525=CARTESIAN_POINT ( 'NONE',  ( 2.765530957081996366, 297.1406250017070079, -6.676582343750003368 ) ) ;
#39527=AXIS2_PLACEMENT_3D ( 'NONE', #24536, #18518, #9050 ) ;
#39528=CARTESIAN_POINT ( 'NONE',  ( 8.311093377946834337, 200.4687499965860411, 8.311093377946839666 ) ) ;
#39536=CARTESIAN_POINT ( 'NONE',  ( 10.00000000000000178, 20.00000000000000000, 0.000000000000000000 ) ) ;
#39539=ORIENTED_EDGE ( 'NONE', *, *, #5394, .T. ) ;
#39555=ADVANCED_FACE ( 'NONE', ( #62089 ), #67381, .T. ) ;
#39558=CARTESIAN_POINT ( 'NONE',  ( -11.35316468749999785, 83.38541666325265567, -3.042071309553167513 ) ) ;
#39559=DIRECTION ( 'NONE',  ( 0.000000000000000000, 0.000000000000000000, 1.000000000000000000 ) ) ;
#39563=CARTESIAN_POINT ( 'NONE',  ( 4.721056650415999201, 290.2343750017069510, -4.721056650415999201 ) ) ;
#39565=CARTESIAN_POINT ( 'NONE',  ( 9.832129032723416984, 200.3645833299193555, 5.676582343750006032 ) ) ;
#39567=ORIENTED_EDGE ( 'NONE', *, *, #5842, .T. ) ;
#39571=CARTESIAN_POINT ( 'NONE',  ( 6.951808397369818766E-16, 162.3437499965860127, -11.35316468750000141 ) ) ;
#39578=CARTESIAN_POINT ( 'NONE',  ( 11.35316468749999785, 50.57291666325268409, 3.042071309553174174 ) ) ;
#39583=CARTESIAN_POINT ( 'NONE',  ( -3.042071309553164404, 57.23958332991934839, -11.35316468749999963 ) ) ;
#39589=CARTESIAN_POINT ( 'NONE',  ( -8.311093377946836114, 42.65624999658600558, -8.311093377946837890 ) ) ;
#39591=CARTESIAN_POINT ( 'NONE',  ( 2.997893585525398702E-11, 31.24999999999767653, -10.00000000000000178 ) ) ;
#39592=( BOUNDED_CURVE ( )  B_SPLINE_CURVE ( 2, ( #42623, #26768, #54709, #26376, #19980, #31308, #54336, #19242, #13570 ),
 .UNSPECIFIED., .F., .F. ) 
 B_SPLINE_CURVE_WITH_KNOTS ( ( 3, 2, 2, 2, 3 ),
 ( 0.06249999999999773792, 0.07291666666666440921, 0.08333333333333108051, 0.09374999999999775180, 0.1041666666666644370 ),
 .UNSPECIFIED. ) 
 CURVE ( )  GEOMETRIC_REPRESENTATION_ITEM ( )  RATIONAL_B_SPLINE_CURVE ( ( 1.000000000000016431, 0.9238795325112701962, 1.000000000000000000, 0.9238795325112867385, 1.000000000000000000, 0.9238795325112867385, 1.000000000000000000, 0.9238795325113030588, 0.9999999999999836797 ) ) 
 REPRESENTATION_ITEM ( '' )  );
#39593=CARTESIAN_POINT ( 'NONE',  ( 11.35316468749999785, 175.5729166632526415, 3.042071309553174174 ) ) ;
#39594=CARTESIAN_POINT ( 'NONE',  ( 10.00000000000000178, 142.0833333265053966, -2.679491924311226736 ) ) ;
#39597=CARTESIAN_POINT ( 'NONE',  ( -3.042071309553173730, 34.63541666325269119, 11.35316468749999785 ) ) ;
#39598=CARTESIAN_POINT ( 'NONE',  ( -8.660254037844387298, 78.95833332650536818, -5.000000000000004441 ) ) ;
#39599=CARTESIAN_POINT ( 'NONE',  ( 11.35316468750000141, 185.7812499965860411, 0.000000000000000000 ) ) ;
#39606=CARTESIAN_POINT ( 'NONE',  ( 3.042071309553159519, 164.7395833299193271, 11.35316468750000141 ) ) ;
#39608=CARTESIAN_POINT ( 'NONE',  ( 2.249999999999997335, 255.9999999999998295, 5.427273999917215264 ) ) ;
#39614=DIRECTION ( 'NONE',  ( -0.000000000000000000, 1.000000000000000000, -0.000000000000000000 ) ) ;
#39615=CARTESIAN_POINT ( 'NONE',  ( -11.35316468749999785, 113.3854166632526841, -3.042071309553167513 ) ) ;
#39616=CARTESIAN_POINT ( 'NONE',  ( 7.320508075688771044, 11.24999999317203248, 7.320508075688775484 ) ) ;
#39622=EDGE_CURVE ( 'NONE', #16277, #49691, #47307, .T. ) ;
#39625=EDGE_CURVE ( 'NONE', #1761, #44090, #55031, .T. ) ;
#39636=CARTESIAN_POINT ( 'NONE',  ( 6.123233995736767268E-16, 113.1249999931720396, -10.00000000000000178 ) ) ;
#39647=CARTESIAN_POINT ( 'NONE',  ( -2.679491924311225848, 121.4583333333333428, -10.00000000000000178 ) ) ;
#39649=CARTESIAN_POINT ( 'NONE',  ( 1.226468279477575784E-15, 287.8593750017070079, 6.676582343750001591 ) ) ;
#39651=DIRECTION ( 'NONE',  ( -0.000000000000000000, 1.000000000000000000, -0.000000000000000000 ) ) ;
#39659=CARTESIAN_POINT ( 'NONE',  ( -5.000000000000005329, 215.2083333265053682, 8.660254037844387298 ) ) ;
#39661=CARTESIAN_POINT ( 'NONE',  ( -2.085542519210945728E-15, 19.53124999658601979, 11.35316468750000141 ) ) ;
#39663=CARTESIAN_POINT ( 'NONE',  ( 11.35316468749999963, 211.3020833299193839, -3.042071309553165293 ) ) ;
#39664=CARTESIAN_POINT ( 'NONE',  ( -4.999999999999998224, 133.5416666598387110, -8.660254037844389075 ) ) ;
#39669=CARTESIAN_POINT ( 'NONE',  ( 8.311093377946837890, 21.40624999658601268, -8.311093377946837890 ) ) ;
#39671=DIRECTION ( 'NONE',  ( 0.000000000000000000, 0.000000000000000000, 1.000000000000000000 ) ) ;
#39675=CARTESIAN_POINT ( 'NONE',  ( 8.311093377946837890, 6.406249996586016238, -8.311093377946837890 ) ) ;
#39677=CARTESIAN_POINT ( 'NONE',  ( 3.042071309553167069, 136.8229166632526699, -11.35316468749999785 ) ) ;
#39678=CARTESIAN_POINT ( 'NONE',  ( -2.679491924311235618, 105.4166666598387110, 10.00000000000000000 ) ) ;
#39680=CARTESIAN_POINT ( 'NONE',  ( -2.679491924311235174, 5.416666659838698550, 10.00000000000000000 ) ) ;
#39684=CARTESIAN_POINT ( 'NONE',  ( 6.123233995736767268E-16, 153.1249999931720538, -10.00000000000000178 ) ) ;
#39685=CARTESIAN_POINT ( 'NONE',  ( 6.676582343750004256, 289.0468750017070079, 2.765530957081995478 ) ) ;
#39693=CARTESIAN_POINT ( 'NONE',  ( 8.660254037844385522, 216.4583333265053682, 5.000000000000005329 ) ) ;
#39694=CARTESIAN_POINT ( 'NONE',  ( -15.99999999999998579, 237.9999999999999716, 0.000000000000000000 ) ) ;
#39696=CARTESIAN_POINT ( 'NONE',  ( 11.35316468749999963, 81.30208332991935549, -3.042071309553165293 ) ) ;
#39697=( BOUNDED_CURVE ( )  B_SPLINE_CURVE ( 2, ( #7357, #12995, #47337, #23960, #46967, #52641, #54120, #19395, #71078, #25049, #12271, #70718, #69997 ),
 .UNSPECIFIED., .F., .F. ) 
 B_SPLINE_CURVE_WITH_KNOTS ( ( 3, 2, 2, 2, 2, 2, 3 ),
 ( 0.3097826086956522174, 0.3115942028985507761, 0.3134057971014493349, 0.3152173913043478937, 0.3170289855072464524, 0.3188405797101449557, 0.3206521739130435145 ),
 .UNSPECIFIED. ) 
 CURVE ( )  GEOMETRIC_REPRESENTATION_ITEM ( )  RATIONAL_B_SPLINE_CURVE ( ( 0.9999999999999990008, 0.9659258262890693114, 1.000000000000000000, 0.9659258262890683122, 1.000000000000000000, 0.9659258262890683122, 1.000000000000000000, 0.9659258262890683122, 1.000000000000000000, 0.9659258262890683122, 1.000000000000000000, 0.9659258262890673130, 1.000000000000001110 ) ) 
 REPRESENTATION_ITEM ( '' )  );
#39703=CARTESIAN_POINT ( 'NONE',  ( 8.660254037844385522, 114.5833333333333712, 5.000000000000005329 ) ) ;
#39709=CARTESIAN_POINT ( 'NONE',  ( 8.660254037844380193, 109.5833333333333428, 5.000000000000002665 ) ) ;
#39718=AXIS2_PLACEMENT_3D ( 'NONE', #29107, #50619, #63058 ) ;
#39723=ORIENTED_EDGE ( 'NONE', *, *, #21735, .F. ) ;
#39727=CARTESIAN_POINT ( 'NONE',  ( -10.00000000000000178, 87.50000000000001421, -1.224646799147353454E-15 ) ) ;
#39730=CARTESIAN_POINT ( 'NONE',  ( 4.721056650415999201, 298.2343750017069510, -4.721056650415999201 ) ) ;
#39731=ADVANCED_FACE ( 'NONE', ( #46224 ), #7720, .T. ) ;
#39740=CARTESIAN_POINT ( 'NONE',  ( 7.320508075688771044, 204.3750000000000000, 7.320508075688775484 ) ) ;
#39742=CARTESIAN_POINT ( 'NONE',  ( 9.832129032723420536, 166.5104166632526983, -5.676582343749999815 ) ) ;
#39744=CARTESIAN_POINT ( 'NONE',  ( -1.836970198721029983E-15, 175.6249999931720538, 10.00000000000000178 ) ) ;
#39747=CARTESIAN_POINT ( 'NONE',  ( -11.35316468749999785, 28.38541666325268054, -3.042071309553167513 ) ) ;
#39751=CARTESIAN_POINT ( 'NONE',  ( 0.000000000000000000, 300.0000000000000000, 0.000000000000000000 ) ) ;
#39755=CARTESIAN_POINT ( 'NONE',  ( 10.00000000000000000, 66.66666665983871098, 2.679491924311236062 ) ) ;
#39758=CARTESIAN_POINT ( 'NONE',  ( 10.00000000000022204, 215.2083333333334849, -2.679491924311286688 ) ) ;
#39767=CARTESIAN_POINT ( 'NONE',  ( -9.832129032723418760, 147.8645833299193555, -5.676582343750004256 ) ) ;
#39770=CARTESIAN_POINT ( 'NONE',  ( 0.000000000000000000, 300.0000000000000000, 10.00000000000000178 ) ) ;
#39779=CARTESIAN_POINT ( 'NONE',  ( -8.311093377946841443, 129.2187499965860127, 8.311093377946834337 ) ) ;
#39783=CARTESIAN_POINT ( 'NONE',  ( -9.832129032723420536, 34.01041666325269119, 5.676582343749997150 ) ) ;
#39790=EDGE_CURVE ( 'NONE', #26710, #3422, #30724, .T. ) ;
#39792=CARTESIAN_POINT ( 'NONE',  ( 4.242640687119287435, 296.4375000034140157, 4.242640687119285658 ) ) ;
#39795=CARTESIAN_POINT ( 'NONE',  ( -5.676582343750006032, 159.4270833299193555, 9.832129032723418760 ) ) ;
#39801=EDGE_CURVE ( 'NONE', #61049, #64051, #57461, .T. ) ;
#39807=EDGE_CURVE ( 'NONE', #29212, #28203, #5898, .T. ) ;
#39808=CARTESIAN_POINT ( 'NONE',  ( -2.679491924311247164, 56.45833333333338544, -10.00000000000007994 ) ) ;
#39813=DIRECTION ( 'NONE',  ( -0.000000000000000000, -0.000000000000000000, 1.000000000000000000 ) ) ;
#39814=CARTESIAN_POINT ( 'NONE',  ( -10.00000000000000000, 37.29166666666667140, -2.679491924311229845 ) ) ;
#39827=CARTESIAN_POINT ( 'NONE',  ( -1.967015505459129087E-11, 148.7499999999984936, 10.00000000000000533 ) ) ;
#39828=DIRECTION ( 'NONE',  ( -0.000000000000000000, 1.000000000000000000, -0.000000000000000000 ) ) ;
#39829=CARTESIAN_POINT ( 'NONE',  ( 10.00000000000000000, 159.7916666666666288, 2.679491924311236062 ) ) ;
#39833=CARTESIAN_POINT ( 'NONE',  ( -9.832129032723420536, 134.0104166632526983, 5.676582343749997150 ) ) ;
#39842=CARTESIAN_POINT ( 'NONE',  ( 8.218888959140699058, 225.4831672038039585, -5.726997447258057150 ) ) ;
#39847=CARTESIAN_POINT ( 'NONE',  ( -11.35316468750000141, 218.5937499965860411, -1.390361679473963753E-15 ) ) ;
#39854=CARTESIAN_POINT ( 'NONE',  ( -9.832129032723420536, 98.69791666325269830, 5.676582343749997150 ) ) ;
#39860=CARTESIAN_POINT ( 'NONE',  ( 8.311093377946834337, 100.1562499965860127, 8.311093377946839666 ) ) ;
#39865=CARTESIAN_POINT ( 'NONE',  ( -7.320508075688778149, 214.9999999931720254, 7.320508075688769267 ) ) ;
#39869=CARTESIAN_POINT ( 'NONE',  ( 3.042071309553167513, 101.8229166632526699, -11.35316468749999785 ) ) ;
#39872=CARTESIAN_POINT ( 'NONE',  ( 7.320508075688834992, 174.3750000000000284, 7.320508075688839433 ) ) ;
#39874=CARTESIAN_POINT ( 'NONE',  ( 5.000000000000001776, 177.7083333265053682, -8.660254037844389075 ) ) ;
#39877=CARTESIAN_POINT ( 'NONE',  ( 8.311093377946837890, 91.71874999658601268, -8.311093377946837890 ) ) ;
#39878=CARTESIAN_POINT ( 'NONE',  ( 6.676582343750001591, 290.9531250017069510, -8.176455196517173205E-16 ) ) ;
#39881=CARTESIAN_POINT ( 'NONE',  ( -8.311093377946836114, 217.6562499965860127, -8.311093377946837890 ) ) ;
#39885=CARTESIAN_POINT ( 'NONE',  ( 11.35316468750000141, 225.7812499965860127, 0.000000000000000000 ) ) ;
#39886=CARTESIAN_POINT ( 'NONE',  ( 6.123233995736767268E-16, 123.1249999931720396, -10.00000000000000178 ) ) ;
#39887=CARTESIAN_POINT ( 'NONE',  ( 2.679491924302094485, 198.9583333333325186, 10.00000000000527400 ) ) ;
#39888=CARTESIAN_POINT ( 'NONE',  ( -6.676582343750003368, 298.3906250017070079, -2.765530957081996810 ) ) ;
#39889=ORIENTED_EDGE ( 'NONE', *, *, #57548, .F. ) ;
#39890=CARTESIAN_POINT ( 'NONE',  ( -8.311093377946841443, 209.2187499965859843, 8.311093377946834337 ) ) ;
#39899=CARTESIAN_POINT ( 'NONE',  ( 6.123233995736767268E-16, 21.25000000000000000, -10.00000000000000178 ) ) ;
#39904=VERTEX_POINT ( 'NONE', #49179 ) ;
#39912=CARTESIAN_POINT ( 'NONE',  ( 8.660254037844385522, 71.45833332650538239, 5.000000000000005329 ) ) ;
#39922=EDGE_CURVE ( 'NONE', #9475, #28855, #36762, .T. ) ;
#39926=CARTESIAN_POINT ( 'NONE',  ( 11.35316468749999963, 91.30208332991934128, -3.042071309553165293 ) ) ;
#39931=CARTESIAN_POINT ( 'NONE',  ( 10.00000000000000178, 69.79166666666665719, 2.679491924311236062 ) ) ;
#39934=CARTESIAN_POINT ( 'NONE',  ( -3.042071309553173730, 199.3229166632526983, 11.35316468749999785 ) ) ;
#39939=CARTESIAN_POINT ( 'NONE',  ( -9.832129032723420536, 164.0104166632526983, 5.676582343749997150 ) ) ;
#39942=CARTESIAN_POINT ( 'NONE',  ( -7.320508075688773708, 208.1250000000000000, 7.320508075688764826 ) ) ;
#39947=CARTESIAN_POINT ( 'NONE',  ( 11.35316468750000141, 55.78124999658601268, 0.000000000000000000 ) ) ;
#39953=CARTESIAN_POINT ( 'NONE',  ( 6.123233995736767268E-16, 168.1249999931720538, -10.00000000000000178 ) ) ;
#39954=CARTESIAN_POINT ( 'NONE',  ( -2.085542519210945728E-15, 59.53124999658601979, 11.35316468750000141 ) ) ;
#39959=CARTESIAN_POINT ( 'NONE',  ( -1.903569318090136080E-11, 13.74999999999851852, 10.00000000000000178 ) ) ;
#39961=CARTESIAN_POINT ( 'NONE',  ( 9.832129032723420536, 66.19791666325268409, -5.676582343749999815 ) ) ;
#39964=CARTESIAN_POINT ( 'NONE',  ( 11.35316468750000141, 170.7812499965860411, 0.000000000000000000 ) ) ;
#39965=CARTESIAN_POINT ( 'NONE',  ( -10.00000000000000000, 139.1666666598387110, -2.679491924311229845 ) ) ;
#39967=( GEOMETRIC_REPRESENTATION_CONTEXT ( 3 ) GLOBAL_UNCERTAINTY_ASSIGNED_CONTEXT ( ( #6853 ) ) GLOBAL_UNIT_ASSIGNED_CONTEXT ( ( #3888, #27250, #61592 ) ) REPRESENTATION_CONTEXT ( 'NONE', 'WORKASPACE' ) );
#39968=CARTESIAN_POINT ( 'NONE',  ( 8.311093377946834337, 50.46874999658601979, 8.311093377946839666 ) ) ;
#39969=CARTESIAN_POINT ( 'NONE',  ( 6.000000000000001776, 295.5625000034140157, -7.347880794884121708E-16 ) ) ;
#39970=CARTESIAN_POINT ( 'NONE',  ( 6.951808397369818766E-16, 177.0312499965860411, -11.35316468750000141 ) ) ;
#39977=CARTESIAN_POINT ( 'NONE',  ( 8.311093377946837890, 181.4062499965860411, -8.311093377946837890 ) ) ;
#39983=ORIENTED_EDGE ( 'NONE', *, *, #30218, .T. ) ;
#39987=CARTESIAN_POINT ( 'NONE',  ( 5.676582343749993598, 115.2604166632526983, 9.832129032723422313 ) ) ;
#39991=CIRCLE ( 'NONE', #35165, 6.000000000000001776 ) ;
#39997=EDGE_CURVE ( 'NONE', #47712, #2022, #41575, .T. ) ;
#40002=ORIENTED_EDGE ( 'NONE', *, *, #49379, .T. ) ;
#40005=CARTESIAN_POINT ( 'NONE',  ( -3.673940397442060854E-16, 293.7500000000000000, -6.000000000000001776 ) ) ;
#40019=CARTESIAN_POINT ( 'NONE',  ( -4.999999999999998224, 116.6666666666666714, -8.660254037844389075 ) ) ;
#40021=CARTESIAN_POINT ( 'NONE',  ( 2.765530957082001251, 289.9218750017069510, 6.676582343750000703 ) ) ;
#40034=CARTESIAN_POINT ( 'NONE',  ( -9.832129032723420536, 8.697916663252684089, 5.676582343749997150 ) ) ;
#40036=CARTESIAN_POINT ( 'NONE',  ( -3.042071309553164404, 202.5520833299193839, -11.35316468749999963 ) ) ;
#40042=CARTESIAN_POINT ( 'NONE',  ( -11.35316468750000141, 28.28124999658601624, -1.390361679473963753E-15 ) ) ;
#40048=CARTESIAN_POINT ( 'NONE',  ( 6.951808397369818766E-16, 22.03124999658601624, -11.35316468750000141 ) ) ;
#40050=AXIS2_PLACEMENT_3D ( 'NONE', #39751, #29556, #46529 ) ;
#40051=CARTESIAN_POINT ( 'NONE',  ( 11.35316468749999963, 140.9895833299193555, -3.042071309553165293 ) ) ;
#40053=CARTESIAN_POINT ( 'NONE',  ( 2.679491924311228956, 97.91666665983871098, -10.00000000000000000 ) ) ;
#40061=CARTESIAN_POINT ( 'NONE',  ( 6.676582343750003368, 296.0156250017069510, -2.765530957081997254 ) ) ;
#40062=CARTESIAN_POINT ( 'NONE',  ( -5.676582343749998039, 132.4479166632526983, -9.832129032723420536 ) ) ;
#40063=FACE_OUTER_BOUND ( 'NONE', #57176, .T. ) ;
#40070=CARTESIAN_POINT ( 'NONE',  ( 0.000000000000000000, 300.0000000000000000, 0.000000000000000000 ) ) ;
#40072=CARTESIAN_POINT ( 'NONE',  ( -11.35316468750000141, 73.59374999658602690, -1.390361679473963753E-15 ) ) ;
#40077=ORIENTED_EDGE ( 'NONE', *, *, #38576, .F. ) ;
#40097=CARTESIAN_POINT ( 'NONE',  ( -3.673940397442060854E-16, 291.7500000000000000, -6.000000000000001776 ) ) ;
#40103=CARTESIAN_POINT ( 'NONE',  ( -4.999999999999998224, 76.66666666666667140, -8.660254037844389075 ) ) ;
#40105=CARTESIAN_POINT ( 'NONE',  ( 2.485281374238571317, 288.6875000000000568, -6.000000000000003553 ) ) ;
#40107=CARTESIAN_POINT ( 'NONE',  ( 4.242640687119285658, 294.6249999999999432, -4.242640687119286547 ) ) ;
#40110=CARTESIAN_POINT ( 'NONE',  ( 8.660254037844389075, 57.29166665983870388, -5.000000000000000000 ) ) ;
#40113=DIRECTION ( 'NONE',  ( -0.000000000000000000, 1.000000000000000000, -0.000000000000000000 ) ) ;
#40115=CARTESIAN_POINT ( 'NONE',  ( -10.00000000000000355, 197.7083333333332860, 2.679491924311223183 ) ) ;
#40117=CARTESIAN_POINT ( 'NONE',  ( -5.676582343750006032, 174.4270833299193555, 9.832129032723418760 ) ) ;
#40118=CARTESIAN_POINT ( 'NONE',  ( -7.320508075688776373, 38.12499999999999289, 7.320508075688768379 ) ) ;
#40122=ORIENTED_EDGE ( 'NONE', *, *, #54211, .F. ) ;
#40124=CARTESIAN_POINT ( 'NONE',  ( 5.676582343750001591, 31.92708332991935194, -9.832129032723420536 ) ) ;
#40128=FACE_OUTER_BOUND ( 'NONE', #16329, .T. ) ;
#40134=CARTESIAN_POINT ( 'NONE',  ( 7.320508075688771044, 56.24999999317203248, 7.320508075688775484 ) ) ;
#40137=CARTESIAN_POINT ( 'NONE',  ( 9.999999999999996447, 55.20833333333332860, -2.679491924311226292 ) ) ;
#40139=CARTESIAN_POINT ( 'NONE',  ( 4.999999999999993783, 101.0416666598386968, 8.660254037844390851 ) ) ;
#40145=CARTESIAN_POINT ( 'NONE',  ( 1.226468279477575784E-15, 295.8593750017070079, 6.676582343750001591 ) ) ;
#40148=CARTESIAN_POINT ( 'NONE',  ( -5.676582343749998039, 147.4479166632526983, -9.832129032723420536 ) ) ;
#40159=CARTESIAN_POINT ( 'NONE',  ( -8.311093377946836114, 132.9687499965860411, -8.311093377946837890 ) ) ;
#40162=AXIS2_PLACEMENT_3D ( 'NONE', #28511, #6262, #22097 ) ;
#40164=CARTESIAN_POINT ( 'NONE',  ( 11.35316468750000141, 31.09374999658601979, 0.000000000000000000 ) ) ;
#40171=CARTESIAN_POINT ( 'NONE',  ( -3.673940397442060854E-16, 295.8125000034140157, -6.000000000000001776 ) ) ;
#40175=CARTESIAN_POINT ( 'NONE',  ( 11.35316468749999785, 155.8854166632526699, 3.042071309553174174 ) ) ;
#40188=CARTESIAN_POINT ( 'NONE',  ( -4.242640687119286547, 297.9375000034140157, -4.242640687119286547 ) ) ;
#40189=CARTESIAN_POINT ( 'NONE',  ( -2.679491924311226292, 43.33333332650536107, -10.00000000000000178 ) ) ;
#40190=CARTESIAN_POINT ( 'NONE',  ( 7.320508075688774596, 45.62500000000000000, -7.320508075688774596 ) ) ;
#40194=CARTESIAN_POINT ( 'NONE',  ( -6.000000000000000888, 299.0625000000000000, 2.485281374238575758 ) ) ;
#40195=CARTESIAN_POINT ( 'NONE',  ( 3.153939666463669656E-13, 33.75000000000002842, 9.999999999999998224 ) ) ;
#40203=FACE_OUTER_BOUND ( 'NONE', #12141, .T. ) ;
#40204=CARTESIAN_POINT ( 'NONE',  ( 6.123233995736767268E-16, 161.2500000000000000, -10.00000000000000178 ) ) ;
#40207=CARTESIAN_POINT ( 'NONE',  ( 8.311093377946837890, 126.7187499965860269, -8.311093377946837890 ) ) ;
#40215=EDGE_CURVE ( 'NONE', #1694, #14172, #43165, .T. ) ;
#40216=CARTESIAN_POINT ( 'NONE',  ( 11.35316468749999963, 1.302083329919349941, -3.042071309553165293 ) ) ;
#40220=CARTESIAN_POINT ( 'NONE',  ( -8.311093377946836114, 222.9687499965860127, -8.311093377946837890 ) ) ;
#40227=CARTESIAN_POINT ( 'NONE',  ( -5.676582343750006032, 109.1145833299193555, 9.832129032723418760 ) ) ;
#40233=CARTESIAN_POINT ( 'NONE',  ( -5.676582343750006032, 104.1145833299193697, 9.832129032723418760 ) ) ;
#40238=CARTESIAN_POINT ( 'NONE',  ( 8.660254037844385522, 226.4583333265053966, 5.000000000000005329 ) ) ;
#40242=CARTESIAN_POINT ( 'NONE',  ( 5.676582343750001591, 101.6145833299193697, -9.832129032723420536 ) ) ;
#40245=CARTESIAN_POINT ( 'NONE',  ( 2.679491924310192008, 168.9583333333332291, 10.00000000000059863 ) ) ;
#40248=CARTESIAN_POINT ( 'NONE',  ( 8.660254037844389075, 197.2916666598387110, -5.000000000000000000 ) ) ;
#40251=CARTESIAN_POINT ( 'NONE',  ( -9.832129032723418760, 93.17708332991935549, -5.676582343750004256 ) ) ;
#40252=CARTESIAN_POINT ( 'NONE',  ( -4.088227598258586603E-16, 289.2031250017069510, -6.676582343750001591 ) ) ;
#40255=CARTESIAN_POINT ( 'NONE',  ( -8.311093377946841443, 223.9062499965860411, 8.311093377946830785 ) ) ;
#40257=FACE_OUTER_BOUND ( 'NONE', #36122, .T. ) ;
#40258=CARTESIAN_POINT ( 'NONE',  ( 3.042071309553159519, 219.7395833299193271, 11.35316468750000141 ) ) ;
#40260=CARTESIAN_POINT ( 'NONE',  ( 4.999999999999993783, 46.04166665983869677, 8.660254037844390851 ) ) ;
#40261=CARTESIAN_POINT ( 'NONE',  ( -7.320508075688773708, 98.74999999317202537, -7.320508075688774596 ) ) ;
#40262=CARTESIAN_POINT ( 'NONE',  ( 6.676582343750004256, 297.8906250017069510, 2.765530957081995478 ) ) ;
#40263=EDGE_CURVE ( 'NONE', #9014, #13929, #72969, .T. ) ;
#40266=CARTESIAN_POINT ( 'NONE',  ( -2.085542519210945728E-15, 204.8437499965860411, 11.35316468750000141 ) ) ;
#40272=PRODUCT_DEFINITION_CONTEXT ( 'detailed design', #70807, 'design' ) ;
#40274=CARTESIAN_POINT ( 'NONE',  ( -2.679491924311235618, 33.54166666666667140, 10.00000000000000000 ) ) ;
#40285=CARTESIAN_POINT ( 'NONE',  ( 2.765530957082001251, 297.7656250017069510, 6.676582343749999815 ) ) ;
#40295=CARTESIAN_POINT ( 'NONE',  ( -3.042071309553164404, 82.55208332991936970, -11.35316468749999963 ) ) ;
#40296=DIRECTION ( 'NONE',  ( 0.000000000000000000, 0.000000000000000000, 1.000000000000000000 ) ) ;
#40300=CARTESIAN_POINT ( 'NONE',  ( -6.676582343749999815, 287.6718750017070079, 2.765530957082001251 ) ) ;
#40306=CARTESIAN_POINT ( 'NONE',  ( -5.676582343749998039, 197.4479166632526983, -9.832129032723420536 ) ) ;
#40310=CARTESIAN_POINT ( 'NONE',  ( 3.042071309553159519, 180.0520833299193271, 11.35316468750000141 ) ) ;
#40313=CARTESIAN_POINT ( 'NONE',  ( -8.660254037844381969, 112.0833333333333286, -5.000000000000000888 ) ) ;
#40317=CARTESIAN_POINT ( 'NONE',  ( 5.676582343749993598, 49.94791666325268409, 9.832129032723422313 ) ) ;
#40323=CARTESIAN_POINT ( 'NONE',  ( -11.35316468750000141, 58.48958332991933418, 3.042071309553159963 ) ) ;
#40328=CARTESIAN_POINT ( 'NONE',  ( 5.676582343749993598, 59.94791666325268409, 9.832129032723422313 ) ) ;
#40333=CARTESIAN_POINT ( 'NONE',  ( -2.679491924311235618, 155.4166666598387394, 10.00000000000000000 ) ) ;
#40336=CARTESIAN_POINT ( 'NONE',  ( -10.00000000000000355, 54.58333332650536818, 2.679491924311223183 ) ) ;
#40337=CARTESIAN_POINT ( 'NONE',  ( 8.311093377946837890, 51.71874999658602690, -8.311093377946837890 ) ) ;
#40339=CARTESIAN_POINT ( 'NONE',  ( 11.35316468749999963, 175.9895833299193555, -3.042071309553165293 ) ) ;
#40340=VERTEX_POINT ( 'NONE', #42790 ) ;
#40345=CARTESIAN_POINT ( 'NONE',  ( 5.676582343749993598, 184.9479166632526983, 9.832129032723422313 ) ) ;
#40347=CARTESIAN_POINT ( 'NONE',  ( 2.250000000000000888, 272.7999999999997272, 5.427799975595259063 ) ) ;
#40350=ORIENTED_EDGE ( 'NONE', *, *, #15012, .F. ) ;
#40351=CARTESIAN_POINT ( 'NONE',  ( 8.311093377946837890, 171.7187499965860127, -8.311093377946837890 ) ) ;
#40352=EDGE_CURVE ( 'NONE', #31834, #57818, #25682, .T. ) ;
#40354=CARTESIAN_POINT ( 'NONE',  ( 5.676582343750001591, 131.9270833299193555, -9.832129032723420536 ) ) ;
#40365=( BOUNDED_CURVE ( )  B_SPLINE_CURVE ( 2, ( #9900, #26105, #55187, #32930, #67981, #55936, #43467, #72524, #61581, #66481, #38944, #38201, #32166 ),
 .UNSPECIFIED., .F., .F. ) 
 B_SPLINE_CURVE_WITH_KNOTS ( ( 3, 2, 2, 2, 2, 2, 3 ),
 ( 0.1576086956521739191, 0.1594202898550724501, 0.1612318840579710089, 0.1630434782608695676, 0.1648550724637681264, 0.1666666666666666574, 0.1684782608695652162 ),
 .UNSPECIFIED. ) 
 CURVE ( )  GEOMETRIC_REPRESENTATION_ITEM ( )  RATIONAL_B_SPLINE_CURVE ( ( 1.000000000000000000, 0.9659258262890683122, 1.000000000000000000, 0.9659258262890683122, 1.000000000000000000, 0.9659258262890683122, 1.000000000000000000, 0.9659258262890683122, 1.000000000000000000, 0.9659258262890683122, 1.000000000000000000, 0.9659258262890683122, 1.000000000000000000 ) ) 
 REPRESENTATION_ITEM ( '' )  );
#40374=AXIS2_PLACEMENT_3D ( 'NONE', #809, #22668, #6081 ) ;
#40387=CARTESIAN_POINT ( 'NONE',  ( -2.485281374238268004, 290.2500000034139589, 6.000000000000304645 ) ) ;
#40388=CARTESIAN_POINT ( 'NONE',  ( 4.721056650415999201, 298.2343750017069510, -4.721056650415999201 ) ) ;
#40389=ADVANCED_FACE ( 'NONE', ( #56741 ), #57110, .T. ) ;
#40390=CARTESIAN_POINT ( 'NONE',  ( 10.00000000000000000, 129.7916666666666856, 2.679491924311236062 ) ) ;
#40407=CARTESIAN_POINT ( 'NONE',  ( 5.676582343750001591, 21.61458332991935194, -9.832129032723420536 ) ) ;
#40410=CARTESIAN_POINT ( 'NONE',  ( -8.311093377946836114, 222.9687499965860127, -8.311093377946837890 ) ) ;
#40413=CARTESIAN_POINT ( 'NONE',  ( -7.320508075688892724, 41.87500000000009237, -7.320508075688893612 ) ) ;
#40416=CARTESIAN_POINT ( 'NONE',  ( 8.311093377946834337, 20.15624999658600913, 8.311093377946839666 ) ) ;
#40418=CARTESIAN_POINT ( 'NONE',  ( -5.000000000000008882, 153.3333333333333428, 8.660254037844392627 ) ) ;
#40421=CARTESIAN_POINT ( 'NONE',  ( 3.042071309553159519, 24.73958332991934839, 11.35316468750000141 ) ) ;
#40423=CARTESIAN_POINT ( 'NONE',  ( -11.35316468750000141, 133.4895833299193839, 3.042071309553159963 ) ) ;
#40424=CARTESIAN_POINT ( 'NONE',  ( 6.123233995736767268E-16, 108.1249999931720396, -10.00000000000000178 ) ) ;
#40430=CARTESIAN_POINT ( 'NONE',  ( 9.832129032723416984, 10.67708332991935016, 5.676582343750006032 ) ) ;
#40431=CARTESIAN_POINT ( 'NONE',  ( -10.00000000000000355, 154.5833333265053682, 2.679491924311223183 ) ) ;
#40432=CARTESIAN_POINT ( 'NONE',  ( 4.721056650416000089, 296.8281250017069510, 4.721056650415999201 ) ) ;
#40433=CARTESIAN_POINT ( 'NONE',  ( -8.311093377946841443, 143.9062499965860127, 8.311093377946834337 ) ) ;
#40436=CARTESIAN_POINT ( 'NONE',  ( 0.000000000000000000, 300.0000000000000000, 0.000000000000000000 ) ) ;
#40441=ADVANCED_FACE ( 'NONE', ( #22378 ), #27304, .T. ) ;
#40445=CARTESIAN_POINT ( 'NONE',  ( -11.35316468750000141, 83.80208332991934128, 3.042071309553159963 ) ) ;
#40452=CARTESIAN_POINT ( 'NONE',  ( -3.673940397442060854E-16, 292.8125000034140157, -6.000000000000001776 ) ) ;
#40475=CARTESIAN_POINT ( 'NONE',  ( 10.00000000000000178, 80.20833333333334281, -2.679491924311226736 ) ) ;
#40477=CARTESIAN_POINT ( 'NONE',  ( 9.832129032723416984, 60.67708332991934839, 5.676582343750006032 ) ) ;
#40478=CARTESIAN_POINT ( 'NONE',  ( -4.242640687119286547, 288.8750000000000000, -4.242640687119286547 ) ) ;
#40480=ORIENTED_EDGE ( 'NONE', *, *, #58228, .T. ) ;
#40487=CARTESIAN_POINT ( 'NONE',  ( 1.102182119232618108E-15, 293.2500000000000000, 6.000000000000001776 ) ) ;
#40489=CARTESIAN_POINT ( 'NONE',  ( 6.123233995736767268E-16, 196.2500000000000000, -10.00000000000000178 ) ) ;
#40492=CARTESIAN_POINT ( 'NONE',  ( -2.085542519210945728E-15, 184.8437499965860411, 11.35316468750000141 ) ) ;
#40493=CARTESIAN_POINT ( 'NONE',  ( -8.660254037844579145, 212.0833333333334565, -5.000000000000115463 ) ) ;
#40495=CARTESIAN_POINT ( 'NONE',  ( -1.836970198721029983E-15, 85.62499999317203958, 10.00000000000000178 ) ) ;
#40498=CARTESIAN_POINT ( 'NONE',  ( -11.35316468750000141, 33.59374999658601268, -1.390361679473963753E-15 ) ) ;
#40508=CARTESIAN_POINT ( 'NONE',  ( 2.679491924311228956, 67.91666665983868256, -10.00000000000000000 ) ) ;
#40511=CARTESIAN_POINT ( 'NONE',  ( 8.660254037844579145, 215.4166666666667993, -5.000000000000111022 ) ) ;
#40517=CARTESIAN_POINT ( 'NONE',  ( 2.765530957081996366, 299.2968750017070079, -6.676582343750003368 ) ) ;
#40518=CARTESIAN_POINT ( 'NONE',  ( 7.320508075688774596, 42.49999999317203248, -7.320508075688774596 ) ) ;
#40519=CARTESIAN_POINT ( 'NONE',  ( 5.676582343749993598, 149.9479166632526983, 9.832129032723422313 ) ) ;
#40528=CARTESIAN_POINT ( 'NONE',  ( -11.35316468750000141, 123.5937499965860269, -1.390361679473963753E-15 ) ) ;
#40532=CARTESIAN_POINT ( 'NONE',  ( -11.35316468750000141, 38.80208332991934839, 3.042071309553159963 ) ) ;
#40539=CARTESIAN_POINT ( 'NONE',  ( 6.000000000000003553, 296.5000000034139589, 2.485281374238571317 ) ) ;
#40544=CARTESIAN_POINT ( 'NONE',  ( -9.832129032723418760, 153.1770833299193555, -5.676582343750004256 ) ) ;
#40563=CARTESIAN_POINT ( 'NONE',  ( -1.836970198721029983E-15, 210.6249999931720538, 10.00000000000000178 ) ) ;
#40565=CARTESIAN_POINT ( 'NONE',  ( -2.679491924311235618, 43.54166666666667140, 10.00000000000000000 ) ) ;
#40569=CARTESIAN_POINT ( 'NONE',  ( 10.00000000000000178, 197.0833333265053398, -2.679491924311226736 ) ) ;
#40570=EDGE_LOOP ( 'NONE', ( #43635, #11583, #25844, #18924 ) ) ;
#40573=CARTESIAN_POINT ( 'NONE',  ( -10.00000000000000178, 9.374999993172032475, -1.224646799147353454E-15 ) ) ;
#40576=CARTESIAN_POINT ( 'NONE',  ( 6.123233995736767268E-16, 203.1249999931720538, -10.00000000000000178 ) ) ;
#40577=( BOUNDED_SURFACE ( )  B_SPLINE_SURFACE ( 1, 2, ( 
 ( #58994, #58621, #6563, #24266, #23157, #40517, #17872, #46169, #69187, #52953, #64269, #5822, #181, #53326, #58261, #6927, #17499, #52214, #41261, #63521, #34881, #24631, #28818, #12577, #11844, #7299, #35606, #29570, #35244, #547, #47642, #57516, #18618, #57886, #51835, #52580, #1287, #23529, #6193, #12938, #46543, #69561, #1650, #34512, #11477, #18245, #40889, #63895, #12206, #29938, #70664, #918, #23903, #47277, #46912, #41629, #69937, #70303, #64640, #35975, #40145, #63150, #2005, #43470, #14041, #25368, #24995, #3496, #13671, #66111, #60080, #20452, #48012, #2748, #31038, #48385, #8781, #71388, #71024, #66484, #37077, #19713, #19342, #26484, #36710, #14420, #59357, #7669, #54440, #54814, #31793, #3125, #2372, #20081, #30675, #37453, #26108, #49129, #60451, #72140, #25735, #8400, #42725, #42355, #65371, #59722, #32170, #14793, #31413, #49509, #48756, #37832, #53694, #60829, #9153, #8030, #54063, #71764, #65739, #43094, #55190, #18982, #41985, #64996, #36342, #13305, #32933, #72901, #56301, #44606, #72528, #28363, #22315, #10645, #44236, #33676, #62685, #15174, #43853, #27238, #9903, #11022, #4617, #56680, #16653, #16279, #38947, #4997, #55563, #21209, #50254, #3876, #26872, #27996, #21951, #38205, #32553, #34056, #15916, #39321, #49886, #55939, #73644, #67249, #15543, #57051, #61209, #44979, #38583, #39685, #67984, #61948, #67620, #61584, #5363, #9539, #51005, #4251, #73276, #10276, #74014, #21580, #33303, #45341, #27615, #50625, #20836, #66866, #62319, #68359, #63066, #34424, #69103 ),
 ( #29113, #18532, #70222, #12851, #11388, #58177, #64187, #46824, #51747, #34796, #8227, #46458, #96, #69476, #5733, #51372, #35890, #69849, #52132, #23821, #47191, #57426, #35522, #17410, #12492, #6483, #29486, #41539, #58534, #6841, #52867, #17036, #18161, #41177, #465, #29856, #35161, #23443, #52496, #1199, #24180, #64555, #40432, #63432, #58907, #834, #11759, #28731, #23074, #46084, #17787, #57801, #74382, #40800, #63807, #40061, #22693, #6108, #12123, #45711, #68723, #38776, #54634, #25562, #60653, #48948, #71585, #61402, #55758, #72343, #48575, #32750, #67064, #20273, #9728, #31989, #71959, #55011, #15363, #49712, #72726, #4074, #26689, #3317, #19908, #37278, #31613, #43295, #9350, #21029, #44054, #38399, #42915, #27068, #37654, #21401, #65934, #32369, #26305, #49328, #66310, #44424, #50081, #20656, #43673, #8975, #2943, #67439, #73095, #66684, #14616, #15737, #14988, #38026, #55384, #14240, #60272, #61025, #54262, #3693, #61779, #31237, #2573, #8598, #25932, #11213, #62143, #73463, #16852, #33872, #16102, #11579, #51196, #34241, #23269, #27431, #39878, #45169, #10467, #68549, #56872, #10096, #40626, #34614, #22896, #56500, #45908, #288, #50446, #56130, #39514, #22141, #46278, #62880, #68921, #28933, #28558, #74207, #17231, #67811, #33497, #62511, #39139, #4816, #40252, #57243, #21771, #44798, #69297, #28184, #51564, #27812, #68180, #5555, #50823, #73834, #17608, #16476, #74580, #10837, #51951, #63254, #22510, #5188, #45531, #33133, #57620, #5932, #4439, #6308, #30048, #1756, #52692 ) ),
 .UNSPECIFIED., .F., .F., .F. ) 
 B_SPLINE_SURFACE_WITH_KNOTS ( ( 2, 2 ),
 ( 3, 2, 2, 2, 2, 2, 2, 2, 2, 2, 2, 2, 2, 2, 2, 2, 2, 2, 2, 2, 2, 2, 2, 2, 2, 2, 2, 2, 2, 2, 2, 2, 2, 2, 2, 2, 2, 2, 2, 2, 2, 2, 2, 2, 2, 2, 2, 2, 2, 2, 2, 2, 2, 2, 2, 2, 2, 2, 2, 2, 2, 2, 2, 2, 2, 2, 2, 2, 2, 2, 2, 2, 2, 2, 2, 2, 2, 2, 2, 2, 2, 2, 2, 2, 2, 2, 2, 2, 2, 2, 2, 2, 2, 2, 2, 2, 3 ),
 ( 0.000000000000000000, 1.000000000000000000 ),
 ( 0.000000000000000000, 0.01041666666666666609, 0.02083333333333333218, 0.03125000000000000000, 0.04166666666666666435, 0.05208333333333333565, 0.06250000000000000000, 0.07291666666666667129, 0.08333333333333332871, 0.09375000000000000000, 0.1041666666666666713, 0.1145833333333333287, 0.1250000000000000000, 0.1354166666666666574, 0.1458333333333333426, 0.1562500000000000000, 0.1666666666666666574, 0.1770833333333333426, 0.1875000000000000000, 0.1979166666666666574, 0.2083333333333333426, 0.2187500000000000000, 0.2291666666666666574, 0.2395833333333333426, 0.2500000000000000000, 0.2604166666666666852, 0.2708333333333333148, 0.2812500000000000000, 0.2916666666666666852, 0.3020833333333333148, 0.3125000000000000000, 0.3229166666666666852, 0.3333333333333333148, 0.3437500000000000000, 0.3541666666666666852, 0.3645833333333333148, 0.3750000000000000000, 0.3854166666666666852, 0.3958333333333333148, 0.4062500000000000000, 0.4166666666666666852, 0.4270833333333333148, 0.4375000000000000000, 0.4479166666666666852, 0.4583333333333333148, 0.4687500000000000000, 0.4791666666666666852, 0.4895833333333333148, 0.5000000000000000000, 0.5104166666666666297, 0.5208333333333333703, 0.5312500000000000000, 0.5416666666666666297, 0.5520833333333333703, 0.5625000000000000000, 0.5729166666666666297, 0.5833333333333333703, 0.5937500000000000000, 0.6041666666666666297, 0.6145833333333333703, 0.6250000000000000000, 0.6354166666666666297, 0.6458333333333333703, 0.6562500000000000000, 0.6666666666666666297, 0.6770833333333333703, 0.6875000000000000000, 0.6979166666666666297, 0.7083333333333333703, 0.7187500000000000000, 0.7291666666666666297, 0.7395833333333333703, 0.7500000000000000000, 0.7604166666666666297, 0.7708333333333333703, 0.7812500000000000000, 0.7916666666666666297, 0.8020833333333333703, 0.8125000000000000000, 0.8229166666666666297, 0.8333333333333333703, 0.8437500000000000000, 0.8541666666666666297, 0.8645833333333333703, 0.8750000000000000000, 0.8854166666666666297, 0.8958333333333333703, 0.9062500000000000000, 0.9166666666666666297, 0.9270833333333333703, 0.9375000000000000000, 0.9479166666666666297, 0.9583333333333333703, 0.9687500000000000000, 0.9791666666666666297, 0.9895833333333333703, 1.000000000000000000 ),
 .UNSPECIFIED. ) 
 GEOMETRIC_REPRESENTATION_ITEM ( )  RATIONAL_B_SPLINE_SURFACE ( (
 ( 1.000000000000000000, 0.9238795325112867385, 1.000000000000000000, 0.9238795325112867385, 1.000000000000000000, 0.9238795325112867385, 1.000000000000000000, 0.9238795325112867385, 1.000000000000000000, 0.9238795325112867385, 1.000000000000000000, 0.9238795325112867385, 1.000000000000000000, 0.9238795325112867385, 1.000000000000000000, 0.9238795325112867385, 1.000000000000000000, 0.9238795325112867385, 1.000000000000000000, 0.9238795325112867385, 1.000000000000000000, 0.9238795325112867385, 1.000000000000000000, 0.9238795325112867385, 1.000000000000000000, 0.9238795325112867385, 1.000000000000000000, 0.9238795325112867385, 1.000000000000000000, 0.9238795325112867385, 1.000000000000000000, 0.9238795325112867385, 1.000000000000000000, 0.9238795325112867385, 1.000000000000000000, 0.9238795325112867385, 1.000000000000000000, 0.9238795325112867385, 1.000000000000000000, 0.9238795325112867385, 1.000000000000000000, 0.9238795325112867385, 1.000000000000000000, 0.9238795325112867385, 1.000000000000000000, 0.9238795325112867385, 1.000000000000000000, 0.9238795325112867385, 1.000000000000000000, 0.9238795325112867385, 1.000000000000000000, 0.9238795325112867385, 1.000000000000000000, 0.9238795325112867385, 1.000000000000000000, 0.9238795325112867385, 1.000000000000000000, 0.9238795325112867385, 1.000000000000000000, 0.9238795325112867385, 1.000000000000000000, 0.9238795325112867385, 1.000000000000000000, 0.9238795325112867385, 1.000000000000000000, 0.9238795325112867385, 1.000000000000000000, 0.9238795325112867385, 1.000000000000000000, 0.9238795325112867385, 1.000000000000000000, 0.9238795325112867385, 1.000000000000000000, 0.9238795325112867385, 1.000000000000000000, 0.9238795325112867385, 1.000000000000000000, 0.9238795325112867385, 1.000000000000000000, 0.9238795325112867385, 1.000000000000000000, 0.9238795325112867385, 1.000000000000000000, 0.9238795325112867385, 1.000000000000000000, 0.9238795325112867385, 1.000000000000000000, 0.9238795325112867385, 1.000000000000000000, 0.9238795325112867385, 1.000000000000000000, 0.9238795325112867385, 1.000000000000000000, 0.9238795325112867385, 1.000000000000000000, 0.9238795325112867385, 1.000000000000000000, 0.9238795325112867385, 1.000000000000000000, 0.9238795325112867385, 1.000000000000000000, 0.9238795325112867385, 1.000000000000000000, 0.9238795325112867385, 1.000000000000000000, 0.9238795325112867385, 1.000000000000000000, 0.9238795325112867385, 1.000000000000000000, 0.9238795325112867385, 1.000000000000000000, 0.9238795325112867385, 1.000000000000000000, 0.9238795325112867385, 1.000000000000000000, 0.9238795325112867385, 1.000000000000000000, 0.9238795325112867385, 1.000000000000000000, 0.9238795325112867385, 1.000000000000000000, 0.9238795325112867385, 1.000000000000000000, 0.9238795325112867385, 1.000000000000000000, 0.9238795325112867385, 1.000000000000000000, 0.9238795325112867385, 1.000000000000000000, 0.9238795325112867385, 1.000000000000000000, 0.9238795325112867385, 1.000000000000000000, 0.9238795325112867385, 1.000000000000000000, 0.9238795325112867385, 1.000000000000000000, 0.9238795325112867385, 1.000000000000000000, 0.9238795325112867385, 1.000000000000000000, 0.9238795325112867385, 1.000000000000000000, 0.9238795325112867385, 1.000000000000000000, 0.9238795325112867385, 1.000000000000000000, 0.9238795325112867385, 1.000000000000000000, 0.9238795325112867385, 1.000000000000000000, 0.9238795325112867385, 1.000000000000000000, 0.9238795325112867385, 1.000000000000000000, 0.9238795325112867385, 1.000000000000000000, 0.9238795325112867385, 1.000000000000000000, 0.9238795325112867385, 1.000000000000000000, 0.9238795325112867385, 1.000000000000000000, 0.9238795325112867385, 1.000000000000000000, 0.9238795325112867385, 1.000000000000000000, 0.9238795325112867385, 1.000000000000000000, 0.9238795325112867385, 1.000000000000000000, 0.9238795325112867385, 1.000000000000000000, 0.9238795325112867385, 1.000000000000000000, 0.9238795325112867385, 1.000000000000000000, 0.9238795325112867385, 1.000000000000000000, 0.9238795325112867385, 1.000000000000000000, 0.9238795325112867385, 1.000000000000000000, 0.9238795325112867385, 1.000000000000000000, 0.9238795325112867385, 1.000000000000000000, 0.9238795325112867385, 1.000000000000000000, 0.9238795325112867385, 1.000000000000000000, 0.9238795325112867385, 1.000000000000000000),
 ( 1.000000000000000000, 0.9238795325112867385, 1.000000000000000000, 0.9238795325112867385, 1.000000000000000000, 0.9238795325112867385, 1.000000000000000000, 0.9238795325112867385, 1.000000000000000000, 0.9238795325112867385, 1.000000000000000000, 0.9238795325112867385, 1.000000000000000000, 0.9238795325112867385, 1.000000000000000000, 0.9238795325112867385, 1.000000000000000000, 0.9238795325112867385, 1.000000000000000000, 0.9238795325112867385, 1.000000000000000000, 0.9238795325112867385, 1.000000000000000000, 0.9238795325112867385, 1.000000000000000000, 0.9238795325112867385, 1.000000000000000000, 0.9238795325112867385, 1.000000000000000000, 0.9238795325112867385, 1.000000000000000000, 0.9238795325112867385, 1.000000000000000000, 0.9238795325112867385, 1.000000000000000000, 0.9238795325112867385, 1.000000000000000000, 0.9238795325112867385, 1.000000000000000000, 0.9238795325112867385, 1.000000000000000000, 0.9238795325112867385, 1.000000000000000000, 0.9238795325112867385, 1.000000000000000000, 0.9238795325112867385, 1.000000000000000000, 0.9238795325112867385, 1.000000000000000000, 0.9238795325112867385, 1.000000000000000000, 0.9238795325112867385, 1.000000000000000000, 0.9238795325112867385, 1.000000000000000000, 0.9238795325112867385, 1.000000000000000000, 0.9238795325112867385, 1.000000000000000000, 0.9238795325112867385, 1.000000000000000000, 0.9238795325112867385, 1.000000000000000000, 0.9238795325112867385, 1.000000000000000000, 0.9238795325112867385, 1.000000000000000000, 0.9238795325112867385, 1.000000000000000000, 0.9238795325112867385, 1.000000000000000000, 0.9238795325112867385, 1.000000000000000000, 0.9238795325112867385, 1.000000000000000000, 0.9238795325112867385, 1.000000000000000000, 0.9238795325112867385, 1.000000000000000000, 0.9238795325112867385, 1.000000000000000000, 0.9238795325112867385, 1.000000000000000000, 0.9238795325112867385, 1.000000000000000000, 0.9238795325112867385, 1.000000000000000000, 0.9238795325112867385, 1.000000000000000000, 0.9238795325112867385, 1.000000000000000000, 0.9238795325112867385, 1.000000000000000000, 0.9238795325112867385, 1.000000000000000000, 0.9238795325112867385, 1.000000000000000000, 0.9238795325112867385, 1.000000000000000000, 0.9238795325112867385, 1.000000000000000000, 0.9238795325112867385, 1.000000000000000000, 0.9238795325112867385, 1.000000000000000000, 0.9238795325112867385, 1.000000000000000000, 0.9238795325112867385, 1.000000000000000000, 0.9238795325112867385, 1.000000000000000000, 0.9238795325112867385, 1.000000000000000000, 0.9238795325112867385, 1.000000000000000000, 0.9238795325112867385, 1.000000000000000000, 0.9238795325112867385, 1.000000000000000000, 0.9238795325112867385, 1.000000000000000000, 0.9238795325112867385, 1.000000000000000000, 0.9238795325112867385, 1.000000000000000000, 0.9238795325112867385, 1.000000000000000000, 0.9238795325112867385, 1.000000000000000000, 0.9238795325112867385, 1.000000000000000000, 0.9238795325112867385, 1.000000000000000000, 0.9238795325112867385, 1.000000000000000000, 0.9238795325112867385, 1.000000000000000000, 0.9238795325112867385, 1.000000000000000000, 0.9238795325112867385, 1.000000000000000000, 0.9238795325112867385, 1.000000000000000000, 0.9238795325112867385, 1.000000000000000000, 0.9238795325112867385, 1.000000000000000000, 0.9238795325112867385, 1.000000000000000000, 0.9238795325112867385, 1.000000000000000000, 0.9238795325112867385, 1.000000000000000000, 0.9238795325112867385, 1.000000000000000000, 0.9238795325112867385, 1.000000000000000000, 0.9238795325112867385, 1.000000000000000000, 0.9238795325112867385, 1.000000000000000000, 0.9238795325112867385, 1.000000000000000000, 0.9238795325112867385, 1.000000000000000000, 0.9238795325112867385, 1.000000000000000000, 0.9238795325112867385, 1.000000000000000000, 0.9238795325112867385, 1.000000000000000000, 0.9238795325112867385, 1.000000000000000000, 0.9238795325112867385, 1.000000000000000000, 0.9238795325112867385, 1.000000000000000000, 0.9238795325112867385, 1.000000000000000000, 0.9238795325112867385, 1.000000000000000000, 0.9238795325112867385, 1.000000000000000000, 0.9238795325112867385, 1.000000000000000000, 0.9238795325112867385, 1.000000000000000000, 0.9238795325112867385, 1.000000000000000000, 0.9238795325112867385, 1.000000000000000000, 0.9238795325112867385, 1.000000000000000000) ) ) 
 REPRESENTATION_ITEM ( '' )  SURFACE ( )  );
#40578=CARTESIAN_POINT ( 'NONE',  ( -7.320508075688773708, 156.8750000000000284, -7.320508075688774596 ) ) ;
#40583=CARTESIAN_POINT ( 'NONE',  ( 5.676582343749993598, 130.2604166632526983, 9.832129032723422313 ) ) ;
#40584=CARTESIAN_POINT ( 'NONE',  ( -2.485281374238208052, 294.2500000034139589, 6.000000000000366818 ) ) ;
#40591=FACE_OUTER_BOUND ( 'NONE', #8430, .T. ) ;
#40593=CARTESIAN_POINT ( 'NONE',  ( 5.000000000000047962, 194.1666666666667709, 8.660254037844484998 ) ) ;
#40595=CARTESIAN_POINT ( 'NONE',  ( 7.320508075688771044, 21.24999999317203248, 7.320508075688775484 ) ) ;
#40602=CARTESIAN_POINT ( 'NONE',  ( 3.042071309553159519, 114.7395833299193555, 11.35316468750000141 ) ) ;
#40608=CARTESIAN_POINT ( 'NONE',  ( -11.35316468750000141, 98.48958332991936970, 3.042071309553159963 ) ) ;
#40612=CARTESIAN_POINT ( 'NONE',  ( -7.320508075688773708, 213.7499999931719969, -7.320508075688774596 ) ) ;
#40616=CARTESIAN_POINT ( 'NONE',  ( -11.35316468750000141, 98.48958332991935549, 3.042071309553159963 ) ) ;
#40622=CARTESIAN_POINT ( 'NONE',  ( 8.660254037844389075, 202.2916666598387110, -5.000000000000000000 ) ) ;
#40625=CARTESIAN_POINT ( 'NONE',  ( -11.35316468750000141, 93.59374999658602690, -1.390361679473963753E-15 ) ) ;
#40626=CARTESIAN_POINT ( 'NONE',  ( -4.721056650415998313, 290.5781250017069510, 4.721056650416000089 ) ) ;
#40629=CARTESIAN_POINT ( 'NONE',  ( 3.042071309553167069, 2.135416663252682756, -11.35316468749999785 ) ) ;
#40633=CARTESIAN_POINT ( 'NONE',  ( -11.35316468750000141, 223.4895833299193555, 3.042071309553159963 ) ) ;
#40635=FACE_OUTER_BOUND ( 'NONE', #3514, .T. ) ;
#40636=CARTESIAN_POINT ( 'NONE',  ( 6.676582343750003368, 295.0156250017069510, -2.765530957081997254 ) ) ;
#40639=CARTESIAN_POINT ( 'NONE',  ( -8.311093377946836114, 212.9687499965860127, -8.311093377946837890 ) ) ;
#40641=ADVANCED_FACE ( 'NONE', ( #40868 ), #29547, .T. ) ;
#40645=ORIENTED_EDGE ( 'NONE', *, *, #56011, .T. ) ;
#40648=CARTESIAN_POINT ( 'NONE',  ( 2.679491924311222739, 23.95833333333332860, 10.00000000000000355 ) ) ;
#40659=CARTESIAN_POINT ( 'NONE',  ( 1.226468279477575784E-15, 295.7031250017069510, 6.676582343750001591 ) ) ;
#40662=ORIENTED_EDGE ( 'NONE', *, *, #50624, .T. ) ;
#40668=CARTESIAN_POINT ( 'NONE',  ( -11.35316468749999785, 88.38541666325268409, -3.042071309553167513 ) ) ;
#40673=CARTESIAN_POINT ( 'NONE',  ( 7.320508075688776373, 70.62500000000000000, -7.320508075688776373 ) ) ;
#40677=CARTESIAN_POINT ( 'NONE',  ( -10.00000000000000355, 179.5833333265053966, 2.679491924311223183 ) ) ;
#40678=ADVANCED_FACE ( 'NONE', ( #52933 ), #23883, .T. ) ;
#40679=CARTESIAN_POINT ( 'NONE',  ( -9.832129032723420536, 193.6979166632526983, 5.676582343749997150 ) ) ;
#40683=CARTESIAN_POINT ( 'NONE',  ( 5.676582343750001591, 181.9270833299193555, -9.832129032723420536 ) ) ;
#40686=CARTESIAN_POINT ( 'NONE',  ( -4.999999999999998224, 88.54166665983869677, -8.660254037844389075 ) ) ;
#40690=CARTESIAN_POINT ( 'NONE',  ( -2.085542519210945728E-15, 74.53124999658602690, 11.35316468750000141 ) ) ;
#40693=ORIENTED_EDGE ( 'NONE', *, *, #24114, .T. ) ;
#40696=CARTESIAN_POINT ( 'NONE',  ( 9.832129032723420536, 56.19791666325268409, -5.676582343749999815 ) ) ;
#40701=CARTESIAN_POINT ( 'NONE',  ( 11.35316468749999963, 65.98958332991935549, -3.042071309553165293 ) ) ;
#40705=CARTESIAN_POINT ( 'NONE',  ( -10.00000000000000000, 149.1666666598387110, -2.679491924311229845 ) ) ;
#40708=CARTESIAN_POINT ( 'NONE',  ( -11.35316468750000141, 53.59374999658601979, -1.390361679473963753E-15 ) ) ;
#40710=CARTESIAN_POINT ( 'NONE',  ( 9.832129032723416984, 185.3645833299193555, 5.676582343750006032 ) ) ;
#40714=CARTESIAN_POINT ( 'NONE',  ( 7.320508075688774596, 162.4999999931720538, -7.320508075688774596 ) ) ;
#40716=CARTESIAN_POINT ( 'NONE',  ( 11.35316468749999785, 180.5729166632526983, 3.042071309553174174 ) ) ;
#40722=CARTESIAN_POINT ( 'NONE',  ( 8.311093377946834337, 165.4687499965859843, 8.311093377946839666 ) ) ;
#40724=CARTESIAN_POINT ( 'NONE',  ( -11.35316468750000141, 133.8020833299193555, 3.042071309553159963 ) ) ;
#40737=CARTESIAN_POINT ( 'NONE',  ( -7.320508075688818117, 178.1250000000000568, 7.320508075688810123 ) ) ;
#40753=CARTESIAN_POINT ( 'NONE',  ( 3.170472398252169882E-12, 128.7500000000002558, 10.00000000000000178 ) ) ;
#40754=CARTESIAN_POINT ( 'NONE',  ( 10.00000000000000178, 140.0000000000000000, 0.000000000000000000 ) ) ;
#40772=CARTESIAN_POINT ( 'NONE',  ( 11.35316468750000141, 25.78124999658601624, 0.000000000000000000 ) ) ;
#40774=CARTESIAN_POINT ( 'NONE',  ( -9.832129032723420536, 219.0104166632526983, 5.676582343749997150 ) ) ;
#40777=CARTESIAN_POINT ( 'NONE',  ( -5.000000000000080824, 41.66666666666677088, -8.660254037844531183 ) ) ;
#40782=CARTESIAN_POINT ( 'NONE',  ( 5.676582343750001591, 26.61458332991935194, -9.832129032723420536 ) ) ;
#40787=CARTESIAN_POINT ( 'NONE',  ( 11.35316468749999963, 20.98958332991935194, -3.042071309553165293 ) ) ;
#40789=CARTESIAN_POINT ( 'NONE',  ( 9.832129032723416984, 135.3645833299193555, 5.676582343750006032 ) ) ;
#40790=CARTESIAN_POINT ( 'NONE',  ( -8.660254037844390851, 114.7916666598387110, 4.999999999999998224 ) ) ;
#40793=CARTESIAN_POINT ( 'NONE',  ( 4.999999999999993783, 171.0416666598387110, 8.660254037844390851 ) ) ;
#40797=CARTESIAN_POINT ( 'NONE',  ( 11.35316468749999963, 6.302083329919350163, -3.042071309553165293 ) ) ;
#40800=CARTESIAN_POINT ( 'NONE',  ( 2.765530957081996366, 296.1406250017070647, -6.676582343750003368 ) ) ;
#40801=CARTESIAN_POINT ( 'NONE',  ( -11.35316468750000141, 133.2812499965860127, -1.390361679473963753E-15 ) ) ;
#40813=CARTESIAN_POINT ( 'NONE',  ( 5.676582343750001591, 86.92708332991935549, -9.832129032723420536 ) ) ;
#40816=( BOUNDED_CURVE ( )  B_SPLINE_CURVE ( 2, ( #27613, #15915, #50623, #21949, #41901, #58174, #24548, #64910, #64552, #58903, #70578, #41174, #12489, #35518, #47554, #58531, #11757, #46455, #463, #34421, #41536, #1567, #47187, #6838, #18895, #40797, #6480, #12848, #46820, #5731, #24177, #64184, #23818, #70219, #52863, #23072, #18529, #29111, #29852, #30216, #35887, #69474, #57424, #63803, #63429, #52130, #40430, #1195, #28729, #51745, #34794, #7214, #94, #53236, #69101, #46081, #17407, #57798, #6106, #23441, #12120, #35158, #17784, #29483, #69846, #52492, #830, #18158, #49036, #24905, #42999, #66019, #42266, #14326, #54722, #3029, #55097, #2656, #19622, #36987, #31319, #20742, #60740, #42637, #36622, #72043, #8685, #72434, #65649, #14702, #53971, #26012, #43759, #47922, #49412, #60359, #70941, #66394, #25647, #2282, #59629, #26387, #31700, #13216, #36254, #20360, #59992, #19991, #37359, #7581, #19255, #71302, #59269, #1918, #9061, #30950, #54346, #43377, #37740, #3403, #30586, #32075, #65278, #13584, #53606, #7945, #25277, #48295, #13945, #8309, #48663, #71671, #67523, #44142, #56958, #38857, #73548, #10552, #74290, #15822, #5273, #67154, #28275, #61861, #21856, #33584, #27898, #50908, #44887, #21491, #50166, #22600, #66773, #56588, #33960, #4901, #39225, #51281, #73183, #10182, #45252, #39597, #44512, #22226, #3777, #15077, #33215, #55466, #56212, #38111, #72812, #15449, #27149, #38485, #4162, #61111, #4526, #21119, #61488, #9812, #67891, #16184, #27521, #73921, #62225, #49796, #32835, #55844, #9441, #32458, #68264, #50532, #16560, #62593, #10924, #26779, #12403, #6393, #17691, #51657, #11664, #68635, #372, #57707, #58813, #74650, #6013, #29758, #52773, #69755, #29399, #29017, #35798, #18068, #53147, #18441, #23353, #69010, #6755, #41084, #30132, #7124, #52035, #47096, #1482, #63339, #41454, #46366, #1111, #45621, #45994, #58446, #70134, #22988, #16944, #12036, #11298, #39968, #62974, #28642, #17316, #23726, #34331, #40337, #69381, #57331, #5642, #64468, #34699, #35070, #24087, #46730, #40708, #63712, #58082, #52408, #742, #12766, #64094, #35437, #36535, #53885, #31612, #60652, #24823, #43294, #59546, #18812, #48206, #13129, #71958, #2572, #30866, #37277, #71584, #7494, #53518, #65185, #8974, #66309, #54633, #41816, #2197, #42172, #64826, #70859, #48947, #71214, #36164, #59184, #25192, #47471, #19534, #7862, #37653, #1836, #42551, #8597, #2942, #48574, #8226, #65563, #13860, #31988, #30499, #36903, #47836, #20272, #60271, #55010, #25931, #14615, #59911, #24463, #70494, #13497, #19170, #31236, #54261, #25561, #19907, #42914, #65933, #14239, #16475, #50445, #3316, #26304, #10466, #50080, #10095, #56129, #72342, #61024, #61401, #49327, #66683, #50822, #21028, #44423, #62142, #38025, #33871, #33132, #44797, #9349, #32368, #27811, #55383, #67063, #39513, #32749, #72725, #9727, #26688, #4073, #3692, #68179, #73094, #4438, #21770, #62510, #27430, #49711, #15362, #44053, #20655, #33496, #21400, #73462, #55757, #27067, #10836, #43672, #14987, #67438, #73833, #15736, #56499, #38398, #38775, #67810, #61778, #16101, #39138, #4815, #22140, #45168, #11212, #51563, #62879, #34986, #18356, #41370, #34240, #63625, #64379, #58366, #16851, #6671, #56871, #6307, #51195, #11578, #74579, #22509, #28557, #29675, #5931, #74206, #45530, #57619, #5187, #34613, #68920, #70046, #57242, #17230, #41001, #64008, #29312, #63253, #28932, #287, #12679, #68548, #51950, #5554, #52691, #69668, #28183, #12323, #47014, #23268, #1025, #39877, #22895, #24005, #46277, #35355, #45907, #69296, #40251, #17607, #40625, #11955, #52321, #58001, #657, #23643, #46650, #17982, #13770, #30047, #18725, #19084, #58728, #24379, #8506, #53433, #2108, #36080, #70409, #66216, #42460, #2480, #41734, #64744, #60183, #13042, #24736, #71868, #65099, #30413, #42087, #59098, #36448, #7406, #25839, #7774, #65477, #36814, #48859, #59823, #1755, #47746, #70770, #35713, #42823, #53798, #8139, #13410, #59461, #20182, #7039, #43199, #30778, #31522, #25102, #65841, #47386, #71493, #54174, #48119, #25472, #71125, #31142, #54544, #14149, #53060, #19448, #2851, #48489, #1393, #19817, #37184, #45076, #44705, #39048, #50727, #21312, #50355, #73374, #44334, #43958, #72633, #14521, #22048, #56039, #56402, #27338, #61686, #4721, #20937, #38307, #67720, #26973, #60559, #4348, #67345, #3984, #61313, #3226, #66967, #73742, #20561, #66591, #49617, #60933, #26595, #37560, #15271, #43575, #9255, #14896, #15643, #8883, #31896, #37933, #38684, #54917, #32278, #55292, #26213, #27716, #16018, #49987, #73003, #32658, #9638, #3598, #21679, #10007, #55667, #33039, #62051, #10376, #49233, #33402, #72246, #22416, #28464, #52228, #560, #17512, #51851, #51472, #58274, #40528, #932, #40902, #22792, #16753, #29215, #63534, #52595, #45812, #69576, #34147, #6208, #23915, #63910, #74485, #23543, #68090, #68453, #46555, #17887, #45438, #6576, #34525, #33776, #39418, #29582, #51103, #39779, #68823, #74115, #62782, #12222, #11859, #56776, #35258, #11124, #57530, #16379, #69201, #62417, #10742, #5097, #57147, #195, #28088, #40159, #17135, #5463, #23171, #63165, #11490, #5838, #28832, #46183, #34894, #57901, #1298, #25005, #13680, #36721, #14052, #36353, #53336, #70675, #65006, #54452, #64284, #1662, #70316, #19725, #59732, #2760, #2382, #48396, #12949, #8042, #46924, #58632, #8411, #19353, #6940, #25379, #59368, #35989, #18632, #31426, #60093, #42367, #69949, #18258, #54074, #18992, #53706, #52965, #24279, #31047, #71034, #12590, #29952, #71400, #65382, #42736, #47291, #41641, #41274, #2016, #65750, #64652, #59006, #37090, #7311, #30318, #35618, #24643, #47654, #41998, #13315, #7679, #30686, #48024, #32563, #44246, #61591, #9911, #55572, #55201, #9163, #56310, #33312, #67258, #67629, #38592, #72912, #38955, #25747, #10287, #72540, #73286, #32180, #55949, #37462, #48768, #49520, #14429, #3506, #61958, #31805, #3135, #60842, #72150, #37845, #71775, #26495, #20091, #20846, #60463, #21589, #3887, #43864, #32942, #21219, #8792, #54826, #66493, #43105, #15925, #4259, #38214, #9549, #66879, #15184, #26119, #15554, #26881, #27249, #50264, #44615, #49897, #61219, #66122, #49138, #20461, #43481, #14804, #18455, #52788, #70507, #12050, #29412, #58826, #18082, #50634, #70148, #17330, #13142, #52422, #67993, #35084, #41829, #11679, #57722, #40722, #52050, #17706, #64841, #58095, #34714, #387, #6027, #58461, #36178, #4629, #29032, #1124, #63353, #23368, #46381, #27625, #47483, #35814, #41099, #64106, #23742, #6407, #69397, #47111, #12416, #756, #63728, #46745, #41468, #40351, #35449, #18826, #69768, #6770, #64482, #12779, #29774, #24100, #7138, #73652, #30145, #21961, #53161, #1495, #24478, #44987, #54648, #43687, #36917, #60668, #25206, #66699, #2211, #55023, #65576, #43308, #59198, #59559, #71973, #8988, #13508, #49340, #25575, #24835, #30513, #72357, #42186, #7875, #59925, #65200, #36548, #42565, #7507, #47852, #32005, #48220, #48590, #66323, #60285, #20669, #15002, #53532, #53898, #65950, #20287, #31250, #13873, #71228, #14256, #19920, #1849, #30880, #8239, #19548, #70872, #54276, #14629, #8612, #19185, #2586, #71598, #42928, #37292, #37668, #31627, #2956, #25945, #48962, #3331, #26319, #61790, #38787, #15377, #28198, #10109, #44809, #56513, #73847, #22154, #67822, #67451, #21415, #68563, #45545, #4829, #5201, #50836, #10479, #51209, #44438, #33147, #56141, #10851, #15747, #68194, #49724, #38039, #4451, #26705, #27443, #74220, #44068, #38413, #73107, #9740, #50093, #22525, #50458, #67077, #32762, #61414, #33885, #16114, #73474, #45181, #33511, #21043, #55770, #4087, #61039, #9363, #16490, #21781, #39152, #62155, #27828, #27080, #39528, #62524, #56886, #32382, #55397, #3706, #72740, #28946, #30063, #45922, #51965, #1040, #24020, #41015, #674, #302, #7054, #64025, #24393, #64397, #46292, #40266, #52707, #12337, #47027, #53075, #23281, #18371, #47401, #34627, #12695, #69312, #70063, #16865, #17245, #29690, #41386, #68934, #1409, #58018, #57258, #62895, #39890, #74597, #17621, #22910, #63267, #35728, #35370, #5570, #28570, #58744, #58382, #6688, #51578, #11592, #11228, #34256, #57634, #5947, #40639, #63640, #23659, #11970, #46665, #35001, #6323, #29327, #52336, #69685, #17997, #3240, #19464, #60573, #26226, #25853, #20195, #31911, #2495, #48503, #8897, #71508, #47761, #7789, #70424, #18741, #37198, #37574, #8520, #42837, #54932, #2122, #42475, #48874, #8152, #41748, #60197, #25488, #59838, #31537, #14165, #59113, #54558, #65114, #70784, #30793, #42102, #53813, #64758, #25116, #24751, #13425, #1769, #19832, #13057, #36096, #19097, #65855, #7421, #71881, #30428, #43214, #53448, #2866 ),
 .UNSPECIFIED., .F., .F. ) 
 B_SPLINE_CURVE_WITH_KNOTS ( ( 3, 2, 2, 2, 2, 2, 2, 2, 2, 2, 2, 2, 2, 2, 2, 2, 2, 2, 2, 2, 2, 2, 2, 2, 2, 2, 2, 2, 2, 2, 2, 2, 2, 2, 2, 2, 2, 2, 2, 2, 2, 2, 2, 2, 2, 2, 2, 2, 2, 2, 2, 2, 2, 2, 2, 2, 2, 2, 2, 2, 2, 2, 2, 2, 2, 2, 2, 2, 2, 2, 2, 2, 2, 2, 2, 2, 2, 2, 2, 2, 2, 2, 2, 2, 2, 2, 2, 2, 2, 2, 2, 2, 2, 2, 2, 2, 2, 2, 2, 2, 2, 2, 2, 2, 2, 2, 2, 2, 2, 2, 2, 2, 2, 2, 2, 2, 2, 2, 2, 2, 2, 2, 2, 2, 2, 2, 2, 2, 2, 2, 2, 2, 2, 2, 2, 2, 2, 2, 2, 2, 2, 2, 2, 2, 2, 2, 2, 2, 2, 2, 2, 2, 2, 2, 2, 2, 2, 2, 2, 2, 2, 2, 2, 2, 2, 2, 2, 2, 2, 2, 2, 2, 2, 2, 2, 2, 2, 2, 2, 2, 2, 2, 2, 2, 2, 2, 2, 2, 2, 2, 2, 2, 2, 2, 2, 2, 2, 2, 2, 2, 2, 2, 2, 2, 2, 2, 2, 2, 2, 2, 2, 2, 2, 2, 2, 2, 2, 2, 2, 2, 2, 2, 2, 2, 2, 2, 2, 2, 2, 2, 2, 2, 2, 2, 2, 2, 2, 2, 2, 2, 2, 2, 2, 2, 2, 2, 2, 2, 2, 2, 2, 2, 2, 2, 2, 2, 2, 2, 2, 2, 2, 2, 2, 2, 2, 2, 2, 2, 2, 2, 2, 2, 2, 2, 2, 2, 2, 2, 2, 2, 2, 2, 2, 2, 2, 2, 2, 2, 2, 2, 2, 2, 2, 2, 2, 2, 2, 2, 2, 2, 2, 2, 2, 2, 2, 2, 2, 2, 2, 2, 2, 2, 2, 2, 2, 2, 2, 2, 2, 2, 2, 2, 2, 2, 2, 2, 2, 2, 2, 2, 2, 2, 2, 2, 2, 2, 2, 2, 2, 2, 2, 2, 2, 2, 2, 2, 2, 2, 2, 2, 2, 2, 2, 2, 2, 2, 2, 2, 2, 2, 2, 2, 2, 2, 2, 2, 2, 2, 2, 2, 2, 2, 2, 2, 2, 2, 2, 2, 2, 2, 2, 2, 2, 2, 2, 2, 2, 2, 2, 2, 2, 2, 2, 2, 2, 2, 2, 2, 2, 2, 2, 2, 2, 2, 2, 2, 2, 2, 2, 2, 2, 2, 2, 2, 2, 2, 2, 2, 2, 2, 2, 2, 2, 2, 2, 2, 2, 2, 2, 2, 2, 2, 2, 2, 2, 2, 2, 2, 2, 2, 2, 2, 2, 2, 2, 2, 2, 2, 2, 2, 2, 2, 2, 2, 2, 2, 2, 2, 2, 2, 2, 2, 2, 2, 2, 2, 2, 2, 2, 2, 2, 2, 2, 2, 2, 2, 2, 2, 2, 2, 2, 2, 2, 2, 2, 2, 2, 2, 2, 2, 2, 2, 2, 2, 2, 2, 2, 2, 2, 2, 2, 2, 2, 2, 2, 2, 2, 2, 2, 2, 2, 2, 2, 2, 2, 2, 2, 2, 2, 2, 2, 2, 2, 2, 2, 2, 2, 2, 2, 2, 2, 2, 2, 2, 2, 2, 2, 2, 2, 2, 3 ),
 ( 0.000000000000000000, 0.001843655950715879319, 0.003687311901431758639, 0.005530967852147637524, 0.007374623802863517277, 0.009218279753579396163, 0.01106193570429527505, 0.01290559165501115740, 0.01474924760572703455, 0.01659290355644291518, 0.01843655950715879233, 0.02028021545787467295, 0.02212387140859055010, 0.02396752735930643072, 0.02581118331002231481, 0.02765483926073818849, 0.02949849521145406911, 0.03134215116216994973, 0.03318580711288583035, 0.03502946306360170403, 0.03687311901431758465, 0.03871677496503347221, 0.04056043091574934589, 0.04240408686646522651, 0.04424774281718110019, 0.04609139876789698081, 0.04793505471861286144, 0.04977871066932874899, 0.05162236662004462961, 0.05346602257076050330, 0.05530967852147637698, 0.05715333447219225760, 0.05899699042290813822, 0.06084064637362402578, 0.06268430232433989946, 0.06452795827505578008, 0.06637161422577166070, 0.06821527017648754132, 0.07005892612720340806, 0.07190258207791928868, 0.07374623802863516930, 0.07558989397935104992, 0.07743354993006694442, 0.07927720588078281116, 0.08112086183149869179, 0.08296451778221457241, 0.08480817373293045303, 0.08665182968364633365, 0.08849548563436220039, 0.09033914158507809489, 0.09218279753579396163, 0.09402645348650984225, 0.09587010943722572287, 0.09771376538794160349, 0.09955742133865749799, 0.1014010772893733647, 0.1032447332400892592, 0.1050883891908051260, 0.1069320451415210066, 0.1087757010922368872, 0.1106193570429527540, 0.1124630129936686485, 0.1143066689443845152, 0.1161503248951003958, 0.1179939808458162764, 0.1198376367965321432, 0.1216812927472480516, 0.1235249486979639183, 0.1253686046486797989, 0.1272122605993956657, 0.1290559165501115602, 0.1308995725008273991, 0.1327432284515433214, 0.1345868844022592159, 0.1364305403529750826, 0.1382741963036909494, 0.1401178522544068161, 0.1419615082051227384, 0.1438051641558385774, 0.1456488201065544719, 0.1474924760572703386, 0.1493361320079862331, 0.1511797879587020998, 0.1530234439094179943, 0.1548670998601338888, 0.1567107558108497278, 0.1585544117615656223, 0.1603980677122815168, 0.1622417236629973836, 0.1640853796137132503, 0.1659290355644291448, 0.1677726915151450116, 0.1696163474658609061, 0.1714600034165767728, 0.1733036593672926673, 0.1751473153180085063, 0.1769909712687244008, 0.1788346272194403230, 0.1806782831701561898, 0.1825219391208720565, 0.1843655950715879233, 0.1862092510223038178, 0.1880529069730196845, 0.1898965629237355790, 0.1917402188744514457, 0.1935838748251673402, 0.1954275307758832070, 0.1972711867265991015, 0.1991148426773149960, 0.2009584986280308350, 0.2028021545787467295, 0.2046458105294626240, 0.2064894664801785185, 0.2083331224308943574, 0.2101767783816102519, 0.2120204343323261187, 0.2138640902830420132, 0.2157077462337578799, 0.2175514021844737744, 0.2193950581351896689, 0.2212387140859055079, 0.2230823700366214302, 0.2249260259873372969, 0.2267696819380531637, 0.2286133378887690304, 0.2304569938394849249, 0.2323006497902007916, 0.2341443057409166861, 0.2359879616916325529, 0.2378316176423484474, 0.2396752735930642864, 0.2415189295437802086, 0.2433625854944961031, 0.2452062414452119421, 0.2470498973959278366, 0.2488935533466437033, 0.2507372092973595978, 0.2525808652480754923, 0.2544245211987913313, 0.2562681771495072258, 0.2581118331002231203, 0.2599554890509390148, 0.2617991450016547983, 0.2636428009523707483, 0.2654864569030866428, 0.2673301128538025373, 0.2691737688045184318, 0.2710174247552342708, 0.2728610807059501653, 0.2747047366566660043, 0.2765483926073818988, 0.2783920485580977378, 0.2802357045088136323, 0.2820793604595295823, 0.2839230164102454768, 0.2857666723609613713, 0.2876103283116771547, 0.2894539842623930492, 0.2912976402131089437, 0.2931412961638248382, 0.2949849521145406772, 0.2968286080652565717, 0.2986722640159724662, 0.3005159199666883607, 0.3023595759174041997, 0.3042032318681200942, 0.3060468878188359887, 0.3078905437695518832, 0.3097341997202677777, 0.3115778556709836167, 0.3134215116216994557, 0.3152651675724153502, 0.3171088235231312447, 0.3189524794738471392, 0.3207961354245630337, 0.3226397913752789282, 0.3244834473259947671, 0.3263271032767106061, 0.3281707592274265006, 0.3300144151781423951, 0.3318580711288582896, 0.3337017270795741841, 0.3355453830302900231, 0.3373890389810059176, 0.3392326949317218121, 0.3410763508824377066, 0.3429200068331535456, 0.3447636627838694401, 0.3466073187345853346, 0.3484509746853012291, 0.3502946306360170126, 0.3521382865867329071, 0.3539819425374488016, 0.3558255984881647516, 0.3576692544388806461, 0.3595129103895964851, 0.3613565663403123795, 0.3632002222910282185, 0.3650438782417441130, 0.3668875341924599520, 0.3687311901431758465, 0.3705748460938917410, 0.3724185020446076355, 0.3742621579953235855, 0.3761058139460393690, 0.3779494698967552635, 0.3797931258474711580, 0.3816367817981870525, 0.3834804377489028915, 0.3853240936996187860, 0.3871677496503346805, 0.3890114056010505195, 0.3908550615517664140, 0.3926987175024823085, 0.3945423734531982030, 0.3963860294039140975, 0.3982296853546299920, 0.4000733413053458309, 0.4019169972560616699, 0.4037606532067775644, 0.4056043091574934589, 0.4074479651082092979, 0.4092916210589252479, 0.4111352770096411424, 0.4129789329603570369, 0.4148225889110728204, 0.4166662448617887149, 0.4185099008125046094, 0.4203535567632205039, 0.4221972127139363984, 0.4240408686646522374, 0.4258845246153681319, 0.4277281805660840264, 0.4295718365167999209, 0.4314154924675157599, 0.4332591484182316544, 0.4351028043689475489, 0.4369464603196634434, 0.4387901162703793378, 0.4406337722210951213, 0.4424774281718110158, 0.4443210841225269103, 0.4461647400732428603, 0.4480083960239586993, 0.4498520519746745938, 0.4516957079253904328, 0.4535393638761063273, 0.4553830198268221663, 0.4572266757775380608, 0.4590703317282539553, 0.4609139876789698498, 0.4627576436296857443, 0.4646012995804015833, 0.4664449555311174778, 0.4682886114818333723, 0.4701322674325492668, 0.4719759233832651057, 0.4738195793339810002, 0.4756632352846968947, 0.4775068912354127337, 0.4793505471861285727, 0.4811942031368444672, 0.4830378590875604172, 0.4848815150382763117, 0.4867251709889922062, 0.4885688269397080452, 0.4904124828904238842, 0.4922561388411397787, 0.4940997947918556732, 0.4959434507425715122, 0.4977871066932874067, 0.4996307626440033012, 0.5014744185947191957, 0.5033180745454350902, 0.5051617304961509847, 0.5070053864468668792, 0.5088490423975826626, 0.5106926983482985571, 0.5125363542990144516, 0.5143800102497303461, 0.5162236662004462406, 0.5180673221511621351, 0.5199109781018780296, 0.5217546340525938131, 0.5235982900033095966, 0.5254419459540254911, 0.5272856019047414966, 0.5291292578554573911, 0.5309729138061732856, 0.5328165697568891801, 0.5346602257076050746, 0.5365038816583209691, 0.5383475376090368636, 0.5401911935597526471, 0.5420348495104685416, 0.5438785054611844361, 0.5457221614119003306, 0.5475658173626161140, 0.5494094733133320085, 0.5512531292640479030, 0.5530967852147637975, 0.5549404411654796920, 0.5567840971161954755, 0.5586277530669113700, 0.5604714090176272645, 0.5623150649683431590, 0.5641587209190591645, 0.5660023768697750590, 0.5678460328204909535, 0.5696896887712068480, 0.5715333447219227425, 0.5733770006726384150, 0.5752206566233543095, 0.5770643125740702040, 0.5789079685247860985, 0.5807516244755019930, 0.5825952804262178875, 0.5844389363769337820, 0.5862825923276496765, 0.5881262482783654599, 0.5899699042290813544, 0.5918135601797972489, 0.5936572161305131434, 0.5955008720812290379, 0.5973445280319449324, 0.5991881839826607159, 0.6010318399333767214, 0.6028754958840926159, 0.6047191518348083994, 0.6065628077855242939, 0.6084064637362401884, 0.6102501196869560829, 0.6120937756376719774, 0.6139374315883878719, 0.6157810875391037664, 0.6176247434898196609, 0.6194683994405355554, 0.6213120553912513389, 0.6231557113419672334, 0.6249993672926830168, 0.6268430232433989113, 0.6286866791941148058, 0.6305303351448307003, 0.6323739910955465948, 0.6342176470462624893, 0.6360613029969782728, 0.6379049589476942783, 0.6397486148984101728, 0.6415922708491260673, 0.6434359267998419618, 0.6452795827505578563, 0.6471232387012737508, 0.6489668946519895343, 0.6508105506027054288, 0.6526542065534212123, 0.6544978625041371068, 0.6563415184548530013, 0.6581851744055688958, 0.6600288303562847902, 0.6618724863070006847, 0.6637161422577165792, 0.6655597982084324737, 0.6674034541591483682, 0.6692471101098641517, 0.6710907660605800462, 0.6729344220112960517, 0.6747780779620118352, 0.6766217339127277297, 0.6784653898634436242, 0.6803090458141595187, 0.6821527017648754132, 0.6839963577155913077, 0.6858400136663070912, 0.6876836696170229857, 0.6895273255677388802, 0.6913709815184547747, 0.6932146374691706692, 0.6950582934198865637, 0.6969019493706024582, 0.6987456053213183527, 0.7005892612720340251, 0.7024329172227499196, 0.7042765731734658141, 0.7061202291241817086, 0.7079638850748976031, 0.7098075410256136086, 0.7116511969763295031, 0.7134948529270453976, 0.7153385088777612921, 0.7171821648284770756, 0.7190258207791929701, 0.7208694767299088646, 0.7227131326806247591, 0.7245567886313406536, 0.7264004445820564371, 0.7282441005327723316, 0.7300877564834882261, 0.7319314124342041206, 0.7337750683849199040, 0.7356187243356357985, 0.7374623802863516930, 0.7393060362370675875, 0.7411496921877834820, 0.7429933481384993765, 0.7448370040892152710, 0.7466806600399312766, 0.7485243159906471710, 0.7503679719413629545, 0.7522116278920787380, 0.7540552838427946325, 0.7558989397935105270, 0.7577425957442264215, 0.7595862516949423160, 0.7614299076456582105, 0.7632735635963741050, 0.7651172195470898885, 0.7669608754978057830, 0.7688045314485216775, 0.7706481873992375720, 0.7724918433499534665, 0.7743354993006693610, 0.7761791552513851444, 0.7780228112021010389, 0.7798664671528169334, 0.7817101231035328279, 0.7835537790542487224, 0.7853974350049646169, 0.7872410909556805114, 0.7890847469063964059, 0.7909284028571123004, 0.7927720588078281949, 0.7946157147585440894, 0.7964593707092599839, 0.7983030266599757674, 0.8001466826106916619, 0.8019903385614074454, 0.8038339945121233399, 0.8056776504628392344, 0.8075213064135551289, 0.8093649623642710234, 0.8112086183149869179, 0.8130522742657027013, 0.8148959302164185958, 0.8167395861671344903, 0.8185832421178504958, 0.8204268980685663903, 0.8222705540192822848, 0.8241142099699981793, 0.8259578659207140738, 0.8278015218714298573, 0.8296451778221456408, 0.8314888337728615353, 0.8333324897235774298, 0.8351761456742933243, 0.8370198016250092188, 0.8388634575757251133, 0.8407071135264410078, 0.8425507694771569023, 0.8443944254278727968, 0.8462380813785885803, 0.8480817373293044747, 0.8499253932800203692, 0.8517690492307362637, 0.8536127051814520472, 0.8554563611321680527, 0.8573000170828839472, 0.8591436730335998417, 0.8609873289843157362, 0.8628309849350315197, 0.8646746408857474142, 0.8665182968364633087, 0.8683619527871792032, 0.8702056087378950977, 0.8720492646886109922, 0.8738929206393268867, 0.8757365765900427812, 0.8775802325407586757, 0.8794238884914743482, 0.8812675444421902426, 0.8831112003929061371, 0.8849548563436220316, 0.8867985122943379261, 0.8886421682450538206, 0.8904858241957698262, 0.8923294801464857207, 0.8941731360972015041, 0.8960167920479173986, 0.8978604479986332931, 0.8997041039493491876, 0.9015477599000650821, 0.9033914158507808656, 0.9052350718014967601, 0.9070787277522126546, 0.9089223837029285491, 0.9107660396536443326, 0.9126096956043602271, 0.9144533515550761216, 0.9162970075057920161, 0.9181406634565079106, 0.9199843194072238051, 0.9218279753579396996, 0.9236716313086555941, 0.9255152872593714886, 0.9273589432100873831, 0.9292025991608031665, 0.9310462551115190610, 0.9328899110622349555, 0.9347335670129508500, 0.9365772229636667445, 0.9384208789143826390, 0.9402645348650985335, 0.9421081908158143170, 0.9439518467665302115, 0.9457955027172461060, 0.9476391586679620005, 0.9494828146186778950, 0.9513264705693937895, 0.9531701265201096840, 0.9550137824708254675, 0.9568574384215413620, 0.9587010943722571454, 0.9605447503229730399, 0.9623884062736889344, 0.9642320622244049400, 0.9660757181751208345, 0.9679193741258367290, 0.9697630300765526234, 0.9716066860272685179, 0.9734503419779844124, 0.9752939979287001959, 0.9771376538794160904, 0.9789813098301319849, 0.9808249657808477684, 0.9826686217315636629, 0.9845122776822795574, 0.9863559336329954519, 0.9881995895837113464, 0.9900432455344272409, 0.9918869014851430244, 0.9937305574358589189, 0.9951533035133235394 ),
 .UNSPECIFIED. ) 
 CURVE ( )  GEOMETRIC_REPRESENTATION_ITEM ( )  RATIONAL_B_SPLINE_CURVE ( ( 1.000000000000000000, 0.9659258262890683122, 1.000000000000000000, 0.9659258262890683122, 1.000000000000000000, 0.9659258262890683122, 1.000000000000000000, 0.9659258262890683122, 1.000000000000000000, 0.9659258262890683122, 1.000000000000000000, 0.9659258262890683122, 1.000000000000000000, 0.9659258262890683122, 1.000000000000000000, 0.9659258262890683122, 1.000000000000000000, 0.9659258262890683122, 1.000000000000000000, 0.9659258262890683122, 1.000000000000000000, 0.9659258262890683122, 1.000000000000000000, 0.9659258262890683122, 1.000000000000000000, 0.9659258262890683122, 1.000000000000000000, 0.9659258262890683122, 1.000000000000000000, 0.9659258262890683122, 1.000000000000000000, 0.9659258262890683122, 1.000000000000000000, 0.9659258262890683122, 1.000000000000000000, 0.9659258262890683122, 1.000000000000000000, 0.9659258262890683122, 1.000000000000000000, 0.9659258262890683122, 1.000000000000000000, 0.9659258262890683122, 1.000000000000000000, 0.9659258262890683122, 1.000000000000000000, 0.9659258262890683122, 1.000000000000000000, 0.9659258262890683122, 1.000000000000000000, 0.9659258262890683122, 1.000000000000000000, 0.9659258262890683122, 1.000000000000000000, 0.9659258262890683122, 1.000000000000000000, 0.9659258262890683122, 1.000000000000000000, 0.9659258262890683122, 1.000000000000000000, 0.9659258262890683122, 1.000000000000000000, 0.9659258262890683122, 1.000000000000000000, 0.9659258262890683122, 1.000000000000000000, 0.9659258262890683122, 1.000000000000000000, 0.9659258262890683122, 1.000000000000000000, 0.9659258262890683122, 1.000000000000000000, 0.9659258262890683122, 1.000000000000000000, 0.9659258262890683122, 1.000000000000000000, 0.9659258262890683122, 1.000000000000000000, 0.9659258262890683122, 1.000000000000000000, 0.9659258262890683122, 1.000000000000000000, 0.9659258262890683122, 1.000000000000000000, 0.9659258262890683122, 1.000000000000000000, 0.9659258262890683122, 1.000000000000000000, 0.9659258262890683122, 1.000000000000000000, 0.9659258262890683122, 1.000000000000000000, 0.9659258262890683122, 1.000000000000000000, 0.9659258262890683122, 1.000000000000000000, 0.9659258262890683122, 1.000000000000000000, 0.9659258262890683122, 1.000000000000000000, 0.9659258262890683122, 1.000000000000000000, 0.9659258262890683122, 1.000000000000000000, 0.9659258262890683122, 1.000000000000000000, 0.9659258262890683122, 1.000000000000000000, 0.9659258262890683122, 1.000000000000000000, 0.9659258262890683122, 1.000000000000000000, 0.9659258262890683122, 1.000000000000000000, 0.9659258262890683122, 1.000000000000000000, 0.9659258262890683122, 1.000000000000000000, 0.9659258262890683122, 1.000000000000000000, 0.9659258262890683122, 1.000000000000000000, 0.9659258262890683122, 1.000000000000000000, 0.9659258262890683122, 1.000000000000000000, 0.9659258262890683122, 1.000000000000000000, 0.9659258262890683122, 1.000000000000000000, 0.9659258262890683122, 1.000000000000000000, 0.9659258262890683122, 1.000000000000000000, 0.9659258262890683122, 1.000000000000000000, 0.9659258262890683122, 1.000000000000000000, 0.9659258262890683122, 1.000000000000000000, 0.9659258262890683122, 1.000000000000000000, 0.9659258262890683122, 1.000000000000000000, 0.9659258262890683122, 1.000000000000000000, 0.9659258262890683122, 1.000000000000000000, 0.9659258262890683122, 1.000000000000000000, 0.9659258262890683122, 1.000000000000000000, 0.9659258262890683122, 1.000000000000000000, 0.9659258262890683122, 1.000000000000000000, 0.9659258262890683122, 1.000000000000000000, 0.9659258262890683122, 1.000000000000000000, 0.9659258262890683122, 1.000000000000000000, 0.9659258262890683122, 1.000000000000000000, 0.9659258262890683122, 1.000000000000000000, 0.9659258262890683122, 1.000000000000000000, 0.9659258262890683122, 1.000000000000000000, 0.9659258262890683122, 1.000000000000000000, 0.9659258262890683122, 1.000000000000000000, 0.9659258262890683122, 1.000000000000000000, 0.9659258262890683122, 1.000000000000000000, 0.9659258262890683122, 1.000000000000000000, 0.9659258262890683122, 1.000000000000000000, 0.9659258262890683122, 1.000000000000000000, 0.9659258262890683122, 1.000000000000000000, 0.9659258262890683122, 1.000000000000000000, 0.9659258262890683122, 1.000000000000000000, 0.9659258262890683122, 1.000000000000000000, 0.9659258262890683122, 1.000000000000000000, 0.9659258262890683122, 1.000000000000000000, 0.9659258262890683122, 1.000000000000000000, 0.9659258262890683122, 1.000000000000000000, 0.9659258262890683122, 1.000000000000000000, 0.9659258262890683122, 1.000000000000000000, 0.9659258262890683122, 1.000000000000000000, 0.9659258262890683122, 1.000000000000000000, 0.9659258262890683122, 1.000000000000000000, 0.9659258262890683122, 1.000000000000000000, 0.9659258262890683122, 1.000000000000000000, 0.9659258262890683122, 1.000000000000000000, 0.9659258262890683122, 1.000000000000000000, 0.9659258262890683122, 1.000000000000000000, 0.9659258262890683122, 1.000000000000000000, 0.9659258262890683122, 1.000000000000000000, 0.9659258262890683122, 1.000000000000000000, 0.9659258262890683122, 1.000000000000000000, 0.9659258262890683122, 1.000000000000000000, 0.9659258262890683122, 1.000000000000000000, 0.9659258262890683122, 1.000000000000000000, 0.9659258262890683122, 1.000000000000000000, 0.9659258262890683122, 1.000000000000000000, 0.9659258262890683122, 1.000000000000000000, 0.9659258262890683122, 1.000000000000000000, 0.9659258262890683122, 1.000000000000000000, 0.9659258262890683122, 1.000000000000000000, 0.9659258262890683122, 1.000000000000000000, 0.9659258262890683122, 1.000000000000000000, 0.9659258262890683122, 1.000000000000000000, 0.9659258262890683122, 1.000000000000000000, 0.9659258262890683122, 1.000000000000000000, 0.9659258262890683122, 1.000000000000000000, 0.9659258262890683122, 1.000000000000000000, 0.9659258262890683122, 1.000000000000000000, 0.9659258262890683122, 1.000000000000000000, 0.9659258262890683122, 1.000000000000000000, 0.9659258262890683122, 1.000000000000000000, 0.9659258262890683122, 1.000000000000000000, 0.9659258262890683122, 1.000000000000000000, 0.9659258262890683122, 1.000000000000000000, 0.9659258262890683122, 1.000000000000000000, 0.9659258262890683122, 1.000000000000000000, 0.9659258262890683122, 1.000000000000000000, 0.9659258262890683122, 1.000000000000000000, 0.9659258262890683122, 1.000000000000000000, 0.9659258262890683122, 1.000000000000000000, 0.9659258262890683122, 1.000000000000000000, 0.9659258262890683122, 1.000000000000000000, 0.9659258262890683122, 1.000000000000000000, 0.9659258262890683122, 1.000000000000000000, 0.9659258262890683122, 1.000000000000000000, 0.9659258262890683122, 1.000000000000000000, 0.9659258262890683122, 1.000000000000000000, 0.9659258262890683122, 1.000000000000000000, 0.9659258262890683122, 1.000000000000000000, 0.9659258262890683122, 1.000000000000000000, 0.9659258262890683122, 1.000000000000000000, 0.9659258262890683122, 1.000000000000000000, 0.9659258262890683122, 1.000000000000000000, 0.9659258262890683122, 1.000000000000000000, 0.9659258262890683122, 1.000000000000000000, 0.9659258262890683122, 1.000000000000000000, 0.9659258262890683122, 1.000000000000000000, 0.9659258262890683122, 1.000000000000000000, 0.9659258262890683122, 1.000000000000000000, 0.9659258262890683122, 1.000000000000000000, 0.9659258262890683122, 1.000000000000000000, 0.9659258262890683122, 1.000000000000000000, 0.9659258262890683122, 1.000000000000000000, 0.9659258262890683122, 1.000000000000000000, 0.9659258262890683122, 1.000000000000000000, 0.9659258262890683122, 1.000000000000000000, 0.9659258262890683122, 1.000000000000000000, 0.9659258262890683122, 1.000000000000000000, 0.9659258262890683122, 1.000000000000000000, 0.9659258262890683122, 1.000000000000000000, 0.9659258262890683122, 1.000000000000000000, 0.9659258262890683122, 1.000000000000000000, 0.9659258262890683122, 1.000000000000000000, 0.9659258262890683122, 1.000000000000000000, 0.9659258262890683122, 1.000000000000000000, 0.9659258262890683122, 1.000000000000000000, 0.9659258262890683122, 1.000000000000000000, 0.9659258262890683122, 1.000000000000000000, 0.9659258262890683122, 1.000000000000000000, 0.9659258262890683122, 1.000000000000000000, 0.9659258262890683122, 1.000000000000000000, 0.9659258262890683122, 1.000000000000000000, 0.9659258262890683122, 1.000000000000000000, 0.9659258262890683122, 1.000000000000000000, 0.9659258262890683122, 1.000000000000000000, 0.9659258262890683122, 1.000000000000000000, 0.9659258262890683122, 1.000000000000000000, 0.9659258262890683122, 1.000000000000000000, 0.9659258262890683122, 1.000000000000000000, 0.9659258262890683122, 1.000000000000000000, 0.9659258262890683122, 1.000000000000000000, 0.9659258262890683122, 1.000000000000000000, 0.9659258262890683122, 1.000000000000000000, 0.9659258262890683122, 1.000000000000000000, 0.9659258262890683122, 1.000000000000000000, 0.9659258262890683122, 1.000000000000000000, 0.9659258262890683122, 1.000000000000000000, 0.9659258262890683122, 1.000000000000000000, 0.9659258262890683122, 1.000000000000000000, 0.9659258262890683122, 1.000000000000000000, 0.9659258262890683122, 1.000000000000000000, 0.9659258262890683122, 1.000000000000000000, 0.9659258262890683122, 1.000000000000000000, 0.9659258262890683122, 1.000000000000000000, 0.9659258262890683122, 1.000000000000000000, 0.9659258262890683122, 1.000000000000000000, 0.9659258262890683122, 1.000000000000000000, 0.9659258262890683122, 1.000000000000000000, 0.9659258262890683122, 1.000000000000000000, 0.9659258262890683122, 1.000000000000000000, 0.9659258262890683122, 1.000000000000000000, 0.9659258262890683122, 1.000000000000000000, 0.9659258262890683122, 1.000000000000000000, 0.9659258262890683122, 1.000000000000000000, 0.9659258262890683122, 1.000000000000000000, 0.9659258262890683122, 1.000000000000000000, 0.9659258262890683122, 1.000000000000000000, 0.9659258262890683122, 1.000000000000000000, 0.9659258262890683122, 1.000000000000000000, 0.9659258262890683122, 1.000000000000000000, 0.9659258262890683122, 1.000000000000000000, 0.9659258262890683122, 1.000000000000000000, 0.9659258262890683122, 1.000000000000000000, 0.9659258262890683122, 1.000000000000000000, 0.9659258262890683122, 1.000000000000000000, 0.9659258262890683122, 1.000000000000000000, 0.9659258262890683122, 1.000000000000000000, 0.9659258262890683122, 1.000000000000000000, 0.9659258262890683122, 1.000000000000000000, 0.9659258262890683122, 1.000000000000000000, 0.9659258262890683122, 1.000000000000000000, 0.9659258262890683122, 1.000000000000000000, 0.9659258262890683122, 1.000000000000000000, 0.9659258262890683122, 1.000000000000000000, 0.9659258262890683122, 1.000000000000000000, 0.9659258262890683122, 1.000000000000000000, 0.9659258262890683122, 1.000000000000000000, 0.9659258262890683122, 1.000000000000000000, 0.9659258262890683122, 1.000000000000000000, 0.9659258262890683122, 1.000000000000000000, 0.9659258262890683122, 1.000000000000000000, 0.9659258262890683122, 1.000000000000000000, 0.9659258262890683122, 1.000000000000000000, 0.9659258262890683122, 1.000000000000000000, 0.9659258262890683122, 1.000000000000000000, 0.9659258262890683122, 1.000000000000000000, 0.9659258262890683122, 1.000000000000000000, 0.9659258262890683122, 1.000000000000000000, 0.9659258262890683122, 1.000000000000000000, 0.9659258262890683122, 1.000000000000000000, 0.9659258262890683122, 1.000000000000000000, 0.9659258262890683122, 1.000000000000000000, 0.9659258262890683122, 1.000000000000000000, 0.9659258262890683122, 1.000000000000000000, 0.9659258262890683122, 1.000000000000000000, 0.9659258262890683122, 1.000000000000000000, 0.9659258262890683122, 1.000000000000000000, 0.9659258262890683122, 1.000000000000000000, 0.9659258262890683122, 1.000000000000000000, 0.9659258262890683122, 1.000000000000000000, 0.9659258262890683122, 1.000000000000000000, 0.9659258262890683122, 1.000000000000000000, 0.9659258262890683122, 1.000000000000000000, 0.9659258262890683122, 1.000000000000000000, 0.9659258262890683122, 1.000000000000000000, 0.9659258262890683122, 1.000000000000000000, 0.9659258262890683122, 1.000000000000000000, 0.9659258262890683122, 1.000000000000000000, 0.9659258262890683122, 1.000000000000000000, 0.9659258262890683122, 1.000000000000000000, 0.9659258262890683122, 1.000000000000000000, 0.9659258262890683122, 1.000000000000000000, 0.9659258262890683122, 1.000000000000000000, 0.9659258262890683122, 1.000000000000000000, 0.9659258262890683122, 1.000000000000000000, 0.9659258262890683122, 1.000000000000000000, 0.9659258262890683122, 1.000000000000000000, 0.9659258262890683122, 1.000000000000000000, 0.9659258262890683122, 1.000000000000000000, 0.9659258262890683122, 1.000000000000000000, 0.9659258262890683122, 1.000000000000000000, 0.9659258262890683122, 1.000000000000000000, 0.9659258262890683122, 1.000000000000000000, 0.9659258262890683122, 1.000000000000000000, 0.9659258262890683122, 1.000000000000000000, 0.9659258262890683122, 1.000000000000000000, 0.9659258262890683122, 1.000000000000000000, 0.9659258262890683122, 1.000000000000000000, 0.9659258262890683122, 1.000000000000000000, 0.9659258262890683122, 1.000000000000000000, 0.9659258262890683122, 1.000000000000000000, 0.9659258262890683122, 1.000000000000000000, 0.9659258262890683122, 1.000000000000000000, 0.9659258262890683122, 1.000000000000000000, 0.9659258262890683122, 1.000000000000000000, 0.9659258262890683122, 1.000000000000000000, 0.9659258262890683122, 1.000000000000000000, 0.9659258262890683122, 1.000000000000000000, 0.9659258262890683122, 1.000000000000000000, 0.9659258262890683122, 1.000000000000000000, 0.9659258262890683122, 1.000000000000000000, 0.9659258262890683122, 1.000000000000000000, 0.9659258262890683122, 1.000000000000000000, 0.9659258262890683122, 1.000000000000000000, 0.9659258262890683122, 1.000000000000000000, 0.9659258262890683122, 1.000000000000000000, 0.9659258262890683122, 1.000000000000000000, 0.9659258262890683122, 1.000000000000000000, 0.9659258262890683122, 1.000000000000000000, 0.9659258262890683122, 1.000000000000000000, 0.9659258262890683122, 1.000000000000000000, 0.9659258262890683122, 1.000000000000000000, 0.9659258262890683122, 1.000000000000000000, 0.9659258262890683122, 1.000000000000000000, 0.9659258262890683122, 1.000000000000000000, 0.9659258262890683122, 1.000000000000000000, 0.9659258262890683122, 1.000000000000000000, 0.9659258262890683122, 1.000000000000000000, 0.9659258262890683122, 1.000000000000000000, 0.9659258262890683122, 1.000000000000000000, 0.9659258262890683122, 1.000000000000000000, 0.9659258262890683122, 1.000000000000000000, 0.9659258262890683122, 1.000000000000000000, 0.9659258262890683122, 1.000000000000000000, 0.9659258262890683122, 1.000000000000000000, 0.9659258262890683122, 1.000000000000000000, 0.9659258262890683122, 1.000000000000000000, 0.9659258262890683122, 1.000000000000000000, 0.9659258262890683122, 1.000000000000000000, 0.9659258262890683122, 1.000000000000000000, 0.9659258262890683122, 1.000000000000000000, 0.9659258262890683122, 1.000000000000000000, 0.9659258262890683122, 1.000000000000000000, 0.9659258262890683122, 1.000000000000000000, 0.9659258262890683122, 1.000000000000000000, 0.9659258262890683122, 1.000000000000000000, 0.9659258262890683122, 1.000000000000000000, 0.9659258262890683122, 1.000000000000000000, 0.9659258262890683122, 1.000000000000000000, 0.9659258262890683122, 1.000000000000000000, 0.9659258262890683122, 1.000000000000000000, 0.9659258262890683122, 1.000000000000000000, 0.9659258262890683122, 1.000000000000000000, 0.9659258262890683122, 1.000000000000000000, 0.9659258262890683122, 1.000000000000000000, 0.9659258262890683122, 1.000000000000000000, 0.9659258262890683122, 1.000000000000000000, 0.9659258262890683122, 1.000000000000000000, 0.9659258262890683122, 1.000000000000000000, 0.9659258262890683122, 1.000000000000000000, 0.9659258262890683122, 1.000000000000000000, 0.9659258262890683122, 1.000000000000000000, 0.9659258262890683122, 1.000000000000000000, 0.9659258262890683122, 1.000000000000000000, 0.9659258262890683122, 1.000000000000000000, 0.9659258262890683122, 1.000000000000000000, 0.9659258262890683122, 1.000000000000000000, 0.9659258262890683122, 1.000000000000000000, 0.9659258262890683122, 1.000000000000000000, 0.9659258262890683122, 1.000000000000000000, 0.9659258262890683122, 1.000000000000000000, 0.9659258262890683122, 1.000000000000000000, 0.9659258262890683122, 1.000000000000000000, 0.9659258262890683122, 1.000000000000000000, 0.9659258262890683122, 1.000000000000000000, 0.9659258262890683122, 1.000000000000000000, 0.9659258262890683122, 1.000000000000000000, 0.9659258262890683122, 1.000000000000000000, 0.9659258262890683122, 1.000000000000000000, 0.9659258262890683122, 1.000000000000000000, 0.9659258262890683122, 1.000000000000000000, 0.9659258262890683122, 1.000000000000000000, 0.9659258262890683122, 1.000000000000000000, 0.9659258262890683122, 1.000000000000000000, 0.9659258262890683122, 1.000000000000000000, 0.9659258262890683122, 1.000000000000000000, 0.9659258262890683122, 1.000000000000000000, 0.9659258262890683122, 1.000000000000000000, 0.9659258262890683122, 1.000000000000000000, 0.9659258262890683122, 1.000000000000000000, 0.9659258262890683122, 1.000000000000000000, 0.9659258262890683122, 1.000000000000000000, 0.9659258262890683122, 1.000000000000000000, 0.9659258262890683122, 1.000000000000000000, 0.9659258262890683122, 1.000000000000000000, 0.9659258262890683122, 1.000000000000000000, 0.9659258262890683122, 1.000000000000000000, 0.9659258262890683122, 1.000000000000000000, 0.9659258262890683122, 1.000000000000000000, 0.9659258262890683122, 1.000000000000000000, 0.9659258262890683122, 1.000000000000000000, 0.9659258262890683122, 1.000000000000000000, 0.9659258262890683122, 1.000000000000000000, 0.9659258262890683122, 1.000000000000000000, 0.9659258262890683122, 1.000000000000000000, 0.9659258262890683122, 1.000000000000000000, 0.9659258262890683122, 1.000000000000000000, 0.9659258262890683122, 1.000000000000000000, 0.9659258262890683122, 1.000000000000000000, 0.9659258262890683122, 1.000000000000000000, 0.9659258262890683122, 1.000000000000000000, 0.9659258262890683122, 1.000000000000000000, 0.9659258262890683122, 1.000000000000000000, 0.9659258262890683122, 1.000000000000000000, 0.9659258262890683122, 1.000000000000000000, 0.9659258262890683122, 1.000000000000000000, 0.9659258262890683122, 1.000000000000000000, 0.9659258262890683122, 1.000000000000000000, 0.9659258262890683122, 1.000000000000000000, 0.9659258262890683122, 1.000000000000000000, 0.9659258262890683122, 1.000000000000000000, 0.9659258262890683122, 1.000000000000000000, 0.9659258262890683122, 1.000000000000000000, 0.9659258262890683122, 1.000000000000000000, 0.9659258262890683122, 1.000000000000000000, 0.9659258262890683122, 1.000000000000000000, 0.9659258262890683122, 1.000000000000000000, 0.9659258262890683122, 1.000000000000000000, 0.9659258262890683122, 1.000000000000000000, 0.9659258262890683122, 1.000000000000000000, 0.9659258262890683122, 1.000000000000000000, 0.9659258262890683122, 1.000000000000000000, 0.9659258262890683122, 1.000000000000000000, 0.9659258262890683122, 1.000000000000000000, 0.9659258262890683122, 1.000000000000000000, 0.9659258262890683122, 1.000000000000000000, 0.9659258262890683122, 1.000000000000000000, 0.9659258262890683122, 1.000000000000000000, 0.9659258262890683122, 1.000000000000000000, 0.9659258262890683122, 1.000000000000000000, 0.9659258262890683122, 1.000000000000000000, 0.9659258262890683122, 1.000000000000000000, 0.9659258262890683122, 1.000000000000000000, 0.9659258262890683122, 1.000000000000000000, 0.9659258262890683122, 1.000000000000000000, 0.9659258262890683122, 1.000000000000000000, 0.9659258262890683122, 1.000000000000000000, 0.9659258262890683122, 1.000000000000000000, 0.9659258262890683122, 1.000000000000000000, 0.9659258262890683122, 1.000000000000000000, 0.9659258262890683122, 1.000000000000000000, 0.9659258262890683122, 1.000000000000000000, 0.9659258262890683122, 1.000000000000000000, 0.9659258262890683122, 1.000000000000000000, 0.9659258262890683122, 1.000000000000000000, 0.9659258262890683122, 1.000000000000000000, 0.9659258262890683122, 1.000000000000000000, 0.9659258262890683122, 1.000000000000000000, 0.9659258262890683122, 1.000000000000000000, 0.9659258262890683122, 1.000000000000000000, 0.9659258262890683122, 1.000000000000000000, 0.9659258262890683122, 1.000000000000000000, 0.9659258262890683122, 1.000000000000000000, 0.9659258262890683122, 1.000000000000000000, 0.9659258262890683122, 1.000000000000000000, 0.9659258262890683122, 1.000000000000000000, 0.9659258262890683122, 1.000000000000000000, 0.9659258262890683122, 1.000000000000000000, 0.9659258262890683122, 1.000000000000000000, 0.9659258262890683122, 1.000000000000000000, 0.9659258262890683122, 1.000000000000000000, 0.9659258262890683122, 1.000000000000000000, 0.9659258262890683122, 1.000000000000000000, 0.9659258262890683122, 1.000000000000000000, 0.9659258262890683122, 1.000000000000000000, 0.9659258262890683122, 1.000000000000000000, 0.9659258262890683122, 1.000000000000000000, 0.9659258262890683122, 1.000000000000000000, 0.9659258262890683122, 1.000000000000000000, 0.9659258262890683122, 1.000000000000000000, 0.9659258262890683122, 1.000000000000000000, 0.9659258262890683122, 1.000000000000000000, 0.9659258262890683122, 1.000000000000000000, 0.9659258262890683122, 1.000000000000000000, 0.9659258262890683122, 1.000000000000000000, 0.9659258262890683122, 1.000000000000000000, 0.9659258262890683122, 1.000000000000000000, 0.9659258262890683122, 1.000000000000000000, 0.9659258262890683122, 1.000000000000000000, 0.9659258262890683122, 1.000000000000000000, 0.9659258262890683122, 1.000000000000000000, 0.9659258262890683122, 1.000000000000000000, 0.9659258262890683122, 1.000000000000000000, 0.9659258262890683122, 1.000000000000000000, 0.9659258262890683122, 1.000000000000000000, 0.9659258262890683122, 1.000000000000000000, 0.9659258262890683122, 1.000000000000000000, 0.9659258262890683122, 1.000000000000000000, 0.9659258262890683122, 1.000000000000000000, 0.9659258262890683122, 1.000000000000000000, 0.9659258262890683122, 1.000000000000000000, 0.9659258262890683122, 1.000000000000000000, 0.9659258262890683122, 1.000000000000000000, 0.9659258262890683122, 1.000000000000000000, 0.9659258262890683122, 1.000000000000000000, 0.9659258262890683122, 1.000000000000000000, 0.9659258262890683122, 1.000000000000000000, 0.9659258262890683122, 1.000000000000000000, 0.9659258262890683122, 1.000000000000000000, 0.9659258262890683122, 1.000000000000000000, 0.9659258262890683122, 1.000000000000000000, 0.9659258262890683122, 1.000000000000000000, 0.9659258262890683122, 1.000000000000000000, 0.9659258262890683122, 1.000000000000000000, 0.9659258262890683122, 1.000000000000000000, 0.9659258262890683122, 1.000000000000000000, 0.9659258262890683122, 1.000000000000000000, 0.9659258262890683122, 1.000000000000000000, 0.9659258262890683122, 1.000000000000000000, 0.9659258262890683122, 1.000000000000000000, 0.9659258262890683122, 1.000000000000000000, 0.9659258262890683122, 1.000000000000000000, 0.9659258262890683122, 1.000000000000000000, 0.9659258262890683122, 1.000000000000000000, 0.9659258262890683122, 1.000000000000000000, 0.9659258262890683122, 1.000000000000000000, 0.9659258262890683122, 1.000000000000000000, 0.9659258262890683122, 1.000000000000000000, 0.9659258262890683122, 1.000000000000000000, 0.9659258262890683122, 1.000000000000000000, 0.9659258262890683122, 1.000000000000000000, 0.9659258262890683122, 1.000000000000000000, 0.9659258262890683122, 1.000000000000000000, 0.9659258262890683122, 1.000000000000000000, 0.9659258262890683122, 1.000000000000000000, 0.9659258262890683122, 1.000000000000000000, 0.9659258262890683122, 1.000000000000000000, 0.9659258262890683122, 1.000000000000000000, 0.9659258262890683122, 1.000000000000000000, 0.9659258262890683122, 1.000000000000000000, 0.9659258262890683122, 1.000000000000000000, 0.9659258262890683122, 1.000000000000000000, 0.9659258262890683122, 1.000000000000000000, 0.9659258262890683122, 1.000000000000000000, 0.9659258262890683122, 1.000000000000000000, 0.9659258262890683122, 1.000000000000000000, 0.9659258262890683122, 1.000000000000000000, 0.9737050196533417745, 0.9879936201322587763 ) ) 
 REPRESENTATION_ITEM ( '' )  );
#40818=ORIENTED_EDGE ( 'NONE', *, *, #64560, .F. ) ;
#40827=ADVANCED_FACE ( 'NONE', ( #31770 ), #42332, .T. ) ;
#40847=CARTESIAN_POINT ( 'NONE',  ( 10.00000000000000000, 99.79166666666667140, 2.679491924311236062 ) ) ;
#40849=CARTESIAN_POINT ( 'NONE',  ( -11.35316468750000141, 63.59374999658601268, -1.390361679473963753E-15 ) ) ;
#40850=CARTESIAN_POINT ( 'NONE',  ( 6.000000000000001776, 288.5000000000000000, -7.347880794884121708E-16 ) ) ;
#40854=AXIS2_PLACEMENT_3D ( 'NONE', #67482, #62553, #39559 ) ;
#40857=CARTESIAN_POINT ( 'NONE',  ( 6.123233995736767268E-16, 58.12499999317203248, -10.00000000000000178 ) ) ;
#40860=CARTESIAN_POINT ( 'NONE',  ( -4.242640687119285658, 293.1249999999999432, 4.242640687119287435 ) ) ;
#40862=CARTESIAN_POINT ( 'NONE',  ( 10.00000000000000178, 220.0000000000000000, 0.000000000000000000 ) ) ;
#40863=ADVANCED_FACE ( 'NONE', ( #3474 ), #31392, .T. ) ;
#40865=CARTESIAN_POINT ( 'NONE',  ( 11.35316468749999963, 186.3020833299193555, -3.042071309553165293 ) ) ;
#40866=CARTESIAN_POINT ( 'NONE',  ( -4.999999999999996447, 36.66666666666665719, -8.660254037844387298 ) ) ;
#40867=CARTESIAN_POINT ( 'NONE',  ( 8.660254037844389075, 177.2916666598387110, -5.000000000000000000 ) ) ;
#40868=FACE_OUTER_BOUND ( 'NONE', #43489, .T. ) ;
#40869=CARTESIAN_POINT ( 'NONE',  ( -6.000000000000001776, 297.0625000034140157, 0.000000000000000000 ) ) ;
#40873=CARTESIAN_POINT ( 'NONE',  ( 8.311093377946834337, 35.46874999658600558, 8.311093377946839666 ) ) ;
#40876=CARTESIAN_POINT ( 'NONE',  ( -8.660254037844387298, 123.9583333265053682, -5.000000000000004441 ) ) ;
#40878=CARTESIAN_POINT ( 'NONE',  ( -9.999999999999982236, 102.7083333333333286, 2.679491924311216966 ) ) ;
#40880=CARTESIAN_POINT ( 'NONE',  ( 8.660254037844385522, 76.45833332650536818, 5.000000000000005329 ) ) ;
#40883=CARTESIAN_POINT ( 'NONE',  ( 6.123233995736767268E-16, 56.25000000000000000, -10.00000000000000178 ) ) ;
#40886=VERTEX_POINT ( 'NONE', #15151 ) ;
#40887=ORIENTED_EDGE ( 'NONE', *, *, #68094, .T. ) ;
#40889=CARTESIAN_POINT ( 'NONE',  ( -4.721056650415998313, 296.7343750017069510, 4.721056650416000089 ) ) ;
#40892=CARTESIAN_POINT ( 'NONE',  ( -2.085542519210945728E-15, 154.5312499965860127, 11.35316468750000141 ) ) ;
#40893=CARTESIAN_POINT ( 'NONE',  ( 9.999999999999985789, 105.2083333333333286, -2.679491924311223183 ) ) ;
#40902=CARTESIAN_POINT ( 'NONE',  ( -9.832129032723420536, 124.0104166632526841, 5.676582343749997150 ) ) ;
#40906=CARTESIAN_POINT ( 'NONE',  ( -5.676582343750006032, 44.42708332991934839, 9.832129032723418760 ) ) ;
#40909=CARTESIAN_POINT ( 'NONE',  ( -10.00000000000000355, 194.5833333265053682, 2.679491924311223183 ) ) ;
#40913=CARTESIAN_POINT ( 'NONE',  ( 4.242640687119287435, 295.4375000034140157, 4.242640687119285658 ) ) ;
#40918=( BOUNDED_CURVE ( )  B_SPLINE_CURVE ( 2, ( #45705, #50996, #57794, #28725, #39317, #21945, #74376, #27609, #34417, #6102, #57420, #39680, #62679 ),
 .UNSPECIFIED., .F., .F. ) 
 B_SPLINE_CURVE_WITH_KNOTS ( ( 3, 2, 2, 2, 2, 2, 3 ),
 ( 0.005434782608695652023, 0.007246376811594202987, 0.009057971014492753950, 0.01086956521739130405, 0.01268115942028985588, 0.01449275362318840597, 0.01630434782608695607 ),
 .UNSPECIFIED. ) 
 CURVE ( )  GEOMETRIC_REPRESENTATION_ITEM ( )  RATIONAL_B_SPLINE_CURVE ( ( 1.000000000000000000, 0.9659258262890683122, 1.000000000000000000, 0.9659258262890683122, 1.000000000000000000, 0.9659258262890683122, 1.000000000000000000, 0.9659258262890683122, 1.000000000000000000, 0.9659258262890683122, 1.000000000000000000, 0.9659258262890683122, 1.000000000000000000 ) ) 
 REPRESENTATION_ITEM ( '' )  );
#40920=AXIS2_PLACEMENT_3D ( 'NONE', #62314, #74008, #90 ) ;
#40923=AXIS2_PLACEMENT_3D ( 'NONE', #37699, #38445, #9019 ) ;
#40934=ORIENTED_EDGE ( 'NONE', *, *, #65292, .F. ) ;
#40940=CARTESIAN_POINT ( 'NONE',  ( 10.00000000000000000, 59.79166666666667851, 2.679491924311236062 ) ) ;
#40954=CARTESIAN_POINT ( 'NONE',  ( -7.320508075688778149, 158.1249999999999716, 7.320508075688769267 ) ) ;
#40958=CARTESIAN_POINT ( 'NONE',  ( -8.311093377946841443, 144.2187499965860127, 8.311093377946830785 ) ) ;
#40960=CARTESIAN_POINT ( 'NONE',  ( -1.836970198721029983E-15, 25.62499999317203248, 10.00000000000000178 ) ) ;
#40965=CARTESIAN_POINT ( 'NONE',  ( 11.35316468750000141, 1.093749996586016682, 0.000000000000000000 ) ) ;
#40968=CARTESIAN_POINT ( 'NONE',  ( 10.00000000000011013, 195.0000000000000568, 0.000000000000000000 ) ) ;
#40971=CARTESIAN_POINT ( 'NONE',  ( -1.836970198721029983E-15, 30.62499999317203248, 10.00000000000000178 ) ) ;
#40978=CARTESIAN_POINT ( 'NONE',  ( -5.676582343749998039, 112.4479166632526983, -9.832129032723420536 ) ) ;
#40983=CARTESIAN_POINT ( 'NONE',  ( -2.085542519210945728E-15, 114.5312499965860269, 11.35316468750000141 ) ) ;
#40984=ORIENTED_EDGE ( 'NONE', *, *, #28735, .F. ) ;
#40988=CARTESIAN_POINT ( 'NONE',  ( 2.679491924311222739, 225.8333333265053398, 10.00000000000000355 ) ) ;
#40992=CARTESIAN_POINT ( 'NONE',  ( -3.042071309553163960, 102.2395833299193697, -11.35316468749999963 ) ) ;
#40995=CARTESIAN_POINT ( 'NONE',  ( -2.220555325575947149E-11, 176.2500000000017621, -10.00000000000000533 ) ) ;
#40998=CARTESIAN_POINT ( 'NONE',  ( 2.679491924311228956, 192.9166666598387110, -10.00000000000000000 ) ) ;
#41001=CARTESIAN_POINT ( 'NONE',  ( -9.832129032723418760, 88.17708332991934128, -5.676582343750004256 ) ) ;
#41005=CARTESIAN_POINT ( 'NONE',  ( 3.042071309553159519, 5.052083329919351051, 11.35316468750000141 ) ) ;
#41008=CARTESIAN_POINT ( 'NONE',  ( 3.042071309553167513, 221.8229166632526983, -11.35316468749999785 ) ) ;
#41010=CARTESIAN_POINT ( 'NONE',  ( -1.836970198721029983E-15, 45.62499999317203958, 10.00000000000000178 ) ) ;
#41012=CARTESIAN_POINT ( 'NONE',  ( 4.721056650416000089, 294.8281250017069510, 4.721056650415999201 ) ) ;
#41015=CARTESIAN_POINT ( 'NONE',  ( -9.832129032723418760, 203.1770833299193555, -5.676582343750004256 ) ) ;
#41022=ORIENTED_EDGE ( 'NONE', *, *, #62342, .T. ) ;
#41025=CARTESIAN_POINT ( 'NONE',  ( 7.320508075688771044, 24.37499999999999645, 7.320508075688775484 ) ) ;
#41026=DIRECTION ( 'NONE',  ( 0.000000000000000000, 0.000000000000000000, 1.000000000000000000 ) ) ;
#41036=CARTESIAN_POINT ( 'NONE',  ( 10.00000000000000178, 152.0833333265053682, -2.679491924311226736 ) ) ;
#41037=CARTESIAN_POINT ( 'NONE',  ( 6.676582343750002480, 297.0156250017069510, -2.765530957081997254 ) ) ;
#41043=ORIENTED_EDGE ( 'NONE', *, *, #28829, .T. ) ;
#41045=CARTESIAN_POINT ( 'NONE',  ( 11.35316468750000141, 101.0937499965860127, 0.000000000000000000 ) ) ;
#41055=CARTESIAN_POINT ( 'NONE',  ( 3.042071309553167069, 216.8229166632526699, -11.35316468749999785 ) ) ;
#41059=CARTESIAN_POINT ( 'NONE',  ( 11.35316468750000141, 176.0937499965860411, 0.000000000000000000 ) ) ;
#41061=CARTESIAN_POINT ( 'NONE',  ( -6.000000000000001776, 296.0625000034140157, 0.000000000000000000 ) ) ;
#41062=CARTESIAN_POINT ( 'NONE',  ( 1.567784982238203817E-13, 108.7500000000000426, 10.00000000000000533 ) ) ;
#41066=CARTESIAN_POINT ( 'NONE',  ( 9.832129032723416984, 65.36458332991935549, 5.676582343750006032 ) ) ;
#41072=CARTESIAN_POINT ( 'NONE',  ( -8.311093377946836114, 77.65624999658602690, -8.311093377946837890 ) ) ;
#41077=CARTESIAN_POINT ( 'NONE',  ( 9.832129032723420536, 61.19791666325267698, -5.676582343749999815 ) ) ;
#41081=CARTESIAN_POINT ( 'NONE',  ( 10.00000000000000178, 162.0833333265053682, -2.679491924311226736 ) ) ;
#41084=CARTESIAN_POINT ( 'NONE',  ( 8.311093377946837890, 46.71874999658602690, -8.311093377946837890 ) ) ;
#41086=CARTESIAN_POINT ( 'NONE',  ( 3.042071309553159519, 184.7395833299193839, 11.35316468750000141 ) ) ;
#41092=CARTESIAN_POINT ( 'NONE',  ( -5.676582343749998039, 177.4479166632526983, -9.832129032723420536 ) ) ;
#41099=CARTESIAN_POINT ( 'NONE',  ( -5.676582343750006032, 169.4270833299193555, 9.832129032723418760 ) ) ;
#41102=CARTESIAN_POINT ( 'NONE',  ( -11.35316468749999785, 128.3854166632526699, -3.042071309553167513 ) ) ;
#41112=( BOUNDED_CURVE ( )  B_SPLINE_CURVE ( 2, ( #47342, #41324, #30370, #1714, #7362, #71448, #18683, #65054, #36772 ),
 .UNSPECIFIED., .F., .F. ) 
 B_SPLINE_CURVE_WITH_KNOTS ( ( 3, 2, 2, 2, 3 ),
 ( 0.1041666666666644370, 0.1145833333333311083, 0.1249999999999977796, 0.1354166666666644647, 0.1458333333333311499 ),
 .UNSPECIFIED. ) 
 CURVE ( )  GEOMETRIC_REPRESENTATION_ITEM ( )  RATIONAL_B_SPLINE_CURVE ( ( 1.000000000000016431, 0.9238795325112704182, 1.000000000000000000, 0.9238795325112867385, 1.000000000000000000, 0.9238795325112867385, 1.000000000000000000, 0.9238795325113027257, 0.9999999999999840128 ) ) 
 REPRESENTATION_ITEM ( '' )  );
#41121=CARTESIAN_POINT ( 'NONE',  ( -10.00000000000018296, 157.2916666666667709, -2.679491924311279583 ) ) ;
#41129=CARTESIAN_POINT ( 'NONE',  ( 1.102182119232618108E-15, 290.3125000034140157, 6.000000000000001776 ) ) ;
#41131=CARTESIAN_POINT ( 'NONE',  ( 6.676582343750003368, 299.0468750017069510, 2.765530957081995478 ) ) ;
#41132=CARTESIAN_POINT ( 'NONE',  ( 5.000000000000001776, 140.8333333333333428, -8.660254037844389075 ) ) ;
#41149=CARTESIAN_POINT ( 'NONE',  ( 8.660254037844385522, 51.45833332650536818, 5.000000000000005329 ) ) ;
#41151=CARTESIAN_POINT ( 'NONE',  ( -5.676582343749998039, 27.44791666325268409, -9.832129032723420536 ) ) ;
#41152=CARTESIAN_POINT ( 'NONE',  ( 7.320508075689011740, 24.37500000000018829, 7.320508075689014404 ) ) ;
#41153=CARTESIAN_POINT ( 'NONE',  ( 11.35316468749999785, 215.8854166632526983, 3.042071309553174174 ) ) ;
#41159=CARTESIAN_POINT ( 'NONE',  ( -3.042071309553164404, 42.23958332991933418, -11.35316468749999963 ) ) ;
#41165=CARTESIAN_POINT ( 'NONE',  ( -8.311093377946841443, 23.90624999658601979, 8.311093377946834337 ) ) ;
#41167=CARTESIAN_POINT ( 'NONE',  ( 11.35316468750000141, 145.7812499965860411, 0.000000000000000000 ) ) ;
#41168=CARTESIAN_POINT ( 'NONE',  ( -1.836970198721029983E-15, 110.6249999931720396, 10.00000000000000178 ) ) ;
#41173=EDGE_LOOP ( 'NONE', ( #27853, #41022, #62032, #49355 ) ) ;
#41174=CARTESIAN_POINT ( 'NONE',  ( -11.35316468749999785, 3.385416663252682756, -3.042071309553167957 ) ) ;
#41177=CARTESIAN_POINT ( 'NONE',  ( -6.676582343750003368, 297.3906250017068942, -2.765530957081996810 ) ) ;
#41179=CARTESIAN_POINT ( 'NONE',  ( 9.832129032723420536, 136.1979166632526983, -5.676582343749999815 ) ) ;
#41187=CARTESIAN_POINT ( 'NONE',  ( -3.171697045051319909E-12, 121.2500000000002558, -10.00000000000000178 ) ) ;
#41189=CARTESIAN_POINT ( 'NONE',  ( -3.042071309553173730, 89.63541666325268409, 11.35316468749999785 ) ) ;
#41204=LINE ( 'NONE', #52523, #5968 ) ;
#41220=CARTESIAN_POINT ( 'NONE',  ( 2.679491924311222739, 88.95833333333332860, 10.00000000000000355 ) ) ;
#41223=CARTESIAN_POINT ( 'NONE',  ( 3.042071309553167069, 57.13541666325268409, -11.35316468749999785 ) ) ;
#41224=CARTESIAN_POINT ( 'NONE',  ( -6.000000000000000888, 290.0625000000000000, 2.485281374238575758 ) ) ;
#41227=LINE ( 'NONE', #5047, #66257 ) ;
#41236=CARTESIAN_POINT ( 'NONE',  ( 5.000000000000001776, 220.8333333333333428, -8.660254037844389075 ) ) ;
#41238=CARTESIAN_POINT ( 'NONE',  ( 11.35316468749999785, 180.8854166632526699, 3.042071309553174174 ) ) ;
#41240=CARTESIAN_POINT ( 'NONE',  ( 10.00000000000000178, 176.8749999931720538, 0.000000000000000000 ) ) ;
#41245=CARTESIAN_POINT ( 'NONE',  ( -9.832129032723418760, 43.17708332991934839, -5.676582343750004256 ) ) ;
#41250=CARTESIAN_POINT ( 'NONE',  ( -9.999999999999980460, 102.5000000000000000, -1.224646799147350693E-15 ) ) ;
#41252=CARTESIAN_POINT ( 'NONE',  ( -10.00000000000000355, 79.58333332650536818, 2.679491924311223183 ) ) ;
#41255=CARTESIAN_POINT ( 'NONE',  ( -8.660254037844392627, 72.91666666666667140, 5.000000000000000888 ) ) ;
#41256=CARTESIAN_POINT ( 'NONE',  ( -10.00000000000000355, 49.58333332650536818, 2.679491924311223183 ) ) ;
#41261=CARTESIAN_POINT ( 'NONE',  ( -4.721056650415999201, 298.4843750017070079, -4.721056650415999201 ) ) ;
#41263=CARTESIAN_POINT ( 'NONE',  ( 1.224646799147353454E-15, 300.0000000000000000, -10.00000000000000178 ) ) ;
#41264=CARTESIAN_POINT ( 'NONE',  ( 5.676582343749993598, 154.9479166632526983, 9.832129032723422313 ) ) ;
#41274=CARTESIAN_POINT ( 'NONE',  ( 5.676582343749993598, 145.2604166632526699, 9.832129032723422313 ) ) ;
#41276=CARTESIAN_POINT ( 'NONE',  ( 2.485281374238152097, 298.7500000034140157, -6.000000000000420997 ) ) ;
#41278=CARTESIAN_POINT ( 'NONE',  ( -11.35316468750000141, 43.80208332991934839, 3.042071309553159963 ) ) ;
#41285=CARTESIAN_POINT ( 'NONE',  ( -6.000000000000003553, 293.0000000034139589, -2.485281374238571317 ) ) ;
#41294=CARTESIAN_POINT ( 'NONE',  ( -2.679491924311235174, 65.41666665983871098, 10.00000000000000000 ) ) ;
#41302=CARTESIAN_POINT ( 'NONE',  ( -1.269107444400135093E-11, 58.74999999999901945, 10.00000000000000178 ) ) ;
#41309=CARTESIAN_POINT ( 'NONE',  ( -4.999999999999998224, 43.54166665983870388, -8.660254037844389075 ) ) ;
#41310=CARTESIAN_POINT ( 'NONE',  ( 6.123233995736767268E-16, 61.25000000000000711, -10.00000000000000178 ) ) ;
#41312=CARTESIAN_POINT ( 'NONE',  ( 6.000000000000001776, 299.5000000000000000, -7.347880794884121708E-16 ) ) ;
#41313=CARTESIAN_POINT ( 'NONE',  ( -10.00000000000000355, 34.58333332650536818, 2.679491924311223183 ) ) ;
#41320=CARTESIAN_POINT ( 'NONE',  ( 7.347880794884121708E-16, 284.0000000000000000, -6.000000000000001776 ) ) ;
#41321=DIRECTION ( 'NONE',  ( -0.000000000000000000, 1.000000000000000000, -0.000000000000000000 ) ) ;
#41322=CARTESIAN_POINT ( 'NONE',  ( -1.836970198721029983E-15, 200.6249999931720538, 10.00000000000000178 ) ) ;
#41323=CARTESIAN_POINT ( 'NONE',  ( 10.00000000000000178, 175.2083333333333144, -2.679491924311226736 ) ) ;
#41324=CARTESIAN_POINT ( 'NONE',  ( 2.485281374238163199, 297.7500000034140726, -6.000000000000410338 ) ) ;
#41326=CARTESIAN_POINT ( 'NONE',  ( -2.085542519210945728E-15, 139.8437499965860127, 11.35316468750000141 ) ) ;
#41327=CARTESIAN_POINT ( 'NONE',  ( 6.000000000000001776, 294.5625000034140157, -7.347880794884121708E-16 ) ) ;
#41339=CARTESIAN_POINT ( 'NONE',  ( 5.000000000000001776, 32.70833332650536107, -8.660254037844389075 ) ) ;
#41348=CARTESIAN_POINT ( 'NONE',  ( 2.679491924311224071, 28.95833333333333570, 10.00000000000000711 ) ) ;
#41349=CARTESIAN_POINT ( 'NONE',  ( -6.607085568835331379, 225.9999999999999716, 7.535105736105112584 ) ) ;
#41352=CARTESIAN_POINT ( 'NONE',  ( 5.676582343749993598, 114.9479166632526983, 9.832129032723422313 ) ) ;
#41360=CARTESIAN_POINT ( 'NONE',  ( 11.35316468749999963, 110.9895833299193555, -3.042071309553165293 ) ) ;
#41363=CARTESIAN_POINT ( 'NONE',  ( 8.660254037844390851, 50.41666666666667851, -5.000000000000002665 ) ) ;
#41365=( BOUNDED_CURVE ( )  B_SPLINE_CURVE ( 2, ( #72759, #2974, #42945, #20686, #43705, #15023, #20304, #65965, #37306, #38058, #66719, #54665, #32781 ),
 .UNSPECIFIED., .F., .F. ) 
 B_SPLINE_CURVE_WITH_KNOTS ( ( 3, 2, 2, 2, 2, 2, 3 ),
 ( 1.020494457342402184, 1.025727047095130073, 1.030959636847857963, 1.036192226600586075, 1.041424816353313965, 1.046657406106042076, 1.051889995858769966 ),
 .UNSPECIFIED. ) 
 CURVE ( )  GEOMETRIC_REPRESENTATION_ITEM ( )  RATIONAL_B_SPLINE_CURVE ( ( 1.000000000000096145, 0.9659258262889722779, 1.000000000000000000, 0.9659258262890683122, 1.000000000000000000, 0.9659258262890683122, 1.000000000000000000, 0.9659258262890683122, 1.000000000000000000, 0.9659258262890683122, 1.000000000000000000, 0.9659258262890683122, 1.000000000000000000 ) ) 
 REPRESENTATION_ITEM ( '' )  );
#41366=CARTESIAN_POINT ( 'NONE',  ( -2.679491924311225848, 198.3333333265053398, -10.00000000000000178 ) ) ;
#41370=CARTESIAN_POINT ( 'NONE',  ( -8.311093377946836114, 82.96874999658602690, -8.311093377946837890 ) ) ;
#41374=CARTESIAN_POINT ( 'NONE',  ( 11.35316468749999785, 15.88541666325268586, 3.042071309553174174 ) ) ;
#41376=CARTESIAN_POINT ( 'NONE',  ( -8.660254037844397956, 137.9166666666667140, 5.000000000000002665 ) ) ;
#41378=CARTESIAN_POINT ( 'NONE',  ( -3.042071309553163960, 222.2395833299193555, -11.35316468749999963 ) ) ;
#41382=CARTESIAN_POINT ( 'NONE',  ( 6.676582343750003368, 292.0156250017069510, -2.765530957081997254 ) ) ;
#41386=CARTESIAN_POINT ( 'NONE',  ( -8.311093377946836114, 207.9687499965859843, -8.311093377946837890 ) ) ;
#41391=VECTOR ( 'NONE', #45707, 1000.000000000000000 ) ;
#41394=CARTESIAN_POINT ( 'NONE',  ( 2.679491924311228956, 31.04166666666666430, -10.00000000000000000 ) ) ;
#41397=ORIENTED_EDGE ( 'NONE', *, *, #60989, .T. ) ;
#41403=CARTESIAN_POINT ( 'NONE',  ( 6.676582343750003368, 295.8906250017069510, 2.765530957081995478 ) ) ;
#41415=CARTESIAN_POINT ( 'NONE',  ( 9.832129032723416984, 100.6770833299193555, 5.676582343750006032 ) ) ;
#41425=CARTESIAN_POINT ( 'NONE',  ( -9.832129032723418760, 212.8645833299193555, -5.676582343750004256 ) ) ;
#41429=CARTESIAN_POINT ( 'NONE',  ( 8.311093377946834337, 180.4687499965859843, 8.311093377946839666 ) ) ;
#41431=CARTESIAN_POINT ( 'NONE',  ( -6.000000000000003553, 296.0000000034139589, -2.485281374238571317 ) ) ;
#41436=CARTESIAN_POINT ( 'NONE',  ( -11.35316468750000141, 68.28124999658602690, -1.390361679473963753E-15 ) ) ;
#41437=EDGE_CURVE ( 'NONE', #57818, #20466, #65258, .T. ) ;
#41441=CARTESIAN_POINT ( 'NONE',  ( -1.836970198721029983E-15, 190.6249999931720254, 10.00000000000000178 ) ) ;
#41443=CARTESIAN_POINT ( 'NONE',  ( -3.042071309553173730, 74.32291666325268409, 11.35316468749999785 ) ) ;
#41448=CARTESIAN_POINT ( 'NONE',  ( -11.35316468750000141, 53.28124999658601979, -1.390361679473963753E-15 ) ) ;
#41450=CARTESIAN_POINT ( 'NONE',  ( 0.000000000000000000, 300.0000000000000000, 0.000000000000000000 ) ) ;
#41451=CARTESIAN_POINT ( 'NONE',  ( 8.660254037844385522, 151.4583333265053682, 5.000000000000005329 ) ) ;
#41453=CARTESIAN_POINT ( 'NONE',  ( 10.00000000000000711, 19.79166666666667140, 2.679491924311237838 ) ) ;
#41454=CARTESIAN_POINT ( 'NONE',  ( -9.832129032723418760, 48.17708332991934839, -5.676582343750004256 ) ) ;
#41457=CARTESIAN_POINT ( 'NONE',  ( -5.676582343749998039, 197.4479166632526983, -9.832129032723420536 ) ) ;
#41458=ORIENTED_EDGE ( 'NONE', *, *, #9748, .T. ) ;
#41461=CARTESIAN_POINT ( 'NONE',  ( 2.679491924311228956, 62.91666665983869677, -10.00000000000000000 ) ) ;
#41463=CARTESIAN_POINT ( 'NONE',  ( 5.676582343750001591, 176.6145833299193555, -9.832129032723420536 ) ) ;
#41466=DIRECTION ( 'NONE',  ( 0.000000000000000000, 0.000000000000000000, 1.000000000000000000 ) ) ;
#41468=CARTESIAN_POINT ( 'NONE',  ( 9.832129032723420536, 171.5104166632526983, -5.676582343749999815 ) ) ;
#41482=LINE ( 'NONE', #24495, #22551 ) ;
#41484=ORIENTED_EDGE ( 'NONE', *, *, #48437, .T. ) ;
#41491=ORIENTED_EDGE ( 'NONE', *, *, #48563, .F. ) ;
#41497=CARTESIAN_POINT ( 'NONE',  ( 6.676582343750002480, 299.1718750017070079, -2.765530957081997254 ) ) ;
#41498=CARTESIAN_POINT ( 'NONE',  ( 10.00000000000000000, 134.7916666666666572, 2.679491924311236062 ) ) ;
#41513=CARTESIAN_POINT ( 'NONE',  ( -9.832129032723420536, 33.69791666325268409, 5.676582343749997150 ) ) ;
#41514=CARTESIAN_POINT ( 'NONE',  ( -3.673940397442060854E-16, 288.7500000000000000, -6.000000000000001776 ) ) ;
#41515=CARTESIAN_POINT ( 'NONE',  ( 9.832129032723416984, 215.6770833299193555, 5.676582343750006032 ) ) ;
#41521=CARTESIAN_POINT ( 'NONE',  ( -9.832129032723418760, 37.86458332991934839, -5.676582343750004256 ) ) ;
#41524=EDGE_CURVE ( 'NONE', #57671, #18660, #2264, .T. ) ;
#41525=CARTESIAN_POINT ( 'NONE',  ( -4.242640687119286547, 294.9375000034140157, -4.242640687119286547 ) ) ;
#41528=CARTESIAN_POINT ( 'NONE',  ( 11.35316468749999785, 20.57291666325268409, 3.042071309553174174 ) ) ;
#41530=CARTESIAN_POINT ( 'NONE',  ( 11.35316468749999785, 150.5729166632526699, 3.042071309553174174 ) ) ;
#41531=CARTESIAN_POINT ( 'NONE',  ( 10.00000000000000178, 112.0833333265053824, -2.679491924311226736 ) ) ;
#41533=CARTESIAN_POINT ( 'NONE',  ( -3.673940397442060854E-16, 293.8125000034140157, -6.000000000000001776 ) ) ;
#41536=CARTESIAN_POINT ( 'NONE',  ( 5.676582343749993598, 5.260416663252683200, 9.832129032723422313 ) ) ;
#41539=CARTESIAN_POINT ( 'NONE',  ( 2.765530957082001251, 297.7656250017069510, 6.676582343750000703 ) ) ;
#41541=CARTESIAN_POINT ( 'NONE',  ( -3.042071309553173730, 134.3229166632526983, 11.35316468749999785 ) ) ;
#41548=ORIENTED_EDGE ( 'NONE', *, *, #21030, .F. ) ;
#41549=CARTESIAN_POINT ( 'NONE',  ( 0.000000000000000000, 300.0000000000000000, 0.000000000000000000 ) ) ;
#41551=CARTESIAN_POINT ( 'NONE',  ( -5.676582343750006032, 89.42708332991934128, 9.832129032723418760 ) ) ;
#41556=ORIENTED_EDGE ( 'NONE', *, *, #51034, .T. ) ;
#41575=( BOUNDED_CURVE ( )  B_SPLINE_CURVE ( 2, ( #19049, #13734, #24339, #6999, #63970, #36779, #59060, #52284, #30377, #47349, #65438, #70373, #12282 ),
 .UNSPECIFIED., .F., .F. ) 
 B_SPLINE_CURVE_WITH_KNOTS ( ( 3, 2, 2, 2, 2, 2, 3 ),
 ( 0.4510869565217391353, 0.4528985507246376940, 0.4547101449275362528, 0.4565217391304348116, 0.4583333333333333703, 0.4601449275362319291, 0.4619565217391304879 ),
 .UNSPECIFIED. ) 
 CURVE ( )  GEOMETRIC_REPRESENTATION_ITEM ( )  RATIONAL_B_SPLINE_CURVE ( ( 1.000000000000000000, 0.9659258262890683122, 1.000000000000000000, 0.9659258262890683122, 1.000000000000000000, 0.9659258262890683122, 1.000000000000000000, 0.9659258262890683122, 1.000000000000000000, 0.9659258262890683122, 1.000000000000000000, 0.9659258262890673130, 1.000000000000001110 ) ) 
 REPRESENTATION_ITEM ( '' )  );
#41582=CARTESIAN_POINT ( 'NONE',  ( -8.660254037844380193, 97.91666666666667140, 4.999999999999992006 ) ) ;
#41586=CARTESIAN_POINT ( 'NONE',  ( 5.000000000000001776, 100.8333333333333428, -8.660254037844389075 ) ) ;
#41587=EDGE_CURVE ( 'NONE', #4343, #60165, #43544, .T. ) ;
#41590=CARTESIAN_POINT ( 'NONE',  ( 5.676582343749993598, 60.26041666325268409, 9.832129032723422313 ) ) ;
#41591=CARTESIAN_POINT ( 'NONE',  ( -2.765530957081998586, 297.7968750017069510, 6.676582343750001591 ) ) ;
#41594=CARTESIAN_POINT ( 'NONE',  ( 1.332431167089188095E-11, 191.2499999999989768, -10.00000000000000533 ) ) ;
#41597=CARTESIAN_POINT ( 'NONE',  ( -8.660254037844387298, 103.9583333265053824, -5.000000000000004441 ) ) ;
#41601=CARTESIAN_POINT ( 'NONE',  ( -5.000000000000005329, 208.3333333333333428, 8.660254037844387298 ) ) ;
#41603=CARTESIAN_POINT ( 'NONE',  ( -9.832129032723420536, 184.0104166632526983, 5.676582343749997150 ) ) ;
#41610=CARTESIAN_POINT ( 'NONE',  ( -11.35316468750000141, 48.80208332991934128, 3.042071309553159963 ) ) ;
#41613=CARTESIAN_POINT ( 'NONE',  ( 3.508320828368888034, 227.0932894534376487, -10.79750125662090632 ) ) ;
#41616=CARTESIAN_POINT ( 'NONE',  ( 10.00000000000000355, 10.00000000000000178, 0.000000000000000000 ) ) ;
#41618=CARTESIAN_POINT ( 'NONE',  ( -7.320508075688757721, 101.8750000000000000, -7.320508075688758609 ) ) ;
#41620=CARTESIAN_POINT ( 'NONE',  ( 8.660254037844389075, 82.29166665983871098, -5.000000000000000000 ) ) ;
#41626=DIRECTION ( 'NONE',  ( 0.000000000000000000, 0.000000000000000000, 1.000000000000000000 ) ) ;
#41629=CARTESIAN_POINT ( 'NONE',  ( 6.676582343750003368, 296.1718750017069510, -2.765530957081997254 ) ) ;
#41632=CARTESIAN_POINT ( 'NONE',  ( -8.311093377946836114, 152.6562499965859843, -8.311093377946837890 ) ) ;
#41634=CARTESIAN_POINT ( 'NONE',  ( 5.000000000000001776, 2.708333326505365957, -8.660254037844389075 ) ) ;
#41638=ORIENTED_EDGE ( 'NONE', *, *, #42649, .T. ) ;
#41641=CARTESIAN_POINT ( 'NONE',  ( 3.042071309553159519, 145.0520833299193555, 11.35316468750000141 ) ) ;
#41645=CARTESIAN_POINT ( 'NONE',  ( 11.35316468749999785, 45.88541666325268409, 3.042071309553174174 ) ) ;
#41651=CARTESIAN_POINT ( 'NONE',  ( -4.242640687119286547, 292.9375000034140157, -4.242640687119286547 ) ) ;
#41662=VECTOR ( 'NONE', #56782, 1000.000000000000000 ) ;
#41675=CARTESIAN_POINT ( 'NONE',  ( 2.485281374238196062, 296.6875000000000000, -6.000000000000377476 ) ) ;
#41677=CARTESIAN_POINT ( 'NONE',  ( 6.123233995736767268E-16, 51.25000000000000711, -10.00000000000000178 ) ) ;
#41679=CARTESIAN_POINT ( 'NONE',  ( 6.000000000000001776, 294.5000000000000000, -7.347880794884121708E-16 ) ) ;
#41689=CARTESIAN_POINT ( 'NONE',  ( -2.679491924311235618, 178.5416666666666856, 10.00000000000000000 ) ) ;
#41692=CARTESIAN_POINT ( 'NONE',  ( 5.676582343750001591, 146.9270833299193555, -9.832129032723420536 ) ) ;
#41694=CARTESIAN_POINT ( 'NONE',  ( 0.000000000000000000, 300.0000000000000000, 0.000000000000000000 ) ) ;
#41705=CARTESIAN_POINT ( 'NONE',  ( -5.000000000000005329, 30.20833332650536818, 8.660254037844387298 ) ) ;
#41708=CARTESIAN_POINT ( 'NONE',  ( 1.567784982238203817E-13, 108.7500000000000426, 10.00000000000000533 ) ) ;
#41713=CARTESIAN_POINT ( 'NONE',  ( 2.485281374238919927, 292.3750000034140157, 5.999999999999654499 ) ) ;
#41717=CARTESIAN_POINT ( 'NONE',  ( 8.311093377946834337, 110.1562499965860269, 8.311093377946839666 ) ) ;
#41724=CARTESIAN_POINT ( 'NONE',  ( 1.046914569402248141, 225.9999999999998863, -9.958971312565205736 ) ) ;
#41725=CARTESIAN_POINT ( 'NONE',  ( 3.042071309553167513, 106.8229166632526841, -11.35316468749999785 ) ) ;
#41730=CARTESIAN_POINT ( 'NONE',  ( -2.679491924311235618, 195.4166666598387394, 10.00000000000000000 ) ) ;
#41734=CARTESIAN_POINT ( 'NONE',  ( -9.832129032723418760, 98.17708332991935549, -5.676582343750004256 ) ) ;
#41738=CARTESIAN_POINT ( 'NONE',  ( -8.311093377946841443, 9.218749996586016238, 8.311093377946830785 ) ) ;
#41746=CARTESIAN_POINT ( 'NONE',  ( -6.676582343750003368, 292.3906250017068942, -2.765530957081996810 ) ) ;
#41748=CARTESIAN_POINT ( 'NONE',  ( 5.676582343749993598, 220.2604166632526983, 9.832129032723422313 ) ) ;
#41758=CARTESIAN_POINT ( 'NONE',  ( -8.660254037844387298, 32.08333333333333570, -5.000000000000004441 ) ) ;
#41767=CARTESIAN_POINT ( 'NONE',  ( -6.676582343749999815, 295.5156250017069510, 2.765530957082001251 ) ) ;
#41771=ADVANCED_FACE ( 'NONE', ( #54149 ), #30391, .T. ) ;
#41777=CARTESIAN_POINT ( 'NONE',  ( -3.042071309553173730, 104.6354166632526699, 11.35316468749999785 ) ) ;
#41785=CARTESIAN_POINT ( 'NONE',  ( 8.311093377946834337, 215.1562499965860127, 8.311093377946839666 ) ) ;
#41792=CARTESIAN_POINT ( 'NONE',  ( -2.085542519210945728E-15, 174.8437499965860411, 11.35316468750000141 ) ) ;
#41799=CARTESIAN_POINT ( 'NONE',  ( -9.832129032723418760, 67.86458332991935549, -5.676582343750004256 ) ) ;
#41801=DIRECTION ( 'NONE',  ( -0.000000000000000000, 1.000000000000000000, -0.000000000000000000 ) ) ;
#41804=CARTESIAN_POINT ( 'NONE',  ( 3.153939666463669656E-13, 33.75000000000002842, 9.999999999999998224 ) ) ;
#41805=CARTESIAN_POINT ( 'NONE',  ( -5.676582343749998039, 77.44791666325269830, -9.832129032723420536 ) ) ;
#41810=CARTESIAN_POINT ( 'NONE',  ( -8.311093377946841443, 68.90624999658602690, 8.311093377946834337 ) ) ;
#41813=CARTESIAN_POINT ( 'NONE',  ( -10.00000000000000355, 154.5833333265053682, 2.679491924311223183 ) ) ;
#41816=CARTESIAN_POINT ( 'NONE',  ( -3.042071309553173730, 59.63541666325267698, 11.35316468749999785 ) ) ;
#41818=CARTESIAN_POINT ( 'NONE',  ( 11.35316468750000141, 195.7812499965860127, 0.000000000000000000 ) ) ;
#41822=CARTESIAN_POINT ( 'NONE',  ( 7.320508075688771044, 61.24999999317203958, 7.320508075688775484 ) ) ;
#41824=CARTESIAN_POINT ( 'NONE',  ( -3.042071309553163960, 187.2395833299193555, -11.35316468749999963 ) ) ;
#41827=CARTESIAN_POINT ( 'NONE',  ( 6.123233995736767268E-16, 188.1249999931720254, -10.00000000000000178 ) ) ;
#41829=CARTESIAN_POINT ( 'NONE',  ( -2.085542519210945728E-15, 164.8437499965860127, 11.35316468750000141 ) ) ;
#41832=CARTESIAN_POINT ( 'NONE',  ( 10.15167889325737960, 225.9999999999999147, -4.663489317652536492 ) ) ;
#41847=CARTESIAN_POINT ( 'NONE',  ( 10.00000000000005151, 179.7916666666667425, 2.679491924311249829 ) ) ;
#41861=CARTESIAN_POINT ( 'NONE',  ( 4.721056650416000089, 297.9843750017070079, 4.721056650415999201 ) ) ;
#41862=CARTESIAN_POINT ( 'NONE',  ( -8.660254037844387298, 132.0833333333333428, -5.000000000000004441 ) ) ;
#41878=CARTESIAN_POINT ( 'NONE',  ( -3.042071309553173730, 24.32291666325268764, 11.35316468749999785 ) ) ;
#41880=CARTESIAN_POINT ( 'NONE',  ( -11.35316468750000141, 218.8020833299193271, 3.042071309553159963 ) ) ;
#41886=CARTESIAN_POINT ( 'NONE',  ( -2.085542519210945728E-15, 39.53124999658601268, 11.35316468750000141 ) ) ;
#41892=CARTESIAN_POINT ( 'NONE',  ( -8.311093377946836114, 37.65624999658601979, -8.311093377946837890 ) ) ;
#41894=CARTESIAN_POINT ( 'NONE',  ( -8.311093377946841443, 148.9062499965860127, 8.311093377946830785 ) ) ;
#41896=CARTESIAN_POINT ( 'NONE',  ( 2.679491924311228956, 117.9166666598387110, -10.00000000000000000 ) ) ;
#41900=VERTEX_POINT ( 'NONE', #65074 ) ;
#41901=CARTESIAN_POINT ( 'NONE',  ( 5.676582343750001591, 1.927083329919350163, -9.832129032723420536 ) ) ;
#41906=CARTESIAN_POINT ( 'NONE',  ( -5.676582343750006032, 144.1145833299193555, 9.832129032723418760 ) ) ;
#41913=EDGE_CURVE ( 'NONE', #27622, #71712, #64281, .T. ) ;
#41914=CARTESIAN_POINT ( 'NONE',  ( 7.320508075688774596, 119.3750000000000142, 7.320508075688778149 ) ) ;
#41915=CARTESIAN_POINT ( 'NONE',  ( -11.35316468750000141, 93.80208332991934128, 3.042071309553159963 ) ) ;
#41935=CARTESIAN_POINT ( 'NONE',  ( -2.679491924332892516, 23.54166666666491636, 9.999999999987878141 ) ) ;
#41938=CARTESIAN_POINT ( 'NONE',  ( 8.660254037844385522, 121.4583333265053824, 5.000000000000005329 ) ) ;
#41940=ORIENTED_EDGE ( 'NONE', *, *, #23812, .F. ) ;
#41947=CARTESIAN_POINT ( 'NONE',  ( -4.999999999999998224, 91.66666666666667140, -8.660254037844389075 ) ) ;
#41949=CARTESIAN_POINT ( 'NONE',  ( -2.765530957081996810, 294.4218750017069510, -6.676582343750003368 ) ) ;
#41951=CARTESIAN_POINT ( 'NONE',  ( -10.00000000000000000, 174.1666666598386826, -2.679491924311229845 ) ) ;
#41954=CARTESIAN_POINT ( 'NONE',  ( -10.00000000000000355, 52.29166666666665719, -2.679491924311230733 ) ) ;
#41959=CARTESIAN_POINT ( 'NONE',  ( 7.320508075688774596, 210.6249999999999716, -7.320508075688774596 ) ) ;
#41961=CARTESIAN_POINT ( 'NONE',  ( -8.311093377946836114, 177.9687499965860127, -8.311093377946837890 ) ) ;
#41962=CARTESIAN_POINT ( 'NONE',  ( 6.123233995736767268E-16, 193.1249999931720254, -10.00000000000000178 ) ) ;
#41968=CARTESIAN_POINT ( 'NONE',  ( -3.042071309553164404, 52.55208332991934839, -11.35316468749999963 ) ) ;
#41970=CARTESIAN_POINT ( 'NONE',  ( 3.042071309553159519, 220.0520833299193271, 11.35316468750000141 ) ) ;
#41972=CARTESIAN_POINT ( 'NONE',  ( 7.320508075688775484, 10.62500000000000178, -7.320508075688775484 ) ) ;
#41976=EDGE_CURVE ( 'NONE', #26852, #4267, #31502, .T. ) ;
#41977=CARTESIAN_POINT ( 'NONE',  ( 10.00000000000000178, 77.08333332650536818, -2.679491924311226736 ) ) ;
#41985=CARTESIAN_POINT ( 'NONE',  ( 4.721056650416000089, 291.9843750017070079, 4.721056650415999201 ) ) ;
#41987=CARTESIAN_POINT ( 'NONE',  ( 9.832129032723416984, 160.3645833299193839, 5.676582343750006032 ) ) ;
#41988=CARTESIAN_POINT ( 'NONE',  ( 10.00000000000000178, 4.791666666666666963, 2.679491924311235618 ) ) ;
#41998=CARTESIAN_POINT ( 'NONE',  ( -3.042071309553163960, 147.5520833299193271, -11.35316468749999963 ) ) ;
#42002=CARTESIAN_POINT ( 'NONE',  ( 5.676582343749993598, 55.26041666325268409, 9.832129032723422313 ) ) ;
#42003=ORIENTED_EDGE ( 'NONE', *, *, #19546, .F. ) ;
#42009=CARTESIAN_POINT ( 'NONE',  ( -4.242640687119286547, 291.9375000034140157, -4.242640687119286547 ) ) ;
#42025=LINE ( 'NONE', #18658, #24754 ) ;
#42027=ORIENTED_EDGE ( 'NONE', *, *, #61369, .F. ) ;
#42029=VERTEX_POINT ( 'NONE', #2828 ) ;
#42033=CARTESIAN_POINT ( 'NONE',  ( -8.660254037844390851, 52.91666666666666430, 4.999999999999998224 ) ) ;
#42036=CARTESIAN_POINT ( 'NONE',  ( 4.242640687119285658, 295.6249999999999432, -4.242640687119286547 ) ) ;
#42037=CARTESIAN_POINT ( 'NONE',  ( -8.660254037844390851, 34.79166665983870388, 4.999999999999998224 ) ) ;
#42046=CARTESIAN_POINT ( 'NONE',  ( 6.123233995736767268E-16, 181.2500000000000284, -10.00000000000000178 ) ) ;
#42049=CARTESIAN_POINT ( 'NONE',  ( 5.676582343749993598, 140.2604166632526983, 9.832129032723422313 ) ) ;
#42056=CARTESIAN_POINT ( 'NONE',  ( -9.832129032723418760, 8.177083329919350163, -5.676582343750004256 ) ) ;
#42061=CARTESIAN_POINT ( 'NONE',  ( -10.00000000000000000, 29.16666665983869677, -2.679491924311229845 ) ) ;
#42067=CARTESIAN_POINT ( 'NONE',  ( 5.000000000000001776, 7.708333326505366401, -8.660254037844389075 ) ) ;
#42069=CARTESIAN_POINT ( 'NONE',  ( 2.485281374238225816, 292.7500000034140157, -6.000000000000346390 ) ) ;
#42072=CARTESIAN_POINT ( 'NONE',  ( -5.676582343750006032, 114.1145833299193555, 9.832129032723418760 ) ) ;
#42080=CARTESIAN_POINT ( 'NONE',  ( 3.090148520752590944, 225.9998984954551418, -9.510618362637927703 ) ) ;
#42081=CARTESIAN_POINT ( 'NONE',  ( 6.951808397369818766E-16, 117.0312499965860269, -11.35316468750000141 ) ) ;
#42084=CARTESIAN_POINT ( 'NONE',  ( -8.660254037844387298, 203.9583333265053682, -5.000000000000004441 ) ) ;
#42087=CARTESIAN_POINT ( 'NONE',  ( -2.085542519210945728E-15, 99.84374999658601268, 11.35316468750000141 ) ) ;
#42091=CARTESIAN_POINT ( 'NONE',  ( 5.676582343749993598, 10.26041666325268409, 9.832129032723422313 ) ) ;
#42097=ADVANCED_FACE ( 'NONE', ( #54895 ), #71845, .T. ) ;
#42100=CARTESIAN_POINT ( 'NONE',  ( -4.721056650415999201, 292.3281250017069510, -4.721056650415999201 ) ) ;
#42101=CARTESIAN_POINT ( 'NONE',  ( 2.679491924311222739, 125.8333333265053682, 10.00000000000000355 ) ) ;
#42102=CARTESIAN_POINT ( 'NONE',  ( -3.042071309553163960, 222.5520833299193271, -11.35316468749999963 ) ) ;
#42122=CARTESIAN_POINT ( 'NONE',  ( 2.765530957081996366, 293.1406250017069510, -6.676582343750002480 ) ) ;
#42134=CARTESIAN_POINT ( 'NONE',  ( 11.35316468750000141, 96.09374999658601268, 0.000000000000000000 ) ) ;
#42142=CARTESIAN_POINT ( 'NONE',  ( 11.35316468749999963, 210.9895833299193839, -3.042071309553165293 ) ) ;
#42146=CARTESIAN_POINT ( 'NONE',  ( 8.311093377946834337, 200.4687499965860411, 8.311093377946839666 ) ) ;
#42153=CARTESIAN_POINT ( 'NONE',  ( -3.042071309553173730, 79.32291666325271251, 11.35316468749999785 ) ) ;
#42155=DIRECTION ( 'NONE',  ( 0.000000000000000000, 0.000000000000000000, 1.000000000000000000 ) ) ;
#42156=VERTEX_POINT ( 'NONE', #1621 ) ;
#42159=CARTESIAN_POINT ( 'NONE',  ( 11.35316468749999785, 75.57291666325269830, 3.042071309553174174 ) ) ;
#42166=CARTESIAN_POINT ( 'NONE',  ( -11.35316468750000141, 68.48958332991935549, 3.042071309553159963 ) ) ;
#42168=CARTESIAN_POINT ( 'NONE',  ( -1.836970198721029983E-15, 25.62499999317203248, 10.00000000000000178 ) ) ;
#42169=CARTESIAN_POINT ( 'NONE',  ( -7.320508075688778149, 169.9999999931720254, 7.320508075688769267 ) ) ;
#42172=CARTESIAN_POINT ( 'NONE',  ( 3.042071309553159519, 60.05208332991934128, 11.35316468750000141 ) ) ;
#42175=CARTESIAN_POINT ( 'NONE',  ( 11.35316468749999785, 200.5729166632526983, 3.042071309553174174 ) ) ;
#42176=VERTEX_POINT ( 'NONE', #2715 ) ;
#42179=CARTESIAN_POINT ( 'NONE',  ( -1.836970198721029983E-15, 60.62499999317203958, 10.00000000000000178 ) ) ;
#42181=CARTESIAN_POINT ( 'NONE',  ( -9.832129032723420536, 193.6979166632526983, 5.676582343749997150 ) ) ;
#42186=CARTESIAN_POINT ( 'NONE',  ( -5.676582343750006032, 179.4270833299193555, 9.832129032723418760 ) ) ;
#42187=EDGE_CURVE ( 'NONE', #70240, #3720, #2148, .T. ) ;
#42191=ORIENTED_EDGE ( 'NONE', *, *, #23025, .F. ) ;
#42194=CARTESIAN_POINT ( 'NONE',  ( 8.660254037844389075, 0.4166666666666666852, -5.000000000000000000 ) ) ;
#42196=EDGE_CURVE ( 'NONE', #60229, #38928, #13641, .T. ) ;
#42200=CARTESIAN_POINT ( 'NONE',  ( 3.153939666463620179E-13, 188.7500000000000284, 9.999999999999998224 ) ) ;
#42205=DIRECTION ( 'NONE',  ( -0.000000000000000000, 1.000000000000000000, -0.000000000000000000 ) ) ;
#42209=( BOUNDED_CURVE ( )  B_SPLINE_CURVE ( 2, ( #62509, #26687, #15735, #10465, #39137, #33495, #14986, #61777, #10835 ),
 .UNSPECIFIED., .F., .F. ) 
 B_SPLINE_CURVE_WITH_KNOTS ( ( 3, 2, 2, 2, 3 ),
 ( 0.1874999999999978351, 0.1979166666666645202, 0.2083333333333312054, 0.2187499999999978906, 0.2291666666666645480 ),
 .UNSPECIFIED. ) 
 CURVE ( )  GEOMETRIC_REPRESENTATION_ITEM ( )  RATIONAL_B_SPLINE_CURVE ( ( 1.000000000000015765, 0.9238795325112709733, 1.000000000000000000, 0.9238795325112867385, 1.000000000000000000, 0.9238795325112867385, 1.000000000000000000, 0.9238795325113021706, 0.9999999999999845679 ) ) 
 REPRESENTATION_ITEM ( '' )  );
#42218=CARTESIAN_POINT ( 'NONE',  ( -5.000000000000005329, 115.2083333265053682, 8.660254037844387298 ) ) ;
#42222=CARTESIAN_POINT ( 'NONE',  ( -4.721056650415998313, 294.7343750017069510, 4.721056650416000089 ) ) ;
#42223=CARTESIAN_POINT ( 'NONE',  ( -4.999999999999998224, 151.6666666666666856, -8.660254037844389075 ) ) ;
#42240=CARTESIAN_POINT ( 'NONE',  ( 8.311093377946834337, 35.15624999658602690, 8.311093377946839666 ) ) ;
#42242=CARTESIAN_POINT ( 'NONE',  ( 10.00000000000000178, 6.874999993172033363, 0.000000000000000000 ) ) ;
#42249=CARTESIAN_POINT ( 'NONE',  ( 11.35316468750000141, 40.78124999658601268, 0.000000000000000000 ) ) ;
#42256=CARTESIAN_POINT ( 'NONE',  ( 8.311093377946834337, 30.15624999658601624, 8.311093377946839666 ) ) ;
#42259=CARTESIAN_POINT ( 'NONE',  ( -11.35316468749999785, 153.0729166632527267, -3.042071309553167513 ) ) ;
#42260=CARTESIAN_POINT ( 'NONE',  ( -10.00000000000000000, 134.1666666598386826, -2.679491924311229845 ) ) ;
#42266=CARTESIAN_POINT ( 'NONE',  ( 11.35316468750000141, 16.09374999658601979, 0.000000000000000000 ) ) ;
#42272=CARTESIAN_POINT ( 'NONE',  ( -3.042071309553163960, 152.2395833299193271, -11.35316468749999963 ) ) ;
#42273=FACE_OUTER_BOUND ( 'NONE', #73657, .T. ) ;
#42280=DIRECTION ( 'NONE',  ( -0.000000000000000000, 1.000000000000000000, -0.000000000000000000 ) ) ;
#42281=CARTESIAN_POINT ( 'NONE',  ( 3.042071309553159519, 105.0520833299193271, 11.35316468750000141 ) ) ;
#42301=CARTESIAN_POINT ( 'NONE',  ( 2.679491924311222739, 120.8333333265053682, 10.00000000000000355 ) ) ;
#42303=VERTEX_POINT ( 'NONE', #32520 ) ;
#42313=CARTESIAN_POINT ( 'NONE',  ( -7.320508075688773708, 96.87499999999998579, -7.320508075688774596 ) ) ;
#42315=CARTESIAN_POINT ( 'NONE',  ( 6.676582343750004256, 297.0468750017068942, 2.765530957081995478 ) ) ;
#42317=FACE_OUTER_BOUND ( 'NONE', #66950, .T. ) ;
#42320=CARTESIAN_POINT ( 'NONE',  ( -2.679491924312192630, 53.54166666666657903, 9.999999999999451106 ) ) ;
#42325=CARTESIAN_POINT ( 'NONE',  ( 8.660254037844389075, 215.4166666666666856, -5.000000000000000000 ) ) ;
#42326=( BOUNDED_CURVE ( )  B_SPLINE_CURVE ( 2, ( #9226, #32248, #8856, #8473, #38276, #3571, #32628, #54888, #37529, #65811, #26561, #66187, #49586 ),
 .UNSPECIFIED., .F., .F. ) 
 B_SPLINE_CURVE_WITH_KNOTS ( ( 3, 2, 2, 2, 2, 2, 3 ),
 ( 0.1250000000000000000, 0.1268115942028985588, 0.1286231884057970898, 0.1304347826086956486, 0.1322463768115942073, 0.1340579710144927661, 0.1358695652173912971 ),
 .UNSPECIFIED. ) 
 CURVE ( )  GEOMETRIC_REPRESENTATION_ITEM ( )  RATIONAL_B_SPLINE_CURVE ( ( 1.000000000000000000, 0.9659258262890683122, 1.000000000000000000, 0.9659258262890683122, 1.000000000000000000, 0.9659258262890683122, 1.000000000000000000, 0.9659258262890683122, 1.000000000000000000, 0.9659258262890683122, 1.000000000000000000, 0.9659258262890683122, 1.000000000000000000 ) ) 
 REPRESENTATION_ITEM ( '' )  );
#42328=CARTESIAN_POINT ( 'NONE',  ( 5.676582343749993598, 190.2604166632526983, 9.832129032723422313 ) ) ;
#42332=CYLINDRICAL_SURFACE ( 'NONE', #37040, 10.00000000000000178 ) ;
#42335=AXIS2_PLACEMENT_3D ( 'NONE', #2433, #41321, #65429 ) ;
#42337=CARTESIAN_POINT ( 'NONE',  ( -8.311093377946841443, 54.21874999658601979, 8.311093377946830785 ) ) ;
#42339=CARTESIAN_POINT ( 'NONE',  ( 6.951808397369818766E-16, 222.3437499965860127, -11.35316468750000141 ) ) ;
#42346=CARTESIAN_POINT ( 'NONE',  ( 8.311093377946834337, 110.1562499965860269, 8.311093377946839666 ) ) ;
#42347=CARTESIAN_POINT ( 'NONE',  ( -1.836970198721029983E-15, 75.62499999317203958, 10.00000000000000178 ) ) ;
#42355=CARTESIAN_POINT ( 'NONE',  ( 6.676582343750003368, 293.1718750017070647, -2.765530957081997254 ) ) ;
#42357=CARTESIAN_POINT ( 'NONE',  ( -2.085542519210945728E-15, 169.5312499965860411, 11.35316468750000141 ) ) ;
#42367=CARTESIAN_POINT ( 'NONE',  ( 8.311093377946837890, 141.7187499965859843, -8.311093377946837890 ) ) ;
#42371=CARTESIAN_POINT ( 'NONE',  ( 3.042071309553159519, 45.05208332991935549, 11.35316468750000141 ) ) ;
#42377=CARTESIAN_POINT ( 'NONE',  ( 2.485281374238575314, 291.3750000034140157, 6.000000000000000888 ) ) ;
#42383=CARTESIAN_POINT ( 'NONE',  ( -1.836970198721029983E-15, 35.62499999317203248, 10.00000000000000178 ) ) ;
#42394=ORIENTED_EDGE ( 'NONE', *, *, #28240, .T. ) ;
#42399=CARTESIAN_POINT ( 'NONE',  ( -8.660254037844387298, 52.08333333333333570, -5.000000000000004441 ) ) ;
#42401=CARTESIAN_POINT ( 'NONE',  ( -6.000000000000003553, 296.9374999999999432, -2.485281374238571317 ) ) ;
#42404=EDGE_CURVE ( 'NONE', #57815, #38960, #51653, .T. ) ;
#42408=CARTESIAN_POINT ( 'NONE',  ( 11.35316468750000141, 0.7812499965860163487, 0.000000000000000000 ) ) ;
#42410=CYLINDRICAL_SURFACE ( 'NONE', #42335, 10.00000000000000178 ) ;
#42412=CARTESIAN_POINT ( 'NONE',  ( 10.00000000000000178, 170.0000000000000000, 0.000000000000000000 ) ) ;
#42416=CARTESIAN_POINT ( 'NONE',  ( -5.676582343749998039, 147.7604166632526699, -9.832129032723420536 ) ) ;
#42421=CARTESIAN_POINT ( 'NONE',  ( 1.102182119232618108E-15, 294.2500000000000000, 6.000000000000001776 ) ) ;
#42424=CARTESIAN_POINT ( 'NONE',  ( 9.832129032723416984, 5.677083329919350163, 5.676582343750006032 ) ) ;
#42432=CARTESIAN_POINT ( 'NONE',  ( -8.660254037844390851, 39.79166665983870388, 4.999999999999998224 ) ) ;
#42443=CARTESIAN_POINT ( 'NONE',  ( -11.35316468750000141, 128.2812499965860127, -1.390361679473963753E-15 ) ) ;
#42451=CARTESIAN_POINT ( 'NONE',  ( 8.311093377946837890, 116.4062499965860269, -8.311093377946837890 ) ) ;
#42457=CARTESIAN_POINT ( 'NONE',  ( 7.320508075688774596, 212.4999999931719969, -7.320508075688774596 ) ) ;
#42460=CARTESIAN_POINT ( 'NONE',  ( -5.676582343749998039, 97.76041666325269830, -9.832129032723420536 ) ) ;
#42465=CARTESIAN_POINT ( 'NONE',  ( -11.35316468750000141, 13.80208332991934661, 3.042071309553159963 ) ) ;
#42473=CARTESIAN_POINT ( 'NONE',  ( 6.676582343750003368, 291.0156250017069510, -2.765530957081997254 ) ) ;
#42474=CARTESIAN_POINT ( 'NONE',  ( 7.320508075688774596, 127.4999999931720538, -7.320508075688774596 ) ) ;
#42475=CARTESIAN_POINT ( 'NONE',  ( -3.042071309553173730, 219.6354166632526699, 11.35316468749999785 ) ) ;
#42477=CARTESIAN_POINT ( 'NONE',  ( 11.35316468750000141, 131.0937499965860127, 0.000000000000000000 ) ) ;
#42494=EDGE_CURVE ( 'NONE', #9076, #12154, #38551, .T. ) ;
#42496=CARTESIAN_POINT ( 'NONE',  ( -1.377000000000000002, 261.4319999999996753, 5.673918265509175107 ) ) ;
#42497=CARTESIAN_POINT ( 'NONE',  ( 2.765530957082001251, 292.7656250017069510, 6.676582343749999815 ) ) ;
#42509=CARTESIAN_POINT ( 'NONE',  ( -9.832129032723420536, 104.0104166632526841, 5.676582343749997150 ) ) ;
#42519=CARTESIAN_POINT ( 'NONE',  ( 11.35316468750000141, 215.7812499965860411, 0.000000000000000000 ) ) ;
#42525=CARTESIAN_POINT ( 'NONE',  ( 9.832129032723416984, 195.6770833299193839, 5.676582343750006032 ) ) ;
#42531=CARTESIAN_POINT ( 'NONE',  ( -11.35316468750000141, 78.28124999658601268, -1.390361679473963753E-15 ) ) ;
#42537=CARTESIAN_POINT ( 'NONE',  ( -3.042071309553164404, 82.23958332991935549, -11.35316468749999963 ) ) ;
#42544=CARTESIAN_POINT ( 'NONE',  ( -11.35316468749999785, 78.07291666325269830, -3.042071309553167957 ) ) ;
#42548=CARTESIAN_POINT ( 'NONE',  ( -10.00000000000000178, 164.3749999931720254, -1.224646799147353454E-15 ) ) ;
#42550=CARTESIAN_POINT ( 'NONE',  ( 0.000000000000000000, 300.0000000000000000, 0.000000000000000000 ) ) ;
#42551=CARTESIAN_POINT ( 'NONE',  ( -5.676582343749998039, 62.76041666325269119, -9.832129032723420536 ) ) ;
#42552=( BOUNDED_CURVE ( )  B_SPLINE_CURVE ( 2, ( #8580, #48929, #2923, #54616, #60253, #42894, #48556, #8207, #30846, #53867, #7839, #31966, #37635 ),
 .UNSPECIFIED., .F., .F. ) 
 B_SPLINE_CURVE_WITH_KNOTS ( ( 3, 2, 2, 2, 2, 2, 3 ),
 ( 1.742685697302758463, 1.747919628595612451, 1.753153559888466662, 1.758387491181320650, 1.763621422474174860, 1.768855353767028848, 1.774089285059882615 ),
 .UNSPECIFIED. ) 
 CURVE ( )  GEOMETRIC_REPRESENTATION_ITEM ( )  RATIONAL_B_SPLINE_CURVE ( ( 1.000000000000271561, 0.9659258262887968627, 1.000000000000000000, 0.9659258262890683122, 1.000000000000000000, 0.9659258262890683122, 1.000000000000000000, 0.9659258262890683122, 1.000000000000000000, 0.9659258262890683122, 1.000000000000000000, 0.9659258262890662028, 1.000000000000001998 ) ) 
 REPRESENTATION_ITEM ( '' )  );
#42554=CARTESIAN_POINT ( 'NONE',  ( -5.676582343749998039, 192.4479166632526983, -9.832129032723420536 ) ) ;
#42559=CARTESIAN_POINT ( 'NONE',  ( -3.042071309553173730, 189.3229166632526699, 11.35316468749999785 ) ) ;
#42561=CARTESIAN_POINT ( 'NONE',  ( -4.999999999999998224, 193.5416666598387110, -8.660254037844389075 ) ) ;
#42564=ORIENTED_EDGE ( 'NONE', *, *, #9043, .F. ) ;
#42565=CARTESIAN_POINT ( 'NONE',  ( 8.311093377946834337, 180.4687499965859843, 8.311093377946839666 ) ) ;
#42571=CARTESIAN_POINT ( 'NONE',  ( -10.00000000000000178, 2.500000000000000000, -1.224646799147353454E-15 ) ) ;
#42594=CARTESIAN_POINT ( 'NONE',  ( 6.676582343750001591, 295.1093750017069510, -8.176455196517173205E-16 ) ) ;
#42595=CARTESIAN_POINT ( 'NONE',  ( 8.660254037844385522, 154.5833333333333428, 5.000000000000005329 ) ) ;
#42613=CARTESIAN_POINT ( 'NONE',  ( -5.676582343749998039, 37.44791666325268409, -9.832129032723420536 ) ) ;
#42615=CARTESIAN_POINT ( 'NONE',  ( 8.660254037844389075, 12.29166665983870033, -5.000000000000000000 ) ) ;
#42616=CARTESIAN_POINT ( 'NONE',  ( 1.102182119232618108E-15, 295.2500000000000000, 6.000000000000001776 ) ) ;
#42617=ORIENTED_EDGE ( 'NONE', *, *, #58204, .F. ) ;
#42620=CARTESIAN_POINT ( 'NONE',  ( -11.35316468749999785, 33.07291666325268409, -3.042071309553167513 ) ) ;
#42623=CARTESIAN_POINT ( 'NONE',  ( 1.102182119232618108E-15, 299.2500000000000000, 6.000000000000001776 ) ) ;
#42626=CARTESIAN_POINT ( 'NONE',  ( -9.832129032723418760, 37.86458332991934839, -5.676582343750004256 ) ) ;
#42627=EDGE_CURVE ( 'NONE', #30484, #19919, #5700, .T. ) ;
#42629=CARTESIAN_POINT ( 'NONE',  ( 9.832129032723420536, 151.1979166632526983, -5.676582343749999815 ) ) ;
#42632=CARTESIAN_POINT ( 'NONE',  ( 10.00000000000000000, 126.6666666598386826, 2.679491924311236062 ) ) ;
#42637=CARTESIAN_POINT ( 'NONE',  ( -11.35316468749999785, 18.38541666325268054, -3.042071309553167957 ) ) ;
#42642=CARTESIAN_POINT ( 'NONE',  ( 3.042071309553159519, 154.7395833299193555, 11.35316468750000141 ) ) ;
#42645=CARTESIAN_POINT ( 'NONE',  ( -1.836970198721029983E-15, 225.6249999931720254, 10.00000000000000178 ) ) ;
#42649=EDGE_CURVE ( 'NONE', #67735, #67846, #71822, .T. ) ;
#42650=DIRECTION ( 'NONE',  ( -0.000000000000000000, 1.000000000000000000, -0.000000000000000000 ) ) ;
#42651=DIRECTION ( 'NONE',  ( 0.000000000000000000, 0.000000000000000000, 1.000000000000000000 ) ) ;
#42652=CARTESIAN_POINT ( 'NONE',  ( -11.35316468749999785, 108.3854166632526841, -3.042071309553167513 ) ) ;
#42661=( BOUNDED_CURVE ( )  B_SPLINE_CURVE ( 2, ( #50172, #61867, #27155, #67161, #39233, #62233, #72440, #72818, #38863, #21498, #15828, #43383, #15456 ),
 .UNSPECIFIED., .F., .F. ) 
 B_SPLINE_CURVE_WITH_KNOTS ( ( 3, 2, 2, 2, 2, 2, 3 ),
 ( 0.07849216663199026778, 0.08372612650475230733, 0.08896008637751434689, 0.09419404625027635869, 0.09942800612303839825, 0.1046619659958004378, 0.1098959258685624774 ),
 .UNSPECIFIED. ) 
 CURVE ( )  GEOMETRIC_REPRESENTATION_ITEM ( )  RATIONAL_B_SPLINE_CURVE ( ( 1.000000000000247802, 0.9659258262888206215, 1.000000000000000000, 0.9659258262890683122, 1.000000000000000000, 0.9659258262890683122, 1.000000000000000000, 0.9659258262890683122, 1.000000000000000000, 0.9659258262890683122, 1.000000000000000000, 0.9659258262890684232, 0.9999999999999998890 ) ) 
 REPRESENTATION_ITEM ( '' )  );
#42671=CARTESIAN_POINT ( 'NONE',  ( -10.00000000000000000, 224.1666666598387110, -2.679491924311229845 ) ) ;
#42678=CARTESIAN_POINT ( 'NONE',  ( 7.320508075688773708, 124.3750000000000000, 7.320508075688777261 ) ) ;
#42683=CARTESIAN_POINT ( 'NONE',  ( -7.320508075688773708, 111.8750000000000000, -7.320508075688774596 ) ) ;
#42685=CARTESIAN_POINT ( 'NONE',  ( 6.676582343750001591, 296.1093750017069510, -8.176455196517173205E-16 ) ) ;
#42687=CARTESIAN_POINT ( 'NONE',  ( 2.679491924311379947, 188.9583333333333712, 9.999999999999959144 ) ) ;
#42695=CARTESIAN_POINT ( 'NONE',  ( -7.320508075688778149, 223.1250000000000284, 7.320508075688769267 ) ) ;
#42697=CARTESIAN_POINT ( 'NONE',  ( -8.311093377946836114, 197.9687499965860411, -8.311093377946837890 ) ) ;
#42698=CARTESIAN_POINT ( 'NONE',  ( 8.660254037844385522, 191.4583333265053966, 5.000000000000005329 ) ) ;
#42702=CARTESIAN_POINT ( 'NONE',  ( -3.673940397442060854E-16, 297.7500000000000000, -6.000000000000001776 ) ) ;
#42706=CARTESIAN_POINT ( 'NONE',  ( 8.311093377946834337, 45.46874999658601268, 8.311093377946839666 ) ) ;
#42715=CARTESIAN_POINT ( 'NONE',  ( -8.311093377946836114, 112.6562499965860127, -8.311093377946837890 ) ) ;
#42717=CARTESIAN_POINT ( 'NONE',  ( 2.679491924311222739, 90.83333332650536818, 10.00000000000000355 ) ) ;
#42723=CARTESIAN_POINT ( 'NONE',  ( -3.220560865819809937, 225.9999999999999432, -9.489879397300258645 ) ) ;
#42725=CARTESIAN_POINT ( 'NONE',  ( 4.721056650415999201, 293.2343750017069510, -4.721056650415999201 ) ) ;
#42728=CARTESIAN_POINT ( 'NONE',  ( -5.676582343749998039, 172.4479166632526983, -9.832129032723420536 ) ) ;
#42729=CARTESIAN_POINT ( 'NONE',  ( 8.660254037844385522, 4.583333333333333925, 5.000000000000006217 ) ) ;
#42731=CARTESIAN_POINT ( 'NONE',  ( -7.320508075688810123, 193.1250000000000568, 7.320508075688802130 ) ) ;
#42733=ORIENTED_EDGE ( 'NONE', *, *, #16874, .F. ) ;
#42736=CARTESIAN_POINT ( 'NONE',  ( -3.042071309553173730, 144.6354166632526983, 11.35316468749999785 ) ) ;
#42739=CARTESIAN_POINT ( 'NONE',  ( 11.35316468749999963, 66.30208332991935549, -3.042071309553165293 ) ) ;
#42746=CARTESIAN_POINT ( 'NONE',  ( -2.485281374238572649, 287.2500000034139589, 6.000000000000002665 ) ) ;
#42766=ORIENTED_EDGE ( 'NONE', *, *, #9662, .F. ) ;
#42768=CARTESIAN_POINT ( 'NONE',  ( 6.000000000000003553, 296.4374999999999432, 2.485281374238571317 ) ) ;
#42770=CARTESIAN_POINT ( 'NONE',  ( 5.000000000000001776, 65.83333333333334281, -8.660254037844389075 ) ) ;
#42772=CARTESIAN_POINT ( 'NONE',  ( 2.485281374238575314, 295.3125000000000000, 6.000000000000000888 ) ) ;
#42782=CARTESIAN_POINT ( 'NONE',  ( 3.153939666463620179E-13, 188.7500000000000284, 9.999999999999998224 ) ) ;
#42783=CARTESIAN_POINT ( 'NONE',  ( -2.679491924311235618, 173.5416666666666288, 10.00000000000000000 ) ) ;
#42786=CARTESIAN_POINT ( 'NONE',  ( 5.676582343750001591, 156.9270833299193555, -9.832129032723420536 ) ) ;
#42787=CARTESIAN_POINT ( 'NONE',  ( 6.000000000000003553, 294.6250000034140157, -2.485281374238571761 ) ) ;
#42790=CARTESIAN_POINT ( 'NONE',  ( 0.000000000000000000, 237.9999999999999716, 10.00000000000000178 ) ) ;
#42791=CARTESIAN_POINT ( 'NONE',  ( -7.320508075688779925, 168.1250000000000284, 7.320508075688771044 ) ) ;
#42793=CARTESIAN_POINT ( 'NONE',  ( 9.832129032723416984, 15.67708332991935016, 5.676582343750006032 ) ) ;
#42799=CARTESIAN_POINT ( 'NONE',  ( -8.660254037844390851, 54.79166665983869677, 4.999999999999998224 ) ) ;
#42809=CARTESIAN_POINT ( 'NONE',  ( 9.832129032723420536, 131.1979166632526983, -5.676582343749999815 ) ) ;
#42813=DIRECTION ( 'NONE',  ( 0.000000000000000000, 0.000000000000000000, 1.000000000000000000 ) ) ;
#42816=CARTESIAN_POINT ( 'NONE',  ( -1.836970198721029983E-15, 43.75000000000000711, 10.00000000000000178 ) ) ;
#42817=CARTESIAN_POINT ( 'NONE',  ( -11.35316468750000141, 113.4895833299193413, 3.042071309553159963 ) ) ;
#42819=CARTESIAN_POINT ( 'NONE',  ( 10.00000000000000533, 49.79166666666667140, 2.679491924311236506 ) ) ;
#42821=CARTESIAN_POINT ( 'NONE',  ( -7.320508075688773708, 23.74999999317202892, -7.320508075688774596 ) ) ;
#42823=CARTESIAN_POINT ( 'NONE',  ( -5.676582343749998039, 102.7604166632526841, -9.832129032723420536 ) ) ;
#42827=CARTESIAN_POINT ( 'NONE',  ( -11.35316468749999785, 18.38541666325267698, -3.042071309553167513 ) ) ;
#42829=CARTESIAN_POINT ( 'NONE',  ( 10.00000000000000178, 181.8749999931720538, 0.000000000000000000 ) ) ;
#42834=CARTESIAN_POINT ( 'NONE',  ( 4.721056650415999201, 293.0781250017069510, -4.721056650415999201 ) ) ;
#42835=AXIS2_PLACEMENT_3D ( 'NONE', #54924, #66597, #47753 ) ;
#42837=CARTESIAN_POINT ( 'NONE',  ( -9.832129032723420536, 219.0104166632526983, 5.676582343749997150 ) ) ;
#42839=CARTESIAN_POINT ( 'NONE',  ( -11.35316468749999785, 123.3854166632526699, -3.042071309553167513 ) ) ;
#42851=CARTESIAN_POINT ( 'NONE',  ( -8.660254037844472563, 172.9166666666667425, 5.000000000000047073 ) ) ;
#42853=ORIENTED_EDGE ( 'NONE', *, *, #38700, .F. ) ;
#42856=CARTESIAN_POINT ( 'NONE',  ( 0.000000000000000000, 300.0000000000000000, 0.000000000000000000 ) ) ;
#42859=CARTESIAN_POINT ( 'NONE',  ( -2.765530957081998142, 291.6406250017068942, 6.676582343750000703 ) ) ;
#42861=CARTESIAN_POINT ( 'NONE',  ( 7.320508075688774596, 137.4999999931720254, -7.320508075688774596 ) ) ;
#42870=DIRECTION ( 'NONE',  ( -0.000000000000000000, -1.000000000000000000, -0.000000000000000000 ) ) ;
#42872=CARTESIAN_POINT ( 'NONE',  ( -3.042071309553173730, 109.6354166632526557, 11.35316468749999785 ) ) ;
#42873=CARTESIAN_POINT ( 'NONE',  ( 2.679491924311075302, 210.8333333265053682, 10.00000000000008704 ) ) ;
#42880=CARTESIAN_POINT ( 'NONE',  ( 11.35316468750000141, 220.7812499965860127, 0.000000000000000000 ) ) ;
#42885=CARTESIAN_POINT ( 'NONE',  ( 5.676582343749993598, 200.2604166632526983, 9.832129032723422313 ) ) ;
#42887=CARTESIAN_POINT ( 'NONE',  ( 4.529167459315944555, 225.9997407208379911, 8.915528146188176351 ) ) ;
#42892=CARTESIAN_POINT ( 'NONE',  ( 9.832129032723416984, 80.36458332991935549, 5.676582343750006032 ) ) ;
#42893=ORIENTED_EDGE ( 'NONE', *, *, #41587, .F. ) ;
#42894=CARTESIAN_POINT ( 'NONE',  ( 10.00000000000001066, 139.7916666666666856, 2.679491924311238282 ) ) ;
#42898=CARTESIAN_POINT ( 'NONE',  ( 8.311093377946837890, 91.40624999658604111, -8.311093377946837890 ) ) ;
#42903=CARTESIAN_POINT ( 'NONE',  ( 2.679491924311304452, 73.95833333333334281, 9.999999999999992895 ) ) ;
#42905=CARTESIAN_POINT ( 'NONE',  ( 5.676582343749993598, 69.94791666325268409, 9.832129032723422313 ) ) ;
#42907=CARTESIAN_POINT ( 'NONE',  ( 8.660254037844389075, 130.4166666666666856, -5.000000000000000000 ) ) ;
#42910=CARTESIAN_POINT ( 'NONE',  ( -8.660254037844390851, 164.7916666598387110, 4.999999999999998224 ) ) ;
#42914=CARTESIAN_POINT ( 'NONE',  ( -8.311093377946836114, 67.96874999658601268, -8.311093377946837890 ) ) ;
#42915=CARTESIAN_POINT ( 'NONE',  ( 1.226468279477575784E-15, 293.7031250017069510, 6.676582343750001591 ) ) ;
#42917=CARTESIAN_POINT ( 'NONE',  ( -8.311093377946841443, 193.9062499965860411, 8.311093377946830785 ) ) ;
#42923=CARTESIAN_POINT ( 'NONE',  ( 5.676582343750001591, 196.6145833299193839, -9.832129032723420536 ) ) ;
#42928=CARTESIAN_POINT ( 'NONE',  ( 8.311093377946837890, 186.7187499965860127, -8.311093377946837890 ) ) ;
#42930=CARTESIAN_POINT ( 'NONE',  ( -1.237384350715592869E-11, 93.74999999999903366, 9.999999999999998224 ) ) ;
#42936=CARTESIAN_POINT ( 'NONE',  ( 10.00000000000000178, 5.000000000000000000, 0.000000000000000000 ) ) ;
#42945=CARTESIAN_POINT ( 'NONE',  ( -5.000000000000055955, 81.66666666666672825, -8.660254037844488550 ) ) ;
#42956=CARTESIAN_POINT ( 'NONE',  ( 8.311093377946834337, 55.46874999658601268, 8.311093377946839666 ) ) ;
#42961=CARTESIAN_POINT ( 'NONE',  ( -6.676582343749999815, 293.6718750017070079, 2.765530957082001251 ) ) ;
#42962=CARTESIAN_POINT ( 'NONE',  ( 6.123233995736767268E-16, 146.2500000000000284, -10.00000000000000178 ) ) ;
#42972=CARTESIAN_POINT ( 'NONE',  ( -2.679491924311226292, 131.4583333333333428, -10.00000000000000178 ) ) ;
#42974=CARTESIAN_POINT ( 'NONE',  ( 2.485281374238858643, 288.3750000034139589, 5.999999999999716671 ) ) ;
#42977=CARTESIAN_POINT ( 'NONE',  ( 5.676582343749993598, 39.94791666325269119, 9.832129032723422313 ) ) ;
#42981=CARTESIAN_POINT ( 'NONE',  ( -8.660254037844390851, 14.79166665983870210, 4.999999999999998224 ) ) ;
#42982=ORIENTED_EDGE ( 'NONE', *, *, #33182, .F. ) ;
#42983=CYLINDRICAL_SURFACE ( 'NONE', #27768, 10.00000000000000178 ) ;
#42984=CARTESIAN_POINT ( 'NONE',  ( 0.000000000000000000, 225.9999999999999432, 15.99999999999998579 ) ) ;
#42985=CARTESIAN_POINT ( 'NONE',  ( 9.832129032723420536, 46.19791666325268409, -5.676582343749999815 ) ) ;
#42992=CARTESIAN_POINT ( 'NONE',  ( -2.085542519210945728E-15, 34.53124999658601268, 11.35316468750000141 ) ) ;
#42994=CARTESIAN_POINT ( 'NONE',  ( -5.676582343750006032, 159.1145833299193839, 9.832129032723418760 ) ) ;
#42995=CARTESIAN_POINT ( 'NONE',  ( 8.660254037844389075, 132.2916666598387110, -5.000000000000000000 ) ) ;
#42998=CARTESIAN_POINT ( 'NONE',  ( -2.485281374238855090, 288.8125000000000000, -5.999999999999718447 ) ) ;
#42999=CARTESIAN_POINT ( 'NONE',  ( 9.832129032723416984, 15.67708332991935016, 5.676582343750006032 ) ) ;
#43000=CARTESIAN_POINT ( 'NONE',  ( -7.320508075688784366, 18.12500000000000711, 7.320508075688776373 ) ) ;
#43002=CARTESIAN_POINT ( 'NONE',  ( 0.000000000000000000, 300.0000000000000000, 0.000000000000000000 ) ) ;
#43006=CARTESIAN_POINT ( 'NONE',  ( -11.35316468750000141, 148.4895833299193555, 3.042071309553159963 ) ) ;
#43016=CARTESIAN_POINT ( 'NONE',  ( 6.951808397369818766E-16, 107.3437499965860269, -11.35316468750000141 ) ) ;
#43019=ORIENTED_EDGE ( 'NONE', *, *, #65680, .T. ) ;
#43033=DIRECTION ( 'NONE',  ( -0.000000000000000000, 1.000000000000000000, -0.000000000000000000 ) ) ;
#43040=CARTESIAN_POINT ( 'NONE',  ( 1.226468279477575784E-15, 298.7031250017070079, 6.676582343750001591 ) ) ;
#43043=ORIENTED_EDGE ( 'NONE', *, *, #22371, .T. ) ;
#43045=CARTESIAN_POINT ( 'NONE',  ( 2.679491924311223183, 123.9583333333333286, 10.00000000000000533 ) ) ;
#43049=CARTESIAN_POINT ( 'NONE',  ( -9.999999999999996447, 32.29166666666667140, -2.679491924311229401 ) ) ;
#43050=CARTESIAN_POINT ( 'NONE',  ( -8.660254037844387298, 112.0833333333333428, -5.000000000000004441 ) ) ;
#43051=EDGE_CURVE ( 'NONE', #26730, #26852, #20400, .T. ) ;
#43054=CARTESIAN_POINT ( 'NONE',  ( 6.676582343750001591, 294.1093750017069510, -8.176455196517173205E-16 ) ) ;
#43058=EDGE_CURVE ( 'NONE', #11129, #57815, #31291, .T. ) ;
#43061=CARTESIAN_POINT ( 'NONE',  ( -8.660254037844390851, 184.7916666598387110, 4.999999999999998224 ) ) ;
#43066=CARTESIAN_POINT ( 'NONE',  ( -11.35316468750000141, 3.489583329919349719, 3.042071309553159963 ) ) ;
#43068=CARTESIAN_POINT ( 'NONE',  ( -8.311093377946841443, 194.2187499965859843, 8.311093377946830785 ) ) ;
#43069=CARTESIAN_POINT ( 'NONE',  ( 4.999999999999993783, 191.0416666598387110, 8.660254037844390851 ) ) ;
#43077=CARTESIAN_POINT ( 'NONE',  ( -11.35316468750000141, 43.80208332991934839, 3.042071309553159963 ) ) ;
#43083=CARTESIAN_POINT ( 'NONE',  ( 6.123233995736767268E-16, 203.1249999931720538, -10.00000000000000178 ) ) ;
#43085=CARTESIAN_POINT ( 'NONE',  ( -8.311093377946836114, 122.6562499965860269, -8.311093377946837890 ) ) ;
#43086=CARTESIAN_POINT ( 'NONE',  ( -8.660254037844390851, 84.79166665983869677, 4.999999999999998224 ) ) ;
#43090=DIRECTION ( 'NONE',  ( -0.000000000000000000, 1.000000000000000000, -0.000000000000000000 ) ) ;
#43094=CARTESIAN_POINT ( 'NONE',  ( 6.676582343750003368, 292.1718750017070079, -2.765530957081997254 ) ) ;
#43097=CARTESIAN_POINT ( 'NONE',  ( -9.832129032723420536, 168.6979166632526983, 5.676582343749997150 ) ) ;
#43105=CARTESIAN_POINT ( 'NONE',  ( -5.676582343749998039, 157.7604166632526983, -9.832129032723420536 ) ) ;
#43109=CARTESIAN_POINT ( 'NONE',  ( -5.676582343749998039, 67.76041666325268409, -9.832129032723420536 ) ) ;
#43116=CARTESIAN_POINT ( 'NONE',  ( -3.673940397442060854E-16, 288.8125000034140157, -6.000000000000001776 ) ) ;
#43124=SHAPE_REPRESENTATION ( 'spindle', ( #57354 ), #69405 ) ;
#43137=EDGE_CURVE ( 'NONE', #18660, #26901, #64717, .T. ) ;
#43144=CARTESIAN_POINT ( 'NONE',  ( -2.679491924311235618, 68.54166666666667140, 10.00000000000000000 ) ) ;
#43146=CARTESIAN_POINT ( 'NONE',  ( -3.673940397442060854E-16, 294.7500000000000000, -6.000000000000001776 ) ) ;
#43148=CARTESIAN_POINT ( 'NONE',  ( 6.123233995736767268E-16, 126.2500000000000000, -10.00000000000000178 ) ) ;
#43149=ORIENTED_EDGE ( 'NONE', *, *, #66554, .F. ) ;
#43157=EDGE_CURVE ( 'NONE', #1871, #73371, #5460, .T. ) ;
#43159=CARTESIAN_POINT ( 'NONE',  ( 8.660254037844389075, 185.4166666666666856, -5.000000000000000000 ) ) ;
#43161=CARTESIAN_POINT ( 'NONE',  ( -3.042071309553173730, 159.6354166632526983, 11.35316468749999785 ) ) ;
#43165=LINE ( 'NONE', #3565, #34609 ) ;
#43166=ORIENTED_EDGE ( 'NONE', *, *, #58204, .T. ) ;
#43168=CARTESIAN_POINT ( 'NONE',  ( 9.832129032723416984, 10.67708332991935016, 5.676582343750006032 ) ) ;
#43174=CARTESIAN_POINT ( 'NONE',  ( -10.00000000000000000, 44.16666665983871098, -2.679491924311229845 ) ) ;
#43180=CARTESIAN_POINT ( 'NONE',  ( 3.153939666463620179E-13, 158.7500000000000284, 9.999999999999998224 ) ) ;
#43186=CARTESIAN_POINT ( 'NONE',  ( -3.042071309553173730, 124.3229166632526983, 11.35316468749999785 ) ) ;
#43193=CARTESIAN_POINT ( 'NONE',  ( 11.35316468750000141, 120.7812499965860269, 0.000000000000000000 ) ) ;
#43197=ORIENTED_EDGE ( 'NONE', *, *, #73539, .F. ) ;
#43199=CARTESIAN_POINT ( 'NONE',  ( -8.311093377946841443, 104.2187499965860127, 8.311093377946834337 ) ) ;
#43204=EDGE_CURVE ( 'NONE', #38870, #37587, #56562, .T. ) ;
#43205=CARTESIAN_POINT ( 'NONE',  ( -5.676582343750006032, 29.42708332991935194, 9.832129032723418760 ) ) ;
#43209=CARTESIAN_POINT ( 'NONE',  ( 8.660254037844385522, 116.4583333265053824, 5.000000000000005329 ) ) ;
#43212=CARTESIAN_POINT ( 'NONE',  ( 2.765530957082001251, 288.7656250017068942, 6.676582343750000703 ) ) ;
#43213=CARTESIAN_POINT ( 'NONE',  ( 4.999999999999993783, 126.0416666598387110, 8.660254037844390851 ) ) ;
#43214=CARTESIAN_POINT ( 'NONE',  ( 9.832129032723416984, 225.6770833299193839, 5.676582343750006032 ) ) ;
#43216=CARTESIAN_POINT ( 'NONE',  ( -8.311093377946841443, 139.2187499965860127, 8.311093377946830785 ) ) ;
#43224=ORIENTED_EDGE ( 'NONE', *, *, #9942, .T. ) ;
#43228=CIRCLE ( 'NONE', #11901, 6.000000000000001776 ) ;
#43234=FACE_OUTER_BOUND ( 'NONE', #31123, .T. ) ;
#43235=CARTESIAN_POINT ( 'NONE',  ( 9.832129032723420536, 191.1979166632526983, -5.676582343749999815 ) ) ;
#43238=CARTESIAN_POINT ( 'NONE',  ( -6.676582343750001591, 293.4531250017069510, 0.000000000000000000 ) ) ;
#43240=CARTESIAN_POINT ( 'NONE',  ( -1.237384350715592869E-11, 93.74999999999903366, 9.999999999999998224 ) ) ;
#43251=CARTESIAN_POINT ( 'NONE',  ( 9.832129032723416984, 110.6770833299193555, 5.676582343750006032 ) ) ;
#43252=DIRECTION ( 'NONE',  ( 0.000000000000000000, 0.000000000000000000, 1.000000000000000000 ) ) ;
#43258=CARTESIAN_POINT ( 'NONE',  ( 6.000000000000003553, 287.6250000034140157, -2.485281374238571761 ) ) ;
#43264=CARTESIAN_POINT ( 'NONE',  ( -3.042071309553164404, 187.5520833299193555, -11.35316468749999963 ) ) ;
#43271=CARTESIAN_POINT ( 'NONE',  ( 11.35316468749999963, 75.98958332991935549, -3.042071309553165293 ) ) ;
#43278=CARTESIAN_POINT ( 'NONE',  ( 9.832129032723416984, 90.36458332991935549, 5.676582343750006032 ) ) ;
#43283=CARTESIAN_POINT ( 'NONE',  ( 0.000000000000000000, 300.0000000000000000, 10.00000000000000178 ) ) ;
#43287=CARTESIAN_POINT ( 'NONE',  ( -9.832129032723420536, 78.69791666325269830, 5.676582343749997150 ) ) ;
#43290=CARTESIAN_POINT ( 'NONE',  ( 8.660254037844385522, 129.5833333333333144, 5.000000000000005329 ) ) ;
#43291=CARTESIAN_POINT ( 'NONE',  ( -1.836970198721029983E-15, 165.6249999931720254, 10.00000000000000178 ) ) ;
#43294=CARTESIAN_POINT ( 'NONE',  ( 11.35316468749999963, 56.30208332991934839, -3.042071309553165293 ) ) ;
#43295=CARTESIAN_POINT ( 'NONE',  ( 6.676582343750003368, 294.0156250017070079, -2.765530957081997254 ) ) ;
#43298=CARTESIAN_POINT ( 'NONE',  ( 11.35316468749999785, 210.5729166632526983, 3.042071309553174174 ) ) ;
#43301=CARTESIAN_POINT ( 'NONE',  ( 1.224646799147353454E-15, 300.0000000000000000, -10.00000000000000178 ) ) ;
#43303=CARTESIAN_POINT ( 'NONE',  ( 3.042071309553159519, 194.7395833299193555, 11.35316468750000141 ) ) ;
#43306=CARTESIAN_POINT ( 'NONE',  ( 4.721056650416000089, 298.8281250017069510, 4.721056650415999201 ) ) ;
#43308=CARTESIAN_POINT ( 'NONE',  ( 3.042071309553167513, 177.1354166632526983, -11.35316468749999785 ) ) ;
#43314=CARTESIAN_POINT ( 'NONE',  ( -2.679491924311225848, 1.458333333333333259, -10.00000000000000178 ) ) ;
#43318=EDGE_CURVE ( 'NONE', #58068, #30219, #61415, .T. ) ;
#43332=CARTESIAN_POINT ( 'NONE',  ( 3.042071309553159519, 75.05208332991935549, 11.35316468750000141 ) ) ;
#43336=CARTESIAN_POINT ( 'NONE',  ( -6.676582343750002480, 295.5468750017069510, -2.765530957081996810 ) ) ;
#43337=CARTESIAN_POINT ( 'NONE',  ( 8.660254037844385522, 149.5833333333333428, 5.000000000000005329 ) ) ;
#43349=CARTESIAN_POINT ( 'NONE',  ( 6.000000000000001776, 289.5625000034140157, -7.347880794884121708E-16 ) ) ;
#43355=CARTESIAN_POINT ( 'NONE',  ( 9.832129032723420536, 46.19791666325268409, -5.676582343749999815 ) ) ;
#43357=CARTESIAN_POINT ( 'NONE',  ( 10.00000000000000000, 6.666666659838698550, 2.679491924311236062 ) ) ;
#43362=CARTESIAN_POINT ( 'NONE',  ( -9.832129032723420536, 53.69791666325267698, 5.676582343749997150 ) ) ;
#43368=CARTESIAN_POINT ( 'NONE',  ( 11.35316468749999963, 30.98958332991934839, -3.042071309553165293 ) ) ;
#43372=CARTESIAN_POINT ( 'NONE',  ( 6.951808397369818766E-16, 157.0312499965860127, -11.35316468750000141 ) ) ;
#43373=CARTESIAN_POINT ( 'NONE',  ( -5.000000000000005329, 135.2083333265053682, 8.660254037844387298 ) ) ;
#43376=CARTESIAN_POINT ( 'NONE',  ( 10.00000000000000178, 21.87499999317203248, 0.000000000000000000 ) ) ;
#43377=CARTESIAN_POINT ( 'NONE',  ( 8.311093377946834337, 25.46874999658601624, 8.311093377946839666 ) ) ;
#43383=CARTESIAN_POINT ( 'NONE',  ( -2.679491924311246276, 8.541666666666673180, 10.00000000000000355 ) ) ;
#43384=CARTESIAN_POINT ( 'NONE',  ( -3.042071309553163960, 147.2395833299193555, -11.35316468749999963 ) ) ;
#43390=EDGE_CURVE ( 'NONE', #22486, #70240, #57703, .T. ) ;
#43395=CARTESIAN_POINT ( 'NONE',  ( 11.35316468750000141, 106.0937499965860269, 0.000000000000000000 ) ) ;
#43399=ORIENTED_EDGE ( 'NONE', *, *, #48230, .F. ) ;
#43428=CARTESIAN_POINT ( 'NONE',  ( 7.320508075688774596, 110.6249999999999858, -7.320508075688774596 ) ) ;
#43431=CARTESIAN_POINT ( 'NONE',  ( -6.676582343750001591, 292.6093750017069510, 0.000000000000000000 ) ) ;
#43442=CARTESIAN_POINT ( 'NONE',  ( -3.042071309553164404, 2.239583329919349719, -11.35316468749999963 ) ) ;
#43444=CARTESIAN_POINT ( 'NONE',  ( 3.042071309553159519, 195.0520833299193271, 11.35316468750000141 ) ) ;
#43452=EDGE_CURVE ( 'NONE', #3208, #26622, #43228, .T. ) ;
#43453=CARTESIAN_POINT ( 'NONE',  ( -8.311093377946836114, 12.65624999658601801, -8.311093377946837890 ) ) ;
#43461=CARTESIAN_POINT ( 'NONE',  ( 5.676582343749993598, 119.9479166632526841, 9.832129032723422313 ) ) ;
#43462=EDGE_CURVE ( 'NONE', #47712, #30170, #36511, .T. ) ;
#43463=CARTESIAN_POINT ( 'NONE',  ( 7.320508075688774596, 92.49999999317205379, -7.320508075688774596 ) ) ;
#43467=CARTESIAN_POINT ( 'NONE',  ( -10.00000000000000178, 39.37499999317203958, -1.224646799147353454E-15 ) ) ;
#43470=CARTESIAN_POINT ( 'NONE',  ( -6.676582343750000703, 295.6718750017070079, 2.765530957082001251 ) ) ;
#43471=CARTESIAN_POINT ( 'NONE',  ( 4.999999999999993783, 186.0416666598387110, 8.660254037844390851 ) ) ;
#43473=CARTESIAN_POINT ( 'NONE',  ( 11.35316468749999785, 175.5729166632526415, 3.042071309553174174 ) ) ;
#43481=CARTESIAN_POINT ( 'NONE',  ( 9.832129032723420536, 161.5104166632526983, -5.676582343749999815 ) ) ;
#43485=CARTESIAN_POINT ( 'NONE',  ( 9.832129032723416984, 60.67708332991934839, 5.676582343750006032 ) ) ;
#43489=EDGE_LOOP ( 'NONE', ( #47553, #70030, #47423, #23286 ) ) ;
#43491=CARTESIAN_POINT ( 'NONE',  ( 2.485281374238571317, 288.7500000034139589, -6.000000000000003553 ) ) ;
#43493=CARTESIAN_POINT ( 'NONE',  ( 10.00000000000000178, 67.08333332650538239, -2.679491924311226736 ) ) ;
#43501=ORIENTED_EDGE ( 'NONE', *, *, #41913, .T. ) ;
#43509=CARTESIAN_POINT ( 'NONE',  ( 6.000000000000003553, 299.5625000000000000, -2.485281374238571761 ) ) ;
#43512=CARTESIAN_POINT ( 'NONE',  ( -1.836970198721029983E-15, 8.750000000000000000, 10.00000000000000178 ) ) ;
#43514=CARTESIAN_POINT ( 'NONE',  ( 6.123233995736767268E-16, 71.25000000000001421, -10.00000000000000178 ) ) ;
#43516=CARTESIAN_POINT ( 'NONE',  ( -4.242640687119285658, 291.1249999999999432, 4.242640687119287435 ) ) ;
#43518=DIRECTION ( 'NONE',  ( 0.000000000000000000, -1.000000000000000000, -0.000000000000000000 ) ) ;
#43519=( BOUNDED_CURVE ( )  B_SPLINE_CURVE ( 2, ( #32971, #14455, #9574, #55227, #32592, #15208, #66517, #9938, #55599 ),
 .UNSPECIFIED., .F., .F. ) 
 B_SPLINE_CURVE_WITH_KNOTS ( ( 3, 2, 2, 2, 3 ),
 ( 0.8124999999999983347, 0.8229166666666649643, 0.8333333333333317050, 0.8437499999999983347, 0.8541666666666649643 ),
 .UNSPECIFIED. ) 
 CURVE ( )  GEOMETRIC_REPRESENTATION_ITEM ( )  RATIONAL_B_SPLINE_CURVE ( ( 1.000000000000012212, 0.9238795325112745260, 1.000000000000000000, 0.9238795325112867385, 1.000000000000000000, 0.9238795325112867385, 1.000000000000000000, 0.9238795325112989509, 0.9999999999999877875 ) ) 
 REPRESENTATION_ITEM ( '' )  );
#43528=CARTESIAN_POINT ( 'NONE',  ( -5.000000000000005329, 188.3333333333333428, 8.660254037844387298 ) ) ;
#43531=CARTESIAN_POINT ( 'NONE',  ( -2.085542519210945728E-15, 159.8437499965860127, 11.35316468750000141 ) ) ;
#43533=CARTESIAN_POINT ( 'NONE',  ( 2.249999999999997780, 255.9999999999999432, 7.677076266392047543 ) ) ;
#43539=CARTESIAN_POINT ( 'NONE',  ( -3.042071309553173730, 4.635416663252684089, 11.35316468749999785 ) ) ;
#43544=( BOUNDED_CURVE ( )  B_SPLINE_CURVE ( 2, ( #59973, #3665, #49688, #15712, #73070, #25258, #19602, #72703, #10072, #21004, #15338, #44400, #70923 ),
 .UNSPECIFIED., .F., .F. ) 
 B_SPLINE_CURVE_WITH_KNOTS ( ( 3, 2, 2, 2, 2, 2, 3 ),
 ( 2.307884339682968911, 2.313118351314716659, 2.318352362946464851, 2.323586374578212599, 2.328820386209960347, 2.334054397841708539, 2.339288409473456287 ),
 .UNSPECIFIED. ) 
 CURVE ( )  GEOMETRIC_REPRESENTATION_ITEM ( )  RATIONAL_B_SPLINE_CURVE ( ( 0.9999999999999916733, 0.9659258262890766389, 1.000000000000000000, 0.9659258262890683122, 1.000000000000000000, 0.9659258262890683122, 1.000000000000000000, 0.9659258262890683122, 1.000000000000000000, 0.9659258262890683122, 1.000000000000000000, 0.9659258262890766389, 0.9999999999999916733 ) ) 
 REPRESENTATION_ITEM ( '' )  );
#43546=CARTESIAN_POINT ( 'NONE',  ( 10.00000000000000178, 52.08333332650537528, -2.679491924311226736 ) ) ;
#43550=CARTESIAN_POINT ( 'NONE',  ( 9.999999999999982236, 99.79166666666665719, 2.679491924311231621 ) ) ;
#43553=CARTESIAN_POINT ( 'NONE',  ( 7.320508075688787919, 159.3750000000000284, 7.320508075688790584 ) ) ;
#43555=ORIENTED_EDGE ( 'NONE', *, *, #60759, .T. ) ;
#43557=AXIS2_PLACEMENT_3D ( 'NONE', #2920, #35501, #18509 ) ;
#43558=CARTESIAN_POINT ( 'NONE',  ( 6.123233995736767268E-16, 161.2500000000000000, -10.00000000000000178 ) ) ;
#43560=CARTESIAN_POINT ( 'NONE',  ( 8.311093377946837890, 126.4062499965860269, -8.311093377946837890 ) ) ;
#43567=CARTESIAN_POINT ( 'NONE',  ( 7.320508075688789695, 44.37500000000001421, 7.320508075688792360 ) ) ;
#43568=CARTESIAN_POINT ( 'NONE',  ( -3.042071309553173730, 129.3229166632526983, 11.35316468749999785 ) ) ;
#43571=EDGE_CURVE ( 'NONE', #50470, #51437, #53702, .T. ) ;
#43575=CARTESIAN_POINT ( 'NONE',  ( 11.35316468750000141, 116.0937499965860127, 0.000000000000000000 ) ) ;
#43580=CARTESIAN_POINT ( 'NONE',  ( 6.951808397369818766E-16, 17.34374999658601624, -11.35316468750000141 ) ) ;
#43587=CARTESIAN_POINT ( 'NONE',  ( -4.721056650415998313, 287.5781250017069510, 4.721056650416000089 ) ) ;
#43588=CARTESIAN_POINT ( 'NONE',  ( 5.000000000000001776, 112.7083333265053682, -8.660254037844389075 ) ) ;
#43591=CARTESIAN_POINT ( 'NONE',  ( -11.35316468750000141, 138.5937499965860127, -1.390361679473963753E-15 ) ) ;
#43597=ORIENTED_EDGE ( 'NONE', *, *, #34372, .T. ) ;
#43608=CARTESIAN_POINT ( 'NONE',  ( 0.000000000000000000, 300.0000000000000000, 0.000000000000000000 ) ) ;
#43609=CARTESIAN_POINT ( 'NONE',  ( -5.676582343749998039, 182.4479166632526983, -9.832129032723420536 ) ) ;
#43611=CARTESIAN_POINT ( 'NONE',  ( 1.224646799147353454E-15, 300.0000000000000000, -10.00000000000000178 ) ) ;
#43612=CARTESIAN_POINT ( 'NONE',  ( -4.721056650415999201, 291.3281250017069510, -4.721056650415999201 ) ) ;
#43617=VERTEX_POINT ( 'NONE', #44676 ) ;
#43629=CARTESIAN_POINT ( 'NONE',  ( 5.676582343749993598, 120.2604166632526841, 9.832129032723422313 ) ) ;
#43630=CARTESIAN_POINT ( 'NONE',  ( 1.102182119232618108E-15, 296.2500000000000000, 6.000000000000001776 ) ) ;
#43635=ORIENTED_EDGE ( 'NONE', *, *, #63139, .T. ) ;
#43642=CARTESIAN_POINT ( 'NONE',  ( -9.832129032723420536, 194.0104166632526983, 5.676582343749997150 ) ) ;
#43648=DIRECTION ( 'NONE',  ( -0.000000000000000000, -0.000000000000000000, 1.000000000000000000 ) ) ;
#43649=CARTESIAN_POINT ( 'NONE',  ( -8.311093377946841443, 78.90624999658602690, 8.311093377946830785 ) ) ;
#43651=( BOUNDED_CURVE ( )  B_SPLINE_CURVE ( 2, ( #57395, #6455, #24149, #58506, #41149, #47161, #46056, #63, #6812, #58148, #23045, #12825, #17006 ),
 .UNSPECIFIED., .F., .F. ) 
 B_SPLINE_CURVE_WITH_KNOTS ( ( 3, 2, 2, 2, 2, 2, 3 ),
 ( 0.2119565217391304324, 0.2137681159420289911, 0.2155797101449275499, 0.2173913043478260809, 0.2192028985507246397, 0.2210144927536231985, 0.2228260869565217295 ),
 .UNSPECIFIED. ) 
 CURVE ( )  GEOMETRIC_REPRESENTATION_ITEM ( )  RATIONAL_B_SPLINE_CURVE ( ( 1.000000000000000000, 0.9659258262890683122, 1.000000000000000000, 0.9659258262890683122, 1.000000000000000000, 0.9659258262890683122, 1.000000000000000000, 0.9659258262890683122, 1.000000000000000000, 0.9659258262890683122, 1.000000000000000000, 0.9659258262890683122, 1.000000000000000000 ) ) 
 REPRESENTATION_ITEM ( '' )  );
#43656=CARTESIAN_POINT ( 'NONE',  ( -9.832129032723418760, 92.86458332991935549, -5.676582343750004256 ) ) ;
#43664=CARTESIAN_POINT ( 'NONE',  ( -9.832129032723418760, 92.86458332991935549, -5.676582343750004256 ) ) ;
#43668=CARTESIAN_POINT ( 'NONE',  ( 2.679491924311222739, 170.8333333265053398, 10.00000000000000355 ) ) ;
#43672=CARTESIAN_POINT ( 'NONE',  ( -11.35316468750000141, 78.80208332991935549, 3.042071309553159963 ) ) ;
#43673=CARTESIAN_POINT ( 'NONE',  ( 6.676582343750001591, 292.9531250017069510, -8.176455196517173205E-16 ) ) ;
#43675=CARTESIAN_POINT ( 'NONE',  ( 11.35316468749999785, 215.5729166632526699, 3.042071309553174174 ) ) ;
#43682=CARTESIAN_POINT ( 'NONE',  ( -5.676582343749998039, 212.4479166632526983, -9.832129032723420536 ) ) ;
#43687=CARTESIAN_POINT ( 'NONE',  ( 8.311093377946834337, 175.4687499965860127, 8.311093377946839666 ) ) ;
#43695=CARTESIAN_POINT ( 'NONE',  ( -10.00000000000000000, 7.291666666666665186, -2.679491924311229845 ) ) ;
#43702=CARTESIAN_POINT ( 'NONE',  ( 1.102182119232618108E-15, 293.3125000034140157, 6.000000000000001776 ) ) ;
#43705=CARTESIAN_POINT ( 'NONE',  ( -8.660254037844486774, 82.08333333333341386, -5.000000000000061284 ) ) ;
#43716=CARTESIAN_POINT ( 'NONE',  ( 8.311093377946834337, 80.46874999658601268, 8.311093377946839666 ) ) ;
#43721=CARTESIAN_POINT ( 'NONE',  ( -6.676582343750001591, 295.6093750017069510, 0.000000000000000000 ) ) ;
#43732=CARTESIAN_POINT ( 'NONE',  ( 0.000000000000000000, 300.0000000000000000, 0.000000000000000000 ) ) ;
#43737=CARTESIAN_POINT ( 'NONE',  ( 9.832129032723416984, 35.36458332991934839, 5.676582343750006032 ) ) ;
#43738=CARTESIAN_POINT ( 'NONE',  ( 4.999999999999995559, 149.1666666666666288, 8.660254037844394404 ) ) ;
#43739=CARTESIAN_POINT ( 'NONE',  ( -10.00000000000000000, 9.166666659838700326, -2.679491924311229845 ) ) ;
#43745=CARTESIAN_POINT ( 'NONE',  ( -3.042071309553173730, 54.32291666325268409, 11.35316468749999785 ) ) ;
#43751=CARTESIAN_POINT ( 'NONE',  ( -3.042071309553173730, 49.32291666325267698, 11.35316468749999785 ) ) ;
#43753=CARTESIAN_POINT ( 'NONE',  ( 8.660254037844387298, 205.4166666666666856, -4.999999999999999112 ) ) ;
#43754=CARTESIAN_POINT ( 'NONE',  ( -5.676582343750006032, 164.1145833299193555, 9.832129032723418760 ) ) ;
#43755=CARTESIAN_POINT ( 'NONE',  ( -2.679491924311225848, 133.3333333265053398, -10.00000000000000178 ) ) ;
#43758=CARTESIAN_POINT ( 'NONE',  ( -2.485281374238288432, 289.1875000000000568, 6.000000000000285105 ) ) ;
#43759=CARTESIAN_POINT ( 'NONE',  ( 5.676582343749993598, 20.26041666325268409, 9.832129032723422313 ) ) ;
#43766=CARTESIAN_POINT ( 'NONE',  ( -11.35316468750000141, 158.2812499965860127, -1.390361679473963753E-15 ) ) ;
#43777=CARTESIAN_POINT ( 'NONE',  ( -11.35316468749999785, 98.38541666325268409, -3.042071309553167513 ) ) ;
#43790=CARTESIAN_POINT ( 'NONE',  ( -2.679491924311235174, 160.4166666598386826, 10.00000000000000000 ) ) ;
#43795=AXIS2_PLACEMENT_3D ( 'NONE', #46625, #69645, #6648 ) ;
#43812=CARTESIAN_POINT ( 'NONE',  ( -7.320508075688773708, 106.8750000000000142, -7.320508075688774596 ) ) ;
#43814=CARTESIAN_POINT ( 'NONE',  ( 1.226468279477575784E-15, 290.8593750017070079, 6.676582343750001591 ) ) ;
#43822=CARTESIAN_POINT ( 'NONE',  ( -2.679491924311521167, 183.3333333265053966, -9.999999999999833022 ) ) ;
#43827=CARTESIAN_POINT ( 'NONE',  ( 5.676582343749993598, 4.947916663252683200, 9.832129032723422313 ) ) ;
#43829=CARTESIAN_POINT ( 'NONE',  ( -2.085542519210945728E-15, 199.8437499965860127, 11.35316468750000141 ) ) ;
#43832=CARTESIAN_POINT ( 'NONE',  ( 0.000000000000000000, 300.0000000000000000, 6.000000000000001776 ) ) ;
#43837=CARTESIAN_POINT ( 'NONE',  ( -11.35316468749999785, 13.07291666325268409, -3.042071309553167513 ) ) ;
#43845=CARTESIAN_POINT ( 'NONE',  ( 11.35316468749999785, 125.5729166632526983, 3.042071309553174174 ) ) ;
#43846=CARTESIAN_POINT ( 'NONE',  ( 4.999999999999993783, 86.04166665983869677, 8.660254037844390851 ) ) ;
#43849=CARTESIAN_POINT ( 'NONE',  ( -1.836970198721029983E-15, 200.6249999931720538, 10.00000000000000178 ) ) ;
#43852=CARTESIAN_POINT ( 'NONE',  ( -9.489879397300773789, 225.9999999999999716, 3.220560865818566931 ) ) ;
#43853=CARTESIAN_POINT ( 'NONE',  ( 4.721056650416000089, 290.9843750017070079, 4.721056650415999201 ) ) ;
#43858=CARTESIAN_POINT ( 'NONE',  ( 2.679491924311228956, 202.9166666598387110, -10.00000000000000000 ) ) ;
#43862=ADVANCED_FACE ( 'NONE', ( #15988 ), #9975, .T. ) ;
#43864=CARTESIAN_POINT ( 'NONE',  ( 9.832129032723420536, 156.5104166632526983, -5.676582343749999815 ) ) ;
#43865=CARTESIAN_POINT ( 'NONE',  ( -7.320508075688781702, 218.1250000000000284, 7.320508075688773708 ) ) ;
#43868=CARTESIAN_POINT ( 'NONE',  ( -9.832129032723420536, 59.01041666325268409, 5.676582343749997150 ) ) ;
#43874=CARTESIAN_POINT ( 'NONE',  ( 6.000000000000001776, 289.5625000034140157, -7.347880794884121708E-16 ) ) ;
#43885=ORIENTED_EDGE ( 'NONE', *, *, #12385, .F. ) ;
#43895=CARTESIAN_POINT ( 'NONE',  ( 6.000000000000001776, 299.5000000000000000, -7.347880794884121708E-16 ) ) ;
#43898=CARTESIAN_POINT ( 'NONE',  ( 2.220677790255211837E-11, 201.2499999999982663, -9.999999999999998224 ) ) ;
#43901=CARTESIAN_POINT ( 'NONE',  ( -5.000000000000005329, 63.33333333333333570, 8.660254037844387298 ) ) ;
#43904=CARTESIAN_POINT ( 'NONE',  ( 2.485281374238575314, 292.3125000000000000, 6.000000000000000888 ) ) ;
#43916=CARTESIAN_POINT ( 'NONE',  ( -7.320508075688778149, 193.1250000000000284, 7.320508075688769267 ) ) ;
#43919=CARTESIAN_POINT ( 'NONE',  ( -3.042071309553173730, 154.6354166632526699, 11.35316468749999785 ) ) ;
#43920=DIRECTION ( 'NONE',  ( 0.000000000000000000, 0.000000000000000000, 1.000000000000000000 ) ) ;
#43924=CARTESIAN_POINT ( 'NONE',  ( 1.224646799147353454E-15, 300.0000000000000000, -10.00000000000000178 ) ) ;
#43926=CARTESIAN_POINT ( 'NONE',  ( -11.35316468749999785, 23.38541666325268054, -3.042071309553167513 ) ) ;
#43932=CARTESIAN_POINT ( 'NONE',  ( -2.679491924311225848, 43.33333332650535397, -10.00000000000000178 ) ) ;
#43941=ORIENTED_EDGE ( 'NONE', *, *, #30429, .T. ) ;
#43942=CARTESIAN_POINT ( 'NONE',  ( -8.660254037844387298, 222.0833333333333428, -5.000000000000004441 ) ) ;
#43945=CARTESIAN_POINT ( 'NONE',  ( 5.676582343749993598, 129.9479166632526983, 9.832129032723422313 ) ) ;
#43949=FACE_OUTER_BOUND ( 'NONE', #22003, .T. ) ;
#43953=CARTESIAN_POINT ( 'NONE',  ( 8.311093377946834337, 130.1562499965860411, 8.311093377946839666 ) ) ;
#43956=DIRECTION ( 'NONE',  ( -0.000000000000000000, 1.000000000000000000, -0.000000000000000000 ) ) ;
#43958=CARTESIAN_POINT ( 'NONE',  ( 5.676582343749993598, 110.2604166632526841, 9.832129032723422313 ) ) ;
#43962=CARTESIAN_POINT ( 'NONE',  ( -8.311093377946841443, 24.21874999658601979, 8.311093377946830785 ) ) ;
#43967=EDGE_CURVE ( 'NONE', #53778, #11319, #72428, .T. ) ;
#43970=CARTESIAN_POINT ( 'NONE',  ( 4.721056650416000089, 287.8281250017069510, 4.721056650415999201 ) ) ;
#43971=DIRECTION ( 'NONE',  ( 0.000000000000000000, 0.000000000000000000, 1.000000000000000000 ) ) ;
#43974=CARTESIAN_POINT ( 'NONE',  ( 9.832129032723416984, 140.6770833299193555, 5.676582343750006032 ) ) ;
#43980=ADVANCED_FACE ( 'NONE', ( #40128 ), #23514, .T. ) ;
#43992=CARTESIAN_POINT ( 'NONE',  ( 9.832129032723416984, 180.3645833299193555, 5.676582343750006032 ) ) ;
#43995=CARTESIAN_POINT ( 'NONE',  ( 2.765530957081996366, 290.1406250017069510, -6.676582343750002480 ) ) ;
#43998=CARTESIAN_POINT ( 'NONE',  ( -2.679491924283695425, 66.45833333333087012, -10.00000000001589839 ) ) ;
#44005=DIRECTION ( 'NONE',  ( 0.000000000000000000, 0.000000000000000000, 1.000000000000000000 ) ) ;
#44010=CARTESIAN_POINT ( 'NONE',  ( 5.676582343749993598, 110.2604166632526841, 9.832129032723422313 ) ) ;
#44015=DIRECTION ( 'NONE',  ( -0.000000000000000000, 1.000000000000000000, -0.000000000000000000 ) ) ;
#44018=CARTESIAN_POINT ( 'NONE',  ( 9.830368419987745909, 224.8520141495858127, 1.857876432389923282 ) ) ;
#44019=CARTESIAN_POINT ( 'NONE',  ( 11.35316468749999963, 225.9895833299193839, -3.042071309553165293 ) ) ;
#44024=CARTESIAN_POINT ( 'NONE',  ( -9.832129032723418760, 213.1770833299193555, -5.676582343750004256 ) ) ;
#44032=CARTESIAN_POINT ( 'NONE',  ( -3.042071309553164404, 92.23958332991935549, -11.35316468749999963 ) ) ;
#44038=CARTESIAN_POINT ( 'NONE',  ( -11.35316468749999785, 88.07291666325266988, -3.042071309553167513 ) ) ;
#44046=CARTESIAN_POINT ( 'NONE',  ( -8.311093377946841443, 83.90624999658602690, 8.311093377946834337 ) ) ;
#44051=CARTESIAN_POINT ( 'NONE',  ( -8.660254037844387298, 183.9583333265053682, -5.000000000000004441 ) ) ;
#44052=CARTESIAN_POINT ( 'NONE',  ( -6.000000000000001776, 287.0625000034140157, 0.000000000000000000 ) ) ;
#44053=CARTESIAN_POINT ( 'NONE',  ( 3.042071309553167513, 77.13541666325266988, -11.35316468749999785 ) ) ;
#44054=CARTESIAN_POINT ( 'NONE',  ( 4.721056650416000089, 293.8281250017069510, 4.721056650415999201 ) ) ;
#44056=CARTESIAN_POINT ( 'NONE',  ( -8.311093377946841443, 208.9062499965860411, 8.311093377946830785 ) ) ;
#44057=EDGE_LOOP ( 'NONE', ( #36624, #69980, #25503, #32682 ) ) ;
#44058=CARTESIAN_POINT ( 'NONE',  ( -7.320508075688773708, 68.74999999317202537, -7.320508075688774596 ) ) ;
#44062=CARTESIAN_POINT ( 'NONE',  ( 11.35316468749999963, 200.9895833299193839, -3.042071309553165293 ) ) ;
#44068=CARTESIAN_POINT ( 'NONE',  ( 3.042071309553159519, 195.0520833299193271, 11.35316468750000141 ) ) ;
#44075=CARTESIAN_POINT ( 'NONE',  ( -10.00000000000000178, 12.50000000000000000, -1.224646799147353454E-15 ) ) ;
#44088=CARTESIAN_POINT ( 'NONE',  ( 1.267086777181619559E-12, 183.7500000000001137, 10.00000000000000178 ) ) ;
#44090=VERTEX_POINT ( 'NONE', #6914 ) ;
#44099=CARTESIAN_POINT ( 'NONE',  ( -5.676582343750006032, 69.42708332991935549, 9.832129032723418760 ) ) ;
#44104=CARTESIAN_POINT ( 'NONE',  ( 6.676582343750003368, 289.0468750017070079, 2.765530957081995478 ) ) ;
#44113=CARTESIAN_POINT ( 'NONE',  ( -3.042071309553164404, 167.5520833299193271, -11.35316468749999963 ) ) ;
#44116=CARTESIAN_POINT ( 'NONE',  ( -3.673940397442060854E-16, 289.8125000034140157, -6.000000000000001776 ) ) ;
#44121=CARTESIAN_POINT ( 'NONE',  ( -11.35316468750000141, 38.28124999658602690, -1.390361679473963753E-15 ) ) ;
#44124=CARTESIAN_POINT ( 'NONE',  ( -8.660254037844387298, 18.95833332650536818, -5.000000000000004441 ) ) ;
#44129=CARTESIAN_POINT ( 'NONE',  ( 8.311093377946834337, 50.15624999658601268, 8.311093377946839666 ) ) ;
#44135=CARTESIAN_POINT ( 'NONE',  ( 9.832129032723420536, 51.19791666325268409, -5.676582343749999815 ) ) ;
#44138=CARTESIAN_POINT ( 'NONE',  ( 5.676582343749993598, 159.9479166632526983, 9.832129032723422313 ) ) ;
#44139=CARTESIAN_POINT ( 'NONE',  ( -2.679491924311235618, 140.4166666598387110, 10.00000000000000000 ) ) ;
#44142=CARTESIAN_POINT ( 'NONE',  ( -11.35316468750000141, 28.80208332991935194, 3.042071309553159963 ) ) ;
#44143=CARTESIAN_POINT ( 'NONE',  ( -2.679491924311284468, 16.45833333333334636, -9.999999999999980460 ) ) ;
#44144=ORIENTED_EDGE ( 'NONE', *, *, #14931, .T. ) ;
#44147=CARTESIAN_POINT ( 'NONE',  ( 9.832129032723416984, 165.3645833299193555, 5.676582343750006032 ) ) ;
#44155=CARTESIAN_POINT ( 'NONE',  ( -7.320508075688773708, 118.7499999931720396, -7.320508075688774596 ) ) ;
#44157=CARTESIAN_POINT ( 'NONE',  ( 3.042071309553167069, 117.1354166632526557, -11.35316468749999785 ) ) ;
#44174=CARTESIAN_POINT ( 'NONE',  ( -1.967015505459129087E-11, 148.7499999999984936, 10.00000000000000533 ) ) ;
#44190=CARTESIAN_POINT ( 'NONE',  ( -2.679491924311225848, 111.4583333333333286, -10.00000000000000178 ) ) ;
#44192=CARTESIAN_POINT ( 'NONE',  ( -6.676582343750001591, 291.6093750017069510, 0.000000000000000000 ) ) ;
#44205=CARTESIAN_POINT ( 'NONE',  ( -1.836970198721029983E-15, 95.62499999317203958, 10.00000000000000178 ) ) ;
#44207=CARTESIAN_POINT ( 'NONE',  ( 3.090143665460689970, 225.9995416778970707, -9.510573701245009559 ) ) ;
#44209=CARTESIAN_POINT ( 'NONE',  ( -9.832129032723420536, 204.0104166632526983, 5.676582343749997150 ) ) ;
#44210=CARTESIAN_POINT ( 'NONE',  ( -3.042071309553164404, 2.239583329919349719, -11.35316468749999963 ) ) ;
#44214=CARTESIAN_POINT ( 'NONE',  ( 0.000000000000000000, 300.0000000000000000, 0.000000000000000000 ) ) ;
#44217=CARTESIAN_POINT ( 'NONE',  ( -9.832129032723420536, 13.69791666325268409, 5.676582343749997150 ) ) ;
#44223=CARTESIAN_POINT ( 'NONE',  ( 11.35316468749999785, 10.57291666325268409, 3.042071309553174174 ) ) ;
#44226=CARTESIAN_POINT ( 'NONE',  ( -8.311093377946841443, 123.9062499965860411, 8.311093377946830785 ) ) ;
#44229=CARTESIAN_POINT ( 'NONE',  ( -10.00000000000000355, 84.58333332650538239, 2.679491924311223183 ) ) ;
#44232=CARTESIAN_POINT ( 'NONE',  ( 6.123233995736767268E-16, 198.1249999931720538, -10.00000000000000178 ) ) ;
#44233=CARTESIAN_POINT ( 'NONE',  ( 10.00000000000000711, 145.2083333333333144, -2.679491924311228512 ) ) ;
#44234=ORIENTED_EDGE ( 'NONE', *, *, #69038, .T. ) ;
#44236=CARTESIAN_POINT ( 'NONE',  ( 4.721056650415999201, 291.2343750017069510, -4.721056650415999201 ) ) ;
#44240=CARTESIAN_POINT ( 'NONE',  ( -7.320508075688773708, 208.7499999931720254, -7.320508075688774596 ) ) ;
#44245=CARTESIAN_POINT ( 'NONE',  ( 7.320508075688771044, 156.2499999931720538, 7.320508075688775484 ) ) ;
#44246=CARTESIAN_POINT ( 'NONE',  ( -11.35316468750000141, 148.8020833299193555, 3.042071309553159963 ) ) ;
#44250=CARTESIAN_POINT ( 'NONE',  ( 11.35316468749999785, 60.88541666325269119, 3.042071309553174174 ) ) ;
#44251=ORIENTED_EDGE ( 'NONE', *, *, #11874, .T. ) ;
#44257=CARTESIAN_POINT ( 'NONE',  ( -2.485281374238571761, 287.8750000034139589, -6.000000000000003553 ) ) ;
#44279=CARTESIAN_POINT ( 'NONE',  ( -5.000000000000005329, 68.33333333333334281, 8.660254037844387298 ) ) ;
#44281=CARTESIAN_POINT ( 'NONE',  ( 4.242640687119287435, 291.3750000000000000, 4.242640687119285658 ) ) ;
#44290=CARTESIAN_POINT ( 'NONE',  ( -7.320508075688806571, 78.12500000000004263, 7.320508075688797689 ) ) ;
#44291=CARTESIAN_POINT ( 'NONE',  ( 10.00000000000000000, 184.7916666666666572, 2.679491924311236062 ) ) ;
#44294=CARTESIAN_POINT ( 'NONE',  ( 9.832129032723416984, 155.6770833299193555, 5.676582343750006032 ) ) ;
#44297=CARTESIAN_POINT ( 'NONE',  ( 1.934925017735378189E-11, 153.7500000000015348, 10.00000000000000533 ) ) ;
#44300=CARTESIAN_POINT ( 'NONE',  ( 8.311093377946834337, 25.46874999658601624, 8.311093377946839666 ) ) ;
#44307=CARTESIAN_POINT ( 'NONE',  ( -10.00000000000000000, 49.16666665983869677, -2.679491924311229845 ) ) ;
#44310=CARTESIAN_POINT ( 'NONE',  ( 1.224646799147353454E-15, 300.0000000000000000, -10.00000000000000178 ) ) ;
#44312=DIRECTION ( 'NONE',  ( -0.000000000000000000, 1.000000000000000000, -0.000000000000000000 ) ) ;
#44313=CARTESIAN_POINT ( 'NONE',  ( 2.679491924311959039, 163.9583333333334565, 9.999999999999579003 ) ) ;
#44315=( BOUNDED_CURVE ( )  B_SPLINE_CURVE ( 2, ( #42179, #30873, #35076, #41822, #13135, #59190, #6399, #64832, #7500, #13502, #58820, #41461, #58088 ),
 .UNSPECIFIED., .F., .F. ) 
 B_SPLINE_CURVE_WITH_KNOTS ( ( 3, 2, 2, 2, 2, 2, 3 ),
 ( 0.2554347826086956208, 0.2572463768115941241, 0.2590579710144926828, 0.2608695652173912416, 0.2626811594202898559, 0.2644927536231884146, 0.2663043478260869734 ),
 .UNSPECIFIED. ) 
 CURVE ( )  GEOMETRIC_REPRESENTATION_ITEM ( )  RATIONAL_B_SPLINE_CURVE ( ( 1.000000000000001110, 0.9659258262890673130, 1.000000000000000000, 0.9659258262890683122, 1.000000000000000000, 0.9659258262890683122, 1.000000000000000000, 0.9659258262890683122, 1.000000000000000000, 0.9659258262890683122, 1.000000000000000000, 0.9659258262890683122, 1.000000000000000000 ) ) 
 REPRESENTATION_ITEM ( '' )  );
#44321=CARTESIAN_POINT ( 'NONE',  ( 3.042071309553159519, 139.7395833299193555, 11.35316468750000141 ) ) ;
#44325=CARTESIAN_POINT ( 'NONE',  ( 1.332431167089188095E-11, 191.2499999999989768, -10.00000000000000533 ) ) ;
#44328=CARTESIAN_POINT ( 'NONE',  ( 8.311093377946837890, 131.4062499965860411, -8.311093377946837890 ) ) ;
#44329=CARTESIAN_POINT ( 'NONE',  ( 5.000000000000001776, 147.7083333265053682, -8.660254037844389075 ) ) ;
#44330=EDGE_LOOP ( 'NONE', ( #24994, #60258, #43501, #59686 ) ) ;
#44331=AXIS2_PLACEMENT_3D ( 'NONE', #12908, #29907, #70994 ) ;
#44334=CARTESIAN_POINT ( 'NONE',  ( 3.042071309553159519, 110.0520833299193413, 11.35316468750000141 ) ) ;
#44338=CARTESIAN_POINT ( 'NONE',  ( -8.311093377946836114, 22.96874999658601624, -8.311093377946837890 ) ) ;
#44339=( BOUNDED_CURVE ( )  B_SPLINE_CURVE ( 2, ( #29557, #18235, #14028, #19330, #60817, #37441, #36332, #49117, #53682, #31027, #8770, #1993, #24985 ),
 .UNSPECIFIED., .F., .F. ) 
 B_SPLINE_CURVE_WITH_KNOTS ( ( 3, 2, 2, 2, 2, 2, 3 ),
 ( 0.2445652173913043514, 0.2463768115942029102, 0.2481884057971014135, 0.2499999999999999722, 0.2518115942028985033, 0.2536231884057970620, 0.2554347826086956208 ),
 .UNSPECIFIED. ) 
 CURVE ( )  GEOMETRIC_REPRESENTATION_ITEM ( )  RATIONAL_B_SPLINE_CURVE ( ( 1.000000000000000000, 0.9659258262890683122, 1.000000000000000000, 0.9659258262890683122, 1.000000000000000000, 0.9659258262890683122, 1.000000000000000000, 0.9659258262890683122, 1.000000000000000000, 0.9659258262890683122, 1.000000000000000000, 0.9659258262890693114, 0.9999999999999990008 ) ) 
 REPRESENTATION_ITEM ( '' )  );
#44346=CARTESIAN_POINT ( 'NONE',  ( -2.765530957081998586, 288.6406250017069510, 6.676582343750001591 ) ) ;
#44348=CARTESIAN_POINT ( 'NONE',  ( -2.485281374238187180, 297.1875000000000568, 6.000000000000385469 ) ) ;
#44351=CARTESIAN_POINT ( 'NONE',  ( -11.35316468749999785, 148.3854166632526983, -3.042071309553167513 ) ) ;
#44356=EDGE_LOOP ( 'NONE', ( #59036, #30228, #23563, #18815 ) ) ;
#44365=CARTESIAN_POINT ( 'NONE',  ( 3.042071309553167069, 186.8229166632527267, -11.35316468749999785 ) ) ;
#44370=CARTESIAN_POINT ( 'NONE',  ( 7.320508075688771044, 131.2499999931720254, 7.320508075688775484 ) ) ;
#44383=CARTESIAN_POINT ( 'NONE',  ( 11.35316468749999785, 120.8854166632526841, 3.042071309553174174 ) ) ;
#44394=CARTESIAN_POINT ( 'NONE',  ( 3.042071309553159519, 205.0520833299193271, 11.35316468750000141 ) ) ;
#44396=CARTESIAN_POINT ( 'NONE',  ( 10.14468825070462898, 226.0000000000000000, 4.203934788660792954 ) ) ;
#44400=CARTESIAN_POINT ( 'NONE',  ( 2.679491924311817375, 186.0416666666666288, -9.999999999999653610 ) ) ;
#44402=CARTESIAN_POINT ( 'NONE',  ( -2.085542519210945728E-15, 94.53124999658601268, 11.35316468750000141 ) ) ;
#44408=CARTESIAN_POINT ( 'NONE',  ( 5.676582343750001591, 86.61458332991936970, -9.832129032723420536 ) ) ;
#44410=CARTESIAN_POINT ( 'NONE',  ( -6.338291171875001240, 299.8046875008535039, 0.000000000000000000 ) ) ;
#44413=DIRECTION ( 'NONE',  ( -0.000000000000000000, 1.000000000000000000, -0.000000000000000000 ) ) ;
#44417=CARTESIAN_POINT ( 'NONE',  ( -5.676582343750006032, 89.11458332991935549, 9.832129032723418760 ) ) ;
#44421=CARTESIAN_POINT ( 'NONE',  ( -7.320508075688778149, 179.9999999931720254, 7.320508075688769267 ) ) ;
#44423=CARTESIAN_POINT ( 'NONE',  ( 8.311093377946837890, 71.71874999658601268, -8.311093377946837890 ) ) ;
#44424=CARTESIAN_POINT ( 'NONE',  ( 2.765530957081996366, 293.1406250017069510, -6.676582343750003368 ) ) ;
#44426=CARTESIAN_POINT ( 'NONE',  ( 3.042071309553159519, 214.7395833299193271, 11.35316468750000141 ) ) ;
#44429=CARTESIAN_POINT ( 'NONE',  ( 0.000000000000000000, 300.0000000000000000, 0.000000000000000000 ) ) ;
#44432=CARTESIAN_POINT ( 'NONE',  ( 3.042071309553159519, 209.7395833299193839, 11.35316468750000141 ) ) ;
#44435=DIRECTION ( 'NONE',  ( -0.000000000000000000, 1.000000000000000000, -0.000000000000000000 ) ) ;
#44438=CARTESIAN_POINT ( 'NONE',  ( -3.042071309553163960, 192.5520833299193271, -11.35316468749999963 ) ) ;
#44446=CARTESIAN_POINT ( 'NONE',  ( 7.320508075688774596, 10.62500000000000000, -7.320508075688774596 ) ) ;
#44455=CARTESIAN_POINT ( 'NONE',  ( 2.679491924311228956, 17.91666665983870388, -10.00000000000000000 ) ) ;
#44465=ORIENTED_EDGE ( 'NONE', *, *, #21867, .F. ) ;
#44466=EDGE_LOOP ( 'NONE', ( #57997, #21131, #42617, #58371 ) ) ;
#44468=CARTESIAN_POINT ( 'NONE',  ( -5.676582343749998039, 77.76041666325268409, -9.832129032723420536 ) ) ;
#44473=CARTESIAN_POINT ( 'NONE',  ( -4.721056650415999201, 291.4843750017070079, -4.721056650415999201 ) ) ;
#44482=CARTESIAN_POINT ( 'NONE',  ( 9.832129032723416984, 170.6770833299193555, 5.676582343750006032 ) ) ;
#44485=CARTESIAN_POINT ( 'NONE',  ( 6.123233995736767268E-16, 18.12499999317203248, -10.00000000000000178 ) ) ;
#44490=CARTESIAN_POINT ( 'NONE',  ( 3.042071309553159519, 59.73958332991934839, 11.35316468750000141 ) ) ;
#44492=CARTESIAN_POINT ( 'NONE',  ( -2.679491924311225848, 28.33333332650536818, -10.00000000000000178 ) ) ;
#44497=CARTESIAN_POINT ( 'NONE',  ( -3.042071309553164404, 52.23958332991934128, -11.35316468749999963 ) ) ;
#44503=CARTESIAN_POINT ( 'NONE',  ( -9.832129032723418760, 42.86458332991934839, -5.676582343750004256 ) ) ;
#44507=CARTESIAN_POINT ( 'NONE',  ( -11.35316468749999785, 178.0729166632526415, -3.042071309553167513 ) ) ;
#44509=CARTESIAN_POINT ( 'NONE',  ( -10.00000000000000178, 144.3749999931720538, -1.224646799147353454E-15 ) ) ;
#44512=CARTESIAN_POINT ( 'NONE',  ( -2.085542519210945728E-15, 34.84374999658601268, 11.35316468750000141 ) ) ;
#44518=CARTESIAN_POINT ( 'NONE',  ( 5.676582343749993598, 169.9479166632526983, 9.832129032723422313 ) ) ;
#44529=CARTESIAN_POINT ( 'NONE',  ( 9.832129032723416984, 110.6770833299193555, 5.676582343750006032 ) ) ;
#44552=CARTESIAN_POINT ( 'NONE',  ( 2.679491924311222739, 70.83333332650538239, 10.00000000000000355 ) ) ;
#44554=ORIENTED_EDGE ( 'NONE', *, *, #60989, .F. ) ;
#44563=CARTESIAN_POINT ( 'NONE',  ( -2.679491924311225848, 126.4583333333333428, -10.00000000000000178 ) ) ;
#44565=CARTESIAN_POINT ( 'NONE',  ( -4.088227598258586603E-16, 293.3593750017070079, -6.676582343750001591 ) ) ;
#44579=CARTESIAN_POINT ( 'NONE',  ( -10.00000000000000000, 214.1666666598386826, -2.679491924311229845 ) ) ;
#44580=CARTESIAN_POINT ( 'NONE',  ( 11.35316468749999785, 10.57291666325268409, 3.042071309553174174 ) ) ;
#44583=CARTESIAN_POINT ( 'NONE',  ( 3.042071309553167069, 207.1354166632526415, -11.35316468749999785 ) ) ;
#44590=CARTESIAN_POINT ( 'NONE',  ( 8.311093377946834337, 10.15624999658601801, 8.311093377946839666 ) ) ;
#44592=CARTESIAN_POINT ( 'NONE',  ( 2.679491924286489191, 208.9583333333311543, 10.00000000001428369 ) ) ;
#44596=CARTESIAN_POINT ( 'NONE',  ( 11.35316468749999963, 10.98958332991935016, -3.042071309553165293 ) ) ;
#44598=CARTESIAN_POINT ( 'NONE',  ( 3.042071309553167069, 116.8229166632526983, -11.35316468749999785 ) ) ;
#44599=CARTESIAN_POINT ( 'NONE',  ( 10.00000000000000178, 101.8749999931720396, 0.000000000000000000 ) ) ;
#44602=CARTESIAN_POINT ( 'NONE',  ( -8.660254037844390851, 199.7916666598387110, 4.999999999999998224 ) ) ;
#44605=DIRECTION ( 'NONE',  ( -0.000000000000000000, 1.000000000000000000, -0.000000000000000000 ) ) ;
#44606=CARTESIAN_POINT ( 'NONE',  ( -6.676582343750003368, 291.5468750017069510, -2.765530957081996810 ) ) ;
#44615=CARTESIAN_POINT ( 'NONE',  ( 5.676582343749993598, 160.2604166632526983, 9.832129032723422313 ) ) ;
#44619=CARTESIAN_POINT ( 'NONE',  ( -3.042071309553164404, 77.55208332991932707, -11.35316468749999963 ) ) ;
#44623=EDGE_LOOP ( 'NONE', ( #27653, #69100, #38254 ) ) ;
#44631=DIRECTION ( 'NONE',  ( -1.000000000000000000, 0.000000000000000000, -0.000000000000000000 ) ) ;
#44634=AXIS2_PLACEMENT_3D ( 'NONE', #19557, #20296, #61046 ) ;
#44635=VERTEX_POINT ( 'NONE', #17597 ) ;
#44649=CARTESIAN_POINT ( 'NONE',  ( 4.999999999999993783, 84.16666666666667140, 8.660254037844390851 ) ) ;
#44651=CARTESIAN_POINT ( 'NONE',  ( 6.000000000000003553, 293.4374999999998863, 2.485281374238571317 ) ) ;
#44655=ORIENTED_EDGE ( 'NONE', *, *, #48677, .T. ) ;
#44656=( BOUNDED_CURVE ( )  B_SPLINE_CURVE ( 2, ( #33075, #72283, #27373, #31556, #50393, #73408, #21712, #44741, #54580 ),
 .UNSPECIFIED., .F., .F. ) 
 B_SPLINE_CURVE_WITH_KNOTS ( ( 3, 2, 2, 2, 3 ),
 ( 0.3541666666666646313, 0.3645833333333312609, 0.3749999999999980016, 0.3854166666666646868, 0.3958333333333313164 ),
 .UNSPECIFIED. ) 
 CURVE ( )  GEOMETRIC_REPRESENTATION_ITEM ( )  RATIONAL_B_SPLINE_CURVE ( ( 1.000000000000015099, 0.9238795325112717505, 1.000000000000000000, 0.9238795325112867385, 1.000000000000000000, 0.9238795325112867385, 1.000000000000000000, 0.9238795325113013934, 0.9999999999999853451 ) ) 
 REPRESENTATION_ITEM ( '' )  );
#44664=CARTESIAN_POINT ( 'NONE',  ( -8.660254037844387298, 192.0833333333333428, -5.000000000000004441 ) ) ;
#44668=CARTESIAN_POINT ( 'NONE',  ( -11.35316468750000141, 163.5937499965860127, -1.390361679473963753E-15 ) ) ;
#44670=CARTESIAN_POINT ( 'NONE',  ( 7.320508075688907823, 155.6250000000001137, -7.320508075688907823 ) ) ;
#44674=CARTESIAN_POINT ( 'NONE',  ( -11.35316468750000141, 23.80208332991934839, 3.042071309553159963 ) ) ;
#44676=CARTESIAN_POINT ( 'NONE',  ( 1.224646799147353454E-15, 0.000000000000000000, -10.00000000000000178 ) ) ;
#44680=CARTESIAN_POINT ( 'NONE',  ( -8.660254037844387298, 63.95833332650536818, -5.000000000000004441 ) ) ;
#44685=CARTESIAN_POINT ( 'NONE',  ( 8.660254037844389075, 165.4166666666666856, -5.000000000000000000 ) ) ;
#44686=ORIENTED_EDGE ( 'NONE', *, *, #21049, .F. ) ;
#44688=CARTESIAN_POINT ( 'NONE',  ( -5.000000000000005329, 223.3333333333333428, 8.660254037844387298 ) ) ;
#44692=CARTESIAN_POINT ( 'NONE',  ( -2.085542519210945728E-15, 139.5312499965860411, 11.35316468750000141 ) ) ;
#44696=CARTESIAN_POINT ( 'NONE',  ( 6.123233995736767268E-16, 46.25000000000000711, -10.00000000000000178 ) ) ;
#44705=CARTESIAN_POINT ( 'NONE',  ( -11.35316468750000141, 108.8020833299193555, 3.042071309553159963 ) ) ;
#44709=CARTESIAN_POINT ( 'NONE',  ( 3.042071309553159519, 35.05208332991935549, 11.35316468750000141 ) ) ;
#44717=CARTESIAN_POINT ( 'NONE',  ( -4.721056650415998313, 289.5781250017069510, 4.721056650416000089 ) ) ;
#44721=CARTESIAN_POINT ( 'NONE',  ( -2.085542519210945728E-15, 139.8437499965860127, 11.35316468750000141 ) ) ;
#44726=ORIENTED_EDGE ( 'NONE', *, *, #56751, .T. ) ;
#44737=CARTESIAN_POINT ( 'NONE',  ( 5.676582343749993598, 189.9479166632526983, 9.832129032723422313 ) ) ;
#44741=CARTESIAN_POINT ( 'NONE',  ( 2.485281374238939911, 295.3125000000000568, 5.999999999999634959 ) ) ;
#44742=CARTESIAN_POINT ( 'NONE',  ( -6.676582343750001591, 287.4531250017069510, 0.000000000000000000 ) ) ;
#44743=CARTESIAN_POINT ( 'NONE',  ( 9.999999999999998224, 34.99999999999999289, 0.000000000000000000 ) ) ;
#44744=CARTESIAN_POINT ( 'NONE',  ( 4.999999999999991118, 94.16666666666667140, 8.660254037844387298 ) ) ;
#44754=CARTESIAN_POINT ( 'NONE',  ( -10.00000000000000355, 142.7083333333333712, 2.679491924311223183 ) ) ;
#44758=CARTESIAN_POINT ( 'NONE',  ( 11.35316468749999963, 126.3020833299193555, -3.042071309553165293 ) ) ;
#44764=ORIENTED_EDGE ( 'NONE', *, *, #39189, .T. ) ;
#44765=CARTESIAN_POINT ( 'NONE',  ( 8.434195340655811890, 224.5471093110514289, 5.405325235466309053 ) ) ;
#44767=CARTESIAN_POINT ( 'NONE',  ( 0.000000000000000000, 300.0000000000000000, 0.000000000000000000 ) ) ;
#44769=CARTESIAN_POINT ( 'NONE',  ( 11.35316468749999785, 200.8854166632526699, 3.042071309553174174 ) ) ;
#44775=CARTESIAN_POINT ( 'NONE',  ( -8.311093377946836114, 92.65624999658602690, -8.311093377946837890 ) ) ;
#44783=CARTESIAN_POINT ( 'NONE',  ( 8.311093377946837890, 106.4062499965859985, -8.311093377946837890 ) ) ;
#44791=CARTESIAN_POINT ( 'NONE',  ( -5.676582343749998039, 82.44791666325268409, -9.832129032723420536 ) ) ;
#44794=CARTESIAN_POINT ( 'NONE',  ( 6.123233995736767268E-16, 126.2500000000000000, -10.00000000000000178 ) ) ;
#44795=CARTESIAN_POINT ( 'NONE',  ( 10.00000000000000178, 176.8749999931720538, 0.000000000000000000 ) ) ;
#44797=CARTESIAN_POINT ( 'NONE',  ( -5.676582343749998039, 72.76041666325268409, -9.832129032723420536 ) ) ;
#44798=CARTESIAN_POINT ( 'NONE',  ( 6.676582343750003368, 289.0156250017070079, -2.765530957081997254 ) ) ;
#44800=CARTESIAN_POINT ( 'NONE',  ( -9.832129032723418760, 222.8645833299193839, -5.676582343750004256 ) ) ;
#44805=CARTESIAN_POINT ( 'NONE',  ( -8.311093377946841443, 208.9062499965860127, 8.311093377946834337 ) ) ;
#44807=CARTESIAN_POINT ( 'NONE',  ( 4.721056650415999201, 299.0781250017069510, -4.721056650415999201 ) ) ;
#44808=EDGE_LOOP ( 'NONE', ( #19266, #40887, #70692, #11806 ) ) ;
#44809=CARTESIAN_POINT ( 'NONE',  ( -3.042071309553173730, 189.6354166632526983, 11.35316468749999785 ) ) ;
#44818=CARTESIAN_POINT ( 'NONE',  ( -7.320508075688773708, 11.87500000000000000, -7.320508075688774596 ) ) ;
#44827=EDGE_CURVE ( 'NONE', #14172, #4343, #69572, .T. ) ;
#44839=ORIENTED_EDGE ( 'NONE', *, *, #37961, .T. ) ;
#44840=ORIENTED_EDGE ( 'NONE', *, *, #28735, .T. ) ;
#44842=CARTESIAN_POINT ( 'NONE',  ( -11.35316468750000141, 68.59374999658601268, -1.390361679473963753E-15 ) ) ;
#44847=CARTESIAN_POINT ( 'NONE',  ( 1.226468279477575784E-15, 291.8593750017070079, 6.676582343750001591 ) ) ;
#44848=CARTESIAN_POINT ( 'NONE',  ( 2.679491924311228956, 77.91666665983871098, -10.00000000000000000 ) ) ;
#44857=CARTESIAN_POINT ( 'NONE',  ( 8.311093377946837890, 171.7187499965860127, -8.311093377946837890 ) ) ;
#44865=CARTESIAN_POINT ( 'NONE',  ( 11.35316468750000141, 50.78124999658601979, 0.000000000000000000 ) ) ;
#44867=CARTESIAN_POINT ( 'NONE',  ( 10.00000000000000178, 17.08333332650536818, -2.679491924311226736 ) ) ;
#44872=CARTESIAN_POINT ( 'NONE',  ( -5.676582343749998039, 57.44791666325268409, -9.832129032723420536 ) ) ;
#44878=CARTESIAN_POINT ( 'NONE',  ( -9.832129032723418760, 52.86458332991934839, -5.676582343750004256 ) ) ;
#44882=CARTESIAN_POINT ( 'NONE',  ( -2.085542519210945728E-15, 179.5312499965860411, 11.35316468750000141 ) ) ;
#44883=CARTESIAN_POINT ( 'NONE',  ( -1.836970198721029983E-15, 145.6249999931720538, 10.00000000000000178 ) ) ;
#44887=CARTESIAN_POINT ( 'NONE',  ( 5.676582343750001591, 31.92708332991935194, -9.832129032723420536 ) ) ;
#44889=CARTESIAN_POINT ( 'NONE',  ( -11.35316468750000141, 168.4895833299193839, 3.042071309553159963 ) ) ;
#44894=CARTESIAN_POINT ( 'NONE',  ( -8.311093377946836114, 167.6562499965860411, -8.311093377946837890 ) ) ;
#44905=CARTESIAN_POINT ( 'NONE',  ( -8.311093377946836114, 112.9687499965860269, -8.311093377946837890 ) ) ;
#44909=EDGE_CURVE ( 'NONE', #72057, #17570, #59234, .T. ) ;
#44928=VERTEX_POINT ( 'NONE', #2099 ) ;
#44936=CARTESIAN_POINT ( 'NONE',  ( -10.00000000000000000, 117.2916666666666430, -2.679491924311229845 ) ) ;
#44939=CARTESIAN_POINT ( 'NONE',  ( 4.721056650415999201, 291.2343750017069510, -4.721056650415999201 ) ) ;
#44947=CARTESIAN_POINT ( 'NONE',  ( -2.249999999999998224, 283.9999999998748308, 5.427273999917394676 ) ) ;
#44953=CARTESIAN_POINT ( 'NONE',  ( -5.676582343750006032, 9.114583329919350163, 9.832129032723418760 ) ) ;
#44955=CARTESIAN_POINT ( 'NONE',  ( -8.311093377946841443, 214.2187499965860411, 8.311093377946830785 ) ) ;
#44962=CARTESIAN_POINT ( 'NONE',  ( -11.35316468750000141, 8.489583329919348387, 3.042071309553159963 ) ) ;
#44964=CARTESIAN_POINT ( 'NONE',  ( 2.485281374238919927, 292.3125000000000568, 5.999999999999654499 ) ) ;
#44968=CARTESIAN_POINT ( 'NONE',  ( -2.085542519210945728E-15, 4.531249996586016238, 11.35316468750000141 ) ) ;
#44970=CARTESIAN_POINT ( 'NONE',  ( -9.832129032723418760, 137.8645833299193555, -5.676582343750004256 ) ) ;
#44971=CARTESIAN_POINT ( 'NONE',  ( 8.660254037844389075, 102.2916666598386968, -5.000000000000000000 ) ) ;
#44974=FACE_OUTER_BOUND ( 'NONE', #22229, .T. ) ;
#44976=CARTESIAN_POINT ( 'NONE',  ( 10.00000000000000533, 144.7916666666666856, 2.679491924311237394 ) ) ;
#44979=CARTESIAN_POINT ( 'NONE',  ( 6.676582343750003368, 289.1718750017070647, -2.765530957081997254 ) ) ;
#44980=CYLINDRICAL_SURFACE ( 'NONE', #66426, 10.00000000000000178 ) ;
#44987=CARTESIAN_POINT ( 'NONE',  ( 3.042071309553159519, 175.0520833299193555, 11.35316468750000141 ) ) ;
#44991=CARTESIAN_POINT ( 'NONE',  ( 11.35316468749999963, 71.30208332991932707, -3.042071309553165293 ) ) ;
#44999=CARTESIAN_POINT ( 'NONE',  ( 2.679491924311222739, 113.9583333333333570, 10.00000000000000355 ) ) ;
#45000=CARTESIAN_POINT ( 'NONE',  ( 8.660254037844389075, 67.29166665983869677, -5.000000000000000000 ) ) ;
#45008=CYLINDRICAL_SURFACE ( 'NONE', #36119, 10.00000000000000178 ) ;
#45016=AXIS2_PLACEMENT_3D ( 'NONE', #61306, #66583, #11387 ) ;
#45022=DIRECTION ( 'NONE',  ( -0.000000000000000000, 1.000000000000000000, -0.000000000000000000 ) ) ;
#45025=CARTESIAN_POINT ( 'NONE',  ( 2.679491924311222739, 83.95833333333332860, 10.00000000000000355 ) ) ;
#45027=CARTESIAN_POINT ( 'NONE',  ( 2.485281374238571317, 290.6875000000000000, -6.000000000000003553 ) ) ;
#45031=EDGE_CURVE ( 'NONE', #37922, #36060, #67150, .T. ) ;
#45034=DIRECTION ( 'NONE',  ( -0.000000000000000000, 1.000000000000000000, -0.000000000000000000 ) ) ;
#45038=CARTESIAN_POINT ( 'NONE',  ( 8.660254037844389075, 195.4166666666666856, -5.000000000000000000 ) ) ;
#45041=CARTESIAN_POINT ( 'NONE',  ( -8.311093377946836114, 172.9687499965860127, -8.311093377946837890 ) ) ;
#45047=CARTESIAN_POINT ( 'NONE',  ( 5.676582343749993598, 25.26041666325268764, 9.832129032723422313 ) ) ;
#45053=CARTESIAN_POINT ( 'NONE',  ( 7.320508075688771044, 61.24999999317203958, 7.320508075688775484 ) ) ;
#45059=ORIENTED_EDGE ( 'NONE', *, *, #47047, .F. ) ;
#45064=CARTESIAN_POINT ( 'NONE',  ( -11.35316468749999785, 143.0729166632526983, -3.042071309553167513 ) ) ;
#45065=VERTEX_POINT ( 'NONE', #37175 ) ;
#45076=CARTESIAN_POINT ( 'NONE',  ( -11.35316468750000141, 108.5937499965860269, -1.390361679473963753E-15 ) ) ;
#45080=CARTESIAN_POINT ( 'NONE',  ( 9.832129032723420536, 41.51041666325268409, -5.676582343749999815 ) ) ;
#45086=CARTESIAN_POINT ( 'NONE',  ( 1.102182119232618108E-15, 297.3125000034140157, 6.000000000000001776 ) ) ;
#45090=CARTESIAN_POINT ( 'NONE',  ( 5.676582343750001591, 156.9270833299193555, -9.832129032723420536 ) ) ;
#45107=CARTESIAN_POINT ( 'NONE',  ( -8.660254037844390851, 37.91666666666667140, 4.999999999999998224 ) ) ;
#45111=CARTESIAN_POINT ( 'NONE',  ( 7.320508075688857197, 80.62500000000005684, -7.320508075688857197 ) ) ;
#45113=VERTEX_POINT ( 'NONE', #20930 ) ;
#45121=CARTESIAN_POINT ( 'NONE',  ( -5.000000000000005329, 158.3333333333333428, 8.660254037844387298 ) ) ;
#45125=CARTESIAN_POINT ( 'NONE',  ( 9.832129032723420536, 131.5104166632526983, -5.676582343749999815 ) ) ;
#45132=CARTESIAN_POINT ( 'NONE',  ( 8.681524064790902884, 225.4138481035093662, -4.971750072494869777 ) ) ;
#45136=CARTESIAN_POINT ( 'NONE',  ( -8.311093377946836114, 202.9687499965860411, -8.311093377946837890 ) ) ;
#45143=CARTESIAN_POINT ( 'NONE',  ( -3.042071309553164404, 97.23958332991936970, -11.35316468749999963 ) ) ;
#45150=CARTESIAN_POINT ( 'NONE',  ( 6.951808397369818766E-16, 102.0312499965860269, -11.35316468750000141 ) ) ;
#45152=DIRECTION ( 'NONE',  ( -0.8660254037844389297, -0.4999999999999994449, 0.000000000000000000 ) ) ;
#45154=CARTESIAN_POINT ( 'NONE',  ( 10.00000000000000000, 221.6666666598387110, 2.679491924311236062 ) ) ;
#45158=CARTESIAN_POINT ( 'NONE',  ( -9.832129032723420536, 83.69791666325268409, 5.676582343749997150 ) ) ;
#45164=CARTESIAN_POINT ( 'NONE',  ( 10.00000000000000000, 176.6666666598387110, 2.679491924311236062 ) ) ;
#45168=CARTESIAN_POINT ( 'NONE',  ( 8.311093377946837890, 81.71874999658601268, -8.311093377946837890 ) ) ;
#45169=CARTESIAN_POINT ( 'NONE',  ( 6.676582343750004256, 290.8906250017069510, 2.765530957081995478 ) ) ;
#45172=CARTESIAN_POINT ( 'NONE',  ( 3.508320828368888034, 226.7807894534376203, -10.79750125662090632 ) ) ;
#45173=ORIENTED_EDGE ( 'NONE', *, *, #69841, .F. ) ;
#45176=CARTESIAN_POINT ( 'NONE',  ( 11.35316468749999963, 210.9895833299193839, -3.042071309553165293 ) ) ;
#45179=CARTESIAN_POINT ( 'NONE',  ( -6.676582343750003368, 297.3906250017068942, -2.765530957081996810 ) ) ;
#45181=CARTESIAN_POINT ( 'NONE',  ( -5.676582343749998039, 197.7604166632526983, -9.832129032723420536 ) ) ;
#45189=CARTESIAN_POINT ( 'NONE',  ( -4.999999999999998224, 11.66666666666666785, -8.660254037844389075 ) ) ;
#45210=CARTESIAN_POINT ( 'NONE',  ( 3.042071309553167069, 82.13541666325269830, -11.35316468749999785 ) ) ;
#45215=CARTESIAN_POINT ( 'NONE',  ( 4.721056650416000089, 289.9843750017070079, 4.721056650415999201 ) ) ;
#45216=CARTESIAN_POINT ( 'NONE',  ( 8.660254037844389075, 77.29166665983871098, -5.000000000000000000 ) ) ;
#45218=AXIS2_PLACEMENT_3D ( 'NONE', #65938, #30871, #48210 ) ;
#45219=CARTESIAN_POINT ( 'NONE',  ( -8.311093377946841443, 193.9062499965860411, 8.311093377946830785 ) ) ;
#45226=CARTESIAN_POINT ( 'NONE',  ( 11.35316468750000141, 171.0937499965860127, 0.000000000000000000 ) ) ;
#45230=CARTESIAN_POINT ( 'NONE',  ( -7.320508075688773708, 113.1249999999999858, 7.320508075688764826 ) ) ;
#45233=CARTESIAN_POINT ( 'NONE',  ( -3.042071309553173730, 54.32291666325269119, 11.35316468749999785 ) ) ;
#45239=CARTESIAN_POINT ( 'NONE',  ( 3.042071309553159519, 59.73958332991933418, 11.35316468750000141 ) ) ;
#45245=CARTESIAN_POINT ( 'NONE',  ( -11.35316468750000141, 43.28124999658601268, -1.390361679473963753E-15 ) ) ;
#45248=CARTESIAN_POINT ( 'NONE',  ( 9.832129032723420536, 176.1979166632526983, -5.676582343749999815 ) ) ;
#45249=CARTESIAN_POINT ( 'NONE',  ( -8.660254037844387298, 143.9583333265053682, -5.000000000000004441 ) ) ;
#45252=CARTESIAN_POINT ( 'NONE',  ( -5.676582343750006032, 34.42708332991935549, 9.832129032723418760 ) ) ;
#45254=CARTESIAN_POINT ( 'NONE',  ( -3.042071309553164404, 182.2395833299193555, -11.35316468749999963 ) ) ;
#45261=CARTESIAN_POINT ( 'NONE',  ( 8.311093377946837890, 161.4062499965860695, -8.311093377946837890 ) ) ;
#45271=CARTESIAN_POINT ( 'NONE',  ( 5.676582343750001591, 111.9270833299193555, -9.832129032723420536 ) ) ;
#45299=CARTESIAN_POINT ( 'NONE',  ( 10.00000000000000178, 115.2083333333333144, -2.679491924311226736 ) ) ;
#45301=CARTESIAN_POINT ( 'NONE',  ( 2.765530957081996366, 289.2968750017070079, -6.676582343750003368 ) ) ;
#45312=CARTESIAN_POINT ( 'NONE',  ( -8.660254037844390851, 214.7916666598387110, 4.999999999999998224 ) ) ;
#45314=CARTESIAN_POINT ( 'NONE',  ( -11.35316468750000141, 18.48958332991934483, 3.042071309553159963 ) ) ;
#45316=CARTESIAN_POINT ( 'NONE',  ( 3.042071309553167069, 202.1354166632526983, -11.35316468749999785 ) ) ;
#45317=CARTESIAN_POINT ( 'NONE',  ( 8.311093377946837890, 1.406249996586016238, -8.311093377946837890 ) ) ;
#45318=CARTESIAN_POINT ( 'NONE',  ( -8.660254037844387298, 218.9583333265053966, -5.000000000000004441 ) ) ;
#45319=CARTESIAN_POINT ( 'NONE',  ( 0.000000000000000000, 300.0000000000000000, 0.000000000000000000 ) ) ;
#45321=ADVANCED_FACE ( 'NONE', ( #22408 ), #68443, .T. ) ;
#45323=CARTESIAN_POINT ( 'NONE',  ( 8.311093377946837890, 26.40624999658601268, -8.311093377946837890 ) ) ;
#45326=CARTESIAN_POINT ( 'NONE',  ( 10.00000000000000178, 210.2083333333333428, -2.679491924311227180 ) ) ;
#45330=CARTESIAN_POINT ( 'NONE',  ( -11.35316468750000141, 3.489583329919349719, 3.042071309553159963 ) ) ;
#45332=CARTESIAN_POINT ( 'NONE',  ( -3.042071309553173730, 129.3229166632526983, 11.35316468749999785 ) ) ;
#45333=CARTESIAN_POINT ( 'NONE',  ( 5.000000000000001776, 107.7083333265053682, -8.660254037844389075 ) ) ;
#45335=FACE_OUTER_BOUND ( 'NONE', #13845, .T. ) ;
#45341=CARTESIAN_POINT ( 'NONE',  ( 6.676582343750003368, 288.1718750017069510, -2.765530957081997254 ) ) ;
#45351=CARTESIAN_POINT ( 'NONE',  ( 8.660254037844389075, 217.2916666598387110, -5.000000000000000000 ) ) ;
#45354=CARTESIAN_POINT ( 'NONE',  ( -3.042071309553173730, 69.63541666325268409, 11.35316468749999785 ) ) ;
#45358=ORIENTED_EDGE ( 'NONE', *, *, #42649, .F. ) ;
#45367=ORIENTED_EDGE ( 'NONE', *, *, #74316, .T. ) ;
#45383=CARTESIAN_POINT ( 'NONE',  ( -10.00000000000000000, 87.29166666666667140, -2.679491924311229845 ) ) ;
#45385=CARTESIAN_POINT ( 'NONE',  ( -6.000000000000001776, 289.0000000000000000, 0.000000000000000000 ) ) ;
#45391=DIRECTION ( 'NONE',  ( 0.000000000000000000, 0.000000000000000000, 1.000000000000000000 ) ) ;
#45394=CARTESIAN_POINT ( 'NONE',  ( -2.679491924311225848, 196.4583333333333428, -10.00000000000000178 ) ) ;
#45396=CARTESIAN_POINT ( 'NONE',  ( 3.042071309553159519, 165.0520833299193839, 11.35316468750000141 ) ) ;
#45397=CARTESIAN_POINT ( 'NONE',  ( -1.173938163346586453E-11, 213.7499999999991189, 10.00000000000000178 ) ) ;
#45399=DIRECTION ( 'NONE',  ( 0.000000000000000000, 0.000000000000000000, 1.000000000000000000 ) ) ;
#45403=CARTESIAN_POINT ( 'NONE',  ( 6.951808397369818766E-16, 27.34374999658601979, -11.35316468750000141 ) ) ;
#45410=CARTESIAN_POINT ( 'NONE',  ( -7.320508075688778149, 64.99999999317203958, 7.320508075688769267 ) ) ;
#45420=CARTESIAN_POINT ( 'NONE',  ( -8.660254037844481445, 197.9166666666667425, 5.000000000000052403 ) ) ;
#45424=CARTESIAN_POINT ( 'NONE',  ( -5.676582343750006032, 139.1145833299193555, 9.832129032723418760 ) ) ;
#45432=CARTESIAN_POINT ( 'NONE',  ( 1.224646799147353454E-15, 300.0000000000000000, -10.00000000000000178 ) ) ;
#45438=CARTESIAN_POINT ( 'NONE',  ( -5.676582343749998039, 127.7604166632526841, -9.832129032723420536 ) ) ;
#45442=CARTESIAN_POINT ( 'NONE',  ( -3.042071309553173730, 39.63541666325267698, 11.35316468749999785 ) ) ;
#45448=CARTESIAN_POINT ( 'NONE',  ( 1.102182119232618108E-15, 296.3125000034140157, 6.000000000000001776 ) ) ;
#45451=CARTESIAN_POINT ( 'NONE',  ( 11.35316468749999963, 156.3020833299192986, -3.042071309553165293 ) ) ;
#45455=EDGE_CURVE ( 'NONE', #48752, #12154, #42661, .T. ) ;
#45462=CARTESIAN_POINT ( 'NONE',  ( -2.679491924317145113, 58.54166666666618823, 9.999999999996678213 ) ) ;
#45469=CARTESIAN_POINT ( 'NONE',  ( -5.000000000000005329, 43.33333333333333570, 8.660254037844387298 ) ) ;
#45472=CARTESIAN_POINT ( 'NONE',  ( -6.000000000000001776, 300.0000000000000000, 0.000000000000000000 ) ) ;
#45474=CARTESIAN_POINT ( 'NONE',  ( 4.999999999999993783, 196.0416666598387110, 8.660254037844390851 ) ) ;
#45480=CARTESIAN_POINT ( 'NONE',  ( -8.660254037844387298, 147.0833333333333428, -5.000000000000004441 ) ) ;
#45482=CARTESIAN_POINT ( 'NONE',  ( -1.836970198721029983E-15, 163.7500000000000000, 10.00000000000000178 ) ) ;
#45486=CARTESIAN_POINT ( 'NONE',  ( 6.951808397369818766E-16, 127.3437499965860127, -11.35316468750000141 ) ) ;
#45493=CARTESIAN_POINT ( 'NONE',  ( 4.545654900257371622, 224.1260959769811905, 8.912008146339848835 ) ) ;
#45499=CARTESIAN_POINT ( 'NONE',  ( 9.832129032723420536, 211.5104166632526699, -5.676582343749999815 ) ) ;
#45506=CARTESIAN_POINT ( 'NONE',  ( 9.832129032723420536, 91.19791666325269830, -5.676582343749999815 ) ) ;
#45507=VERTEX_POINT ( 'NONE', #55851 ) ;
#45514=CARTESIAN_POINT ( 'NONE',  ( 8.311093377946834337, 105.1562499965860269, 8.311093377946839666 ) ) ;
#45518=CARTESIAN_POINT ( 'NONE',  ( -5.000000000000005329, 220.2083333265053966, 8.660254037844387298 ) ) ;
#45522=CARTESIAN_POINT ( 'NONE',  ( 11.35316468749999785, 105.5729166632526983, 3.042071309553174174 ) ) ;
#45525=CARTESIAN_POINT ( 'NONE',  ( 10.00000000000000178, 170.0000000000000000, 0.000000000000000000 ) ) ;
#45527=CARTESIAN_POINT ( 'NONE',  ( -8.660254037844390851, 179.7916666598387110, 4.999999999999998224 ) ) ;
#45530=CARTESIAN_POINT ( 'NONE',  ( 9.832129032723420536, 86.51041666325268409, -5.676582343749999815 ) ) ;
#45531=CARTESIAN_POINT ( 'NONE',  ( 6.676582343750001591, 287.9531250017069510, -8.176455196517173205E-16 ) ) ;
#45535=CARTESIAN_POINT ( 'NONE',  ( -3.042071309553164404, 2.552083329919349275, -11.35316468749999963 ) ) ;
#45540=CARTESIAN_POINT ( 'NONE',  ( 9.832129032723416984, 225.3645833299193839, 5.676582343750006032 ) ) ;
#45542=CARTESIAN_POINT ( 'NONE',  ( 6.676582343750004256, 296.8906250017068942, 2.765530957081995478 ) ) ;
#45545=CARTESIAN_POINT ( 'NONE',  ( 11.35316468749999963, 191.3020833299193839, -3.042071309553165293 ) ) ;
#45546=( BOUNDED_CURVE ( )  B_SPLINE_CURVE ( 2, ( #30131, #52407, #52772, #1481, #45993, #68634, #23725, #40336, #23352, #1110, #11297, #69009, #17690 ),
 .UNSPECIFIED., .F., .F. ) 
 B_SPLINE_CURVE_WITH_KNOTS ( ( 3, 2, 2, 2, 2, 2, 3 ),
 ( 0.2228260869565217295, 0.2246376811594202882, 0.2264492753623188470, 0.2282608695652174058, 0.2300724637681159646, 0.2318840579710145233, 0.2336956521739130821 ),
 .UNSPECIFIED. ) 
 CURVE ( )  GEOMETRIC_REPRESENTATION_ITEM ( )  RATIONAL_B_SPLINE_CURVE ( ( 1.000000000000000000, 0.9659258262890683122, 1.000000000000000000, 0.9659258262890683122, 1.000000000000000000, 0.9659258262890683122, 1.000000000000000000, 0.9659258262890683122, 1.000000000000000000, 0.9659258262890683122, 1.000000000000000000, 0.9659258262890677571, 1.000000000000000444 ) ) 
 REPRESENTATION_ITEM ( '' )  );
#45551=ORIENTED_EDGE ( 'NONE', *, *, #55671, .F. ) ;
#45556=CARTESIAN_POINT ( 'NONE',  ( 2.679491924311228956, 21.04166666666666075, -10.00000000000000000 ) ) ;
#45559=CYLINDRICAL_SURFACE ( 'NONE', #7852, 10.00000000000000178 ) ;
#45565=CARTESIAN_POINT ( 'NONE',  ( -1.836970198721029983E-15, 15.62499999317203248, 10.00000000000000178 ) ) ;
#45572=ORIENTED_EDGE ( 'NONE', *, *, #45455, .T. ) ;
#45579=CARTESIAN_POINT ( 'NONE',  ( 6.951808397369818766E-16, 87.34374999658602690, -11.35316468750000141 ) ) ;
#45580=FACE_OUTER_BOUND ( 'NONE', #58193, .T. ) ;
#45585=CYLINDRICAL_SURFACE ( 'NONE', #14252, 6.000000000000001776 ) ;
#45587=CARTESIAN_POINT ( 'NONE',  ( -3.042071309553164404, 202.2395833299193271, -11.35316468749999963 ) ) ;
#45589=ORIENTED_EDGE ( 'NONE', *, *, #41437, .F. ) ;
#45593=CARTESIAN_POINT ( 'NONE',  ( -5.676582343749998039, 172.7604166632526983, -9.832129032723420536 ) ) ;
#45597=CARTESIAN_POINT ( 'NONE',  ( -2.679491924311235174, 90.41666665983871098, 10.00000000000000000 ) ) ;
#45600=CARTESIAN_POINT ( 'NONE',  ( -8.311093377946836114, 52.65624999658601979, -8.311093377946837890 ) ) ;
#45604=ORIENTED_EDGE ( 'NONE', *, *, #33369, .T. ) ;
#45606=CARTESIAN_POINT ( 'NONE',  ( -8.311093377946836114, 67.65624999658599847, -8.311093377946837890 ) ) ;
#45607=VECTOR ( 'NONE', #7092, 1000.000000000000000 ) ;
#45611=CARTESIAN_POINT ( 'NONE',  ( -8.660254037844387298, 12.08333333333333570, -5.000000000000004441 ) ) ;
#45613=CARTESIAN_POINT ( 'NONE',  ( 11.35316468750000141, 55.78124999658601268, 0.000000000000000000 ) ) ;
#45616=CARTESIAN_POINT ( 'NONE',  ( 8.311093377946837890, 171.4062499965860127, -8.311093377946837890 ) ) ;
#45617=VECTOR ( 'NONE', #38916, 1000.000000000000000 ) ;
#45618=CARTESIAN_POINT ( 'NONE',  ( -4.999999999999998224, 143.5416666598386826, -8.660254037844389075 ) ) ;
#45621=CARTESIAN_POINT ( 'NONE',  ( -11.35316468750000141, 48.80208332991934839, 3.042071309553159963 ) ) ;
#45623=CARTESIAN_POINT ( 'NONE',  ( -9.832129032723418760, 177.8645833299193555, -5.676582343750004256 ) ) ;
#45630=CARTESIAN_POINT ( 'NONE',  ( -5.676582343749998039, 167.4479166632526983, -9.832129032723420536 ) ) ;
#45634=DIRECTION ( 'NONE',  ( -0.000000000000000000, 1.000000000000000000, -0.000000000000000000 ) ) ;
#45637=CARTESIAN_POINT ( 'NONE',  ( 8.311093377946837890, 121.7187499965860411, -8.311093377946837890 ) ) ;
#45650=VECTOR ( 'NONE', #66321, 1000.000000000000000 ) ;
#45659=ORIENTED_EDGE ( 'NONE', *, *, #25040, .F. ) ;
#45666=DIRECTION ( 'NONE',  ( 0.000000000000000000, 0.000000000000000000, 1.000000000000000000 ) ) ;
#45668=CARTESIAN_POINT ( 'NONE',  ( -4.999999999999998224, 121.6666666666666714, -8.660254037844389075 ) ) ;
#45683=CARTESIAN_POINT ( 'NONE',  ( -2.085542519210945728E-15, 14.53124999658601624, 11.35316468750000141 ) ) ;
#45684=CYLINDRICAL_SURFACE ( 'NONE', #11047, 10.00000000000000178 ) ;
#45685=CARTESIAN_POINT ( 'NONE',  ( 9.832129032723416984, 205.6770833299193555, 5.676582343750006032 ) ) ;
#45690=ORIENTED_EDGE ( 'NONE', *, *, #36215, .F. ) ;
#45692=CARTESIAN_POINT ( 'NONE',  ( 3.042071309553167069, 16.82291666325268054, -11.35316468749999785 ) ) ;
#45694=CARTESIAN_POINT ( 'NONE',  ( 10.00000000000000355, 210.0000000000000284, 0.000000000000000000 ) ) ;
#45699=CARTESIAN_POINT ( 'NONE',  ( 6.951808397369818766E-16, 2.031249996586016238, -11.35316468750000141 ) ) ;
#45701=CARTESIAN_POINT ( 'NONE',  ( -11.35316468749999785, 138.0729166632526699, -3.042071309553167513 ) ) ;
#45703=CARTESIAN_POINT ( 'NONE',  ( 10.00000000000000178, 102.0833333265053682, -2.679491924311226736 ) ) ;
#45705=CARTESIAN_POINT ( 'NONE',  ( 6.123233995736767268E-16, 3.124999993172032919, -10.00000000000000178 ) ) ;
#45707=DIRECTION ( 'NONE',  ( -0.000000000000000000, 1.000000000000000000, -0.000000000000000000 ) ) ;
#45710=CARTESIAN_POINT ( 'NONE',  ( 0.000000000000000000, 300.0000000000000000, 0.000000000000000000 ) ) ;
#45711=CARTESIAN_POINT ( 'NONE',  ( 2.765530957082001251, 295.7656250017069510, 6.676582343750000703 ) ) ;
#45712=CARTESIAN_POINT ( 'NONE',  ( 5.676582343749993598, 129.9479166632526983, 9.832129032723422313 ) ) ;
#45719=ORIENTED_EDGE ( 'NONE', *, *, #67296, .T. ) ;
#45723=CARTESIAN_POINT ( 'NONE',  ( 11.35316468750000141, 71.09374999658601268, 0.000000000000000000 ) ) ;
#45729=CARTESIAN_POINT ( 'NONE',  ( -1.836970198721029983E-15, 20.62499999317203603, 10.00000000000000178 ) ) ;
#45744=( BOUNDED_CURVE ( )  B_SPLINE_CURVE ( 2, ( #54027, #37041, #14002, #47604, #64234, #64608, #18582, #7996, #47977, #60041, #2336, #58585, #24962 ),
 .UNSPECIFIED., .F., .F. ) 
 B_SPLINE_CURVE_WITH_KNOTS ( ( 3, 2, 2, 2, 2, 2, 3 ),
 ( 0.6141304347826087584, 0.6159420289855073172, 0.6177536231884058759, 0.6195652173913044347, 0.6213768115942029935, 0.6231884057971015523, 0.6250000000000001110 ),
 .UNSPECIFIED. ) 
 CURVE ( )  GEOMETRIC_REPRESENTATION_ITEM ( )  RATIONAL_B_SPLINE_CURVE ( ( 0.9999999999999978906, 0.9659258262890704216, 1.000000000000000000, 0.9659258262890683122, 1.000000000000000000, 0.9659258262890683122, 1.000000000000000000, 0.9659258262890683122, 1.000000000000000000, 0.9659258262890683122, 1.000000000000000000, 0.9659258262890662028, 1.000000000000001998 ) ) 
 REPRESENTATION_ITEM ( '' )  );
#45757=CARTESIAN_POINT ( 'NONE',  ( -10.00000000000000355, 82.70833333333332860, 2.679491924311223183 ) ) ;
#45761=CARTESIAN_POINT ( 'NONE',  ( -3.673940397442060854E-16, 288.7500000000000000, -6.000000000000001776 ) ) ;
#45772=CARTESIAN_POINT ( 'NONE',  ( 2.679491924311222739, 203.9583333333333428, 10.00000000000000355 ) ) ;
#45774=CARTESIAN_POINT ( 'NONE',  ( -11.35316468749999785, 173.3854166632526983, -3.042071309553167513 ) ) ;
#45778=CARTESIAN_POINT ( 'NONE',  ( 2.679491924311222739, 85.83333332650538239, 10.00000000000000355 ) ) ;
#45781=CARTESIAN_POINT ( 'NONE',  ( 9.832129032723420536, 36.51041666325267698, -5.676582343749999815 ) ) ;
#45790=CARTESIAN_POINT ( 'NONE',  ( 10.00000000000000178, 56.87499999317203248, 0.000000000000000000 ) ) ;
#45795=CARTESIAN_POINT ( 'NONE',  ( 2.679491924311149464, 100.8333333265053682, 10.00000000000004619 ) ) ;
#45801=CARTESIAN_POINT ( 'NONE',  ( -5.676582343749998039, 142.4479166632526699, -9.832129032723420536 ) ) ;
#45809=AXIS2_PLACEMENT_3D ( 'NONE', #16690, #21993, #12802 ) ;
#45812=CARTESIAN_POINT ( 'NONE',  ( 5.676582343749993598, 125.2604166632526841, 9.832129032723422313 ) ) ;
#45816=CARTESIAN_POINT ( 'NONE',  ( -11.35316468750000141, 33.59374999658601268, -1.390361679473963753E-15 ) ) ;
#45825=CARTESIAN_POINT ( 'NONE',  ( -6.000000000000000888, 295.1250000034140157, 2.485281374238575758 ) ) ;
#45828=CARTESIAN_POINT ( 'NONE',  ( -3.042071309553173730, 154.6354166632526699, 11.35316468749999785 ) ) ;
#45844=CARTESIAN_POINT ( 'NONE',  ( 4.999999999999993783, 39.16666666666667140, 8.660254037844390851 ) ) ;
#45856=CARTESIAN_POINT ( 'NONE',  ( -8.660254037844387298, 138.9583333265053682, -5.000000000000004441 ) ) ;
#45858=CARTESIAN_POINT ( 'NONE',  ( 2.679491924311222739, 158.9583333333333144, 10.00000000000000355 ) ) ;
#45863=CARTESIAN_POINT ( 'NONE',  ( -3.042071309553173730, 134.6354166632526983, 11.35316468749999785 ) ) ;
#45870=AXIS2_PLACEMENT_3D ( 'NONE', #11965, #7049, #34996 ) ;
#45877=CARTESIAN_POINT ( 'NONE',  ( 8.311093377946834337, 225.4687499965860411, 8.311093377946839666 ) ) ;
#45883=CARTESIAN_POINT ( 'NONE',  ( -5.676582343750006032, 104.1145833299193697, 9.832129032723418760 ) ) ;
#45884=ORIENTED_EDGE ( 'NONE', *, *, #33802, .T. ) ;
#45890=CARTESIAN_POINT ( 'NONE',  ( 3.042071309553167069, 96.82291666325269830, -11.35316468749999785 ) ) ;
#45894=CARTESIAN_POINT ( 'NONE',  ( 7.320508075688771044, 226.2499999931720254, 7.320508075688775484 ) ) ;
#45898=CARTESIAN_POINT ( 'NONE',  ( -8.311093377946841443, 98.90624999658602690, 8.311093377946834337 ) ) ;
#45901=CARTESIAN_POINT ( 'NONE',  ( 10.00000000000000000, 169.7916666666666856, 2.679491924311235618 ) ) ;
#45903=CARTESIAN_POINT ( 'NONE',  ( 10.00000000000000178, 202.0833333265053966, -2.679491924311226736 ) ) ;
#45907=CARTESIAN_POINT ( 'NONE',  ( -5.676582343749998039, 92.76041666325268409, -9.832129032723420536 ) ) ;
#45908=CARTESIAN_POINT ( 'NONE',  ( -4.721056650415999201, 290.3281250017069510, -4.721056650415999201 ) ) ;
#45911=CARTESIAN_POINT ( 'NONE',  ( -11.35316468750000141, 223.2812499965860127, -1.390361679473963753E-15 ) ) ;
#45915=CYLINDRICAL_SURFACE ( 'NONE', #27507, 10.00000000000000178 ) ;
#45916=CARTESIAN_POINT ( 'NONE',  ( 8.311093377946834337, 215.1562499965860127, 8.311093377946839666 ) ) ;
#45919=CARTESIAN_POINT ( 'NONE',  ( 1.226468279477575784E-15, 295.7031250017069510, 6.676582343750001591 ) ) ;
#45921=CARTESIAN_POINT ( 'NONE',  ( -3.673940397442060854E-16, 295.8125000034140157, -6.000000000000001776 ) ) ;
#45922=CARTESIAN_POINT ( 'NONE',  ( 6.951808397369818766E-16, 202.3437499965860127, -11.35316468750000141 ) ) ;
#45928=CIRCLE ( 'NONE', #64030, 6.000000000000001776 ) ;
#45932=CARTESIAN_POINT ( 'NONE',  ( -10.00000000000000000, 32.29166666666667140, -2.679491924311229845 ) ) ;
#45942=CARTESIAN_POINT ( 'NONE',  ( 4.999999999999993783, 151.0416666598387110, 8.660254037844390851 ) ) ;
#45943=CARTESIAN_POINT ( 'NONE',  ( 6.676582343750003368, 294.8906250017069510, 2.765530957081995478 ) ) ;
#45952=CARTESIAN_POINT ( 'NONE',  ( -11.35316468750000141, 83.80208332991934128, 3.042071309553159963 ) ) ;
#45963=CARTESIAN_POINT ( 'NONE',  ( 3.042071309553159519, 199.7395833299193555, 11.35316468750000141 ) ) ;
#45968=CARTESIAN_POINT ( 'NONE',  ( -11.35316468750000141, 183.8020833299193271, 3.042071309553159963 ) ) ;
#45975=CARTESIAN_POINT ( 'NONE',  ( -11.35316468750000141, 58.48958332991934128, 3.042071309553159963 ) ) ;
#45981=CARTESIAN_POINT ( 'NONE',  ( 8.311093377946834337, 65.15624999658602690, 8.311093377946839666 ) ) ;
#45986=CARTESIAN_POINT ( 'NONE',  ( 9.832129032723416984, 60.36458332991934839, 5.676582343750006032 ) ) ;
#45989=CARTESIAN_POINT ( 'NONE',  ( 11.35316468749999963, 175.9895833299193555, -3.042071309553165293 ) ) ;
#45991=CARTESIAN_POINT ( 'NONE',  ( 8.660254037844389075, 157.2916666598387110, -5.000000000000000000 ) ) ;
#45993=CARTESIAN_POINT ( 'NONE',  ( -8.660254037844387298, 53.95833332650536818, -5.000000000000004441 ) ) ;
#45994=CARTESIAN_POINT ( 'NONE',  ( -9.832129032723420536, 49.01041666325269119, 5.676582343749997150 ) ) ;
#45996=CARTESIAN_POINT ( 'NONE',  ( -9.832129032723418760, 187.8645833299193839, -5.676582343750004256 ) ) ;
#46002=CARTESIAN_POINT ( 'NONE',  ( -8.311093377946841443, 183.9062499965860411, 8.311093377946834337 ) ) ;
#46010=CARTESIAN_POINT ( 'NONE',  ( -5.676582343750006032, 129.4270833299193555, 9.832129032723418760 ) ) ;
#46024=ORIENTED_EDGE ( 'NONE', *, *, #19272, .F. ) ;
#46030=ORIENTED_EDGE ( 'NONE', *, *, #20580, .F. ) ;
#46034=ORIENTED_EDGE ( 'NONE', *, *, #70768, .T. ) ;
#46041=CARTESIAN_POINT ( 'NONE',  ( -6.676582343749999815, 297.6718750017070079, 2.765530957082001251 ) ) ;
#46042=CARTESIAN_POINT ( 'NONE',  ( 7.320508075688774596, 125.6250000000000142, -7.320508075688774596 ) ) ;
#46044=CARTESIAN_POINT ( 'NONE',  ( -4.721056650415998313, 287.7343750017069510, 4.721056650416000089 ) ) ;
#46056=CARTESIAN_POINT ( 'NONE',  ( 10.00000000000000178, 51.87499999317203248, 0.000000000000000000 ) ) ;
#46058=CARTESIAN_POINT ( 'NONE',  ( -5.676582343749998039, 12.44791666325268409, -9.832129032723420536 ) ) ;
#46060=CARTESIAN_POINT ( 'NONE',  ( 11.35316468749999963, 221.3020833299192986, -3.042071309553165293 ) ) ;
#46065=CARTESIAN_POINT ( 'NONE',  ( 9.832129032723420536, 16.19791666325268054, -5.676582343749999815 ) ) ;
#46071=CARTESIAN_POINT ( 'NONE',  ( 3.042071309553167513, 21.82291666325268054, -11.35316468749999785 ) ) ;
#46074=CARTESIAN_POINT ( 'NONE',  ( -5.676582343749998039, 132.4479166632526983, -9.832129032723420536 ) ) ;
#46075=CARTESIAN_POINT ( 'NONE',  ( 7.320508075688771044, 106.2499999931720396, 7.320508075688775484 ) ) ;
#46081=CARTESIAN_POINT ( 'NONE',  ( -3.042071309553163960, 12.55208332991935016, -11.35316468749999963 ) ) ;
#46084=CARTESIAN_POINT ( 'NONE',  ( -6.676582343750003368, 296.3906250017069510, -2.765530957081996810 ) ) ;
#46085=CARTESIAN_POINT ( 'NONE',  ( -2.085542519210945728E-15, 134.5312499965860411, 11.35316468750000141 ) ) ;
#46096=CARTESIAN_POINT ( 'NONE',  ( -3.042071309553173730, 94.63541666325269830, 11.35316468749999785 ) ) ;
#46102=EDGE_LOOP ( 'NONE', ( #56036, #65603, #2584, #42853 ) ) ;
#46104=CARTESIAN_POINT ( 'NONE',  ( -1.836970198721029983E-15, 110.6249999931720396, 10.00000000000000178 ) ) ;
#46109=VECTOR ( 'NONE', #9442, 1000.000000000000000 ) ;
#46110=CARTESIAN_POINT ( 'NONE',  ( 1.567784982238203817E-13, 108.7500000000000426, 10.00000000000000533 ) ) ;
#46122=VERTEX_POINT ( 'NONE', #21409 ) ;
#46129=CARTESIAN_POINT ( 'NONE',  ( 8.660254037844385522, 84.58333333333334281, 5.000000000000005329 ) ) ;
#46131=CARTESIAN_POINT ( 'NONE',  ( 3.042071309553159519, 65.05208332991932707, 11.35316468750000141 ) ) ;
#46132=CARTESIAN_POINT ( 'NONE',  ( 6.000000000000003553, 289.4375000000000000, 2.485281374238571317 ) ) ;
#46134=B_SPLINE_CURVE_WITH_KNOTS ( 'NONE', 3,
 ( #42887, #20628, #32722, #60625, #61374, #48549, #55356, #71559, #2916, #54236, #31588, #60246, #44396, #27039, #4047, #38369, #37627, #3661 ),
 .UNSPECIFIED., .F., .F.,
 ( 4, 2, 2, 2, 2, 2, 2, 2, 4 ),
 ( 0.000000000000000000, 0.001314736723651638338, 0.002629473447303276677, 0.003944210170954915232, 0.005258946894606553353, 0.006573683618258192342, 0.007888420341909830463, 0.009203157065561471187, 0.01051789378921311191 ),
 .UNSPECIFIED. ) ;
#46138=LINE ( 'NONE', #11076, #52712 ) ;
#46143=CARTESIAN_POINT ( 'NONE',  ( 8.660254037844385522, 204.5833333333333428, 5.000000000000005329 ) ) ;
#46145=CARTESIAN_POINT ( 'NONE',  ( -9.832129032723418760, 163.1770833299193839, -5.676582343750004256 ) ) ;
#46147=CARTESIAN_POINT ( 'NONE',  ( 8.660254037844385522, 176.4583333265053682, 5.000000000000005329 ) ) ;
#46152=CARTESIAN_POINT ( 'NONE',  ( 9.832129032723416984, 40.67708332991935549, 5.676582343750006032 ) ) ;
#46161=CARTESIAN_POINT ( 'NONE',  ( -8.660254037844387298, 68.95833332650536818, -5.000000000000004441 ) ) ;
#46168=CARTESIAN_POINT ( 'NONE',  ( -10.00000000000011191, 197.7083333333334281, 2.679491924311252049 ) ) ;
#46169=CARTESIAN_POINT ( 'NONE',  ( 6.676582343750003368, 299.1718750017069510, -2.765530957081997254 ) ) ;
#46170=CARTESIAN_POINT ( 'NONE',  ( -10.00000000000001243, 162.2916666666666856, -2.679491924311233841 ) ) ;
#46171=LINE ( 'NONE', #41263, #61791 ) ;
#46172=AXIS2_PLACEMENT_3D ( 'NONE', #30330, #52976, #36364 ) ;
#46173=CARTESIAN_POINT ( 'NONE',  ( -9.832129032723418760, 152.8645833299193555, -5.676582343750004256 ) ) ;
#46183=CARTESIAN_POINT ( 'NONE',  ( -3.042071309553173730, 134.6354166632526699, 11.35316468749999785 ) ) ;
#46187=CARTESIAN_POINT ( 'NONE',  ( -3.042071309553164404, 32.55208332991934128, -11.35316468749999963 ) ) ;
#46196=CARTESIAN_POINT ( 'NONE',  ( -6.000000000000003553, 295.0000000034140157, -2.485281374238571317 ) ) ;
#46200=( BOUNDED_CURVE ( )  B_SPLINE_CURVE ( 2, ( #10703, #56739, #51063, #51811, #40493, #57863, #34110, #6169, #73704, #57108, #22016, #74076, #45397 ),
 .UNSPECIFIED., .F., .F. ) 
 B_SPLINE_CURVE_WITH_KNOTS ( ( 3, 2, 2, 2, 2, 2, 3 ),
 ( 2.653284597091381869, 2.658518511020140807, 2.663752424948899744, 2.668986338877658682, 2.674220252806417619, 2.679454166735176557, 2.684688080663935494 ),
 .UNSPECIFIED. ) 
 CURVE ( )  GEOMETRIC_REPRESENTATION_ITEM ( )  RATIONAL_B_SPLINE_CURVE ( ( 0.9999999999999978906, 0.9659258262890704216, 1.000000000000000000, 0.9659258262890683122, 1.000000000000000000, 0.9659258262890683122, 1.000000000000000000, 0.9659258262890683122, 1.000000000000000000, 0.9659258262890683122, 1.000000000000000000, 0.9659258262891455837, 0.9999999999999227285 ) ) 
 REPRESENTATION_ITEM ( '' )  );
#46202=CARTESIAN_POINT ( 'NONE',  ( -2.085542519210945728E-15, 149.8437499965860411, 11.35316468750000141 ) ) ;
#46213=CARTESIAN_POINT ( 'NONE',  ( -5.000000000000045297, 58.33333333333338544, 8.660254037844454800 ) ) ;
#46215=VERTEX_POINT ( 'NONE', #8089 ) ;
#46218=CARTESIAN_POINT ( 'NONE',  ( -5.999999999999999112, 298.1250000034140157, 2.485281374238575314 ) ) ;
#46219=CARTESIAN_POINT ( 'NONE',  ( -2.679491924311272477, 45.41666665983869677, 9.999999999999978684 ) ) ;
#46220=CARTESIAN_POINT ( 'NONE',  ( 4.999999999999993783, 44.16666666666666430, 8.660254037844390851 ) ) ;
#46224=FACE_OUTER_BOUND ( 'NONE', #52269, .T. ) ;
#46231=CARTESIAN_POINT ( 'NONE',  ( -9.999999999999998224, 147.2916666666666572, -2.679491924311230289 ) ) ;
#46232=CARTESIAN_POINT ( 'NONE',  ( 4.999999999999993783, 201.0416666598387110, 8.660254037844390851 ) ) ;
#46233=CARTESIAN_POINT ( 'NONE',  ( 8.660254037844389075, 155.4166666666666856, -5.000000000000000000 ) ) ;
#46236=CARTESIAN_POINT ( 'NONE',  ( 3.042071309553167069, 132.1354166632526699, -11.35316468749999785 ) ) ;
#46242=VERTEX_POINT ( 'NONE', #60138 ) ;
#46243=CARTESIAN_POINT ( 'NONE',  ( 8.311093377946837890, 1.718749996586016682, -8.311093377946837890 ) ) ;
#46246=CARTESIAN_POINT ( 'NONE',  ( 8.660254037844385522, 26.45833332650536818, 5.000000000000005329 ) ) ;
#46254=CARTESIAN_POINT ( 'NONE',  ( -9.832129032723418760, 112.8645833299193555, -5.676582343750004256 ) ) ;
#46260=CARTESIAN_POINT ( 'NONE',  ( 8.311093377946837890, 96.40624999658602690, -8.311093377946837890 ) ) ;
#46265=CARTESIAN_POINT ( 'NONE',  ( 6.123233995736767268E-16, 223.1249999931720254, -10.00000000000000178 ) ) ;
#46267=LINE ( 'NONE', #35344, #2230 ) ;
#46269=CARTESIAN_POINT ( 'NONE',  ( 9.832129032723420536, 96.19791666325269830, -5.676582343749999815 ) ) ;
#46273=ORIENTED_EDGE ( 'NONE', *, *, #30429, .F. ) ;
#46274=CARTESIAN_POINT ( 'NONE',  ( 10.00000000000000178, 197.0833333265053398, -2.679491924311226736 ) ) ;
#46277=CARTESIAN_POINT ( 'NONE',  ( 6.951808397369818766E-16, 92.34374999658602690, -11.35316468750000141 ) ) ;
#46278=CARTESIAN_POINT ( 'NONE',  ( 6.676582343750001591, 289.9531250017069510, -8.176455196517173205E-16 ) ) ;
#46281=CARTESIAN_POINT ( 'NONE',  ( 4.643183940729320724, 226.6963029853575335, -10.42876187888753847 ) ) ;
#46284=CARTESIAN_POINT ( 'NONE',  ( -11.35316468750000141, 218.4895833299193271, 3.042071309553159963 ) ) ;
#46288=DIRECTION ( 'NONE',  ( -0.000000000000000000, 1.000000000000000000, -0.000000000000000000 ) ) ;
#46289=CARTESIAN_POINT ( 'NONE',  ( 2.765530957082001251, 297.7656250017069510, 6.676582343750000703 ) ) ;
#46292=CARTESIAN_POINT ( 'NONE',  ( -3.042071309553173730, 204.6354166632526699, 11.35316468749999785 ) ) ;
#46300=CARTESIAN_POINT ( 'NONE',  ( 7.320508075688771044, 34.37500000000000711, 7.320508075688775484 ) ) ;
#46315=CARTESIAN_POINT ( 'NONE',  ( -4.721056650415998313, 297.5781250017069510, 4.721056650416000089 ) ) ;
#46325=CARTESIAN_POINT ( 'NONE',  ( -11.35316468750000141, 88.59374999658602690, -1.390361679473963753E-15 ) ) ;
#46330=CARTESIAN_POINT ( 'NONE',  ( 6.676582343750003368, 288.0468750017070079, 2.765530957081995478 ) ) ;
#46334=CARTESIAN_POINT ( 'NONE',  ( -8.311093377946841443, 203.9062499965859843, 8.311093377946830785 ) ) ;
#46338=CARTESIAN_POINT ( 'NONE',  ( 9.832129032723420536, 186.5104166632526983, -5.676582343749999815 ) ) ;
#46341=CARTESIAN_POINT ( 'NONE',  ( -9.999999999999996447, 207.5000000000000853, -1.224646799147352862E-15 ) ) ;
#46346=CARTESIAN_POINT ( 'NONE',  ( -5.676582343749998039, 72.44791666325268409, -9.832129032723420536 ) ) ;
#46352=CARTESIAN_POINT ( 'NONE',  ( 11.35316468749999785, 60.57291666325269119, 3.042071309553174174 ) ) ;
#46357=CARTESIAN_POINT ( 'NONE',  ( 5.676582343749993598, 64.94791666325269830, 9.832129032723422313 ) ) ;
#46362=CARTESIAN_POINT ( 'NONE',  ( 10.00000000000000178, 152.0833333265053682, -2.679491924311226736 ) ) ;
#46366=CARTESIAN_POINT ( 'NONE',  ( -11.35316468749999785, 48.38541666325268409, -3.042071309553167957 ) ) ;
#46369=CARTESIAN_POINT ( 'NONE',  ( -5.676582343749998039, 182.4479166632526983, -9.832129032723420536 ) ) ;
#46375=CARTESIAN_POINT ( 'NONE',  ( -9.832129032723420536, 173.6979166632526983, 5.676582343749997150 ) ) ;
#46381=CARTESIAN_POINT ( 'NONE',  ( -11.35316468750000141, 168.5937499965860127, -1.390361679473963753E-15 ) ) ;
#46384=CARTESIAN_POINT ( 'NONE',  ( 5.676582343749993598, 130.2604166632526983, 9.832129032723422313 ) ) ;
#46399=AXIS2_PLACEMENT_3D ( 'NONE', #59972, #53585, #30197 ) ;
#46403=ORIENTED_EDGE ( 'NONE', *, *, #25514, .T. ) ;
#46415=CARTESIAN_POINT ( 'NONE',  ( 6.676582343750001591, 297.1093750017069510, -8.176455196517173205E-16 ) ) ;
#46416=CARTESIAN_POINT ( 'NONE',  ( -10.00000000000000355, 137.7083333333333428, 2.679491924311223183 ) ) ;
#46418=CARTESIAN_POINT ( 'NONE',  ( -1.224646799147353454E-15, 225.9999999999999432, 10.00000000000000178 ) ) ;
#46433=CARTESIAN_POINT ( 'NONE',  ( -11.35316468749999785, 28.07291666325268054, -3.042071309553167513 ) ) ;
#46435=CARTESIAN_POINT ( 'NONE',  ( 3.042071309553159519, 220.0520833299193271, 11.35316468750000141 ) ) ;
#46440=CARTESIAN_POINT ( 'NONE',  ( 9.832129032723420536, 26.19791666325268409, -5.676582343749999815 ) ) ;
#46443=CARTESIAN_POINT ( 'NONE',  ( -2.679491924309608919, 151.4583333333332007, -10.00000000000094502 ) ) ;
#46446=CARTESIAN_POINT ( 'NONE',  ( 11.35316468749999785, 15.57291666325268409, 3.042071309553174174 ) ) ;
#46449=CARTESIAN_POINT ( 'NONE',  ( -3.042071309553164404, 132.2395833299193555, -11.35316468749999963 ) ) ;
#46450=CARTESIAN_POINT ( 'NONE',  ( 2.679491924311222739, 120.8333333265053540, 10.00000000000000355 ) ) ;
#46455=CARTESIAN_POINT ( 'NONE',  ( -3.042071309553173730, 4.635416663252683200, 11.35316468749999785 ) ) ;
#46457=CARTESIAN_POINT ( 'NONE',  ( 6.000000000000001776, 289.5000000000000000, -7.347880794884121708E-16 ) ) ;
#46458=CARTESIAN_POINT ( 'NONE',  ( 2.765530957082001251, 298.7656250017069510, 6.676582343750000703 ) ) ;
#46459=CARTESIAN_POINT ( 'NONE',  ( 9.832129032723416984, 140.3645833299193555, 5.676582343750006032 ) ) ;
#46466=CARTESIAN_POINT ( 'NONE',  ( 10.00000000000000178, 217.0833333265053682, -2.679491924311226736 ) ) ;
#46467=CYLINDRICAL_SURFACE ( 'NONE', #3822, 10.00000000000000178 ) ;
#46468=CARTESIAN_POINT ( 'NONE',  ( -9.832129032723420536, 89.01041666325268409, 5.676582343749997150 ) ) ;
#46499=CARTESIAN_POINT ( 'NONE',  ( 2.679491924311228956, 91.04166666666665719, -10.00000000000000000 ) ) ;
#46501=CARTESIAN_POINT ( 'NONE',  ( -9.832129032723420536, 59.01041666325268409, 5.676582343749997150 ) ) ;
#46502=CARTESIAN_POINT ( 'NONE',  ( 4.242640687119287435, 289.3750000000000000, 4.242640687119285658 ) ) ;
#46503=CIRCLE ( 'NONE', #26025, 8.000000000000003553 ) ;
#46510=LINE ( 'NONE', #7267, #23771 ) ;
#46511=FACE_OUTER_BOUND ( 'NONE', #59791, .T. ) ;
#46516=CARTESIAN_POINT ( 'NONE',  ( 7.320508075688774596, 205.6250000000000000, -7.320508075688774596 ) ) ;
#46518=CARTESIAN_POINT ( 'NONE',  ( 3.042071309553159519, 175.0520833299193839, 11.35316468750000141 ) ) ;
#46522=CARTESIAN_POINT ( 'NONE',  ( 10.00000000000000000, 86.66666665983869677, 2.679491924311235618 ) ) ;
#46525=CARTESIAN_POINT ( 'NONE',  ( -3.042071309553173730, 39.63541666325267698, 11.35316468749999785 ) ) ;
#46529=DIRECTION ( 'NONE',  ( 0.000000000000000000, 0.000000000000000000, 1.000000000000000000 ) ) ;
#46534=CARTESIAN_POINT ( 'NONE',  ( -7.320508075688773708, 78.74999999317203958, -7.320508075688774596 ) ) ;
#46541=ORIENTED_EDGE ( 'NONE', *, *, #36582, .F. ) ;
#46542=CARTESIAN_POINT ( 'NONE',  ( -7.320508075688857197, 198.1250000000000853, 7.320508075688848315 ) ) ;
#46543=CARTESIAN_POINT ( 'NONE',  ( 6.676582343750001591, 297.1093750017069510, -8.176455196517173205E-16 ) ) ;
#46544=CARTESIAN_POINT ( 'NONE',  ( 2.679491924311228956, 42.91666665983869677, -10.00000000000000000 ) ) ;
#46545=CARTESIAN_POINT ( 'NONE',  ( 6.951808397369818766E-16, 152.0312499965860411, -11.35316468750000141 ) ) ;
#46546=CARTESIAN_POINT ( 'NONE',  ( -2.485281374238967000, 297.8125000000000568, -5.999999999999608313 ) ) ;
#46555=CARTESIAN_POINT ( 'NONE',  ( 6.951808397369818766E-16, 127.3437499965860127, -11.35316468750000141 ) ) ;
#46559=CARTESIAN_POINT ( 'NONE',  ( -9.832129032723418760, 53.17708332991935549, -5.676582343750004256 ) ) ;
#46560=VERTEX_POINT ( 'NONE', #20891 ) ;
#46561=CARTESIAN_POINT ( 'NONE',  ( 8.660254037844389075, 37.29166665983869677, -5.000000000000000000 ) ) ;
#46566=CARTESIAN_POINT ( 'NONE',  ( 4.242640687119285658, 295.6875000034139589, -4.242640687119286547 ) ) ;
#46588=CARTESIAN_POINT ( 'NONE',  ( -10.00000000000000178, 47.50000000000000000, -1.224646799147353454E-15 ) ) ;
#46591=CARTESIAN_POINT ( 'NONE',  ( -2.485281374238572649, 299.1874999999999432, 6.000000000000002665 ) ) ;
#46599=CARTESIAN_POINT ( 'NONE',  ( -7.320508075688773708, 146.8749999999999716, -7.320508075688774596 ) ) ;
#46601=CARTESIAN_POINT ( 'NONE',  ( -2.679491924311235618, 163.5416666666666572, 10.00000000000000000 ) ) ;
#46605=CARTESIAN_POINT ( 'NONE',  ( -11.35316468750000141, 143.8020833299193555, 3.042071309553159963 ) ) ;
#46614=CARTESIAN_POINT ( 'NONE',  ( 6.951808397369818766E-16, 2.343749996586016682, -11.35316468750000141 ) ) ;
#46619=CARTESIAN_POINT ( 'NONE',  ( -8.660254037844390851, 24.79166665983870033, 4.999999999999998224 ) ) ;
#46625=CARTESIAN_POINT ( 'NONE',  ( 0.000000000000000000, 300.0000000000000000, 0.000000000000000000 ) ) ;
#46626=CARTESIAN_POINT ( 'NONE',  ( -9.832129032723418760, 107.8645833299193555, -5.676582343750004256 ) ) ;
#46632=CARTESIAN_POINT ( 'NONE',  ( -2.085542519210945728E-15, 119.5312499965860269, 11.35316468750000141 ) ) ;
#46634=DIRECTION ( 'NONE',  ( -0.000000000000000000, 1.000000000000000000, -0.000000000000000000 ) ) ;
#46636=CARTESIAN_POINT ( 'NONE',  ( -1.836970198721029983E-15, 215.6249999931720538, 10.00000000000000178 ) ) ;
#46640=CARTESIAN_POINT ( 'NONE',  ( 8.311093377946834337, 95.15624999658601268, 8.311093377946839666 ) ) ;
#46644=CARTESIAN_POINT ( 'NONE',  ( 8.660254037844465458, 175.4166666666667140, -5.000000000000044409 ) ) ;
#46646=( BOUNDED_CURVE ( )  B_SPLINE_CURVE ( 2, ( #68102, #33414, #27730, #73387, #56414, #61325, #9651, #50740, #16392, #32289, #43588, #32671, #10755 ),
 .UNSPECIFIED., .F., .F. ) 
 B_SPLINE_CURVE_WITH_KNOTS ( ( 3, 2, 2, 2, 2, 2, 3 ),
 ( 0.4728260869565217850, 0.4746376811594203438, 0.4764492753623189025, 0.4782608695652174058, 0.4800724637681159646, 0.4818840579710144678, 0.4836956521739130266 ),
 .UNSPECIFIED. ) 
 CURVE ( )  GEOMETRIC_REPRESENTATION_ITEM ( )  RATIONAL_B_SPLINE_CURVE ( ( 0.9999999999999990008, 0.9659258262890693114, 1.000000000000000000, 0.9659258262890683122, 1.000000000000000000, 0.9659258262890683122, 1.000000000000000000, 0.9659258262890683122, 1.000000000000000000, 0.9659258262890683122, 1.000000000000000000, 0.9659258262890683122, 1.000000000000000000 ) ) 
 REPRESENTATION_ITEM ( '' )  );
#46647=CARTESIAN_POINT ( 'NONE',  ( 6.123233995736767268E-16, 193.1249999931720254, -10.00000000000000178 ) ) ;
#46650=CARTESIAN_POINT ( 'NONE',  ( -2.085542519210945728E-15, 94.84374999658601268, 11.35316468750000141 ) ) ;
#46654=CARTESIAN_POINT ( 'NONE',  ( 3.042071309553167069, 7.135416663252682312, -11.35316468749999785 ) ) ;
#46658=CARTESIAN_POINT ( 'NONE',  ( 11.35316468750000141, 215.7812499965860411, 0.000000000000000000 ) ) ;
#46661=CARTESIAN_POINT ( 'NONE',  ( -8.660254037844387298, 98.95833332650536818, -5.000000000000004441 ) ) ;
#46662=CARTESIAN_POINT ( 'NONE',  ( -2.765530957081998586, 296.6406250017069510, 6.676582343750001591 ) ) ;
#46665=CARTESIAN_POINT ( 'NONE',  ( -11.35316468750000141, 213.8020833299193839, 3.042071309553159963 ) ) ;
#46673=CARTESIAN_POINT ( 'NONE',  ( 8.660254037844385522, 34.58333333333333570, 5.000000000000005329 ) ) ;
#46682=CARTESIAN_POINT ( 'NONE',  ( 2.765530957082001251, 296.7656250017069510, 6.676582343749999815 ) ) ;
#46691=CARTESIAN_POINT ( 'NONE',  ( 8.311093377946834337, 90.46874999658599847, 8.311093377946839666 ) ) ;
#46700=CARTESIAN_POINT ( 'NONE',  ( 11.35316468749999785, 195.5729166632526983, 3.042071309553174174 ) ) ;
#46702=ADVANCED_FACE ( 'NONE', ( #46511 ), #22369, .T. ) ;
#46705=CARTESIAN_POINT ( 'NONE',  ( 5.676582343750001591, 186.9270833299193555, -9.832129032723420536 ) ) ;
#46711=CARTESIAN_POINT ( 'NONE',  ( -3.042071309553173730, 74.32291666325268409, 11.35316468749999785 ) ) ;
#46717=CARTESIAN_POINT ( 'NONE',  ( 5.676582343749993598, 69.94791666325268409, 9.832129032723422313 ) ) ;
#46722=CARTESIAN_POINT ( 'NONE',  ( -5.676582343750006032, 59.11458332991934839, 9.832129032723418760 ) ) ;
#46727=CARTESIAN_POINT ( 'NONE',  ( 2.679491924311222739, 155.8333333265053682, 10.00000000000000355 ) ) ;
#46730=CARTESIAN_POINT ( 'NONE',  ( -11.35316468749999785, 53.38541666325267698, -3.042071309553167957 ) ) ;
#46733=CARTESIAN_POINT ( 'NONE',  ( -2.085542519210945728E-15, 184.5312499965860411, 11.35316468750000141 ) ) ;
#46737=CARTESIAN_POINT ( 'NONE',  ( 2.679491924311222739, 160.8333333265053682, 10.00000000000000355 ) ) ;
#46739=CARTESIAN_POINT ( 'NONE',  ( 3.042071309553159519, 179.7395833299193555, 11.35316468750000141 ) ) ;
#46740=CARTESIAN_POINT ( 'NONE',  ( 1.224646799147353454E-15, 300.0000000000000000, -10.00000000000000178 ) ) ;
#46745=CARTESIAN_POINT ( 'NONE',  ( 11.35316468749999963, 171.3020833299193555, -3.042071309553165293 ) ) ;
#46749=CARTESIAN_POINT ( 'NONE',  ( -11.35316468749999785, 133.3854166632526699, -3.042071309553167513 ) ) ;
#46758=CARTESIAN_POINT ( 'NONE',  ( -2.679491924310637874, 186.4583333333332291, -10.00000000000034284 ) ) ;
#46762=VECTOR ( 'NONE', #57751, 1000.000000000000000 ) ;
#46765=ORIENTED_EDGE ( 'NONE', *, *, #20580, .T. ) ;
#46769=ORIENTED_EDGE ( 'NONE', *, *, #8357, .T. ) ;
#46775=CARTESIAN_POINT ( 'NONE',  ( -10.00000000000000178, 255.9999999999999432, 0.000000000000000000 ) ) ;
#46777=CARTESIAN_POINT ( 'NONE',  ( -6.676582343750002480, 296.5468750017069510, -2.765530957081996810 ) ) ;
#46778=CARTESIAN_POINT ( 'NONE',  ( 4.999999999999993783, 139.1666666666666856, 8.660254037844390851 ) ) ;
#46792=CARTESIAN_POINT ( 'NONE',  ( 0.000000000000000000, 300.0000000000000000, 0.000000000000000000 ) ) ;
#46797=CARTESIAN_POINT ( 'NONE',  ( 11.35316468749999963, 25.98958332991935194, -3.042071309553165293 ) ) ;
#46798=CARTESIAN_POINT ( 'NONE',  ( 5.000000000000166089, 25.83333333333352755, -8.660254037844673292 ) ) ;
#46799=CARTESIAN_POINT ( 'NONE',  ( 11.35316468749999785, 225.8854166632526699, 3.042071309553174174 ) ) ;
#46805=CARTESIAN_POINT ( 'NONE',  ( 11.35316468750000141, 20.78124999658601624, 0.000000000000000000 ) ) ;
#46811=CARTESIAN_POINT ( 'NONE',  ( -11.35316468750000141, 18.28124999658601624, -1.390361679473963753E-15 ) ) ;
#46813=CARTESIAN_POINT ( 'NONE',  ( 3.042071309553159519, 144.7395833299193839, 11.35316468750000141 ) ) ;
#46815=CARTESIAN_POINT ( 'NONE',  ( 2.679491924311222739, 115.8333333265053682, 10.00000000000000355 ) ) ;
#46817=CARTESIAN_POINT ( 'NONE',  ( 10.00000000000000178, 172.0833333265053682, -2.679491924311226736 ) ) ;
#46820=CARTESIAN_POINT ( 'NONE',  ( 5.676582343750001591, 6.927083329919350163, -9.832129032723420536 ) ) ;
#46824=CARTESIAN_POINT ( 'NONE',  ( 6.676582343750003368, 299.0156250017069510, -2.765530957081997254 ) ) ;
#46826=CARTESIAN_POINT ( 'NONE',  ( -5.676582343750006032, 134.1145833299193555, 9.832129032723418760 ) ) ;
#46835=CARTESIAN_POINT ( 'NONE',  ( 10.00000000000000355, 119.7916666666666714, 2.679491924311236506 ) ) ;
#46838=CARTESIAN_POINT ( 'NONE',  ( -8.311093377946841443, 89.21874999658602690, 8.311093377946830785 ) ) ;
#46849=( BOUNDED_CURVE ( )  B_SPLINE_CURVE ( 2, ( #54663, #2972, #32018, #53546, #65963, #9379, #25592, #71613, #43702 ),
 .UNSPECIFIED., .F., .F. ) 
 B_SPLINE_CURVE_WITH_KNOTS ( ( 3, 2, 2, 2, 3 ),
 ( 0.4374999999999980571, 0.4479166666666647423, 0.4583333333333313719, 0.4687499999999980571, 0.4791666666666647423 ),
 .UNSPECIFIED. ) 
 CURVE ( )  GEOMETRIC_REPRESENTATION_ITEM ( )  RATIONAL_B_SPLINE_CURVE ( ( 1.000000000000014211, 0.9238795325112725276, 1.000000000000000000, 0.9238795325112867385, 1.000000000000000000, 0.9238795325112867385, 1.000000000000000000, 0.9238795325113009493, 0.9999999999999857891 ) ) 
 REPRESENTATION_ITEM ( '' )  );
#46854=ORIENTED_EDGE ( 'NONE', *, *, #31273, .T. ) ;
#46862=CARTESIAN_POINT ( 'NONE',  ( 8.660254037844389075, 122.2916666598387110, -5.000000000000000000 ) ) ;
#46869=CARTESIAN_POINT ( 'NONE',  ( -2.679491924306005579, 98.54166666666711194, 10.00000000000300560 ) ) ;
#46873=CARTESIAN_POINT ( 'NONE',  ( -8.660254037844390851, 97.91666666666668561, 4.999999999999998224 ) ) ;
#46875=CARTESIAN_POINT ( 'NONE',  ( -5.676582343750006032, 59.42708332991934839, 9.832129032723418760 ) ) ;
#46876=CARTESIAN_POINT ( 'NONE',  ( -2.485281374238572649, 289.1875000000000000, 6.000000000000002665 ) ) ;
#46882=CARTESIAN_POINT ( 'NONE',  ( 2.679491924311224960, 83.95833333333332860, 10.00000000000001243 ) ) ;
#46887=CARTESIAN_POINT ( 'NONE',  ( 8.660254037844389075, 220.4166666666666856, -5.000000000000000000 ) ) ;
#46889=CARTESIAN_POINT ( 'NONE',  ( 5.676582343750001591, 176.9270833299193555, -9.832129032723420536 ) ) ;
#46896=CARTESIAN_POINT ( 'NONE',  ( 6.951808397369818766E-16, 42.34374999658601979, -11.35316468750000141 ) ) ;
#46899=CARTESIAN_POINT ( 'NONE',  ( 2.679491924311213857, 8.958333333333333925, 10.00000000000000888 ) ) ;
#46903=CARTESIAN_POINT ( 'NONE',  ( -2.679491924311235618, 75.41666665983869677, 10.00000000000000000 ) ) ;
#46906=CARTESIAN_POINT ( 'NONE',  ( -1.836970198721029983E-15, 63.75000000000000000, 10.00000000000000178 ) ) ;
#46907=CARTESIAN_POINT ( 'NONE',  ( -8.660254037844387298, 48.95833332650536818, -5.000000000000004441 ) ) ;
#46912=CARTESIAN_POINT ( 'NONE',  ( 4.721056650415999201, 296.2343750017069510, -4.721056650415999201 ) ) ;
#46915=CARTESIAN_POINT ( 'NONE',  ( 6.951808397369818766E-16, 157.0312499965860127, -11.35316468750000141 ) ) ;
#46917=CARTESIAN_POINT ( 'NONE',  ( 0.000000000000000000, 300.0000000000000000, 0.000000000000000000 ) ) ;
#46924=CARTESIAN_POINT ( 'NONE',  ( -5.676582343750006032, 139.4270833299193555, 9.832129032723418760 ) ) ;
#46928=CARTESIAN_POINT ( 'NONE',  ( 3.042071309553167069, 52.13541666325268409, -11.35316468749999785 ) ) ;
#46930=CYLINDRICAL_SURFACE ( 'NONE', #12735, 6.000000000000001776 ) ;
#46934=CARTESIAN_POINT ( 'NONE',  ( -2.485281374238571761, 291.8750000034140157, -6.000000000000003553 ) ) ;
#46942=ORIENTED_EDGE ( 'NONE', *, *, #43137, .F. ) ;
#46952=( BOUNDED_CURVE ( )  B_SPLINE_CURVE ( 2, ( #10005, #49984, #32276, #42821, #60182, #72244, #14519, #8503, #73001, #21310, #37931, #31520, #66214 ),
 .UNSPECIFIED., .F., .F. ) 
 B_SPLINE_CURVE_WITH_KNOTS ( ( 3, 2, 2, 2, 2, 2, 3 ),
 ( 0.09239130434782608092, 0.09420289855072463969, 0.09601449275362318458, 0.09782608695652174335, 0.09963768115942028825, 0.1014492753623188470, 0.1032608695652173919 ),
 .UNSPECIFIED. ) 
 CURVE ( )  GEOMETRIC_REPRESENTATION_ITEM ( )  RATIONAL_B_SPLINE_CURVE ( ( 1.000000000000000000, 0.9659258262890683122, 1.000000000000000000, 0.9659258262890683122, 1.000000000000000000, 0.9659258262890683122, 1.000000000000000000, 0.9659258262890683122, 1.000000000000000000, 0.9659258262890683122, 1.000000000000000000, 0.9659258262890683122, 1.000000000000000000 ) ) 
 REPRESENTATION_ITEM ( '' )  );
#46957=CARTESIAN_POINT ( 'NONE',  ( 6.123233995736767268E-16, 73.12499999317203958, -10.00000000000000178 ) ) ;
#46958=CARTESIAN_POINT ( 'NONE',  ( 8.660254037844389075, 60.41666666666666430, -5.000000000000000000 ) ) ;
#46966=CARTESIAN_POINT ( 'NONE',  ( -6.362988438888832046E-13, 88.74999999999995737, 9.999999999999998224 ) ) ;
#46967=CARTESIAN_POINT ( 'NONE',  ( -8.660254037844387298, 73.95833332650536818, -5.000000000000004441 ) ) ;
#46969=CARTESIAN_POINT ( 'NONE',  ( 1.584317714026805320E-12, 163.7500000000001137, 9.999999999999998224 ) ) ;
#46970=CARTESIAN_POINT ( 'NONE',  ( -10.00000000000000178, 177.5000000000000284, -1.224646799147353454E-15 ) ) ;
#46974=CARTESIAN_POINT ( 'NONE',  ( 5.676582343749993598, 145.2604166632526699, 9.832129032723422313 ) ) ;
#46975=CARTESIAN_POINT ( 'NONE',  ( 11.35316468750000141, 0.9374999965860164597, 0.000000000000000000 ) ) ;
#46985=CARTESIAN_POINT ( 'NONE',  ( -2.679491924311225848, 33.33333332650536107, -10.00000000000000178 ) ) ;
#46993=CARTESIAN_POINT ( 'NONE',  ( 4.999999999999996447, 29.16666666666667140, 8.660254037844394404 ) ) ;
#46994=CARTESIAN_POINT ( 'NONE',  ( -4.433107781481984588, 226.0000000000000284, -8.987711252925484118 ) ) ;
#46997=CARTESIAN_POINT ( 'NONE',  ( 6.951808397369818766E-16, 122.0312499965860269, -11.35316468750000141 ) ) ;
#47006=CARTESIAN_POINT ( 'NONE',  ( 5.676582343750001591, 96.61458332991935549, -9.832129032723420536 ) ) ;
#47009=CARTESIAN_POINT ( 'NONE',  ( -2.250000000000000000, 300.0000000000000000, 7.677076266392047543 ) ) ;
#47010=ORIENTED_EDGE ( 'NONE', *, *, #56330, .T. ) ;
#47011=CARTESIAN_POINT ( 'NONE',  ( 7.320508075688771044, 196.2499999931719969, 7.320508075688775484 ) ) ;
#47014=CARTESIAN_POINT ( 'NONE',  ( 11.35316468750000141, 91.09374999658602690, 0.000000000000000000 ) ) ;
#47015=CARTESIAN_POINT ( 'NONE',  ( 1.102182119232618108E-15, 298.2500000000000000, 6.000000000000001776 ) ) ;
#47018=CARTESIAN_POINT ( 'NONE',  ( -9.832129032723418760, 13.17708332991935194, -5.676582343750004256 ) ) ;
#47022=CARTESIAN_POINT ( 'NONE',  ( 6.951808397369818766E-16, 222.0312499965860127, -11.35316468750000141 ) ) ;
#47024=CARTESIAN_POINT ( 'NONE',  ( -4.721056650415999201, 294.3281250017069510, -4.721056650415999201 ) ) ;
#47027=CARTESIAN_POINT ( 'NONE',  ( 8.311093377946834337, 205.4687499965859843, 8.311093377946839666 ) ) ;
#47038=CARTESIAN_POINT ( 'NONE',  ( -1.836970198721029983E-15, 28.75000000000000000, 10.00000000000000178 ) ) ;
#47047=EDGE_CURVE ( 'NONE', #10894, #65462, #50837, .T. ) ;
#47048=CARTESIAN_POINT ( 'NONE',  ( -2.295000000000000373, 284.2799999999998590, 5.414444767710663520 ) ) ;
#47049=CARTESIAN_POINT ( 'NONE',  ( -4.721056650415998313, 295.5781250017069510, 4.721056650416000089 ) ) ;
#47057=CARTESIAN_POINT ( 'NONE',  ( -11.35316468750000141, 98.80208332991932707, 3.042071309553159963 ) ) ;
#47067=CARTESIAN_POINT ( 'NONE',  ( 11.35316468749999785, 210.5729166632526983, 3.042071309553174174 ) ) ;
#47068=( BOUNDED_CURVE ( )  B_SPLINE_CURVE ( 2, ( #66121, #32562, #3134, #44245, #15553, #38591, #73285, #4258, #9162, #21588, #61590, #50263, #8791 ),
 .UNSPECIFIED., .F., .F. ) 
 B_SPLINE_CURVE_WITH_KNOTS ( ( 3, 2, 2, 2, 2, 2, 3 ),
 ( 0.6684782608695651884, 0.6702898550724637472, 0.6721014492753623060, 0.6739130434782608647, 0.6757246376811594235, 0.6775362318840579823, 0.6793478260869565410 ),
 .UNSPECIFIED. ) 
 CURVE ( )  GEOMETRIC_REPRESENTATION_ITEM ( )  RATIONAL_B_SPLINE_CURVE ( ( 1.000000000000000000, 0.9659258262890683122, 1.000000000000000000, 0.9659258262890683122, 1.000000000000000000, 0.9659258262890683122, 1.000000000000000000, 0.9659258262890683122, 1.000000000000000000, 0.9659258262890683122, 1.000000000000000000, 0.9659258262890683122, 1.000000000000000000 ) ) 
 REPRESENTATION_ITEM ( '' )  );
#47072=CARTESIAN_POINT ( 'NONE',  ( 11.35316468749999963, 181.3020833299192986, -3.042071309553165293 ) ) ;
#47079=CARTESIAN_POINT ( 'NONE',  ( -8.311093377946836114, 72.65624999658604111, -8.311093377946837890 ) ) ;
#47084=CARTESIAN_POINT ( 'NONE',  ( 9.832129032723416984, 70.36458332991936970, 5.676582343750006032 ) ) ;
#47089=CARTESIAN_POINT ( 'NONE',  ( -11.35316468750000141, 63.48958332991935549, 3.042071309553159963 ) ) ;
#47091=CARTESIAN_POINT ( 'NONE',  ( -10.00000000000000000, 14.16666665983870033, -2.679491924311229845 ) ) ;
#47092=CARTESIAN_POINT ( 'NONE',  ( -5.000000000000005329, 155.2083333265053682, 8.660254037844387298 ) ) ;
#47095=CARTESIAN_POINT ( 'NONE',  ( 7.320508075688779925, 20.62500000000000000, -7.320508075688779925 ) ) ;
#47096=CARTESIAN_POINT ( 'NONE',  ( -3.042071309553163960, 47.55208332991934839, -11.35316468749999963 ) ) ;
#47098=CARTESIAN_POINT ( 'NONE',  ( 5.676582343750001591, 196.6145833299193839, -9.832129032723420536 ) ) ;
#47099=ORIENTED_EDGE ( 'NONE', *, *, #43157, .T. ) ;
#47104=CARTESIAN_POINT ( 'NONE',  ( -2.085542519210945728E-15, 179.5312499965860411, 11.35316468750000141 ) ) ;
#47111=CARTESIAN_POINT ( 'NONE',  ( 8.311093377946834337, 170.4687499965860127, 8.311093377946839666 ) ) ;
#47114=CARTESIAN_POINT ( 'NONE',  ( 9.832129032723420536, 131.5104166632526983, -5.676582343749999815 ) ) ;
#47115=DIRECTION ( 'NONE',  ( -0.000000000000000000, 1.000000000000000000, -0.000000000000000000 ) ) ;
#47118=ADVANCED_FACE ( 'NONE', ( #36400 ), #42410, .T. ) ;
#47129=CARTESIAN_POINT ( 'NONE',  ( -5.000000000000031974, 178.3333333333333997, 8.660254037844435260 ) ) ;
#47135=ORIENTED_EDGE ( 'NONE', *, *, #64967, .F. ) ;
#47147=CARTESIAN_POINT ( 'NONE',  ( 2.679491924311228956, 131.0416666666666856, -10.00000000000000000 ) ) ;
#47161=CARTESIAN_POINT ( 'NONE',  ( 10.00000000000000000, 51.66666665983870388, 2.679491924311235618 ) ) ;
#47164=CARTESIAN_POINT ( 'NONE',  ( -5.676582343749998039, 32.44791666325268409, -9.832129032723420536 ) ) ;
#47166=CARTESIAN_POINT ( 'NONE',  ( 8.660254037844389075, 2.291666659838699438, -5.000000000000000000 ) ) ;
#47170=VECTOR ( 'NONE', #43648, 1000.000000000000000 ) ;
#47173=CARTESIAN_POINT ( 'NONE',  ( 3.042071309553167069, 31.82291666325268054, -11.35316468749999785 ) ) ;
#47176=CARTESIAN_POINT ( 'NONE',  ( -10.00000000000000711, 152.2916666666667140, -2.679491924311232953 ) ) ;
#47179=CARTESIAN_POINT ( 'NONE',  ( -5.676582343750006032, 19.11458332991934839, 9.832129032723418760 ) ) ;
#47181=CARTESIAN_POINT ( 'NONE',  ( -2.085542519210945728E-15, 144.5312499965860411, 11.35316468750000141 ) ) ;
#47182=CARTESIAN_POINT ( 'NONE',  ( -5.000000000000005329, 120.2083333265053824, 8.660254037844387298 ) ) ;
#47184=DIRECTION ( 'NONE',  ( -0.000000000000000000, 1.000000000000000000, -0.000000000000000000 ) ) ;
#47187=CARTESIAN_POINT ( 'NONE',  ( 9.832129032723416984, 5.677083329919350163, 5.676582343750006032 ) ) ;
#47189=ORIENTED_EDGE ( 'NONE', *, *, #44909, .F. ) ;
#47191=CARTESIAN_POINT ( 'NONE',  ( -4.088227598258586603E-16, 298.2031250017070079, -6.676582343750001591 ) ) ;
#47193=CARTESIAN_POINT ( 'NONE',  ( -5.676582343749998039, 137.4479166632526983, -9.832129032723420536 ) ) ;
#47202=CARTESIAN_POINT ( 'NONE',  ( -2.679491924311382611, 205.4166666598386826, 9.999999999999914735 ) ) ;
#47204=CARTESIAN_POINT ( 'NONE',  ( 8.311093377946834337, 90.46874999658599847, 8.311093377946839666 ) ) ;
#47223=DIRECTION ( 'NONE',  ( -0.000000000000000000, 1.000000000000000000, -0.000000000000000000 ) ) ;
#47224=EDGE_CURVE ( 'NONE', #48362, #38468, #55242, .T. ) ;
#47236=CARTESIAN_POINT ( 'NONE',  ( 10.00000000000000178, 100.2083333333333428, -2.679491924311226736 ) ) ;
#47239=CARTESIAN_POINT ( 'NONE',  ( 3.042071309553159519, 55.05208332991934128, 11.35316468750000141 ) ) ;
#47240=CARTESIAN_POINT ( 'NONE',  ( 4.721056650415999201, 296.2343750017069510, -4.721056650415999201 ) ) ;
#47242=CARTESIAN_POINT ( 'NONE',  ( 10.00000000000004086, 189.7916666666667140, 2.679491924311245388 ) ) ;
#47246=CARTESIAN_POINT ( 'NONE',  ( 1.681385197618709730E-11, 51.24999999999869971, -10.00000000000000178 ) ) ;
#47249=CARTESIAN_POINT ( 'NONE',  ( 0.000000000000000000, 300.0000000000000000, 0.000000000000000000 ) ) ;
#47251=CARTESIAN_POINT ( 'NONE',  ( -5.000000000000005329, 218.3333333333333428, 8.660254037844387298 ) ) ;
#47253=CARTESIAN_POINT ( 'NONE',  ( -2.085542519210945728E-15, 179.8437499965860411, 11.35316468750000141 ) ) ;
#47260=CARTESIAN_POINT ( 'NONE',  ( 11.35316468750000141, 36.09374999658601979, 0.000000000000000000 ) ) ;
#47262=CARTESIAN_POINT ( 'NONE',  ( 11.35316468749999785, 215.8854166632526983, 3.042071309553174174 ) ) ;
#47264=CARTESIAN_POINT ( 'NONE',  ( 4.999999999999994671, 9.166666666666666075, 8.660254037844390851 ) ) ;
#47268=CARTESIAN_POINT ( 'NONE',  ( -10.00000000000000000, 69.16666665983868256, -2.679491924311229845 ) ) ;
#47277=CARTESIAN_POINT ( 'NONE',  ( 2.765530957081996366, 296.2968750017070079, -6.676582343750003368 ) ) ;
#47278=CARTESIAN_POINT ( 'NONE',  ( -10.00000000000001243, 142.2916666666666856, -2.679491924311233841 ) ) ;
#47280=CARTESIAN_POINT ( 'NONE',  ( 5.676582343750001591, 156.6145833299193839, -9.832129032723420536 ) ) ;
#47282=CARTESIAN_POINT ( 'NONE',  ( 7.320508075688775484, 5.625000000000000000, -7.320508075688775484 ) ) ;
#47287=ORIENTED_EDGE ( 'NONE', *, *, #31636, .T. ) ;
#47288=( BOUNDED_CURVE ( )  B_SPLINE_CURVE ( 2, ( #30491, #42903, #8589, #31228, #2934, #48938, #2563, #25552, #13488, #48566, #65923, #70849, #53508 ),
 .UNSPECIFIED., .F., .F. ) 
 B_SPLINE_CURVE_WITH_KNOTS ( ( 3, 2, 2, 2, 2, 2, 3 ),
 ( 0.9262938265175630903, 0.9315262799636203628, 0.9367587334096776353, 0.9419911868557350187, 0.9472236403017922912, 0.9524560937478495637, 0.9576885471939067251 ),
 .UNSPECIFIED. ) 
 CURVE ( )  GEOMETRIC_REPRESENTATION_ITEM ( )  RATIONAL_B_SPLINE_CURVE ( ( 0.9999999999999990008, 0.9659258262890693114, 1.000000000000000000, 0.9659258262890683122, 1.000000000000000000, 0.9659258262890683122, 1.000000000000000000, 0.9659258262890683122, 1.000000000000000000, 0.9659258262890683122, 1.000000000000000000, 0.9659258262891518010, 0.9999999999999165112 ) ) 
 REPRESENTATION_ITEM ( '' )  );
#47291=CARTESIAN_POINT ( 'NONE',  ( -2.085542519210945728E-15, 144.8437499965860411, 11.35316468750000141 ) ) ;
#47297=CARTESIAN_POINT ( 'NONE',  ( -3.042071309553173730, 49.63541666325267698, 11.35316468749999785 ) ) ;
#47298=ORIENTED_EDGE ( 'NONE', *, *, #49305, .F. ) ;
#47299=CARTESIAN_POINT ( 'NONE',  ( -7.320508075688782590, 28.12500000000000355, 7.320508075688774596 ) ) ;
#47303=CARTESIAN_POINT ( 'NONE',  ( -4.242640687119285658, 294.1875000034139589, 4.242640687119287435 ) ) ;
#47307=( BOUNDED_CURVE ( )  B_SPLINE_CURVE ( 2, ( #22087, #33815, #74524, #68490, #21714, #73410, #4383, #68864, #50395, #45111, #11158, #33077, #67759 ),
 .UNSPECIFIED., .F., .F. ) 
 B_SPLINE_CURVE_WITH_KNOTS ( ( 3, 2, 2, 2, 2, 2, 3 ),
 ( 0.9890912047459377021, 0.9943250801786815973, 0.9995589556114257146, 1.004792831044169832, 1.010026706476913949, 1.015260581909658066, 1.020494457342402184 ),
 .UNSPECIFIED. ) 
 CURVE ( )  GEOMETRIC_REPRESENTATION_ITEM ( )  RATIONAL_B_SPLINE_CURVE ( ( 1.000000000000001110, 0.9659258262890673130, 1.000000000000000000, 0.9659258262890683122, 1.000000000000000000, 0.9659258262890683122, 1.000000000000000000, 0.9659258262890683122, 1.000000000000000000, 0.9659258262890683122, 1.000000000000000000, 0.9659258262891643465, 0.9999999999999039657 ) ) 
 REPRESENTATION_ITEM ( '' )  );
#47328=CARTESIAN_POINT ( 'NONE',  ( 7.320508075688774596, 50.62500000000000711, -7.320508075688774596 ) ) ;
#47330=CARTESIAN_POINT ( 'NONE',  ( 4.242640687119285658, 294.6249999999999432, -4.242640687119286547 ) ) ;
#47336=CARTESIAN_POINT ( 'NONE',  ( -1.836970198721029983E-15, 65.62499999317203958, 10.00000000000000178 ) ) ;
#47337=CARTESIAN_POINT ( 'NONE',  ( -4.999999999999998224, 73.54166665983869677, -8.660254037844389075 ) ) ;
#47340=LINE ( 'NONE', #63206, #7784 ) ;
#47341=CARTESIAN_POINT ( 'NONE',  ( -10.00000000000000000, 177.2916666666666856, -2.679491924311229845 ) ) ;
#47342=CARTESIAN_POINT ( 'NONE',  ( -3.673940397442060854E-16, 297.8125000034140157, -6.000000000000001776 ) ) ;
#47345=CARTESIAN_POINT ( 'NONE',  ( 11.35316468749999963, 146.3020833299193555, -3.042071309553165293 ) ) ;
#47349=CARTESIAN_POINT ( 'NONE',  ( 7.320508075688774596, 107.4999999931720254, -7.320508075688774596 ) ) ;
#47350=CARTESIAN_POINT ( 'NONE',  ( -2.485281374238217822, 294.1875000000000568, 6.000000000000357048 ) ) ;
#47351=EDGE_LOOP ( 'NONE', ( #58705, #26057, #20308, #61109 ) ) ;
#47352=CIRCLE ( 'NONE', #14813, 15.99999999999998579 ) ;
#47357=CARTESIAN_POINT ( 'NONE',  ( 10.00000000000000000, 41.66666665983870388, 2.679491924311236062 ) ) ;
#47368=CARTESIAN_POINT ( 'NONE',  ( -8.311093377946836114, 112.6562499965860127, -8.311093377946837890 ) ) ;
#47376=CARTESIAN_POINT ( 'NONE',  ( 9.832129032723416984, 110.3645833299193555, 5.676582343750006032 ) ) ;
#47380=CARTESIAN_POINT ( 'NONE',  ( 2.679491924311149464, 80.83333332650533976, 10.00000000000004619 ) ) ;
#47382=CARTESIAN_POINT ( 'NONE',  ( -5.000000000000005329, 200.2083333265053682, 8.660254037844387298 ) ) ;
#47384=AXIS2_PLACEMENT_3D ( 'NONE', #56679, #34055, #57050 ) ;
#47386=CARTESIAN_POINT ( 'NONE',  ( 5.676582343749993598, 105.2604166632526841, 9.832129032723422313 ) ) ;
#47390=EDGE_CURVE ( 'NONE', #70797, #57404, #27689, .T. ) ;
#47391=CARTESIAN_POINT ( 'NONE',  ( -3.042071309553164404, 12.55208332991935194, -11.35316468749999963 ) ) ;
#47392=ORIENTED_EDGE ( 'NONE', *, *, #22567, .F. ) ;
#47393=CARTESIAN_POINT ( 'NONE',  ( -10.00000000000001421, 137.7083333333333428, 2.679491924311226292 ) ) ;
#47398=CARTESIAN_POINT ( 'NONE',  ( -10.00000000000000355, 149.5833333265053682, 2.679491924311223183 ) ) ;
#47399=CARTESIAN_POINT ( 'NONE',  ( -4.088227598258586603E-16, 293.2031250017069510, -6.676582343750001591 ) ) ;
#47401=CARTESIAN_POINT ( 'NONE',  ( 11.35316468749999963, 206.3020833299193271, -3.042071309553165293 ) ) ;
#47410=CARTESIAN_POINT ( 'NONE',  ( 6.123233995736767268E-16, 26.25000000000000355, -10.00000000000000178 ) ) ;
#47418=CARTESIAN_POINT ( 'NONE',  ( 2.295000000000000373, 284.2799999999998590, 5.414445227811098604 ) ) ;
#47419=CARTESIAN_POINT ( 'NONE',  ( 6.676582343750002480, 295.0156250017069510, -2.765530957081997254 ) ) ;
#47423=ORIENTED_EDGE ( 'NONE', *, *, #66288, .T. ) ;
#47430=CARTESIAN_POINT ( 'NONE',  ( 8.311093377946834337, 100.4687499965860269, 8.311093377946839666 ) ) ;
#47439=CARTESIAN_POINT ( 'NONE',  ( -9.832129032723418760, 207.8645833299193555, -5.676582343750004256 ) ) ;
#47445=CARTESIAN_POINT ( 'NONE',  ( -5.676582343750006032, 179.4270833299193555, 9.832129032723418760 ) ) ;
#47452=CARTESIAN_POINT ( 'NONE',  ( -5.676582343750006032, 69.11458332991936970, 9.832129032723418760 ) ) ;
#47459=CARTESIAN_POINT ( 'NONE',  ( 8.311093377946834337, 75.15624999658602690, 8.311093377946839666 ) ) ;
#47464=CARTESIAN_POINT ( 'NONE',  ( -3.042071309553163960, 67.23958332991934128, -11.35316468749999963 ) ) ;
#47468=CARTESIAN_POINT ( 'NONE',  ( -7.320508075688778149, 149.9999999931720538, 7.320508075688769267 ) ) ;
#47471=CARTESIAN_POINT ( 'NONE',  ( 8.311093377946837890, 61.71874999658601979, -8.311093377946837890 ) ) ;
#47473=CARTESIAN_POINT ( 'NONE',  ( -9.832129032723420536, 193.6979166632526983, 5.676582343749997150 ) ) ;
#47478=CARTESIAN_POINT ( 'NONE',  ( 9.832129032723420536, 181.1979166632526983, -5.676582343749999815 ) ) ;
#47479=DIRECTION ( 'NONE',  ( -0.000000000000000000, 1.000000000000000000, -0.000000000000000000 ) ) ;
#47483=CARTESIAN_POINT ( 'NONE',  ( -9.832129032723420536, 169.0104166632526983, 5.676582343749997150 ) ) ;
#47486=CARTESIAN_POINT ( 'NONE',  ( 10.92737078412413609, 225.9999999999999147, -3.080083792328916825 ) ) ;
#47509=CARTESIAN_POINT ( 'NONE',  ( -7.320508075688773708, 113.7499999931720254, -7.320508075688774596 ) ) ;
#47511=CYLINDRICAL_SURFACE ( 'NONE', #11995, 10.00000000000000178 ) ;
#47513=CARTESIAN_POINT ( 'NONE',  ( -2.765530957081996810, 299.4218750017069510, -6.676582343750002480 ) ) ;
#47514=CARTESIAN_POINT ( 'NONE',  ( -7.320508075688773708, 131.8749999999999716, -7.320508075688774596 ) ) ;
#47530=CARTESIAN_POINT ( 'NONE',  ( 6.951808397369818766E-16, 22.03124999658601624, -11.35316468750000141 ) ) ;
#47531=CARTESIAN_POINT ( 'NONE',  ( 10.00000000000033040, 25.20833333333352755, -2.679491924311314666 ) ) ;
#47532=CARTESIAN_POINT ( 'NONE',  ( -11.35316468750000141, 223.8020833299192986, 3.042071309553159963 ) ) ;
#47533=FACE_BOUND ( 'NONE', #63821, .T. ) ;
#47540=CARTESIAN_POINT ( 'NONE',  ( -3.042071309553173730, 39.32291666325267698, 11.35316468749999785 ) ) ;
#47544=LINE ( 'NONE', #58163, #15410 ) ;
#47546=CARTESIAN_POINT ( 'NONE',  ( 5.676582343750001591, 36.61458332991934839, -9.832129032723420536 ) ) ;
#47548=CARTESIAN_POINT ( 'NONE',  ( -5.676582343750006032, 144.1145833299193555, 9.832129032723418760 ) ) ;
#47549=CARTESIAN_POINT ( 'NONE',  ( 8.660254037844389075, 117.2916666598386968, -5.000000000000000000 ) ) ;
#47553=ORIENTED_EDGE ( 'NONE', *, *, #57729, .F. ) ;
#47554=CARTESIAN_POINT ( 'NONE',  ( -9.832129032723420536, 4.010416663252683200, 5.676582343749997150 ) ) ;
#47556=CARTESIAN_POINT ( 'NONE',  ( 6.000000000000003553, 289.5625000000001137, -2.485281374238571761 ) ) ;
#47558=CARTESIAN_POINT ( 'NONE',  ( -5.676582343749998039, 142.4479166632526699, -9.832129032723420536 ) ) ;
#47567=CARTESIAN_POINT ( 'NONE',  ( -2.679491924311226292, 203.3333333265053966, -10.00000000000000178 ) ) ;
#47569=CARTESIAN_POINT ( 'NONE',  ( -8.311093377946836114, 92.96874999658602690, -8.311093377946837890 ) ) ;
#47587=CARTESIAN_POINT ( 'NONE',  ( 0.000000000000000000, 300.0000000000000000, 0.000000000000000000 ) ) ;
#47599=CARTESIAN_POINT ( 'NONE',  ( -5.000000000000005329, 88.33333333333332860, 8.660254037844387298 ) ) ;
#47602=CARTESIAN_POINT ( 'NONE',  ( -6.676582343750001591, 297.6093750017069510, 0.000000000000000000 ) ) ;
#47604=CARTESIAN_POINT ( 'NONE',  ( -7.320508075688773708, 143.7499999931719969, -7.320508075688774596 ) ) ;
#47612=CARTESIAN_POINT ( 'NONE',  ( -7.320508075688773708, 216.8750000000000000, -7.320508075688774596 ) ) ;
#47615=CARTESIAN_POINT ( 'NONE',  ( -9.832129032723418760, 178.1770833299193555, -5.676582343750004256 ) ) ;
#47623=CARTESIAN_POINT ( 'NONE',  ( 5.676582343750001591, 51.92708332991935549, -9.832129032723420536 ) ) ;
#47626=CARTESIAN_POINT ( 'NONE',  ( -5.676582343750006032, 219.4270833299193555, 9.832129032723418760 ) ) ;
#47630=CARTESIAN_POINT ( 'NONE',  ( -8.660254037844373087, 102.9166666666666572, 4.999999999999987566 ) ) ;
#47633=CARTESIAN_POINT ( 'NONE',  ( -7.320508075688778149, 74.99999999317202537, 7.320508075688769267 ) ) ;
#47641=VERTEX_POINT ( 'NONE', #8581 ) ;
#47642=CARTESIAN_POINT ( 'NONE',  ( -4.721056650415998313, 297.7343750017069510, 4.721056650416000089 ) ) ;
#47643=CARTESIAN_POINT ( 'NONE',  ( -5.000000000000011546, 143.3333333333333428, 8.660254037844397956 ) ) ;
#47645=CARTESIAN_POINT ( 'NONE',  ( -3.042071309553164404, 162.2395833299193271, -11.35316468749999963 ) ) ;
#47654=CARTESIAN_POINT ( 'NONE',  ( 6.951808397369818766E-16, 147.3437499965860411, -11.35316468750000141 ) ) ;
#47656=CARTESIAN_POINT ( 'NONE',  ( 6.000000000000003553, 298.6250000034140157, -2.485281374238571761 ) ) ;
#47658=CARTESIAN_POINT ( 'NONE',  ( -8.311093377946841443, 49.21874999658600558, 8.311093377946830785 ) ) ;
#47659=ORIENTED_EDGE ( 'NONE', *, *, #8136, .T. ) ;
#47663=CARTESIAN_POINT ( 'NONE',  ( -4.242640687119285658, 292.1875000034139589, 4.242640687119287435 ) ) ;
#47680=DIRECTION ( 'NONE',  ( -0.000000000000000000, 1.000000000000000000, -0.000000000000000000 ) ) ;
#47687=CARTESIAN_POINT ( 'NONE',  ( -2.679491924311235618, 53.54166666666667140, 10.00000000000000000 ) ) ;
#47689=CARTESIAN_POINT ( 'NONE',  ( -4.242640687119285658, 297.1250000000000000, 4.242640687119287435 ) ) ;
#47702=CARTESIAN_POINT ( 'NONE',  ( 2.679491924311228956, 181.0416666666666856, -10.00000000000000000 ) ) ;
#47706=CARTESIAN_POINT ( 'NONE',  ( -5.676582343750006032, 139.4270833299193555, 9.832129032723418760 ) ) ;
#47712=VERTEX_POINT ( 'NONE', #25544 ) ;
#47713=CARTESIAN_POINT ( 'NONE',  ( 11.35316468749999963, 6.302083329919350163, -3.042071309553165293 ) ) ;
#47720=CARTESIAN_POINT ( 'NONE',  ( 7.320508075688774596, 32.49999999317203248, -7.320508075688774596 ) ) ;
#47729=CARTESIAN_POINT ( 'NONE',  ( 3.042071309553159519, 109.7395833299193697, 11.35316468750000141 ) ) ;
#47733=DIRECTION ( 'NONE',  ( -0.000000000000000000, 1.000000000000000000, -0.000000000000000000 ) ) ;
#47737=CARTESIAN_POINT ( 'NONE',  ( -3.042071309553173730, 114.3229166632526841, 11.35316468749999785 ) ) ;
#47742=CARTESIAN_POINT ( 'NONE',  ( 5.000000000000001776, 202.7083333265053682, -8.660254037844389075 ) ) ;
#47743=EDGE_CURVE ( 'NONE', #40340, #11129, #65216, .T. ) ;
#47746=CARTESIAN_POINT ( 'NONE',  ( 3.042071309553167513, 102.1354166632526841, -11.35316468749999785 ) ) ;
#47751=CARTESIAN_POINT ( 'NONE',  ( -5.676582343750006032, 9.427083329919350163, 9.832129032723418760 ) ) ;
#47752=VERTEX_POINT ( 'NONE', #20254 ) ;
#47753=DIRECTION ( 'NONE',  ( 0.000000000000000000, 0.000000000000000000, 1.000000000000000000 ) ) ;
#47755=CARTESIAN_POINT ( 'NONE',  ( 11.27292232226671054, 225.9999999999999432, 1.347431162485829281 ) ) ;
#47758=CARTESIAN_POINT ( 'NONE',  ( 2.679491924326688590, 201.0416666666652930, -9.999999999991077360 ) ) ;
#47759=CARTESIAN_POINT ( 'NONE',  ( 4.721056650415999201, 291.0781250017069510, -4.721056650415999201 ) ) ;
#47761=CARTESIAN_POINT ( 'NONE',  ( -3.042071309553163960, 217.5520833299193555, -11.35316468749999963 ) ) ;
#47775=ORIENTED_EDGE ( 'NONE', *, *, #19546, .T. ) ;
#47778=DIRECTION ( 'NONE',  ( 0.000000000000000000, 0.000000000000000000, 1.000000000000000000 ) ) ;
#47781=CARTESIAN_POINT ( 'NONE',  ( -2.295000000000000373, 261.4319999999996753, 5.413230550752030190 ) ) ;
#47782=CARTESIAN_POINT ( 'NONE',  ( -6.676582343749999815, 290.5156250017069510, 2.765530957082001251 ) ) ;
#47794=CARTESIAN_POINT ( 'NONE',  ( 6.951808397369818766E-16, 102.3437499965860127, -11.35316468750000141 ) ) ;
#47795=CARTESIAN_POINT ( 'NONE',  ( -8.660254037844383745, 122.0833333333333428, -5.000000000000003553 ) ) ;
#47800=ORIENTED_EDGE ( 'NONE', *, *, #70313, .F. ) ;
#47802=CARTESIAN_POINT ( 'NONE',  ( -5.000000000000005329, 180.2083333265053682, 8.660254037844387298 ) ) ;
#47803=CARTESIAN_POINT ( 'NONE',  ( -3.042071309553173730, 219.3229166632526699, 11.35316468749999785 ) ) ;
#47808=CARTESIAN_POINT ( 'NONE',  ( 5.676582343749993598, 195.2604166632526983, 9.832129032723422313 ) ) ;
#47815=CARTESIAN_POINT ( 'NONE',  ( -11.35316468749999785, 73.07291666325268409, -3.042071309553167513 ) ) ;
#47819=CARTESIAN_POINT ( 'NONE',  ( 0.000000000000000000, 237.9999999999999716, 0.000000000000000000 ) ) ;
#47823=CARTESIAN_POINT ( 'NONE',  ( 11.35316468749999785, 80.57291666325268409, 3.042071309553174174 ) ) ;
#47830=CARTESIAN_POINT ( 'NONE',  ( -8.311093377946836114, 72.65624999658601268, -8.311093377946837890 ) ) ;
#47833=CARTESIAN_POINT ( 'NONE',  ( -7.320508075688778149, 164.9999999931720822, 7.320508075688769267 ) ) ;
#47836=CARTESIAN_POINT ( 'NONE',  ( -2.085542519210945728E-15, 64.84374999658601268, 11.35316468750000141 ) ) ;
#47837=( BOUNDED_CURVE ( )  B_SPLINE_CURVE ( 2, ( #43898, #49554, #38245, #14087, #49928, #31462, #72943, #65413, #59768, #8077, #31078, #54106, #60124 ),
 .UNSPECIFIED., .F., .F. ) 
 B_SPLINE_CURVE_WITH_KNOTS ( ( 3, 2, 2, 2, 2, 2, 3 ),
 ( 2.527683269455331949, 2.532917274740161151, 2.538151280024989909, 2.543385285309819110, 2.548619290594648312, 2.553853295879477070, 2.559087301164306272 ),
 .UNSPECIFIED. ) 
 CURVE ( )  GEOMETRIC_REPRESENTATION_ITEM ( )  RATIONAL_B_SPLINE_CURVE ( ( 1.000000000000219158, 0.9659258262888491542, 1.000000000000000000, 0.9659258262890684232, 1.000000000000000000, 0.9659258262890684232, 1.000000000000000000, 0.9659258262890684232, 1.000000000000000000, 0.9659258262890684232, 1.000000000000000000, 0.9659258262890705327, 0.9999999999999978906 ) ) 
 REPRESENTATION_ITEM ( '' )  );
#47839=CARTESIAN_POINT ( 'NONE',  ( 3.042071309553167069, 201.8229166632526415, -11.35316468749999785 ) ) ;
#47846=CARTESIAN_POINT ( 'NONE',  ( -11.35316468749999785, 188.0729166632526983, -3.042071309553167957 ) ) ;
#47850=CARTESIAN_POINT ( 'NONE',  ( -4.999999999999998224, 188.5416666598387110, -8.660254037844389075 ) ) ;
#47852=CARTESIAN_POINT ( 'NONE',  ( 11.35316468749999785, 180.8854166632526699, 3.042071309553174174 ) ) ;
#47857=CARTESIAN_POINT ( 'NONE',  ( -5.000000000000005329, 3.333333333333333481, 8.660254037844387298 ) ) ;
#47858=VECTOR ( 'NONE', #18297, 1000.000000000000000 ) ;
#47863=CARTESIAN_POINT ( 'NONE',  ( -7.320508075688779925, 188.1250000000000000, 7.320508075688771932 ) ) ;
#47868=CARTESIAN_POINT ( 'NONE',  ( 6.326249034914468552E-13, 178.7500000000000853, 10.00000000000000533 ) ) ;
#47872=CARTESIAN_POINT ( 'NONE',  ( -7.320508075688907823, 156.8750000000001137, -7.320508075688907823 ) ) ;
#47877=ORIENTED_EDGE ( 'NONE', *, *, #2363, .T. ) ;
#47879=CARTESIAN_POINT ( 'NONE',  ( -8.660254037844390851, 114.7916666598387110, 4.999999999999998224 ) ) ;
#47883=CARTESIAN_POINT ( 'NONE',  ( 2.765530957082001251, 292.9218750017069510, 6.676582343749999815 ) ) ;
#47884=CARTESIAN_POINT ( 'NONE',  ( -2.679491924311235618, 128.5416666666666288, 10.00000000000000000 ) ) ;
#47887=CARTESIAN_POINT ( 'NONE',  ( 4.242640687119287435, 290.4375000034140157, 4.242640687119285658 ) ) ;
#47895=CARTESIAN_POINT ( 'NONE',  ( -5.000000000000005329, 133.3333333333333712, 8.660254037844387298 ) ) ;
#47900=CARTESIAN_POINT ( 'NONE',  ( 3.042071309553159519, 34.73958332991934839, 11.35316468750000141 ) ) ;
#47902=CARTESIAN_POINT ( 'NONE',  ( -7.320508075688773708, 3.749999993172032475, -7.320508075688774596 ) ) ;
#47905=ORIENTED_EDGE ( 'NONE', *, *, #6856, .F. ) ;
#47906=DIRECTION ( 'NONE',  ( 0.000000000000000000, 0.000000000000000000, 1.000000000000000000 ) ) ;
#47908=CARTESIAN_POINT ( 'NONE',  ( -5.676582343749998039, 37.44791666325267698, -9.832129032723420536 ) ) ;
#47911=CARTESIAN_POINT ( 'NONE',  ( -10.00000000000000888, 152.5000000000000284, -1.224646799147354440E-15 ) ) ;
#47914=CARTESIAN_POINT ( 'NONE',  ( -9.832129032723420536, 33.69791666325268409, 5.676582343749997150 ) ) ;
#47916=CARTESIAN_POINT ( 'NONE',  ( -11.35316468750000141, 148.4895833299193555, 3.042071309553159963 ) ) ;
#47917=CARTESIAN_POINT ( 'NONE',  ( -5.000000000000005329, 115.2083333265053682, 8.660254037844387298 ) ) ;
#47922=CARTESIAN_POINT ( 'NONE',  ( 8.311093377946834337, 20.46874999658601624, 8.311093377946839666 ) ) ;
#47927=CARTESIAN_POINT ( 'NONE',  ( 5.676582343750001591, 151.6145833299193555, -9.832129032723420536 ) ) ;
#47933=ORIENTED_EDGE ( 'NONE', *, *, #52505, .F. ) ;
#47935=CARTESIAN_POINT ( 'NONE',  ( -3.673940397442060854E-16, 291.8125000034140157, -6.000000000000001776 ) ) ;
#47936=CARTESIAN_POINT ( 'NONE',  ( -3.042071309553173730, 99.63541666325268409, 11.35316468749999785 ) ) ;
#47950=CARTESIAN_POINT ( 'NONE',  ( -8.660254037844390851, 159.7916666598387110, 4.999999999999998224 ) ) ;
#47954=VERTEX_POINT ( 'NONE', #62122 ) ;
#47960=CARTESIAN_POINT ( 'NONE',  ( -10.00000000000000355, 224.5833333265053398, 2.679491924311223183 ) ) ;
#47972=CARTESIAN_POINT ( 'NONE',  ( -7.320508075688778149, 98.12499999999998579, 7.320508075688769267 ) ) ;
#47974=CARTESIAN_POINT ( 'NONE',  ( -2.765530957081998586, 296.7968750017070079, 6.676582343750001591 ) ) ;
#47977=CARTESIAN_POINT ( 'NONE',  ( -8.660254037844390851, 144.7916666598387110, 4.999999999999998224 ) ) ;
#47980=CARTESIAN_POINT ( 'NONE',  ( -10.00000000000000178, 104.3749999931720396, -1.224646799147353454E-15 ) ) ;
#47985=CARTESIAN_POINT ( 'NONE',  ( 8.660254037844385522, 214.5833333333333428, 5.000000000000005329 ) ) ;
#47987=CARTESIAN_POINT ( 'NONE',  ( -11.35316468750000141, 183.8020833299193271, 3.042071309553159963 ) ) ;
#47995=CARTESIAN_POINT ( 'NONE',  ( 9.832129032723420536, 51.51041666325269119, -5.676582343749999815 ) ) ;
#47997=CARTESIAN_POINT ( 'NONE',  ( 6.951808397369818766E-16, 217.3437499965860411, -11.35316468750000141 ) ) ;
#48003=CARTESIAN_POINT ( 'NONE',  ( -11.35316468750000141, 108.2812499965860269, -1.390361679473963753E-15 ) ) ;
#48005=CARTESIAN_POINT ( 'NONE',  ( 2.679491924311222739, 80.83333332650535397, 10.00000000000000355 ) ) ;
#48011=EDGE_LOOP ( 'NONE', ( #21276, #51765, #12722, #50663 ) ) ;
#48012=CARTESIAN_POINT ( 'NONE',  ( 6.676582343750001591, 295.1093750017069510, -8.176455196517173205E-16 ) ) ;
#48014=CARTESIAN_POINT ( 'NONE',  ( 11.35316468750000141, 165.7812499965860411, 0.000000000000000000 ) ) ;
#48015=CARTESIAN_POINT ( 'NONE',  ( 10.00000000000000178, 1.874999993172032697, 0.000000000000000000 ) ) ;
#48024=CARTESIAN_POINT ( 'NONE',  ( -11.35316468749999785, 148.3854166632526983, -3.042071309553167957 ) ) ;
#48026=CARTESIAN_POINT ( 'NONE',  ( -2.485281374238268004, 291.1875000000000568, 6.000000000000304645 ) ) ;
#48028=CARTESIAN_POINT ( 'NONE',  ( -8.311093377946836114, 42.96874999658601268, -8.311093377946837890 ) ) ;
#48035=CARTESIAN_POINT ( 'NONE',  ( -4.242640687119285658, 293.1875000034139589, 4.242640687119287435 ) ) ;
#48040=( BOUNDED_CURVE ( )  B_SPLINE_CURVE ( 2, ( #62220, #33578, #26773, #27515, #16177, #49791, #50526, #39220, #43753, #4155, #73541, #67886, #21114 ),
 .UNSPECIFIED., .F., .F. ) 
 B_SPLINE_CURVE_WITH_KNOTS ( ( 3, 2, 2, 2, 2, 2, 3 ),
 ( 2.559087301164306272, 2.564320718348052530, 2.569554135531799233, 2.574787552715545935, 2.580020969899292194, 2.585254387083038896, 2.590487804266785599 ),
 .UNSPECIFIED. ) 
 CURVE ( )  GEOMETRIC_REPRESENTATION_ITEM ( )  RATIONAL_B_SPLINE_CURVE ( ( 1.000000000000001998, 0.9659258262890662028, 1.000000000000000000, 0.9659258262890683122, 1.000000000000000000, 0.9659258262890683122, 1.000000000000000000, 0.9659258262890683122, 1.000000000000000000, 0.9659258262890683122, 1.000000000000000000, 0.9659258262890704216, 0.9999999999999978906 ) ) 
 REPRESENTATION_ITEM ( '' )  );
#48053=VERTEX_POINT ( 'NONE', #31967 ) ;
#48060=CARTESIAN_POINT ( 'NONE',  ( -2.679491924311225848, 56.45833333333333570, -10.00000000000000178 ) ) ;
#48063=CARTESIAN_POINT ( 'NONE',  ( -6.000000000000000888, 298.0625000000000568, 2.485281374238575758 ) ) ;
#48069=CARTESIAN_POINT ( 'NONE',  ( 7.320508075688759497, 89.37500000000001421, 7.320508075688763050 ) ) ;
#48074=CARTESIAN_POINT ( 'NONE',  ( 2.679491924311228956, 176.0416666666666572, -10.00000000000000000 ) ) ;
#48078=CARTESIAN_POINT ( 'NONE',  ( -3.042071309553164404, 147.5520833299193271, -11.35316468749999963 ) ) ;
#48084=CARTESIAN_POINT ( 'NONE',  ( -3.042071309553173730, 14.63541666325268231, 11.35316468749999785 ) ) ;
#48086=CARTESIAN_POINT ( 'NONE',  ( 1.567784982238203817E-13, 113.7500000000000284, 10.00000000000000533 ) ) ;
#48090=CARTESIAN_POINT ( 'NONE',  ( -8.660254037844387298, 38.95833332650536818, -5.000000000000004441 ) ) ;
#48101=CARTESIAN_POINT ( 'NONE',  ( 8.311093377946837890, 121.4062499965860127, -8.311093377946837890 ) ) ;
#48109=CARTESIAN_POINT ( 'NONE',  ( -9.832129032723418760, 107.8645833299193555, -5.676582343750004256 ) ) ;
#48115=CARTESIAN_POINT ( 'NONE',  ( -7.320508075688773708, 203.7499999931720538, -7.320508075688774596 ) ) ;
#48119=CARTESIAN_POINT ( 'NONE',  ( 11.35316468749999785, 105.8854166632526983, 3.042071309553174174 ) ) ;
#48123=CARTESIAN_POINT ( 'NONE',  ( -3.042071309553173730, 4.635416663252684089, 11.35316468749999785 ) ) ;
#48124=ORIENTED_EDGE ( 'NONE', *, *, #28849, .T. ) ;
#48125=CARTESIAN_POINT ( 'NONE',  ( 7.320508075688771044, 181.2499999931720254, 7.320508075688775484 ) ) ;
#48129=EDGE_CURVE ( 'NONE', #48555, #3208, #39991, .T. ) ;
#48132=CARTESIAN_POINT ( 'NONE',  ( -4.721056650415998313, 294.5781250017069510, 4.721056650416000089 ) ) ;
#48149=DIRECTION ( 'NONE',  ( 0.000000000000000000, 0.000000000000000000, 1.000000000000000000 ) ) ;
#48152=CARTESIAN_POINT ( 'NONE',  ( 4.721056650416000089, 292.8281250017069510, 4.721056650415999201 ) ) ;
#48155=CARTESIAN_POINT ( 'NONE',  ( 10.00000000000000000, 136.6666666598387110, 2.679491924311235618 ) ) ;
#48157=ORIENTED_EDGE ( 'NONE', *, *, #11739, .T. ) ;
#48167=CARTESIAN_POINT ( 'NONE',  ( 8.311093377946837890, 106.7187499965860269, -8.311093377946837890 ) ) ;
#48168=CARTESIAN_POINT ( 'NONE',  ( -3.171697045051319909E-12, 121.2500000000002558, -10.00000000000000178 ) ) ;
#48176=CARTESIAN_POINT ( 'NONE',  ( 3.042071309553159519, 214.7395833299193271, 11.35316468750000141 ) ) ;
#48181=CARTESIAN_POINT ( 'NONE',  ( -8.311093377946836114, 187.9687499965860411, -8.311093377946837890 ) ) ;
#48187=CARTESIAN_POINT ( 'NONE',  ( -3.042071309553164404, 87.23958332991934128, -11.35316468749999963 ) ) ;
#48188=VERTEX_POINT ( 'NONE', #5534 ) ;
#48193=CARTESIAN_POINT ( 'NONE',  ( 3.042071309553159519, 79.73958332991934128, 11.35316468750000141 ) ) ;
#48199=CARTESIAN_POINT ( 'NONE',  ( 3.042071309553167513, 76.82291666325269830, -11.35316468749999785 ) ) ;
#48203=CARTESIAN_POINT ( 'NONE',  ( 6.123233995736767268E-16, 173.1249999931720538, -10.00000000000000178 ) ) ;
#48206=CARTESIAN_POINT ( 'NONE',  ( 5.676582343750001591, 56.92708332991935549, -9.832129032723420536 ) ) ;
#48208=CARTESIAN_POINT ( 'NONE',  ( -11.35316468750000141, 193.4895833299193271, 3.042071309553159963 ) ) ;
#48210=DIRECTION ( 'NONE',  ( 0.000000000000000000, 0.000000000000000000, 1.000000000000000000 ) ) ;
#48214=CARTESIAN_POINT ( 'NONE',  ( -5.676582343749998039, 187.4479166632526983, -9.832129032723420536 ) ) ;
#48219=ADVANCED_FACE ( 'NONE', ( #33850 ), #16829, .F. ) ;
#48220=CARTESIAN_POINT ( 'NONE',  ( 11.35316468749999963, 181.3020833299193271, -3.042071309553165293 ) ) ;
#48230=EDGE_CURVE ( 'NONE', #63519, #70220, #6651, .T. ) ;
#48251=CARTESIAN_POINT ( 'NONE',  ( 0.000000000000000000, 300.0000000000000000, 6.000000000000001776 ) ) ;
#48253=CARTESIAN_POINT ( 'NONE',  ( 6.676582343750001591, 296.1093750017069510, -8.176455196517173205E-16 ) ) ;
#48254=CARTESIAN_POINT ( 'NONE',  ( -8.660254037844387298, 152.0833333333333428, -5.000000000000004441 ) ) ;
#48266=CARTESIAN_POINT ( 'NONE',  ( 2.030339228148215693E-11, 166.2499999999984368, -10.00000000000000178 ) ) ;
#48271=CARTESIAN_POINT ( 'NONE',  ( -11.35316468750000141, 48.48958332991934839, 3.042071309553159963 ) ) ;
#48272=( BOUNDED_CURVE ( )  B_SPLINE_CURVE ( 2, ( #54453, #2761, #8793, #49521, #66494, #72541, #54827, #3136, #20847, #43865, #66880, #15185, #2017 ),
 .UNSPECIFIED., .F., .F. ) 
 B_SPLINE_CURVE_WITH_KNOTS ( ( 3, 2, 2, 2, 2, 2, 3 ),
 ( 2.716084159200326198, 2.721317171148036618, 2.726550183095747037, 2.731783195043457457, 2.737016206991167877, 2.742249218938878297, 2.747482230802302361 ),
 .UNSPECIFIED. ) 
 CURVE ( )  GEOMETRIC_REPRESENTATION_ITEM ( )  RATIONAL_B_SPLINE_CURVE ( ( 1.000000000000004219, 0.9659258262890640934, 1.000000000000000000, 0.9659258262890683122, 1.000000000000000000, 0.9659258262890683122, 1.000000000000000000, 0.9659258262890683122, 1.000000000000000000, 0.9659258262890683122, 1.000000000000000000, 0.9659258262890683122, 1.000000000000000000 ) ) 
 REPRESENTATION_ITEM ( '' )  );
#48273=CARTESIAN_POINT ( 'NONE',  ( 8.660254037844390851, 150.4166666666666572, -5.000000000000001776 ) ) ;
#48274=( BOUNDED_CURVE ( )  B_SPLINE_CURVE ( 2, ( #21388, #26675, #62128, #67423, #15722, #38765, #16461, #73819, #61010, #33482, #61764, #56484, #4801 ),
 .UNSPECIFIED., .F., .F. ) 
 B_SPLINE_CURVE_WITH_KNOTS ( ( 3, 2, 2, 2, 2, 2, 3 ),
 ( 0.8858695652173912416, 0.8876811594202896893, 0.8894927536231882481, 0.8913043478260869179, 0.8931159420289854767, 0.8949275362318840354, 0.8967391304347825942 ),
 .UNSPECIFIED. ) 
 CURVE ( )  GEOMETRIC_REPRESENTATION_ITEM ( )  RATIONAL_B_SPLINE_CURVE ( ( 1.000000000000001998, 0.9659258262890662028, 1.000000000000000000, 0.9659258262890683122, 1.000000000000000000, 0.9659258262890683122, 1.000000000000000000, 0.9659258262890683122, 1.000000000000000000, 0.9659258262890683122, 1.000000000000000000, 0.9659258262890683122, 1.000000000000000000 ) ) 
 REPRESENTATION_ITEM ( '' )  );
#48275=CARTESIAN_POINT ( 'NONE',  ( 2.679491924311222739, 5.833333326505364624, 10.00000000000000355 ) ) ;
#48279=CARTESIAN_POINT ( 'NONE',  ( -1.836970198721029983E-15, 130.6249999931720254, 10.00000000000000178 ) ) ;
#48281=CARTESIAN_POINT ( 'NONE',  ( 5.676582343750001591, 31.61458332991935194, -9.832129032723420536 ) ) ;
#48287=CARTESIAN_POINT ( 'NONE',  ( 9.832129032723416984, 30.36458332991935194, 5.676582343750006032 ) ) ;
#48289=CARTESIAN_POINT ( 'NONE',  ( -9.832129032723418760, 147.8645833299193555, -5.676582343750004256 ) ) ;
#48290=CARTESIAN_POINT ( 'NONE',  ( 10.00000000000000178, 131.8749999931720254, 0.000000000000000000 ) ) ;
#48294=CARTESIAN_POINT ( 'NONE',  ( 2.679491924311222739, 20.83333332650536462, 10.00000000000000355 ) ) ;
#48295=CARTESIAN_POINT ( 'NONE',  ( -3.042071309553163960, 27.55208332991935194, -11.35316468749999963 ) ) ;
#48300=CARTESIAN_POINT ( 'NONE',  ( -5.676582343749998039, 152.4479166632526983, -9.832129032723420536 ) ) ;
#48310=CARTESIAN_POINT ( 'NONE',  ( -3.042071309553164404, 107.5520833299193555, -11.35316468749999963 ) ) ;
#48329=CARTESIAN_POINT ( 'NONE',  ( -5.000000000000170530, 23.33333333333352400, 8.660254037844671515 ) ) ;
#48342=CARTESIAN_POINT ( 'NONE',  ( -10.00000000000000355, 107.7083333333333428, 2.679491924311223183 ) ) ;
#48344=CARTESIAN_POINT ( 'NONE',  ( -6.676582343750001591, 295.6093750017069510, 0.000000000000000000 ) ) ;
#48354=CARTESIAN_POINT ( 'NONE',  ( 7.320508075688771044, 219.3750000000000000, 7.320508075688775484 ) ) ;
#48356=CARTESIAN_POINT ( 'NONE',  ( 8.311093377946837890, 191.7187499965860127, -8.311093377946837890 ) ) ;
#48359=CARTESIAN_POINT ( 'NONE',  ( 0.000000000000000000, 300.0000000000000000, 0.000000000000000000 ) ) ;
#48362=VERTEX_POINT ( 'NONE', #36796 ) ;
#48366=CARTESIAN_POINT ( 'NONE',  ( -2.085542519210945728E-15, 44.84374999658602690, 11.35316468750000141 ) ) ;
#48368=CARTESIAN_POINT ( 'NONE',  ( 5.676582343750001591, 221.9270833299193555, -9.832129032723420536 ) ) ;
#48374=CARTESIAN_POINT ( 'NONE',  ( 3.042071309553159519, 104.7395833299193555, 11.35316468750000141 ) ) ;
#48377=CARTESIAN_POINT ( 'NONE',  ( 10.00000000000000178, 87.08333332650535397, -2.679491924311226736 ) ) ;
#48383=CARTESIAN_POINT ( 'NONE',  ( -6.101298592596269721, 226.0000000000000000, 7.950093002584347701 ) ) ;
#48385=CARTESIAN_POINT ( 'NONE',  ( 2.765530957082001251, 294.9218750017070647, 6.676582343750000703 ) ) ;
#48386=CARTESIAN_POINT ( 'NONE',  ( 10.00000000000000178, 187.0833333265053398, -2.679491924311226736 ) ) ;
#48387=CARTESIAN_POINT ( 'NONE',  ( -11.35316468749999785, 163.0729166632526415, -3.042071309553167513 ) ) ;
#48390=CARTESIAN_POINT ( 'NONE',  ( -10.00000000000004441, 192.2916666666666856, -2.679491924311241835 ) ) ;
#48396=CARTESIAN_POINT ( 'NONE',  ( -11.35316468750000141, 138.8020833299193271, 3.042071309553159963 ) ) ;
#48398=CARTESIAN_POINT ( 'NONE',  ( -4.242640687119285658, 291.1249999999999432, 4.242640687119287435 ) ) ;
#48400=CARTESIAN_POINT ( 'NONE',  ( -11.35316468749999785, 68.38541666325268409, -3.042071309553167513 ) ) ;
#48401=ORIENTED_EDGE ( 'NONE', *, *, #28849, .F. ) ;
#48405=ORIENTED_EDGE ( 'NONE', *, *, #21321, .F. ) ;
#48407=CARTESIAN_POINT ( 'NONE',  ( 6.000000000000003553, 293.5000000034140157, 2.485281374238571317 ) ) ;
#48412=( BOUNDED_CURVE ( )  B_SPLINE_CURVE ( 2, ( #19823, #14528, #30785, #48125, #53805, #31149, #42829, #54181, #26219, #65847, #31528, #59467, #14157 ),
 .UNSPECIFIED., .F., .F. ) 
 B_SPLINE_CURVE_WITH_KNOTS ( ( 3, 2, 2, 2, 2, 2, 3 ),
 ( 0.7771739130434782705, 0.7789855072463768293, 0.7807971014492754991, 0.7826086956521740579, 0.7844202898550726166, 0.7862318840579712864, 0.7880434782608697342 ),
 .UNSPECIFIED. ) 
 CURVE ( )  GEOMETRIC_REPRESENTATION_ITEM ( )  RATIONAL_B_SPLINE_CURVE ( ( 1.000000000000000000, 0.9659258262890683122, 1.000000000000000000, 0.9659258262890683122, 1.000000000000000000, 0.9659258262890683122, 1.000000000000000000, 0.9659258262890683122, 1.000000000000000000, 0.9659258262890683122, 1.000000000000000000, 0.9659258262890640934, 1.000000000000004219 ) ) 
 REPRESENTATION_ITEM ( '' )  );
#48415=EDGE_LOOP ( 'NONE', ( #25910, #65094 ) ) ;
#48422=CARTESIAN_POINT ( 'NONE',  ( -3.673940397442060854E-16, 294.7500000000000000, -6.000000000000001776 ) ) ;
#48426=VERTEX_POINT ( 'NONE', #18333 ) ;
#48430=CARTESIAN_POINT ( 'NONE',  ( 8.660254037844385522, 64.58333333333334281, 5.000000000000005329 ) ) ;
#48432=CARTESIAN_POINT ( 'NONE',  ( -2.485281374238571761, 295.8125000000000000, -6.000000000000003553 ) ) ;
#48437=EDGE_CURVE ( 'NONE', #26901, #44928, #24395, .T. ) ;
#48444=CARTESIAN_POINT ( 'NONE',  ( -8.660254037844390851, 177.9166666666666572, 4.999999999999998224 ) ) ;
#48445=PLANE ( 'NONE',  #59574 ) ;
#48448=CARTESIAN_POINT ( 'NONE',  ( 8.311093377946834337, 155.4687499965859843, 8.311093377946839666 ) ) ;
#48450=CARTESIAN_POINT ( 'NONE',  ( 10.00000000000000178, 27.08333332650536462, -2.679491924311226736 ) ) ;
#48452=CARTESIAN_POINT ( 'NONE',  ( -2.679491924311226292, 83.33333332650536818, -10.00000000000000178 ) ) ;
#48453=CARTESIAN_POINT ( 'NONE',  ( -6.000000000000003553, 293.9374999999998863, -2.485281374238571317 ) ) ;
#48455=CARTESIAN_POINT ( 'NONE',  ( 5.676582343749993598, 10.26041666325268409, 9.832129032723422313 ) ) ;
#48461=CARTESIAN_POINT ( 'NONE',  ( -2.679491924311235618, 35.41666665983870388, 10.00000000000000000 ) ) ;
#48466=CARTESIAN_POINT ( 'NONE',  ( 4.242640687119287435, 291.4375000034140157, 4.242640687119285658 ) ) ;
#48467=DIRECTION ( 'NONE',  ( 0.000000000000000000, 0.000000000000000000, 1.000000000000000000 ) ) ;
#48473=CARTESIAN_POINT ( 'NONE',  ( -11.35316468750000141, 133.2812499965860127, -1.390361679473963753E-15 ) ) ;
#48483=CARTESIAN_POINT ( 'NONE',  ( 8.311093377946837890, 106.4062499965860127, -8.311093377946837890 ) ) ;
#48485=CARTESIAN_POINT ( 'NONE',  ( 10.00000000000000000, 146.6666666598386826, 2.679491924311235618 ) ) ;
#48486=ORIENTED_EDGE ( 'NONE', *, *, #32847, .T. ) ;
#48489=CARTESIAN_POINT ( 'NONE',  ( -5.676582343749998039, 107.7604166632526841, -9.832129032723420536 ) ) ;
#48492=( BOUNDED_CURVE ( )  B_SPLINE_CURVE ( 2, ( #44232, #49124, #10272, #61203, #20449, #9899, #9534, #56297, #44602, #37448, #3872, #66480, #43849 ),
 .UNSPECIFIED., .F., .F. ) 
 B_SPLINE_CURVE_WITH_KNOTS ( ( 3, 2, 2, 2, 2, 2, 3 ),
 ( 0.8532608695652174058, 0.8550724637681159646, 0.8568840579710145233, 0.8586956521739130821, 0.8605072463768116409, 0.8623188405797101996, 0.8641304347826086474 ),
 .UNSPECIFIED. ) 
 CURVE ( )  GEOMETRIC_REPRESENTATION_ITEM ( )  RATIONAL_B_SPLINE_CURVE ( ( 1.000000000000000000, 0.9659258262890683122, 1.000000000000000000, 0.9659258262890683122, 1.000000000000000000, 0.9659258262890683122, 1.000000000000000000, 0.9659258262890683122, 1.000000000000000000, 0.9659258262890683122, 1.000000000000000000, 0.9659258262890683122, 1.000000000000000000 ) ) 
 REPRESENTATION_ITEM ( '' )  );
#48494=CARTESIAN_POINT ( 'NONE',  ( -9.832129032723420536, 19.01041666325268409, 5.676582343749997150 ) ) ;
#48497=CARTESIAN_POINT ( 'NONE',  ( 10.00000000000000000, 116.6666666598387110, 2.679491924311235618 ) ) ;
#48500=CARTESIAN_POINT ( 'NONE',  ( 4.721056650416000089, 293.8281250017069510, 4.721056650415999201 ) ) ;
#48503=CARTESIAN_POINT ( 'NONE',  ( 5.676582343750001591, 216.9270833299193555, -9.832129032723420536 ) ) ;
#48504=CARTESIAN_POINT ( 'NONE',  ( 8.311093377946834337, 135.4687499965860411, 8.311093377946839666 ) ) ;
#48514=CARTESIAN_POINT ( 'NONE',  ( -5.000000000000047073, 171.6666666666667425, -8.660254037844470787 ) ) ;
#48519=FACE_OUTER_BOUND ( 'NONE', #8038, .T. ) ;
#48522=CARTESIAN_POINT ( 'NONE',  ( -4.721056650415998313, 293.5781250017069510, 4.721056650416000089 ) ) ;
#48528=CARTESIAN_POINT ( 'NONE',  ( 6.123233995736767268E-16, 168.1249999931720538, -10.00000000000000178 ) ) ;
#48534=CARTESIAN_POINT ( 'NONE',  ( -11.35316468750000141, 118.8020833299193413, 3.042071309553159963 ) ) ;
#48542=LINE ( 'NONE', #19137, #63377 ) ;
#48543=CARTESIAN_POINT ( 'NONE',  ( 8.311093377946837890, 216.4062499965860127, -8.311093377946837890 ) ) ;
#48547=CARTESIAN_POINT ( 'NONE',  ( 11.35316468750000141, 191.0937499965860127, 0.000000000000000000 ) ) ;
#48549=CARTESIAN_POINT ( 'NONE',  ( 7.247622103906887325, 225.9999999999999147, 7.486376043179081563 ) ) ;
#48553=FACE_OUTER_BOUND ( 'NONE', #35520, .T. ) ;
#48554=CARTESIAN_POINT ( 'NONE',  ( -11.35316468750000141, 78.48958332991935549, 3.042071309553159963 ) ) ;
#48555=VERTEX_POINT ( 'NONE', #8485 ) ;
#48556=CARTESIAN_POINT ( 'NONE',  ( 10.00000000000001066, 140.0000000000000284, 0.000000000000000000 ) ) ;
#48560=CARTESIAN_POINT ( 'NONE',  ( -11.35316468750000141, 88.48958332991934128, 3.042071309553159963 ) ) ;
#48563=EDGE_CURVE ( 'NONE', #18004, #27943, #8970, .T. ) ;
#48566=CARTESIAN_POINT ( 'NONE',  ( 7.320508075688796801, 75.62500000000002842, -7.320508075688796801 ) ) ;
#48568=CARTESIAN_POINT ( 'NONE',  ( -8.311093377946841443, 73.90624999658601268, 8.311093377946834337 ) ) ;
#48571=CARTESIAN_POINT ( 'NONE',  ( -10.00000000000000355, 174.5833333265053682, 2.679491924311223183 ) ) ;
#48574=CARTESIAN_POINT ( 'NONE',  ( -11.35316468749999785, 63.38541666325269119, -3.042071309553167957 ) ) ;
#48575=CARTESIAN_POINT ( 'NONE',  ( 4.721056650415999201, 295.0781250017069510, -4.721056650415999201 ) ) ;
#48577=CARTESIAN_POINT ( 'NONE',  ( 11.35316468749999963, 200.9895833299193839, -3.042071309553165293 ) ) ;
#48583=CARTESIAN_POINT ( 'NONE',  ( 9.832129032723416984, 190.3645833299193839, 5.676582343750006032 ) ) ;
#48587=FACE_OUTER_BOUND ( 'NONE', #72656, .T. ) ;
#48588=EDGE_CURVE ( 'NONE', #56250, #3815, #60962, .T. ) ;
#48590=CARTESIAN_POINT ( 'NONE',  ( 9.832129032723420536, 181.5104166632526699, -5.676582343749999815 ) ) ;
#48594=CARTESIAN_POINT ( 'NONE',  ( -9.999999999999996447, 92.70833333333332860, 2.679491924311221407 ) ) ;
#48612=VERTEX_POINT ( 'NONE', #14502 ) ;
#48618=CARTESIAN_POINT ( 'NONE',  ( -2.085542519210945728E-15, 64.84374999658601268, 11.35316468750000141 ) ) ;
#48619=CARTESIAN_POINT ( 'NONE',  ( 10.00000000000000178, 92.08333332650536818, -2.679491924311226736 ) ) ;
#48623=CARTESIAN_POINT ( 'NONE',  ( -4.088227598258586603E-16, 292.3593750017070079, -6.676582343750001591 ) ) ;
#48624=CARTESIAN_POINT ( 'NONE',  ( 10.00000000000000178, 145.2083333333333144, -2.679491924311226736 ) ) ;
#48634=CARTESIAN_POINT ( 'NONE',  ( -2.679491924311235174, 20.41666665983869677, 10.00000000000000000 ) ) ;
#48639=CARTESIAN_POINT ( 'NONE',  ( 0.000000000000000000, 0.000000000000000000, 10.00000000000000178 ) ) ;
#48640=CARTESIAN_POINT ( 'NONE',  ( -9.832129032723418760, 37.86458332991934839, -5.676582343750004256 ) ) ;
#48642=CARTESIAN_POINT ( 'NONE',  ( 7.320508075688776373, 150.6250000000000000, -7.320508075688776373 ) ) ;
#48643=CARTESIAN_POINT ( 'NONE',  ( -7.320508075688778149, 14.99999999317203425, 7.320508075688769267 ) ) ;
#48645=CARTESIAN_POINT ( 'NONE',  ( -10.00000000000000178, 129.3749999931720254, -1.224646799147353454E-15 ) ) ;
#48646=B_SPLINE_CURVE_WITH_KNOTS ( 'NONE', 3,
 ( #47486, #29779, #41832, #36550, #7141, #35817, #1499, #70509, #24481, #64845, #13146, #36183, #25208, #59201, #30515, #53535 ),
 .UNSPECIFIED., .F., .F.,
 ( 4, 2, 2, 2, 2, 2, 2, 4 ),
 ( 0.000000000000000000, 0.002635095253036493727, 0.003952642879554739072, 0.005270190506072984851, 0.006587738132591231498, 0.007905285759109476409, 0.009222833385627722189, 0.01054038101214596797 ),
 .UNSPECIFIED. ) ;
#48648=CARTESIAN_POINT ( 'NONE',  ( 11.35316468749999963, 30.98958332991935194, -3.042071309553165293 ) ) ;
#48654=CARTESIAN_POINT ( 'NONE',  ( 5.676582343750001591, 31.61458332991935194, -9.832129032723420536 ) ) ;
#48656=CARTESIAN_POINT ( 'NONE',  ( 5.676582343750001591, 156.6145833299193839, -9.832129032723420536 ) ) ;
#48658=CARTESIAN_POINT ( 'NONE',  ( 10.00000000000000178, 132.0833333265053398, -2.679491924311226736 ) ) ;
#48660=VECTOR ( 'NONE', #1708, 1000.000000000000000 ) ;
#48662=LINE ( 'NONE', #25276, #3857 ) ;
#48663=CARTESIAN_POINT ( 'NONE',  ( -9.832129032723418760, 28.17708332991935194, -5.676582343750004256 ) ) ;
#48670=CARTESIAN_POINT ( 'NONE',  ( -2.085542519210945728E-15, 154.5312499965860127, 11.35316468750000141 ) ) ;
#48677=EDGE_CURVE ( 'NONE', #57404, #21228, #19529, .T. ) ;
#48679=CARTESIAN_POINT ( 'NONE',  ( -4.242640687119285658, 292.1875000034139589, 4.242640687119287435 ) ) ;
#48680=CARTESIAN_POINT ( 'NONE',  ( -5.676582343749998039, 107.7604166632526841, -9.832129032723420536 ) ) ;
#48700=CARTESIAN_POINT ( 'NONE',  ( -7.320508075688773708, 223.7499999931720538, -7.320508075688774596 ) ) ;
#48714=CARTESIAN_POINT ( 'NONE',  ( 4.999999999999993783, 109.1666666666666714, 8.660254037844390851 ) ) ;
#48716=CARTESIAN_POINT ( 'NONE',  ( 6.676582343750003368, 294.1718750017070079, -2.765530957081997254 ) ) ;
#48718=ORIENTED_EDGE ( 'NONE', *, *, #51396, .F. ) ;
#48719=CARTESIAN_POINT ( 'NONE',  ( 10.00000000000004263, 190.0000000000000284, 0.000000000000000000 ) ) ;
#48727=CARTESIAN_POINT ( 'NONE',  ( -9.832129032723420536, 3.697916663252683200, 5.676582343749997150 ) ) ;
#48730=CARTESIAN_POINT ( 'NONE',  ( -3.042071309553164404, 197.5520833299193555, -11.35316468749999963 ) ) ;
#48738=CARTESIAN_POINT ( 'NONE',  ( 8.311093377946834337, 50.46874999658601979, 8.311093377946839666 ) ) ;
#48746=CARTESIAN_POINT ( 'NONE',  ( -9.832129032723420536, 123.6979166632526983, 5.676582343749997150 ) ) ;
#48747=CARTESIAN_POINT ( 'NONE',  ( 2.679491924311222739, 85.83333332650538239, 10.00000000000000355 ) ) ;
#48751=CYLINDRICAL_SURFACE ( 'NONE', #12449, 10.00000000000000178 ) ;
#48752=VERTEX_POINT ( 'NONE', #17871 ) ;
#48753=CARTESIAN_POINT ( 'NONE',  ( -4.433077647033921487, 225.9999999999999147, 8.987638501916837441 ) ) ;
#48756=CARTESIAN_POINT ( 'NONE',  ( -4.721056650415998313, 292.7343750017069510, 4.721056650416000089 ) ) ;
#48759=CARTESIAN_POINT ( 'NONE',  ( 8.311093377946834337, 175.1562499965860127, 8.311093377946839666 ) ) ;
#48768=CARTESIAN_POINT ( 'NONE',  ( -8.311093377946836114, 152.9687499965859843, -8.311093377946837890 ) ) ;
#48772=CARTESIAN_POINT ( 'NONE',  ( -11.35316468749999785, 58.38541666325268409, -3.042071309553167513 ) ) ;
#48779=CARTESIAN_POINT ( 'NONE',  ( -3.673940397442060854E-16, 289.8125000034140157, -6.000000000000001776 ) ) ;
#48802=CARTESIAN_POINT ( 'NONE',  ( -2.679491924311235618, 63.54166666666667851, 10.00000000000000000 ) ) ;
#48804=CARTESIAN_POINT ( 'NONE',  ( -6.000000000000000888, 295.0625000000000000, 2.485281374238575758 ) ) ;
#48810=ORIENTED_EDGE ( 'NONE', *, *, #32915, .T. ) ;
#48817=CARTESIAN_POINT ( 'NONE',  ( -4.999999999999998224, 181.6666666666666572, -8.660254037844389075 ) ) ;
#48821=CARTESIAN_POINT ( 'NONE',  ( 3.042071309553167069, 152.1354166632526983, -11.35316468749999785 ) ) ;
#48826=CARTESIAN_POINT ( 'NONE',  ( -3.673940397442060854E-16, 293.7500000000000000, -6.000000000000001776 ) ) ;
#48828=CARTESIAN_POINT ( 'NONE',  ( -5.676582343749998039, 7.760416663252684089, -9.832129032723420536 ) ) ;
#48834=CARTESIAN_POINT ( 'NONE',  ( 2.679491924311228956, 42.91666665983869677, -10.00000000000000000 ) ) ;
#48844=CARTESIAN_POINT ( 'NONE',  ( 5.676582343749993598, 134.9479166632526983, 9.832129032723422313 ) ) ;
#48852=CARTESIAN_POINT ( 'NONE',  ( -9.832129032723418760, 132.8645833299193555, -5.676582343750004256 ) ) ;
#48859=CARTESIAN_POINT ( 'NONE',  ( 9.832129032723420536, 101.5104166632526841, -5.676582343749999815 ) ) ;
#48863=CARTESIAN_POINT ( 'NONE',  ( -11.35316468750000141, 28.59374999658601624, -1.390361679473963753E-15 ) ) ;
#48864=ORIENTED_EDGE ( 'NONE', *, *, #42627, .F. ) ;
#48868=EDGE_CURVE ( 'NONE', #3122, #16691, #48662, .T. ) ;
#48871=CARTESIAN_POINT ( 'NONE',  ( -6.676582343750001591, 290.4531250017069510, 0.000000000000000000 ) ) ;
#48874=CARTESIAN_POINT ( 'NONE',  ( -2.085542519210945728E-15, 219.8437499965860411, 11.35316468750000141 ) ) ;
#48875=CARTESIAN_POINT ( 'NONE',  ( -11.35316468750000141, 143.5937499965860411, -1.390361679473963753E-15 ) ) ;
#48890=CARTESIAN_POINT ( 'NONE',  ( 3.042071309553159519, 189.7395833299193271, 11.35316468750000141 ) ) ;
#48893=CARTESIAN_POINT ( 'NONE',  ( 1.226468279477575784E-15, 293.7031250017069510, 6.676582343750001591 ) ) ;
#48894=CARTESIAN_POINT ( 'NONE',  ( 5.000000000000001776, 132.7083333265053682, -8.660254037844389075 ) ) ;
#48896=ORIENTED_EDGE ( 'NONE', *, *, #5924, .F. ) ;
#48900=CARTESIAN_POINT ( 'NONE',  ( 0.000000000000000000, 300.0000000000000000, 0.000000000000000000 ) ) ;
#48902=ORIENTED_EDGE ( 'NONE', *, *, #39463, .T. ) ;
#48903=DIRECTION ( 'NONE',  ( -0.000000000000000000, 1.000000000000000000, -0.000000000000000000 ) ) ;
#48905=CARTESIAN_POINT ( 'NONE',  ( 3.042071309553159519, 110.0520833299193271, 11.35316468750000141 ) ) ;
#48915=CARTESIAN_POINT ( 'NONE',  ( 8.311093377946837890, 226.4062499965860411, -8.311093377946837890 ) ) ;
#48919=CARTESIAN_POINT ( 'NONE',  ( -11.35316468750000141, 198.5937499965860127, -1.390361679473963753E-15 ) ) ;
#48926=CARTESIAN_POINT ( 'NONE',  ( -3.042071309553164404, 77.23958332991935549, -11.35316468749999963 ) ) ;
#48927=ORIENTED_EDGE ( 'NONE', *, *, #42187, .T. ) ;
#48929=CARTESIAN_POINT ( 'NONE',  ( 2.679491924292086047, 138.9583333333316375, 10.00000000001106670 ) ) ;
#48932=DIRECTION ( 'NONE',  ( -0.000000000000000000, 1.000000000000000000, -0.000000000000000000 ) ) ;
#48933=CARTESIAN_POINT ( 'NONE',  ( 6.951808397369818766E-16, 92.03124999658602690, -11.35316468750000141 ) ) ;
#48938=CARTESIAN_POINT ( 'NONE',  ( 10.00000000000003375, 74.79166666666668561, 2.679491924311244500 ) ) ;
#48940=CARTESIAN_POINT ( 'NONE',  ( -2.085542519210945728E-15, 74.53124999658602690, 11.35316468750000141 ) ) ;
#48944=CARTESIAN_POINT ( 'NONE',  ( -5.000000000000005329, 170.2083333265053682, 8.660254037844387298 ) ) ;
#48947=CARTESIAN_POINT ( 'NONE',  ( 9.832129032723416984, 60.67708332991934839, 5.676582343750006032 ) ) ;
#48948=CARTESIAN_POINT ( 'NONE',  ( -6.676582343750003368, 295.3906250017068942, -2.765530957081996810 ) ) ;
#48950=CARTESIAN_POINT ( 'NONE',  ( -11.35316468750000141, 213.2812499965860411, -1.390361679473963753E-15 ) ) ;
#48951=( BOUNDED_CURVE ( )  B_SPLINE_CURVE ( 2, ( #5596, #29715, #17269, #51604, #57658, #74619, #6707, #63665, #5964 ),
 .UNSPECIFIED., .F., .F. ) 
 B_SPLINE_CURVE_WITH_KNOTS ( ( 3, 2, 2, 2, 3 ),
 ( 0.8124999999999983347, 0.8229166666666649643, 0.8333333333333317050, 0.8437499999999983347, 0.8541666666666649643 ),
 .UNSPECIFIED. ) 
 CURVE ( )  GEOMETRIC_REPRESENTATION_ITEM ( )  RATIONAL_B_SPLINE_CURVE ( ( 1.000000000000012212, 0.9238795325112745260, 1.000000000000000000, 0.9238795325112867385, 1.000000000000000000, 0.9238795325112867385, 1.000000000000000000, 0.9238795325112989509, 0.9999999999999877875 ) ) 
 REPRESENTATION_ITEM ( '' )  );
#48957=CARTESIAN_POINT ( 'NONE',  ( -3.042071309553163960, 192.2395833299193555, -11.35316468749999963 ) ) ;
#48960=CARTESIAN_POINT ( 'NONE',  ( -8.660254037844387298, 188.9583333265053966, -5.000000000000004441 ) ) ;
#48962=CARTESIAN_POINT ( 'NONE',  ( -8.311093377946836114, 187.9687499965860127, -8.311093377946837890 ) ) ;
#48964=CARTESIAN_POINT ( 'NONE',  ( -2.679491924316975471, 93.54166666666615981, 9.999999999996678213 ) ) ;
#48966=EDGE_CURVE ( 'NONE', #13169, #19469, #63831, .T. ) ;
#48990=CARTESIAN_POINT ( 'NONE',  ( -8.311093377946841443, 79.21874999658601268, 8.311093377946830785 ) ) ;
#48995=CARTESIAN_POINT ( 'NONE',  ( 1.226468279477575784E-15, 294.8593750017070079, 6.676582343750001591 ) ) ;
#48996=CARTESIAN_POINT ( 'NONE',  ( 4.999999999999993783, 144.1666666666666572, 8.660254037844390851 ) ) ;
#48998=CARTESIAN_POINT ( 'NONE',  ( 6.123233995736767268E-16, 163.1249999931720254, -10.00000000000000178 ) ) ;
#49008=CARTESIAN_POINT ( 'NONE',  ( -5.999999999999999112, 293.1250000034141294, 2.485281374238575314 ) ) ;
#49010=CARTESIAN_POINT ( 'NONE',  ( 8.660254037844387298, 134.5833333333333428, 5.000000000000007105 ) ) ;
#49014=CARTESIAN_POINT ( 'NONE',  ( -11.35316468750000141, 38.48958332991935549, 3.042071309553159963 ) ) ;
#49016=CARTESIAN_POINT ( 'NONE',  ( -4.999999999999998224, 8.541666659838698550, -8.660254037844389075 ) ) ;
#49019=CARTESIAN_POINT ( 'NONE',  ( -8.660254037844387298, 128.9583333265053966, -5.000000000000004441 ) ) ;
#49021=CARTESIAN_POINT ( 'NONE',  ( -3.042071309553164404, 47.23958332991935549, -11.35316468749999963 ) ) ;
#49027=CARTESIAN_POINT ( 'NONE',  ( -9.832129032723418760, 32.86458332991934839, -5.676582343750004256 ) ) ;
#49030=CARTESIAN_POINT ( 'NONE',  ( 9.832129032723420536, 156.1979166632526983, -5.676582343749999815 ) ) ;
#49031=CARTESIAN_POINT ( 'NONE',  ( 7.320508075688774596, 122.4999999931720254, -7.320508075688774596 ) ) ;
#49032=EDGE_CURVE ( 'NONE', #26852, #46122, #12266, .T. ) ;
#49035=DIRECTION ( 'NONE',  ( -0.000000000000000000, 1.000000000000000000, -0.000000000000000000 ) ) ;
#49036=CARTESIAN_POINT ( 'NONE',  ( 5.676582343749993598, 15.26041666325268409, 9.832129032723422313 ) ) ;
#49037=LINE ( 'NONE', #66395, #1497 ) ;
#49041=CARTESIAN_POINT ( 'NONE',  ( 0.000000000000000000, 300.0000000000000000, 10.00000000000000178 ) ) ;
#49043=CARTESIAN_POINT ( 'NONE',  ( -9.832129032723420536, 158.6979166632526983, 5.676582343749997150 ) ) ;
#49051=LINE ( 'NONE', #3045, #2770 ) ;
#49052=CARTESIAN_POINT ( 'NONE',  ( -2.485281374238895502, 291.8750000034140157, -5.999999999999677591 ) ) ;
#49053=CARTESIAN_POINT ( 'NONE',  ( 5.676582343749993598, 105.2604166632526841, 9.832129032723422313 ) ) ;
#49085=CARTESIAN_POINT ( 'NONE',  ( -7.320508075688778149, 108.1250000000000284, 7.320508075688769267 ) ) ;
#49087=CARTESIAN_POINT ( 'NONE',  ( -4.088227598258586603E-16, 292.3593750017070079, -6.676582343750001591 ) ) ;
#49100=CARTESIAN_POINT ( 'NONE',  ( -8.311093377946836114, 7.656249996586014461, -8.311093377946837890 ) ) ;
#49103=CARTESIAN_POINT ( 'NONE',  ( -2.085542519210945728E-15, 189.8437499965860127, 11.35316468750000141 ) ) ;
#49111=CARTESIAN_POINT ( 'NONE',  ( 9.832129032723416984, 10.36458332991935016, 5.676582343750006032 ) ) ;
#49117=CARTESIAN_POINT ( 'NONE',  ( -10.00000000000000355, 59.58333332650536107, 2.679491924311223183 ) ) ;
#49119=CARTESIAN_POINT ( 'NONE',  ( -9.832129032723418760, 117.8645833299193697, -5.676582343750004256 ) ) ;
#49120=CARTESIAN_POINT ( 'NONE',  ( -7.320508075688778149, 94.99999999317202537, 7.320508075688769267 ) ) ;
#49124=CARTESIAN_POINT ( 'NONE',  ( -2.679491924311226292, 198.3333333265053398, -10.00000000000000178 ) ) ;
#49125=CARTESIAN_POINT ( 'NONE',  ( -1.836970198721029983E-15, 143.7500000000000284, 10.00000000000000178 ) ) ;
#49127=CARTESIAN_POINT ( 'NONE',  ( -9.935911514116300580, 225.9999999999999432, -1.307310426733117481 ) ) ;
#49128=EDGE_CURVE ( 'NONE', #61049, #44090, #16559, .T. ) ;
#49129=CARTESIAN_POINT ( 'NONE',  ( -6.676582343750003368, 293.5468750017070079, -2.765530957081996810 ) ) ;
#49131=CARTESIAN_POINT ( 'NONE',  ( 3.042071309553167069, 171.8229166632526983, -11.35316468749999785 ) ) ;
#49138=CARTESIAN_POINT ( 'NONE',  ( 11.35316468750000141, 161.0937499965860127, 0.000000000000000000 ) ) ;
#49143=CARTESIAN_POINT ( 'NONE',  ( -3.042071309553173730, 59.63541666325267698, 11.35316468749999785 ) ) ;
#49150=CARTESIAN_POINT ( 'NONE',  ( -4.242640687119285658, 287.1875000034139589, 4.242640687119287435 ) ) ;
#49151=CIRCLE ( 'NONE', #52783, 15.99999999999998579 ) ;
#49155=ADVANCED_FACE ( 'NONE', ( #74289 ), #38484, .T. ) ;
#49158=ADVANCED_FACE ( 'NONE', ( #56211 ), #15076, .T. ) ;
#49169=ORIENTED_EDGE ( 'NONE', *, *, #8136, .F. ) ;
#49172=CARTESIAN_POINT ( 'NONE',  ( -7.320508075688775484, 3.124999999999998224, 7.320508075688766603 ) ) ;
#49176=CARTESIAN_POINT ( 'NONE',  ( 7.320508075688774596, 65.62500000000000000, -7.320508075688774596 ) ) ;
#49178=CARTESIAN_POINT ( 'NONE',  ( 4.242640687119287435, 292.3750000000000000, 4.242640687119285658 ) ) ;
#49179=CARTESIAN_POINT ( 'NONE',  ( -3.166186134455097228E-13, 141.2500000000000284, -9.999999999999998224 ) ) ;
#49190=CARTESIAN_POINT ( 'NONE',  ( 8.660254037844385522, 184.5833333333333428, 5.000000000000005329 ) ) ;
#49193=CARTESIAN_POINT ( 'NONE',  ( -8.311093377946841443, 149.2187499965860411, 8.311093377946830785 ) ) ;
#49194=FACE_OUTER_BOUND ( 'NONE', #48011, .T. ) ;
#49196=LINE ( 'NONE', #72207, #19840 ) ;
#49202=CARTESIAN_POINT ( 'NONE',  ( -3.042071309553164404, 12.55208332991935194, -11.35316468749999963 ) ) ;
#49209=CARTESIAN_POINT ( 'NONE',  ( 6.123233995736767268E-16, 48.12499999317203958, -10.00000000000000178 ) ) ;
#49212=CARTESIAN_POINT ( 'NONE',  ( 6.123233995736767268E-16, 221.2500000000000000, -10.00000000000000178 ) ) ;
#49214=CARTESIAN_POINT ( 'NONE',  ( 0.000000000000000000, 300.0000000000000000, 10.00000000000000178 ) ) ;
#49215=CARTESIAN_POINT ( 'NONE',  ( 7.320508075688771044, 164.3750000000000568, 7.320508075688775484 ) ) ;
#49217=CARTESIAN_POINT ( 'NONE',  ( -4.999999999999998224, 221.6666666666666856, -8.660254037844389075 ) ) ;
#49220=CARTESIAN_POINT ( 'NONE',  ( -8.311093377946836114, 127.6562499965860411, -8.311093377946837890 ) ) ;
#49228=CARTESIAN_POINT ( 'NONE',  ( 5.676582343749993598, 124.9479166632526983, 9.832129032723422313 ) ) ;
#49229=CARTESIAN_POINT ( 'NONE',  ( 10.00000000000000178, 146.8749999931720538, 0.000000000000000000 ) ) ;
#49230=VERTEX_POINT ( 'NONE', #12402 ) ;
#49233=CARTESIAN_POINT ( 'NONE',  ( 11.35316468749999963, 121.3020833299193555, -3.042071309553165293 ) ) ;
#49237=CARTESIAN_POINT ( 'NONE',  ( 8.311093377946837890, 16.71874999658601268, -8.311093377946837890 ) ) ;
#49244=CARTESIAN_POINT ( 'NONE',  ( -6.676582343750000703, 287.5156250017069510, 2.765530957082001251 ) ) ;
#49245=CARTESIAN_POINT ( 'NONE',  ( 0.000000000000000000, 237.9999999999999716, 0.000000000000000000 ) ) ;
#49248=ORIENTED_EDGE ( 'NONE', *, *, #35143, .T. ) ;
#49249=CARTESIAN_POINT ( 'NONE',  ( 5.676582343749993598, 145.2604166632526699, 9.832129032723422313 ) ) ;
#49255=ORIENTED_EDGE ( 'NONE', *, *, #14309, .F. ) ;
#49265=CYLINDRICAL_SURFACE ( 'NONE', #37879, 10.00000000000000178 ) ;
#49266=CARTESIAN_POINT ( 'NONE',  ( -3.042071309553164404, 192.2395833299193555, -11.35316468749999963 ) ) ;
#49269=CARTESIAN_POINT ( 'NONE',  ( 4.721056650416000089, 290.8281250017069510, 4.721056650415999201 ) ) ;
#49270=CARTESIAN_POINT ( 'NONE',  ( 6.123233995736767268E-16, 133.1249999931720254, -10.00000000000000178 ) ) ;
#49271=CARTESIAN_POINT ( 'NONE',  ( 4.999999999999999112, 95.83333333333334281, -8.660254037844383745 ) ) ;
#49283=CARTESIAN_POINT ( 'NONE',  ( -8.311093377946836114, 112.9687499965860269, -8.311093377946837890 ) ) ;
#49284=CARTESIAN_POINT ( 'NONE',  ( 10.00000000000000178, 212.0833333265053682, -2.679491924311226736 ) ) ;
#49291=CARTESIAN_POINT ( 'NONE',  ( -3.042071309553173730, 224.3229166632527267, 11.35316468749999785 ) ) ;
#49296=CARTESIAN_POINT ( 'NONE',  ( -5.676582343749998039, 187.7604166632526983, -9.832129032723420536 ) ) ;
#49303=CARTESIAN_POINT ( 'NONE',  ( -3.042071309553173730, 84.32291666325268409, 11.35316468749999785 ) ) ;
#49305=EDGE_CURVE ( 'NONE', #56251, #42029, #73959, .T. ) ;
#49309=CARTESIAN_POINT ( 'NONE',  ( 5.676582343749993598, 94.94791666325269830, 9.832129032723422313 ) ) ;
#49318=CARTESIAN_POINT ( 'NONE',  ( 8.311093377946837890, 91.40624999658602690, -8.311093377946837890 ) ) ;
#49324=CARTESIAN_POINT ( 'NONE',  ( -7.320508075688778149, 174.9999999931720538, 7.320508075688769267 ) ) ;
#49327=CARTESIAN_POINT ( 'NONE',  ( 11.35316468749999785, 70.88541666325266988, 3.042071309553174174 ) ) ;
#49328=CARTESIAN_POINT ( 'NONE',  ( -2.765530957081996810, 293.2656250017068942, -6.676582343750003368 ) ) ;
#49330=CARTESIAN_POINT ( 'NONE',  ( 11.35316468749999963, 205.9895833299193271, -3.042071309553165293 ) ) ;
#49336=CARTESIAN_POINT ( 'NONE',  ( -8.311093377946841443, 198.9062499965860411, 8.311093377946834337 ) ) ;
#49339=ORIENTED_EDGE ( 'NONE', *, *, #43157, .F. ) ;
#49340=CARTESIAN_POINT ( 'NONE',  ( -11.35316468749999785, 178.3854166632526699, -3.042071309553167957 ) ) ;
#49343=CARTESIAN_POINT ( 'NONE',  ( -7.320508075688767491, 91.87500000000001421, -7.320508075688768379 ) ) ;
#49347=CARTESIAN_POINT ( 'NONE',  ( 10.00000000000000178, 5.208333333333333037, -2.679491924311226736 ) ) ;
#49354=VECTOR ( 'NONE', #62030, 1000.000000000000000 ) ;
#49355=ORIENTED_EDGE ( 'NONE', *, *, #64835, .F. ) ;
#49360=CARTESIAN_POINT ( 'NONE',  ( -6.676582343750001591, 299.5312500017070079, 0.000000000000000000 ) ) ;
#49368=CARTESIAN_POINT ( 'NONE',  ( -11.35316468750000141, 78.80208332991935549, 3.042071309553159963 ) ) ;
#49373=CARTESIAN_POINT ( 'NONE',  ( -6.676582343749999815, 294.6718750017070079, 2.765530957082001251 ) ) ;
#49375=DIRECTION ( 'NONE',  ( -0.000000000000000000, 1.000000000000000000, -0.000000000000000000 ) ) ;
#49379=EDGE_CURVE ( 'NONE', #27119, #19863, #45546, .T. ) ;
#49385=FACE_OUTER_BOUND ( 'NONE', #15472, .T. ) ;
#49390=CARTESIAN_POINT ( 'NONE',  ( -8.311093377946841443, 43.90624999658601268, 8.311093377946830785 ) ) ;
#49392=CARTESIAN_POINT ( 'NONE',  ( 2.679491924311228956, 2.916666659838698994, -10.00000000000000000 ) ) ;
#49395=CARTESIAN_POINT ( 'NONE',  ( 10.00000000000000178, 141.8749999931720538, 0.000000000000000000 ) ) ;
#49397=CARTESIAN_POINT ( 'NONE',  ( 6.951808397369818766E-16, 52.03124999658601979, -11.35316468750000141 ) ) ;
#49403=CARTESIAN_POINT ( 'NONE',  ( 9.832129032723420536, 41.19791666325268409, -5.676582343749999815 ) ) ;
#49406=CARTESIAN_POINT ( 'NONE',  ( -8.311093377946841443, 163.9062499965859843, 8.311093377946830785 ) ) ;
#49408=CARTESIAN_POINT ( 'NONE',  ( 6.123233995736767268E-16, 133.1249999931720254, -10.00000000000000178 ) ) ;
#49412=CARTESIAN_POINT ( 'NONE',  ( 9.832129032723416984, 20.67708332991935194, 5.676582343750006032 ) ) ;
#49419=CARTESIAN_POINT ( 'NONE',  ( 5.676582343750001591, 156.6145833299193839, -9.832129032723420536 ) ) ;
#49432=CARTESIAN_POINT ( 'NONE',  ( -2.485281374238227592, 292.2500000034139589, 6.000000000000345501 ) ) ;
#49433=CARTESIAN_POINT ( 'NONE',  ( 9.832129032723416984, 105.6770833299193413, 5.676582343750006032 ) ) ;
#49442=VECTOR ( 'NONE', #55240, 1000.000000000000000 ) ;
#49458=ORIENTED_EDGE ( 'NONE', *, *, #7633, .T. ) ;
#49464=CARTESIAN_POINT ( 'NONE',  ( 5.000000000000040856, 60.83333333333337833, -8.660254037844454800 ) ) ;
#49465=CARTESIAN_POINT ( 'NONE',  ( 6.123233995736767268E-16, 106.2500000000000142, -10.00000000000000178 ) ) ;
#49468=CARTESIAN_POINT ( 'NONE',  ( 6.676582343750004256, 291.0468750017070079, 2.765530957081995478 ) ) ;
#49472=CARTESIAN_POINT ( 'NONE',  ( -8.660254037844390851, 174.7916666598387110, 4.999999999999998224 ) ) ;
#49475=CARTESIAN_POINT ( 'NONE',  ( -1.836970198721029983E-15, 185.6249999931720538, 10.00000000000000178 ) ) ;
#49480=DIRECTION ( 'NONE',  ( 0.000000000000000000, 0.000000000000000000, 1.000000000000000000 ) ) ;
#49481=CARTESIAN_POINT ( 'NONE',  ( 10.00000000000000178, 225.2083333333333144, -2.679491924311226736 ) ) ;
#49483=CARTESIAN_POINT ( 'NONE',  ( 8.311093377946837890, 196.7187499965860127, -8.311093377946837890 ) ) ;
#49487=DIRECTION ( 'NONE',  ( -0.000000000000000000, 1.000000000000000000, -0.000000000000000000 ) ) ;
#49492=CARTESIAN_POINT ( 'NONE',  ( 9.832129032723416984, 5.364583329919349275, 5.676582343750006032 ) ) ;
#49501=CARTESIAN_POINT ( 'NONE',  ( 11.35316468749999785, 120.5729166632526699, 3.042071309553174174 ) ) ;
#49502=CARTESIAN_POINT ( 'NONE',  ( -1.836970198721029983E-15, 95.62499999317203958, 10.00000000000000178 ) ) ;
#49507=EDGE_LOOP ( 'NONE', ( #66645, #73591, #66949, #72091, #67168, #19569, #45572, #17966, #31754, #53865, #47877, #54923, #61405, #47775, #45367, #68925, #18894, #22583, #70414, #15347, #49458, #58048, #3043, #48124, #2322, #13406, #68214, #69887, #33523, #19939, #60030, #70101, #57345, #58037, #62228, #73024, #40480, #178, #70704, #29500, #6839, #12991, #16659, #15031, #59024, #34144, #41458, #31489, #73878, #52705, #50851, #41556, #26344, #57551, #15914, #42394, #67468, #33381, #898, #10508, #24777, #37471, #8778, #4374, #43555, #20683, #5228, #9222, #8821, #17497, #37850, #1860, #67638, #44840, #60958, #43166, #961, #19358, #65864, #13354, #47287, #20362, #44655, #63972, #16360, #59729, #1068, #11035, #63189, #43941, #32189, #5200, #19730, #54061 ) ) ;
#49509=CARTESIAN_POINT ( 'NONE',  ( -2.765530957081998586, 292.7968750017070079, 6.676582343750001591 ) ) ;
#49510=CARTESIAN_POINT ( 'NONE',  ( 5.000000000000001776, 187.7083333265053966, -8.660254037844389075 ) ) ;
#49512=CARTESIAN_POINT ( 'NONE',  ( 5.676582343750001591, 171.6145833299193555, -9.832129032723420536 ) ) ;
#49515=CARTESIAN_POINT ( 'NONE',  ( -4.999999999999998224, 203.5416666598387110, -8.660254037844389075 ) ) ;
#49520=CARTESIAN_POINT ( 'NONE',  ( -9.832129032723418760, 153.1770833299193555, -5.676582343750004256 ) ) ;
#49521=CARTESIAN_POINT ( 'NONE',  ( -7.320508075688777261, 216.8750000000000000, -7.320508075688778149 ) ) ;
#49524=CARTESIAN_POINT ( 'NONE',  ( 9.832129032723420536, 61.51041666325268409, -5.676582343749999815 ) ) ;
#49530=CARTESIAN_POINT ( 'NONE',  ( -6.000000000000003553, 290.0000000034140157, -2.485281374238571317 ) ) ;
#49532=CARTESIAN_POINT ( 'NONE',  ( -2.222453528114265639E-12, 168.7499999999998295, 10.00000000000000178 ) ) ;
#49544=ADVANCED_FACE ( 'NONE', ( #24462 ), #59183, .T. ) ;
#49554=CARTESIAN_POINT ( 'NONE',  ( -2.679491924295767102, 201.4583333333319501, -10.00000000000892442 ) ) ;
#49557=CARTESIAN_POINT ( 'NONE',  ( -10.00000000000000000, 67.29166666666667140, -2.679491924311229845 ) ) ;
#49560=CARTESIAN_POINT ( 'NONE',  ( -6.000000000000003553, 291.9374999999999432, -2.485281374238571317 ) ) ;
#49571=CARTESIAN_POINT ( 'NONE',  ( -10.00000000000000178, 192.5000000000000000, -1.224646799147353454E-15 ) ) ;
#49572=CARTESIAN_POINT ( 'NONE',  ( 11.35316468750000141, 1.093749996586016682, 0.000000000000000000 ) ) ;
#49574=CARTESIAN_POINT ( 'NONE',  ( -11.35316468750000141, 158.5937499965860127, -1.390361679473963753E-15 ) ) ;
#49581=CARTESIAN_POINT ( 'NONE',  ( -5.676582343749998039, 22.76041666325268409, -9.832129032723420536 ) ) ;
#49586=CARTESIAN_POINT ( 'NONE',  ( 6.123233995736767268E-16, 33.12499999317203248, -10.00000000000000178 ) ) ;
#49589=CARTESIAN_POINT ( 'NONE',  ( -10.00000000000000355, 44.58333332650536818, 2.679491924311223183 ) ) ;
#49593=CARTESIAN_POINT ( 'NONE',  ( 2.679491924311226292, 218.9583333333333428, 10.00000000000001421 ) ) ;
#49601=CARTESIAN_POINT ( 'NONE',  ( 5.000000000000004441, 30.83333333333333925, -8.660254037844390851 ) ) ;
#49604=CARTESIAN_POINT ( 'NONE',  ( -5.676582343750006032, 134.1145833299193555, 9.832129032723418760 ) ) ;
#49606=CARTESIAN_POINT ( 'NONE',  ( -6.000000000000001776, 298.0000000000000000, 0.000000000000000000 ) ) ;
#49610=CARTESIAN_POINT ( 'NONE',  ( -7.320508075688778149, 154.9999999931720538, 7.320508075688769267 ) ) ;
#49612=CARTESIAN_POINT ( 'NONE',  ( 9.832129032723420536, 121.1979166632526983, -5.676582343749999815 ) ) ;
#49617=CARTESIAN_POINT ( 'NONE',  ( 3.042071309553159519, 115.0520833299193555, 11.35316468750000141 ) ) ;
#49621=CARTESIAN_POINT ( 'NONE',  ( -5.676582343749998039, 22.76041666325268409, -9.832129032723420536 ) ) ;
#49627=PRODUCT_DEFINITION ( 'UNKNOWN', '', #74308, #40272 ) ;
#49630=CARTESIAN_POINT ( 'NONE',  ( -2.765530957081998586, 290.6406250017069510, 6.676582343750001591 ) ) ;
#49633=ORIENTED_EDGE ( 'NONE', *, *, #31063, .F. ) ;
#49634=CARTESIAN_POINT ( 'NONE',  ( -5.676582343750006032, 144.4270833299193555, 9.832129032723418760 ) ) ;
#49650=CARTESIAN_POINT ( 'NONE',  ( -11.35316468749999785, 193.0729166632526415, -3.042071309553167513 ) ) ;
#49652=CARTESIAN_POINT ( 'NONE',  ( -3.673940397442060854E-16, 290.8125000034140157, -6.000000000000001776 ) ) ;
#49653=CARTESIAN_POINT ( 'NONE',  ( 6.676582343750003368, 287.8906250017069510, 2.765530957081995478 ) ) ;
#49654=CARTESIAN_POINT ( 'NONE',  ( -1.836970198721029983E-15, 130.6249999931720254, 10.00000000000000178 ) ) ;
#49667=CARTESIAN_POINT ( 'NONE',  ( 11.35316468749999785, 115.8854166632526841, 3.042071309553174174 ) ) ;
#49674=AXIS2_PLACEMENT_3D ( 'NONE', #42550, #71957, #37276 ) ;
#49676=EDGE_CURVE ( 'NONE', #31901, #50470, #42209, .T. ) ;
#49677=CARTESIAN_POINT ( 'NONE',  ( 11.35316468749999963, 220.9895833299193555, -3.042071309553165293 ) ) ;
#49682=CARTESIAN_POINT ( 'NONE',  ( 5.676582343749993598, 210.2604166632526699, 9.832129032723422313 ) ) ;
#49684=CYLINDRICAL_SURFACE ( 'NONE', #26518, 10.00000000000000178 ) ;
#49688=CARTESIAN_POINT ( 'NONE',  ( 4.999999999999991118, 184.1666666666666856, 8.660254037844387298 ) ) ;
#49690=CARTESIAN_POINT ( 'NONE',  ( 11.35316468749999785, 85.57291666325268409, 3.042071309553174174 ) ) ;
#49691=VERTEX_POINT ( 'NONE', #4437 ) ;
#49697=CARTESIAN_POINT ( 'NONE',  ( -3.042071309553164404, 92.23958332991935549, -11.35316468749999963 ) ) ;
#49698=VERTEX_POINT ( 'NONE', #44052 ) ;
#49701=LINE ( 'NONE', #55746, #71929 ) ;
#49705=CARTESIAN_POINT ( 'NONE',  ( 8.311093377946837890, 81.40624999658601268, -8.311093377946837890 ) ) ;
#49709=CARTESIAN_POINT ( 'NONE',  ( 8.660254037844389075, 182.2916666598387110, -5.000000000000000000 ) ) ;
#49711=CARTESIAN_POINT ( 'NONE',  ( 8.311093377946837890, 76.71874999658601268, -8.311093377946837890 ) ) ;
#49712=CARTESIAN_POINT ( 'NONE',  ( -6.676582343750000703, 294.5156250017069510, 2.765530957082001251 ) ) ;
#49714=CARTESIAN_POINT ( 'NONE',  ( 9.832129032723416984, 205.3645833299193555, 5.676582343750006032 ) ) ;
#49715=ORIENTED_EDGE ( 'NONE', *, *, #2490, .T. ) ;
#49719=CARTESIAN_POINT ( 'NONE',  ( -3.042071309553163960, 202.2395833299193555, -11.35316468749999963 ) ) ;
#49722=CARTESIAN_POINT ( 'NONE',  ( -4.721056650415999201, 299.3281250017069510, -4.721056650415999201 ) ) ;
#49724=CARTESIAN_POINT ( 'NONE',  ( -11.35316468750000141, 193.8020833299193271, 3.042071309553159963 ) ) ;
#49727=CARTESIAN_POINT ( 'NONE',  ( 6.123233995736767268E-16, 91.25000000000001421, -10.00000000000000178 ) ) ;
#49729=ORIENTED_EDGE ( 'NONE', *, *, #4466, .T. ) ;
#49732=CARTESIAN_POINT ( 'NONE',  ( -8.660254037844390851, 17.91666666666666785, 4.999999999999998224 ) ) ;
#49750=ORIENTED_EDGE ( 'NONE', *, *, #68085, .F. ) ;
#49752=CARTESIAN_POINT ( 'NONE',  ( 9.832129032723420536, 71.51041666325268409, -5.676582343749999815 ) ) ;
#49757=CARTESIAN_POINT ( 'NONE',  ( -4.088227598258586603E-16, 289.3593750017070079, -6.676582343750001591 ) ) ;
#49766=CARTESIAN_POINT ( 'NONE',  ( -3.042071309553173730, 169.6354166632526699, 11.35316468749999785 ) ) ;
#49775=CARTESIAN_POINT ( 'NONE',  ( -8.311093377946841443, 38.90624999658599847, 8.311093377946830785 ) ) ;
#49777=CARTESIAN_POINT ( 'NONE',  ( -7.320508075688773708, 23.74999999317202892, -7.320508075688774596 ) ) ;
#49780=LINE ( 'NONE', #55827, #19364 ) ;
#49783=CARTESIAN_POINT ( 'NONE',  ( -3.042071309553173730, 49.32291666325266988, 11.35316468749999785 ) ) ;
#49789=CARTESIAN_POINT ( 'NONE',  ( 6.951808397369818766E-16, 47.03124999658601979, -11.35316468750000141 ) ) ;
#49791=CARTESIAN_POINT ( 'NONE',  ( 9.999999999999996447, 204.7916666666667140, 2.679491924311235174 ) ) ;
#49792=CARTESIAN_POINT ( 'NONE',  ( 9.832129032723420536, 161.1979166632526983, -5.676582343749999815 ) ) ;
#49793=CARTESIAN_POINT ( 'NONE',  ( 2.679491924311228956, 127.9166666598386968, -10.00000000000000000 ) ) ;
#49796=CARTESIAN_POINT ( 'NONE',  ( -3.042071309553173730, 39.63541666325267698, 11.35316468749999785 ) ) ;
#49799=DIRECTION ( 'NONE',  ( -0.000000000000000000, 1.000000000000000000, -0.000000000000000000 ) ) ;
#49803=CARTESIAN_POINT ( 'NONE',  ( 8.311093377946834337, 170.1562499965860127, 8.311093377946839666 ) ) ;
#49811=CARTESIAN_POINT ( 'NONE',  ( 11.35316468749999785, 110.8854166632526699, 3.042071309553174174 ) ) ;
#49815=VERTEX_POINT ( 'NONE', #55382 ) ;
#49827=ORIENTED_EDGE ( 'NONE', *, *, #17341, .F. ) ;
#49828=LINE ( 'NONE', #2316, #5328 ) ;
#49832=CARTESIAN_POINT ( 'NONE',  ( 6.676582343750002480, 299.0156250017069510, -2.765530957081997254 ) ) ;
#49834=ORIENTED_EDGE ( 'NONE', *, *, #74065, .T. ) ;
#49835=ORIENTED_EDGE ( 'NONE', *, *, #56867, .F. ) ;
#49842=CARTESIAN_POINT ( 'NONE',  ( -10.00000000000000178, 107.5000000000000142, -1.224646799147353454E-15 ) ) ;
#49845=CARTESIAN_POINT ( 'NONE',  ( -4.721056650415999201, 293.4843750017070079, -4.721056650415999201 ) ) ;
#49859=CARTESIAN_POINT ( 'NONE',  ( 4.089758525567003034, 225.9150540747923515, -9.185782198135839849 ) ) ;
#49861=CARTESIAN_POINT ( 'NONE',  ( 9.832129032723420536, 211.5104166632526699, -5.676582343749999815 ) ) ;
#49862=CARTESIAN_POINT ( 'NONE',  ( 3.042071309553167069, 1.822916663252682756, -11.35316468749999785 ) ) ;
#49866=CARTESIAN_POINT ( 'NONE',  ( 4.242640687119287435, 297.3750000000000000, 4.242640687119285658 ) ) ;
#49867=ORIENTED_EDGE ( 'NONE', *, *, #14652, .F. ) ;
#49869=CARTESIAN_POINT ( 'NONE',  ( 11.35316468750000141, 5.781249996586016238, 0.000000000000000000 ) ) ;
#49876=CARTESIAN_POINT ( 'NONE',  ( -2.085542519210945728E-15, 9.531249996586018014, 11.35316468750000141 ) ) ;
#49878=CARTESIAN_POINT ( 'NONE',  ( -3.042071309553164404, 122.2395833299193271, -11.35316468749999963 ) ) ;
#49879=CARTESIAN_POINT ( 'NONE',  ( -10.00000000000000178, 89.37499999317203958, -1.224646799147353454E-15 ) ) ;
#49883=CARTESIAN_POINT ( 'NONE',  ( 1.491046635511791134E-11, 146.2499999999988631, -9.999999999999998224 ) ) ;
#49885=LINE ( 'NONE', #72900, #59307 ) ;
#49886=CARTESIAN_POINT ( 'NONE',  ( -6.676582343750001591, 289.6093750017069510, 0.000000000000000000 ) ) ;
#49891=CARTESIAN_POINT ( 'NONE',  ( 7.320508075688774596, 202.4999999931720538, -7.320508075688774596 ) ) ;
#49897=CARTESIAN_POINT ( 'NONE',  ( 8.311093377946834337, 160.4687499965860411, 8.311093377946839666 ) ) ;
#49901=CARTESIAN_POINT ( 'NONE',  ( -3.042071309553164404, 62.55208332991934839, -11.35316468749999963 ) ) ;
#49907=CARTESIAN_POINT ( 'NONE',  ( 6.000000000000001776, 288.5625000034140157, -7.347880794884121708E-16 ) ) ;
#49928=CARTESIAN_POINT ( 'NONE',  ( -8.660254037844387298, 202.0833333333333428, -5.000000000000004441 ) ) ;
#49931=CARTESIAN_POINT ( 'NONE',  ( 4.999999999999993783, 64.16666666666667140, 8.660254037844390851 ) ) ;
#49932=AXIS2_PLACEMENT_3D ( 'NONE', #37968, #66249, #55324 ) ;
#49935=CARTESIAN_POINT ( 'NONE',  ( -3.673940397442060854E-16, 291.7500000000000000, -6.000000000000001776 ) ) ;
#49946=CARTESIAN_POINT ( 'NONE',  ( -10.00000000000004263, 77.70833333333338544, 2.679491924311233397 ) ) ;
#49947=CARTESIAN_POINT ( 'NONE',  ( 5.000000000000001776, 185.8333333333333428, -8.660254037844389075 ) ) ;
#49950=CARTESIAN_POINT ( 'NONE',  ( -11.35316468749999785, 148.3854166632526983, -3.042071309553167513 ) ) ;
#49954=CARTESIAN_POINT ( 'NONE',  ( -8.660254037844390851, 84.79166665983869677, 4.999999999999998224 ) ) ;
#49957=CARTESIAN_POINT ( 'NONE',  ( -2.085542519210945728E-15, 24.84374999658601624, 11.35316468750000141 ) ) ;
#49963=CARTESIAN_POINT ( 'NONE',  ( -10.00000000000000178, 49.37499999317203248, -1.224646799147353454E-15 ) ) ;
#49968=CARTESIAN_POINT ( 'NONE',  ( 2.485281374238919927, 291.3750000034139589, 5.999999999999654499 ) ) ;
#49969=CARTESIAN_POINT ( 'NONE',  ( 6.123233995736767268E-16, 161.2500000000000000, -10.00000000000000178 ) ) ;
#49971=ORIENTED_EDGE ( 'NONE', *, *, #13614, .F. ) ;
#49972=CARTESIAN_POINT ( 'NONE',  ( -7.320508075688773708, 221.8750000000000284, -7.320508075688774596 ) ) ;
#49974=CARTESIAN_POINT ( 'NONE',  ( 8.311093377946834337, 125.1562499965860411, 8.311093377946839666 ) ) ;
#49981=CARTESIAN_POINT ( 'NONE',  ( -3.042071309553163960, 122.2395833299193271, -11.35316468749999963 ) ) ;
#49984=CARTESIAN_POINT ( 'NONE',  ( -2.679491924311226292, 23.33333332650536818, -10.00000000000000178 ) ) ;
#49987=CARTESIAN_POINT ( 'NONE',  ( -9.832129032723420536, 119.0104166632526841, 5.676582343749997150 ) ) ;
#49991=CARTESIAN_POINT ( 'NONE',  ( 11.35316468750000141, 26.09374999658601624, 0.000000000000000000 ) ) ;
#49993=CARTESIAN_POINT ( 'NONE',  ( 0.000000000000000000, 300.0000000000000000, 0.000000000000000000 ) ) ;
#49996=CARTESIAN_POINT ( 'NONE',  ( 1.102182119232618108E-15, 298.3125000034140157, 6.000000000000001776 ) ) ;
#49998=CARTESIAN_POINT ( 'NONE',  ( -4.721056650415998313, 290.5781250017069510, 4.721056650416000089 ) ) ;
#50002=CARTESIAN_POINT ( 'NONE',  ( -9.832129032723420536, 144.0104166632526699, 5.676582343749997150 ) ) ;
#50019=CARTESIAN_POINT ( 'NONE',  ( -2.085542519210945728E-15, 184.5312499965860411, 11.35316468750000141 ) ) ;
#50022=CARTESIAN_POINT ( 'NONE',  ( -6.676582343749999815, 288.5156250017069510, 2.765530957082001251 ) ) ;
#50037=CARTESIAN_POINT ( 'NONE',  ( -8.311093377946841443, 114.2187499965860269, 8.311093377946830785 ) ) ;
#50042=CARTESIAN_POINT ( 'NONE',  ( 0.000000000000000000, 300.0000000000000000, 6.000000000000001776 ) ) ;
#50045=CARTESIAN_POINT ( 'NONE',  ( 6.000000000000003553, 287.5000000034140157, 2.485281374238571317 ) ) ;
#50048=CARTESIAN_POINT ( 'NONE',  ( 11.35316468749999785, 205.8854166632526415, 3.042071309553174174 ) ) ;
#50056=CARTESIAN_POINT ( 'NONE',  ( -8.311093377946841443, 88.90624999658602690, 8.311093377946830785 ) ) ;
#50059=( BOUNDED_CURVE ( )  B_SPLINE_CURVE ( 2, ( #28994, #57684, #22963, #58060, #11273, #69732, #34305, #350, #63688, #5620, #12015, #18047, #41062 ),
 .UNSPECIFIED., .F., .F. ) 
 B_SPLINE_CURVE_WITH_KNOTS ( ( 3, 2, 2, 2, 2, 2, 3 ),
 ( 1.334491602770097263, 1.339725126200808969, 1.344958649631520675, 1.350192173062232381, 1.355425696492944088, 1.360659219923655794, 1.365892743354367500 ),
 .UNSPECIFIED. ) 
 CURVE ( )  GEOMETRIC_REPRESENTATION_ITEM ( )  RATIONAL_B_SPLINE_CURVE ( ( 1.000000000000001998, 0.9659258262890663138, 1.000000000000000000, 0.9659258262890684232, 1.000000000000000000, 0.9659258262890684232, 1.000000000000000000, 0.9659258262890684232, 1.000000000000000000, 0.9659258262890684232, 1.000000000000000000, 0.9659258262890684232, 1.000000000000000000 ) ) 
 REPRESENTATION_ITEM ( '' )  );
#50064=CARTESIAN_POINT ( 'NONE',  ( 8.311093377946834337, 85.15624999658602690, 8.311093377946839666 ) ) ;
#50065=ORIENTED_EDGE ( 'NONE', *, *, #3806, .F. ) ;
#50072=CARTESIAN_POINT ( 'NONE',  ( 3.042071309553167513, 86.82291666325266988, -11.35316468749999785 ) ) ;
#50073=AXIS2_PLACEMENT_3D ( 'NONE', #21495, #57336, #21860 ) ;
#50077=CARTESIAN_POINT ( 'NONE',  ( 4.999999999999993783, 181.0416666598387110, 8.660254037844390851 ) ) ;
#50080=CARTESIAN_POINT ( 'NONE',  ( -3.042071309553173730, 69.63541666325268409, 11.35316468749999785 ) ) ;
#50081=CARTESIAN_POINT ( 'NONE',  ( 4.721056650415999201, 293.0781250017069510, -4.721056650415999201 ) ) ;
#50084=CARTESIAN_POINT ( 'NONE',  ( -3.042071309553173730, 214.3229166632526983, 11.35316468749999785 ) ) ;
#50089=CARTESIAN_POINT ( 'NONE',  ( -8.311093377946836114, 207.6562499965860127, -8.311093377946837890 ) ) ;
#50092=ORIENTED_EDGE ( 'NONE', *, *, #30218, .F. ) ;
#50093=CARTESIAN_POINT ( 'NONE',  ( 11.35316468749999785, 195.8854166632526415, 3.042071309553174174 ) ) ;
#50102=CARTESIAN_POINT ( 'NONE',  ( 10.00000000000000178, 10.00000000000000000, 0.000000000000000000 ) ) ;
#50110=ORIENTED_EDGE ( 'NONE', *, *, #36316, .T. ) ;
#50114=FACE_OUTER_BOUND ( 'NONE', #60867, .T. ) ;
#50121=EDGE_LOOP ( 'NONE', ( #50487, #1494, #18989, #50341 ) ) ;
#50123=CARTESIAN_POINT ( 'NONE',  ( -5.676582343749998039, 72.76041666325268409, -9.832129032723420536 ) ) ;
#50128=CARTESIAN_POINT ( 'NONE',  ( 6.676582343750001591, 292.1093750017069510, -8.176455196517173205E-16 ) ) ;
#50133=AXIS2_PLACEMENT_3D ( 'NONE', #71857, #25829, #20551 ) ;
#50137=CARTESIAN_POINT ( 'NONE',  ( -5.676582343750006032, 164.4270833299193555, 9.832129032723418760 ) ) ;
#50145=CARTESIAN_POINT ( 'NONE',  ( 5.676582343750001591, 51.61458332991934839, -9.832129032723420536 ) ) ;
#50147=CARTESIAN_POINT ( 'NONE',  ( 8.660254037844389075, 17.29166665983869677, -5.000000000000000000 ) ) ;
#50150=CARTESIAN_POINT ( 'NONE',  ( 6.123233995736767268E-16, 143.1249999931720538, -10.00000000000000178 ) ) ;
#50152=CARTESIAN_POINT ( 'NONE',  ( -2.085542519210945728E-15, 44.53124999658601979, 11.35316468750000141 ) ) ;
#50156=CARTESIAN_POINT ( 'NONE',  ( -2.679491924324485019, 13.54166666666547769, 9.999999999992347455 ) ) ;
#50158=CARTESIAN_POINT ( 'NONE',  ( 5.676582343749993598, 44.94791666325267698, 9.832129032723422313 ) ) ;
#50161=( BOUNDED_CURVE ( )  B_SPLINE_CURVE ( 2, ( #41129, #40387, #10975, #12444, #418, #62642, #74338, #23398, #69799 ),
 .UNSPECIFIED., .F., .F. ) 
 B_SPLINE_CURVE_WITH_KNOTS ( ( 3, 2, 2, 2, 3 ),
 ( 0.7291666666666649643, 0.7395833333333317050, 0.7499999999999983347, 0.7604166666666649643, 0.7708333333333317050 ),
 .UNSPECIFIED. ) 
 CURVE ( )  GEOMETRIC_REPRESENTATION_ITEM ( )  RATIONAL_B_SPLINE_CURVE ( ( 1.000000000000012212, 0.9238795325112745260, 1.000000000000000000, 0.9238795325112867385, 1.000000000000000000, 0.9238795325112867385, 1.000000000000000000, 0.9238795325112989509, 0.9999999999999877875 ) ) 
 REPRESENTATION_ITEM ( '' )  );
#50162=CARTESIAN_POINT ( 'NONE',  ( -11.35316468749999785, 168.0729166632526699, -3.042071309553167513 ) ) ;
#50163=CARTESIAN_POINT ( 'NONE',  ( -7.320508075688778149, 144.9999999931719969, 7.320508075688769267 ) ) ;
#50166=CARTESIAN_POINT ( 'NONE',  ( 6.951808397369818766E-16, 32.34374999658601268, -11.35316468750000141 ) ) ;
#50168=ORIENTED_EDGE ( 'NONE', *, *, #56608, .F. ) ;
#50172=CARTESIAN_POINT ( 'NONE',  ( 1.881637226502129035E-11, 6.249999999998538058, -10.00000000000000178 ) ) ;
#50173=CARTESIAN_POINT ( 'NONE',  ( 6.951808397369818766E-16, 172.0312499965860411, -11.35316468750000141 ) ) ;
#50182=CARTESIAN_POINT ( 'NONE',  ( -8.311093377946836114, 117.9687499965860127, -8.311093377946837890 ) ) ;
#50203=CARTESIAN_POINT ( 'NONE',  ( 8.660254037844389075, 72.29166665983869677, -5.000000000000000000 ) ) ;
#50205=ORIENTED_EDGE ( 'NONE', *, *, #72251, .F. ) ;
#50212=CARTESIAN_POINT ( 'NONE',  ( 8.660254037844385522, 124.5833333333333428, 5.000000000000005329 ) ) ;
#50214=CARTESIAN_POINT ( 'NONE',  ( -6.676582343750001591, 293.6093750017069510, 0.000000000000000000 ) ) ;
#50218=CARTESIAN_POINT ( 'NONE',  ( -2.679491924311235174, 175.4166666598387110, 10.00000000000000000 ) ) ;
#50227=CARTESIAN_POINT ( 'NONE',  ( 6.123233995736767268E-16, 213.1249999931720538, -10.00000000000000178 ) ) ;
#50228=CARTESIAN_POINT ( 'NONE',  ( -8.660254037844387298, 222.0833333333333428, -5.000000000000004441 ) ) ;
#50230=CARTESIAN_POINT ( 'NONE',  ( -8.311093377946836114, 202.9687499965860411, -8.311093377946837890 ) ) ;
#50238=CARTESIAN_POINT ( 'NONE',  ( -11.35316468750000141, 3.489583329919349719, 3.042071309553159963 ) ) ;
#50241=FACE_OUTER_BOUND ( 'NONE', #1793, .T. ) ;
#50243=CARTESIAN_POINT ( 'NONE',  ( 6.951808397369818766E-16, 7.031249996586016238, -11.35316468750000141 ) ) ;
#50245=CARTESIAN_POINT ( 'NONE',  ( -5.676582343750006032, 124.1145833299193555, 9.832129032723418760 ) ) ;
#50247=CARTESIAN_POINT ( 'NONE',  ( -8.660254037844390851, 99.79166665983871098, 4.999999999999998224 ) ) ;
#50253=CARTESIAN_POINT ( 'NONE',  ( -2.679491924307398687, 116.4583333333330302, -10.00000000000221512 ) ) ;
#50254=CARTESIAN_POINT ( 'NONE',  ( 4.721056650415999201, 290.2343750017069510, -4.721056650415999201 ) ) ;
#50263=CARTESIAN_POINT ( 'NONE',  ( 2.679491924311228956, 157.9166666598386826, -10.00000000000000000 ) ) ;
#50264=CARTESIAN_POINT ( 'NONE',  ( 3.042071309553159519, 160.0520833299193555, 11.35316468750000141 ) ) ;
#50268=CARTESIAN_POINT ( 'NONE',  ( -11.35316468750000141, 78.80208332991935549, 3.042071309553159963 ) ) ;
#50269=( BOUNDED_CURVE ( )  B_SPLINE_CURVE ( 2, ( #10772, #51885, #28865, #46218, #21708, #16785, #40188, #63191, #39078 ),
 .UNSPECIFIED., .F., .F. ) 
 B_SPLINE_CURVE_WITH_KNOTS ( ( 3, 2, 2, 2, 3 ),
 ( 0.06249999999999773792, 0.07291666666666440921, 0.08333333333333108051, 0.09374999999999775180, 0.1041666666666644370 ),
 .UNSPECIFIED. ) 
 CURVE ( )  GEOMETRIC_REPRESENTATION_ITEM ( )  RATIONAL_B_SPLINE_CURVE ( ( 1.000000000000016431, 0.9238795325112701962, 1.000000000000000000, 0.9238795325112867385, 1.000000000000000000, 0.9238795325112867385, 1.000000000000000000, 0.9238795325113030588, 0.9999999999999836797 ) ) 
 REPRESENTATION_ITEM ( '' )  );
#50273=ORIENTED_EDGE ( 'NONE', *, *, #10577, .T. ) ;
#50277=CARTESIAN_POINT ( 'NONE',  ( 2.485281374238571317, 287.7500000034140157, -6.000000000000003553 ) ) ;
#50285=ORIENTED_EDGE ( 'NONE', *, *, #32915, .F. ) ;
#50301=CARTESIAN_POINT ( 'NONE',  ( 7.320508075688774596, 75.62500000000000000, -7.320508075688774596 ) ) ;
#50303=CARTESIAN_POINT ( 'NONE',  ( -2.485281374238571761, 291.8125000000000000, -6.000000000000003553 ) ) ;
#50314=CARTESIAN_POINT ( 'NONE',  ( -1.836970198721029983E-15, 193.7500000000000000, 10.00000000000000178 ) ) ;
#50317=CARTESIAN_POINT ( 'NONE',  ( -9.832129032723418760, 173.1770833299193555, -5.676582343750004256 ) ) ;
#50318=CARTESIAN_POINT ( 'NONE',  ( 0.000000000000000000, 300.0000000000000000, 10.00000000000000178 ) ) ;
#50323=CARTESIAN_POINT ( 'NONE',  ( -3.042071309553173730, 29.63541666325268054, 11.35316468749999785 ) ) ;
#50329=CARTESIAN_POINT ( 'NONE',  ( 7.320508075688771044, 51.24999999317203958, 7.320508075688775484 ) ) ;
#50332=CARTESIAN_POINT ( 'NONE',  ( 8.660254037844394404, 219.5833333333333428, 5.000000000000011546 ) ) ;
#50340=CARTESIAN_POINT ( 'NONE',  ( 8.311093377946834337, 140.1562499965860127, 8.311093377946839666 ) ) ;
#50341=ORIENTED_EDGE ( 'NONE', *, *, #38594, .F. ) ;
#50355=CARTESIAN_POINT ( 'NONE',  ( -3.042071309553173730, 109.6354166632526699, 11.35316468749999785 ) ) ;
#50359=CARTESIAN_POINT ( 'NONE',  ( -5.676582343750006032, 34.42708332991935549, 9.832129032723418760 ) ) ;
#50368=CARTESIAN_POINT ( 'NONE',  ( 6.676582343750001591, 289.9531250017069510, -8.176455196517173205E-16 ) ) ;
#50372=CARTESIAN_POINT ( 'NONE',  ( -5.676582343749998039, 137.7604166632526983, -9.832129032723420536 ) ) ;
#50379=EDGE_CURVE ( 'NONE', #23110, #29212, #7310, .T. ) ;
#50384=AXIS2_PLACEMENT_3D ( 'NONE', #56560, #27491, #3748 ) ;
#50386=ORIENTED_EDGE ( 'NONE', *, *, #56567, .F. ) ;
#50388=CARTESIAN_POINT ( 'NONE',  ( -4.999999999999998224, 208.5416666598387394, -8.660254037844389075 ) ) ;
#50390=CARTESIAN_POINT ( 'NONE',  ( 6.951808397369818766E-16, 182.0312499965860411, -11.35316468750000141 ) ) ;
#50393=CARTESIAN_POINT ( 'NONE',  ( 6.000000000000001776, 295.5000000000000000, -7.347880794884121708E-16 ) ) ;
#50394=CARTESIAN_POINT ( 'NONE',  ( -4.088227598258586603E-16, 288.2031250017069510, -6.676582343750001591 ) ) ;
#50395=CARTESIAN_POINT ( 'NONE',  ( 8.660254037844484998, 80.41666666666672825, -5.000000000000056843 ) ) ;
#50396=CARTESIAN_POINT ( 'NONE',  ( -7.320508075688780814, 68.12500000000000000, 7.320508075688771932 ) ) ;
#50401=CARTESIAN_POINT ( 'NONE',  ( -1.836970198721029983E-15, 10.62499999317203425, 10.00000000000000178 ) ) ;
#50405=CARTESIAN_POINT ( 'NONE',  ( -10.00000000000000178, 147.5000000000000284, -1.224646799147353454E-15 ) ) ;
#50409=CARTESIAN_POINT ( 'NONE',  ( -9.832129032723418760, 128.1770833299193555, -5.676582343750004256 ) ) ;
#50414=DIRECTION ( 'NONE',  ( -0.000000000000000000, 1.000000000000000000, -0.000000000000000000 ) ) ;
#50419=CARTESIAN_POINT ( 'NONE',  ( 8.311093377946837890, 211.7187499965860127, -8.311093377946837890 ) ) ;
#50426=CARTESIAN_POINT ( 'NONE',  ( 9.832129032723416984, 90.36458332991935549, 5.676582343750006032 ) ) ;
#50432=CARTESIAN_POINT ( 'NONE',  ( 6.951808397369818766E-16, 97.03124999658602690, -11.35316468750000141 ) ) ;
#50439=CARTESIAN_POINT ( 'NONE',  ( -3.042071309553163960, 87.23958332991935549, -11.35316468749999963 ) ) ;
#50443=CARTESIAN_POINT ( 'NONE',  ( 10.00000000000000178, 186.8749999931720538, 0.000000000000000000 ) ) ;
#50445=CARTESIAN_POINT ( 'NONE',  ( -11.35316468750000141, 68.80208332991935549, 3.042071309553159963 ) ) ;
#50446=CARTESIAN_POINT ( 'NONE',  ( -4.088227598258586603E-16, 290.2031250017069510, -6.676582343750001591 ) ) ;
#50448=CARTESIAN_POINT ( 'NONE',  ( 5.676582343750001591, 206.6145833299193555, -9.832129032723420536 ) ) ;
#50449=ORIENTED_EDGE ( 'NONE', *, *, #26613, .T. ) ;
#50453=CARTESIAN_POINT ( 'NONE',  ( 3.042071309553159519, 199.7395833299193555, 11.35316468750000141 ) ) ;
#50457=ORIENTED_EDGE ( 'NONE', *, *, #12372, .T. ) ;
#50458=CARTESIAN_POINT ( 'NONE',  ( 11.35316468749999963, 196.3020833299193271, -3.042071309553165293 ) ) ;
#50466=CARTESIAN_POINT ( 'NONE',  ( 8.660254037844389075, 10.41666666666666785, -5.000000000000000000 ) ) ;
#50469=( BOUNDED_CURVE ( )  B_SPLINE_CURVE ( 2, ( #1891, #31677, #36960, #7917, #72406, #37715, #60715, #42974, #24878 ),
 .UNSPECIFIED., .F., .F. ) 
 B_SPLINE_CURVE_WITH_KNOTS ( ( 3, 2, 2, 2, 3 ),
 ( 0.8541666666666649643, 0.8645833333333317050, 0.8749999999999984457, 0.8854166666666650753, 0.8958333333333318160 ),
 .UNSPECIFIED. ) 
 CURVE ( )  GEOMETRIC_REPRESENTATION_ITEM ( )  RATIONAL_B_SPLINE_CURVE ( ( 1.000000000000012212, 0.9238795325112745260, 1.000000000000000000, 0.9238795325112867385, 1.000000000000000000, 0.9238795325112867385, 1.000000000000000000, 0.9238795325112980628, 0.9999999999999886757 ) ) 
 REPRESENTATION_ITEM ( '' )  );
#50470=VERTEX_POINT ( 'NONE', #64651 ) ;
#50474=ORIENTED_EDGE ( 'NONE', *, *, #18214, .F. ) ;
#50487=ORIENTED_EDGE ( 'NONE', *, *, #38096, .T. ) ;
#50489=CARTESIAN_POINT ( 'NONE',  ( 5.676582343749993598, 75.26041666325268409, 9.832129032723422313 ) ) ;
#50490=CYLINDRICAL_SURFACE ( 'NONE', #40854, 10.00000000000000178 ) ;
#50494=CARTESIAN_POINT ( 'NONE',  ( 1.226468279477575784E-15, 288.8593750017070079, 6.676582343750001591 ) ) ;
#50497=CARTESIAN_POINT ( 'NONE',  ( 0.000000000000000000, 300.0000000000000000, 0.000000000000000000 ) ) ;
#50503=CARTESIAN_POINT ( 'NONE',  ( -11.35316468750000141, 173.5937499965860411, -1.390361679473963753E-15 ) ) ;
#50507=DIRECTION ( 'NONE',  ( 0.000000000000000000, 0.000000000000000000, 1.000000000000000000 ) ) ;
#50511=CARTESIAN_POINT ( 'NONE',  ( 3.042071309553159519, 54.73958332991934839, 11.35316468750000141 ) ) ;
#50513=CARTESIAN_POINT ( 'NONE',  ( 5.000000000000001776, 17.70833332650536818, -8.660254037844389075 ) ) ;
#50517=CARTESIAN_POINT ( 'NONE',  ( -11.35316468750000141, 53.28124999658601979, -1.390361679473963753E-15 ) ) ;
#50523=CARTESIAN_POINT ( 'NONE',  ( -11.35316468749999785, 43.07291666325267698, -3.042071309553167957 ) ) ;
#50526=CARTESIAN_POINT ( 'NONE',  ( 10.00000000000000000, 205.0000000000000284, 0.000000000000000000 ) ) ;
#50527=CARTESIAN_POINT ( 'NONE',  ( -5.676582343750006032, 179.1145833299193555, 9.832129032723418760 ) ) ;
#50529=CARTESIAN_POINT ( 'NONE',  ( 8.660254037844385522, 136.4583333265053682, 5.000000000000005329 ) ) ;
#50532=CARTESIAN_POINT ( 'NONE',  ( 11.35316468749999785, 40.88541666325268409, 3.042071309553174174 ) ) ;
#50541=CARTESIAN_POINT ( 'NONE',  ( -5.676582343749998039, 172.4479166632526983, -9.832129032723420536 ) ) ;
#50552=CARTESIAN_POINT ( 'NONE',  ( 8.311093377946834337, 115.4687499965860269, 8.311093377946839666 ) ) ;
#50581=CARTESIAN_POINT ( 'NONE',  ( -10.00000000000000000, 127.2916666666666714, -2.679491924311229845 ) ) ;
#50583=CARTESIAN_POINT ( 'NONE',  ( -4.721056650415998313, 290.7343750017069510, 4.721056650416000089 ) ) ;
#50586=CYLINDRICAL_SURFACE ( 'NONE', #16877, 10.00000000000000178 ) ;
#50595=CARTESIAN_POINT ( 'NONE',  ( -1.836970198721029983E-15, 215.6249999931720538, 10.00000000000000178 ) ) ;
#50597=CARTESIAN_POINT ( 'NONE',  ( 8.311093377946834337, 15.15624999658601624, 8.311093377946839666 ) ) ;
#50599=CARTESIAN_POINT ( 'NONE',  ( -5.676582343750006032, 209.4270833299193555, 9.832129032723418760 ) ) ;
#50607=CARTESIAN_POINT ( 'NONE',  ( 3.042071309553167069, 11.82291666325268231, -11.35316468749999785 ) ) ;
#50611=DIRECTION ( 'NONE',  ( 0.000000000000000000, 0.000000000000000000, 1.000000000000000000 ) ) ;
#50613=CARTESIAN_POINT ( 'NONE',  ( -11.35316468750000141, 3.281249996586016238, -1.390361679473963753E-15 ) ) ;
#50616=CARTESIAN_POINT ( 'NONE',  ( 11.35316468749999785, 135.5729166632526983, 3.042071309553174174 ) ) ;
#50617=CARTESIAN_POINT ( 'NONE',  ( 10.00000000000000000, 101.6666666598386826, 2.679491924311236062 ) ) ;
#50619=DIRECTION ( 'NONE',  ( -0.000000000000000000, 1.000000000000000000, -0.000000000000000000 ) ) ;
#50623=CARTESIAN_POINT ( 'NONE',  ( 9.832129032723420536, 1.510416663252683422, -5.676582343749999815 ) ) ;
#50624=EDGE_CURVE ( 'NONE', #18394, #33017, #47068, .T. ) ;
#50625=CARTESIAN_POINT ( 'NONE',  ( 6.676582343750004256, 288.0468750017070079, 2.765530957081995478 ) ) ;
#50631=VERTEX_POINT ( 'NONE', #9910 ) ;
#50634=CARTESIAN_POINT ( 'NONE',  ( -11.35316468749999785, 163.3854166632526699, -3.042071309553167957 ) ) ;
#50635=PLANE ( 'NONE',  #27836 ) ;
#50638=CARTESIAN_POINT ( 'NONE',  ( -11.35316468750000141, 78.59374999658601268, -1.390361679473963753E-15 ) ) ;
#50644=CARTESIAN_POINT ( 'NONE',  ( 8.660254037844385522, 66.45833332650536818, 5.000000000000005329 ) ) ;
#50651=FACE_OUTER_BOUND ( 'NONE', #44623, .T. ) ;
#50663=ORIENTED_EDGE ( 'NONE', *, *, #10876, .F. ) ;
#50665=CARTESIAN_POINT ( 'NONE',  ( 0.000000000000000000, 300.0000000000000000, 10.00000000000000178 ) ) ;
#50668=CARTESIAN_POINT ( 'NONE',  ( 6.123233995736767268E-16, 86.25000000000001421, -10.00000000000000178 ) ) ;
#50670=CARTESIAN_POINT ( 'NONE',  ( -6.000000000000001776, 292.0000000000000000, 0.000000000000000000 ) ) ;
#50674=DIRECTION ( 'NONE',  ( -0.000000000000000000, 1.000000000000000000, -0.000000000000000000 ) ) ;
#50677=DIRECTION ( 'NONE',  ( -0.000000000000000000, 1.000000000000000000, -0.000000000000000000 ) ) ;
#50681=CARTESIAN_POINT ( 'NONE',  ( 10.00000000000000178, 200.0000000000000000, 0.000000000000000000 ) ) ;
#50684=CARTESIAN_POINT ( 'NONE',  ( 11.35316468749999963, 171.3020833299193555, -3.042071309553165293 ) ) ;
#50688=DIRECTION ( 'NONE',  ( 0.000000000000000000, 0.000000000000000000, 1.000000000000000000 ) ) ;
#50691=CARTESIAN_POINT ( 'NONE',  ( -8.311093377946836114, 17.96874999658601979, -8.311093377946837890 ) ) ;
#50699=CARTESIAN_POINT ( 'NONE',  ( -10.00000000000000355, 59.58333332650535397, 2.679491924311223183 ) ) ;
#50702=DIRECTION ( 'NONE',  ( 0.000000000000000000, 1.000000000000000000, 0.000000000000000000 ) ) ;
#50704=CARTESIAN_POINT ( 'NONE',  ( 2.030339228148215693E-11, 166.2499999999984368, -10.00000000000000178 ) ) ;
#50713=CARTESIAN_POINT ( 'NONE',  ( -11.35316468750000141, 138.4895833299193271, 3.042071309553159963 ) ) ;
#50727=CARTESIAN_POINT ( 'NONE',  ( -8.311093377946841443, 109.2187499965860127, 8.311093377946834337 ) ) ;
#50731=CARTESIAN_POINT ( 'NONE',  ( -5.676582343750006032, 39.42708332991935549, 9.832129032723418760 ) ) ;
#50739=CARTESIAN_POINT ( 'NONE',  ( 4.242640687119287435, 297.4375000034140157, 4.242640687119285658 ) ) ;
#50740=CARTESIAN_POINT ( 'NONE',  ( 10.00000000000000178, 112.0833333265053682, -2.679491924311226736 ) ) ;
#50742=CARTESIAN_POINT ( 'NONE',  ( 9.832129032723416984, 155.6770833299193555, 5.676582343750006032 ) ) ;
#50756=CARTESIAN_POINT ( 'NONE',  ( -7.320508075688773708, 208.7499999931719969, -7.320508075688774596 ) ) ;
#50758=CARTESIAN_POINT ( 'NONE',  ( 2.679491924311222739, 38.95833333333333570, 10.00000000000000355 ) ) ;
#50762=CARTESIAN_POINT ( 'NONE',  ( -2.765530957081998142, 287.6406250017069510, 6.676582343750000703 ) ) ;
#50773=CARTESIAN_POINT ( 'NONE',  ( 2.679491924311228956, 166.0416666666666572, -10.00000000000000000 ) ) ;
#50777=CARTESIAN_POINT ( 'NONE',  ( -3.042071309553173730, 129.6354166632526415, 11.35316468749999785 ) ) ;
#50791=CARTESIAN_POINT ( 'NONE',  ( 5.676582343750001591, 206.9270833299193555, -9.832129032723420536 ) ) ;
#50798=CARTESIAN_POINT ( 'NONE',  ( 5.676582343750001591, 96.61458332991935549, -9.832129032723420536 ) ) ;
#50806=CARTESIAN_POINT ( 'NONE',  ( -8.311093377946841443, 108.9062499965860127, 8.311093377946830785 ) ) ;
#50814=CARTESIAN_POINT ( 'NONE',  ( 5.676582343750001591, 81.61458332991935549, -9.832129032723420536 ) ) ;
#50815=ADVANCED_FACE ( 'NONE', ( #33686 ), #5741, .T. ) ;
#50819=CARTESIAN_POINT ( 'NONE',  ( -8.660254037844387298, 188.9583333265053966, -5.000000000000004441 ) ) ;
#50822=CARTESIAN_POINT ( 'NONE',  ( 11.35316468749999963, 71.30208332991932707, -3.042071309553165293 ) ) ;
#50823=CARTESIAN_POINT ( 'NONE',  ( -4.721056650415998313, 288.5781250017069510, 4.721056650416000089 ) ) ;
#50824=CARTESIAN_POINT ( 'NONE',  ( -3.166186134455097228E-13, 211.2500000000000568, -9.999999999999998224 ) ) ;
#50826=CARTESIAN_POINT ( 'NONE',  ( 11.35316468749999963, 220.9895833299193555, -3.042071309553165293 ) ) ;
#50829=CARTESIAN_POINT ( 'NONE',  ( -6.338291171875001240, 299.2578125025604550, 0.000000000000000000 ) ) ;
#50831=CARTESIAN_POINT ( 'NONE',  ( -2.085542519210945728E-15, 209.5312499965860411, 11.35316468750000141 ) ) ;
#50833=CARTESIAN_POINT ( 'NONE',  ( -5.000000000000005329, 100.2083333265053682, 8.660254037844387298 ) ) ;
#50834=CARTESIAN_POINT ( 'NONE',  ( 6.676582343750004256, 298.8906250017069510, 2.765530957081995478 ) ) ;
#50836=CARTESIAN_POINT ( 'NONE',  ( 5.676582343750001591, 191.9270833299193555, -9.832129032723420536 ) ) ;
#50837=( BOUNDED_CURVE ( )  B_SPLINE_CURVE ( 2, ( #23221, #63961, #58318, #46599, #45480, #46231, #52642, #978, #5141, #23961, #10787, #33823, #39827 ),
 .UNSPECIFIED., .F., .F. ) 
 B_SPLINE_CURVE_WITH_KNOTS ( ( 3, 2, 2, 2, 2, 2, 3 ),
 ( 1.836885797912684914, 1.842119258028978912, 1.847352718145273132, 1.852586178261567573, 1.857819638377861793, 1.863053098494156234, 1.868286558610450454 ),
 .UNSPECIFIED. ) 
 CURVE ( )  GEOMETRIC_REPRESENTATION_ITEM ( )  RATIONAL_B_SPLINE_CURVE ( ( 1.000000000000097922, 0.9659258262889700575, 0.9999999999999998890, 0.9659258262890682012, 0.9999999999999998890, 0.9659258262890682012, 0.9999999999999998890, 0.9659258262890682012, 0.9999999999999998890, 0.9659258262890682012, 0.9999999999999998890, 0.9659258262892623792, 0.9999999999998057110 ) ) 
 REPRESENTATION_ITEM ( '' )  );
#50843=CARTESIAN_POINT ( 'NONE',  ( 10.00000000000000000, 14.79166666666666607, 2.679491924311236062 ) ) ;
#50845=ORIENTED_EDGE ( 'NONE', *, *, #74221, .F. ) ;
#50850=EDGE_CURVE ( 'NONE', #27032, #63005, #73090, .T. ) ;
#50851=ORIENTED_EDGE ( 'NONE', *, *, #3789, .T. ) ;
#50852=CARTESIAN_POINT ( 'NONE',  ( 2.679491924311222739, 15.83333332650536640, 10.00000000000000355 ) ) ;
#50865=CARTESIAN_POINT ( 'NONE',  ( 11.35316468749999785, 85.88541666325268409, 3.042071309553174174 ) ) ;
#50870=CARTESIAN_POINT ( 'NONE',  ( 4.721056650415999201, 288.2343750017069510, -4.721056650415999201 ) ) ;
#50874=CARTESIAN_POINT ( 'NONE',  ( 6.951808397369818766E-16, 197.0312499965860411, -11.35316468750000141 ) ) ;
#50880=CARTESIAN_POINT ( 'NONE',  ( 5.676582343750001591, 171.9270833299193555, -9.832129032723420536 ) ) ;
#50887=CARTESIAN_POINT ( 'NONE',  ( 9.832129032723416984, 60.36458332991935549, 5.676582343750006032 ) ) ;
#50893=CARTESIAN_POINT ( 'NONE',  ( -5.676582343750006032, 59.11458332991934839, 9.832129032723418760 ) ) ;
#50899=CARTESIAN_POINT ( 'NONE',  ( 9.832129032723416984, 45.36458332991934839, 5.676582343750006032 ) ) ;
#50903=CARTESIAN_POINT ( 'NONE',  ( -11.35316468750000141, 173.2812499965860411, -1.390361679473963753E-15 ) ) ;
#50904=CARTESIAN_POINT ( 'NONE',  ( 6.123233995736767268E-16, 148.1249999931720538, -10.00000000000000178 ) ) ;
#50908=CARTESIAN_POINT ( 'NONE',  ( 8.311093377946837890, 31.71874999658601979, -8.311093377946837890 ) ) ;
#50909=CARTESIAN_POINT ( 'NONE',  ( 6.951808397369818766E-16, 187.0312499965860127, -11.35316468750000141 ) ) ;
#50916=CARTESIAN_POINT ( 'NONE',  ( 11.35316468750000141, 160.7812499965860127, 0.000000000000000000 ) ) ;
#50928=CARTESIAN_POINT ( 'NONE',  ( 11.35316468749999785, 120.8854166632526841, 3.042071309553174174 ) ) ;
#50930=CARTESIAN_POINT ( 'NONE',  ( -1.349999999999999867, 255.9999999999997726, 5.686520093750665694 ) ) ;
#50949=DIRECTION ( 'NONE',  ( -0.000000000000000000, 1.000000000000000000, -0.000000000000000000 ) ) ;
#50958=CARTESIAN_POINT ( 'NONE',  ( -8.660254037844390851, 127.9166666666666856, 4.999999999999998224 ) ) ;
#50961=CARTESIAN_POINT ( 'NONE',  ( 1.560533225284023162, 225.9999999999998863, 9.885282897026870685 ) ) ;
#50972=CARTESIAN_POINT ( 'NONE',  ( 1.224646799147353454E-15, 300.0000000000000000, -10.00000000000000178 ) ) ;
#50974=CARTESIAN_POINT ( 'NONE',  ( -11.35316468749999785, 13.07291666325268409, -3.042071309553167513 ) ) ;
#50976=CARTESIAN_POINT ( 'NONE',  ( 6.951808397369818766E-16, 212.3437499965860411, -11.35316468750000141 ) ) ;
#50977=CARTESIAN_POINT ( 'NONE',  ( -2.679491924311226292, 133.3333333265053398, -10.00000000000000178 ) ) ;
#50984=CARTESIAN_POINT ( 'NONE',  ( 9.832129032723416984, 20.36458332991935194, 5.676582343750006032 ) ) ;
#50990=CARTESIAN_POINT ( 'NONE',  ( 3.042071309553159519, 4.739583329919349275, 11.35316468750000141 ) ) ;
#50992=CARTESIAN_POINT ( 'NONE',  ( 11.35316468749999963, 135.9895833299193271, -3.042071309553165293 ) ) ;
#50994=CARTESIAN_POINT ( 'NONE',  ( -8.660254037844387298, 103.9583333265053824, -5.000000000000004441 ) ) ;
#50996=CARTESIAN_POINT ( 'NONE',  ( -2.679491924311226292, 3.333333326505365513, -10.00000000000000178 ) ) ;
#51003=ADVANCED_FACE ( 'NONE', ( #7227 ), #30230, .T. ) ;
#51005=CARTESIAN_POINT ( 'NONE',  ( -6.676582343750001591, 288.6093750017069510, 0.000000000000000000 ) ) ;
#51012=CARTESIAN_POINT ( 'NONE',  ( 5.000000000000001776, 217.7083333265053682, -8.660254037844389075 ) ) ;
#51016=CARTESIAN_POINT ( 'NONE',  ( 9.832129032723416984, 75.67708332991934128, 5.676582343750006032 ) ) ;
#51017=ORIENTED_EDGE ( 'NONE', *, *, #42187, .F. ) ;
#51032=EDGE_CURVE ( 'NONE', #10283, #14049, #67360, .T. ) ;
#51034=EDGE_CURVE ( 'NONE', #51512, #22380, #70654, .T. ) ;
#51049=CARTESIAN_POINT ( 'NONE',  ( -4.999999999999998224, 86.66666666666667140, -8.660254037844389075 ) ) ;
#51051=CARTESIAN_POINT ( 'NONE',  ( 6.000000000000003553, 288.4375000000000000, 2.485281374238571317 ) ) ;
#51060=CARTESIAN_POINT ( 'NONE',  ( -7.320508075688778149, 198.1250000000000000, 7.320508075688769267 ) ) ;
#51062=CARTESIAN_POINT ( 'NONE',  ( 3.042071309553167069, 167.1354166632526415, -11.35316468749999785 ) ) ;
#51063=CARTESIAN_POINT ( 'NONE',  ( -5.000000000000109246, 211.6666666666667993, -8.660254037844580921 ) ) ;
#51070=CARTESIAN_POINT ( 'NONE',  ( 11.35316468750000141, 26.09374999658601624, 0.000000000000000000 ) ) ;
#51073=CARTESIAN_POINT ( 'NONE',  ( -1.836970198721029983E-15, 220.6249999931720538, 10.00000000000000178 ) ) ;
#51077=CARTESIAN_POINT ( 'NONE',  ( 5.000000000000001776, 62.70833332650536818, -8.660254037844389075 ) ) ;
#51088=CARTESIAN_POINT ( 'NONE',  ( 1.584317714026805320E-12, 163.7500000000001137, 9.999999999999998224 ) ) ;
#51089=CARTESIAN_POINT ( 'NONE',  ( 6.123233995736767268E-16, 43.12499999317203248, -10.00000000000000178 ) ) ;
#51090=CARTESIAN_POINT ( 'NONE',  ( 6.951808397369818766E-16, 142.0312499965860411, -11.35316468750000141 ) ) ;
#51103=CARTESIAN_POINT ( 'NONE',  ( -9.832129032723420536, 129.0104166632526983, 5.676582343749997150 ) ) ;
#51107=CARTESIAN_POINT ( 'NONE',  ( -11.35316468750000141, 33.80208332991934839, 3.042071309553159963 ) ) ;
#51114=CARTESIAN_POINT ( 'NONE',  ( 6.000000000000003553, 295.6250000034140157, -2.485281374238571761 ) ) ;
#51117=EDGE_CURVE ( 'NONE', #67846, #70240, #49051, .T. ) ;
#51118=CARTESIAN_POINT ( 'NONE',  ( -11.35316468750000141, 158.5937499965860127, -1.390361679473963753E-15 ) ) ;
#51126=EDGE_CURVE ( 'NONE', #33772, #38706, #32473, .T. ) ;
#51130=ORIENTED_EDGE ( 'NONE', *, *, #51862, .F. ) ;
#51135=CARTESIAN_POINT ( 'NONE',  ( 10.00000000000000000, 34.79166666666666430, 2.679491924311236062 ) ) ;
#51138=CARTESIAN_POINT ( 'NONE',  ( -6.676582343750001591, 290.4531250017069510, 0.000000000000000000 ) ) ;
#51150=CARTESIAN_POINT ( 'NONE',  ( -4.999999999999998224, 166.6666666666666856, -8.660254037844389075 ) ) ;
#51153=( BOUNDED_CURVE ( )  B_SPLINE_CURVE ( 2, ( #17386, #5709, #34400, #442, #45318, #27974, #23421, #34774, #68333, #57401, #28708, #11734, #28340 ),
 .UNSPECIFIED., .F., .F. ) 
 B_SPLINE_CURVE_WITH_KNOTS ( ( 3, 2, 2, 2, 2, 2, 3 ),
 ( 0.9402173913043480047, 0.9420289855072465635, 0.9438405797101451222, 0.9456521739130436810, 0.9474637681159421287, 0.9492753623188406875, 0.9510869565217392463 ),
 .UNSPECIFIED. ) 
 CURVE ( )  GEOMETRIC_REPRESENTATION_ITEM ( )  RATIONAL_B_SPLINE_CURVE ( ( 0.9999999999999957812, 0.9659258262890725311, 1.000000000000000000, 0.9659258262890683122, 1.000000000000000000, 0.9659258262890683122, 1.000000000000000000, 0.9659258262890683122, 1.000000000000000000, 0.9659258262890683122, 1.000000000000000000, 0.9659258262890662028, 1.000000000000001998 ) ) 
 REPRESENTATION_ITEM ( '' )  );
#51155=CARTESIAN_POINT ( 'NONE',  ( -11.35316468750000141, 133.8020833299193555, 3.042071309553159963 ) ) ;
#51160=ORIENTED_EDGE ( 'NONE', *, *, #53428, .T. ) ;
#51161=CARTESIAN_POINT ( 'NONE',  ( 7.080414546044030644, 225.6242882639226082, -7.067909898757898546 ) ) ;
#51162=DIRECTION ( 'NONE',  ( 0.000000000000000000, 0.000000000000000000, 1.000000000000000000 ) ) ;
#51165=CARTESIAN_POINT ( 'NONE',  ( 5.676582343750001591, 211.9270833299193555, -9.832129032723420536 ) ) ;
#51171=CARTESIAN_POINT ( 'NONE',  ( 11.35316468749999963, 90.98958332991935549, -3.042071309553165293 ) ) ;
#51179=CARTESIAN_POINT ( 'NONE',  ( 11.35316468749999963, 95.98958332991935549, -3.042071309553165293 ) ) ;
#51183=CARTESIAN_POINT ( 'NONE',  ( -4.999999999999998224, 218.5416666598387110, -8.660254037844389075 ) ) ;
#51187=CARTESIAN_POINT ( 'NONE',  ( 11.35316468750000141, 105.7812499965860269, 0.000000000000000000 ) ) ;
#51192=CARTESIAN_POINT ( 'NONE',  ( -8.660254037844390851, 184.7916666598387110, 4.999999999999998224 ) ) ;
#51195=CARTESIAN_POINT ( 'NONE',  ( -2.085542519210945728E-15, 84.84374999658601268, 11.35316468750000141 ) ) ;
#51196=CARTESIAN_POINT ( 'NONE',  ( -4.088227598258586603E-16, 291.2031250017069510, -6.676582343750001591 ) ) ;
#51199=CARTESIAN_POINT ( 'NONE',  ( 11.35316468749999963, 225.9895833299193839, -3.042071309553165293 ) ) ;
#51202=DIRECTION ( 'NONE',  ( -0.000000000000000000, 1.000000000000000000, -0.000000000000000000 ) ) ;
#51204=CARTESIAN_POINT ( 'NONE',  ( 5.676582343749993598, 219.9479166632526983, 9.832129032723422313 ) ) ;
#51206=CARTESIAN_POINT ( 'NONE',  ( -5.000000000000097700, 158.3333333333334565, 8.660254037844545394 ) ) ;
#51207=CARTESIAN_POINT ( 'NONE',  ( 6.676582343750003368, 298.0156250017070079, -2.765530957081997254 ) ) ;
#51209=CARTESIAN_POINT ( 'NONE',  ( 6.951808397369818766E-16, 192.3437499965860127, -11.35316468750000141 ) ) ;
#51220=CARTESIAN_POINT ( 'NONE',  ( 7.320508075688774596, 20.62499999999999289, -7.320508075688774596 ) ) ;
#51233=VERTEX_POINT ( 'NONE', #37755 ) ;
#51236=ORIENTED_EDGE ( 'NONE', *, *, #16314, .T. ) ;
#51239=CARTESIAN_POINT ( 'NONE',  ( -8.311093377946836114, 87.96874999658602690, -8.311093377946837890 ) ) ;
#51244=CARTESIAN_POINT ( 'NONE',  ( -6.676582343750002480, 291.5468750017069510, -2.765530957081996810 ) ) ;
#51249=CARTESIAN_POINT ( 'NONE',  ( -3.042071309553173730, 194.3229166632526699, 11.35316468749999785 ) ) ;
#51254=CARTESIAN_POINT ( 'NONE',  ( 3.042071309553167069, 167.1354166632526415, -11.35316468749999785 ) ) ;
#51257=CARTESIAN_POINT ( 'NONE',  ( 0.000000000000000000, 300.0000000000000000, 10.00000000000000178 ) ) ;
#51258=CARTESIAN_POINT ( 'NONE',  ( -7.320508075688773708, 88.74999999317202537, -7.320508075688774596 ) ) ;
#51261=CARTESIAN_POINT ( 'NONE',  ( 8.311093377946837890, 51.40624999658602690, -8.311093377946837890 ) ) ;
#51267=CARTESIAN_POINT ( 'NONE',  ( 8.311093377946837890, 61.40624999658602690, -8.311093377946837890 ) ) ;
#51273=CARTESIAN_POINT ( 'NONE',  ( -3.042071309553163960, 62.23958332991934128, -11.35316468749999963 ) ) ;
#51275=CARTESIAN_POINT ( 'NONE',  ( -10.00000000000000355, 14.58333332650536462, 2.679491924311223183 ) ) ;
#51276=CARTESIAN_POINT ( 'NONE',  ( -3.042071309553173730, 169.3229166632526699, 11.35316468749999785 ) ) ;
#51278=CARTESIAN_POINT ( 'NONE',  ( -7.320508075688773708, 138.7499999931720254, -7.320508075688774596 ) ) ;
#51281=CARTESIAN_POINT ( 'NONE',  ( -11.35316468750000141, 33.80208332991935549, 3.042071309553159963 ) ) ;
#51282=CARTESIAN_POINT ( 'NONE',  ( -3.673940397442060854E-16, 295.8125000034140157, -6.000000000000001776 ) ) ;
#51283=CARTESIAN_POINT ( 'NONE',  ( -9.832129032723420536, 188.6979166632526983, 5.676582343749997150 ) ) ;
#51290=CARTESIAN_POINT ( 'NONE',  ( 3.042071309553159519, 159.7395833299193555, 11.35316468750000141 ) ) ;
#51297=DIRECTION ( 'NONE',  ( 0.000000000000000000, 0.000000000000000000, 1.000000000000000000 ) ) ;
#51298=CARTESIAN_POINT ( 'NONE',  ( -9.832129032723420536, 114.0104166632526983, 5.676582343749997150 ) ) ;
#51299=CARTESIAN_POINT ( 'NONE',  ( 7.320508075688774596, 12.49999999317203425, -7.320508075688774596 ) ) ;
#51302=EDGE_CURVE ( 'NONE', #20100, #63756, #8323, .T. ) ;
#51314=CARTESIAN_POINT ( 'NONE',  ( 10.92737078412413609, 225.9999999999999147, -3.080083792328916825 ) ) ;
#51331=CARTESIAN_POINT ( 'NONE',  ( 7.320508075688771044, 119.3750000000000142, 7.320508075688775484 ) ) ;
#51334=CARTESIAN_POINT ( 'NONE',  ( 4.721056650415999201, 288.2343750017069510, -4.721056650415999201 ) ) ;
#51344=CARTESIAN_POINT ( 'NONE',  ( -5.676582343749998039, 17.44791666325268409, -9.832129032723420536 ) ) ;
#51345=CARTESIAN_POINT ( 'NONE',  ( 2.679491924305073436, 1.041666666667218299, -10.00000000000355094 ) ) ;
#51346=CARTESIAN_POINT ( 'NONE',  ( 9.832129032723416984, 210.6770833299193555, 5.676582343750006032 ) ) ;
#51351=ORIENTED_EDGE ( 'NONE', *, *, #70144, .F. ) ;
#51353=CARTESIAN_POINT ( 'NONE',  ( 11.35316468749999963, 25.98958332991935194, -3.042071309553165293 ) ) ;
#51356=CARTESIAN_POINT ( 'NONE',  ( 2.679491924311082407, 211.0416666666666572, -10.00000000000008349 ) ) ;
#51360=CARTESIAN_POINT ( 'NONE',  ( -11.35316468750000141, 8.489583329919348387, 3.042071309553159963 ) ) ;
#51362=CARTESIAN_POINT ( 'NONE',  ( 8.311093377946834337, 130.1562499965860411, 8.311093377946839666 ) ) ;
#51363=CARTESIAN_POINT ( 'NONE',  ( 10.00000000000000000, 96.66666665983871098, 2.679491924311236062 ) ) ;
#51367=LINE ( 'NONE', #16649, #41391 ) ;
#51369=CARTESIAN_POINT ( 'NONE',  ( -10.00000000000000533, 117.2916666666666714, -2.679491924311231177 ) ) ;
#51372=CARTESIAN_POINT ( 'NONE',  ( -6.676582343750000703, 298.5156250017070079, 2.765530957082001251 ) ) ;
#51373=CARTESIAN_POINT ( 'NONE',  ( 6.951808397369818766E-16, 132.0312499965860127, -11.35316468750000141 ) ) ;
#51384=CARTESIAN_POINT ( 'NONE',  ( -5.676582343749998039, 72.76041666325268409, -9.832129032723420536 ) ) ;
#51391=CARTESIAN_POINT ( 'NONE',  ( -10.00000000000000000, 109.1666666598386968, -2.679491924311229845 ) ) ;
#51396=EDGE_CURVE ( 'NONE', #21207, #33772, #36504, .T. ) ;
#51397=CARTESIAN_POINT ( 'NONE',  ( 8.660254037844383745, 110.4166666666666714, -4.999999999999997335 ) ) ;
#51411=CARTESIAN_POINT ( 'NONE',  ( -4.242640687119286547, 291.8750000000000000, -4.242640687119286547 ) ) ;
#51417=CARTESIAN_POINT ( 'NONE',  ( 7.320508075688774596, 80.62500000000000000, -7.320508075688774596 ) ) ;
#51419=CARTESIAN_POINT ( 'NONE',  ( 1.102182119232618108E-15, 290.2500000000000000, 6.000000000000001776 ) ) ;
#51422=CARTESIAN_POINT ( 'NONE',  ( 4.242640687119287435, 294.3750000000000000, 4.242640687119285658 ) ) ;
#51426=CARTESIAN_POINT ( 'NONE',  ( 8.660254037844385522, 56.45833332650536818, 5.000000000000005329 ) ) ;
#51430=CARTESIAN_POINT ( 'NONE',  ( 7.320508075688771044, 199.3750000000000000, 7.320508075688775484 ) ) ;
#51432=CARTESIAN_POINT ( 'NONE',  ( -11.35316468749999785, 168.3854166632526699, -3.042071309553167513 ) ) ;
#51437=VERTEX_POINT ( 'NONE', #45921 ) ;
#51439=CARTESIAN_POINT ( 'NONE',  ( 8.311093377946834337, 40.46874999658601979, 8.311093377946839666 ) ) ;
#51442=DIRECTION ( 'NONE',  ( 0.000000000000000000, 0.000000000000000000, 1.000000000000000000 ) ) ;
#51446=CARTESIAN_POINT ( 'NONE',  ( 5.000000000000001776, 67.70833332650536818, -8.660254037844389075 ) ) ;
#51459=CARTESIAN_POINT ( 'NONE',  ( -9.832129032723420536, 138.6979166632526983, 5.676582343749997150 ) ) ;
#51460=CARTESIAN_POINT ( 'NONE',  ( 7.320508075688763050, 105.6250000000000142, -7.320508075688763050 ) ) ;
#51472=CARTESIAN_POINT ( 'NONE',  ( -9.832129032723418760, 123.1770833299193555, -5.676582343750004256 ) ) ;
#51477=CARTESIAN_POINT ( 'NONE',  ( -3.042071309553164404, 42.55208332991933418, -11.35316468749999963 ) ) ;
#51479=DIRECTION ( 'NONE',  ( -0.000000000000000000, 1.000000000000000000, -0.000000000000000000 ) ) ;
#51484=CARTESIAN_POINT ( 'NONE',  ( -4.242640687119286547, 297.9375000034140157, -4.242640687119286547 ) ) ;
#51488=CARTESIAN_POINT ( 'NONE',  ( -11.35316468750000141, 153.5937499965860127, -1.390361679473963753E-15 ) ) ;
#51501=ORIENTED_EDGE ( 'NONE', *, *, #25586, .F. ) ;
#51506=CARTESIAN_POINT ( 'NONE',  ( 10.00000000000000178, 45.20833333333332860, -2.679491924311226736 ) ) ;
#51512=VERTEX_POINT ( 'NONE', #35369 ) ;
#51518=CARTESIAN_POINT ( 'NONE',  ( -4.999999999999998224, 138.5416666598387110, -8.660254037844389075 ) ) ;
#51519=CARTESIAN_POINT ( 'NONE',  ( -7.320508075688778149, 163.1250000000000284, 7.320508075688769267 ) ) ;
#51523=CARTESIAN_POINT ( 'NONE',  ( 5.676582343749993598, 125.2604166632526841, 9.832129032723422313 ) ) ;
#51534=CARTESIAN_POINT ( 'NONE',  ( 11.35316468749999963, 221.3020833299192986, -3.042071309553165293 ) ) ;
#51541=CARTESIAN_POINT ( 'NONE',  ( 9.832129032723416984, 100.3645833299193697, 5.676582343750006032 ) ) ;
#51547=CARTESIAN_POINT ( 'NONE',  ( -9.832129032723418760, 102.8645833299193697, -5.676582343750004256 ) ) ;
#51551=CARTESIAN_POINT ( 'NONE',  ( -7.320508075688778149, 224.9999999931720254, 7.320508075688769267 ) ) ;
#51554=CARTESIAN_POINT ( 'NONE',  ( 5.676582343749993598, 99.94791666325268409, 9.832129032723422313 ) ) ;
#51559=ORIENTED_EDGE ( 'NONE', *, *, #48966, .T. ) ;
#51560=CARTESIAN_POINT ( 'NONE',  ( 2.679491924311222739, 200.8333333265053398, 10.00000000000000355 ) ) ;
#51563=CARTESIAN_POINT ( 'NONE',  ( 3.042071309553167513, 82.13541666325269830, -11.35316468749999785 ) ) ;
#51564=CARTESIAN_POINT ( 'NONE',  ( 4.721056650416000089, 288.8281250017069510, 4.721056650415999201 ) ) ;
#51568=CARTESIAN_POINT ( 'NONE',  ( -2.085542519210945728E-15, 224.5312499965860127, 11.35316468750000141 ) ) ;
#51573=CARTESIAN_POINT ( 'NONE',  ( -9.832129032723420536, 213.6979166632526983, 5.676582343749997150 ) ) ;
#51575=CARTESIAN_POINT ( 'NONE',  ( 1.226468279477575784E-15, 296.7031250017070079, 6.676582343750001591 ) ) ;
#51578=CARTESIAN_POINT ( 'NONE',  ( 8.311093377946837890, 211.7187499965860127, -8.311093377946837890 ) ) ;
#51588=CARTESIAN_POINT ( 'NONE',  ( -7.320508075688773708, 26.87500000000000355, -7.320508075688774596 ) ) ;
#51589=AXIS2_PLACEMENT_3D ( 'NONE', #61290, #44312, #14499 ) ;
#51601=CARTESIAN_POINT ( 'NONE',  ( 2.765530957081996366, 295.1406250017069510, -6.676582343750002480 ) ) ;
#51604=CARTESIAN_POINT ( 'NONE',  ( -5.999999999999999112, 289.1250000034141294, 2.485281374238575314 ) ) ;
#51613=CARTESIAN_POINT ( 'NONE',  ( -8.311093377946841443, 89.21874999658602690, 8.311093377946830785 ) ) ;
#51622=CARTESIAN_POINT ( 'NONE',  ( -9.832129032723420536, 203.6979166632526983, 5.676582343749997150 ) ) ;
#51625=EDGE_CURVE ( 'NONE', #29110, #28748, #51945, .T. ) ;
#51629=CARTESIAN_POINT ( 'NONE',  ( -8.311093377946836114, 177.9687499965860127, -8.311093377946837890 ) ) ;
#51633=CARTESIAN_POINT ( 'NONE',  ( -8.660254037844390851, 89.79166665983869677, 4.999999999999998224 ) ) ;
#51637=CARTESIAN_POINT ( 'NONE',  ( -11.35316468750000141, 58.28124999658601268, -1.390361679473963753E-15 ) ) ;
#51643=CARTESIAN_POINT ( 'NONE',  ( -11.35316468750000141, 58.28124999658601268, -1.390361679473963753E-15 ) ) ;
#51649=CARTESIAN_POINT ( 'NONE',  ( -11.35316468749999785, 58.07291666325268409, -3.042071309553167957 ) ) ;
#51652=CARTESIAN_POINT ( 'NONE',  ( -8.311093377946841443, 173.9062499965860411, 8.311093377946830785 ) ) ;
#51653=CIRCLE ( 'NONE', #27517, 10.00000000000000178 ) ;
#51654=CARTESIAN_POINT ( 'NONE',  ( 7.320508075688771044, 146.2499999931719969, 7.320508075688775484 ) ) ;
#51657=CARTESIAN_POINT ( 'NONE',  ( -3.042071309553163960, 42.55208332991934128, -11.35316468749999963 ) ) ;
#51659=CARTESIAN_POINT ( 'NONE',  ( -11.35316468750000141, 178.4895833299193555, 3.042071309553159963 ) ) ;
#51665=CARTESIAN_POINT ( 'NONE',  ( -8.311093377946836114, 182.6562499965860411, -8.311093377946837890 ) ) ;
#51672=CARTESIAN_POINT ( 'NONE',  ( 11.35316468749999785, 125.8854166632526983, 3.042071309553174174 ) ) ;
#51673=CARTESIAN_POINT ( 'NONE',  ( 2.679491924311222739, 10.83333332650536640, 10.00000000000000355 ) ) ;
#51702=CARTESIAN_POINT ( 'NONE',  ( -4.721056650415998313, 298.7343750017069510, 4.721056650416000089 ) ) ;
#51703=CARTESIAN_POINT ( 'NONE',  ( -7.320508075688773708, 116.8750000000000000, -7.320508075688774596 ) ) ;
#51705=CARTESIAN_POINT ( 'NONE',  ( -2.765530957081996810, 288.4218750017070079, -6.676582343750003368 ) ) ;
#51714=CARTESIAN_POINT ( 'NONE',  ( 2.250000000000000000, 284.0000000000000000, 5.562148865321749014 ) ) ;
#51718=CARTESIAN_POINT ( 'NONE',  ( 11.35316468749999963, 15.98958332991934839, -3.042071309553165293 ) ) ;
#51720=CARTESIAN_POINT ( 'NONE',  ( -2.085542519210945728E-15, 224.8437499965860127, 11.35316468750000141 ) ) ;
#51729=CARTESIAN_POINT ( 'NONE',  ( -9.832129032723420536, 28.69791666325268409, 5.676582343749997150 ) ) ;
#51733=DIRECTION ( 'NONE',  ( 0.000000000000000000, 0.000000000000000000, 1.000000000000000000 ) ) ;
#51735=CARTESIAN_POINT ( 'NONE',  ( -11.35316468749999785, 23.07291666325268054, -3.042071309553167957 ) ) ;
#51737=CARTESIAN_POINT ( 'NONE',  ( -11.35316468750000141, 133.2812499965860127, -1.390361679473963753E-15 ) ) ;
#51739=CARTESIAN_POINT ( 'NONE',  ( 2.679491924311228956, 102.9166666598386826, -10.00000000000000000 ) ) ;
#51744=ORIENTED_EDGE ( 'NONE', *, *, #28892, .F. ) ;
#51745=CARTESIAN_POINT ( 'NONE',  ( 11.35316468749999963, 11.30208332991934839, -3.042071309553165293 ) ) ;
#51747=CARTESIAN_POINT ( 'NONE',  ( 6.676582343750001591, 298.9531250017069510, -8.176455196517173205E-16 ) ) ;
#51748=CARTESIAN_POINT ( 'NONE',  ( -2.085542519210945728E-15, 139.5312499965860411, 11.35316468750000141 ) ) ;
#51760=CARTESIAN_POINT ( 'NONE',  ( 9.832129032723416984, 70.67708332991935549, 5.676582343750006032 ) ) ;
#51765=ORIENTED_EDGE ( 'NONE', *, *, #23518, .T. ) ;
#51767=CARTESIAN_POINT ( 'NONE',  ( -8.660254037844387298, 108.9583333265053682, -5.000000000000004441 ) ) ;
#51772=PRODUCT ( 'spindle', 'spindle', '', ( #28594 ) ) ;
#51775=DIRECTION ( 'NONE',  ( -0.000000000000000000, 1.000000000000000000, -0.000000000000000000 ) ) ;
#51786=VERTEX_POINT ( 'NONE', #38697 ) ;
#51792=CARTESIAN_POINT ( 'NONE',  ( 10.00000000000000000, 79.79166666666668561, 2.679491924311236062 ) ) ;
#51793=EDGE_CURVE ( 'NONE', #53587, #14276, #18655, .T. ) ;
#51796=CARTESIAN_POINT ( 'NONE',  ( -3.042071309553173730, 59.63541666325267698, 11.35316468749999785 ) ) ;
#51797=CARTESIAN_POINT ( 'NONE',  ( 2.485281374238575314, 290.3124999999999432, 6.000000000000000888 ) ) ;
#51802=CARTESIAN_POINT ( 'NONE',  ( 5.000000000000001776, 57.70833332650537528, -8.660254037844389075 ) ) ;
#51807=( BOUNDED_CURVE ( )  B_SPLINE_CURVE ( 2, ( #3517, #32192, #72551, #21599, #51767, #51391, #28751, #28382, #114, #34072, #74030, #4641, #46104 ),
 .UNSPECIFIED., .F., .F. ) 
 B_SPLINE_CURVE_WITH_KNOTS ( ( 3, 2, 2, 2, 2, 2, 3 ),
 ( 0.4619565217391304879, 0.4637681159420290466, 0.4655797101449276054, 0.4673913043478261642, 0.4692028985507246674, 0.4710144927536232262, 0.4728260869565217850 ),
 .UNSPECIFIED. ) 
 CURVE ( )  GEOMETRIC_REPRESENTATION_ITEM ( )  RATIONAL_B_SPLINE_CURVE ( ( 0.9999999999999990008, 0.9659258262890693114, 1.000000000000000000, 0.9659258262890683122, 1.000000000000000000, 0.9659258262890683122, 1.000000000000000000, 0.9659258262890683122, 1.000000000000000000, 0.9659258262890683122, 1.000000000000000000, 0.9659258262890673130, 1.000000000000001110 ) ) 
 REPRESENTATION_ITEM ( '' )  );
#51808=CARTESIAN_POINT ( 'NONE',  ( 4.999999999999993783, 199.1666666666666856, 8.660254037844390851 ) ) ;
#51810=CARTESIAN_POINT ( 'NONE',  ( 3.042071309553167069, 162.1354166632526983, -11.35316468749999785 ) ) ;
#51811=CARTESIAN_POINT ( 'NONE',  ( -7.320508075688936245, 211.8750000000000853, -7.320508075688936245 ) ) ;
#51812=CARTESIAN_POINT ( 'NONE',  ( 2.679491924311222739, 175.8333333265053966, 10.00000000000000355 ) ) ;
#51814=CARTESIAN_POINT ( 'NONE',  ( -2.485281374238967000, 296.8750000034140726, -5.999999999999608313 ) ) ;
#51818=CARTESIAN_POINT ( 'NONE',  ( 11.35316468749999963, 36.30208332991935549, -3.042071309553165293 ) ) ;
#51822=CARTESIAN_POINT ( 'NONE',  ( 4.999999999999993783, 221.0416666598387110, 8.660254037844390851 ) ) ;
#51823=FACE_OUTER_BOUND ( 'NONE', #6233, .T. ) ;
#51826=CARTESIAN_POINT ( 'NONE',  ( 2.679491924311228956, 62.91666665983868967, -10.00000000000000000 ) ) ;
#51834=CARTESIAN_POINT ( 'NONE',  ( -2.679491924304188810, 196.4583333333328596, -10.00000000000419043 ) ) ;
#51835=CARTESIAN_POINT ( 'NONE',  ( -4.721056650415999201, 297.4843750017070079, -4.721056650415999201 ) ) ;
#51837=DIRECTION ( 'NONE',  ( -0.000000000000000000, 1.000000000000000000, -0.000000000000000000 ) ) ;
#51838=CARTESIAN_POINT ( 'NONE',  ( -3.042071309553164404, 142.2395833299193839, -11.35316468749999963 ) ) ;
#51844=ADVANCED_FACE ( 'NONE', ( #16029 ), #72261, .T. ) ;
#51847=EDGE_CURVE ( 'NONE', #63005, #56250, #67357, .T. ) ;
#51851=CARTESIAN_POINT ( 'NONE',  ( -8.311093377946836114, 122.9687499965860127, -8.311093377946837890 ) ) ;
#51855=CARTESIAN_POINT ( 'NONE',  ( -5.676582343749998039, 37.76041666325267698, -9.832129032723420536 ) ) ;
#51862=EDGE_CURVE ( 'NONE', #23203, #62806, #47352, .T. ) ;
#51866=CARTESIAN_POINT ( 'NONE',  ( -3.673940397442060854E-16, 297.8125000034140157, -6.000000000000001776 ) ) ;
#51870=CARTESIAN_POINT ( 'NONE',  ( -9.832129032723420536, 154.0104166632526983, 5.676582343749997150 ) ) ;
#51881=CARTESIAN_POINT ( 'NONE',  ( -10.00000000000007816, 57.29166666666671404, -2.679491924311251605 ) ) ;
#51885=CARTESIAN_POINT ( 'NONE',  ( -2.485281374238159646, 298.2500000034140157, 6.000000000000414779 ) ) ;
#51887=CARTESIAN_POINT ( 'NONE',  ( -1.836970198721029983E-15, 38.75000000000000000, 10.00000000000000178 ) ) ;
#51892=CARTESIAN_POINT ( 'NONE',  ( 2.679491924311228956, 197.9166666598386826, -10.00000000000000000 ) ) ;
#51897=CARTESIAN_POINT ( 'NONE',  ( -7.320508075688778149, 9.999999993172032475, 7.320508075688769267 ) ) ;
#51901=CARTESIAN_POINT ( 'NONE',  ( 7.320508075688774596, 155.6250000000000284, -7.320508075688774596 ) ) ;
#51905=CARTESIAN_POINT ( 'NONE',  ( 3.042071309553159519, 130.0520833299193555, 11.35316468750000141 ) ) ;
#51917=EDGE_CURVE ( 'NONE', #73747, #64725, #46646, .T. ) ;
#51918=CARTESIAN_POINT ( 'NONE',  ( -4.999999999999998224, 18.54166665983870033, -8.660254037844389075 ) ) ;
#51925=CARTESIAN_POINT ( 'NONE',  ( -11.35316468750000141, 103.2812499965860269, -1.390361679473963753E-15 ) ) ;
#51930=CARTESIAN_POINT ( 'NONE',  ( 8.660254037844525854, 40.41666666666676377, -5.000000000000079936 ) ) ;
#51932=CARTESIAN_POINT ( 'NONE',  ( 5.676582343750001591, 101.6145833299193697, -9.832129032723420536 ) ) ;
#51936=CARTESIAN_POINT ( 'NONE',  ( 2.679491924311228956, 217.9166666598387110, -10.00000000000000000 ) ) ;
#51940=CARTESIAN_POINT ( 'NONE',  ( 5.676582343749993598, 94.94791666325269830, 9.832129032723422313 ) ) ;
#51945=( BOUNDED_CURVE ( )  B_SPLINE_CURVE ( 2, ( #2865, #42101, #43213, #53812, #8151, #71139, #36828, #19463, #65113, #42474, #3239, #59837, #13424 ),
 .UNSPECIFIED., .F., .F. ) 
 B_SPLINE_CURVE_WITH_KNOTS ( ( 3, 2, 2, 2, 2, 2, 3 ),
 ( 0.5380434782608695121, 0.5398550724637680709, 0.5416666666666666297, 0.5434782608695651884, 0.5452898550724637472, 0.5471014492753623060, 0.5489130434782608647 ),
 .UNSPECIFIED. ) 
 CURVE ( )  GEOMETRIC_REPRESENTATION_ITEM ( )  RATIONAL_B_SPLINE_CURVE ( ( 1.000000000000000000, 0.9659258262890683122, 1.000000000000000000, 0.9659258262890683122, 1.000000000000000000, 0.9659258262890683122, 1.000000000000000000, 0.9659258262890683122, 1.000000000000000000, 0.9659258262890683122, 1.000000000000000000, 0.9659258262890683122, 1.000000000000000000 ) ) 
 REPRESENTATION_ITEM ( '' )  );
#51946=CARTESIAN_POINT ( 'NONE',  ( -7.320508075688778149, 189.9999999931720538, 7.320508075688769267 ) ) ;
#51950=CARTESIAN_POINT ( 'NONE',  ( -2.085542519210945728E-15, 89.84374999658602690, 11.35316468750000141 ) ) ;
#51951=CARTESIAN_POINT ( 'NONE',  ( -4.088227598258586603E-16, 288.2031250017069510, -6.676582343750001591 ) ) ;
#51954=CARTESIAN_POINT ( 'NONE',  ( 11.35316468750000141, 220.7812499965860127, 0.000000000000000000 ) ) ;
#51959=CARTESIAN_POINT ( 'NONE',  ( 11.35316468749999785, 220.5729166632526415, 3.042071309553174174 ) ) ;
#51961=CARTESIAN_POINT ( 'NONE',  ( -7.320508075688912264, 158.1250000000000853, 7.320508075688904270 ) ) ;
#51962=CARTESIAN_POINT ( 'NONE',  ( -6.676582343750001591, 298.4531250017069510, 0.000000000000000000 ) ) ;
#51963=EDGE_LOOP ( 'NONE', ( #46769, #43597, #24492, #35382 ) ) ;
#51965=CARTESIAN_POINT ( 'NONE',  ( -3.042071309553163960, 202.5520833299193555, -11.35316468749999963 ) ) ;
#51973=CARTESIAN_POINT ( 'NONE',  ( 8.660254037844389075, 30.41666666666666785, -5.000000000000000000 ) ) ;
#51983=CARTESIAN_POINT ( 'NONE',  ( 6.123233995736767268E-16, 153.1249999931720538, -10.00000000000000178 ) ) ;
#51984=CARTESIAN_POINT ( 'NONE',  ( -6.676582343749999815, 294.5156250017069510, 2.765530957082001251 ) ) ;
#51993=ORIENTED_EDGE ( 'NONE', *, *, #16701, .F. ) ;
#51995=CARTESIAN_POINT ( 'NONE',  ( 9.832129032723416984, 85.67708332991935549, 5.676582343750006032 ) ) ;
#52002=AXIS2_PLACEMENT_3D ( 'NONE', #47819, #41801, #42155 ) ;
#52004=CARTESIAN_POINT ( 'NONE',  ( -5.676582343750006032, 199.1145833299193555, 9.832129032723418760 ) ) ;
#52008=CARTESIAN_POINT ( 'NONE',  ( 9.832129032723416984, 185.6770833299193555, 5.676582343750006032 ) ) ;
#52016=CARTESIAN_POINT ( 'NONE',  ( 3.042071309553159519, 64.73958332991935549, 11.35316468750000141 ) ) ;
#52022=CARTESIAN_POINT ( 'NONE',  ( 8.311093377946837890, 56.40624999658600558, -8.311093377946837890 ) ) ;
#52028=CARTESIAN_POINT ( 'NONE',  ( -2.085542519210945728E-15, 54.53124999658601979, 11.35316468750000141 ) ) ;
#52031=CARTESIAN_POINT ( 'NONE',  ( 6.123233995736767268E-16, 158.1249999931720254, -10.00000000000000178 ) ) ;
#52035=CARTESIAN_POINT ( 'NONE',  ( 6.951808397369818766E-16, 47.34374999658602690, -11.35316468750000141 ) ) ;
#52036=( BOUNDED_CURVE ( )  B_SPLINE_CURVE ( 2, ( #53116, #1451, #34670, #35766, #17658, #30469, #6723, #40677, #24432, #29730, #47802, #13097, #57673 ),
 .UNSPECIFIED., .F., .F. ) 
 B_SPLINE_CURVE_WITH_KNOTS ( ( 3, 2, 2, 2, 2, 2, 3 ),
 ( 0.7663043478260869179, 0.7681159420289854767, 0.7699275362318840354, 0.7717391304347825942, 0.7735507246376811530, 0.7753623188405797118, 0.7771739130434782705 ),
 .UNSPECIFIED. ) 
 CURVE ( )  GEOMETRIC_REPRESENTATION_ITEM ( )  RATIONAL_B_SPLINE_CURVE ( ( 1.000000000000000000, 0.9659258262890683122, 1.000000000000000000, 0.9659258262890683122, 1.000000000000000000, 0.9659258262890683122, 1.000000000000000000, 0.9659258262890683122, 1.000000000000000000, 0.9659258262890683122, 1.000000000000000000, 0.9659258262890683122, 1.000000000000000000 ) ) 
 REPRESENTATION_ITEM ( '' )  );
#52038=CARTESIAN_POINT ( 'NONE',  ( -8.311093377946841443, 178.9062499965859843, 8.311093377946830785 ) ) ;
#52044=CARTESIAN_POINT ( 'NONE',  ( -11.35316468749999785, 183.0729166632526983, -3.042071309553167957 ) ) ;
#52050=CARTESIAN_POINT ( 'NONE',  ( 9.832129032723416984, 165.6770833299193555, 5.676582343750006032 ) ) ;
#52052=CARTESIAN_POINT ( 'NONE',  ( -9.832129032723418760, 123.1770833299193555, -5.676582343750004256 ) ) ;
#52066=CARTESIAN_POINT ( 'NONE',  ( 1.491046635511791134E-11, 146.2499999999988631, -9.999999999999998224 ) ) ;
#52086=FACE_BOUND ( 'NONE', #27612, .T. ) ;
#52088=CARTESIAN_POINT ( 'NONE',  ( -6.676582343750002480, 298.5468750017069510, -2.765530957081996810 ) ) ;
#52089=CARTESIAN_POINT ( 'NONE',  ( 7.320508075688774596, 135.6249999999999432, -7.320508075688774596 ) ) ;
#52091=CARTESIAN_POINT ( 'NONE',  ( 6.676582343750004256, 288.0468750017070079, 2.765530957081995478 ) ) ;
#52101=DIRECTION ( 'NONE',  ( 0.000000000000000000, 0.000000000000000000, 1.000000000000000000 ) ) ;
#52106=CARTESIAN_POINT ( 'NONE',  ( 11.35316468749999785, 25.57291666325268409, 3.042071309553174174 ) ) ;
#52107=CARTESIAN_POINT ( 'NONE',  ( -1.237384350715592869E-11, 93.74999999999903366, 9.999999999999998224 ) ) ;
#52108=CARTESIAN_POINT ( 'NONE',  ( -3.042071309553173730, 224.6354166632526983, 11.35316468749999785 ) ) ;
#52115=CARTESIAN_POINT ( 'NONE',  ( 11.35316468750000141, 25.78124999658601624, 0.000000000000000000 ) ) ;
#52118=CARTESIAN_POINT ( 'NONE',  ( 1.934925017735378189E-11, 153.7500000000015348, 10.00000000000000533 ) ) ;
#52121=CARTESIAN_POINT ( 'NONE',  ( -5.676582343749998039, 17.44791666325268409, -9.832129032723420536 ) ) ;
#52123=CARTESIAN_POINT ( 'NONE',  ( 5.676582343749993598, 139.9479166632526983, 9.832129032723422313 ) ) ;
#52124=CARTESIAN_POINT ( 'NONE',  ( -1.836970198721029983E-15, 120.6249999931720396, 10.00000000000000178 ) ) ;
#52130=CARTESIAN_POINT ( 'NONE',  ( 8.311093377946834337, 10.46874999658601624, 8.311093377946839666 ) ) ;
#52132=CARTESIAN_POINT ( 'NONE',  ( -4.721056650415999201, 298.3281250017069510, -4.721056650415999201 ) ) ;
#52133=CARTESIAN_POINT ( 'NONE',  ( 11.35316468749999785, 145.5729166632526983, 3.042071309553174174 ) ) ;
#52141=FACE_OUTER_BOUND ( 'NONE', #65747, .T. ) ;
#52142=CARTESIAN_POINT ( 'NONE',  ( 8.311093377946834337, 95.46874999658601268, 8.311093377946839666 ) ) ;
#52154=AXIS2_PLACEMENT_3D ( 'NONE', #2556, #48932, #36886 ) ;
#52176=CARTESIAN_POINT ( 'NONE',  ( -10.00000000000000355, 92.70833333333332860, 2.679491924311223183 ) ) ;
#52178=CARTESIAN_POINT ( 'NONE',  ( 8.311093377946837890, 66.71874999658602690, -8.311093377946837890 ) ) ;
#52179=CARTESIAN_POINT ( 'NONE',  ( 2.485281374238571317, 289.6874999999999432, -6.000000000000003553 ) ) ;
#52185=CARTESIAN_POINT ( 'NONE',  ( 10.00000000000000888, 84.79166666666668561, 2.679491924311237838 ) ) ;
#52190=CARTESIAN_POINT ( 'NONE',  ( -8.660254037844390851, 207.9166666666666572, 4.999999999999998224 ) ) ;
#52192=CARTESIAN_POINT ( 'NONE',  ( 8.311093377946834337, 175.4687499965860127, 8.311093377946839666 ) ) ;
#52195=CARTESIAN_POINT ( 'NONE',  ( 0.000000000000000000, 300.0000000000000000, 0.000000000000000000 ) ) ;
#52196=CARTESIAN_POINT ( 'NONE',  ( 4.999999999999993783, 86.04166665983869677, 8.660254037844390851 ) ) ;
#52199=CARTESIAN_POINT ( 'NONE',  ( -8.311093377946836114, 42.96874999658601268, -8.311093377946837890 ) ) ;
#52202=CARTESIAN_POINT ( 'NONE',  ( 10.00000000000000178, 222.0833333265053682, -2.679491924311226736 ) ) ;
#52205=CARTESIAN_POINT ( 'NONE',  ( -2.679491924311235618, 70.41666665983869677, 10.00000000000000000 ) ) ;
#52214=CARTESIAN_POINT ( 'NONE',  ( -6.676582343750003368, 298.5468750017069510, -2.765530957081996810 ) ) ;
#52216=CARTESIAN_POINT ( 'NONE',  ( 7.320508075688771044, 41.24999999317203248, 7.320508075688775484 ) ) ;
#52218=CARTESIAN_POINT ( 'NONE',  ( 11.35316468749999785, 150.5729166632526699, 3.042071309553174174 ) ) ;
#52219=CARTESIAN_POINT ( 'NONE',  ( -1.522892193876115035E-11, 103.7499999999988205, 10.00000000000000178 ) ) ;
#52228=CARTESIAN_POINT ( 'NONE',  ( 6.951808397369818766E-16, 122.3437499965860269, -11.35316468750000141 ) ) ;
#52232=CARTESIAN_POINT ( 'NONE',  ( 6.951808397369818766E-16, 47.34374999658602690, -11.35316468750000141 ) ) ;
#52239=CARTESIAN_POINT ( 'NONE',  ( -6.000000000000000888, 296.1250000034139589, 2.485281374238575758 ) ) ;
#52253=ADVANCED_FACE ( 'NONE', ( #7326 ), #59745, .T. ) ;
#52260=EDGE_LOOP ( 'NONE', ( #18510, #47905 ) ) ;
#52261=CARTESIAN_POINT ( 'NONE',  ( -7.320508075688778149, 44.99999999317203958, 7.320508075688769267 ) ) ;
#52262=CARTESIAN_POINT ( 'NONE',  ( 2.679491924311228956, 46.04166666666666430, -10.00000000000000000 ) ) ;
#52269=EDGE_LOOP ( 'NONE', ( #23602, #33623, #3636, #49750 ) ) ;
#52272=CARTESIAN_POINT ( 'NONE',  ( 4.999999999999985789, 89.16666666666665719, 8.660254037844378416 ) ) ;
#52275=CARTESIAN_POINT ( 'NONE',  ( -6.000000000000001776, 300.0000000000000000, 0.000000000000000000 ) ) ;
#52276=CARTESIAN_POINT ( 'NONE',  ( 7.320508075688774596, 160.6249999999999716, -7.320508075688774596 ) ) ;
#52280=CARTESIAN_POINT ( 'NONE',  ( 9.832129032723416984, 140.6770833299193555, 5.676582343750006032 ) ) ;
#52281=CARTESIAN_POINT ( 'NONE',  ( -3.673940397442060854E-16, 293.8125000034140157, -6.000000000000001776 ) ) ;
#52284=CARTESIAN_POINT ( 'NONE',  ( 10.00000000000000178, 107.0833333265053398, -2.679491924311226736 ) ) ;
#52288=CARTESIAN_POINT ( 'NONE',  ( 8.660254037844481445, 195.4166666666667425, -5.000000000000054179 ) ) ;
#52290=EDGE_CURVE ( 'NONE', #21207, #22380, #71045, .T. ) ;
#52291=CARTESIAN_POINT ( 'NONE',  ( -2.679491924311235618, 25.41666665983869677, 10.00000000000000000 ) ) ;
#52298=CYLINDRICAL_SURFACE ( 'NONE', #43795, 10.00000000000000178 ) ;
#52299=CARTESIAN_POINT ( 'NONE',  ( 5.676582343750001591, 106.6145833299193555, -9.832129032723420536 ) ) ;
#52305=CARTESIAN_POINT ( 'NONE',  ( -9.832129032723420536, 113.6979166632526983, 5.676582343749997150 ) ) ;
#52309=CARTESIAN_POINT ( 'NONE',  ( -10.00000000000000000, 219.1666666598387110, -2.679491924311229845 ) ) ;
#52311=DIRECTION ( 'NONE',  ( -0.000000000000000000, 1.000000000000000000, -0.000000000000000000 ) ) ;
#52313=CARTESIAN_POINT ( 'NONE',  ( 8.311093377946837890, 96.40624999658602690, -8.311093377946837890 ) ) ;
#52316=CARTESIAN_POINT ( 'NONE',  ( 7.320508075688774596, 170.6250000000000000, -7.320508075688774596 ) ) ;
#52317=VERTEX_POINT ( 'NONE', #65395 ) ;
#52318=CARTESIAN_POINT ( 'NONE',  ( 5.000000000000001776, 197.7083333265053966, -8.660254037844389075 ) ) ;
#52321=CARTESIAN_POINT ( 'NONE',  ( -9.832129032723420536, 94.01041666325268409, 5.676582343749997150 ) ) ;
#52325=CARTESIAN_POINT ( 'NONE',  ( 8.311093377946834337, 220.1562499965860127, 8.311093377946839666 ) ) ;
#52329=CARTESIAN_POINT ( 'NONE',  ( 8.311093377946837890, 216.4062499965860127, -8.311093377946837890 ) ) ;
#52334=CARTESIAN_POINT ( 'NONE',  ( 4.721056650415999201, 297.0781250017069510, -4.721056650415999201 ) ) ;
#52336=CARTESIAN_POINT ( 'NONE',  ( -3.042071309553173730, 214.6354166632526983, 11.35316468749999785 ) ) ;
#52345=CARTESIAN_POINT ( 'NONE',  ( -8.660254037844390851, 32.91666666666667140, 4.999999999999998224 ) ) ;
#52348=CARTESIAN_POINT ( 'NONE',  ( 0.000000000000000000, 300.0000000000000000, 0.000000000000000000 ) ) ;
#52355=CARTESIAN_POINT ( 'NONE',  ( -6.676582343749999815, 297.5156250017070079, 2.765530957082001251 ) ) ;
#52366=CARTESIAN_POINT ( 'NONE',  ( 5.676582343750001591, 86.92708332991935549, -9.832129032723420536 ) ) ;
#52375=CARTESIAN_POINT ( 'NONE',  ( 11.35316468750000141, 195.7812499965860127, 0.000000000000000000 ) ) ;
#52381=CARTESIAN_POINT ( 'NONE',  ( 8.311093377946837890, 186.7187499965860127, -8.311093377946837890 ) ) ;
#52388=CARTESIAN_POINT ( 'NONE',  ( 8.311093377946837890, 71.40624999658602690, -8.311093377946837890 ) ) ;
#52390=DIRECTION ( 'NONE',  ( -0.000000000000000000, 1.000000000000000000, -0.000000000000000000 ) ) ;
#52395=CARTESIAN_POINT ( 'NONE',  ( 5.676582343750001591, 71.61458332991935549, -9.832129032723420536 ) ) ;
#52400=CARTESIAN_POINT ( 'NONE',  ( 9.832129032723420536, 56.19791666325268409, -5.676582343749999815 ) ) ;
#52404=CARTESIAN_POINT ( 'NONE',  ( 10.00000000000000178, 161.8749999931720254, 0.000000000000000000 ) ) ;
#52407=CARTESIAN_POINT ( 'NONE',  ( -2.679491924311226292, 53.33333332650536107, -10.00000000000000178 ) ) ;
#52408=CARTESIAN_POINT ( 'NONE',  ( -8.311093377946841443, 54.21874999658601979, 8.311093377946834337 ) ) ;
#52410=CARTESIAN_POINT ( 'NONE',  ( 11.35316468750000141, 180.7812499965860411, 0.000000000000000000 ) ) ;
#52415=CARTESIAN_POINT ( 'NONE',  ( -5.676582343750006032, 184.1145833299193555, 9.832129032723418760 ) ) ;
#52417=CARTESIAN_POINT ( 'NONE',  ( -1.836970198721029983E-15, 83.75000000000000000, 10.00000000000000178 ) ) ;
#52422=CARTESIAN_POINT ( 'NONE',  ( -8.311093377946841443, 164.2187499965860411, 8.311093377946834337 ) ) ;
#52424=CARTESIAN_POINT ( 'NONE',  ( 3.042071309553159519, 135.0520833299193555, 11.35316468750000141 ) ) ;
#52427=ORIENTED_EDGE ( 'NONE', *, *, #71804, .T. ) ;
#52438=CARTESIAN_POINT ( 'NONE',  ( 1.102182119232618108E-15, 293.2500000000000000, 6.000000000000001776 ) ) ;
#52440=EDGE_LOOP ( 'NONE', ( #40693, #50457, #36916, #5343 ) ) ;
#52452=CARTESIAN_POINT ( 'NONE',  ( -2.765530957081998142, 296.7968750017070079, 6.676582343750000703 ) ) ;
#52453=CARTESIAN_POINT ( 'NONE',  ( -1.836970198721029983E-15, 128.7500000000000000, 10.00000000000000178 ) ) ;
#52455=CARTESIAN_POINT ( 'NONE',  ( -6.676582343750001591, 289.6093750017069510, 0.000000000000000000 ) ) ;
#52470=CARTESIAN_POINT ( 'NONE',  ( -8.311093377946841443, 28.90624999658601979, 8.311093377946830785 ) ) ;
#52471=CARTESIAN_POINT ( 'NONE',  ( 2.679491924289742144, 23.95833333333158777, 10.00000000001278444 ) ) ;
#52472=CARTESIAN_POINT ( 'NONE',  ( -3.042071309553164404, 217.5520833299193555, -11.35316468749999963 ) ) ;
#52478=CARTESIAN_POINT ( 'NONE',  ( -2.085542519210945728E-15, 19.53124999658601979, 11.35316468750000141 ) ) ;
#52481=CARTESIAN_POINT ( 'NONE',  ( -6.000000000000001776, 295.0625000034140157, 0.000000000000000000 ) ) ;
#52482=CARTESIAN_POINT ( 'NONE',  ( 0.000000000000000000, 300.0000000000000000, 10.00000000000000178 ) ) ;
#52484=CARTESIAN_POINT ( 'NONE',  ( -3.042071309553163960, 17.23958332991935194, -11.35316468749999963 ) ) ;
#52486=CARTESIAN_POINT ( 'NONE',  ( -9.832129032723420536, 143.6979166632526699, 5.676582343749997150 ) ) ;
#52487=CARTESIAN_POINT ( 'NONE',  ( -2.679491924311235618, 115.4166666598386968, 10.00000000000000000 ) ) ;
#52489=CARTESIAN_POINT ( 'NONE',  ( 2.679491924311228956, 172.9166666598386826, -10.00000000000000000 ) ) ;
#52492=CARTESIAN_POINT ( 'NONE',  ( -3.042071309553173730, 14.63541666325268231, 11.35316468749999785 ) ) ;
#52493=( BOUNDED_CURVE ( )  B_SPLINE_CURVE ( 2, ( #64072, #36415, #68986, #12380, #40313, #59429, #30747, #63317, #2077, #45230, #10901, #33935, #48086 ),
 .UNSPECIFIED., .F., .F. ) 
 B_SPLINE_CURVE_WITH_KNOTS ( ( 3, 2, 2, 2, 2, 2, 3 ),
 ( 1.397287049208421728, 1.402520683848244909, 1.407754318488068090, 1.412987953127891272, 1.418221587767714453, 1.423455222407537857, 1.428688857047360816 ),
 .UNSPECIFIED. ) 
 CURVE ( )  GEOMETRIC_REPRESENTATION_ITEM ( )  RATIONAL_B_SPLINE_CURVE ( ( 1.000000000000238032, 0.9659258262888302804, 1.000000000000000000, 0.9659258262890683122, 1.000000000000000000, 0.9659258262890683122, 1.000000000000000000, 0.9659258262890683122, 1.000000000000000000, 0.9659258262890683122, 1.000000000000000000, 0.9659258262890683122, 1.000000000000000000 ) ) 
 REPRESENTATION_ITEM ( '' )  );
#52496=CARTESIAN_POINT ( 'NONE',  ( 4.721056650415999201, 297.0781250017069510, -4.721056650415999201 ) ) ;
#52497=CARTESIAN_POINT ( 'NONE',  ( 3.042071309553159519, 139.7395833299193839, 11.35316468750000141 ) ) ;
#52505=EDGE_CURVE ( 'NONE', #63519, #14543, #34099, .T. ) ;
#52509=CARTESIAN_POINT ( 'NONE',  ( 11.35316468749999785, 90.88541666325266988, 3.042071309553174174 ) ) ;
#52521=CARTESIAN_POINT ( 'NONE',  ( 0.000000000000000000, 300.0000000000000000, 15.99999999999998579 ) ) ;
#52523=CARTESIAN_POINT ( 'NONE',  ( 0.000000000000000000, 300.0000000000000000, 10.00000000000000178 ) ) ;
#52532=VERTEX_POINT ( 'NONE', #49532 ) ;
#52535=CARTESIAN_POINT ( 'NONE',  ( 6.123233995736767268E-16, 96.25000000000000000, -10.00000000000000178 ) ) ;
#52539=CARTESIAN_POINT ( 'NONE',  ( 6.123233995736767268E-16, 91.25000000000001421, -10.00000000000000178 ) ) ;
#52541=CARTESIAN_POINT ( 'NONE',  ( -11.35316468750000141, 63.80208332991934839, 3.042071309553159963 ) ) ;
#52542=CARTESIAN_POINT ( 'NONE',  ( -4.088227598258586603E-16, 298.3593750017070079, -6.676582343750001591 ) ) ;
#52551=CARTESIAN_POINT ( 'NONE',  ( -2.485281374238895502, 292.8124999999999432, -5.999999999999677591 ) ) ;
#52553=CARTESIAN_POINT ( 'NONE',  ( 4.999999999999993783, 219.1666666666666856, 8.660254037844390851 ) ) ;
#52555=CARTESIAN_POINT ( 'NONE',  ( -3.042071309553164404, 177.5520833299193839, -11.35316468749999963 ) ) ;
#52561=CARTESIAN_POINT ( 'NONE',  ( -2.085542519210945728E-15, 34.84374999658601268, 11.35316468750000141 ) ) ;
#52571=CARTESIAN_POINT ( 'NONE',  ( 7.320508075688774596, 72.49999999317203958, -7.320508075688774596 ) ) ;
#52574=CARTESIAN_POINT ( 'NONE',  ( 8.660254037844385522, 55.41666666666666430, -4.999999999999997335 ) ) ;
#52579=CARTESIAN_POINT ( 'NONE',  ( 7.320508075688774596, 22.49999999317202892, -7.320508075688774596 ) ) ;
#52580=CARTESIAN_POINT ( 'NONE',  ( -2.765530957081996810, 297.4218750017069510, -6.676582343750003368 ) ) ;
#52583=CARTESIAN_POINT ( 'NONE',  ( -3.042071309553164404, 152.2395833299193271, -11.35316468749999963 ) ) ;
#52595=CARTESIAN_POINT ( 'NONE',  ( 3.042071309553159519, 125.0520833299193555, 11.35316468750000141 ) ) ;
#52597=CARTESIAN_POINT ( 'NONE',  ( 4.242640687119287435, 298.4375000034140157, 4.242640687119285658 ) ) ;
#52599=CARTESIAN_POINT ( 'NONE',  ( -2.085542519210945728E-15, 49.84374999658601268, 11.35316468750000141 ) ) ;
#52600=ORIENTED_EDGE ( 'NONE', *, *, #42494, .T. ) ;
#52605=CARTESIAN_POINT ( 'NONE',  ( -2.485281374238572649, 293.2500000034140157, 6.000000000000002665 ) ) ;
#52614=CARTESIAN_POINT ( 'NONE',  ( -1.836970198721029983E-15, 65.62499999317203958, 10.00000000000000178 ) ) ;
#52625=ADVANCED_BREP_SHAPE_REPRESENTATION ( '', ( #18038, #57354 ), #69405 ) ;
#52631=CARTESIAN_POINT ( 'NONE',  ( 4.999999999999993783, 59.16666666666667140, 8.660254037844390851 ) ) ;
#52635=CARTESIAN_POINT ( 'NONE',  ( -2.485281374238855090, 287.8750000034139589, -5.999999999999718447 ) ) ;
#52641=CARTESIAN_POINT ( 'NONE',  ( -10.00000000000000000, 74.16666665983869677, -2.679491924311229845 ) ) ;
#52642=CARTESIAN_POINT ( 'NONE',  ( -10.00000000000000178, 147.5000000000000284, -1.224646799147353454E-15 ) ) ;
#52644=CARTESIAN_POINT ( 'NONE',  ( 2.679491924311222739, 168.9583333333333428, 10.00000000000000355 ) ) ;
#52648=CARTESIAN_POINT ( 'NONE',  ( -5.676582343750006032, 144.4270833299193555, 9.832129032723418760 ) ) ;
#52656=CARTESIAN_POINT ( 'NONE',  ( 6.424498079411709028, 225.6958308926248833, -7.668941570935106533 ) ) ;
#52660=CARTESIAN_POINT ( 'NONE',  ( 10.00000000000000178, 42.08333332650537528, -2.679491924311226736 ) ) ;
#52667=ORIENTED_EDGE ( 'NONE', *, *, #2314, .F. ) ;
#52672=CARTESIAN_POINT ( 'NONE',  ( -9.832129032723420536, 118.6979166632526841, 5.676582343749997150 ) ) ;
#52678=CARTESIAN_POINT ( 'NONE',  ( 8.660254037844389075, 222.2916666598387110, -5.000000000000000000 ) ) ;
#52682=CARTESIAN_POINT ( 'NONE',  ( 6.951808397369818766E-16, 102.0312499965860269, -11.35316468750000141 ) ) ;
#52686=ORIENTED_EDGE ( 'NONE', *, *, #51302, .F. ) ;
#52688=CARTESIAN_POINT ( 'NONE',  ( 5.000000000000001776, 192.7083333265053966, -8.660254037844389075 ) ) ;
#52689=DIRECTION ( 'NONE',  ( 0.000000000000000000, 0.000000000000000000, 1.000000000000000000 ) ) ;
#52691=CARTESIAN_POINT ( 'NONE',  ( 5.676582343749993598, 90.26041666325268409, 9.832129032723422313 ) ) ;
#52692=CARTESIAN_POINT ( 'NONE',  ( -6.676582343750001591, 287.4531250017069510, 0.000000000000000000 ) ) ;
#52695=CARTESIAN_POINT ( 'NONE',  ( -11.35316468750000141, 3.802083329919349275, 3.042071309553159963 ) ) ;
#52699=CARTESIAN_POINT ( 'NONE',  ( 3.042071309553167513, 216.8229166632526699, -11.35316468749999785 ) ) ;
#52702=CARTESIAN_POINT ( 'NONE',  ( -2.679491924311087736, 150.4166666598387110, 10.00000000000008349 ) ) ;
#52703=CARTESIAN_POINT ( 'NONE',  ( -6.676582343750003368, 293.3906250017069510, -2.765530957081996810 ) ) ;
#52705=ORIENTED_EDGE ( 'NONE', *, *, #26791, .T. ) ;
#52707=CARTESIAN_POINT ( 'NONE',  ( 3.042071309553159519, 205.0520833299192986, 11.35316468750000141 ) ) ;
#52712=VECTOR ( 'NONE', #22368, 1000.000000000000000 ) ;
#52716=CARTESIAN_POINT ( 'NONE',  ( -10.00000000000000000, 27.29166666666666430, -2.679491924311229845 ) ) ;
#52725=CARTESIAN_POINT ( 'NONE',  ( -0.4590000000000000746, 284.2799999999998590, 5.818592113970287194 ) ) ;
#52726=CARTESIAN_POINT ( 'NONE',  ( 6.676582343750001591, 295.9531250017069510, -8.176455196517173205E-16 ) ) ;
#52730=VERTEX_POINT ( 'NONE', #55825 ) ;
#52736=CARTESIAN_POINT ( 'NONE',  ( -11.35316468749999785, 103.3854166632526699, -3.042071309553167513 ) ) ;
#52744=DIRECTION ( 'NONE',  ( -0.000000000000000000, 1.000000000000000000, -0.000000000000000000 ) ) ;
#52746=CARTESIAN_POINT ( 'NONE',  ( 3.042071309553159519, 219.7395833299193271, 11.35316468750000141 ) ) ;
#52750=CARTESIAN_POINT ( 'NONE',  ( -8.311093377946841443, 174.2187499965860127, 8.311093377946830785 ) ) ;
#52752=CARTESIAN_POINT ( 'NONE',  ( -5.999999999999999112, 296.1250000034140726, 2.485281374238575314 ) ) ;
#52756=CARTESIAN_POINT ( 'NONE',  ( -3.042071309553173730, 69.32291666325268409, 11.35316468749999785 ) ) ;
#52757=CARTESIAN_POINT ( 'NONE',  ( 0.000000000000000000, 300.0000000000000000, 0.000000000000000000 ) ) ;
#52761=CARTESIAN_POINT ( 'NONE',  ( 11.35316468750000141, 80.78124999658602690, 0.000000000000000000 ) ) ;
#52766=CARTESIAN_POINT ( 'NONE',  ( -8.311093377946836114, 62.65624999658601979, -8.311093377946837890 ) ) ;
#52768=AXIS2_PLACEMENT_3D ( 'NONE', #8137, #19446, #2106 ) ;
#52770=CARTESIAN_POINT ( 'NONE',  ( 8.660254037844385522, 156.4583333265053966, 5.000000000000005329 ) ) ;
#52772=CARTESIAN_POINT ( 'NONE',  ( -4.999999999999998224, 53.54166665983870388, -8.660254037844389075 ) ) ;
#52773=CARTESIAN_POINT ( 'NONE',  ( -5.676582343750006032, 44.42708332991934839, 9.832129032723418760 ) ) ;
#52775=CARTESIAN_POINT ( 'NONE',  ( 9.832129032723420536, 196.1979166632526983, -5.676582343749999815 ) ) ;
#52781=CARTESIAN_POINT ( 'NONE',  ( 9.832129032723420536, 186.1979166632526983, -5.676582343749999815 ) ) ;
#52783=AXIS2_PLACEMENT_3D ( 'NONE', #73999, #16637, #39671 ) ;
#52788=CARTESIAN_POINT ( 'NONE',  ( 3.042071309553167513, 162.1354166632526699, -11.35316468749999785 ) ) ;
#52792=CARTESIAN_POINT ( 'NONE',  ( -8.311093377946836114, 132.9687499965860411, -8.311093377946837890 ) ) ;
#52798=DIRECTION ( 'NONE',  ( 0.000000000000000000, 0.000000000000000000, 1.000000000000000000 ) ) ;
#52801=CARTESIAN_POINT ( 'NONE',  ( -10.00000000000000355, 187.2916666666666572, -2.679491924311231177 ) ) ;
#52805=CARTESIAN_POINT ( 'NONE',  ( 0.000000000000000000, 300.0000000000000000, 0.000000000000000000 ) ) ;
#52811=CYLINDRICAL_SURFACE ( 'NONE', #45809, 10.00000000000000178 ) ;
#52820=CARTESIAN_POINT ( 'NONE',  ( 6.676582343750003368, 297.0468750017069510, 2.765530957081995478 ) ) ;
#52821=CARTESIAN_POINT ( 'NONE',  ( 10.00000000000000178, 130.2083333333333712, -2.679491924311226736 ) ) ;
#52826=EDGE_CURVE ( 'NONE', #27743, #2057, #62066, .T. ) ;
#52828=CARTESIAN_POINT ( 'NONE',  ( -3.673940397442060854E-16, 290.8125000034140157, -6.000000000000001776 ) ) ;
#52839=CARTESIAN_POINT ( 'NONE',  ( -5.676582343750006032, 29.11458332991935194, 9.832129032723418760 ) ) ;
#52841=CARTESIAN_POINT ( 'NONE',  ( 7.320508075689014404, 25.62500000000018829, -7.320508075689014404 ) ) ;
#52842=CARTESIAN_POINT ( 'NONE',  ( 9.832129032723416984, 220.6770833299193555, 5.676582343750006032 ) ) ;
#52848=CARTESIAN_POINT ( 'NONE',  ( -8.311093377946836114, 32.65624999658600558, -8.311093377946837890 ) ) ;
#52854=CARTESIAN_POINT ( 'NONE',  ( 5.676582343750001591, 16.61458332991935194, -9.832129032723420536 ) ) ;
#52856=CARTESIAN_POINT ( 'NONE',  ( -11.35316468750000141, 148.2812499965860411, -1.390361679473963753E-15 ) ) ;
#52858=CARTESIAN_POINT ( 'NONE',  ( 2.679491924311228956, 112.9166666598387252, -10.00000000000000000 ) ) ;
#52863=CARTESIAN_POINT ( 'NONE',  ( -9.832129032723418760, 8.177083329919350163, -5.676582343750004256 ) ) ;
#52867=CARTESIAN_POINT ( 'NONE',  ( -4.721056650415998313, 297.5781250017069510, 4.721056650416000089 ) ) ;
#52869=CARTESIAN_POINT ( 'NONE',  ( -9.832129032723420536, 138.6979166632526983, 5.676582343749997150 ) ) ;
#52881=CARTESIAN_POINT ( 'NONE',  ( 3.042071309553167069, 87.13541666325268409, -11.35316468749999785 ) ) ;
#52899=CARTESIAN_POINT ( 'NONE',  ( -5.000000000000005329, 225.2083333265053966, 8.660254037844387298 ) ) ;
#52903=ORIENTED_EDGE ( 'NONE', *, *, #43390, .T. ) ;
#52911=CARTESIAN_POINT ( 'NONE',  ( -2.679491924311235618, 98.54166666666667140, 10.00000000000000000 ) ) ;
#52913=CARTESIAN_POINT ( 'NONE',  ( 5.676582343749993598, 65.26041666325268409, 9.832129032723422313 ) ) ;
#52914=CARTESIAN_POINT ( 'NONE',  ( 6.676582343750004256, 296.0468750017069510, 2.765530957081995478 ) ) ;
#52922=CARTESIAN_POINT ( 'NONE',  ( 1.224646799147353454E-15, 300.0000000000000000, -10.00000000000000178 ) ) ;
#52924=CARTESIAN_POINT ( 'NONE',  ( -3.673940397442060854E-16, 292.7500000000000000, -6.000000000000001776 ) ) ;
#52926=CARTESIAN_POINT ( 'NONE',  ( -2.679491924311225848, 211.4583333333333144, -10.00000000000000178 ) ) ;
#52930=CARTESIAN_POINT ( 'NONE',  ( -11.35316468750000141, 178.8020833299193271, 3.042071309553159963 ) ) ;
#52933=FACE_OUTER_BOUND ( 'NONE', #1692, .T. ) ;
#52936=AXIS2_PLACEMENT_3D ( 'NONE', #3466, #10247, #49480 ) ;
#52938=CARTESIAN_POINT ( 'NONE',  ( -8.311093377946836114, 32.96874999658600558, -8.311093377946837890 ) ) ;
#52940=CARTESIAN_POINT ( 'NONE',  ( -9.832129032723418760, 218.1770833299193555, -5.676582343750004256 ) ) ;
#52946=CARTESIAN_POINT ( 'NONE',  ( -7.320508075688778149, 69.99999999317203958, 7.320508075688769267 ) ) ;
#52952=ORIENTED_EDGE ( 'NONE', *, *, #56034, .F. ) ;
#52953=CARTESIAN_POINT ( 'NONE',  ( 6.676582343750004256, 299.0468750017069510, 2.765530957081995478 ) ) ;
#52954=CARTESIAN_POINT ( 'NONE',  ( -8.660254037844397956, 142.0833333333333712, -5.000000000000010658 ) ) ;
#52956=CARTESIAN_POINT ( 'NONE',  ( -5.676582343750006032, 154.1145833299193555, 9.832129032723418760 ) ) ;
#52965=CARTESIAN_POINT ( 'NONE',  ( -8.311093377946836114, 142.9687499965859843, -8.311093377946837890 ) ) ;
#52969=CARTESIAN_POINT ( 'NONE',  ( -11.35316468750000141, 53.59374999658601979, -1.390361679473963753E-15 ) ) ;
#52971=CARTESIAN_POINT ( 'NONE',  ( -5.000000000000008882, 28.33333333333333925, 8.660254037844390851 ) ) ;
#52975=CARTESIAN_POINT ( 'NONE',  ( 6.000000000000003553, 291.6250000034139589, -2.485281374238571761 ) ) ;
#52976=DIRECTION ( 'NONE',  ( -0.000000000000000000, 1.000000000000000000, -0.000000000000000000 ) ) ;
#52981=VECTOR ( 'NONE', #73339, 1000.000000000000000 ) ;
#52990=ADVANCED_FACE ( 'NONE', ( #56905 ), #14321, .F. ) ;
#53002=CARTESIAN_POINT ( 'NONE',  ( 2.679491924311228956, 56.04166666666667140, -10.00000000000000000 ) ) ;
#53005=CARTESIAN_POINT ( 'NONE',  ( 0.000000000000000000, 300.0000000000000000, 0.000000000000000000 ) ) ;
#53015=CARTESIAN_POINT ( 'NONE',  ( 8.660254037844385522, 179.5833333333333428, 5.000000000000005329 ) ) ;
#53020=CARTESIAN_POINT ( 'NONE',  ( 3.042071309553159519, 140.0520833299193271, 11.35316468750000141 ) ) ;
#53022=DIRECTION ( 'NONE',  ( 0.000000000000000000, 0.000000000000000000, 1.000000000000000000 ) ) ;
#53027=CARTESIAN_POINT ( 'NONE',  ( 5.730382604041190930, 225.7665013914169947, -8.216451592654051339 ) ) ;
#53032=CARTESIAN_POINT ( 'NONE',  ( 2.679491924311222739, 40.83333332650536818, 10.00000000000000355 ) ) ;
#53040=CARTESIAN_POINT ( 'NONE',  ( 6.000000000000001776, 292.5625000034140157, -7.347880794884121708E-16 ) ) ;
#53041=CARTESIAN_POINT ( 'NONE',  ( -9.679794093948311584, 225.9999999999999716, -2.594496013589457917 ) ) ;
#53044=CARTESIAN_POINT ( 'NONE',  ( -8.311093377946841443, 118.9062499965860269, 8.311093377946830785 ) ) ;
#53047=VECTOR ( 'NONE', #56396, 1000.000000000000000 ) ;
#53049=CARTESIAN_POINT ( 'NONE',  ( 7.320508075688774596, 227.4999999931720254, -7.320508075688774596 ) ) ;
#53053=CARTESIAN_POINT ( 'NONE',  ( 5.676582343749993598, 114.9479166632526983, 9.832129032723422313 ) ) ;
#53058=CARTESIAN_POINT ( 'NONE',  ( 8.660254037844385522, 196.4583333265053966, 5.000000000000005329 ) ) ;
#53060=CARTESIAN_POINT ( 'NONE',  ( 3.042071309553167513, 107.1354166632526841, -11.35316468749999785 ) ) ;
#53064=CARTESIAN_POINT ( 'NONE',  ( 11.35316468750000141, 11.09374999658601624, 0.000000000000000000 ) ) ;
#53068=CARTESIAN_POINT ( 'NONE',  ( 11.33169192104559997, 226.0000000000000000, -1.645653018074211493 ) ) ;
#53072=CARTESIAN_POINT ( 'NONE',  ( 6.676582343750003368, 294.0156250017070079, -2.765530957081997254 ) ) ;
#53075=CARTESIAN_POINT ( 'NONE',  ( 9.832129032723416984, 205.6770833299193555, 5.676582343750006032 ) ) ;
#53078=EDGE_CURVE ( 'NONE', #71712, #46560, #18212, .T. ) ;
#53082=CARTESIAN_POINT ( 'NONE',  ( 1.224646799147353454E-15, 255.9999999999999432, -10.00000000000000178 ) ) ;
#53084=CARTESIAN_POINT ( 'NONE',  ( 6.123233995736767268E-16, 31.25000000000000000, -10.00000000000000178 ) ) ;
#53092=EDGE_CURVE ( 'NONE', #31972, #28551, #67757, .T. ) ;
#53096=CARTESIAN_POINT ( 'NONE',  ( -1.377000000000000002, 272.8559999999997672, 5.668134320366531753 ) ) ;
#53097=CARTESIAN_POINT ( 'NONE',  ( -4.088227598258586603E-16, 295.2031250017069510, -6.676582343750001591 ) ) ;
#53099=CARTESIAN_POINT ( 'NONE',  ( 7.320508075688771044, 136.2499999931720538, 7.320508075688775484 ) ) ;
#53108=CARTESIAN_POINT ( 'NONE',  ( -3.042071309553164404, 107.5520833299193555, -11.35316468749999963 ) ) ;
#53116=CARTESIAN_POINT ( 'NONE',  ( 6.123233995736767268E-16, 178.1249999931720538, -10.00000000000000178 ) ) ;
#53117=EDGE_CURVE ( 'NONE', #46122, #60284, #32313, .T. ) ;
#53118=VECTOR ( 'NONE', #50414, 1000.000000000000000 ) ;
#53119=CARTESIAN_POINT ( 'NONE',  ( 5.676582343749993598, 214.9479166632526983, 9.832129032723422313 ) ) ;
#53123=CARTESIAN_POINT ( 'NONE',  ( 9.832129032723420536, 181.5104166632526699, -5.676582343749999815 ) ) ;
#53125=DIRECTION ( 'NONE',  ( 0.000000000000000000, 0.000000000000000000, 1.000000000000000000 ) ) ;
#53130=CARTESIAN_POINT ( 'NONE',  ( -11.35316468750000141, 68.48958332991935549, 3.042071309553159963 ) ) ;
#53136=CARTESIAN_POINT ( 'NONE',  ( 5.676582343750001591, 81.61458332991935549, -9.832129032723420536 ) ) ;
#53141=CARTESIAN_POINT ( 'NONE',  ( 11.35316468749999785, 70.57291666325268409, 3.042071309553174174 ) ) ;
#53144=CARTESIAN_POINT ( 'NONE',  ( -2.679491924311235618, 160.4166666598386541, 10.00000000000000000 ) ) ;
#53147=CARTESIAN_POINT ( 'NONE',  ( 9.832129032723416984, 45.67708332991934839, 5.676582343750006032 ) ) ;
#53150=CARTESIAN_POINT ( 'NONE',  ( -11.35316468749999785, 193.0729166632526415, -3.042071309553167513 ) ) ;
#53151=EDGE_LOOP ( 'NONE', ( #70429, #1523, #5585, #25421 ) ) ;
#53154=CARTESIAN_POINT ( 'NONE',  ( 10.00000000000000000, 161.6666666598386826, 2.679491924311235618 ) ) ;
#53156=CARTESIAN_POINT ( 'NONE',  ( 3.042071309553159519, 174.7395833299193555, 11.35316468750000141 ) ) ;
#53159=CARTESIAN_POINT ( 'NONE',  ( -2.679491924311078410, 188.3333333265053682, -10.00000000000008527 ) ) ;
#53161=CARTESIAN_POINT ( 'NONE',  ( -5.676582343750006032, 174.4270833299193555, 9.832129032723418760 ) ) ;
#53162=STYLED_ITEM('',(#74692),#18038);
#53166=ORIENTED_EDGE ( 'NONE', *, *, #12611, .T. ) ;
#53180=ORIENTED_EDGE ( 'NONE', *, *, #39622, .F. ) ;
#53193=CARTESIAN_POINT ( 'NONE',  ( 2.765530957081996366, 297.2968750017070079, -6.676582343750002480 ) ) ;
#53194=CARTESIAN_POINT ( 'NONE',  ( -4.999999999999998224, 131.6666666666666856, -8.660254037844389075 ) ) ;
#53211=CARTESIAN_POINT ( 'NONE',  ( 6.951808397369818766E-16, 27.03124999658601979, -11.35316468750000141 ) ) ;
#53213=CARTESIAN_POINT ( 'NONE',  ( -2.085542519210945728E-15, 219.8437499965860411, 11.35316468750000141 ) ) ;
#53217=ORIENTED_EDGE ( 'NONE', *, *, #17399, .T. ) ;
#53219=EDGE_CURVE ( 'NONE', #23868, #71352, #44656, .T. ) ;
#53221=CARTESIAN_POINT ( 'NONE',  ( -3.042071309553164404, 37.23958332991934839, -11.35316468749999963 ) ) ;
#53227=CARTESIAN_POINT ( 'NONE',  ( -11.35316468749999785, 13.07291666325268409, -3.042071309553167957 ) ) ;
#53229=CARTESIAN_POINT ( 'NONE',  ( -3.042071309553164404, 152.2395833299193271, -11.35316468749999963 ) ) ;
#53230=CARTESIAN_POINT ( 'NONE',  ( -10.00000000000000000, 114.1666666598386968, -2.679491924311229845 ) ) ;
#53236=CARTESIAN_POINT ( 'NONE',  ( 3.042071309553167513, 12.13541666325268231, -11.35316468749999785 ) ) ;
#53240=CARTESIAN_POINT ( 'NONE',  ( 3.042071309553167513, 136.8229166632526699, -11.35316468749999785 ) ) ;
#53241=CARTESIAN_POINT ( 'NONE',  ( 0.000000000000000000, 300.0000000000000000, 0.000000000000000000 ) ) ;
#53251=CARTESIAN_POINT ( 'NONE',  ( -11.35316468750000141, 88.59374999658602690, -1.390361679473963753E-15 ) ) ;
#53271=CARTESIAN_POINT ( 'NONE',  ( -10.00000000000033040, 22.29166666666685970, -2.679491924311318662 ) ) ;
#53285=CARTESIAN_POINT ( 'NONE',  ( -4.999999999999998224, 96.66666666666668561, -8.660254037844389075 ) ) ;
#53288=CARTESIAN_POINT ( 'NONE',  ( 2.765530957082001251, 296.9218750017069510, 6.676582343750000703 ) ) ;
#53300=CARTESIAN_POINT ( 'NONE',  ( 6.123233995736767268E-16, 216.2500000000000284, -10.00000000000000178 ) ) ;
#53303=CARTESIAN_POINT ( 'NONE',  ( 5.676582343749993598, 175.2604166632526699, 9.832129032723422313 ) ) ;
#53310=CARTESIAN_POINT ( 'NONE',  ( 8.311093377946837890, 51.71874999658601979, -8.311093377946837890 ) ) ;
#53312=CARTESIAN_POINT ( 'NONE',  ( -3.042071309553173730, 214.6354166632526983, 11.35316468749999785 ) ) ;
#53314=CARTESIAN_POINT ( 'NONE',  ( -10.00000000000000355, 124.5833333265053682, 2.679491924311223183 ) ) ;
#53318=CARTESIAN_POINT ( 'NONE',  ( 7.320508075688771044, 76.24999999317203958, 7.320508075688775484 ) ) ;
#53321=CARTESIAN_POINT ( 'NONE',  ( -5.000000000000007994, 73.33333333333332860, 8.660254037844390851 ) ) ;
#53326=CARTESIAN_POINT ( 'NONE',  ( -2.765530957081998586, 298.7968750017069510, 6.676582343750001591 ) ) ;
#53328=CARTESIAN_POINT ( 'NONE',  ( 5.676582343750001591, 151.6145833299193555, -9.832129032723420536 ) ) ;
#53336=CARTESIAN_POINT ( 'NONE',  ( 9.832129032723420536, 136.5104166632526983, -5.676582343749999815 ) ) ;
#53340=CARTESIAN_POINT ( 'NONE',  ( -8.311093377946841443, 54.21874999658601979, 8.311093377946830785 ) ) ;
#53348=CARTESIAN_POINT ( 'NONE',  ( -3.673940397442060854E-16, 290.8125000034140157, -6.000000000000001776 ) ) ;
#53349=CARTESIAN_POINT ( 'NONE',  ( 1.224646799147353454E-15, 300.0000000000000000, -10.00000000000000178 ) ) ;
#53354=( BOUNDED_CURVE ( )  B_SPLINE_CURVE ( 2, ( #70490, #65181, #13124, #20265, #43290, #24817, #66304, #36160, #42907, #54256, #18808, #64823, #14611 ),
 .UNSPECIFIED., .F., .F. ) 
 B_SPLINE_CURVE_WITH_KNOTS ( ( 3, 2, 2, 2, 2, 2, 3 ),
 ( 1.617086391009537660, 1.622319942449755636, 1.627553493889973169, 1.632787045330191145, 1.638020596770409121, 1.643254148210627097, 1.648487699650845073 ),
 .UNSPECIFIED. ) 
 CURVE ( )  GEOMETRIC_REPRESENTATION_ITEM ( )  RATIONAL_B_SPLINE_CURVE ( ( 0.9999999999999791278, 0.9659258262890892954, 1.000000000000000000, 0.9659258262890684232, 1.000000000000000000, 0.9659258262890684232, 1.000000000000000000, 0.9659258262890684232, 1.000000000000000000, 0.9659258262890684232, 1.000000000000000000, 0.9659258262890684232, 1.000000000000000000 ) ) 
 REPRESENTATION_ITEM ( '' )  );
#53375=CARTESIAN_POINT ( 'NONE',  ( -7.320508075688778149, 58.12499999999999289, 7.320508075688769267 ) ) ;
#53377=CARTESIAN_POINT ( 'NONE',  ( 2.485281374238571317, 295.6875000000000000, -6.000000000000003553 ) ) ;
#53386=DIRECTION ( 'NONE',  ( -0.000000000000000000, 1.000000000000000000, 0.000000000000000000 ) ) ;
#53387=CARTESIAN_POINT ( 'NONE',  ( 5.000000000000001776, 180.8333333333333428, -8.660254037844389075 ) ) ;
#53388=CARTESIAN_POINT ( 'NONE',  ( -3.673940397442060854E-16, 299.7500000000000000, -6.000000000000001776 ) ) ;
#53389=EDGE_CURVE ( 'NONE', #45507, #60229, #69775, .T. ) ;
#53392=CARTESIAN_POINT ( 'NONE',  ( 11.35316468749999785, 140.8854166632526415, 3.042071309553174174 ) ) ;
#53394=CARTESIAN_POINT ( 'NONE',  ( -3.673940397442060854E-16, 291.7500000000000000, -6.000000000000001776 ) ) ;
#53400=CARTESIAN_POINT ( 'NONE',  ( 11.35316468749999785, 5.885416663252683200, 3.042071309553174174 ) ) ;
#53405=CARTESIAN_POINT ( 'NONE',  ( -8.660254037844390851, 29.79166665983870388, 4.999999999999998224 ) ) ;
#53416=CARTESIAN_POINT ( 'NONE',  ( -3.042071309553164404, 112.2395833299193697, -11.35316468749999963 ) ) ;
#53423=CARTESIAN_POINT ( 'NONE',  ( -9.999999999999998224, 182.7083333333333428, 2.679491924311222295 ) ) ;
#53424=CARTESIAN_POINT ( 'NONE',  ( 5.676582343750001591, 106.6145833299193555, -9.832129032723420536 ) ) ;
#53426=CARTESIAN_POINT ( 'NONE',  ( 8.660254037844389075, 49.58333333333333570, 5.000000000000007994 ) ) ;
#53428=EDGE_CURVE ( 'NONE', #64725, #5834, #67807, .T. ) ;
#53429=CARTESIAN_POINT ( 'NONE',  ( 8.660254037844385522, 206.4583333265053682, 5.000000000000005329 ) ) ;
#53433=CARTESIAN_POINT ( 'NONE',  ( 8.311093377946837890, 96.71874999658599847, -8.311093377946837890 ) ) ;
#53438=CARTESIAN_POINT ( 'NONE',  ( -9.832129032723418760, 3.177083329919349719, -5.676582343750004256 ) ) ;
#53444=CYLINDRICAL_SURFACE ( 'NONE', #20549, 6.000000000000001776 ) ;
#53445=CARTESIAN_POINT ( 'NONE',  ( 10.00000000000000000, 199.7916666666666572, 2.679491924311235618 ) ) ;
#53446=CARTESIAN_POINT ( 'NONE',  ( 2.765530957081996366, 294.1406250017069510, -6.676582343750003368 ) ) ;
#53448=CARTESIAN_POINT ( 'NONE',  ( 10.99653194014283564, 225.8365693605616116, 3.659777347618654808 ) ) ;
#53449=ADVANCED_FACE ( 'NONE', ( #2238 ), #50490, .T. ) ;
#53452=EDGE_CURVE ( 'NONE', #45113, #73073, #15781, .T. ) ;
#53462=ORIENTED_EDGE ( 'NONE', *, *, #53219, .T. ) ;
#53467=CARTESIAN_POINT ( 'NONE',  ( -4.088227598258586603E-16, 291.2031250017069510, -6.676582343750001591 ) ) ;
#53478=CARTESIAN_POINT ( 'NONE',  ( -2.085542519210945728E-15, 94.84374999658601268, 11.35316468750000141 ) ) ;
#53479=CARTESIAN_POINT ( 'NONE',  ( -8.660254037844387298, 122.9166666666666998, 4.999999999999997335 ) ) ;
#53487=CARTESIAN_POINT ( 'NONE',  ( -11.35316468750000141, 218.2812499965860411, -1.390361679473963753E-15 ) ) ;
#53491=CARTESIAN_POINT ( 'NONE',  ( 8.311093377946837890, 191.7187499965860127, -8.311093377946837890 ) ) ;
#53498=CARTESIAN_POINT ( 'NONE',  ( 3.042071309553159519, 69.73958332991935549, 11.35316468750000141 ) ) ;
#53502=AXIS2_PLACEMENT_3D ( 'NONE', #12195, #28805, #58981 ) ;
#53504=CARTESIAN_POINT ( 'NONE',  ( -2.085542519210945728E-15, 79.53124999658602690, 11.35316468750000141 ) ) ;
#53508=CARTESIAN_POINT ( 'NONE',  ( 1.268984979720182487E-11, 76.24999999999903366, -10.00000000000000178 ) ) ;
#53510=CARTESIAN_POINT ( 'NONE',  ( -5.676582343749998039, 67.44791666325268409, -9.832129032723420536 ) ) ;
#53515=CARTESIAN_POINT ( 'NONE',  ( 7.320508075688771044, 171.2499999931719969, 7.320508075688775484 ) ) ;
#53518=CARTESIAN_POINT ( 'NONE',  ( -11.35316468750000141, 58.59374999658601979, -1.390361679473963753E-15 ) ) ;
#53520=CARTESIAN_POINT ( 'NONE',  ( 9.832129032723420536, 201.1979166632526983, -5.676582343749999815 ) ) ;
#53526=CARTESIAN_POINT ( 'NONE',  ( 11.35316468750000141, 195.7812499965860127, 0.000000000000000000 ) ) ;
#53532=CARTESIAN_POINT ( 'NONE',  ( -3.042071309553163960, 182.5520833299193271, -11.35316468749999963 ) ) ;
#53535=CARTESIAN_POINT ( 'NONE',  ( 3.090148520752590944, 225.9998984954551418, -9.510618362637927703 ) ) ;
#53544=CARTESIAN_POINT ( 'NONE',  ( -7.320508075688776373, 186.8749999999999432, -7.320508075688777261 ) ) ;
#53546=CARTESIAN_POINT ( 'NONE',  ( 6.000000000000003553, 293.6250000034140157, -2.485281374238571761 ) ) ;
#53560=DIRECTION ( 'NONE',  ( 0.000000000000000000, 0.000000000000000000, 1.000000000000000000 ) ) ;
#53562=CARTESIAN_POINT ( 'NONE',  ( -6.676582343750001591, 293.6093750017069510, 0.000000000000000000 ) ) ;
#53563=CARTESIAN_POINT ( 'NONE',  ( 4.999999999999993783, 129.1666666666666856, 8.660254037844390851 ) ) ;
#53580=CARTESIAN_POINT ( 'NONE',  ( 6.951808397369818766E-16, 32.03124999658601979, -11.35316468750000141 ) ) ;
#53581=( BOUNDED_CURVE ( )  B_SPLINE_CURVE ( 2, ( #65260, #37343, #24530, #31303, #49019, #2642, #48645, #7195, #2266, #30931, #71654, #13564, #48279 ),
 .UNSPECIFIED., .F., .F. ) 
 B_SPLINE_CURVE_WITH_KNOTS ( ( 3, 2, 2, 2, 2, 2, 3 ),
 ( 0.5489130434782608647, 0.5507246376811594235, 0.5525362318840579823, 0.5543478260869565410, 0.5561594202898549888, 0.5579710144927535476, 0.5597826086956521063 ),
 .UNSPECIFIED. ) 
 CURVE ( )  GEOMETRIC_REPRESENTATION_ITEM ( )  RATIONAL_B_SPLINE_CURVE ( ( 1.000000000000000000, 0.9659258262890683122, 1.000000000000000000, 0.9659258262890683122, 1.000000000000000000, 0.9659258262890683122, 1.000000000000000000, 0.9659258262890683122, 1.000000000000000000, 0.9659258262890683122, 1.000000000000000000, 0.9659258262890704216, 0.9999999999999978906 ) ) 
 REPRESENTATION_ITEM ( '' )  );
#53583=( BOUNDED_CURVE ( )  B_SPLINE_CURVE ( 2, ( #39744, #51812, #23135, #35584, #46147, #69164, #41240, #17473, #40867, #63873, #64246, #12556, #58598 ),
 .UNSPECIFIED., .F., .F. ) 
 B_SPLINE_CURVE_WITH_KNOTS ( ( 3, 2, 2, 2, 2, 2, 3 ),
 ( 0.7554347826086956763, 0.7572463768115942351, 0.7590579710144927938, 0.7608695652173913526, 0.7626811594202898004, 0.7644927536231883591, 0.7663043478260869179 ),
 .UNSPECIFIED. ) 
 CURVE ( )  GEOMETRIC_REPRESENTATION_ITEM ( )  RATIONAL_B_SPLINE_CURVE ( ( 1.000000000000000000, 0.9659258262890683122, 1.000000000000000000, 0.9659258262890683122, 1.000000000000000000, 0.9659258262890683122, 1.000000000000000000, 0.9659258262890683122, 1.000000000000000000, 0.9659258262890683122, 1.000000000000000000, 0.9659258262890683122, 1.000000000000000000 ) ) 
 REPRESENTATION_ITEM ( '' )  );
#53584=CARTESIAN_POINT ( 'NONE',  ( -1.836970198721029983E-15, 5.624999993172032475, 10.00000000000000178 ) ) ;
#53585=DIRECTION ( 'NONE',  ( 0.000000000000000000, -1.000000000000000000, 0.000000000000000000 ) ) ;
#53587=VERTEX_POINT ( 'NONE', #16519 ) ;
#53592=CARTESIAN_POINT ( 'NONE',  ( -9.832129032723418760, 32.86458332991934839, -5.676582343750004256 ) ) ;
#53598=CARTESIAN_POINT ( 'NONE',  ( -5.676582343750006032, 34.11458332991934839, 9.832129032723418760 ) ) ;
#53600=CARTESIAN_POINT ( 'NONE',  ( -2.085542519210945728E-15, 149.5312499965860411, 11.35316468750000141 ) ) ;
#53601=CARTESIAN_POINT ( 'NONE',  ( 10.00000000000000178, 116.8749999931720396, 0.000000000000000000 ) ) ;
#53606=CARTESIAN_POINT ( 'NONE',  ( 5.676582343750001591, 26.92708332991935194, -9.832129032723420536 ) ) ;
#53610=CARTESIAN_POINT ( 'NONE',  ( -8.311093377946836114, 157.6562499965860411, -8.311093377946837890 ) ) ;
#53616=EDGE_LOOP ( 'NONE', ( #36117, #1370, #40645, #41397, #58853, #26580, #57739, #61093, #4937, #25528, #53462, #68087, #36074, #70614, #44764, #16384, #27046, #47010, #66062, #31965, #46034, #14633, #1064, #51559, #29658, #45884, #27104, #35242 ) ) ;
#53619=CARTESIAN_POINT ( 'NONE',  ( 8.660254037844390851, 120.4166666666666714, -5.000000000000001776 ) ) ;
#53620=CARTESIAN_POINT ( 'NONE',  ( 1.224646799147353454E-15, 300.0000000000000000, -10.00000000000000178 ) ) ;
#53621=CARTESIAN_POINT ( 'NONE',  ( -11.35316468749999785, 83.38541666325265567, -3.042071309553167513 ) ) ;
#53638=VERTEX_POINT ( 'NONE', #17279 ) ;
#53642=DIRECTION ( 'NONE',  ( 0.000000000000000000, 0.000000000000000000, 1.000000000000000000 ) ) ;
#53654=CARTESIAN_POINT ( 'NONE',  ( -2.679491924311235618, 88.54166666666668561, 10.00000000000000000 ) ) ;
#53656=CARTESIAN_POINT ( 'NONE',  ( -4.721056650415998313, 295.7343750017069510, 4.721056650416000089 ) ) ;
#53665=CARTESIAN_POINT ( 'NONE',  ( -8.660254037844387298, 212.0833333333333428, -5.000000000000004441 ) ) ;
#53667=CARTESIAN_POINT ( 'NONE',  ( 3.042071309553167069, 182.1354166632526699, -11.35316468749999785 ) ) ;
#53675=CARTESIAN_POINT ( 'NONE',  ( -9.832129032723418760, 53.17708332991935549, -5.676582343750004256 ) ) ;
#53678=CARTESIAN_POINT ( 'NONE',  ( 9.832129032723420536, 221.5104166632526983, -5.676582343749999815 ) ) ;
#53682=CARTESIAN_POINT ( 'NONE',  ( -8.660254037844390851, 59.79166665983870388, 4.999999999999998224 ) ) ;
#53685=CARTESIAN_POINT ( 'NONE',  ( -2.085542519210945728E-15, 104.5312499965860269, 11.35316468750000141 ) ) ;
#53686=CARTESIAN_POINT ( 'NONE',  ( 6.123233995736767268E-16, 78.12499999317202537, -10.00000000000000178 ) ) ;
#53694=CARTESIAN_POINT ( 'NONE',  ( -6.676582343750001591, 292.6093750017069510, 0.000000000000000000 ) ) ;
#53696=CARTESIAN_POINT ( 'NONE',  ( 5.676582343750001591, 166.6145833299193555, -9.832129032723420536 ) ) ;
#53697=CARTESIAN_POINT ( 'NONE',  ( 2.679491924311228956, 2.916666659838698994, -10.00000000000000000 ) ) ;
#53702=( BOUNDED_CURVE ( )  B_SPLINE_CURVE ( 2, ( #58790, #63687, #7833, #52752, #41061, #41431, #2171, #35775, #12379 ),
 .UNSPECIFIED., .F., .F. ) 
 B_SPLINE_CURVE_WITH_KNOTS ( ( 3, 2, 2, 2, 3 ),
 ( 0.2291666666666645480, 0.2395833333333312609, 0.2499999999999979183, 0.2604166666666646313, 0.2708333333333312609 ),
 .UNSPECIFIED. ) 
 CURVE ( )  GEOMETRIC_REPRESENTATION_ITEM ( )  RATIONAL_B_SPLINE_CURVE ( ( 1.000000000000015321, 0.9238795325112713064, 1.000000000000000000, 0.9238795325112867385, 1.000000000000000000, 0.9238795325112867385, 1.000000000000000000, 0.9238795325113017265, 0.9999999999999850120 ) ) 
 REPRESENTATION_ITEM ( '' )  );
#53703=ADVANCED_FACE ( 'NONE', ( #45580 ), #18401, .T. ) ;
#53706=CARTESIAN_POINT ( 'NONE',  ( -5.676582343749998039, 142.7604166632526699, -9.832129032723420536 ) ) ;
#53709=CARTESIAN_POINT ( 'NONE',  ( 11.35316468749999963, 46.30208332991934128, -3.042071309553165293 ) ) ;
#53715=CARTESIAN_POINT ( 'NONE',  ( -3.673940397442060854E-16, 291.8125000034140157, -6.000000000000001776 ) ) ;
#53721=( BOUNDED_CURVE ( )  B_SPLINE_CURVE ( 2, ( #36086, #59105, #6678, #30420, #1031, #29681, #64750, #47393, #41376, #58008, #24011, #12685, #69302 ),
 .UNSPECIFIED., .F., .F. ) 
 B_SPLINE_CURVE_WITH_KNOTS ( ( 3, 2, 2, 2, 2, 2, 3 ),
 ( 1.711289316333768351, 1.716522046495266629, 1.721754776656765129, 1.726987506818263407, 1.732220236979761685, 1.737452967141260185, 1.742685697302758463 ),
 .UNSPECIFIED. ) 
 CURVE ( )  GEOMETRIC_REPRESENTATION_ITEM ( )  RATIONAL_B_SPLINE_CURVE ( ( 1.000000000000001998, 0.9659258262890662028, 1.000000000000000000, 0.9659258262890683122, 1.000000000000000000, 0.9659258262890683122, 1.000000000000000000, 0.9659258262890683122, 1.000000000000000000, 0.9659258262890683122, 1.000000000000000000, 0.9659258262893397617, 0.9999999999997285505 ) ) 
 REPRESENTATION_ITEM ( '' )  );
#53739=CARTESIAN_POINT ( 'NONE',  ( 6.000000000000001776, 296.5000000000000000, -7.347880794884121708E-16 ) ) ;
#53741=CARTESIAN_POINT ( 'NONE',  ( 7.320508075688771044, 54.37500000000000000, 7.320508075688775484 ) ) ;
#53743=CARTESIAN_POINT ( 'NONE',  ( 6.000000000000003553, 296.5625000000000000, -2.485281374238571761 ) ) ;
#53744=CARTESIAN_POINT ( 'NONE',  ( -3.673940397442060854E-16, 287.8125000034140157, -6.000000000000001776 ) ) ;
#53753=CARTESIAN_POINT ( 'NONE',  ( 2.679491924311222739, 173.9583333333333144, 10.00000000000000355 ) ) ;
#53757=CARTESIAN_POINT ( 'NONE',  ( 9.832129032723416984, 145.6770833299193555, 5.676582343750006032 ) ) ;
#53765=CARTESIAN_POINT ( 'NONE',  ( 5.676582343750001591, 11.92708332991935016, -9.832129032723420536 ) ) ;
#53768=CARTESIAN_POINT ( 'NONE',  ( -5.000000000000005329, 90.20833332650536818, 8.660254037844387298 ) ) ;
#53772=CARTESIAN_POINT ( 'NONE',  ( 2.679491924311222739, 35.83333332650536818, 10.00000000000000355 ) ) ;
#53777=CARTESIAN_POINT ( 'NONE',  ( -3.673940397442060854E-16, 291.8125000034140157, -6.000000000000001776 ) ) ;
#53778=VERTEX_POINT ( 'NONE', #34287 ) ;
#53780=CARTESIAN_POINT ( 'NONE',  ( 7.320508075688775484, 29.37500000000000355, 7.320508075688779037 ) ) ;
#53783=CARTESIAN_POINT ( 'NONE',  ( 9.832129032723420536, 111.1979166632526983, -5.676582343749999815 ) ) ;
#53791=CARTESIAN_POINT ( 'NONE',  ( -8.311093377946841443, 113.9062499965860127, 8.311093377946834337 ) ) ;
#53794=VERTEX_POINT ( 'NONE', #53845 ) ;
#53795=CARTESIAN_POINT ( 'NONE',  ( 10.00000000000000178, 211.8749999931720538, 0.000000000000000000 ) ) ;
#53798=CARTESIAN_POINT ( 'NONE',  ( -8.311093377946836114, 102.9687499965859985, -8.311093377946837890 ) ) ;
#53803=CARTESIAN_POINT ( 'NONE',  ( -5.676582343750006032, 4.427083329919350163, 9.832129032723418760 ) ) ;
#53805=CARTESIAN_POINT ( 'NONE',  ( 8.660254037844385522, 181.4583333265053682, 5.000000000000005329 ) ) ;
#53811=CARTESIAN_POINT ( 'NONE',  ( 1.226468279477575784E-15, 294.7031250017069510, 6.676582343750001591 ) ) ;
#53812=CARTESIAN_POINT ( 'NONE',  ( 7.320508075688771044, 126.2499999931720396, 7.320508075688775484 ) ) ;
#53813=CARTESIAN_POINT ( 'NONE',  ( -5.676582343749998039, 222.7604166632526983, -9.832129032723420536 ) ) ;
#53831=CARTESIAN_POINT ( 'NONE',  ( -7.320508075688778149, 29.99999999317203248, 7.320508075688769267 ) ) ;
#53835=CARTESIAN_POINT ( 'NONE',  ( -2.765530957081998142, 292.6406250017069510, 6.676582343750000703 ) ) ;
#53837=CARTESIAN_POINT ( 'NONE',  ( 4.999999999999993783, 136.0416666598387110, 8.660254037844390851 ) ) ;
#53844=CARTESIAN_POINT ( 'NONE',  ( 11.35316468749999963, 106.3020833299193413, -3.042071309553165293 ) ) ;
#53845=CARTESIAN_POINT ( 'NONE',  ( 6.123233995736767268E-16, 43.12499999317203248, -10.00000000000000178 ) ) ;
#53851=EDGE_CURVE ( 'NONE', #22380, #38706, #396, .T. ) ;
#53852=CARTESIAN_POINT ( 'NONE',  ( 6.951808397369818766E-16, 207.0312499965860411, -11.35316468750000141 ) ) ;
#53857=CARTESIAN_POINT ( 'NONE',  ( -2.085542519210945728E-15, 194.8437499965860127, 11.35316468750000141 ) ) ;
#53864=CARTESIAN_POINT ( 'NONE',  ( 11.35316468749999963, 85.98958332991936970, -3.042071309553165293 ) ) ;
#53865=ORIENTED_EDGE ( 'NONE', *, *, #37951, .T. ) ;
#53867=CARTESIAN_POINT ( 'NONE',  ( 7.320508075688781702, 140.6250000000000284, -7.320508075688781702 ) ) ;
#53870=CARTESIAN_POINT ( 'NONE',  ( -2.679491924311159234, 46.45833333333334281, -10.00000000000007105 ) ) ;
#53872=CARTESIAN_POINT ( 'NONE',  ( 8.311093377946837890, 71.40624999658602690, -8.311093377946837890 ) ) ;
#53879=CARTESIAN_POINT ( 'NONE',  ( 8.311093377946837890, 76.40624999658602690, -8.311093377946837890 ) ) ;
#53882=CARTESIAN_POINT ( 'NONE',  ( 7.320508075688774596, 172.4999999931719969, -7.320508075688774596 ) ) ;
#53885=CARTESIAN_POINT ( 'NONE',  ( 8.311093377946834337, 55.46874999658601268, 8.311093377946839666 ) ) ;
#53887=CARTESIAN_POINT ( 'NONE',  ( -3.042071309553173730, 194.3229166632526699, 11.35316468749999785 ) ) ;
#53888=VERTEX_POINT ( 'NONE', #1443 ) ;
#53893=CARTESIAN_POINT ( 'NONE',  ( -11.35316468750000141, 188.2812499965860127, -1.390361679473963753E-15 ) ) ;
#53894=VECTOR ( 'NONE', #50677, 1000.000000000000000 ) ;
#53895=CARTESIAN_POINT ( 'NONE',  ( -2.679491924311226292, 193.3333333265053682, -10.00000000000000178 ) ) ;
#53898=CARTESIAN_POINT ( 'NONE',  ( -5.676582343749998039, 182.7604166632526699, -9.832129032723420536 ) ) ;
#53905=CARTESIAN_POINT ( 'NONE',  ( 6.123233995736767268E-16, 6.250000000000000000, -10.00000000000000178 ) ) ;
#53913=FACE_OUTER_BOUND ( 'NONE', #44330, .T. ) ;
#53918=EDGE_CURVE ( 'NONE', #38960, #57815, #10758, .T. ) ;
#53921=EDGE_LOOP ( 'NONE', ( #73466, #67797, #20634, #48896 ) ) ;
#53929=CARTESIAN_POINT ( 'NONE',  ( 6.676582343750003368, 293.0468750017069510, 2.765530957081995478 ) ) ;
#53930=CARTESIAN_POINT ( 'NONE',  ( 10.00000000000000178, 150.0000000000000284, 0.000000000000000000 ) ) ;
#53947=CARTESIAN_POINT ( 'NONE',  ( 5.676582343750001591, 41.61458332991935549, -9.832129032723420536 ) ) ;
#53949=CARTESIAN_POINT ( 'NONE',  ( -8.660254037844387298, 8.958333326505366401, -5.000000000000004441 ) ) ;
#53952=ORIENTED_EDGE ( 'NONE', *, *, #48868, .T. ) ;
#53955=CARTESIAN_POINT ( 'NONE',  ( 5.676582343749993598, 29.94791666325268409, 9.832129032723422313 ) ) ;
#53961=CARTESIAN_POINT ( 'NONE',  ( 11.35316468749999963, 35.98958332991934128, -3.042071309553165293 ) ) ;
#53964=CARTESIAN_POINT ( 'NONE',  ( -3.042071309553173730, 154.3229166632527267, 11.35316468749999785 ) ) ;
#53965=VECTOR ( 'NONE', #13928, 1000.000000000000000 ) ;
#53966=CARTESIAN_POINT ( 'NONE',  ( -7.320508075688773708, 128.7499999931720538, -7.320508075688774596 ) ) ;
#53970=CARTESIAN_POINT ( 'NONE',  ( -1.836970198721029983E-15, 20.62499999317203603, 10.00000000000000178 ) ) ;
#53971=CARTESIAN_POINT ( 'NONE',  ( -2.085542519210945728E-15, 19.84374999658601979, 11.35316468750000141 ) ) ;
#53976=CARTESIAN_POINT ( 'NONE',  ( 9.832129032723416984, 155.3645833299193839, 5.676582343750006032 ) ) ;
#53985=CARTESIAN_POINT ( 'NONE',  ( 9.832129032723416984, 100.6770833299193555, 5.676582343750006032 ) ) ;
#54008=CARTESIAN_POINT ( 'NONE',  ( 2.679491924311228956, 122.9166666598386968, -10.00000000000000000 ) ) ;
#54020=CARTESIAN_POINT ( 'NONE',  ( -10.00000000000000000, 102.2916666666666572, -2.679491924311229845 ) ) ;
#54024=CARTESIAN_POINT ( 'NONE',  ( -6.676582343750000703, 296.6718750017069510, 2.765530957082001251 ) ) ;
#54026=EDGE_CURVE ( 'NONE', #45113, #28745, #8068, .T. ) ;
#54027=CARTESIAN_POINT ( 'NONE',  ( 6.123233995736767268E-16, 143.1249999931720538, -10.00000000000000178 ) ) ;
#54035=CARTESIAN_POINT ( 'NONE',  ( 7.320508075688771044, 214.3749999999999716, 7.320508075688775484 ) ) ;
#54037=CARTESIAN_POINT ( 'NONE',  ( -9.832129032723420536, 189.0104166632526983, 5.676582343749997150 ) ) ;
#54041=DIRECTION ( 'NONE',  ( -0.000000000000000000, 1.000000000000000000, -0.000000000000000000 ) ) ;
#54045=CARTESIAN_POINT ( 'NONE',  ( 11.35316468750000141, 46.09374999658602690, 0.000000000000000000 ) ) ;
#54047=CARTESIAN_POINT ( 'NONE',  ( -9.832129032723418760, 223.1770833299193555, -5.676582343750004256 ) ) ;
#54054=CARTESIAN_POINT ( 'NONE',  ( -9.832129032723420536, 103.6979166632526841, 5.676582343749997150 ) ) ;
#54056=CARTESIAN_POINT ( 'NONE',  ( -1.836970198721029983E-15, 90.62499999317203958, 10.00000000000000178 ) ) ;
#54059=CARTESIAN_POINT ( 'NONE',  ( -8.660254037844390851, 72.08333333333334281, -5.000000000000007105 ) ) ;
#54060=CYLINDRICAL_SURFACE ( 'NONE', #8853, 10.00000000000000178 ) ;
#54061=ORIENTED_EDGE ( 'NONE', *, *, #35551, .T. ) ;
#54063=CARTESIAN_POINT ( 'NONE',  ( -4.088227598258586603E-16, 292.3593750017070079, -6.676582343750001591 ) ) ;
#54064=CARTESIAN_POINT ( 'NONE',  ( -8.311093377946841443, 168.9062499965860411, 8.311093377946830785 ) ) ;
#54070=ORIENTED_EDGE ( 'NONE', *, *, #67401, .F. ) ;
#54071=VECTOR ( 'NONE', #70111, 1000.000000000000000 ) ;
#54074=CARTESIAN_POINT ( 'NONE',  ( 6.951808397369818766E-16, 142.3437499965860411, -11.35316468750000141 ) ) ;
#54078=CARTESIAN_POINT ( 'NONE',  ( 8.311093377946834337, 65.46874999658601268, 8.311093377946839666 ) ) ;
#54085=CARTESIAN_POINT ( 'NONE',  ( -2.485281374238571761, 293.8750000034139589, -6.000000000000003553 ) ) ;
#54101=CARTESIAN_POINT ( 'NONE',  ( -4.242640687119285658, 295.1249999999999432, 4.242640687119287435 ) ) ;
#54106=CARTESIAN_POINT ( 'NONE',  ( -2.679491924311382611, 203.5416666666666572, 9.999999999999912959 ) ) ;
#54109=CARTESIAN_POINT ( 'NONE',  ( -8.660254037844387298, 57.08333333333334281, -5.000000000000004441 ) ) ;
#54111=EDGE_CURVE ( 'NONE', #55396, #23868, #31204, .T. ) ;
#54113=CARTESIAN_POINT ( 'NONE',  ( 2.485281374238571317, 296.6875000000000568, -6.000000000000003553 ) ) ;
#54120=CARTESIAN_POINT ( 'NONE',  ( -10.00000000000000178, 74.37499999317203958, -1.224646799147353454E-15 ) ) ;
#54124=CARTESIAN_POINT ( 'NONE',  ( -7.320508075688778149, 173.1249999999999716, 7.320508075688769267 ) ) ;
#54128=CARTESIAN_POINT ( 'NONE',  ( -2.085542519210945728E-15, 149.8437499965860411, 11.35316468750000141 ) ) ;
#54129=DIRECTION ( 'NONE',  ( 1.000000000000000000, 0.000000000000000000, -0.000000000000000000 ) ) ;
#54134=ORIENTED_EDGE ( 'NONE', *, *, #64585, .F. ) ;
#54135=CARTESIAN_POINT ( 'NONE',  ( -5.676582343750006032, 14.42708332991935016, 9.832129032723418760 ) ) ;
#54143=EDGE_CURVE ( 'NONE', #61723, #48752, #37986, .T. ) ;
#54144=CARTESIAN_POINT ( 'NONE',  ( -4.999999999999998224, 33.54166665983870388, -8.660254037844389075 ) ) ;
#54149=FACE_OUTER_BOUND ( 'NONE', #7353, .T. ) ;
#54151=ORIENTED_EDGE ( 'NONE', *, *, #9203, .T. ) ;
#54152=CARTESIAN_POINT ( 'NONE',  ( 6.000000000000003553, 292.5000000034140157, 2.485281374238571317 ) ) ;
#54156=CARTESIAN_POINT ( 'NONE',  ( 8.311093377946834337, 130.1562499965860411, 8.311093377946839666 ) ) ;
#54159=B_SPLINE_CURVE_WITH_KNOTS ( 'NONE', 5,
 ( #39608, #56970, #5285, #40347, #55854, #58457 ),
 .UNSPECIFIED., .F., .F.,
 ( 6, 6 ),
 ( 0.000000000000000000, 1.000000000000000000 ),
 .UNSPECIFIED. ) ;
#54166=CARTESIAN_POINT ( 'NONE',  ( 8.311093377946837890, 111.4062499965860269, -8.311093377946837890 ) ) ;
#54168=CARTESIAN_POINT ( 'NONE',  ( 8.660254037844385522, 146.4583333265053682, 5.000000000000005329 ) ) ;
#54170=VECTOR ( 'NONE', #11051, 1000.000000000000000 ) ;
#54174=CARTESIAN_POINT ( 'NONE',  ( 9.832129032723416984, 105.6770833299193413, 5.676582343750006032 ) ) ;
#54178=CARTESIAN_POINT ( 'NONE',  ( 6.951808397369818766E-16, 7.343749996586017126, -11.35316468750000141 ) ) ;
#54181=CARTESIAN_POINT ( 'NONE',  ( 10.00000000000000178, 182.0833333265053682, -2.679491924311226736 ) ) ;
#54187=CARTESIAN_POINT ( 'NONE',  ( 4.721056650416000089, 291.8281250017069510, 4.721056650415999201 ) ) ;
#54189=CARTESIAN_POINT ( 'NONE',  ( 3.042071309553167069, 132.1354166632526699, -11.35316468749999785 ) ) ;
#54204=CARTESIAN_POINT ( 'NONE',  ( -2.679491924311226292, 28.33333332650536818, -10.00000000000000178 ) ) ;
#54207=CARTESIAN_POINT ( 'NONE',  ( 2.765530957082001251, 291.7656250017069510, 6.676582343749999815 ) ) ;
#54208=CARTESIAN_POINT ( 'NONE',  ( 2.679491924311075302, 130.8333333265053682, 10.00000000000008704 ) ) ;
#54211=EDGE_CURVE ( 'NONE', #62209, #55468, #7205, .T. ) ;
#54219=CARTESIAN_POINT ( 'NONE',  ( -8.311093377946836114, 102.9687499965859985, -8.311093377946837890 ) ) ;
#54229=CARTESIAN_POINT ( 'NONE',  ( 3.042071309553167069, 211.8229166632527267, -11.35316468749999785 ) ) ;
#54234=CARTESIAN_POINT ( 'NONE',  ( -3.042071309553164404, 197.5520833299193555, -11.35316468749999963 ) ) ;
#54236=CARTESIAN_POINT ( 'NONE',  ( 9.150885453380622536, 225.9999999999998863, 5.663720741180870100 ) ) ;
#54241=CARTESIAN_POINT ( 'NONE',  ( -11.35316468749999785, 88.07291666325266988, -3.042071309553167513 ) ) ;
#54248=CARTESIAN_POINT ( 'NONE',  ( -8.311093377946836114, 87.65624999658601268, -8.311093377946837890 ) ) ;
#54254=CARTESIAN_POINT ( 'NONE',  ( 6.951808397369818766E-16, 77.03124999658601268, -11.35316468750000141 ) ) ;
#54256=CARTESIAN_POINT ( 'NONE',  ( 7.320508075688774596, 130.6250000000000284, -7.320508075688774596 ) ) ;
#54258=CARTESIAN_POINT ( 'NONE',  ( -2.679491924311235618, 170.4166666598386541, 10.00000000000000000 ) ) ;
#54261=CARTESIAN_POINT ( 'NONE',  ( 6.951808397369818766E-16, 67.34374999658601268, -11.35316468750000141 ) ) ;
#54262=CARTESIAN_POINT ( 'NONE',  ( 4.721056650415999201, 292.0781250017069510, -4.721056650415999201 ) ) ;
#54265=CARTESIAN_POINT ( 'NONE',  ( 6.951808397369818766E-16, 192.0312499965860127, -11.35316468750000141 ) ) ;
#54271=CARTESIAN_POINT ( 'NONE',  ( 8.311093377946834337, 195.1562499965860411, 8.311093377946839666 ) ) ;
#54274=CARTESIAN_POINT ( 'NONE',  ( -7.320508075688778149, 189.9999999931720538, 7.320508075688769267 ) ) ;
#54276=CARTESIAN_POINT ( 'NONE',  ( 8.311093377946834337, 185.4687499965860127, 8.311093377946839666 ) ) ;
#54279=AXIS2_PLACEMENT_3D ( 'NONE', #44767, #67780, #51162 ) ;
#54290=VERTEX_POINT ( 'NONE', #16433 ) ;
#54304=CARTESIAN_POINT ( 'NONE',  ( 5.676582343750001591, 61.92708332991934839, -9.832129032723420536 ) ) ;
#54305=CARTESIAN_POINT ( 'NONE',  ( 8.660254037844385522, 91.45833332650536818, 5.000000000000005329 ) ) ;
#54309=CARTESIAN_POINT ( 'NONE',  ( -6.676582343750001591, 294.6093750017069510, 0.000000000000000000 ) ) ;
#54310=CARTESIAN_POINT ( 'NONE',  ( 10.00000000000000178, 150.2083333333333428, -2.679491924311226736 ) ) ;
#54313=DIRECTION ( 'NONE',  ( -0.000000000000000000, 1.000000000000000000, -0.000000000000000000 ) ) ;
#54321=DIRECTION ( 'NONE',  ( -0.000000000000000000, 1.000000000000000000, -0.000000000000000000 ) ) ;
#54323=CARTESIAN_POINT ( 'NONE',  ( 7.320508075688777261, 135.6249999999999716, -7.320508075688777261 ) ) ;
#54327=CARTESIAN_POINT ( 'NONE',  ( -11.35316468750000141, 43.48958332991935549, 3.042071309553159963 ) ) ;
#54329=CARTESIAN_POINT ( 'NONE',  ( -10.00000000000000000, 14.16666665983870210, -2.679491924311229845 ) ) ;
#54333=CARTESIAN_POINT ( 'NONE',  ( 6.951808397369818766E-16, 42.03124999658601268, -11.35316468750000141 ) ) ;
#54336=CARTESIAN_POINT ( 'NONE',  ( -4.242640687119286547, 298.8750000000000000, -4.242640687119286547 ) ) ;
#54339=CARTESIAN_POINT ( 'NONE',  ( -3.042071309553173730, 39.32291666325267698, 11.35316468749999785 ) ) ;
#54341=CARTESIAN_POINT ( 'NONE',  ( -3.042071309553173730, 164.3229166632526415, 11.35316468749999785 ) ) ;
#54342=CARTESIAN_POINT ( 'NONE',  ( -2.679491924311235618, 125.4166666598386968, 10.00000000000000000 ) ) ;
#54346=CARTESIAN_POINT ( 'NONE',  ( 5.676582343749993598, 25.26041666325268764, 9.832129032723422313 ) ) ;
#54352=CARTESIAN_POINT ( 'NONE',  ( -5.676582343750006032, 149.1145833299193555, 9.832129032723418760 ) ) ;
#54354=AXIS2_PLACEMENT_3D ( 'NONE', #44214, #32149, #73256 ) ;
#54362=DIRECTION ( 'NONE',  ( -0.000000000000000000, 1.000000000000000000, -0.000000000000000000 ) ) ;
#54365=CARTESIAN_POINT ( 'NONE',  ( 8.311093377946834337, 105.4687499965860127, 8.311093377946839666 ) ) ;
#54368=ORIENTED_EDGE ( 'NONE', *, *, #23212, .F. ) ;
#54391=ORIENTED_EDGE ( 'NONE', *, *, #8487, .F. ) ;
#54399=CARTESIAN_POINT ( 'NONE',  ( -7.320508075688778149, 113.1250000000000142, 7.320508075688769267 ) ) ;
#54401=CARTESIAN_POINT ( 'NONE',  ( -2.765530957081996810, 296.4218750017070079, -6.676582343750003368 ) ) ;
#54410=CARTESIAN_POINT ( 'NONE',  ( 1.102182119232618108E-15, 289.2500000000000000, 6.000000000000001776 ) ) ;
#54412=CARTESIAN_POINT ( 'NONE',  ( 3.042071309553159519, 4.739583329919349275, 11.35316468750000141 ) ) ;
#54414=CARTESIAN_POINT ( 'NONE',  ( -8.311093377946841443, 189.2187499965860411, 8.311093377946830785 ) ) ;
#54423=CARTESIAN_POINT ( 'NONE',  ( -11.35316468750000141, 48.59374999658601268, -1.390361679473963753E-15 ) ) ;
#54431=CARTESIAN_POINT ( 'NONE',  ( -11.35316468750000141, 128.2812499965860127, -1.390361679473963753E-15 ) ) ;
#54432=CARTESIAN_POINT ( 'NONE',  ( -4.999999999999998224, 93.54166665983871098, -8.660254037844389075 ) ) ;
#54438=CARTESIAN_POINT ( 'NONE',  ( -7.950158476760519122, 225.9999999999998863, 6.101342341042199635 ) ) ;
#54440=CARTESIAN_POINT ( 'NONE',  ( 6.676582343750001591, 294.1093750017069510, -8.176455196517173205E-16 ) ) ;
#54443=CARTESIAN_POINT ( 'NONE',  ( -3.042071309553173730, 174.3229166632526983, 11.35316468749999785 ) ) ;
#54446=CARTESIAN_POINT ( 'NONE',  ( 6.123233995736767268E-16, 83.12499999317203958, -10.00000000000000178 ) ) ;
#54448=ORIENTED_EDGE ( 'NONE', *, *, #74038, .F. ) ;
#54452=CARTESIAN_POINT ( 'NONE',  ( 3.042071309553167513, 137.1354166632526983, -11.35316468749999785 ) ) ;
#54453=CARTESIAN_POINT ( 'NONE',  ( 6.350741970897364085E-13, 216.2499999999999432, -9.999999999999998224 ) ) ;
#54457=CARTESIAN_POINT ( 'NONE',  ( 3.042071309553159519, 65.05208332991932707, 11.35316468750000141 ) ) ;
#54465=CARTESIAN_POINT ( 'NONE',  ( -6.000000000000001776, 290.0625000034140157, 0.000000000000000000 ) ) ;
#54490=CARTESIAN_POINT ( 'NONE',  ( -1.836970198721029983E-15, 73.75000000000001421, 10.00000000000000178 ) ) ;
#54492=CARTESIAN_POINT ( 'NONE',  ( -3.673940397442060854E-16, 296.7500000000000000, -6.000000000000001776 ) ) ;
#54503=CARTESIAN_POINT ( 'NONE',  ( 5.000000000000001776, 190.8333333333333428, -8.660254037844389075 ) ) ;
#54506=CARTESIAN_POINT ( 'NONE',  ( -8.311093377946836114, 152.9687499965859558, -8.311093377946837890 ) ) ;
#54507=CARTESIAN_POINT ( 'NONE',  ( 4.242640687119287435, 294.4375000034140157, 4.242640687119285658 ) ) ;
#54510=CARTESIAN_POINT ( 'NONE',  ( -2.679491924311235174, 85.41666665983869677, 10.00000000000000000 ) ) ;
#54511=CARTESIAN_POINT ( 'NONE',  ( -4.242640687119286547, 293.8750000000000000, -4.242640687119286547 ) ) ;
#54513=CARTESIAN_POINT ( 'NONE',  ( -8.311093377946841443, 14.21874999658601979, 8.311093377946830785 ) ) ;
#54515=CARTESIAN_POINT ( 'NONE',  ( 0.000000000000000000, 300.0000000000000000, 0.000000000000000000 ) ) ;
#54518=CARTESIAN_POINT ( 'NONE',  ( 10.00000000000000000, 46.66666665983868967, 2.679491924311236062 ) ) ;
#54524=ORIENTED_EDGE ( 'NONE', *, *, #38594, .T. ) ;
#54528=CARTESIAN_POINT ( 'NONE',  ( -8.311093377946841443, 133.9062499965860411, 8.311093377946830785 ) ) ;
#54529=ORIENTED_EDGE ( 'NONE', *, *, #24114, .F. ) ;
#54530=EDGE_CURVE ( 'NONE', #53638, #62209, #64047, .T. ) ;
#54537=CARTESIAN_POINT ( 'NONE',  ( -2.085542519210945728E-15, 119.5312499965860269, 11.35316468750000141 ) ) ;
#54539=CARTESIAN_POINT ( 'NONE',  ( 4.999999999999993783, 81.04166665983871098, 8.660254037844390851 ) ) ;
#54544=CARTESIAN_POINT ( 'NONE',  ( 8.311093377946837890, 106.7187499965860269, -8.311093377946837890 ) ) ;
#54548=CARTESIAN_POINT ( 'NONE',  ( -8.311093377946841443, 19.21874999658601979, 8.311093377946830785 ) ) ;
#54552=CARTESIAN_POINT ( 'NONE',  ( 10.92737078412413609, 225.9999999999999147, -3.080083792328916825 ) ) ;
#54556=CARTESIAN_POINT ( 'NONE',  ( -6.000000000000003553, 299.0000000034139589, -2.485281374238571317 ) ) ;
#54558=CARTESIAN_POINT ( 'NONE',  ( 8.311093377946837890, 221.7187499965860127, -8.311093377946837890 ) ) ;
#54559=ADVANCED_FACE ( 'NONE', ( #23967 ), #25058, .T. ) ;
#54560=CARTESIAN_POINT ( 'NONE',  ( 11.35316468749999963, 136.3020833299193555, -3.042071309553165293 ) ) ;
#54576=DIRECTION ( 'NONE',  ( -0.000000000000000000, 1.000000000000000000, -0.000000000000000000 ) ) ;
#54578=CARTESIAN_POINT ( 'NONE',  ( -5.676582343750006032, 184.1145833299193555, 9.832129032723418760 ) ) ;
#54580=CARTESIAN_POINT ( 'NONE',  ( 1.102182119232618108E-15, 295.2500000000000000, 6.000000000000001776 ) ) ;
#54581=CARTESIAN_POINT ( 'NONE',  ( 4.721056650415999201, 291.0781250017069510, -4.721056650415999201 ) ) ;
#54593=CARTESIAN_POINT ( 'NONE',  ( -4.242640687119286547, 298.9375000034140157, -4.242640687119286547 ) ) ;
#54595=CARTESIAN_POINT ( 'NONE',  ( -3.042071309553173730, 119.6354166632526841, 11.35316468749999785 ) ) ;
#54600=DIRECTION ( 'NONE',  ( -0.000000000000000000, 1.000000000000000000, -0.000000000000000000 ) ) ;
#54603=CARTESIAN_POINT ( 'NONE',  ( 8.311093377946837890, 221.4062499965860411, -8.311093377946837890 ) ) ;
#54607=CARTESIAN_POINT ( 'NONE',  ( -2.085542519210945728E-15, 189.8437499965860127, 11.35316468750000141 ) ) ;
#54614=CARTESIAN_POINT ( 'NONE',  ( -11.35316468750000141, 88.48958332991934128, 3.042071309553159963 ) ) ;
#54616=CARTESIAN_POINT ( 'NONE',  ( 7.320508075688779037, 139.3750000000000000, 7.320508075688782590 ) ) ;
#54620=CARTESIAN_POINT ( 'NONE',  ( -5.676582343750006032, 89.11458332991935549, 9.832129032723418760 ) ) ;
#54627=CARTESIAN_POINT ( 'NONE',  ( 6.951808397369818766E-16, 72.03124999658602690, -11.35316468750000141 ) ) ;
#54630=CARTESIAN_POINT ( 'NONE',  ( 8.660254037844385522, 171.4583333265053682, 5.000000000000005329 ) ) ;
#54633=CARTESIAN_POINT ( 'NONE',  ( -5.676582343750006032, 59.42708332991934839, 9.832129032723418760 ) ) ;
#54634=CARTESIAN_POINT ( 'NONE',  ( -4.721056650415998313, 295.5781250017069510, 4.721056650416000089 ) ) ;
#54636=CARTESIAN_POINT ( 'NONE',  ( -2.085542519210945728E-15, 209.5312499965860411, 11.35316468750000141 ) ) ;
#54642=CARTESIAN_POINT ( 'NONE',  ( -11.35316468750000141, 198.4895833299193555, 3.042071309553159963 ) ) ;
#54648=CARTESIAN_POINT ( 'NONE',  ( 5.676582343749993598, 175.2604166632526699, 9.832129032723422313 ) ) ;
#54654=CARTESIAN_POINT ( 'NONE',  ( -8.660254037844390851, 7.916666666666666963, 4.999999999999998224 ) ) ;
#54656=AXIS2_PLACEMENT_3D ( 'NONE', #35889, #24179, #18531 ) ;
#54663=CARTESIAN_POINT ( 'NONE',  ( -3.673940397442060854E-16, 293.8125000034140157, -6.000000000000001776 ) ) ;
#54665=CARTESIAN_POINT ( 'NONE',  ( -2.679491924311265816, 83.54166666666672825, 10.00000000000011546 ) ) ;
#54670=ADVANCED_FACE ( 'NONE', ( #49194 ), #39010, .T. ) ;
#54677=CARTESIAN_POINT ( 'NONE',  ( -3.042071309553173730, 74.63541666325268409, 11.35316468749999785 ) ) ;
#54678=CARTESIAN_POINT ( 'NONE',  ( 5.000000000000001776, 92.70833332650536818, -8.660254037844389075 ) ) ;
#54682=CARTESIAN_POINT ( 'NONE',  ( 4.721056650415999201, 292.2343750017069510, -4.721056650415999201 ) ) ;
#54683=CARTESIAN_POINT ( 'NONE',  ( -2.679491924311225848, 151.4583333333333428, -10.00000000000000178 ) ) ;
#54685=CARTESIAN_POINT ( 'NONE',  ( -1.836970198721029983E-15, 165.6249999931720254, 10.00000000000000178 ) ) ;
#54687=CARTESIAN_POINT ( 'NONE',  ( 1.102182119232618108E-15, 293.2500000000000000, 6.000000000000001776 ) ) ;
#54693=CARTESIAN_POINT ( 'NONE',  ( -2.485281374238217822, 293.2500000034140157, 6.000000000000357048 ) ) ;
#54699=CARTESIAN_POINT ( 'NONE',  ( 8.311093377946834337, 45.15624999658601268, 8.311093377946839666 ) ) ;
#54701=CARTESIAN_POINT ( 'NONE',  ( 6.123233995736767268E-16, 8.124999993172032475, -10.00000000000000178 ) ) ;
#54706=CARTESIAN_POINT ( 'NONE',  ( -5.676582343750006032, 49.11458332991935549, 9.832129032723418760 ) ) ;
#54709=CARTESIAN_POINT ( 'NONE',  ( -4.242640687119285658, 299.1250000000000000, 4.242640687119287435 ) ) ;
#54712=CARTESIAN_POINT ( 'NONE',  ( 6.951808397369818766E-16, 27.03124999658601979, -11.35316468750000141 ) ) ;
#54715=CARTESIAN_POINT ( 'NONE',  ( -5.000000000000005329, 50.20833332650537528, 8.660254037844387298 ) ) ;
#54716=CARTESIAN_POINT ( 'NONE',  ( 9.832129032723416984, 155.3645833299193839, 5.676582343750006032 ) ) ;
#54718=CARTESIAN_POINT ( 'NONE',  ( -5.000000000000005329, 130.2083333265053966, 8.660254037844387298 ) ) ;
#54721=CARTESIAN_POINT ( 'NONE',  ( 7.320508075688771044, 21.24999999317203248, 7.320508075688775484 ) ) ;
#54722=CARTESIAN_POINT ( 'NONE',  ( 9.832129032723420536, 16.51041666325268054, -5.676582343749999815 ) ) ;
#54723=EDGE_CURVE ( 'NONE', #14049, #30219, #60894, .T. ) ;
#54730=CARTESIAN_POINT ( 'NONE',  ( 8.311093377946837890, 151.4062499965860127, -8.311093377946837890 ) ) ;
#54737=CARTESIAN_POINT ( 'NONE',  ( -2.679491924311226292, 118.3333333265053966, -10.00000000000000178 ) ) ;
#54739=CARTESIAN_POINT ( 'NONE',  ( -5.676582343749998039, 102.7604166632526841, -9.832129032723420536 ) ) ;
#54741=CARTESIAN_POINT ( 'NONE',  ( 10.00000000000001066, 15.00000000000000533, 0.000000000000000000 ) ) ;
#54750=CARTESIAN_POINT ( 'NONE',  ( -8.660254037844387298, 158.9583333265053966, -5.000000000000004441 ) ) ;
#54770=CARTESIAN_POINT ( 'NONE',  ( -8.660254037844387298, 107.0833333333333428, -5.000000000000004441 ) ) ;
#54772=CARTESIAN_POINT ( 'NONE',  ( -6.676582343750000703, 290.6718750017070079, 2.765530957082001251 ) ) ;
#54774=VERTEX_POINT ( 'NONE', #32619 ) ;
#54783=CARTESIAN_POINT ( 'NONE',  ( -8.660254037844390851, 222.9166666666666856, 4.999999999999998224 ) ) ;
#54785=CARTESIAN_POINT ( 'NONE',  ( 11.35316468749999785, 195.8854166632526415, 3.042071309553174174 ) ) ;
#54790=CARTESIAN_POINT ( 'NONE',  ( 6.000000000000001776, 297.5000000000000000, -7.347880794884121708E-16 ) ) ;
#54794=CARTESIAN_POINT ( 'NONE',  ( -9.832129032723420536, 3.697916663252683200, 5.676582343749997150 ) ) ;
#54804=CARTESIAN_POINT ( 'NONE',  ( 9.832129032723420536, 121.1979166632526983, -5.676582343749999815 ) ) ;
#54805=CARTESIAN_POINT ( 'NONE',  ( -2.679491924311225848, 83.33333332650536818, -10.00000000000000178 ) ) ;
#54809=CARTESIAN_POINT ( 'NONE',  ( 6.123233995736767268E-16, 103.1249999931720396, -10.00000000000000178 ) ) ;
#54810=EDGE_LOOP ( 'NONE', ( #51351, #23617, #72232, #68155 ) ) ;
#54814=CARTESIAN_POINT ( 'NONE',  ( 6.676582343750004256, 294.0468750017070079, 2.765530957081995478 ) ) ;
#54815=CARTESIAN_POINT ( 'NONE',  ( 2.679491924311376394, 187.9166666598386541, -9.999999999999914735 ) ) ;
#54817=CARTESIAN_POINT ( 'NONE',  ( -9.832129032723420536, 163.6979166632526983, 5.676582343749997150 ) ) ;
#54826=CARTESIAN_POINT ( 'NONE',  ( 6.951808397369818766E-16, 157.3437499965860127, -11.35316468750000141 ) ) ;
#54827=CARTESIAN_POINT ( 'NONE',  ( -10.00000000000000533, 217.5000000000000284, -1.224646799147354045E-15 ) ) ;
#54830=CARTESIAN_POINT ( 'NONE',  ( 9.832129032723420536, 56.51041666325268409, -5.676582343749999815 ) ) ;
#54835=VERTEX_POINT ( 'NONE', #22752 ) ;
#54837=CARTESIAN_POINT ( 'NONE',  ( -2.485281374238571761, 288.8750000034140157, -6.000000000000003553 ) ) ;
#54858=CARTESIAN_POINT ( 'NONE',  ( -1.836970198721029983E-15, 63.75000000000000000, 10.00000000000000178 ) ) ;
#54860=CARTESIAN_POINT ( 'NONE',  ( 6.000000000000003553, 295.4374999999999432, 2.485281374238571317 ) ) ;
#54864=ORIENTED_EDGE ( 'NONE', *, *, #40263, .F. ) ;
#54865=EDGE_CURVE ( 'NONE', #44090, #54774, #64487, .T. ) ;
#54875=CARTESIAN_POINT ( 'NONE',  ( -7.320508075688773708, 186.8750000000000000, -7.320508075688774596 ) ) ;
#54878=CARTESIAN_POINT ( 'NONE',  ( 5.676582343749993598, 160.2604166632526983, 9.832129032723422313 ) ) ;
#54884=CARTESIAN_POINT ( 'NONE',  ( -2.485281374238172081, 297.2500000034139589, 6.000000000000400568 ) ) ;
#54885=ORIENTED_EDGE ( 'NONE', *, *, #2490, .F. ) ;
#54886=CARTESIAN_POINT ( 'NONE',  ( 3.042071309553159519, 15.05208332991935194, 11.35316468750000141 ) ) ;
#54888=CARTESIAN_POINT ( 'NONE',  ( 10.00000000000000178, 32.08333332650535397, -2.679491924311226736 ) ) ;
#54890=CARTESIAN_POINT ( 'NONE',  ( -7.320508075688773708, 48.74999999317203248, -7.320508075688774596 ) ) ;
#54893=CARTESIAN_POINT ( 'NONE',  ( 7.320508075688779925, 219.3750000000000000, 7.320508075688784366 ) ) ;
#54895=FACE_OUTER_BOUND ( 'NONE', #12936, .T. ) ;
#54898=( BOUNDED_CURVE ( )  B_SPLINE_CURVE ( 2, ( #48998, #8271, #38077, #72008, #15409, #3740, #25239, #37703, #19582, #60322, #36949, #72777, #54685 ),
 .UNSPECIFIED., .F., .F. ) 
 B_SPLINE_CURVE_WITH_KNOTS ( ( 3, 2, 2, 2, 2, 2, 3 ),
 ( 0.7010869565217391353, 0.7028985507246376940, 0.7047101449275362528, 0.7065217391304348116, 0.7083333333333332593, 0.7101449275362318181, 0.7119565217391303769 ),
 .UNSPECIFIED. ) 
 CURVE ( )  GEOMETRIC_REPRESENTATION_ITEM ( )  RATIONAL_B_SPLINE_CURVE ( ( 1.000000000000000000, 0.9659258262890683122, 1.000000000000000000, 0.9659258262890683122, 1.000000000000000000, 0.9659258262890683122, 1.000000000000000000, 0.9659258262890683122, 1.000000000000000000, 0.9659258262890683122, 1.000000000000000000, 0.9659258262890704216, 0.9999999999999978906 ) ) 
 REPRESENTATION_ITEM ( '' )  );
#54903=CARTESIAN_POINT ( 'NONE',  ( 11.35316468750000141, 130.7812499965860127, 0.000000000000000000 ) ) ;
#54911=CARTESIAN_POINT ( 'NONE',  ( 6.951808397369818766E-16, 127.0312499965860269, -11.35316468750000141 ) ) ;
#54917=CARTESIAN_POINT ( 'NONE',  ( -5.676582343749998039, 117.7604166632526841, -9.832129032723420536 ) ) ;
#54921=CARTESIAN_POINT ( 'NONE',  ( 11.35316468749999785, 20.88541666325268764, 3.042071309553174174 ) ) ;
#54923=ORIENTED_EDGE ( 'NONE', *, *, #49305, .T. ) ;
#54924=CARTESIAN_POINT ( 'NONE',  ( 0.000000000000000000, 300.0000000000000000, 0.000000000000000000 ) ) ;
#54927=DIRECTION ( 'NONE',  ( 0.000000000000000000, 0.000000000000000000, 1.000000000000000000 ) ) ;
#54929=CARTESIAN_POINT ( 'NONE',  ( -4.721056650415999201, 289.3281250017069510, -4.721056650415999201 ) ) ;
#54932=CARTESIAN_POINT ( 'NONE',  ( -8.311093377946841443, 219.2187499965860127, 8.311093377946834337 ) ) ;
#54934=CARTESIAN_POINT ( 'NONE',  ( -3.042071309553173730, 144.6354166632526983, 11.35316468749999785 ) ) ;
#54950=CARTESIAN_POINT ( 'NONE',  ( 6.951808397369818766E-16, 192.0312499965860127, -11.35316468750000141 ) ) ;
#54953=CARTESIAN_POINT ( 'NONE',  ( -6.676582343749999815, 291.5156250017069510, 2.765530957082001251 ) ) ;
#54955=CARTESIAN_POINT ( 'NONE',  ( 9.999999999999994671, 94.79166666666667140, 2.679491924311234730 ) ) ;
#54967=CARTESIAN_POINT ( 'NONE',  ( -5.676582343750006032, 119.4270833299193555, 9.832129032723418760 ) ) ;
#54977=CARTESIAN_POINT ( 'NONE',  ( -27.31189167431821119, 229.0752414545900990, -20.81150119242884600 ) ) ;
#54982=CARTESIAN_POINT ( 'NONE',  ( -9.832129032723420536, 199.0104166632526983, 5.676582343749997150 ) ) ;
#54984=CYLINDRICAL_SURFACE ( 'NONE', #27774, 10.00000000000000178 ) ;
#54988=LINE ( 'NONE', #3295, #47170 ) ;
#54989=CARTESIAN_POINT ( 'NONE',  ( 6.951808397369818766E-16, 82.03124999658602690, -11.35316468750000141 ) ) ;
#54994=CARTESIAN_POINT ( 'NONE',  ( 5.000000000000073719, 39.16666666666676377, 8.660254037844529407 ) ) ;
#54996=CARTESIAN_POINT ( 'NONE',  ( -3.042071309553164404, 87.23958332991934128, -11.35316468749999963 ) ) ;
#55000=CARTESIAN_POINT ( 'NONE',  ( 6.123233995736767268E-16, 21.25000000000000000, -10.00000000000000178 ) ) ;
#55004=CARTESIAN_POINT ( 'NONE',  ( 11.35316468749999785, 80.57291666325268409, 3.042071309553174174 ) ) ;
#55005=EDGE_CURVE ( 'NONE', #17320, #73073, #46200, .T. ) ;
#55008=CARTESIAN_POINT ( 'NONE',  ( -2.679491924311225848, 173.3333333265053398, -10.00000000000000178 ) ) ;
#55010=CARTESIAN_POINT ( 'NONE',  ( 8.311093377946834337, 65.46874999658601268, 8.311093377946839666 ) ) ;
#55011=CARTESIAN_POINT ( 'NONE',  ( -2.765530957081998586, 294.6406250017069510, 6.676582343750001591 ) ) ;
#55013=CARTESIAN_POINT ( 'NONE',  ( -8.311093377946836114, 202.6562499965860127, -8.311093377946837890 ) ) ;
#55018=CARTESIAN_POINT ( 'NONE',  ( -8.311093377946841443, 193.9062499965860411, 8.311093377946834337 ) ) ;
#55023=CARTESIAN_POINT ( 'NONE',  ( 8.311093377946837890, 176.7187499965860127, -8.311093377946837890 ) ) ;
#55030=CARTESIAN_POINT ( 'NONE',  ( 2.679491924311222739, 3.958333333333333925, 10.00000000000000355 ) ) ;
#55031=( BOUNDED_CURVE ( )  B_SPLINE_CURVE ( 2, ( #40195, #56074, #5501, #16052, #61721, #28126, #44743, #33439, #10779, #27751, #68124, #56813, #22833 ),
 .UNSPECIFIED., .F., .F. ) 
 B_SPLINE_CURVE_WITH_KNOTS ( ( 3, 2, 2, 2, 2, 2, 3 ),
 ( 0.4238920256284931520, 0.4291260266837255144, 0.4343600277389579878, 0.4395940287941904057, 0.4448280298494227680, 0.4500620309046552414, 0.4552960319598876593 ),
 .UNSPECIFIED. ) 
 CURVE ( )  GEOMETRIC_REPRESENTATION_ITEM ( )  RATIONAL_B_SPLINE_CURVE ( ( 0.9999999999999984457, 0.9659258262890697555, 1.000000000000000000, 0.9659258262890682012, 1.000000000000000000, 0.9659258262890682012, 1.000000000000000000, 0.9659258262890682012, 1.000000000000000000, 0.9659258262890682012, 1.000000000000000000, 0.9659258262890900726, 0.9999999999999781286 ) ) 
 REPRESENTATION_ITEM ( '' )  );
#55050=CARTESIAN_POINT ( 'NONE',  ( 9.832129032723416984, 75.67708332991934128, 5.676582343750006032 ) ) ;
#55055=CARTESIAN_POINT ( 'NONE',  ( 6.676582343750001591, 293.1093750017069510, -8.176455196517173205E-16 ) ) ;
#55059=CARTESIAN_POINT ( 'NONE',  ( 7.347880794884121708E-16, 300.0000000000000000, -6.000000000000001776 ) ) ;
#55072=CARTESIAN_POINT ( 'NONE',  ( -9.832129032723420536, 38.69791666325269119, 5.676582343749997150 ) ) ;
#55073=CARTESIAN_POINT ( 'NONE',  ( -1.967015505459129087E-11, 148.7499999999984936, 10.00000000000000533 ) ) ;
#55074=CARTESIAN_POINT ( 'NONE',  ( 10.00000000000000178, 11.87499999317203248, 0.000000000000000000 ) ) ;
#55077=VECTOR ( 'NONE', #2733, 1000.000000000000000 ) ;
#55078=CARTESIAN_POINT ( 'NONE',  ( 2.679491924311081963, 142.9166666598387110, -10.00000000000008349 ) ) ;
#55080=CARTESIAN_POINT ( 'NONE',  ( 11.35316468749999963, 50.98958332991934839, -3.042071309553165293 ) ) ;
#55087=CARTESIAN_POINT ( 'NONE',  ( -11.35316468750000141, 28.28124999658601624, -1.390361679473963753E-15 ) ) ;
#55088=ADVANCED_FACE ( 'NONE', ( #45335 ), #68718, .T. ) ;
#55090=CARTESIAN_POINT ( 'NONE',  ( -7.320508075688773708, 48.74999999317203248, -7.320508075688774596 ) ) ;
#55091=CARTESIAN_POINT ( 'NONE',  ( 8.311093377946837890, 166.4062499965860127, -8.311093377946837890 ) ) ;
#55093=CARTESIAN_POINT ( 'NONE',  ( -5.000000000000005329, 125.2083333265053540, 8.660254037844387298 ) ) ;
#55097=CARTESIAN_POINT ( 'NONE',  ( 5.676582343750001591, 16.92708332991935194, -9.832129032723420536 ) ) ;
#55102=CARTESIAN_POINT ( 'NONE',  ( 8.311093377946837890, 156.4062499965860411, -8.311093377946837890 ) ) ;
#55111=EDGE_CURVE ( 'NONE', #61723, #9076, #40918, .T. ) ;
#55113=CARTESIAN_POINT ( 'NONE',  ( -6.000000000000001776, 292.0625000034140157, 0.000000000000000000 ) ) ;
#55114=CARTESIAN_POINT ( 'NONE',  ( -8.311093377946836114, 97.96874999658599847, -8.311093377946837890 ) ) ;
#55131=ADVANCED_FACE ( 'NONE', ( #44974 ), #12117, .T. ) ;
#55135=CARTESIAN_POINT ( 'NONE',  ( 4.721056650415999201, 299.0781250017069510, -4.721056650415999201 ) ) ;
#55145=DIRECTION ( 'NONE',  ( -0.000000000000000000, 1.000000000000000000, -0.000000000000000000 ) ) ;
#55146=CARTESIAN_POINT ( 'NONE',  ( 10.00000000000000000, 104.7916666666666572, 2.679491924311236062 ) ) ;
#55148=CARTESIAN_POINT ( 'NONE',  ( -6.676582343750003368, 291.5468750017069510, -2.765530957081996810 ) ) ;
#55155=CARTESIAN_POINT ( 'NONE',  ( -10.00000000000000355, 184.5833333265053113, 2.679491924311223183 ) ) ;
#55162=CARTESIAN_POINT ( 'NONE',  ( 7.320508075688771044, 224.3749999999999716, 7.320508075688775484 ) ) ;
#55164=CARTESIAN_POINT ( 'NONE',  ( -8.311093377946836114, 192.9687499965859843, -8.311093377946837890 ) ) ;
#55165=CARTESIAN_POINT ( 'NONE',  ( 7.320508075688774596, 192.4999999931720538, -7.320508075688774596 ) ) ;
#55173=CARTESIAN_POINT ( 'NONE',  ( -9.832129032723418760, 2.864583329919349719, -5.676582343750004256 ) ) ;
#55181=CARTESIAN_POINT ( 'NONE',  ( 9.832129032723420536, 126.1979166632526983, -5.676582343749999815 ) ) ;
#55182=EDGE_CURVE ( 'NONE', #9475, #32512, #56334, .T. ) ;
#55183=CARTESIAN_POINT ( 'NONE',  ( 8.660254037844385522, 86.45833332650538239, 5.000000000000005329 ) ) ;
#55187=CARTESIAN_POINT ( 'NONE',  ( -4.999999999999998224, 38.54166665983869677, -8.660254037844389075 ) ) ;
#55190=CARTESIAN_POINT ( 'NONE',  ( 6.676582343750001591, 292.1093750017069510, -8.176455196517173205E-16 ) ) ;
#55193=CARTESIAN_POINT ( 'NONE',  ( -3.042071309553164404, 167.2395833299193839, -11.35316468749999963 ) ) ;
#55195=CARTESIAN_POINT ( 'NONE',  ( -8.660254037844390851, 204.7916666598387110, 4.999999999999998224 ) ) ;
#55197=CIRCLE ( 'NONE', #3366, 6.000000000000001776 ) ;
#55201=CARTESIAN_POINT ( 'NONE',  ( -3.042071309553173730, 149.6354166632526983, 11.35316468749999785 ) ) ;
#55205=CARTESIAN_POINT ( 'NONE',  ( 11.35316468749999785, 65.88541666325268409, 3.042071309553174174 ) ) ;
#55209=ORIENTED_EDGE ( 'NONE', *, *, #7927, .T. ) ;
#55211=CARTESIAN_POINT ( 'NONE',  ( -6.000000000000000888, 289.1250000034140726, 2.485281374238575758 ) ) ;
#55223=ADVANCED_FACE ( 'NONE', ( #35883 ), #70938, .T. ) ;
#55227=CARTESIAN_POINT ( 'NONE',  ( -5.999999999999999112, 290.0625000000000000, 2.485281374238575314 ) ) ;
#55236=CARTESIAN_POINT ( 'NONE',  ( -10.00000000000000355, 62.70833333333333570, 2.679491924311223183 ) ) ;
#55238=CARTESIAN_POINT ( 'NONE',  ( -6.000000000000003553, 292.9374999999999432, -2.485281374238571317 ) ) ;
#55240=DIRECTION ( 'NONE',  ( -0.000000000000000000, 1.000000000000000000, -0.000000000000000000 ) ) ;
#55242=( BOUNDED_CURVE ( )  B_SPLINE_CURVE ( 2, ( #9035, #9413, #13920, #36959, #49010, #8283, #32431, #31292, #37335, #54323, #8661, #31676, #3004 ),
 .UNSPECIFIED., .F., .F. ) 
 B_SPLINE_CURVE_WITH_KNOTS ( ( 3, 2, 2, 2, 2, 2, 3 ),
 ( 1.679891585307146773, 1.685124540478250443, 1.690357495649354114, 1.695590450820457784, 1.700823405991561010, 1.706056361162664681, 1.711289316333768351 ),
 .UNSPECIFIED. ) 
 CURVE ( )  GEOMETRIC_REPRESENTATION_ITEM ( )  RATIONAL_B_SPLINE_CURVE ( ( 1.000000000000037526, 0.9659258262890306757, 1.000000000000000000, 0.9659258262890683122, 1.000000000000000000, 0.9659258262890683122, 1.000000000000000000, 0.9659258262890683122, 1.000000000000000000, 0.9659258262890683122, 1.000000000000000000, 0.9659258262890704216, 0.9999999999999978906 ) ) 
 REPRESENTATION_ITEM ( '' )  );
#55249=LINE ( 'NONE', #25796, #31905 ) ;
#55250=CARTESIAN_POINT ( 'NONE',  ( -4.999999999999998224, 186.6666666666666856, -8.660254037844389075 ) ) ;
#55253=CARTESIAN_POINT ( 'NONE',  ( -3.042071309553164404, 152.5520833299193271, -11.35316468749999963 ) ) ;
#55260=VERTEX_POINT ( 'NONE', #6835 ) ;
#55262=CARTESIAN_POINT ( 'NONE',  ( 6.951808397369818766E-16, 22.34374999658601979, -11.35316468750000141 ) ) ;
#55263=CARTESIAN_POINT ( 'NONE',  ( 7.320508075688771044, 96.24999999317202537, 7.320508075688775484 ) ) ;
#55269=CARTESIAN_POINT ( 'NONE',  ( -7.320508075688778149, 49.99999999317202537, 7.320508075688769267 ) ) ;
#55272=CARTESIAN_POINT ( 'NONE',  ( 7.320508075688761274, 100.6249999999999716, -7.320508075688761274 ) ) ;
#55278=CARTESIAN_POINT ( 'NONE',  ( -10.00000000000000178, 222.5000000000000000, -1.224646799147353256E-15 ) ) ;
#55281=CARTESIAN_POINT ( 'NONE',  ( -11.35316468750000141, 123.4895833299193555, 3.042071309553159963 ) ) ;
#55288=CARTESIAN_POINT ( 'NONE',  ( -11.35316468750000141, 123.2812499965860269, -1.390361679473963753E-15 ) ) ;
#55292=CARTESIAN_POINT ( 'NONE',  ( -9.832129032723418760, 118.1770833299193555, -5.676582343750004256 ) ) ;
#55296=CARTESIAN_POINT ( 'NONE',  ( 6.951808397369818766E-16, 22.34374999658601979, -11.35316468750000141 ) ) ;
#55302=CARTESIAN_POINT ( 'NONE',  ( -6.676582343750001591, 287.4531250017069510, 0.000000000000000000 ) ) ;
#55304=CYLINDRICAL_SURFACE ( 'NONE', #26776, 10.00000000000000178 ) ;
#55307=CARTESIAN_POINT ( 'NONE',  ( 6.951808397369818766E-16, 147.3437499965860411, -11.35316468750000141 ) ) ;
#55319=CARTESIAN_POINT ( 'NONE',  ( -2.249999999999998224, 283.9999999998748308, 5.427273999917394676 ) ) ;
#55324=DIRECTION ( 'NONE',  ( 0.000000000000000000, 0.000000000000000000, 1.000000000000000000 ) ) ;
#55325=CARTESIAN_POINT ( 'NONE',  ( -5.676582343749998039, 192.4479166632526983, -9.832129032723420536 ) ) ;
#55327=CARTESIAN_POINT ( 'NONE',  ( -2.485281374238227592, 291.2500000034139589, 6.000000000000345501 ) ) ;
#55330=CARTESIAN_POINT ( 'NONE',  ( -8.660254037844389075, 67.08333333333335702, -5.000000000000006217 ) ) ;
#55342=CARTESIAN_POINT ( 'NONE',  ( 11.35316468749999785, 110.8854166632526699, 3.042071309553174174 ) ) ;
#55350=CARTESIAN_POINT ( 'NONE',  ( -11.35316468750000141, 223.4895833299193555, 3.042071309553159963 ) ) ;
#55354=CARTESIAN_POINT ( 'NONE',  ( 11.35316468749999785, 210.8854166632526983, 3.042071309553174174 ) ) ;
#55356=CARTESIAN_POINT ( 'NONE',  ( 7.600546564020412177, 225.9999999999997726, 7.213721669030190853 ) ) ;
#55361=CARTESIAN_POINT ( 'NONE',  ( -5.676582343750006032, 79.11458332991935549, 9.832129032723418760 ) ) ;
#55368=CARTESIAN_POINT ( 'NONE',  ( -5.676582343749998039, 87.44791666325268409, -9.832129032723420536 ) ) ;
#55376=CARTESIAN_POINT ( 'NONE',  ( -8.311093377946836114, 87.65624999658601268, -8.311093377946837890 ) ) ;
#55380=CARTESIAN_POINT ( 'NONE',  ( 2.679491924311222739, 185.8333333265053398, 10.00000000000000355 ) ) ;
#55382=CARTESIAN_POINT ( 'NONE',  ( -1.836970198721029983E-15, 95.62499999317203958, 10.00000000000000178 ) ) ;
#55383=CARTESIAN_POINT ( 'NONE',  ( -11.35316468750000141, 73.59374999658602690, -1.390361679473963753E-15 ) ) ;
#55384=CARTESIAN_POINT ( 'NONE',  ( -4.721056650415999201, 292.3281250017069510, -4.721056650415999201 ) ) ;
#55386=CARTESIAN_POINT ( 'NONE',  ( 9.832129032723420536, 211.1979166632526983, -5.676582343749999815 ) ) ;
#55387=ORIENTED_EDGE ( 'NONE', *, *, #8639, .F. ) ;
#55392=CARTESIAN_POINT ( 'NONE',  ( 8.311093377946834337, 210.1562499965860127, 8.311093377946839666 ) ) ;
#55395=CARTESIAN_POINT ( 'NONE',  ( -6.676582343750001591, 299.4531250017069510, 0.000000000000000000 ) ) ;
#55396=VERTEX_POINT ( 'NONE', #30581 ) ;
#55397=CARTESIAN_POINT ( 'NONE',  ( 11.35316468749999963, 201.3020833299193555, -3.042071309553165293 ) ) ;
#55404=CARTESIAN_POINT ( 'NONE',  ( -8.660254037844390851, 12.91666666666666785, 4.999999999999998224 ) ) ;
#55417=DIRECTION ( 'NONE',  ( 1.000000000000000000, 0.000000000000000000, -0.000000000000000000 ) ) ;
#55424=CARTESIAN_POINT ( 'NONE',  ( -11.35316468750000141, 73.59374999658602690, -1.390361679473963753E-15 ) ) ;
#55429=CARTESIAN_POINT ( 'NONE',  ( 6.676582343750003368, 291.0468750017070079, 2.765530957081995478 ) ) ;
#55431=CARTESIAN_POINT ( 'NONE',  ( 0.000000000000000000, 300.0000000000000000, 6.000000000000001776 ) ) ;
#55440=CARTESIAN_POINT ( 'NONE',  ( -2.679491924311226292, 18.33333332650536818, -10.00000000000000178 ) ) ;
#55446=CARTESIAN_POINT ( 'NONE',  ( 11.35316468749999963, 40.98958332991935549, -3.042071309553165293 ) ) ;
#55448=CARTESIAN_POINT ( 'NONE',  ( 2.679491924311228956, 17.91666665983870033, -10.00000000000000000 ) ) ;
#55452=CARTESIAN_POINT ( 'NONE',  ( 8.311093377946834337, 45.15624999658601268, 8.311093377946839666 ) ) ;
#55458=CARTESIAN_POINT ( 'NONE',  ( 11.35316468750000141, 50.78124999658601268, 0.000000000000000000 ) ) ;
#55462=CARTESIAN_POINT ( 'NONE',  ( -2.085542519210945728E-15, 164.5312499965860127, 11.35316468750000141 ) ) ;
#55464=CARTESIAN_POINT ( 'NONE',  ( 10.00000000000000178, 126.8749999931720396, 0.000000000000000000 ) ) ;
#55466=CARTESIAN_POINT ( 'NONE',  ( 11.35316468749999785, 35.88541666325268409, 3.042071309553174174 ) ) ;
#55468=VERTEX_POINT ( 'NONE', #41533 ) ;
#55472=CARTESIAN_POINT ( 'NONE',  ( 6.951808397369818766E-16, 162.0312499965860127, -11.35316468750000141 ) ) ;
#55476=EDGE_CURVE ( 'NONE', #61626, #12433, #13580, .T. ) ;
#55481=ORIENTED_EDGE ( 'NONE', *, *, #19554, .F. ) ;
#55484=CARTESIAN_POINT ( 'NONE',  ( 5.676582343750001591, 106.9270833299193413, -9.832129032723420536 ) ) ;
#55505=ADVANCED_FACE ( 'NONE', ( #50651 ), #45008, .T. ) ;
#55513=ORIENTED_EDGE ( 'NONE', *, *, #55111, .F. ) ;
#55515=CARTESIAN_POINT ( 'NONE',  ( 6.000000000000003553, 288.5625000000000000, -2.485281374238571761 ) ) ;
#55520=CARTESIAN_POINT ( 'NONE',  ( 10.00000000000000000, 109.7916666666666572, 2.679491924311236062 ) ) ;
#55523=CARTESIAN_POINT ( 'NONE',  ( 4.721056650416000089, 291.9843750017070079, 4.721056650415999201 ) ) ;
#55537=CARTESIAN_POINT ( 'NONE',  ( -4.999999999999998224, 93.54166665983871098, -8.660254037844389075 ) ) ;
#55538=CARTESIAN_POINT ( 'NONE',  ( 5.000000000000001776, 225.8333333333333712, -8.660254037844389075 ) ) ;
#55540=CARTESIAN_POINT ( 'NONE',  ( 11.35316468749999785, 190.8854166632526983, 3.042071309553174174 ) ) ;
#55541=CARTESIAN_POINT ( 'NONE',  ( -10.00000000000000178, 134.3749999931720254, -1.224646799147353454E-15 ) ) ;
#55547=CARTESIAN_POINT ( 'NONE',  ( -9.832129032723418760, 7.864583329919350163, -5.676582343750004256 ) ) ;
#55551=CARTESIAN_POINT ( 'NONE',  ( 0.000000000000000000, 300.0000000000000000, 0.000000000000000000 ) ) ;
#55553=CARTESIAN_POINT ( 'NONE',  ( -9.832129032723418760, 2.864583329919349719, -5.676582343750004256 ) ) ;
#55555=CARTESIAN_POINT ( 'NONE',  ( -5.676582343750006032, 119.1145833299193697, 9.832129032723418760 ) ) ;
#55556=CARTESIAN_POINT ( 'NONE',  ( -1.836970198721029983E-15, 85.62499999317203958, 10.00000000000000178 ) ) ;
#55562=CARTESIAN_POINT ( 'NONE',  ( 3.153939666463620179E-13, 118.7500000000000426, 9.999999999999998224 ) ) ;
#55563=CARTESIAN_POINT ( 'NONE',  ( -4.088227598258586603E-16, 290.3593750017070079, -6.676582343750001591 ) ) ;
#55567=CARTESIAN_POINT ( 'NONE',  ( -8.660254037844387298, 208.9583333265053682, -5.000000000000004441 ) ) ;
#55572=CARTESIAN_POINT ( 'NONE',  ( -5.676582343750006032, 149.4270833299193555, 9.832129032723418760 ) ) ;
#55575=CARTESIAN_POINT ( 'NONE',  ( -3.042071309553164404, 67.55208332991935549, -11.35316468749999963 ) ) ;
#55582=CARTESIAN_POINT ( 'NONE',  ( -4.242640687119286547, 289.9375000034140157, -4.242640687119286547 ) ) ;
#55588=EDGE_CURVE ( 'NONE', #19469, #271, #68751, .T. ) ;
#55599=CARTESIAN_POINT ( 'NONE',  ( -3.673940397442060854E-16, 289.7500000000000000, -6.000000000000001776 ) ) ;
#55609=CARTESIAN_POINT ( 'NONE',  ( 4.999999999999993783, 69.16666666666667140, 8.660254037844390851 ) ) ;
#55612=CARTESIAN_POINT ( 'NONE',  ( -3.673940397442060854E-16, 292.7500000000000000, -6.000000000000001776 ) ) ;
#55613=CARTESIAN_POINT ( 'NONE',  ( 0.000000000000000000, 300.0000000000000000, 10.00000000000000178 ) ) ;
#55623=CARTESIAN_POINT ( 'NONE',  ( -5.000000000000005329, 193.3333333333333712, 8.660254037844387298 ) ) ;
#55626=CARTESIAN_POINT ( 'NONE',  ( 3.042071309553159519, 160.0520833299193555, 11.35316468750000141 ) ) ;
#55629=CARTESIAN_POINT ( 'NONE',  ( 2.679491924336306674, 156.0416666666645540, -9.999999999985730526 ) ) ;
#55630=CARTESIAN_POINT ( 'NONE',  ( -10.00000000000000178, 84.37499999317203958, -1.224646799147353454E-15 ) ) ;
#55633=CARTESIAN_POINT ( 'NONE',  ( -11.35316468750000141, 18.80208332991934839, 3.042071309553159963 ) ) ;
#55640=CARTESIAN_POINT ( 'NONE',  ( 8.660254037844385522, 46.45833332650536818, 5.000000000000005329 ) ) ;
#55644=CARTESIAN_POINT ( 'NONE',  ( 10.00000000000001421, 220.0000000000000000, 0.000000000000000000 ) ) ;
#55655=CARTESIAN_POINT ( 'NONE',  ( -5.676582343749998039, 122.4479166632526983, -9.832129032723420536 ) ) ;
#55661=CARTESIAN_POINT ( 'NONE',  ( 11.35316468750000141, 130.7812499965860127, 0.000000000000000000 ) ) ;
#55665=LINE ( 'NONE', #20934, #58808 ) ;
#55667=CARTESIAN_POINT ( 'NONE',  ( 8.311093377946834337, 120.4687499965860269, 8.311093377946839666 ) ) ;
#55671=EDGE_CURVE ( 'NONE', #7527, #1761, #41204, .T. ) ;
#55672=CARTESIAN_POINT ( 'NONE',  ( 8.311093377946834337, 25.46874999658601624, 8.311093377946839666 ) ) ;
#55680=CARTESIAN_POINT ( 'NONE',  ( 4.721056650415999201, 290.0781250017069510, -4.721056650415999201 ) ) ;
#55684=CARTESIAN_POINT ( 'NONE',  ( -8.311093377946836114, 147.9687499965860411, -8.311093377946837890 ) ) ;
#55696=EDGE_LOOP ( 'NONE', ( #6636, #38428, #41491, #36427 ) ) ;
#55698=CARTESIAN_POINT ( 'NONE',  ( -6.362988438888832046E-13, 88.74999999999995737, 9.999999999999998224 ) ) ;
#55700=CARTESIAN_POINT ( 'NONE',  ( -11.35316468749999785, 183.0729166632526983, -3.042071309553167513 ) ) ;
#55703=CARTESIAN_POINT ( 'NONE',  ( 2.765530957081996366, 288.1406250017070647, -6.676582343750002480 ) ) ;
#55704=CARTESIAN_POINT ( 'NONE',  ( 2.679491924311228956, 132.9166666598386826, -10.00000000000000000 ) ) ;
#55705=CARTESIAN_POINT ( 'NONE',  ( 7.320508075688769267, 95.62499999999998579, -7.320508075688769267 ) ) ;
#55717=CARTESIAN_POINT ( 'NONE',  ( -3.042071309553164404, 112.5520833299193413, -11.35316468749999963 ) ) ;
#55723=ORIENTED_EDGE ( 'NONE', *, *, #49379, .F. ) ;
#55728=CARTESIAN_POINT ( 'NONE',  ( -11.35316468750000141, 213.8020833299193839, 3.042071309553159963 ) ) ;
#55736=CARTESIAN_POINT ( 'NONE',  ( -5.676582343750006032, 89.11458332991935549, 9.832129032723418760 ) ) ;
#55742=CARTESIAN_POINT ( 'NONE',  ( -3.042071309553173730, 94.32291666325266988, 11.35316468749999785 ) ) ;
#55746=CARTESIAN_POINT ( 'NONE',  ( 0.000000000000000000, 300.0000000000000000, 10.00000000000000178 ) ) ;
#55750=CARTESIAN_POINT ( 'NONE',  ( 5.676582343749993598, 89.94791666325269830, 9.832129032723422313 ) ) ;
#55755=CARTESIAN_POINT ( 'NONE',  ( -1.836970198721029983E-15, 185.6249999931720538, 10.00000000000000178 ) ) ;
#55757=CARTESIAN_POINT ( 'NONE',  ( -9.832129032723418760, 78.17708332991935549, -5.676582343750004256 ) ) ;
#55758=CARTESIAN_POINT ( 'NONE',  ( -4.088227598258586603E-16, 295.2031250017069510, -6.676582343750001591 ) ) ;
#55761=CARTESIAN_POINT ( 'NONE',  ( 11.35316468749999963, 210.9895833299193839, -3.042071309553165293 ) ) ;
#55766=CARTESIAN_POINT ( 'NONE',  ( -5.676582343749998039, 202.4479166632526983, -9.832129032723420536 ) ) ;
#55770=CARTESIAN_POINT ( 'NONE',  ( -11.35316468749999785, 198.3854166632526699, -3.042071309553167957 ) ) ;
#55777=CARTESIAN_POINT ( 'NONE',  ( -10.00000000000000178, 17.50000000000000000, -1.224646799147353454E-15 ) ) ;
#55799=CARTESIAN_POINT ( 'NONE',  ( 8.311093377946837890, 71.71874999658601268, -8.311093377946837890 ) ) ;
#55804=CARTESIAN_POINT ( 'NONE',  ( -6.676582343749999815, 288.6718750017069510, 2.765530957082001251 ) ) ;
#55811=VERTEX_POINT ( 'NONE', #57272 ) ;
#55814=CARTESIAN_POINT ( 'NONE',  ( 11.35316468749999963, 166.3020833299193271, -3.042071309553165293 ) ) ;
#55822=CARTESIAN_POINT ( 'NONE',  ( -11.35316468750000141, 53.28124999658602690, -1.390361679473963753E-15 ) ) ;
#55824=CARTESIAN_POINT ( 'NONE',  ( 10.00000000000000178, 26.87499999317203603, 0.000000000000000000 ) ) ;
#55825=CARTESIAN_POINT ( 'NONE',  ( 6.123233995736767268E-16, 91.25000000000001421, -10.00000000000000178 ) ) ;
#55827=CARTESIAN_POINT ( 'NONE',  ( 0.000000000000000000, 300.0000000000000000, 10.00000000000000178 ) ) ;
#55831=CARTESIAN_POINT ( 'NONE',  ( -2.085542519210945728E-15, 49.53124999658601268, 11.35316468750000141 ) ) ;
#55834=CYLINDRICAL_SURFACE ( 'NONE', #13060, 10.00000000000000178 ) ;
#55837=CARTESIAN_POINT ( 'NONE',  ( -11.35316468750000141, 43.48958332991934839, 3.042071309553159963 ) ) ;
#55840=CARTESIAN_POINT ( 'NONE',  ( 8.311093377946837890, 161.4062499965860411, -8.311093377946837890 ) ) ;
#55841=CARTESIAN_POINT ( 'NONE',  ( 5.000000000000001776, 142.7083333265053682, -8.660254037844389075 ) ) ;
#55843=CARTESIAN_POINT ( 'NONE',  ( 0.000000000000000000, 300.0000000000000000, 0.000000000000000000 ) ) ;
#55844=CARTESIAN_POINT ( 'NONE',  ( 3.042071309553159519, 40.05208332991935549, 11.35316468750000141 ) ) ;
#55846=CARTESIAN_POINT ( 'NONE',  ( -2.679491924311308448, 80.41666665983868256, 9.999999999999957367 ) ) ;
#55847=EDGE_LOOP ( 'NONE', ( #73892, #67256, #33340, #45589 ) ) ;
#55851=CARTESIAN_POINT ( 'NONE',  ( -1.836970198721029983E-15, 90.62499999317203958, 10.00000000000000178 ) ) ;
#55852=CARTESIAN_POINT ( 'NONE',  ( 6.951808397369818766E-16, 167.0312499965860411, -11.35316468750000141 ) ) ;
#55854=CARTESIAN_POINT ( 'NONE',  ( 2.250000000000000444, 278.3999999999996930, 5.425975448606632945 ) ) ;
#55857=EDGE_CURVE ( 'NONE', #10942, #12530, #35741, .T. ) ;
#55859=VERTEX_POINT ( 'NONE', #74234 ) ;
#55862=CARTESIAN_POINT ( 'NONE',  ( -3.042071309553164404, 112.5520833299193413, -11.35316468749999963 ) ) ;
#55863=CARTESIAN_POINT ( 'NONE',  ( 8.660254037844390851, 14.58333333333333925, 5.000000000000009770 ) ) ;
#55891=LINE ( 'NONE', #4205, #38606 ) ;
#55892=CARTESIAN_POINT ( 'NONE',  ( 2.679491924311222739, 118.9583333333333428, 10.00000000000000355 ) ) ;
#55895=CARTESIAN_POINT ( 'NONE',  ( -6.676582343750003368, 290.5468750017071216, -2.765530957081996810 ) ) ;
#55910=CARTESIAN_POINT ( 'NONE',  ( -10.00000000000000355, 214.5833333265053682, 2.679491924311223183 ) ) ;
#55911=CARTESIAN_POINT ( 'NONE',  ( -5.000000000000005329, 223.3333333333333428, 8.660254037844387298 ) ) ;
#55912=CARTESIAN_POINT ( 'NONE',  ( 10.00000000000000000, 0.2083333333333323989, -2.679491924311226736 ) ) ;
#55913=CARTESIAN_POINT ( 'NONE',  ( -9.832129032723418760, 213.1770833299193555, -5.676582343750004256 ) ) ;
#55914=CARTESIAN_POINT ( 'NONE',  ( -10.00000000000000355, 134.5833333265053682, 2.679491924311223183 ) ) ;
#55916=CARTESIAN_POINT ( 'NONE',  ( 4.242640687119287435, 290.3750000000000000, 4.242640687119285658 ) ) ;
#55923=CARTESIAN_POINT ( 'NONE',  ( 5.676582343750001591, 11.61458332991935016, -9.832129032723420536 ) ) ;
#55929=CARTESIAN_POINT ( 'NONE',  ( 5.676582343750001591, 1.614583329919349497, -9.832129032723420536 ) ) ;
#55930=CARTESIAN_POINT ( 'NONE',  ( -5.676582343749998039, 117.4479166632526841, -9.832129032723420536 ) ) ;
#55932=CARTESIAN_POINT ( 'NONE',  ( -10.00000000000000355, 99.58333332650538239, 2.679491924311223183 ) ) ;
#55936=CARTESIAN_POINT ( 'NONE',  ( -10.00000000000000000, 39.16666665983869677, -2.679491924311229845 ) ) ;
#55939=CARTESIAN_POINT ( 'NONE',  ( -6.676582343750003368, 289.5468750017069510, -2.765530957081996810 ) ) ;
#55949=CARTESIAN_POINT ( 'NONE',  ( -3.042071309553163960, 152.5520833299193555, -11.35316468749999963 ) ) ;
#55953=CARTESIAN_POINT ( 'NONE',  ( 8.311093377946837890, 76.71874999658599847, -8.311093377946837890 ) ) ;
#55959=CARTESIAN_POINT ( 'NONE',  ( -2.485281374238572649, 288.2500000034140726, 6.000000000000002665 ) ) ;
#55967=CARTESIAN_POINT ( 'NONE',  ( 7.347880794884121708E-16, 300.0000000000000000, -6.000000000000001776 ) ) ;
#55977=ORIENTED_EDGE ( 'NONE', *, *, #3790, .F. ) ;
#55982=CARTESIAN_POINT ( 'NONE',  ( -2.679491924311225848, 71.45833333333332860, -10.00000000000000178 ) ) ;
#55985=CARTESIAN_POINT ( 'NONE',  ( -4.242640687119286547, 292.8750000000000000, -4.242640687119286547 ) ) ;
#55994=CARTESIAN_POINT ( 'NONE',  ( -10.00000000000000355, 192.7083333333333428, 2.679491924311223183 ) ) ;
#55995=LINE ( 'NONE', #32616, #22323 ) ;
#55997=CARTESIAN_POINT ( 'NONE',  ( 5.676582343749993598, 170.2604166632526983, 9.832129032723422313 ) ) ;
#56001=CARTESIAN_POINT ( 'NONE',  ( 0.000000000000000000, 300.0000000000000000, 0.000000000000000000 ) ) ;
#56004=CARTESIAN_POINT ( 'NONE',  ( -5.676582343750006032, 29.42708332991935194, 9.832129032723418760 ) ) ;
#56011=EDGE_CURVE ( 'NONE', #55859, #55811, #27915, .T. ) ;
#56012=CARTESIAN_POINT ( 'NONE',  ( -2.679491924311225848, 53.33333332650536107, -10.00000000000000178 ) ) ;
#56015=CARTESIAN_POINT ( 'NONE',  ( 5.000000000000007994, 220.8333333333333428, -8.660254037844397956 ) ) ;
#56026=CARTESIAN_POINT ( 'NONE',  ( -8.311093377946841443, 143.9062499965860127, 8.311093377946830785 ) ) ;
#56028=PLANE ( 'NONE',  #15042 ) ;
#56033=CARTESIAN_POINT ( 'NONE',  ( 8.311093377946834337, 125.1562499965860269, 8.311093377946839666 ) ) ;
#56034=EDGE_CURVE ( 'NONE', #73747, #9554, #37494, .T. ) ;
#56036=ORIENTED_EDGE ( 'NONE', *, *, #16314, .F. ) ;
#56039=CARTESIAN_POINT ( 'NONE',  ( 11.35316468750000141, 111.0937499965860127, 0.000000000000000000 ) ) ;
#56043=CARTESIAN_POINT ( 'NONE',  ( -8.311093377946836114, 32.96874999658600558, -8.311093377946837890 ) ) ;
#56050=CARTESIAN_POINT ( 'NONE',  ( 1.226468279477575784E-15, 287.7031250017069510, 6.676582343750001591 ) ) ;
#56054=CARTESIAN_POINT ( 'NONE',  ( 11.35316468750000141, 141.0937499965860127, 0.000000000000000000 ) ) ;
#56062=VECTOR ( 'NONE', #45152, 1000.000000000000227 ) ;
#56069=CARTESIAN_POINT ( 'NONE',  ( -8.311093377946841443, 188.9062499965859843, 8.311093377946830785 ) ) ;
#56071=CARTESIAN_POINT ( 'NONE',  ( -6.000000000000003553, 291.0000000034139589, -2.485281374238571317 ) ) ;
#56072=CARTESIAN_POINT ( 'NONE',  ( 4.721056650416000089, 289.8281250017069510, 4.721056650415999201 ) ) ;
#56074=CARTESIAN_POINT ( 'NONE',  ( 2.679491924311332873, 33.95833333333334991, 9.999999999999936051 ) ) ;
#56084=CARTESIAN_POINT ( 'NONE',  ( 10.00000000000000178, 145.0000000000000284, 0.000000000000000000 ) ) ;
#56088=CARTESIAN_POINT ( 'NONE',  ( 11.35316468750000141, 121.0937499965860269, 0.000000000000000000 ) ) ;
#56095=CARTESIAN_POINT ( 'NONE',  ( 9.527714560998933990, 225.2503231660761003, -3.092998227472968598 ) ) ;
#56099=CARTESIAN_POINT ( 'NONE',  ( 9.832129032723420536, 206.5104166632526983, -5.676582343749999815 ) ) ;
#56105=CARTESIAN_POINT ( 'NONE',  ( -9.832129032723418760, 97.86458332991935549, -5.676582343750004256 ) ) ;
#56112=CARTESIAN_POINT ( 'NONE',  ( -8.311093377946836114, 97.65624999658602690, -8.311093377946837890 ) ) ;
#56120=CARTESIAN_POINT ( 'NONE',  ( -11.35316468749999785, 88.07291666325266988, -3.042071309553167957 ) ) ;
#56125=CARTESIAN_POINT ( 'NONE',  ( -4.999999999999998224, 178.5416666598387110, -8.660254037844389075 ) ) ;
#56129=CARTESIAN_POINT ( 'NONE',  ( 3.042071309553159519, 70.05208332991934128, 11.35316468750000141 ) ) ;
#56130=CARTESIAN_POINT ( 'NONE',  ( 2.765530957081996366, 290.1406250017069510, -6.676582343750003368 ) ) ;
#56132=CARTESIAN_POINT ( 'NONE',  ( -9.832129032723420536, 208.6979166632526983, 5.676582343749997150 ) ) ;
#56133=VERTEX_POINT ( 'NONE', #68764 ) ;
#56137=CARTESIAN_POINT ( 'NONE',  ( 3.042071309553167513, 211.8229166632526699, -11.35316468749999785 ) ) ;
#56141=CARTESIAN_POINT ( 'NONE',  ( -8.311093377946836114, 192.9687499965860127, -8.311093377946837890 ) ) ;
#56148=CARTESIAN_POINT ( 'NONE',  ( -10.00000000000000000, 17.29166666666666430, -2.679491924311229845 ) ) ;
#56158=ADVANCED_FACE ( 'NONE', ( #22352 ), #52811, .T. ) ;
#56171=CARTESIAN_POINT ( 'NONE',  ( -2.085542519210945728E-15, 69.84374999658601268, 11.35316468750000141 ) ) ;
#56176=CARTESIAN_POINT ( 'NONE',  ( -4.721056650415999201, 289.4843750017070079, -4.721056650415999201 ) ) ;
#56185=CARTESIAN_POINT ( 'NONE',  ( -11.35316468749999785, 173.3854166632526983, -3.042071309553167513 ) ) ;
#56193=CARTESIAN_POINT ( 'NONE',  ( 3.042071309553167069, 51.82291666325266988, -11.35316468749999785 ) ) ;
#56194=CARTESIAN_POINT ( 'NONE',  ( 10.00000000000000178, 22.08333332650536818, -2.679491924311226736 ) ) ;
#56197=CARTESIAN_POINT ( 'NONE',  ( 5.000000000000001776, 142.7083333265053682, -8.660254037844389075 ) ) ;
#56199=CARTESIAN_POINT ( 'NONE',  ( -11.35316468750000141, 43.48958332991934839, 3.042071309553159963 ) ) ;
#56205=CARTESIAN_POINT ( 'NONE',  ( 3.042071309553159519, 49.73958332991934839, 11.35316468750000141 ) ) ;
#56208=CARTESIAN_POINT ( 'NONE',  ( 6.951808397369818766E-16, 177.0312499965860411, -11.35316468750000141 ) ) ;
#56209=CARTESIAN_POINT ( 'NONE',  ( 8.660254037844389075, 142.2916666598386826, -5.000000000000000000 ) ) ;
#56211=FACE_OUTER_BOUND ( 'NONE', #44466, .T. ) ;
#56212=CARTESIAN_POINT ( 'NONE',  ( 11.35316468750000141, 36.09374999658601979, 0.000000000000000000 ) ) ;
#56213=CARTESIAN_POINT ( 'NONE',  ( 2.485281374238196062, 295.7500000034141863, -6.000000000000377476 ) ) ;
#56220=CARTESIAN_POINT ( 'NONE',  ( 9.832129032723416984, 170.3645833299193555, 5.676582343750006032 ) ) ;
#56227=FACE_OUTER_BOUND ( 'NONE', #68355, .T. ) ;
#56228=CARTESIAN_POINT ( 'NONE',  ( -2.085542519210945728E-15, 114.8437499965860127, 11.35316468750000141 ) ) ;
#56250=VERTEX_POINT ( 'NONE', #73681 ) ;
#56251=VERTEX_POINT ( 'NONE', #68392 ) ;
#56253=CARTESIAN_POINT ( 'NONE',  ( 6.000000000000003553, 288.4375000000000000, 2.485281374238571317 ) ) ;
#56256=AXIS2_PLACEMENT_3D ( 'NONE', #31091, #8088, #2060 ) ;
#56259=CARTESIAN_POINT ( 'NONE',  ( -7.320508075688773708, 126.8750000000000142, -7.320508075688774596 ) ) ;
#56261=CARTESIAN_POINT ( 'NONE',  ( -2.765530957081998586, 292.7968750017070079, 6.676582343750001591 ) ) ;
#56274=CARTESIAN_POINT ( 'NONE',  ( -8.311093377946836114, 12.65624999658601801, -8.311093377946837890 ) ) ;
#56276=CARTESIAN_POINT ( 'NONE',  ( -11.35316468750000141, 213.8020833299193839, 3.042071309553159963 ) ) ;
#56281=ORIENTED_EDGE ( 'NONE', *, *, #23200, .F. ) ;
#56283=CARTESIAN_POINT ( 'NONE',  ( 8.311093377946834337, 15.15624999658601624, 8.311093377946839666 ) ) ;
#56289=CARTESIAN_POINT ( 'NONE',  ( -3.042071309553163960, 12.23958332991935016, -11.35316468749999963 ) ) ;
#56292=CARTESIAN_POINT ( 'NONE',  ( -3.042071309553173730, 134.3229166632526983, 11.35316468749999785 ) ) ;
#56294=CARTESIAN_POINT ( 'NONE',  ( 5.000000000000001776, 102.7083333265053824, -8.660254037844389075 ) ) ;
#56297=CARTESIAN_POINT ( 'NONE',  ( -10.00000000000000355, 199.5833333265053398, 2.679491924311223183 ) ) ;
#56301=CARTESIAN_POINT ( 'NONE',  ( -6.676582343750001591, 291.6093750017069510, 0.000000000000000000 ) ) ;
#56310=CARTESIAN_POINT ( 'NONE',  ( 3.042071309553159519, 150.0520833299193555, 11.35316468750000141 ) ) ;
#56314=CARTESIAN_POINT ( 'NONE',  ( 11.35316468749999785, 70.88541666325265567, 3.042071309553174174 ) ) ;
#56315=EDGE_LOOP ( 'NONE', ( #18778, #23366, #6349, #39162 ) ) ;
#56326=CARTESIAN_POINT ( 'NONE',  ( 7.320508075688769267, 110.6249999999999858, -7.320508075688769267 ) ) ;
#56330=EDGE_CURVE ( 'NONE', #6481, #29411, #69333, .T. ) ;
#56334=( BOUNDED_CURVE ( )  B_SPLINE_CURVE ( 2, ( #69470, #17780, #40793, #18892, #12845, #64549, #1192, #46817, #7941, #69843, #35515, #52489, #24174 ),
 .UNSPECIFIED., .F., .F. ) 
 B_SPLINE_CURVE_WITH_KNOTS ( ( 3, 2, 2, 2, 2, 2, 3 ),
 ( 0.7336956521739129711, 0.7355072463768115298, 0.7373188405797100886, 0.7391304347826086474, 0.7409420289855072062, 0.7427536231884057649, 0.7445652173913043237 ),
 .UNSPECIFIED. ) 
 CURVE ( )  GEOMETRIC_REPRESENTATION_ITEM ( )  RATIONAL_B_SPLINE_CURVE ( ( 1.000000000000001998, 0.9659258262890662028, 1.000000000000000000, 0.9659258262890683122, 1.000000000000000000, 0.9659258262890683122, 1.000000000000000000, 0.9659258262890683122, 1.000000000000000000, 0.9659258262890683122, 1.000000000000000000, 0.9659258262890683122, 1.000000000000000000 ) ) 
 REPRESENTATION_ITEM ( '' )  );
#56347=CARTESIAN_POINT ( 'NONE',  ( -2.679491924311235618, 83.54166666666664298, 10.00000000000000000 ) ) ;
#56349=CARTESIAN_POINT ( 'NONE',  ( -4.242640687119286547, 290.8750000000000000, -4.242640687119286547 ) ) ;
#56353=LINE ( 'NONE', #27668, #24101 ) ;
#56356=CARTESIAN_POINT ( 'NONE',  ( -1.836970198721029983E-15, 55.62499999317203958, 10.00000000000000178 ) ) ;
#56359=CARTESIAN_POINT ( 'NONE',  ( -8.660254037844417496, 77.08333333333337123, -5.000000000000023093 ) ) ;
#56360=CARTESIAN_POINT ( 'NONE',  ( 8.660254037844389075, 205.4166666666666856, -5.000000000000000000 ) ) ;
#56363=CARTESIAN_POINT ( 'NONE',  ( 9.832129032723416984, 170.6770833299193555, 5.676582343750006032 ) ) ;
#56369=CARTESIAN_POINT ( 'NONE',  ( -11.35316468750000141, 23.59374999658601979, -1.390361679473963753E-15 ) ) ;
#56372=DIRECTION ( 'NONE',  ( -0.000000000000000000, 1.000000000000000000, -0.000000000000000000 ) ) ;
#56376=CARTESIAN_POINT ( 'NONE',  ( -4.999999999999998224, 63.54166665983869677, -8.660254037844389075 ) ) ;
#56379=CARTESIAN_POINT ( 'NONE',  ( 9.999999999999994671, 54.79166666666666430, 2.679491924311234285 ) ) ;
#56381=CARTESIAN_POINT ( 'NONE',  ( 9.999999999999998224, 164.7916666666666856, 2.679491924311235618 ) ) ;
#56388=CARTESIAN_POINT ( 'NONE',  ( -5.676582343749998039, 137.4479166632526983, -9.832129032723420536 ) ) ;
#56396=DIRECTION ( 'NONE',  ( -0.000000000000000000, 1.000000000000000000, -0.000000000000000000 ) ) ;
#56402=CARTESIAN_POINT ( 'NONE',  ( 11.35316468749999963, 111.3020833299193413, -3.042071309553165293 ) ) ;
#56406=CARTESIAN_POINT ( 'NONE',  ( 5.676582343750001591, 36.92708332991935549, -9.832129032723420536 ) ) ;
#56413=CARTESIAN_POINT ( 'NONE',  ( 2.485281374238575314, 295.3750000034139589, 6.000000000000000888 ) ) ;
#56414=CARTESIAN_POINT ( 'NONE',  ( 8.660254037844385522, 111.4583333265053682, 5.000000000000005329 ) ) ;
#56417=CARTESIAN_POINT ( 'NONE',  ( -11.35316468749999785, 153.3854166632526699, -3.042071309553167513 ) ) ;
#56434=CARTESIAN_POINT ( 'NONE',  ( 7.320508075688774596, 35.62500000000000711, -7.320508075688774596 ) ) ;
#56438=CARTESIAN_POINT ( 'NONE',  ( 4.721056650415999201, 289.0781250017069510, -4.721056650415999201 ) ) ;
#56441=CARTESIAN_POINT ( 'NONE',  ( -10.00000000000000355, 67.29166666666667140, -2.679491924311231177 ) ) ;
#56451=CARTESIAN_POINT ( 'NONE',  ( -10.00000000000000000, 152.2916666666666856, -2.679491924311229845 ) ) ;
#56456=CARTESIAN_POINT ( 'NONE',  ( -9.832129032723420536, 124.0104166632526841, 5.676582343749997150 ) ) ;
#56457=CARTESIAN_POINT ( 'NONE',  ( -6.000000000000003553, 295.9374999999999432, -2.485281374238571317 ) ) ;
#56469=CARTESIAN_POINT ( 'NONE',  ( 11.35316468749999963, 206.3020833299193271, -3.042071309553165293 ) ) ;
#56476=CARTESIAN_POINT ( 'NONE',  ( -8.311093377946836114, 97.65624999658602690, -8.311093377946837890 ) ) ;
#56482=CARTESIAN_POINT ( 'NONE',  ( -11.35316468750000141, 108.4895833299193413, 3.042071309553159963 ) ) ;
#56484=CARTESIAN_POINT ( 'NONE',  ( 2.679491924311228956, 207.9166666598387110, -10.00000000000000000 ) ) ;
#56490=CARTESIAN_POINT ( 'NONE',  ( -9.832129032723420536, 88.69791666325268409, 5.676582343749997150 ) ) ;
#56495=CARTESIAN_POINT ( 'NONE',  ( 10.00000000000000000, 181.6666666598387394, 2.679491924311236062 ) ) ;
#56499=CARTESIAN_POINT ( 'NONE',  ( -2.085542519210945728E-15, 79.84374999658601268, 11.35316468750000141 ) ) ;
#56500=CARTESIAN_POINT ( 'NONE',  ( -6.676582343750003368, 290.3906250017070647, -2.765530957081996810 ) ) ;
#56502=CARTESIAN_POINT ( 'NONE',  ( -3.042071309553164404, 217.2395833299192986, -11.35316468749999963 ) ) ;
#56507=CARTESIAN_POINT ( 'NONE',  ( -11.35316468750000141, 203.2812499965860411, -1.390361679473963753E-15 ) ) ;
#56508=AXIS2_PLACEMENT_3D ( 'NONE', #3704, #44435, #8986 ) ;
#56513=CARTESIAN_POINT ( 'NONE',  ( -2.085542519210945728E-15, 189.8437499965860127, 11.35316468750000141 ) ) ;
#56521=CARTESIAN_POINT ( 'NONE',  ( -5.000000000000005329, 8.333333333333333925, 8.660254037844387298 ) ) ;
#56535=ORIENTED_EDGE ( 'NONE', *, *, #73450, .F. ) ;
#56541=ORIENTED_EDGE ( 'NONE', *, *, #6696, .F. ) ;
#56543=CARTESIAN_POINT ( 'NONE',  ( -5.676582343749998039, 82.76041666325268409, -9.832129032723420536 ) ) ;
#56548=CARTESIAN_POINT ( 'NONE',  ( 2.765530957081996366, 288.2968750017070079, -6.676582343750002480 ) ) ;
#56551=CARTESIAN_POINT ( 'NONE',  ( 6.123233995736767268E-16, 78.12499999317202537, -10.00000000000000178 ) ) ;
#56554=CARTESIAN_POINT ( 'NONE',  ( 3.042071309553159519, 204.7395833299193271, 11.35316468750000141 ) ) ;
#56559=CARTESIAN_POINT ( 'NONE',  ( 9.832129032723416984, 165.6770833299193555, 5.676582343750006032 ) ) ;
#56560=CARTESIAN_POINT ( 'NONE',  ( 0.000000000000000000, 300.0000000000000000, 0.000000000000000000 ) ) ;
#56562=LINE ( 'NONE', #51257, #66057 ) ;
#56566=CARTESIAN_POINT ( 'NONE',  ( -8.311093377946836114, 57.65624999658601979, -8.311093377946837890 ) ) ;
#56567=EDGE_CURVE ( 'NONE', #18299, #8118, #56353, .T. ) ;
#56573=CARTESIAN_POINT ( 'NONE',  ( -5.676582343749998039, 67.44791666325268409, -9.832129032723420536 ) ) ;
#56579=CARTESIAN_POINT ( 'NONE',  ( 11.35316468749999785, 50.57291666325268409, 3.042071309553174174 ) ) ;
#56582=CARTESIAN_POINT ( 'NONE',  ( 11.35316468749999785, 170.5729166632526983, 3.042071309553174174 ) ) ;
#56585=CARTESIAN_POINT ( 'NONE',  ( -10.00000000000000178, 139.3749999931720538, -1.224646799147353454E-15 ) ) ;
#56588=CARTESIAN_POINT ( 'NONE',  ( -8.311093377946836114, 32.96874999658600558, -8.311093377946837890 ) ) ;
#56589=CARTESIAN_POINT ( 'NONE',  ( -10.00000000000000355, 79.58333332650536818, 2.679491924311223183 ) ) ;
#56590=CARTESIAN_POINT ( 'NONE',  ( 6.951808397369818766E-16, 182.0312499965860411, -11.35316468750000141 ) ) ;
#56597=CARTESIAN_POINT ( 'NONE',  ( -3.042071309553163960, 167.2395833299193555, -11.35316468749999963 ) ) ;
#56607=CARTESIAN_POINT ( 'NONE',  ( 8.311093377946837890, 111.7187499965859985, -8.311093377946837890 ) ) ;
#56608=EDGE_CURVE ( 'NONE', #69323, #39904, #72193, .T. ) ;
#56637=LINE ( 'NONE', #68312, #49442 ) ;
#56638=CARTESIAN_POINT ( 'NONE',  ( -10.00000000000000178, 127.5000000000000000, -1.224646799147353454E-15 ) ) ;
#56640=CARTESIAN_POINT ( 'NONE',  ( -6.676582343750003368, 288.5468750017070079, -2.765530957081996810 ) ) ;
#56651=CARTESIAN_POINT ( 'NONE',  ( -10.00000000000000178, 214.3749999931720538, -1.224646799147353454E-15 ) ) ;
#56653=CARTESIAN_POINT ( 'NONE',  ( -3.042071309553164404, 12.23958332991935194, -11.35316468749999963 ) ) ;
#56654=CARTESIAN_POINT ( 'NONE',  ( 7.320508075688773708, 0.6249999999999988898, -7.320508075688773708 ) ) ;
#56655=CARTESIAN_POINT ( 'NONE',  ( 6.951808397369818766E-16, 207.3437499965860411, -11.35316468750000141 ) ) ;
#56658=FACE_OUTER_BOUND ( 'NONE', #145, .T. ) ;
#56662=CARTESIAN_POINT ( 'NONE',  ( -11.35316468750000141, 23.28124999658601979, -1.390361679473963753E-15 ) ) ;
#56670=CARTESIAN_POINT ( 'NONE',  ( -9.832129032723420536, 128.6979166632526983, 5.676582343749997150 ) ) ;
#56672=CARTESIAN_POINT ( 'NONE',  ( 8.660254037844385522, 106.4583333265053682, 5.000000000000005329 ) ) ;
#56679=CARTESIAN_POINT ( 'NONE',  ( 0.000000000000000000, 300.0000000000000000, 0.000000000000000000 ) ) ;
#56680=CARTESIAN_POINT ( 'NONE',  ( -6.676582343750000703, 290.6718750017070079, 2.765530957082001251 ) ) ;
#56687=EDGE_CURVE ( 'NONE', #64324, #29716, #58767, .T. ) ;
#56692=CARTESIAN_POINT ( 'NONE',  ( 6.951808397369818766E-16, 82.34374999658601268, -11.35316468750000141 ) ) ;
#56700=CARTESIAN_POINT ( 'NONE',  ( 2.679491924315057449, 116.0416666666663303, -9.999999999997791988 ) ) ;
#56705=VECTOR ( 'NONE', #25959, 1000.000000000000000 ) ;
#56709=ORIENTED_EDGE ( 'NONE', *, *, #39463, .F. ) ;
#56723=CARTESIAN_POINT ( 'NONE',  ( 10.00000000000000178, 85.00000000000000000, 0.000000000000000000 ) ) ;
#56726=CARTESIAN_POINT ( 'NONE',  ( 4.721056650416000089, 298.9843750017070079, 4.721056650415999201 ) ) ;
#56736=CARTESIAN_POINT ( 'NONE',  ( -10.00000000000000178, 197.5000000000000000, -1.224646799147353454E-15 ) ) ;
#56738=CARTESIAN_POINT ( 'NONE',  ( -9.832129032723418760, 168.1770833299193555, -5.676582343750004256 ) ) ;
#56739=CARTESIAN_POINT ( 'NONE',  ( -2.679491924311433237, 211.4583333333334849, -10.00000000000014033 ) ) ;
#56741=FACE_OUTER_BOUND ( 'NONE', #73514, .T. ) ;
#56742=CARTESIAN_POINT ( 'NONE',  ( -5.999999999999999112, 297.1250000034141294, 2.485281374238575314 ) ) ;
#56743=ORIENTED_EDGE ( 'NONE', *, *, #43462, .T. ) ;
#56744=CARTESIAN_POINT ( 'NONE',  ( 11.35316468749999963, 26.30208332991934839, -3.042071309553165293 ) ) ;
#56751=EDGE_CURVE ( 'NONE', #28343, #18004, #41227, .T. ) ;
#56752=CARTESIAN_POINT ( 'NONE',  ( 10.00000000000000000, 61.66666665983871098, 2.679491924311236062 ) ) ;
#56758=ORIENTED_EDGE ( 'NONE', *, *, #58993, .F. ) ;
#56763=CARTESIAN_POINT ( 'NONE',  ( 5.676582343750001591, 141.6145833299193555, -9.832129032723420536 ) ) ;
#56776=CARTESIAN_POINT ( 'NONE',  ( 8.311093377946834337, 130.4687499965860411, 8.311093377946839666 ) ) ;
#56780=CARTESIAN_POINT ( 'NONE',  ( -8.311093377946836114, 37.96874999658601979, -8.311093377946837890 ) ) ;
#56782=DIRECTION ( 'NONE',  ( -0.000000000000000000, 1.000000000000000000, -0.000000000000000000 ) ) ;
#56788=CARTESIAN_POINT ( 'NONE',  ( -2.485281374238572649, 296.2500000034140726, 6.000000000000002665 ) ) ;
#56793=CARTESIAN_POINT ( 'NONE',  ( -8.311093377946836114, 157.9687499965860127, -8.311093377946837890 ) ) ;
#56808=CARTESIAN_POINT ( 'NONE',  ( -2.679491924311235618, 38.54166666666665719, 10.00000000000000000 ) ) ;
#56812=CARTESIAN_POINT ( 'NONE',  ( -4.721056650415998313, 289.5781250017069510, 4.721056650416000089 ) ) ;
#56813=CARTESIAN_POINT ( 'NONE',  ( 2.679491924312774831, 36.04166666666652930, -9.999999999999104716 ) ) ;
#56822=CARTESIAN_POINT ( 'NONE',  ( -8.660254037844387298, 167.0833333333333428, -5.000000000000004441 ) ) ;
#56823=CARTESIAN_POINT ( 'NONE',  ( -6.000000000000003553, 299.9374999999999432, -2.485281374238571317 ) ) ;
#56826=CARTESIAN_POINT ( 'NONE',  ( 8.311093377946834337, 125.4687499965860127, 8.311093377946839666 ) ) ;
#56835=CARTESIAN_POINT ( 'NONE',  ( 2.905213938366133508, 223.9844880932393210, 9.586977549355461647 ) ) ;
#56839=CARTESIAN_POINT ( 'NONE',  ( -11.35316468750000141, 208.8020833299193555, 3.042071309553159963 ) ) ;
#56845=LINE ( 'NONE', #22484, #62840 ) ;
#56846=CARTESIAN_POINT ( 'NONE',  ( -11.35316468750000141, 93.28124999658602690, -1.390361679473963753E-15 ) ) ;
#56848=DIRECTION ( 'NONE',  ( 0.000000000000000000, 1.000000000000000000, 0.000000000000000000 ) ) ;
#56850=CARTESIAN_POINT ( 'NONE',  ( 5.000000000000081712, 40.83333333333342097, -8.660254037844525854 ) ) ;
#56853=CARTESIAN_POINT ( 'NONE',  ( 9.832129032723416984, 100.3645833299193697, 5.676582343750006032 ) ) ;
#56858=CARTESIAN_POINT ( 'NONE',  ( -2.679491924311235618, 225.4166666598386826, 10.00000000000000000 ) ) ;
#56862=CARTESIAN_POINT ( 'NONE',  ( -2.085542519210945728E-15, 94.53124999658601268, 11.35316468750000141 ) ) ;
#56867=EDGE_CURVE ( 'NONE', #12530, #36130, #38045, .T. ) ;
#56868=CARTESIAN_POINT ( 'NONE',  ( 2.679491924311222739, 180.8333333265053966, 10.00000000000000355 ) ) ;
#56871=CARTESIAN_POINT ( 'NONE',  ( -5.676582343750006032, 84.42708332991935549, 9.832129032723418760 ) ) ;
#56872=CARTESIAN_POINT ( 'NONE',  ( 1.226468279477575784E-15, 290.7031250017069510, 6.676582343750001591 ) ) ;
#56875=CARTESIAN_POINT ( 'NONE',  ( -8.311093377946836114, 222.6562499965860411, -8.311093377946837890 ) ) ;
#56880=CARTESIAN_POINT ( 'NONE',  ( 9.832129032723416984, 210.3645833299193555, 5.676582343750006032 ) ) ;
#56882=CARTESIAN_POINT ( 'NONE',  ( -1.836970198721029983E-15, 100.6249999931720396, 10.00000000000000178 ) ) ;
#56883=CARTESIAN_POINT ( 'NONE',  ( -2.765530957081998586, 297.6406250017070079, 6.676582343750001591 ) ) ;
#56884=EDGE_CURVE ( 'NONE', #44635, #48188, #45744, .T. ) ;
#56886=CARTESIAN_POINT ( 'NONE',  ( 11.35316468749999785, 200.8854166632526983, 3.042071309553174174 ) ) ;
#56895=CARTESIAN_POINT ( 'NONE',  ( 2.679491924311228956, 16.04166666666666785, -10.00000000000000000 ) ) ;
#56903=CARTESIAN_POINT ( 'NONE',  ( 8.660254037844389075, 17.29166665983869677, -5.000000000000000000 ) ) ;
#56905=FACE_OUTER_BOUND ( 'NONE', #33704, .T. ) ;
#56911=ORIENTED_EDGE ( 'NONE', *, *, #55857, .F. ) ;
#56917=CARTESIAN_POINT ( 'NONE',  ( -2.085542519210945728E-15, 84.84374999658601268, 11.35316468750000141 ) ) ;
#56922=CARTESIAN_POINT ( 'NONE',  ( 2.765530957082001251, 289.9218750017069510, 6.676582343749999815 ) ) ;
#56925=CARTESIAN_POINT ( 'NONE',  ( -2.085542519210945728E-15, 199.5312499965860411, 11.35316468750000141 ) ) ;
#56931=CARTESIAN_POINT ( 'NONE',  ( 5.676582343750001591, 166.9270833299193555, -9.832129032723420536 ) ) ;
#56937=CARTESIAN_POINT ( 'NONE',  ( -5.676582343750006032, 54.11458332991934839, 9.832129032723418760 ) ) ;
#56943=CARTESIAN_POINT ( 'NONE',  ( -11.35316468750000141, 63.48958332991935549, 3.042071309553159963 ) ) ;
#56947=CARTESIAN_POINT ( 'NONE',  ( -4.999999999999998224, 11.66666666666666785, -8.660254037844389075 ) ) ;
#56949=CARTESIAN_POINT ( 'NONE',  ( -5.676582343750006032, 49.11458332991935549, 9.832129032723418760 ) ) ;
#56952=CARTESIAN_POINT ( 'NONE',  ( 9.832129032723420536, 171.1979166632526983, -5.676582343749999815 ) ) ;
#56953=ADVANCED_FACE ( 'NONE', ( #42317 ), #31378, .T. ) ;
#56954=CARTESIAN_POINT ( 'NONE',  ( 5.000000000000001776, 147.7083333265053682, -8.660254037844389075 ) ) ;
#56957=DIRECTION ( 'NONE',  ( -0.000000000000000000, 1.000000000000000000, -0.000000000000000000 ) ) ;
#56958=CARTESIAN_POINT ( 'NONE',  ( -9.832129032723420536, 29.01041666325268764, 5.676582343749997150 ) ) ;
#56960=CARTESIAN_POINT ( 'NONE',  ( -11.35316468749999785, 188.0729166632526983, -3.042071309553167513 ) ) ;
#56967=CARTESIAN_POINT ( 'NONE',  ( -11.35316468749999785, 163.0729166632526699, -3.042071309553167957 ) ) ;
#56970=CARTESIAN_POINT ( 'NONE',  ( 2.250000000000001332, 261.5999999999996248, 5.425975922785162275 ) ) ;
#56972=CYLINDRICAL_SURFACE ( 'NONE', #20322, 10.00000000000000178 ) ;
#56973=ORIENTED_EDGE ( 'NONE', *, *, #43058, .F. ) ;
#56975=CARTESIAN_POINT ( 'NONE',  ( 0.000000000000000000, 300.0000000000000000, 0.000000000000000000 ) ) ;
#56976=CARTESIAN_POINT ( 'NONE',  ( -2.085542519210945728E-15, 109.8437499965860269, 11.35316468750000141 ) ) ;
#56979=ORIENTED_EDGE ( 'NONE', *, *, #28240, .F. ) ;
#56984=EDGE_CURVE ( 'NONE', #32512, #24671, #10064, .T. ) ;
#57007=CARTESIAN_POINT ( 'NONE',  ( -8.660254037844390851, 117.9166666666666714, 4.999999999999998224 ) ) ;
#57009=CARTESIAN_POINT ( 'NONE',  ( 2.765530957081996366, 288.2968750017070647, -6.676582343750003368 ) ) ;
#57023=CARTESIAN_POINT ( 'NONE',  ( 11.35316468749999963, 20.98958332991935549, -3.042071309553165293 ) ) ;
#57026=CARTESIAN_POINT ( 'NONE',  ( -9.832129032723420536, 209.0104166632526699, 5.676582343749997150 ) ) ;
#57027=CARTESIAN_POINT ( 'NONE',  ( 11.35316468749999963, 0.9895833299193491639, -3.042071309553165293 ) ) ;
#57033=CARTESIAN_POINT ( 'NONE',  ( 11.35316468749999785, 20.57291666325268409, 3.042071309553174174 ) ) ;
#57035=CARTESIAN_POINT ( 'NONE',  ( 8.660254037844389075, 210.4166666666666572, -5.000000000000000888 ) ) ;
#57037=DIRECTION ( 'NONE',  ( -0.000000000000000000, 1.000000000000000000, -0.000000000000000000 ) ) ;
#57039=CARTESIAN_POINT ( 'NONE',  ( 3.042071309553167513, 6.822916663252683200, -11.35316468749999785 ) ) ;
#57041=CARTESIAN_POINT ( 'NONE',  ( 9.832129032723420536, 141.1979166632526699, -5.676582343749999815 ) ) ;
#57042=CARTESIAN_POINT ( 'NONE',  ( -7.320508075688773708, 108.7499999931720254, -7.320508075688774596 ) ) ;
#57049=CARTESIAN_POINT ( 'NONE',  ( -10.00000000000000888, 117.7083333333333428, 2.679491924311224071 ) ) ;
#57050=DIRECTION ( 'NONE',  ( 0.000000000000000000, 0.000000000000000000, 1.000000000000000000 ) ) ;
#57051=CARTESIAN_POINT ( 'NONE',  ( 2.765530957081996366, 289.2968750017070079, -6.676582343750003368 ) ) ;
#57052=CARTESIAN_POINT ( 'NONE',  ( 0.000000000000000000, 300.0000000000000000, 0.000000000000000000 ) ) ;
#57057=ORIENTED_EDGE ( 'NONE', *, *, #31636, .F. ) ;
#57058=ADVANCED_FACE ( 'NONE', ( #66450 ), #50586, .T. ) ;
#57062=CARTESIAN_POINT ( 'NONE',  ( 5.676582343749993598, 75.26041666325268409, 9.832129032723422313 ) ) ;
#57085=CARTESIAN_POINT ( 'NONE',  ( -4.242640687119285658, 292.1249999999999432, 4.242640687119287435 ) ) ;
#57086=EDGE_LOOP ( 'NONE', ( #48864, #2147, #54529, #15751 ) ) ;
#57091=CARTESIAN_POINT ( 'NONE',  ( -7.320508075688773708, 76.87499999999998579, -7.320508075688774596 ) ) ;
#57093=CARTESIAN_POINT ( 'NONE',  ( -4.242640687119285658, 289.1249999999999432, 4.242640687119287435 ) ) ;
#57104=CARTESIAN_POINT ( 'NONE',  ( -8.660254037844390851, 197.9166666666666856, 4.999999999999998224 ) ) ;
#57107=CARTESIAN_POINT ( 'NONE',  ( 6.951808397369818766E-16, 167.3437499965860127, -11.35316468750000141 ) ) ;
#57108=CARTESIAN_POINT ( 'NONE',  ( -7.320508075688939797, 213.1250000000000853, 7.320508075688932692 ) ) ;
#57110=CYLINDRICAL_SURFACE ( 'NONE', #67169, 10.00000000000000178 ) ;
#57115=CARTESIAN_POINT ( 'NONE',  ( -9.832129032723418760, 38.17708332991935549, -5.676582343750004256 ) ) ;
#57119=CARTESIAN_POINT ( 'NONE',  ( 7.320508075688771044, 221.2499999931720538, 7.320508075688775484 ) ) ;
#57123=CARTESIAN_POINT ( 'NONE',  ( 8.660254037844389075, 67.29166665983869677, -5.000000000000000000 ) ) ;
#57135=CARTESIAN_POINT ( 'NONE',  ( -9.832129032723418760, 142.8645833299193555, -5.676582343750004256 ) ) ;
#57141=LINE ( 'NONE', #45432, #53047 ) ;
#57143=ORIENTED_EDGE ( 'NONE', *, *, #47743, .T. ) ;
#57147=CARTESIAN_POINT ( 'NONE',  ( 6.951808397369818766E-16, 132.3437499965860127, -11.35316468750000141 ) ) ;
#57151=CARTESIAN_POINT ( 'NONE',  ( -9.832129032723418760, 33.17708332991934839, -5.676582343750004256 ) ) ;
#57152=ORIENTED_EDGE ( 'NONE', *, *, #25641, .T. ) ;
#57153=CARTESIAN_POINT ( 'NONE',  ( -1.836970198721029983E-15, 35.62499999317203248, 10.00000000000000178 ) ) ;
#57158=CARTESIAN_POINT ( 'NONE',  ( 6.000000000000003553, 294.5000000034139589, 2.485281374238571317 ) ) ;
#57161=CARTESIAN_POINT ( 'NONE',  ( 3.042071309553167069, 152.1354166632526983, -11.35316468749999785 ) ) ;
#57167=ORIENTED_EDGE ( 'NONE', *, *, #21049, .T. ) ;
#57172=EDGE_CURVE ( 'NONE', #64725, #40886, #3838, .T. ) ;
#57174=CARTESIAN_POINT ( 'NONE',  ( -10.00000000000008171, 57.50000000000004974, -1.224646799147362920E-15 ) ) ;
#57176=EDGE_LOOP ( 'NONE', ( #35888, #69739, #37581, #988 ) ) ;
#57178=FACE_OUTER_BOUND ( 'NONE', #61668, .T. ) ;
#57180=CARTESIAN_POINT ( 'NONE',  ( 6.123233995736767268E-16, 41.25000000000000000, -10.00000000000000178 ) ) ;
#57190=VECTOR ( 'NONE', #22098, 1000.000000000000000 ) ;
#57192=CARTESIAN_POINT ( 'NONE',  ( -6.000000000000001776, 287.0625000034140157, 0.000000000000000000 ) ) ;
#57195=CARTESIAN_POINT ( 'NONE',  ( -5.000000000000005329, 163.3333333333333428, 8.660254037844387298 ) ) ;
#57199=CARTESIAN_POINT ( 'NONE',  ( -11.35316468749999785, 128.3854166632526699, -3.042071309553167513 ) ) ;
#57211=CARTESIAN_POINT ( 'NONE',  ( -8.311093377946841443, 219.2187499965859843, 8.311093377946830785 ) ) ;
#57218=CARTESIAN_POINT ( 'NONE',  ( -8.311093377946841443, 98.90624999658604111, 8.311093377946830785 ) ) ;
#57220=DIRECTION ( 'NONE',  ( -0.000000000000000000, 1.000000000000000000, -0.000000000000000000 ) ) ;
#57225=CARTESIAN_POINT ( 'NONE',  ( 8.311093377946837890, 101.4062499965859985, -8.311093377946837890 ) ) ;
#57229=CARTESIAN_POINT ( 'NONE',  ( 8.660254037844385522, 221.4583333265053966, 5.000000000000005329 ) ) ;
#57233=CARTESIAN_POINT ( 'NONE',  ( -8.311093377946836114, 97.65624999658602690, -8.311093377946837890 ) ) ;
#57236=CARTESIAN_POINT ( 'NONE',  ( 6.123233995736767268E-16, 128.1249999931720254, -10.00000000000000178 ) ) ;
#57239=CARTESIAN_POINT ( 'NONE',  ( -7.320508075688778149, 194.9999999931720538, 7.320508075688769267 ) ) ;
#57242=CARTESIAN_POINT ( 'NONE',  ( -5.676582343749998039, 87.76041666325268409, -9.832129032723420536 ) ) ;
#57243=CARTESIAN_POINT ( 'NONE',  ( 2.765530957081996366, 289.1406250017069510, -6.676582343750003368 ) ) ;
#57246=CARTESIAN_POINT ( 'NONE',  ( 8.311093377946837890, 1.718749996586016682, -8.311093377946837890 ) ) ;
#57248=CARTESIAN_POINT ( 'NONE',  ( -7.320508075688778149, 69.99999999317203958, 7.320508075688769267 ) ) ;
#57249=CARTESIAN_POINT ( 'NONE',  ( 6.123233995736767268E-16, 101.2500000000000000, -10.00000000000000178 ) ) ;
#57251=CARTESIAN_POINT ( 'NONE',  ( -5.676582343750006032, 214.1145833299193555, 9.832129032723418760 ) ) ;
#57252=CARTESIAN_POINT ( 'NONE',  ( 10.00000000000000178, 46.87499999317203958, 0.000000000000000000 ) ) ;
#57254=CARTESIAN_POINT ( 'NONE',  ( 2.765530957081996366, 298.1406250017069510, -6.676582343750003368 ) ) ;
#57258=CARTESIAN_POINT ( 'NONE',  ( -11.35316468750000141, 208.8020833299193555, 3.042071309553159963 ) ) ;
#57267=CARTESIAN_POINT ( 'NONE',  ( -4.999999999999998224, 21.66666666666666785, -8.660254037844389075 ) ) ;
#57272=CARTESIAN_POINT ( 'NONE',  ( 1.102182119232618108E-15, 299.2500000000000000, 6.000000000000001776 ) ) ;
#57278=CARTESIAN_POINT ( 'NONE',  ( -4.088227598258586603E-16, 297.2031250017070079, -6.676582343750001591 ) ) ;
#57290=CARTESIAN_POINT ( 'NONE',  ( -3.042071309553173730, 94.63541666325269830, 11.35316468749999785 ) ) ;
#57299=EDGE_CURVE ( 'NONE', #6481, #44928, #11351, .T. ) ;
#57300=CARTESIAN_POINT ( 'NONE',  ( 5.676582343749993598, 199.9479166632526983, 9.832129032723422313 ) ) ;
#57305=CARTESIAN_POINT ( 'NONE',  ( -5.676582343749998039, 162.7604166632526983, -9.832129032723420536 ) ) ;
#57309=CARTESIAN_POINT ( 'NONE',  ( -8.660254037844387298, 88.95833332650536818, -5.000000000000004441 ) ) ;
#57313=CARTESIAN_POINT ( 'NONE',  ( 8.311093377946837890, 56.40624999658600558, -8.311093377946837890 ) ) ;
#57319=CARTESIAN_POINT ( 'NONE',  ( -9.832129032723418760, 62.86458332991935549, -5.676582343750004256 ) ) ;
#57324=CARTESIAN_POINT ( 'NONE',  ( 3.042071309553159519, 59.73958332991933418, 11.35316468750000141 ) ) ;
#57327=CARTESIAN_POINT ( 'NONE',  ( -2.085542519210945728E-15, 174.5312499965860411, 11.35316468750000141 ) ) ;
#57328=CARTESIAN_POINT ( 'NONE',  ( 5.000000000000001776, 137.7083333265053682, -8.660254037844389075 ) ) ;
#57331=CARTESIAN_POINT ( 'NONE',  ( 3.042071309553167513, 52.13541666325268409, -11.35316468749999785 ) ) ;
#57333=CARTESIAN_POINT ( 'NONE',  ( 0.000000000000000000, 300.0000000000000000, 10.00000000000000178 ) ) ;
#57334=CARTESIAN_POINT ( 'NONE',  ( -5.676582343750006032, 184.1145833299193555, 9.832129032723418760 ) ) ;
#57336=DIRECTION ( 'NONE',  ( -0.000000000000000000, 1.000000000000000000, -0.000000000000000000 ) ) ;
#57340=CARTESIAN_POINT ( 'NONE',  ( 8.311093377946834337, 185.1562499965860411, 8.311093377946839666 ) ) ;
#57345=ORIENTED_EDGE ( 'NONE', *, *, #30633, .T. ) ;
#57347=CARTESIAN_POINT ( 'NONE',  ( -3.042071309553164404, 127.5520833299193555, -11.35316468749999963 ) ) ;
#57348=( BOUNDED_CURVE ( )  B_SPLINE_CURVE ( 2, ( #19966, #42972, #59602, #19592, #59964, #30189, #70550, #70915, #58872, #65248, #47895, #14298, #30559 ),
 .UNSPECIFIED., .F., .F. ) 
 B_SPLINE_CURVE_WITH_KNOTS ( ( 3, 2, 2, 2, 2, 2, 3 ),
 ( 1.648487699650845073, 1.653721680593561949, 1.658955661536279047, 1.664189642478995923, 1.669423623421712799, 1.674657604364429897, 1.679891585307146773 ),
 .UNSPECIFIED. ) 
 CURVE ( )  GEOMETRIC_REPRESENTATION_ITEM ( )  RATIONAL_B_SPLINE_CURVE ( ( 0.9999999999999998890, 0.9659258262890682012, 0.9999999999999998890, 0.9659258262890682012, 0.9999999999999998890, 0.9659258262890682012, 0.9999999999999998890, 0.9659258262890682012, 0.9999999999999998890, 0.9659258262890682012, 0.9999999999999998890, 0.9659258262891058378, 0.9999999999999622524 ) ) 
 REPRESENTATION_ITEM ( '' )  );
#57354=AXIS2_PLACEMENT_3D ( 'NONE', #63097, #11422, #34459 ) ;
#57359=CARTESIAN_POINT ( 'NONE',  ( 6.123233995736767268E-16, 53.12499999317203958, -10.00000000000000178 ) ) ;
#57367=CYLINDRICAL_SURFACE ( 'NONE', #68748, 10.00000000000000178 ) ;
#57380=CARTESIAN_POINT ( 'NONE',  ( 2.765530957081996366, 299.2968750017070079, -6.676582343750002480 ) ) ;
#57381=CARTESIAN_POINT ( 'NONE',  ( 2.679491924311222739, 123.9583333333333286, 10.00000000000000355 ) ) ;
#57383=CARTESIAN_POINT ( 'NONE',  ( 4.721056650416000089, 288.9843750017070079, 4.721056650415999201 ) ) ;
#57395=CARTESIAN_POINT ( 'NONE',  ( -1.836970198721029983E-15, 50.62499999317203248, 10.00000000000000178 ) ) ;
#57397=CARTESIAN_POINT ( 'NONE',  ( -9.832129032723420536, 13.69791666325268409, 5.676582343749997150 ) ) ;
#57399=CARTESIAN_POINT ( 'NONE',  ( -11.35316468750000141, 203.5937499965860127, -1.390361679473963753E-15 ) ) ;
#57401=CARTESIAN_POINT ( 'NONE',  ( -7.320508075688778149, 219.9999999931720538, 7.320508075688769267 ) ) ;
#57404=VERTEX_POINT ( 'NONE', #11717 ) ;
#57407=CARTESIAN_POINT ( 'NONE',  ( -11.35316468750000141, 28.48958332991934839, 3.042071309553159963 ) ) ;
#57410=CARTESIAN_POINT ( 'NONE',  ( 7.320508075688771044, 209.3750000000000000, 7.320508075688775484 ) ) ;
#57412=CARTESIAN_POINT ( 'NONE',  ( 2.250000000000000444, 283.9999999999998863, 5.427273995025124975 ) ) ;
#57414=CARTESIAN_POINT ( 'NONE',  ( -11.35316468749999785, 18.07291666325267698, -3.042071309553167957 ) ) ;
#57416=CARTESIAN_POINT ( 'NONE',  ( -5.676582343750006032, 134.1145833299193555, 9.832129032723418760 ) ) ;
#57417=CARTESIAN_POINT ( 'NONE',  ( -10.00000000000000178, 104.3749999931720396, -1.224646799147353454E-15 ) ) ;
#57420=CARTESIAN_POINT ( 'NONE',  ( -5.000000000000005329, 5.208333326505366401, 8.660254037844387298 ) ) ;
#57424=CARTESIAN_POINT ( 'NONE',  ( -2.085542519210945728E-15, 9.843749996586018014, 11.35316468750000141 ) ) ;
#57426=CARTESIAN_POINT ( 'NONE',  ( 2.765530957081996366, 298.1406250017069510, -6.676582343750003368 ) ) ;
#57427=CARTESIAN_POINT ( 'NONE',  ( -8.311093377946841443, 123.9062499965860269, 8.311093377946834337 ) ) ;
#57438=CARTESIAN_POINT ( 'NONE',  ( -8.311093377946841443, 74.21874999658601268, 8.311093377946830785 ) ) ;
#57439=EDGE_LOOP ( 'NONE', ( #21806, #21796, #33002, #48405 ) ) ;
#57444=CARTESIAN_POINT ( 'NONE',  ( 8.248616681371277227E-12, 116.2499999999993747, -10.00000000000000178 ) ) ;
#57461=( BOUNDED_CURVE ( )  B_SPLINE_CURVE ( 2, ( #63572, #971, #29253, #11898, #23582, #64690, #6250, #41313, #42037, #35297, #17550, #59043, #6617 ),
 .UNSPECIFIED., .F., .F. ) 
 B_SPLINE_CURVE_WITH_KNOTS ( ( 3, 2, 2, 2, 2, 2, 3 ),
 ( 0.1358695652173912971, 0.1376811594202898559, 0.1394927536231884146, 0.1413043478260869179, 0.1431159420289854767, 0.1449275362318840354, 0.1467391304347825942 ),
 .UNSPECIFIED. ) 
 CURVE ( )  GEOMETRIC_REPRESENTATION_ITEM ( )  RATIONAL_B_SPLINE_CURVE ( ( 1.000000000000000000, 0.9659258262890683122, 1.000000000000000000, 0.9659258262890683122, 1.000000000000000000, 0.9659258262890683122, 1.000000000000000000, 0.9659258262890683122, 1.000000000000000000, 0.9659258262890683122, 1.000000000000000000, 0.9659258262890688673, 0.9999999999999994449 ) ) 
 REPRESENTATION_ITEM ( '' )  );
#57475=CARTESIAN_POINT ( 'NONE',  ( -10.00000000000000355, 77.70833333333332860, 2.679491924311223183 ) ) ;
#57477=CARTESIAN_POINT ( 'NONE',  ( 11.35316468749999963, 56.30208332991934839, -3.042071309553165293 ) ) ;
#57478=CARTESIAN_POINT ( 'NONE',  ( -6.676582343750003368, 298.5468750017069510, -2.765530957081996810 ) ) ;
#57485=CARTESIAN_POINT ( 'NONE',  ( 7.320508075688774596, 57.49999999317203248, -7.320508075688774596 ) ) ;
#57490=CARTESIAN_POINT ( 'NONE',  ( 10.00000000000000178, 195.2083333333333428, -2.679491924311226736 ) ) ;
#57492=CARTESIAN_POINT ( 'NONE',  ( 8.311093377946834337, 165.4687499965859843, 8.311093377946839666 ) ) ;
#57500=CARTESIAN_POINT ( 'NONE',  ( -2.085542519210945728E-15, 39.84374999658601979, 11.35316468750000141 ) ) ;
#57507=CARTESIAN_POINT ( 'NONE',  ( -7.320508075688773708, 68.74999999317201116, -7.320508075688774596 ) ) ;
#57510=CARTESIAN_POINT ( 'NONE',  ( 10.00000000000005151, 64.79166666666668561, 2.679491924311249385 ) ) ;
#57516=CARTESIAN_POINT ( 'NONE',  ( -6.676582343750000703, 297.6718750017070079, 2.765530957082001251 ) ) ;
#57517=CARTESIAN_POINT ( 'NONE',  ( -8.660254037844399733, 162.9166666666666856, 5.000000000000003553 ) ) ;
#57520=CARTESIAN_POINT ( 'NONE',  ( -5.676582343750006032, 144.1145833299193555, 9.832129032723418760 ) ) ;
#57521=CARTESIAN_POINT ( 'NONE',  ( 1.592277918221149080E-13, 106.2500000000000142, -10.00000000000000178 ) ) ;
#57530=CARTESIAN_POINT ( 'NONE',  ( 11.35316468750000141, 131.0937499965860127, 0.000000000000000000 ) ) ;
#57534=CARTESIAN_POINT ( 'NONE',  ( 6.951808397369818766E-16, 37.34374999658601979, -11.35316468750000141 ) ) ;
#57536=CARTESIAN_POINT ( 'NONE',  ( -2.679491924311227624, 26.45833333333333925, -10.00000000000000888 ) ) ;
#57541=CARTESIAN_POINT ( 'NONE',  ( 6.000000000000003553, 297.6250000034140726, -2.485281374238571761 ) ) ;
#57545=CARTESIAN_POINT ( 'NONE',  ( 8.311093377946834337, 160.4687499965860127, 8.311093377946839666 ) ) ;
#57548=EDGE_CURVE ( 'NONE', #46560, #16691, #17331, .T. ) ;
#57551=ORIENTED_EDGE ( 'NONE', *, *, #21440, .T. ) ;
#57560=CARTESIAN_POINT ( 'NONE',  ( -8.660254037844387298, 208.9583333265053682, -5.000000000000004441 ) ) ;
#57562=CARTESIAN_POINT ( 'NONE',  ( 10.00000000000000000, 39.79166666666667140, 2.679491924311236062 ) ) ;
#57568=ORIENTED_EDGE ( 'NONE', *, *, #65292, .T. ) ;
#57572=DIRECTION ( 'NONE',  ( -0.000000000000000000, 1.000000000000000000, -0.000000000000000000 ) ) ;
#57575=CARTESIAN_POINT ( 'NONE',  ( -7.320508075688773708, 161.8750000000000000, -7.320508075688774596 ) ) ;
#57578=CARTESIAN_POINT ( 'NONE',  ( 5.676582343750001591, 126.9270833299193697, -9.832129032723420536 ) ) ;
#57587=CARTESIAN_POINT ( 'NONE',  ( 5.000000000000055955, 195.8333333333334281, -8.660254037844481445 ) ) ;
#57590=CARTESIAN_POINT ( 'NONE',  ( -4.999999999999998224, 23.54166665983870033, -8.660254037844389075 ) ) ;
#57597=CARTESIAN_POINT ( 'NONE',  ( -9.832129032723420536, 108.6979166632526983, 5.676582343749997150 ) ) ;
#57603=CARTESIAN_POINT ( 'NONE',  ( 5.676582343750001591, 106.6145833299193555, -9.832129032723420536 ) ) ;
#57607=CARTESIAN_POINT ( 'NONE',  ( -1.836970198721029983E-15, 225.6249999931720254, 10.00000000000000178 ) ) ;
#57611=CARTESIAN_POINT ( 'NONE',  ( 3.042071309553159519, 104.7395833299193555, 11.35316468750000141 ) ) ;
#57614=CARTESIAN_POINT ( 'NONE',  ( -1.300830538084598961E-11, 173.7499999999989768, 10.00000000000000178 ) ) ;
#57617=CARTESIAN_POINT ( 'NONE',  ( -2.679491924311225848, 193.3333333265053966, -10.00000000000000178 ) ) ;
#57619=CARTESIAN_POINT ( 'NONE',  ( 8.311093377946837890, 86.71874999658601268, -8.311093377946837890 ) ) ;
#57620=CARTESIAN_POINT ( 'NONE',  ( 4.721056650416000089, 287.8281250017069510, 4.721056650415999201 ) ) ;
#57623=CARTESIAN_POINT ( 'NONE',  ( -5.676582343750006032, 219.1145833299193839, 9.832129032723418760 ) ) ;
#57627=CARTESIAN_POINT ( 'NONE',  ( -9.832129032723420536, 218.6979166632526983, 5.676582343749997150 ) ) ;
#57630=CARTESIAN_POINT ( 'NONE',  ( 2.765530957081996366, 296.1406250017070647, -6.676582343750003368 ) ) ;
#57634=CARTESIAN_POINT ( 'NONE',  ( -3.042071309553163960, 212.5520833299193839, -11.35316468749999963 ) ) ;
#57644=CARTESIAN_POINT ( 'NONE',  ( 7.320508075688774596, 30.62500000000000000, -7.320508075688774596 ) ) ;
#57655=CARTESIAN_POINT ( 'NONE',  ( -4.088227598258586603E-16, 296.2031250017070079, -6.676582343750001591 ) ) ;
#57658=CARTESIAN_POINT ( 'NONE',  ( -6.000000000000001776, 289.0625000034140157, 0.000000000000000000 ) ) ;
#57665=CARTESIAN_POINT ( 'NONE',  ( 9.832129032723420536, 91.51041666325268409, -5.676582343749999815 ) ) ;
#57670=CARTESIAN_POINT ( 'NONE',  ( 5.000000000000003553, 70.83333333333334281, -8.660254037844390851 ) ) ;
#57671=VERTEX_POINT ( 'NONE', #54687 ) ;
#57672=CARTESIAN_POINT ( 'NONE',  ( 2.679491924311296014, 75.83333332650536818, 9.999999999999959144 ) ) ;
#57673=CARTESIAN_POINT ( 'NONE',  ( -1.836970198721029983E-15, 180.6249999931720538, 10.00000000000000178 ) ) ;
#57674=CARTESIAN_POINT ( 'NONE',  ( -9.832129032723420536, 198.6979166632526983, 5.676582343749997150 ) ) ;
#57680=CARTESIAN_POINT ( 'NONE',  ( 9.832129032723416984, 175.6770833299193555, 5.676582343750006032 ) ) ;
#57684=CARTESIAN_POINT ( 'NONE',  ( -2.679491924311077966, 106.4583333333333144, -10.00000000000008171 ) ) ;
#57688=CARTESIAN_POINT ( 'NONE',  ( -11.35316468749999785, 63.07291666325268409, -3.042071309553167513 ) ) ;
#57694=CARTESIAN_POINT ( 'NONE',  ( 5.676582343750001591, 56.61458332991934839, -9.832129032723420536 ) ) ;
#57700=CARTESIAN_POINT ( 'NONE',  ( 6.951808397369818766E-16, 62.03124999658601979, -11.35316468750000141 ) ) ;
#57703=CIRCLE ( 'NONE', #37210, 6.000000000000001776 ) ;
#57704=CARTESIAN_POINT ( 'NONE',  ( -10.00000000000000178, 149.3749999931720538, -1.224646799147353454E-15 ) ) ;
#57707=CARTESIAN_POINT ( 'NONE',  ( -11.35316468749999785, 43.38541666325267698, -3.042071309553167957 ) ) ;
#57709=CARTESIAN_POINT ( 'NONE',  ( 8.311093377946837890, 176.4062499965859843, -8.311093377946837890 ) ) ;
#57710=EDGE_LOOP ( 'NONE', ( #59268, #50065, #35392, #264 ) ) ;
#57715=CARTESIAN_POINT ( 'NONE',  ( -3.042071309553173730, 174.3229166632526983, 11.35316468749999785 ) ) ;
#57722=CARTESIAN_POINT ( 'NONE',  ( 5.676582343749993598, 165.2604166632526983, 9.832129032723422313 ) ) ;
#57724=CARTESIAN_POINT ( 'NONE',  ( -5.676582343750006032, 134.4270833299193555, 9.832129032723418760 ) ) ;
#57725=CARTESIAN_POINT ( 'NONE',  ( 2.249999999999997335, 255.9999999999998295, 5.427273999917215264 ) ) ;
#57729=EDGE_CURVE ( 'NONE', #14276, #31901, #9026, .T. ) ;
#57739=ORIENTED_EDGE ( 'NONE', *, *, #7189, .T. ) ;
#57740=CARTESIAN_POINT ( 'NONE',  ( -8.660254037844435260, 177.0833333333333712, -5.000000000000031086 ) ) ;
#57751=DIRECTION ( 'NONE',  ( -0.000000000000000000, 1.000000000000000000, -0.000000000000000000 ) ) ;
#57756=CARTESIAN_POINT ( 'NONE',  ( -6.676582343750002480, 299.5468750017069510, -2.765530957081996810 ) ) ;
#57757=CARTESIAN_POINT ( 'NONE',  ( 2.679491924311222739, 138.9583333333333712, 10.00000000000000355 ) ) ;
#57759=CARTESIAN_POINT ( 'NONE',  ( 2.765530957082001251, 288.9218750017069510, 6.676582343750000703 ) ) ;
#57774=CARTESIAN_POINT ( 'NONE',  ( 3.042071309553167069, 21.82291666325268054, -11.35316468749999785 ) ) ;
#57776=CARTESIAN_POINT ( 'NONE',  ( 5.676582343749993598, 225.2604166632526983, 9.832129032723422313 ) ) ;
#57779=CARTESIAN_POINT ( 'NONE',  ( -8.660254037844532959, 42.91666666666677088, 5.000000000000080824 ) ) ;
#57783=CARTESIAN_POINT ( 'NONE',  ( -8.311093377946841443, 18.90624999658601624, 8.311093377946830785 ) ) ;
#57788=CARTESIAN_POINT ( 'NONE',  ( 5.676582343750001591, 21.61458332991935194, -9.832129032723420536 ) ) ;
#57790=CARTESIAN_POINT ( 'NONE',  ( -11.35316468750000141, 138.4895833299193271, 3.042071309553159963 ) ) ;
#57792=CARTESIAN_POINT ( 'NONE',  ( 2.679491924311222739, 110.8333333265053824, 10.00000000000000355 ) ) ;
#57794=CARTESIAN_POINT ( 'NONE',  ( -4.999999999999998224, 3.541666659838699438, -8.660254037844389075 ) ) ;
#57798=CARTESIAN_POINT ( 'NONE',  ( -8.311093377946836114, 12.96874999658601446, -8.311093377946837890 ) ) ;
#57799=( BOUNDED_CURVE ( )  B_SPLINE_CURVE ( 2, ( #40487, #6898, #40860, #29909, #63492, #63119, #24235, #52551, #52924 ),
 .UNSPECIFIED., .F., .F. ) 
 B_SPLINE_CURVE_WITH_KNOTS ( ( 3, 2, 2, 2, 3 ),
 ( 0.5624999999999981126, 0.5729166666666647423, 0.5833333333333314830, 0.5937499999999982236, 0.6041666666666648533 ),
 .UNSPECIFIED. ) 
 CURVE ( )  GEOMETRIC_REPRESENTATION_ITEM ( )  RATIONAL_B_SPLINE_CURVE ( ( 1.000000000000013767, 0.9238795325112729717, 1.000000000000000000, 0.9238795325112867385, 1.000000000000000000, 0.9238795325112867385, 1.000000000000000000, 0.9238795325112997281, 0.9999999999999870104 ) ) 
 REPRESENTATION_ITEM ( '' )  );
#57801=CARTESIAN_POINT ( 'NONE',  ( -2.765530957081996810, 296.2656250017069510, -6.676582343750003368 ) ) ;
#57802=CARTESIAN_POINT ( 'NONE',  ( 6.951808397369818766E-16, 137.0312499965860411, -11.35316468750000141 ) ) ;
#57805=CYLINDRICAL_SURFACE ( 'NONE', #15223, 10.00000000000000178 ) ;
#57814=CARTESIAN_POINT ( 'NONE',  ( -8.311093377946841443, 84.21874999658599847, 8.311093377946830785 ) ) ;
#57815=VERTEX_POINT ( 'NONE', #53082 ) ;
#57818=VERTEX_POINT ( 'NONE', #19470 ) ;
#57827=CARTESIAN_POINT ( 'NONE',  ( 9.999999999999996447, 110.0000000000000000, 0.000000000000000000 ) ) ;
#57847=CARTESIAN_POINT ( 'NONE',  ( -8.660254037844390851, 87.91666666666667140, 4.999999999999998224 ) ) ;
#57849=CARTESIAN_POINT ( 'NONE',  ( 11.35316468750000141, 66.09374999658601268, 0.000000000000000000 ) ) ;
#57850=CARTESIAN_POINT ( 'NONE',  ( -4.242640687119285658, 288.1249999999999432, 4.242640687119287435 ) ) ;
#57855=CARTESIAN_POINT ( 'NONE',  ( 8.660254037844396180, 85.41666666666668561, -5.000000000000005329 ) ) ;
#57860=CARTESIAN_POINT ( 'NONE',  ( -10.00000000000000178, 207.5000000000000284, -1.224646799147353454E-15 ) ) ;
#57862=CARTESIAN_POINT ( 'NONE',  ( 8.311093377946834337, 180.4687499965859843, 8.311093377946839666 ) ) ;
#57863=CARTESIAN_POINT ( 'NONE',  ( -10.00000000000022204, 212.2916666666667993, -2.679491924311289797 ) ) ;
#57867=ORIENTED_EDGE ( 'NONE', *, *, #35040, .F. ) ;
#57869=CARTESIAN_POINT ( 'NONE',  ( 5.676582343750001591, 36.92708332991935549, -9.832129032723420536 ) ) ;
#57877=CARTESIAN_POINT ( 'NONE',  ( -5.000000000000005329, 65.20833332650536818, 8.660254037844387298 ) ) ;
#57880=CARTESIAN_POINT ( 'NONE',  ( 5.000000000000027534, 65.83333333333337123, -8.660254037844433483 ) ) ;
#57886=CARTESIAN_POINT ( 'NONE',  ( -6.676582343750003368, 297.5468750017069510, -2.765530957081996810 ) ) ;
#57888=CARTESIAN_POINT ( 'NONE',  ( -7.320508075688771932, 86.87500000000001421, -7.320508075688773708 ) ) ;
#57889=CARTESIAN_POINT ( 'NONE',  ( 5.676582343749993598, 159.9479166632526983, 9.832129032723422313 ) ) ;
#57901=CARTESIAN_POINT ( 'NONE',  ( 3.042071309553159519, 135.0520833299193555, 11.35316468750000141 ) ) ;
#57905=CARTESIAN_POINT ( 'NONE',  ( -11.35316468750000141, 48.80208332991934128, 3.042071309553159963 ) ) ;
#57914=CARTESIAN_POINT ( 'NONE',  ( -4.242640687119285658, 297.1875000034139589, 4.242640687119287435 ) ) ;
#57935=ADVANCED_FACE ( 'NONE', ( #33998 ), #57367, .T. ) ;
#57940=CARTESIAN_POINT ( 'NONE',  ( -8.660254037844387298, 47.08333333333333570, -5.000000000000004441 ) ) ;
#57944=CARTESIAN_POINT ( 'NONE',  ( -6.000000000000003553, 288.0000000034140157, -2.485281374238571317 ) ) ;
#57945=CARTESIAN_POINT ( 'NONE',  ( 10.00000000000000178, 196.8749999931720254, 0.000000000000000000 ) ) ;
#57950=CARTESIAN_POINT ( 'NONE',  ( 2.679491924310923867, 88.95833333333327175, 10.00000000000015454 ) ) ;
#57953=CARTESIAN_POINT ( 'NONE',  ( 10.00000000000000178, 160.0000000000000000, 0.000000000000000000 ) ) ;
#57957=CARTESIAN_POINT ( 'NONE',  ( -11.35316468750000141, 133.5937499965860127, -1.390361679473963753E-15 ) ) ;
#57968=CARTESIAN_POINT ( 'NONE',  ( 10.00000000000010658, 194.7916666666667425, 2.679491924311264039 ) ) ;
#57970=CARTESIAN_POINT ( 'NONE',  ( -7.320508075688778149, 24.99999999317203603, 7.320508075688769267 ) ) ;
#57977=CARTESIAN_POINT ( 'NONE',  ( -8.311093377946841443, 103.9062499965860269, 8.311093377946830785 ) ) ;
#57981=DIRECTION ( 'NONE',  ( -0.000000000000000000, 1.000000000000000000, -0.000000000000000000 ) ) ;
#57985=CARTESIAN_POINT ( 'NONE',  ( -11.35316468749999785, 113.0729166632526841, -3.042071309553167513 ) ) ;
#57989=CARTESIAN_POINT ( 'NONE',  ( -8.660254037844387298, 213.9583333265053682, -5.000000000000004441 ) ) ;
#57992=CARTESIAN_POINT ( 'NONE',  ( -8.660254037844385522, 182.0833333333333712, -5.000000000000003553 ) ) ;
#57993=CARTESIAN_POINT ( 'NONE',  ( -9.832129032723420536, 103.6979166632526841, 5.676582343749997150 ) ) ;
#57997=ORIENTED_EDGE ( 'NONE', *, *, #70464, .T. ) ;
#57998=CARTESIAN_POINT ( 'NONE',  ( 2.679491924311222739, 195.8333333265053682, 10.00000000000000355 ) ) ;
#58001=CARTESIAN_POINT ( 'NONE',  ( -8.311093377946841443, 94.21874999658601268, 8.311093377946834337 ) ) ;
#58006=CARTESIAN_POINT ( 'NONE',  ( -5.676582343749998039, 217.4479166632526983, -9.832129032723420536 ) ) ;
#58008=CARTESIAN_POINT ( 'NONE',  ( -7.320508075688786143, 138.1250000000000000, 7.320508075688777261 ) ) ;
#58010=CARTESIAN_POINT ( 'NONE',  ( -11.35316468750000141, 218.2812499965860411, -1.390361679473963753E-15 ) ) ;
#58015=CARTESIAN_POINT ( 'NONE',  ( 2.765530957082001251, 298.7656250017069510, 6.676582343750000703 ) ) ;
#58016=ORIENTED_EDGE ( 'NONE', *, *, #66554, .T. ) ;
#58018=CARTESIAN_POINT ( 'NONE',  ( -11.35316468750000141, 208.5937499965860411, -1.390361679473963753E-15 ) ) ;
#58025=CARTESIAN_POINT ( 'NONE',  ( -4.999999999999998224, 26.66666666666666785, -8.660254037844389075 ) ) ;
#58028=ORIENTED_EDGE ( 'NONE', *, *, #70566, .T. ) ;
#58034=CARTESIAN_POINT ( 'NONE',  ( 2.679491924311228956, 152.9166666598387394, -10.00000000000000000 ) ) ;
#58035=CARTESIAN_POINT ( 'NONE',  ( 4.721056650416000089, 297.8281250017069510, 4.721056650415999201 ) ) ;
#58037=ORIENTED_EDGE ( 'NONE', *, *, #61369, .T. ) ;
#58042=CARTESIAN_POINT ( 'NONE',  ( 5.676582343750001591, 81.92708332991935549, -9.832129032723420536 ) ) ;
#58048=ORIENTED_EDGE ( 'NONE', *, *, #45031, .T. ) ;
#58053=CARTESIAN_POINT ( 'NONE',  ( 8.311093377946834337, 205.1562499965859843, 8.311093377946839666 ) ) ;
#58057=CARTESIAN_POINT ( 'NONE',  ( 3.042071309553159519, 175.0520833299193839, 11.35316468750000141 ) ) ;
#58060=CARTESIAN_POINT ( 'NONE',  ( -7.320508075688769267, 106.8750000000000284, -7.320508075688770155 ) ) ;
#58064=CARTESIAN_POINT ( 'NONE',  ( -3.042071309553164404, 62.23958332991934839, -11.35316468749999963 ) ) ;
#58068=VERTEX_POINT ( 'NONE', #33619 ) ;
#58071=CARTESIAN_POINT ( 'NONE',  ( -5.676582343750006032, 64.11458332991935549, 9.832129032723418760 ) ) ;
#58076=CARTESIAN_POINT ( 'NONE',  ( 5.676582343749993598, 54.94791666325268409, 9.832129032723422313 ) ) ;
#58078=CARTESIAN_POINT ( 'NONE',  ( -10.00000000000000178, 14.37499999317203425, -1.224646799147353454E-15 ) ) ;
#58079=CARTESIAN_POINT ( 'NONE',  ( -4.999999999999998224, 153.5416666598387110, -8.660254037844389075 ) ) ;
#58082=CARTESIAN_POINT ( 'NONE',  ( -9.832129032723420536, 54.01041666325268409, 5.676582343749997150 ) ) ;
#58084=CARTESIAN_POINT ( 'NONE',  ( 11.35316468749999785, 185.5729166632526983, 3.042071309553174174 ) ) ;
#58088=CARTESIAN_POINT ( 'NONE',  ( 6.123233995736767268E-16, 63.12499999317203248, -10.00000000000000178 ) ) ;
#58090=CARTESIAN_POINT ( 'NONE',  ( 5.676582343749993598, 174.9479166632526699, 9.832129032723422313 ) ) ;
#58095=CARTESIAN_POINT ( 'NONE',  ( 11.35316468749999963, 166.3020833299193271, -3.042071309553165293 ) ) ;
#58097=CARTESIAN_POINT ( 'NONE',  ( 11.35316468750000141, 136.0937499965860127, 0.000000000000000000 ) ) ;
#58109=CARTESIAN_POINT ( 'NONE',  ( -2.220555325575947149E-11, 176.2500000000017621, -10.00000000000000533 ) ) ;
#58121=VERTEX_POINT ( 'NONE', #7891 ) ;
#58130=CARTESIAN_POINT ( 'NONE',  ( 1.226468279477575784E-15, 296.8593750017070079, 6.676582343750001591 ) ) ;
#58131=CARTESIAN_POINT ( 'NONE',  ( 7.320508075688774596, 130.6250000000000284, -7.320508075688774596 ) ) ;
#58135=CARTESIAN_POINT ( 'NONE',  ( -4.721056650415998313, 288.7343750017069510, 4.721056650416000089 ) ) ;
#58138=VECTOR ( 'NONE', #3698, 1000.000000000000000 ) ;
#58148=CARTESIAN_POINT ( 'NONE',  ( 7.320508075688774596, 52.49999999317203958, -7.320508075688774596 ) ) ;
#58150=CARTESIAN_POINT ( 'NONE',  ( -11.35316468750000141, 23.48958332991934483, 3.042071309553159963 ) ) ;
#58151=CARTESIAN_POINT ( 'NONE',  ( -11.35316468750000141, 223.5937499965860127, -1.390361679473963753E-15 ) ) ;
#58158=CARTESIAN_POINT ( 'NONE',  ( -8.311093377946841443, 28.90624999658601979, 8.311093377946830785 ) ) ;
#58162=CARTESIAN_POINT ( 'NONE',  ( -5.000000000000001776, 151.6666666666666856, -8.660254037844394404 ) ) ;
#58163=CARTESIAN_POINT ( 'NONE',  ( 0.000000000000000000, 300.0000000000000000, 10.00000000000000178 ) ) ;
#58165=CARTESIAN_POINT ( 'NONE',  ( -8.311093377946841443, 18.90624999658601979, 8.311093377946834337 ) ) ;
#58168=CARTESIAN_POINT ( 'NONE',  ( -2.085542519210945728E-15, 154.5312499965860127, 11.35316468750000141 ) ) ;
#58169=CARTESIAN_POINT ( 'NONE',  ( 7.320508075688771044, 121.2499999931720254, 7.320508075688775484 ) ) ;
#58174=CARTESIAN_POINT ( 'NONE',  ( 3.042071309553167513, 2.135416663252682756, -11.35316468749999785 ) ) ;
#58176=CYLINDRICAL_SURFACE ( 'NONE', #54656, 6.000000000000001776 ) ;
#58177=CARTESIAN_POINT ( 'NONE',  ( 2.765530957081996366, 299.1406250017068942, -6.676582343750003368 ) ) ;
#58178=CARTESIAN_POINT ( 'NONE',  ( -9.832129032723420536, 143.6979166632526699, 5.676582343749997150 ) ) ;
#58186=DIRECTION ( 'NONE',  ( -0.000000000000000000, 1.000000000000000000, -0.000000000000000000 ) ) ;
#58188=CARTESIAN_POINT ( 'NONE',  ( -5.676582343749998039, 87.76041666325268409, -9.832129032723420536 ) ) ;
#58193=EDGE_LOOP ( 'NONE', ( #26909, #39567, #34033, #20222 ) ) ;
#58204=EDGE_CURVE ( 'NONE', #39497, #14172, #71295, .T. ) ;
#58205=ADVANCED_FACE ( 'NONE', ( #53913 ), #19566, .T. ) ;
#58211=CARTESIAN_POINT ( 'NONE',  ( -1.966770576099810657E-11, 61.25000000000153477, -9.999999999999998224 ) ) ;
#58217=CARTESIAN_POINT ( 'NONE',  ( -9.999999999999991118, 97.70833333333332860, 2.679491924311220075 ) ) ;
#58221=CARTESIAN_POINT ( 'NONE',  ( -10.00000000000000000, 97.29166666666667140, -2.679491924311229845 ) ) ;
#58225=CARTESIAN_POINT ( 'NONE',  ( -3.042071309553164404, 67.55208332991935549, -11.35316468749999963 ) ) ;
#58226=CARTESIAN_POINT ( 'NONE',  ( 1.226468279477575784E-15, 298.8593750017070079, 6.676582343750001591 ) ) ;
#58228=EDGE_CURVE ( 'NONE', #49691, #37587, #41365, .T. ) ;
#58232=CARTESIAN_POINT ( 'NONE',  ( -5.000000000000005329, 105.2083333265053824, 8.660254037844387298 ) ) ;
#58237=CARTESIAN_POINT ( 'NONE',  ( -5.000000000000005329, 213.3333333333333428, 8.660254037844387298 ) ) ;
#58240=CARTESIAN_POINT ( 'NONE',  ( -3.042071309553164404, 187.5520833299193555, -11.35316468749999963 ) ) ;
#58246=CARTESIAN_POINT ( 'NONE',  ( 3.042071309553159519, 40.05208332991935549, 11.35316468750000141 ) ) ;
#58248=EDGE_CURVE ( 'NONE', #71793, #68916, #67471, .T. ) ;
#58251=CARTESIAN_POINT ( 'NONE',  ( 6.123233995736767268E-16, 223.1249999931720254, -10.00000000000000178 ) ) ;
#58253=CARTESIAN_POINT ( 'NONE',  ( 6.123233995736767268E-16, 73.12499999317203958, -10.00000000000000178 ) ) ;
#58256=CARTESIAN_POINT ( 'NONE',  ( 7.320508075688936245, 215.6250000000001421, -7.320508075688936245 ) ) ;
#58261=CARTESIAN_POINT ( 'NONE',  ( -4.721056650415998313, 298.7343750017069510, 4.721056650416000089 ) ) ;
#58264=VECTOR ( 'NONE', #37594, 1000.000000000000000 ) ;
#58265=CARTESIAN_POINT ( 'NONE',  ( -3.042071309553173730, 159.3229166632526699, 11.35316468749999785 ) ) ;
#58267=CYLINDRICAL_SURFACE ( 'NONE', #15183, 10.00000000000000178 ) ;
#58274=CARTESIAN_POINT ( 'NONE',  ( -11.35316468749999785, 123.3854166632526699, -3.042071309553167957 ) ) ;
#58278=CARTESIAN_POINT ( 'NONE',  ( 8.311093377946834337, 50.46874999658601979, 8.311093377946839666 ) ) ;
#58284=CARTESIAN_POINT ( 'NONE',  ( -6.000000000000000888, 292.1250000034140157, 2.485281374238575758 ) ) ;
#58291=CARTESIAN_POINT ( 'NONE',  ( -8.660254037844387298, 63.95833332650536818, -5.000000000000004441 ) ) ;
#58293=ORIENTED_EDGE ( 'NONE', *, *, #56884, .T. ) ;
#58303=ORIENTED_EDGE ( 'NONE', *, *, #12241, .T. ) ;
#58306=CARTESIAN_POINT ( 'NONE',  ( 10.00000000000000178, 50.00000000000000000, 0.000000000000000000 ) ) ;
#58310=CARTESIAN_POINT ( 'NONE',  ( -6.000000000000003553, 298.9375000000000000, -2.485281374238571317 ) ) ;
#58311=CARTESIAN_POINT ( 'NONE',  ( 1.224646799147353454E-15, 300.0000000000000000, -10.00000000000000178 ) ) ;
#58316=CARTESIAN_POINT ( 'NONE',  ( 9.999999999999985789, 90.00000000000001421, 0.000000000000000000 ) ) ;
#58318=CARTESIAN_POINT ( 'NONE',  ( -4.999999999999998224, 146.6666666666666572, -8.660254037844389075 ) ) ;
#58320=CARTESIAN_POINT ( 'NONE',  ( 7.320508075688774596, 165.6250000000000284, -7.320508075688774596 ) ) ;
#58324=CARTESIAN_POINT ( 'NONE',  ( -3.042071309553164404, 137.5520833299193555, -11.35316468749999963 ) ) ;
#58338=CARTESIAN_POINT ( 'NONE',  ( 2.679491924311228956, 32.91666665983868967, -10.00000000000000000 ) ) ;
#58346=DIRECTION ( 'NONE',  ( 0.000000000000000000, -0.000000000000000000, 1.000000000000000000 ) ) ;
#58348=CARTESIAN_POINT ( 'NONE',  ( -10.00000000000005329, 62.29166666666670693, -2.679491924311244944 ) ) ;
#58350=CARTESIAN_POINT ( 'NONE',  ( 11.35316468749999785, 120.5729166632526699, 3.042071309553174174 ) ) ;
#58354=CARTESIAN_POINT ( 'NONE',  ( -1.836970198721029983E-15, 220.6249999931720538, 10.00000000000000178 ) ) ;
#58357=CARTESIAN_POINT ( 'NONE',  ( -8.660254037844389075, 182.9166666666666856, 4.999999999999997335 ) ) ;
#58358=CARTESIAN_POINT ( 'NONE',  ( 9.832129032723420536, 101.1979166632526841, -5.676582343749999815 ) ) ;
#58362=CARTESIAN_POINT ( 'NONE',  ( -10.00000000000000000, 194.1666666598387110, -2.679491924311229845 ) ) ;
#58366=CARTESIAN_POINT ( 'NONE',  ( -11.35316468750000141, 83.80208332991934128, 3.042071309553159963 ) ) ;
#58370=CARTESIAN_POINT ( 'NONE',  ( -5.676582343750006032, 14.42708332991935016, 9.832129032723418760 ) ) ;
#58371=ORIENTED_EDGE ( 'NONE', *, *, #38360, .F. ) ;
#58374=CARTESIAN_POINT ( 'NONE',  ( -11.35316468750000141, 213.2812499965860411, -1.390361679473963753E-15 ) ) ;
#58379=CARTESIAN_POINT ( 'NONE',  ( 6.676582343750001591, 295.9531250017069510, -8.176455196517173205E-16 ) ) ;
#58382=CARTESIAN_POINT ( 'NONE',  ( 11.35316468749999963, 211.3020833299193839, -3.042071309553165293 ) ) ;
#58390=CARTESIAN_POINT ( 'NONE',  ( 2.679491924311222739, 28.95833333333333215, 10.00000000000000355 ) ) ;
#58400=CARTESIAN_POINT ( 'NONE',  ( 6.676582343750002480, 296.0156250017069510, -2.765530957081997254 ) ) ;
#58409=CARTESIAN_POINT ( 'NONE',  ( 9.832129032723420536, 101.5104166632526841, -5.676582343749999815 ) ) ;
#58418=CARTESIAN_POINT ( 'NONE',  ( 9.832129032723420536, 211.1979166632526983, -5.676582343749999815 ) ) ;
#58423=CARTESIAN_POINT ( 'NONE',  ( -3.042071309553164404, 177.5520833299193839, -11.35316468749999963 ) ) ;
#58425=DIRECTION ( 'NONE',  ( -0.000000000000000000, 1.000000000000000000, -0.000000000000000000 ) ) ;
#58429=CARTESIAN_POINT ( 'NONE',  ( -8.311093377946836114, 67.65624999658599847, -8.311093377946837890 ) ) ;
#58430=DIRECTION ( 'NONE',  ( 0.000000000000000000, 0.000000000000000000, 1.000000000000000000 ) ) ;
#58432=ORIENTED_EDGE ( 'NONE', *, *, #11362, .F. ) ;
#58434=CARTESIAN_POINT ( 'NONE',  ( -11.35316468750000141, 78.48958332991935549, 3.042071309553159963 ) ) ;
#58439=CARTESIAN_POINT ( 'NONE',  ( -8.311093377946841443, 53.90624999658601979, 8.311093377946834337 ) ) ;
#58442=DIRECTION ( 'NONE',  ( -0.000000000000000000, 1.000000000000000000, -0.000000000000000000 ) ) ;
#58443=CARTESIAN_POINT ( 'NONE',  ( 7.320508075688774596, 152.4999999931720538, -7.320508075688774596 ) ) ;
#58445=CARTESIAN_POINT ( 'NONE',  ( 10.00000000000001066, 20.00000000000000355, 0.000000000000000000 ) ) ;
#58446=CARTESIAN_POINT ( 'NONE',  ( -8.311093377946841443, 49.21874999658600558, 8.311093377946834337 ) ) ;
#58449=CARTESIAN_POINT ( 'NONE',  ( 11.35316468749999963, 190.9895833299193271, -3.042071309553165293 ) ) ;
#58456=CARTESIAN_POINT ( 'NONE',  ( -2.085542519210945728E-15, 174.5312499965860411, 11.35316468750000141 ) ) ;
#58457=CARTESIAN_POINT ( 'NONE',  ( 2.250000000000000444, 283.9999999999998863, 5.427273995025124975 ) ) ;
#58461=CARTESIAN_POINT ( 'NONE',  ( 3.042071309553167513, 167.1354166632526699, -11.35316468749999785 ) ) ;
#58463=CARTESIAN_POINT ( 'NONE',  ( -11.35316468750000141, 123.8020833299193271, 3.042071309553159963 ) ) ;
#58475=CARTESIAN_POINT ( 'NONE',  ( -10.00000000000005329, 177.2916666666667140, -2.679491924311244944 ) ) ;
#58492=CARTESIAN_POINT ( 'NONE',  ( -6.676582343750001591, 296.6093750017069510, 0.000000000000000000 ) ) ;
#58493=CARTESIAN_POINT ( 'NONE',  ( 6.123233995736767268E-16, 136.2500000000000000, -10.00000000000000178 ) ) ;
#58506=CARTESIAN_POINT ( 'NONE',  ( 7.320508075688771044, 51.24999999317203248, 7.320508075688775484 ) ) ;
#58509=CARTESIAN_POINT ( 'NONE',  ( -11.35316468749999785, 23.07291666325268054, -3.042071309553167513 ) ) ;
#58511=CARTESIAN_POINT ( 'NONE',  ( 9.832129032723420536, 216.5104166632526983, -5.676582343749999815 ) ) ;
#58512=FACE_OUTER_BOUND ( 'NONE', #9547, .T. ) ;
#58517=CARTESIAN_POINT ( 'NONE',  ( -9.832129032723420536, 33.69791666325268409, 5.676582343749997150 ) ) ;
#58523=CARTESIAN_POINT ( 'NONE',  ( -11.35316468750000141, 18.48958332991934483, 3.042071309553159963 ) ) ;
#58525=CARTESIAN_POINT ( 'NONE',  ( -9.832129032723420536, 148.6979166632526983, 5.676582343749997150 ) ) ;
#58526=CARTESIAN_POINT ( 'NONE',  ( -7.320508075688778149, 119.9999999931720396, 7.320508075688769267 ) ) ;
#58531=CARTESIAN_POINT ( 'NONE',  ( -8.311093377946841443, 4.218749996586016238, 8.311093377946834337 ) ) ;
#58534=CARTESIAN_POINT ( 'NONE',  ( 1.226468279477575784E-15, 297.7031250017070079, 6.676582343750001591 ) ) ;
#58536=CARTESIAN_POINT ( 'NONE',  ( 8.311093377946837890, 141.4062499965860127, -8.311093377946837890 ) ) ;
#58548=CARTESIAN_POINT ( 'NONE',  ( 10.00000000000000533, 120.2083333333333428, -2.679491924311227624 ) ) ;
#58550=CARTESIAN_POINT ( 'NONE',  ( 9.832129032723420536, 91.51041666325268409, -5.676582343749999815 ) ) ;
#58554=ORIENTED_EDGE ( 'NONE', *, *, #51625, .T. ) ;
#58568=CARTESIAN_POINT ( 'NONE',  ( -10.00000000000033218, 22.50000000000019185, -1.224646799147393686E-15 ) ) ;
#58579=CARTESIAN_POINT ( 'NONE',  ( 7.320508075688771044, 94.37500000000000000, 7.320508075688775484 ) ) ;
#58581=CARTESIAN_POINT ( 'NONE',  ( -8.311093377946841443, 64.21874999658601268, 8.311093377946830785 ) ) ;
#58582=CARTESIAN_POINT ( 'NONE',  ( 4.721056650415999201, 297.2343750017069510, -4.721056650415999201 ) ) ;
#58585=CARTESIAN_POINT ( 'NONE',  ( -2.679491924311087736, 145.4166666598386826, 10.00000000000008349 ) ) ;
#58586=AXIS2_PLACEMENT_3D ( 'NONE', #48359, #1629, #2350 ) ;
#58589=CARTESIAN_POINT ( 'NONE',  ( 5.000000000000007105, 85.83333333333335702, -8.660254037844396180 ) ) ;
#58594=CARTESIAN_POINT ( 'NONE',  ( 4.999999999999993783, 209.1666666666666572, 8.660254037844390851 ) ) ;
#58596=CARTESIAN_POINT ( 'NONE',  ( -8.311093377946836114, 187.9687499965860411, -8.311093377946837890 ) ) ;
#58598=CARTESIAN_POINT ( 'NONE',  ( 6.123233995736767268E-16, 178.1249999931720538, -10.00000000000000178 ) ) ;
#58603=CARTESIAN_POINT ( 'NONE',  ( -3.042071309553164404, 32.55208332991934128, -11.35316468749999963 ) ) ;
#58605=CARTESIAN_POINT ( 'NONE',  ( 11.35316468750000141, 221.0937499965860127, 0.000000000000000000 ) ) ;
#58607=CARTESIAN_POINT ( 'NONE',  ( -1.836970198721029983E-15, 125.6249999931720254, 10.00000000000000178 ) ) ;
#58611=VECTOR ( 'NONE', #37081, 1000.000000000000000 ) ;
#58613=CARTESIAN_POINT ( 'NONE',  ( 10.00000000000000000, 81.66666665983869677, 2.679491924311236062 ) ) ;
#58621=CARTESIAN_POINT ( 'NONE',  ( -6.676582343750003368, 299.5468750017069510, -2.765530957081996810 ) ) ;
#58622=CARTESIAN_POINT ( 'NONE',  ( -2.679491924311376838, 141.4583333333333428, -9.999999999999928946 ) ) ;
#58624=CARTESIAN_POINT ( 'NONE',  ( -9.832129032723420536, 158.6979166632526983, 5.676582343749997150 ) ) ;
#58632=CARTESIAN_POINT ( 'NONE',  ( -3.042071309553173730, 139.6354166632526699, 11.35316468749999785 ) ) ;
#58636=CARTESIAN_POINT ( 'NONE',  ( -11.35316468749999785, 48.38541666325268409, -3.042071309553167513 ) ) ;
#58638=CARTESIAN_POINT ( 'NONE',  ( -8.660254037844390851, 27.08333333333333925, -5.000000000000007994 ) ) ;
#58644=CARTESIAN_POINT ( 'NONE',  ( -6.000000000000001776, 293.0625000034140157, 0.000000000000000000 ) ) ;
#58651=CARTESIAN_POINT ( 'NONE',  ( 6.123233995736767268E-16, 63.12499999317203248, -10.00000000000000178 ) ) ;
#58668=CARTESIAN_POINT ( 'NONE',  ( -4.999999999999998224, 56.66666666666667140, -8.660254037844389075 ) ) ;
#58677=LINE ( 'NONE', #6986, #48660 ) ;
#58682=CARTESIAN_POINT ( 'NONE',  ( -7.320508075688773708, 176.8750000000000000, -7.320508075688774596 ) ) ;
#58686=CARTESIAN_POINT ( 'NONE',  ( -11.35316468749999785, 143.3854166632526983, -3.042071309553167513 ) ) ;
#58691=CARTESIAN_POINT ( 'NONE',  ( -8.660254037844390851, 167.9166666666666856, 5.000000000000000000 ) ) ;
#58694=CARTESIAN_POINT ( 'NONE',  ( -11.35316468749999785, 3.385416663252682756, -3.042071309553167513 ) ) ;
#58698=CARTESIAN_POINT ( 'NONE',  ( -8.660254037844387298, 33.95833332650536818, -5.000000000000004441 ) ) ;
#58705=ORIENTED_EDGE ( 'NONE', *, *, #33607, .T. ) ;
#58707=CARTESIAN_POINT ( 'NONE',  ( -9.999960627438866823, 226.0000000000000284, -0.6562093533521858868 ) ) ;
#58710=CARTESIAN_POINT ( 'NONE',  ( -5.676582343749998039, 112.4479166632526983, -9.832129032723420536 ) ) ;
#58712=EDGE_CURVE ( 'NONE', #27943, #1761, #60286, .T. ) ;
#58719=CARTESIAN_POINT ( 'NONE',  ( 11.35316468750000141, 115.7812499965860269, 0.000000000000000000 ) ) ;
#58722=CARTESIAN_POINT ( 'NONE',  ( 2.679491924311370177, 145.8333333265053966, 9.999999999999918288 ) ) ;
#58725=CARTESIAN_POINT ( 'NONE',  ( 7.320508075688771044, 191.2499999931720538, 7.320508075688775484 ) ) ;
#58728=CARTESIAN_POINT ( 'NONE',  ( 11.35316468750000141, 96.09374999658601268, 0.000000000000000000 ) ) ;
#58732=CARTESIAN_POINT ( 'NONE',  ( 11.35316468749999785, 10.88541666325268586, 3.042071309553174174 ) ) ;
#58736=CARTESIAN_POINT ( 'NONE',  ( -5.676582343749998039, 217.4479166632526983, -9.832129032723420536 ) ) ;
#58741=CARTESIAN_POINT ( 'NONE',  ( -4.721056650415999201, 291.3281250017069510, -4.721056650415999201 ) ) ;
#58744=CARTESIAN_POINT ( 'NONE',  ( 11.35316468750000141, 211.0937499965860411, 0.000000000000000000 ) ) ;
#58753=CARTESIAN_POINT ( 'NONE',  ( 10.00000000000000178, 30.00000000000000355, 0.000000000000000000 ) ) ;
#58757=DIRECTION ( 'NONE',  ( -0.000000000000000000, 1.000000000000000000, -0.000000000000000000 ) ) ;
#58759=EDGE_CURVE ( 'NONE', #51786, #68916, #8722, .T. ) ;
#58762=CARTESIAN_POINT ( 'NONE',  ( 0.4589999999999999636, 261.4319999999996753, 5.805285082142985331 ) ) ;
#58763=CARTESIAN_POINT ( 'NONE',  ( 4.721056650416000089, 295.8281250017069510, 4.721056650415999201 ) ) ;
#58767=( BOUNDED_CURVE ( )  B_SPLINE_CURVE ( 2, ( #34845, #69901, #40107, #35212, #63113, #23493, #51422, #63860, #28414 ),
 .UNSPECIFIED., .F., .F. ) 
 B_SPLINE_CURVE_WITH_KNOTS ( ( 3, 2, 2, 2, 3 ),
 ( 0.4374999999999980571, 0.4479166666666647423, 0.4583333333333313719, 0.4687499999999980571, 0.4791666666666647423 ),
 .UNSPECIFIED. ) 
 CURVE ( )  GEOMETRIC_REPRESENTATION_ITEM ( )  RATIONAL_B_SPLINE_CURVE ( ( 1.000000000000014211, 0.9238795325112725276, 1.000000000000000000, 0.9238795325112867385, 1.000000000000000000, 0.9238795325112867385, 1.000000000000000000, 0.9238795325113009493, 0.9999999999999857891 ) ) 
 REPRESENTATION_ITEM ( '' )  );
#58775=CARTESIAN_POINT ( 'NONE',  ( -9.832129032723418760, 103.1770833299193555, -5.676582343750004256 ) ) ;
#58780=CARTESIAN_POINT ( 'NONE',  ( 2.679491924305930084, 71.04166666666714036, -10.00000000000306244 ) ) ;
#58783=LINE ( 'NONE', #12734, #63700 ) ;
#58784=CARTESIAN_POINT ( 'NONE',  ( -5.676582343750006032, 214.1145833299193555, 9.832129032723418760 ) ) ;
#58788=CARTESIAN_POINT ( 'NONE',  ( -9.832129032723420536, 179.0104166632526699, 5.676582343749997150 ) ) ;
#58790=CARTESIAN_POINT ( 'NONE',  ( 1.102182119232618108E-15, 296.3125000034140157, 6.000000000000001776 ) ) ;
#58795=CARTESIAN_POINT ( 'NONE',  ( 6.951808397369818766E-16, 67.03124999658602690, -11.35316468750000141 ) ) ;
#58796=FACE_OUTER_BOUND ( 'NONE', #71612, .T. ) ;
#58799=CARTESIAN_POINT ( 'NONE',  ( 6.123233995736767268E-16, 11.25000000000000178, -10.00000000000000178 ) ) ;
#58801=CARTESIAN_POINT ( 'NONE',  ( 8.311093377946837890, 81.40624999658601268, -8.311093377946837890 ) ) ;
#58806=CARTESIAN_POINT ( 'NONE',  ( 6.951808397369818766E-16, 67.03124999658602690, -11.35316468750000141 ) ) ;
#58808=VECTOR ( 'NONE', #43956, 1000.000000000000000 ) ;
#58810=CARTESIAN_POINT ( 'NONE',  ( -2.679491924311225848, 158.3333333265053113, -10.00000000000000178 ) ) ;
#58813=CARTESIAN_POINT ( 'NONE',  ( -11.35316468750000141, 43.59374999658601979, -1.390361679473963753E-15 ) ) ;
#58814=EDGE_CURVE ( 'NONE', #3720, #38699, #55891, .T. ) ;
#58816=CARTESIAN_POINT ( 'NONE',  ( -2.085542519210945728E-15, 194.5312499965860127, 11.35316468750000141 ) ) ;
#58820=CARTESIAN_POINT ( 'NONE',  ( 5.000000000000001776, 62.70833332650536818, -8.660254037844389075 ) ) ;
#58821=CARTESIAN_POINT ( 'NONE',  ( 9.832129032723416984, 175.3645833299193555, 5.676582343750006032 ) ) ;
#58822=FACE_OUTER_BOUND ( 'NONE', #72971, .T. ) ;
#58826=CARTESIAN_POINT ( 'NONE',  ( -8.311093377946836114, 162.9687499965860411, -8.311093377946837890 ) ) ;
#58831=LINE ( 'NONE', #17710, #18906 ) ;
#58842=CARTESIAN_POINT ( 'NONE',  ( -2.679491924327887187, 178.5416666666652361, 9.999999999990450306 ) ) ;
#58849=CARTESIAN_POINT ( 'NONE',  ( 1.102182119232618108E-15, 292.2500000000000000, 6.000000000000001776 ) ) ;
#58853=ORIENTED_EDGE ( 'NONE', *, *, #6099, .T. ) ;
#58859=CARTESIAN_POINT ( 'NONE',  ( 1.226468279477575784E-15, 297.8593750017070079, 6.676582343750001591 ) ) ;
#58860=CARTESIAN_POINT ( 'NONE',  ( -8.660254037844387298, 137.0833333333333428, -5.000000000000004441 ) ) ;
#58872=CARTESIAN_POINT ( 'NONE',  ( -8.660254037844390851, 132.9166666666667140, 4.999999999999998224 ) ) ;
#58877=CARTESIAN_POINT ( 'NONE',  ( -3.042071309553173730, 34.32291666325268409, 11.35316468749999785 ) ) ;
#58881=CARTESIAN_POINT ( 'NONE',  ( -2.085542519210945728E-15, 214.8437499965860411, 11.35316468750000141 ) ) ;
#58888=CARTESIAN_POINT ( 'NONE',  ( 3.042071309553159519, 29.73958332991934839, 11.35316468750000141 ) ) ;
#58891=CARTESIAN_POINT ( 'NONE',  ( -6.000000000000003553, 295.0000000034139589, -2.485281374238571317 ) ) ;
#58894=CARTESIAN_POINT ( 'NONE',  ( 11.35316468749999785, 25.57291666325268409, 3.042071309553174174 ) ) ;
#58897=CARTESIAN_POINT ( 'NONE',  ( 9.832129032723416984, 150.3645833299193555, 5.676582343750006032 ) ) ;
#58898=CARTESIAN_POINT ( 'NONE',  ( 7.320508075688771044, 111.2499999931720396, 7.320508075688775484 ) ) ;
#58903=CARTESIAN_POINT ( 'NONE',  ( -8.311093377946836114, 2.968749996586016238, -8.311093377946837890 ) ) ;
#58906=CARTESIAN_POINT ( 'NONE',  ( 4.242640687119287435, 289.3750000000000000, 4.242640687119285658 ) ) ;
#58907=CARTESIAN_POINT ( 'NONE',  ( 1.226468279477575784E-15, 296.7031250017070079, 6.676582343750001591 ) ) ;
#58909=CARTESIAN_POINT ( 'NONE',  ( 9.832129032723416984, 135.3645833299193555, 5.676582343750006032 ) ) ;
#58920=CARTESIAN_POINT ( 'NONE',  ( -5.676582343749998039, 92.76041666325268409, -9.832129032723420536 ) ) ;
#58925=VERTEX_POINT ( 'NONE', #68681 ) ;
#58936=ORIENTED_EDGE ( 'NONE', *, *, #33802, .F. ) ;
#58947=CARTESIAN_POINT ( 'NONE',  ( -2.679491924311223183, 96.45833333333331439, -9.999999999999989342 ) ) ;
#58951=CARTESIAN_POINT ( 'NONE',  ( 8.660254037844385522, 99.58333333333334281, 5.000000000000005329 ) ) ;
#58953=CARTESIAN_POINT ( 'NONE',  ( -6.676582343750001591, 296.6093750017069510, 0.000000000000000000 ) ) ;
#58960=CARTESIAN_POINT ( 'NONE',  ( -2.679491924311226292, 103.3333333265053824, -10.00000000000000178 ) ) ;
#58963=CYLINDRICAL_SURFACE ( 'NONE', #66796, 10.00000000000000178 ) ;
#58965=CARTESIAN_POINT ( 'NONE',  ( -10.00000000000000000, 212.2916666666666572, -2.679491924311229845 ) ) ;
#58967=CARTESIAN_POINT ( 'NONE',  ( 3.042071309553159519, 185.0520833299193555, 11.35316468750000141 ) ) ;
#58975=CARTESIAN_POINT ( 'NONE',  ( 5.676582343749993598, 50.26041666325269119, 9.832129032723422313 ) ) ;
#58977=CARTESIAN_POINT ( 'NONE',  ( -11.35316468749999785, 223.3854166632526699, -3.042071309553167513 ) ) ;
#58981=DIRECTION ( 'NONE',  ( 0.000000000000000000, 0.000000000000000000, 1.000000000000000000 ) ) ;
#58985=VECTOR ( 'NONE', #62662, 1000.000000000000000 ) ;
#58986=CARTESIAN_POINT ( 'NONE',  ( 8.660254037844389075, 72.29166665983869677, -5.000000000000000000 ) ) ;
#58993=EDGE_CURVE ( 'NONE', #16691, #1871, #50161, .T. ) ;
#58994=CARTESIAN_POINT ( 'NONE',  ( -6.676582343750001591, 299.6093750017069510, 0.000000000000000000 ) ) ;
#58996=CARTESIAN_POINT ( 'NONE',  ( -5.000000000000009770, 18.33333333333333570, 8.660254037844392627 ) ) ;
#58997=CARTESIAN_POINT ( 'NONE',  ( 9.832129032723420536, 161.1979166632526983, -5.676582343749999815 ) ) ;
#59006=CARTESIAN_POINT ( 'NONE',  ( 11.35316468750000141, 146.0937499965860411, 0.000000000000000000 ) ) ;
#59008=CARTESIAN_POINT ( 'NONE',  ( -3.673940397442060854E-16, 298.8125000034140157, -6.000000000000001776 ) ) ;
#59010=CARTESIAN_POINT ( 'NONE',  ( -11.35316468750000141, 48.59374999658601268, -1.390361679473963753E-15 ) ) ;
#59016=CARTESIAN_POINT ( 'NONE',  ( -3.673940397442060854E-16, 292.8125000034140157, -6.000000000000001776 ) ) ;
#59022=CARTESIAN_POINT ( 'NONE',  ( -5.000000000000005329, 65.20833332650536818, 8.660254037844387298 ) ) ;
#59024=ORIENTED_EDGE ( 'NONE', *, *, #10091, .T. ) ;
#59025=EDGE_CURVE ( 'NONE', #23374, #43617, #6132, .T. ) ;
#59036=ORIENTED_EDGE ( 'NONE', *, *, #68936, .T. ) ;
#59040=CARTESIAN_POINT ( 'NONE',  ( 7.320508075688774596, 55.62499999999999289, -7.320508075688774596 ) ) ;
#59042=CARTESIAN_POINT ( 'NONE',  ( 1.102182119232618108E-15, 296.2500000000000000, 6.000000000000001776 ) ) ;
#59043=CARTESIAN_POINT ( 'NONE',  ( -2.679491924311272477, 35.41666665983871098, 9.999999999999978684 ) ) ;
#59053=CARTESIAN_POINT ( 'NONE',  ( -5.000000000000005329, 178.3333333333333428, 8.660254037844387298 ) ) ;
#59057=CARTESIAN_POINT ( 'NONE',  ( 9.832129032723416984, 135.6770833299193555, 5.676582343750006032 ) ) ;
#59058=DIRECTION ( 'NONE',  ( 0.000000000000000000, 0.000000000000000000, 1.000000000000000000 ) ) ;
#59060=CARTESIAN_POINT ( 'NONE',  ( 10.00000000000000178, 106.8749999931720396, 0.000000000000000000 ) ) ;
#59061=CARTESIAN_POINT ( 'NONE',  ( -2.679491924292381810, 166.4583333333316943, -10.00000000001088374 ) ) ;
#59063=ADVANCED_FACE ( 'NONE', ( #52086, #6059 ), #63386, .T. ) ;
#59065=CARTESIAN_POINT ( 'NONE',  ( 6.123233995736767268E-16, 26.25000000000000355, -10.00000000000000178 ) ) ;
#59066=CARTESIAN_POINT ( 'NONE',  ( -1.836970198721029983E-15, 205.6249999931720538, 10.00000000000000178 ) ) ;
#59070=CARTESIAN_POINT ( 'NONE',  ( 10.00000000000000178, 31.87499999317203248, 0.000000000000000000 ) ) ;
#59076=CARTESIAN_POINT ( 'NONE',  ( 7.320508075688774596, 7.499999993172032475, -7.320508075688774596 ) ) ;
#59081=CARTESIAN_POINT ( 'NONE',  ( -3.042071309553173730, 119.3229166632526699, 11.35316468749999785 ) ) ;
#59090=CARTESIAN_POINT ( 'NONE',  ( 9.832129032723420536, 116.1979166632526841, -5.676582343749999815 ) ) ;
#59095=CARTESIAN_POINT ( 'NONE',  ( -7.320508075688778149, 204.9999999931720254, 7.320508075688769267 ) ) ;
#59098=CARTESIAN_POINT ( 'NONE',  ( 3.042071309553159519, 100.0520833299193555, 11.35316468750000141 ) ) ;
#59103=CARTESIAN_POINT ( 'NONE',  ( -9.832129032723420536, 14.01041666325268409, 5.676582343749997150 ) ) ;
#59105=CARTESIAN_POINT ( 'NONE',  ( -2.679491924311081519, 136.4583333333333144, -10.00000000000009770 ) ) ;
#59110=CARTESIAN_POINT ( 'NONE',  ( -7.320508075688773708, 148.7499999931720254, -7.320508075688774596 ) ) ;
#59111=CARTESIAN_POINT ( 'NONE',  ( -2.765530957081998586, 293.6406250017069510, 6.676582343750001591 ) ) ;
#59113=CARTESIAN_POINT ( 'NONE',  ( 9.832129032723420536, 221.5104166632526983, -5.676582343749999815 ) ) ;
#59116=( BOUNDED_CURVE ( )  B_SPLINE_CURVE ( 2, ( #43240, #26253, #44744, #14933, #73040, #54955, #37974, #3265, #60973, #55705, #49271, #10412, #33078 ),
 .UNSPECIFIED., .F., .F. ) 
 B_SPLINE_CURVE_WITH_KNOTS ( ( 3, 2, 2, 2, 2, 2, 3 ),
 ( 1.177487769121809080, 1.182721478772594148, 1.187955188423379438, 1.193188898074164506, 1.198422607724949573, 1.203656317375734863, 1.208890027026519931 ),
 .UNSPECIFIED. ) 
 CURVE ( )  GEOMETRIC_REPRESENTATION_ITEM ( )  RATIONAL_B_SPLINE_CURVE ( ( 1.000000000000081490, 0.9659258262889869329, 1.000000000000000000, 0.9659258262890684232, 1.000000000000000000, 0.9659258262890684232, 1.000000000000000000, 0.9659258262890684232, 1.000000000000000000, 0.9659258262890684232, 1.000000000000000000, 0.9659258262890684232, 1.000000000000000000 ) ) 
 REPRESENTATION_ITEM ( '' )  );
#59134=CARTESIAN_POINT ( 'NONE',  ( -2.295000000000000373, 267.1439999999997212, 5.415579320905394844 ) ) ;
#59135=CARTESIAN_POINT ( 'NONE',  ( 1.226468279477575784E-15, 290.7031250017069510, 6.676582343750001591 ) ) ;
#59145=CARTESIAN_POINT ( 'NONE',  ( 5.676582343750001591, 96.92708332991935549, -9.832129032723420536 ) ) ;
#59152=EDGE_CURVE ( 'NONE', #13169, #73371, #1876, .T. ) ;
#59155=CARTESIAN_POINT ( 'NONE',  ( 6.951808397369818766E-16, 217.0312499965860411, -11.35316468750000141 ) ) ;
#59160=CARTESIAN_POINT ( 'NONE',  ( 11.35316468750000141, 196.0937499965860127, 0.000000000000000000 ) ) ;
#59167=CARTESIAN_POINT ( 'NONE',  ( 5.676582343750001591, 71.61458332991935549, -9.832129032723420536 ) ) ;
#59173=CARTESIAN_POINT ( 'NONE',  ( -5.676582343750006032, 69.11458332991936970, 9.832129032723418760 ) ) ;
#59178=CARTESIAN_POINT ( 'NONE',  ( 9.832129032723416984, 70.36458332991936970, 5.676582343750006032 ) ) ;
#59182=CARTESIAN_POINT ( 'NONE',  ( -10.00000000000000355, 159.5833333265053398, 2.679491924311223183 ) ) ;
#59183=CYLINDRICAL_SURFACE ( 'NONE', #49674, 10.00000000000000178 ) ;
#59184=CARTESIAN_POINT ( 'NONE',  ( 11.35316468749999963, 61.30208332991934839, -3.042071309553165293 ) ) ;
#59186=CARTESIAN_POINT ( 'NONE',  ( 9.832129032723416984, 200.3645833299193555, 5.676582343750006032 ) ) ;
#59190=CARTESIAN_POINT ( 'NONE',  ( 10.00000000000000000, 61.66666665983870388, 2.679491924311235618 ) ) ;
#59192=CARTESIAN_POINT ( 'NONE',  ( 5.676582343749993598, 189.9479166632526983, 9.832129032723422313 ) ) ;
#59195=CARTESIAN_POINT ( 'NONE',  ( -10.00000000000000178, 189.3749999931720254, -1.224646799147353454E-15 ) ) ;
#59198=CARTESIAN_POINT ( 'NONE',  ( 6.951808397369818766E-16, 177.3437499965860411, -11.35316468750000141 ) ) ;
#59201=CARTESIAN_POINT ( 'NONE',  ( 3.959805771731846225, 226.0000000000000568, -9.326041370300968580 ) ) ;
#59212=LINE ( 'NONE', #7523, #18630 ) ;
#59218=CARTESIAN_POINT ( 'NONE',  ( 2.696524195522682164E-11, 156.2499999999978968, -10.00000000000000178 ) ) ;
#59228=CARTESIAN_POINT ( 'NONE',  ( -4.721056650415999201, 294.4843750017070079, -4.721056650415999201 ) ) ;
#59229=CARTESIAN_POINT ( 'NONE',  ( -1.836970198721029983E-15, 138.7500000000000000, 10.00000000000000178 ) ) ;
#59234=B_SPLINE_CURVE_WITH_KNOTS ( 'NONE', 3,
 ( #42080, #70036, #18716, #41724, #24727, #64736 ),
 .UNSPECIFIED., .F., .F.,
 ( 4, 2, 4 ),
 ( 0.4500003403313557193, 0.4750001701656778597, 0.5000000000000000000 ),
 .UNSPECIFIED. ) ;
#59246=CARTESIAN_POINT ( 'NONE',  ( 5.676582343750001591, 31.61458332991935194, -9.832129032723420536 ) ) ;
#59248=CARTESIAN_POINT ( 'NONE',  ( 9.832129032723420536, 221.5104166632526983, -5.676582343749999815 ) ) ;
#59254=CARTESIAN_POINT ( 'NONE',  ( 5.676582343749993598, 39.94791666325268409, 9.832129032723422313 ) ) ;
#59260=CARTESIAN_POINT ( 'NONE',  ( -5.676582343750006032, 39.11458332991934839, 9.832129032723418760 ) ) ;
#59262=CARTESIAN_POINT ( 'NONE',  ( -11.35316468750000141, 143.4895833299193839, 3.042071309553159963 ) ) ;
#59264=CARTESIAN_POINT ( 'NONE',  ( 7.320508075688771044, 116.2499999931720254, 7.320508075688775484 ) ) ;
#59268=ORIENTED_EDGE ( 'NONE', *, *, #10577, .F. ) ;
#59269=CARTESIAN_POINT ( 'NONE',  ( -5.676582343750006032, 24.42708332991935194, 9.832129032723418760 ) ) ;
#59272=CARTESIAN_POINT ( 'NONE',  ( 4.999999999999994671, 105.8333333333333286, -8.660254037844376640 ) ) ;
#59275=CARTESIAN_POINT ( 'NONE',  ( -11.35316468749999785, 143.0729166632526983, -3.042071309553167957 ) ) ;
#59282=ADVANCED_FACE ( 'NONE', ( #24131 ), #47511, .T. ) ;
#59285=CARTESIAN_POINT ( 'NONE',  ( -5.676582343750006032, 94.42708332991935549, 9.832129032723418760 ) ) ;
#59307=VECTOR ( 'NONE', #44605, 1000.000000000000000 ) ;
#59319=CARTESIAN_POINT ( 'NONE',  ( 5.000000000000001776, 95.83333333333334281, -8.660254037844389075 ) ) ;
#59322=CARTESIAN_POINT ( 'NONE',  ( 1.226468279477575784E-15, 297.8593750017070079, 6.676582343750001591 ) ) ;
#59324=CARTESIAN_POINT ( 'NONE',  ( 3.153939666463620179E-13, 188.7500000000000284, 9.999999999999998224 ) ) ;
#59327=CARTESIAN_POINT ( 'NONE',  ( -8.660254037844392627, 52.91666666666666430, 4.999999999999999112 ) ) ;
#59331=CARTESIAN_POINT ( 'NONE',  ( 10.00000000000000000, 209.7916666666667140, 2.679491924311236062 ) ) ;
#59333=CARTESIAN_POINT ( 'NONE',  ( -8.311093377946841443, 184.2187499965860127, 8.311093377946830785 ) ) ;
#59337=DIRECTION ( 'NONE',  ( -0.000000000000000000, 1.000000000000000000, -0.000000000000000000 ) ) ;
#59340=CARTESIAN_POINT ( 'NONE',  ( -8.311093377946836114, 52.96874999658601268, -8.311093377946837890 ) ) ;
#59342=CARTESIAN_POINT ( 'NONE',  ( -8.311093377946841443, 214.2187499965860411, 8.311093377946830785 ) ) ;
#59348=CARTESIAN_POINT ( 'NONE',  ( -8.311093377946836114, 102.6562499965860269, -8.311093377946837890 ) ) ;
#59350=CARTESIAN_POINT ( 'NONE',  ( -4.999999999999998224, 78.54166665983871098, -8.660254037844389075 ) ) ;
#59355=ORIENTED_EDGE ( 'NONE', *, *, #22567, .T. ) ;
#59356=ORIENTED_EDGE ( 'NONE', *, *, #38365, .T. ) ;
#59357=CARTESIAN_POINT ( 'NONE',  ( 4.721056650415999201, 294.2343750017069510, -4.721056650415999201 ) ) ;
#59359=CARTESIAN_POINT ( 'NONE',  ( 3.042071309553159519, 159.7395833299193839, 11.35316468750000141 ) ) ;
#59360=CARTESIAN_POINT ( 'NONE',  ( 10.00000000000000355, 5.208333333333333037, -2.679491924311226736 ) ) ;
#59368=CARTESIAN_POINT ( 'NONE',  ( 9.832129032723416984, 140.6770833299193555, 5.676582343750006032 ) ) ;
#59372=CARTESIAN_POINT ( 'NONE',  ( 11.35316468749999785, 55.88541666325266988, 3.042071309553174174 ) ) ;
#59379=CARTESIAN_POINT ( 'NONE',  ( -2.485281374238571761, 292.8750000034139589, -6.000000000000003553 ) ) ;
#59402=CARTESIAN_POINT ( 'NONE',  ( -1.836970198721029983E-15, 53.75000000000000711, 10.00000000000000178 ) ) ;
#59404=CARTESIAN_POINT ( 'NONE',  ( 2.485281374238575314, 298.3124999999999432, 6.000000000000000888 ) ) ;
#59405=DIRECTION ( 'NONE',  ( -0.000000000000000000, 1.000000000000000000, -0.000000000000000000 ) ) ;
#59410=CARTESIAN_POINT ( 'NONE',  ( 7.320508075688762162, 90.62500000000001421, -7.320508075688762162 ) ) ;
#59415=CARTESIAN_POINT ( 'NONE',  ( 10.00000000000000178, 170.2083333333333428, -2.679491924311226736 ) ) ;
#59419=CARTESIAN_POINT ( 'NONE',  ( -3.042071309553164404, 142.5520833299193271, -11.35316468749999963 ) ) ;
#59426=AXIS2_PLACEMENT_3D ( 'NONE', #41549, #42650, #29864 ) ;
#59427=CARTESIAN_POINT ( 'NONE',  ( 8.311093377946834337, 5.468749996586017126, 8.311093377946839666 ) ) ;
#59429=CARTESIAN_POINT ( 'NONE',  ( -9.999999999999992895, 112.2916666666666714, -2.679491924311228068 ) ) ;
#59434=CARTESIAN_POINT ( 'NONE',  ( -7.320508075688778149, 29.99999999317203603, 7.320508075688769267 ) ) ;
#59443=CARTESIAN_POINT ( 'NONE',  ( -5.000000000000023981, 61.66666666666669272, -8.660254037844433483 ) ) ;
#59445=CARTESIAN_POINT ( 'NONE',  ( 5.676582343749993598, 119.9479166632526841, 9.832129032723422313 ) ) ;
#59453=CARTESIAN_POINT ( 'NONE',  ( -11.35316468749999785, 118.0729166632526841, -3.042071309553167957 ) ) ;
#59457=CARTESIAN_POINT ( 'NONE',  ( 10.00000000000000000, 211.6666666598386541, 2.679491924311236062 ) ) ;
#59461=CARTESIAN_POINT ( 'NONE',  ( -11.35316468750000141, 103.5937499965860269, -1.390361679473963753E-15 ) ) ;
#59465=CARTESIAN_POINT ( 'NONE',  ( 9.832129032723416984, 5.677083329919350163, 5.676582343750006032 ) ) ;
#59467=CARTESIAN_POINT ( 'NONE',  ( 2.679491924310934969, 182.9166666598387394, -10.00000000000017053 ) ) ;
#59474=CARTESIAN_POINT ( 'NONE',  ( 6.676582343750003368, 293.0156250017070079, -2.765530957081997254 ) ) ;
#59478=ADVANCED_FACE ( 'NONE', ( #3736 ), #26735, .T. ) ;
#59493=CARTESIAN_POINT ( 'NONE',  ( -10.00000000000000178, 29.37499999317203248, -1.224646799147353454E-15 ) ) ;
#59495=CARTESIAN_POINT ( 'NONE',  ( -0.4590000000000000746, 272.8559999999997672, 5.793779103868386571 ) ) ;
#59496=CARTESIAN_POINT ( 'NONE',  ( -4.088227598258586603E-16, 293.2031250017069510, -6.676582343750001591 ) ) ;
#59506=CARTESIAN_POINT ( 'NONE',  ( 11.35316468749999785, 100.8854166632526841, 3.042071309553174174 ) ) ;
#59507=DIRECTION ( 'NONE',  ( -0.000000000000000000, 1.000000000000000000, -0.000000000000000000 ) ) ;
#59514=CARTESIAN_POINT ( 'NONE',  ( -8.311093377946836114, 212.6562499965860411, -8.311093377946837890 ) ) ;
#59518=CARTESIAN_POINT ( 'NONE',  ( -3.042071309553173730, 189.6354166632526983, 11.35316468749999785 ) ) ;
#59525=CARTESIAN_POINT ( 'NONE',  ( 11.35316468749999785, 80.57291666325268409, 3.042071309553174174 ) ) ;
#59529=ORIENTED_EDGE ( 'NONE', *, *, #68362, .T. ) ;
#59532=CARTESIAN_POINT ( 'NONE',  ( -11.35316468750000141, 78.28124999658601268, -1.390361679473963753E-15 ) ) ;
#59539=CARTESIAN_POINT ( 'NONE',  ( 9.832129032723420536, 76.19791666325269830, -5.676582343749999815 ) ) ;
#59542=CARTESIAN_POINT ( 'NONE',  ( -2.679491924311225848, 168.3333333265053966, -10.00000000000000178 ) ) ;
#59546=CARTESIAN_POINT ( 'NONE',  ( 9.832129032723420536, 56.51041666325268409, -5.676582343749999815 ) ) ;
#59548=CARTESIAN_POINT ( 'NONE',  ( 8.311093377946837890, 196.4062499965860411, -8.311093377946837890 ) ) ;
#59552=CARTESIAN_POINT ( 'NONE',  ( 8.660254037844389075, 162.2916666598387110, -5.000000000000000000 ) ) ;
#59554=CARTESIAN_POINT ( 'NONE',  ( -3.042071309553173730, 199.3229166632526983, 11.35316468749999785 ) ) ;
#59555=CARTESIAN_POINT ( 'NONE',  ( 0.000000000000000000, 300.0000000000000000, 0.000000000000000000 ) ) ;
#59559=CARTESIAN_POINT ( 'NONE',  ( -3.042071309553163960, 177.5520833299193555, -11.35316468749999963 ) ) ;
#59562=VERTEX_POINT ( 'NONE', #15037 ) ;
#59566=CYLINDRICAL_SURFACE ( 'NONE', #44634, 6.000000000000001776 ) ;
#59574=AXIS2_PLACEMENT_3D ( 'NONE', #24692, #64333, #19776 ) ;
#59586=CARTESIAN_POINT ( 'NONE',  ( 2.679491924311155682, 92.91666665983871098, -10.00000000000004441 ) ) ;
#59588=DIRECTION ( 'NONE',  ( -0.000000000000000000, 1.000000000000000000, -0.000000000000000000 ) ) ;
#59590=CARTESIAN_POINT ( 'NONE',  ( 2.765530957081996366, 293.2968750017070079, -6.676582343750002480 ) ) ;
#59591=CARTESIAN_POINT ( 'NONE',  ( -8.660254037844390851, 152.9166666666666856, 4.999999999999998224 ) ) ;
#59599=DIRECTION ( 'NONE',  ( 0.000000000000000000, 0.000000000000000000, 1.000000000000000000 ) ) ;
#59602=CARTESIAN_POINT ( 'NONE',  ( -4.999999999999998224, 131.6666666666667140, -8.660254037844389075 ) ) ;
#59607=CARTESIAN_POINT ( 'NONE',  ( 8.311093377946834337, 25.15624999658601268, 8.311093377946839666 ) ) ;
#59608=CARTESIAN_POINT ( 'NONE',  ( 8.660254037844389075, 149.5833333333333144, 5.000000000000007105 ) ) ;
#59609=CARTESIAN_POINT ( 'NONE',  ( 8.660254037844385522, 6.458333326505366401, 5.000000000000005329 ) ) ;
#59611=DIRECTION ( 'NONE',  ( -0.000000000000000000, 1.000000000000000000, -0.000000000000000000 ) ) ;
#59615=CARTESIAN_POINT ( 'NONE',  ( 3.042071309553159519, 39.73958332991934128, 11.35316468750000141 ) ) ;
#59621=CARTESIAN_POINT ( 'NONE',  ( -11.35316468750000141, 28.48958332991934839, 3.042071309553159963 ) ) ;
#59623=CARTESIAN_POINT ( 'NONE',  ( -11.35316468750000141, 153.2812499965860127, -1.390361679473963753E-15 ) ) ;
#59624=CARTESIAN_POINT ( 'NONE',  ( 2.679491924311228956, 122.9166666598386968, -10.00000000000000000 ) ) ;
#59629=CARTESIAN_POINT ( 'NONE',  ( 5.676582343750001591, 21.92708332991935194, -9.832129032723420536 ) ) ;
#59634=CARTESIAN_POINT ( 'NONE',  ( -11.35316468750000141, 148.2812499965860411, -1.390361679473963753E-15 ) ) ;
#59643=CARTESIAN_POINT ( 'NONE',  ( 5.000000000000003553, 120.8333333333333286, -8.660254037844390851 ) ) ;
#59645=CARTESIAN_POINT ( 'NONE',  ( -3.042071309553164404, 102.5520833299193555, -11.35316468749999963 ) ) ;
#59648=ORIENTED_EDGE ( 'NONE', *, *, #38912, .T. ) ;
#59649=VERTEX_POINT ( 'NONE', #48639 ) ;
#59654=VECTOR ( 'NONE', #46634, 1000.000000000000000 ) ;
#59667=CARTESIAN_POINT ( 'NONE',  ( -2.319934922699201535E-11, 23.74999999999819522, 10.00000000000000178 ) ) ;
#59681=CARTESIAN_POINT ( 'NONE',  ( -5.000000000000005329, 113.3333333333333428, 8.660254037844387298 ) ) ;
#59685=CARTESIAN_POINT ( 'NONE',  ( 4.721056650416000089, 294.9843750017070079, 4.721056650415999201 ) ) ;
#59686=ORIENTED_EDGE ( 'NONE', *, *, #34629, .F. ) ;
#59687=CARTESIAN_POINT ( 'NONE',  ( 5.000000000000022204, 190.8333333333333712, -8.660254037844422825 ) ) ;
#59695=CARTESIAN_POINT ( 'NONE',  ( -7.320508075688778149, 218.1250000000000000, 7.320508075688769267 ) ) ;
#59697=CARTESIAN_POINT ( 'NONE',  ( 11.35316468749999963, 196.3020833299193271, -3.042071309553165293 ) ) ;
#59705=CARTESIAN_POINT ( 'NONE',  ( 11.35316468750000141, 51.09374999658601268, 0.000000000000000000 ) ) ;
#59708=CARTESIAN_POINT ( 'NONE',  ( 11.35316468750000141, 226.0937499965860127, 0.000000000000000000 ) ) ;
#59713=CARTESIAN_POINT ( 'NONE',  ( 3.042071309553159519, 109.7395833299193697, 11.35316468750000141 ) ) ;
#59714=CARTESIAN_POINT ( 'NONE',  ( 4.999999999999993783, 76.04166665983871098, 8.660254037844390851 ) ) ;
#59722=CARTESIAN_POINT ( 'NONE',  ( 6.676582343750004256, 293.0468750017069510, 2.765530957081995478 ) ) ;
#59724=CARTESIAN_POINT ( 'NONE',  ( -3.042071309553164404, 172.2395833299193839, -11.35316468749999963 ) ) ;
#59725=CARTESIAN_POINT ( 'NONE',  ( 2.679491924311222739, 3.958333333333333481, 10.00000000000000533 ) ) ;
#59727=CARTESIAN_POINT ( 'NONE',  ( -8.660254037844428154, 192.9166666666666856, 5.000000000000020428 ) ) ;
#59729=ORIENTED_EDGE ( 'NONE', *, *, #27893, .T. ) ;
#59732=CARTESIAN_POINT ( 'NONE',  ( -9.832129032723418760, 138.1770833299193555, -5.676582343750004256 ) ) ;
#59738=CARTESIAN_POINT ( 'NONE',  ( 3.042071309553167069, 57.13541666325268409, -11.35316468749999785 ) ) ;
#59744=CARTESIAN_POINT ( 'NONE',  ( 6.000000000000001776, 290.5625000034140157, -7.347880794884121708E-16 ) ) ;
#59745=CYLINDRICAL_SURFACE ( 'NONE', #46172, 10.00000000000000178 ) ;
#59750=( BOUNDED_CURVE ( )  B_SPLINE_CURVE ( 2, ( #68132, #62832, #51518, #22843, #45856, #32704, #29263, #28881, #12998, #69999, #1346, #70721, #35305 ),
 .UNSPECIFIED., .F., .F. ) 
 B_SPLINE_CURVE_WITH_KNOTS ( ( 3, 2, 2, 2, 2, 2, 3 ),
 ( 0.5923913043478260532, 0.5942028985507246119, 0.5960144927536231707, 0.5978260869565217295, 0.5996376811594202882, 0.6014492753623188470, 0.6032608695652174058 ),
 .UNSPECIFIED. ) 
 CURVE ( )  GEOMETRIC_REPRESENTATION_ITEM ( )  RATIONAL_B_SPLINE_CURVE ( ( 1.000000000000000000, 0.9659258262890683122, 1.000000000000000000, 0.9659258262890683122, 1.000000000000000000, 0.9659258262890683122, 1.000000000000000000, 0.9659258262890683122, 1.000000000000000000, 0.9659258262890683122, 1.000000000000000000, 0.9659258262890683122, 1.000000000000000000 ) ) 
 REPRESENTATION_ITEM ( '' )  );
#59751=CARTESIAN_POINT ( 'NONE',  ( -2.679491924311226292, 63.33333332650536818, -10.00000000000000178 ) ) ;
#59768=CARTESIAN_POINT ( 'NONE',  ( -8.660254037844390851, 202.9166666666666856, 4.999999999999998224 ) ) ;
#59771=CARTESIAN_POINT ( 'NONE',  ( -10.00000000000000355, 52.70833333333334281, 2.679491924311223183 ) ) ;
#59773=CARTESIAN_POINT ( 'NONE',  ( 4.242640687119285658, 297.6250000000000000, -4.242640687119286547 ) ) ;
#59783=CARTESIAN_POINT ( 'NONE',  ( 2.679491924311228956, 171.0416666666666572, -10.00000000000000000 ) ) ;
#59786=CARTESIAN_POINT ( 'NONE',  ( -8.311093377946841443, 159.2187499965860127, 8.311093377946830785 ) ) ;
#59791=EDGE_LOOP ( 'NONE', ( #74330, #24032, #15806, #20784 ) ) ;
#59792=CARTESIAN_POINT ( 'NONE',  ( -2.085542519210945728E-15, 9.843749996586018014, 11.35316468750000141 ) ) ;
#59798=CARTESIAN_POINT ( 'NONE',  ( 10.00000000000000000, 36.66666665983869677, 2.679491924311236062 ) ) ;
#59801=LINE ( 'NONE', #15622, #67467 ) ;
#59803=CARTESIAN_POINT ( 'NONE',  ( 6.000000000000001776, 291.5625000034140157, -7.347880794884121708E-16 ) ) ;
#59809=CARTESIAN_POINT ( 'NONE',  ( 11.35316468749999785, 125.5729166632526983, 3.042071309553174174 ) ) ;
#59813=CARTESIAN_POINT ( 'NONE',  ( 0.000000000000000000, 300.0000000000000000, 0.000000000000000000 ) ) ;
#59817=CARTESIAN_POINT ( 'NONE',  ( -2.085542519210945728E-15, 114.5312499965860269, 11.35316468750000141 ) ) ;
#59821=CARTESIAN_POINT ( 'NONE',  ( -2.679491924311225848, 213.3333333265053682, -10.00000000000000178 ) ) ;
#59823=CARTESIAN_POINT ( 'NONE',  ( 8.311093377946837890, 101.7187499965860127, -8.311093377946837890 ) ) ;
#59828=CARTESIAN_POINT ( 'NONE',  ( 5.676582343749993598, 5.260416663252683200, 9.832129032723422313 ) ) ;
#59832=CARTESIAN_POINT ( 'NONE',  ( 11.44979897117363699, 225.9999999999999432, -0.1323599981037845985 ) ) ;
#59836=CARTESIAN_POINT ( 'NONE',  ( 1.226468279477575784E-15, 293.7031250017069510, 6.676582343750001591 ) ) ;
#59837=CARTESIAN_POINT ( 'NONE',  ( 2.679491924311228956, 127.9166666598386968, -10.00000000000000000 ) ) ;
#59838=CARTESIAN_POINT ( 'NONE',  ( 11.35316468749999785, 220.8854166632526699, 3.042071309553174174 ) ) ;
#59839=CARTESIAN_POINT ( 'NONE',  ( 6.951808397369818766E-16, 127.3437499965860127, -11.35316468750000141 ) ) ;
#59845=ORIENTED_EDGE ( 'NONE', *, *, #69177, .T. ) ;
#59859=CARTESIAN_POINT ( 'NONE',  ( 6.676582343750003368, 293.8906250017069510, 2.765530957081995478 ) ) ;
#59861=CARTESIAN_POINT ( 'NONE',  ( 6.123233995736767268E-16, 138.1249999931720538, -10.00000000000000178 ) ) ;
#59871=CARTESIAN_POINT ( 'NONE',  ( -2.085542519210945728E-15, 99.84374999658601268, 11.35316468750000141 ) ) ;
#59878=CARTESIAN_POINT ( 'NONE',  ( -5.676582343750006032, 219.1145833299193839, 9.832129032723418760 ) ) ;
#59884=CARTESIAN_POINT ( 'NONE',  ( 3.042071309553167069, 197.1354166632526415, -11.35316468749999785 ) ) ;
#59890=CARTESIAN_POINT ( 'NONE',  ( -3.673940397442060854E-16, 293.7500000000000000, -6.000000000000001776 ) ) ;
#59891=CARTESIAN_POINT ( 'NONE',  ( -9.832129032723420536, 83.69791666325268409, 5.676582343749997150 ) ) ;
#59895=CARTESIAN_POINT ( 'NONE',  ( -8.660254037844408614, 47.08333333333334991, -5.000000000000017764 ) ) ;
#59897=CARTESIAN_POINT ( 'NONE',  ( 3.042071309553159519, 69.73958332991935549, 11.35316468750000141 ) ) ;
#59904=CARTESIAN_POINT ( 'NONE',  ( -11.35316468750000141, 73.48958332991934128, 3.042071309553159963 ) ) ;
#59908=CARTESIAN_POINT ( 'NONE',  ( -8.660254037844387298, 173.9583333265053682, -5.000000000000004441 ) ) ;
#59911=CARTESIAN_POINT ( 'NONE',  ( 11.35316468750000141, 66.09374999658601268, 0.000000000000000000 ) ) ;
#59913=CARTESIAN_POINT ( 'NONE',  ( -11.35316468750000141, 198.2812499965860411, -1.390361679473963753E-15 ) ) ;
#59919=CARTESIAN_POINT ( 'NONE',  ( 8.311093377946837890, 186.4062499965860411, -8.311093377946837890 ) ) ;
#59925=CARTESIAN_POINT ( 'NONE',  ( -2.085542519210945728E-15, 179.8437499965860411, 11.35316468750000141 ) ) ;
#59928=ORIENTED_EDGE ( 'NONE', *, *, #65680, .F. ) ;
#59938=CARTESIAN_POINT ( 'NONE',  ( 7.320508075688812788, 180.6250000000000284, -7.320508075688812788 ) ) ;
#59947=CARTESIAN_POINT ( 'NONE',  ( 11.35316468750000141, 56.09374999658601979, 0.000000000000000000 ) ) ;
#59952=CARTESIAN_POINT ( 'NONE',  ( -4.088227598258586603E-16, 294.3593750017070079, -6.676582343750001591 ) ) ;
#59953=CARTESIAN_POINT ( 'NONE',  ( -10.00000000000000000, 147.2916666666666288, -2.679491924311229845 ) ) ;
#59963=CARTESIAN_POINT ( 'NONE',  ( -8.660254037844387298, 18.95833332650536818, -5.000000000000004441 ) ) ;
#59964=CARTESIAN_POINT ( 'NONE',  ( -8.660254037844387298, 132.0833333333333712, -5.000000000000004441 ) ) ;
#59969=CARTESIAN_POINT ( 'NONE',  ( 11.35316468750000141, 40.78124999658601268, 0.000000000000000000 ) ) ;
#59971=CARTESIAN_POINT ( 'NONE',  ( -4.999999999999998224, 13.54166665983870033, -8.660254037844389075 ) ) ;
#59972=CARTESIAN_POINT ( 'NONE',  ( -10.00000000000000178, 225.9999999999999432, 0.000000000000000000 ) ) ;
#59973=CARTESIAN_POINT ( 'NONE',  ( 1.267086777181619559E-12, 183.7500000000001137, 10.00000000000000178 ) ) ;
#59978=CARTESIAN_POINT ( 'NONE',  ( 8.311093377946837890, 41.40624999658601268, -8.311093377946837890 ) ) ;
#59984=CARTESIAN_POINT ( 'NONE',  ( 8.311093377946837890, 31.40624999658601979, -8.311093377946837890 ) ) ;
#59986=CARTESIAN_POINT ( 'NONE',  ( 11.35316468749999963, 155.9895833299193555, -3.042071309553165293 ) ) ;
#59988=CARTESIAN_POINT ( 'NONE',  ( -1.836970198721029983E-15, 125.6249999931720254, 10.00000000000000178 ) ) ;
#59992=CARTESIAN_POINT ( 'NONE',  ( -9.832129032723418760, 23.17708332991934839, -5.676582343750004256 ) ) ;
#59994=CARTESIAN_POINT ( 'NONE',  ( 0.000000000000000000, 300.0000000000000000, 0.000000000000000000 ) ) ;
#59998=CARTESIAN_POINT ( 'NONE',  ( 11.35316468749999963, 155.9895833299193555, -3.042071309553165293 ) ) ;
#60007=CARTESIAN_POINT ( 'NONE',  ( -5.676582343750006032, 104.4270833299193555, 9.832129032723418760 ) ) ;
#60027=CARTESIAN_POINT ( 'NONE',  ( 10.00000000000000178, 122.0833333265053682, -2.679491924311226736 ) ) ;
#60030=ORIENTED_EDGE ( 'NONE', *, *, #4836, .T. ) ;
#60036=CARTESIAN_POINT ( 'NONE',  ( -8.660254037844387298, 32.91666666666667140, 4.999999999999996447 ) ) ;
#60037=CARTESIAN_POINT ( 'NONE',  ( 4.999999999999993783, 114.1666666666666856, 8.660254037844390851 ) ) ;
#60039=CARTESIAN_POINT ( 'NONE',  ( -6.676582343750003368, 294.5468750017069510, -2.765530957081996810 ) ) ;
#60041=CARTESIAN_POINT ( 'NONE',  ( -7.320508075688778149, 144.9999999931719969, 7.320508075688769267 ) ) ;
#60044=CARTESIAN_POINT ( 'NONE',  ( -10.00000000000000178, 184.3749999931720538, -1.224646799147353454E-15 ) ) ;
#60049=CARTESIAN_POINT ( 'NONE',  ( 8.311093377946837890, 1.406249996586016682, -8.311093377946837890 ) ) ;
#60051=CARTESIAN_POINT ( 'NONE',  ( 11.35316468750000141, 191.0937499965860127, 0.000000000000000000 ) ) ;
#60052=CARTESIAN_POINT ( 'NONE',  ( -1.836970198721029983E-15, 190.6249999931720254, 10.00000000000000178 ) ) ;
#60060=CARTESIAN_POINT ( 'NONE',  ( -8.311093377946841443, 49.21874999658600558, 8.311093377946830785 ) ) ;
#60064=DIRECTION ( 'NONE',  ( -0.000000000000000000, 1.000000000000000000, -0.000000000000000000 ) ) ;
#60069=CARTESIAN_POINT ( 'NONE',  ( -9.832129032723420536, 113.6979166632526983, 5.676582343749997150 ) ) ;
#60072=CARTESIAN_POINT ( 'NONE',  ( 10.00000000000000000, 91.66666665983869677, 2.679491924311236062 ) ) ;
#60075=CARTESIAN_POINT ( 'NONE',  ( -10.00000000000000533, 72.29166666666667140, -2.679491924311231621 ) ) ;
#60080=CARTESIAN_POINT ( 'NONE',  ( 4.721056650415999201, 295.2343750017069510, -4.721056650415999201 ) ) ;
#60083=CARTESIAN_POINT ( 'NONE',  ( -8.311093377946841443, 173.9062499965860411, 8.311093377946830785 ) ) ;
#60088=ADVANCED_FACE ( 'NONE', ( #19226 ), #65245, .T. ) ;
#60093=CARTESIAN_POINT ( 'NONE',  ( 9.832129032723420536, 141.5104166632526699, -5.676582343749999815 ) ) ;
#60097=CARTESIAN_POINT ( 'NONE',  ( -9.832129032723420536, 69.01041666325268409, 5.676582343749997150 ) ) ;
#60120=ORIENTED_EDGE ( 'NONE', *, *, #26526, .T. ) ;
#60123=CARTESIAN_POINT ( 'NONE',  ( -8.660254037844387298, 2.916666666666664742, 4.999999999999995559 ) ) ;
#60124=CARTESIAN_POINT ( 'NONE',  ( -3.190679070438223991E-13, 203.7500000000000000, 10.00000000000000533 ) ) ;
#60125=CARTESIAN_POINT ( 'NONE',  ( 2.485281374238950125, 296.3125000000001705, 5.999999999999625189 ) ) ;
#60127=CARTESIAN_POINT ( 'NONE',  ( -8.660254037844387298, 72.08333333333332860, -5.000000000000004441 ) ) ;
#60130=CARTESIAN_POINT ( 'NONE',  ( -2.485281374238572649, 297.1875000000000000, 6.000000000000002665 ) ) ;
#60138=CARTESIAN_POINT ( 'NONE',  ( 2.966170491840901068E-11, 66.24999999999768363, -9.999999999999998224 ) ) ;
#60140=CARTESIAN_POINT ( 'NONE',  ( 8.660254037844389075, 180.4166666666666572, -5.000000000000000000 ) ) ;
#60143=CARTESIAN_POINT ( 'NONE',  ( -11.35316468750000141, 148.8020833299193555, 3.042071309553159963 ) ) ;
#60150=CARTESIAN_POINT ( 'NONE',  ( 11.35316468749999785, 10.88541666325268586, 3.042071309553174174 ) ) ;
#60158=CARTESIAN_POINT ( 'NONE',  ( -4.999999999999998224, 43.54166665983870388, -8.660254037844389075 ) ) ;
#60165=VERTEX_POINT ( 'NONE', #38458 ) ;
#60170=CARTESIAN_POINT ( 'NONE',  ( -9.832129032723418760, 122.8645833299193555, -5.676582343750004256 ) ) ;
#60171=ORIENTED_EDGE ( 'NONE', *, *, #68500, .F. ) ;
#60175=FACE_OUTER_BOUND ( 'NONE', #46102, .T. ) ;
#60176=CARTESIAN_POINT ( 'NONE',  ( 7.320508075688792360, 45.62500000000002132, -7.320508075688792360 ) ) ;
#60177=CARTESIAN_POINT ( 'NONE',  ( 6.951808397369818766E-16, 112.0312499965860269, -11.35316468750000141 ) ) ;
#60181=ADVANCED_FACE ( 'NONE', ( #73153 ), #5247, .T. ) ;
#60182=CARTESIAN_POINT ( 'NONE',  ( -8.660254037844387298, 23.95833332650536462, -5.000000000000004441 ) ) ;
#60183=CARTESIAN_POINT ( 'NONE',  ( -11.35316468750000141, 98.59374999658601268, -1.390361679473963753E-15 ) ) ;
#60188=CARTESIAN_POINT ( 'NONE',  ( 3.042071309553167069, 27.13541666325268409, -11.35316468749999785 ) ) ;
#60196=CARTESIAN_POINT ( 'NONE',  ( -4.721056650415998313, 291.5781250017069510, 4.721056650416000089 ) ) ;
#60197=CARTESIAN_POINT ( 'NONE',  ( 8.311093377946834337, 220.4687499965860127, 8.311093377946839666 ) ) ;
#60198=CARTESIAN_POINT ( 'NONE',  ( 3.042071309553167069, 137.1354166632526983, -11.35316468749999785 ) ) ;
#60209=CARTESIAN_POINT ( 'NONE',  ( -3.166186134455097228E-13, 171.2500000000000284, -9.999999999999998224 ) ) ;
#60215=CARTESIAN_POINT ( 'NONE',  ( -5.000000000000005329, 30.20833332650536818, 8.660254037844387298 ) ) ;
#60216=CARTESIAN_POINT ( 'NONE',  ( -8.311093377946836114, 182.6562499965860411, -8.311093377946837890 ) ) ;
#60218=CARTESIAN_POINT ( 'NONE',  ( -0.4590000000000000746, 278.5679999999998699, 5.805285082143462283 ) ) ;
#60219=CARTESIAN_POINT ( 'NONE',  ( -4.721056650415998313, 291.5781250017069510, 4.721056650416000089 ) ) ;
#60229=VERTEX_POINT ( 'NONE', #31109 ) ;
#60232=CARTESIAN_POINT ( 'NONE',  ( -9.832129032723420536, 114.0104166632526983, 5.676582343749997150 ) ) ;
#60240=CARTESIAN_POINT ( 'NONE',  ( 11.35316468749999785, 225.5729166632526983, 3.042071309553174174 ) ) ;
#60244=CARTESIAN_POINT ( 'NONE',  ( -5.676582343749998039, 197.7604166632526983, -9.832129032723420536 ) ) ;
#60246=CARTESIAN_POINT ( 'NONE',  ( 9.919492326333610777, 226.0000000000000000, 4.581766860447704204 ) ) ;
#60251=CARTESIAN_POINT ( 'NONE',  ( -9.832129032723418760, 87.86458332991935549, -5.676582343750004256 ) ) ;
#60253=CARTESIAN_POINT ( 'NONE',  ( 8.660254037844392627, 139.5833333333333712, 5.000000000000009770 ) ) ;
#60257=CARTESIAN_POINT ( 'NONE',  ( -2.085542519210945728E-15, 94.53124999658601268, 11.35316468750000141 ) ) ;
#60258=ORIENTED_EDGE ( 'NONE', *, *, #24035, .T. ) ;
#60264=CARTESIAN_POINT ( 'NONE',  ( 11.35316468749999785, 75.57291666325269830, 3.042071309553174174 ) ) ;
#60268=CARTESIAN_POINT ( 'NONE',  ( 7.320508075688774596, 167.4999999931720822, -7.320508075688774596 ) ) ;
#60271=CARTESIAN_POINT ( 'NONE',  ( 5.676582343749993598, 65.26041666325268409, 9.832129032723422313 ) ) ;
#60272=CARTESIAN_POINT ( 'NONE',  ( -4.088227598258586603E-16, 292.2031250017069510, -6.676582343750001591 ) ) ;
#60274=CARTESIAN_POINT ( 'NONE',  ( -3.042071309553164404, 212.2395833299193839, -11.35316468749999963 ) ) ;
#60280=CARTESIAN_POINT ( 'NONE',  ( -11.35316468750000141, 188.4895833299193555, 3.042071309553159963 ) ) ;
#60284=VERTEX_POINT ( 'NONE', #59065 ) ;
#60285=CARTESIAN_POINT ( 'NONE',  ( 5.676582343750001591, 181.9270833299193555, -9.832129032723420536 ) ) ;
#60286=( BOUNDED_CURVE ( )  B_SPLINE_CURVE ( 2, ( #13994, #7257, #12897, #30631, #37035, #43049, #66068, #3078, #60036, #8354, #26063, #31371, #25693 ),
 .UNSPECIFIED., .F., .F. ) 
 B_SPLINE_CURVE_WITH_KNOTS ( ( 3, 2, 2, 2, 2, 2, 3 ),
 ( 0.3924913403172796134, 0.3977247878691485550, 0.4029582354210174966, 0.4081916829728863272, 0.4134251305247552688, 0.4186585780766242104, 0.4238920256284931520 ),
 .UNSPECIFIED. ) 
 CURVE ( )  GEOMETRIC_REPRESENTATION_ITEM ( )  RATIONAL_B_SPLINE_CURVE ( ( 1.000000000000298428, 0.9659258262887695512, 0.9999999999999998890, 0.9659258262890682012, 0.9999999999999998890, 0.9659258262890682012, 0.9999999999999998890, 0.9659258262890682012, 0.9999999999999998890, 0.9659258262890682012, 0.9999999999999998890, 0.9659258262890666469, 1.000000000000001332 ) ) 
 REPRESENTATION_ITEM ( '' )  );
#60293=CARTESIAN_POINT ( 'NONE',  ( -10.00000000000000178, 7.500000000000000888, -1.224646799147353454E-15 ) ) ;
#60294=( BOUNDED_CURVE ( )  B_SPLINE_CURVE ( 2, ( #49727, #2591, #15007, #49343, #20291, #66326, #19922, #48594, #15379, #38042, #71601, #48964, #42930 ),
 .UNSPECIFIED., .F., .F. ) 
 B_SPLINE_CURVE_WITH_KNOTS ( ( 3, 2, 2, 2, 2, 2, 3 ),
 ( 1.146093318828196539, 1.151325727210465333, 1.156558135592734127, 1.161790543975002921, 1.167022952357271715, 1.172255360739540508, 1.177487769121809080 ),
 .UNSPECIFIED. ) 
 CURVE ( )  GEOMETRIC_REPRESENTATION_ITEM ( )  RATIONAL_B_SPLINE_CURVE ( ( 1.000000000000000000, 0.9659258262890683122, 1.000000000000000000, 0.9659258262890683122, 1.000000000000000000, 0.9659258262890683122, 1.000000000000000000, 0.9659258262890683122, 1.000000000000000000, 0.9659258262890683122, 1.000000000000000000, 0.9659258262891498026, 0.9999999999999185096 ) ) 
 REPRESENTATION_ITEM ( '' )  );
#60312=ORIENTED_EDGE ( 'NONE', *, *, #2401, .T. ) ;
#60314=CARTESIAN_POINT ( 'NONE',  ( -8.311093377946836114, 77.96874999658598426, -8.311093377946837890 ) ) ;
#60319=CARTESIAN_POINT ( 'NONE',  ( 4.721056650416000089, 295.9843750017070079, 4.721056650415999201 ) ) ;
#60320=CARTESIAN_POINT ( 'NONE',  ( -1.836970198721029983E-15, 148.7500000000000284, 10.00000000000000178 ) ) ;
#60322=CARTESIAN_POINT ( 'NONE',  ( -7.320508075688778149, 164.9999999931720538, 7.320508075688769267 ) ) ;
#60337=CARTESIAN_POINT ( 'NONE',  ( 8.311093377946834337, 40.15624999658601268, 8.311093377946839666 ) ) ;
#60339=CARTESIAN_POINT ( 'NONE',  ( -5.000000000000005329, 5.208333326505366401, 8.660254037844387298 ) ) ;
#60343=CARTESIAN_POINT ( 'NONE',  ( -9.832129032723418760, 52.86458332991934839, -5.676582343750004256 ) ) ;
#60350=CARTESIAN_POINT ( 'NONE',  ( 3.042071309553167513, 31.82291666325268054, -11.35316468749999785 ) ) ;
#60352=CARTESIAN_POINT ( 'NONE',  ( -2.679491924311263595, 48.33333332650537528, -9.999999999999980460 ) ) ;
#60353=CARTESIAN_POINT ( 'NONE',  ( -11.35316468750000141, 158.2812499965860127, -1.390361679473963753E-15 ) ) ;
#60354=CARTESIAN_POINT ( 'NONE',  ( -7.320508075688773708, 133.7499999931720538, -7.320508075688774596 ) ) ;
#60358=CARTESIAN_POINT ( 'NONE',  ( -4.242640687119286547, 288.8750000000000000, -4.242640687119286547 ) ) ;
#60359=CARTESIAN_POINT ( 'NONE',  ( 11.35316468749999785, 20.88541666325268409, 3.042071309553174174 ) ) ;
#60366=CARTESIAN_POINT ( 'NONE',  ( -11.35316468750000141, 158.4895833299193555, 3.042071309553159963 ) ) ;
#60370=CARTESIAN_POINT ( 'NONE',  ( 2.394417657446511694, 225.8111685005081029, 10.00000000000000355 ) ) ;
#60376=CARTESIAN_POINT ( 'NONE',  ( -11.35316468750000141, 98.59374999658601268, -1.390361679473963753E-15 ) ) ;
#60411=CARTESIAN_POINT ( 'NONE',  ( -10.00000000000000355, 102.7083333333333286, 2.679491924311223183 ) ) ;
#60414=CARTESIAN_POINT ( 'NONE',  ( 4.721056650416000089, 290.9843750017070079, 4.721056650415999201 ) ) ;
#60421=CARTESIAN_POINT ( 'NONE',  ( -5.000000000000005329, 185.2083333265053682, 8.660254037844387298 ) ) ;
#60426=CARTESIAN_POINT ( 'NONE',  ( 10.00000000000000000, 224.7916666666666288, 2.679491924311236062 ) ) ;
#60428=CARTESIAN_POINT ( 'NONE',  ( 11.35316468749999963, 191.3020833299193839, -3.042071309553165293 ) ) ;
#60442=CARTESIAN_POINT ( 'NONE',  ( 11.35316468750000141, 125.7812499965860127, 0.000000000000000000 ) ) ;
#60443=CARTESIAN_POINT ( 'NONE',  ( 8.660254037844389075, 92.29166665983871098, -5.000000000000000000 ) ) ;
#60451=CARTESIAN_POINT ( 'NONE',  ( -4.721056650415999201, 293.4843750017070079, -4.721056650415999201 ) ) ;
#60454=CARTESIAN_POINT ( 'NONE',  ( 5.676582343749993598, 164.9479166632526983, 9.832129032723422313 ) ) ;
#60461=VECTOR ( 'NONE', #3757, 1000.000000000000000 ) ;
#60463=CARTESIAN_POINT ( 'NONE',  ( 11.35316468749999785, 155.8854166632526699, 3.042071309553174174 ) ) ;
#60467=CARTESIAN_POINT ( 'NONE',  ( 6.951808397369818766E-16, 62.34374999658602690, -11.35316468750000141 ) ) ;
#60475=CARTESIAN_POINT ( 'NONE',  ( 6.000000000000003553, 287.6250000034140157, -2.485281374238571761 ) ) ;
#60501=CARTESIAN_POINT ( 'NONE',  ( 4.999999999999993783, 74.16666666666667140, 8.660254037844390851 ) ) ;
#60503=CARTESIAN_POINT ( 'NONE',  ( -4.242640687119285658, 296.1250000000000000, 4.242640687119287435 ) ) ;
#60516=CARTESIAN_POINT ( 'NONE',  ( -2.679491924311235618, 183.5416666666667140, 10.00000000000000000 ) ) ;
#60519=CARTESIAN_POINT ( 'NONE',  ( 5.676582343749993598, 155.2604166632526983, 9.832129032723422313 ) ) ;
#60527=CARTESIAN_POINT ( 'NONE',  ( 3.042071309553167069, 12.13541666325268054, -11.35316468749999785 ) ) ;
#60533=CARTESIAN_POINT ( 'NONE',  ( -1.836970198721029983E-15, 45.62499999317203958, 10.00000000000000178 ) ) ;
#60536=CARTESIAN_POINT ( 'NONE',  ( 1.224646799147353454E-15, 300.0000000000000000, -10.00000000000000178 ) ) ;
#60539=CARTESIAN_POINT ( 'NONE',  ( 0.000000000000000000, 300.0000000000000000, 0.000000000000000000 ) ) ;
#60541=CARTESIAN_POINT ( 'NONE',  ( 10.00000000000000533, 30.20833333333333570, -2.679491924311228068 ) ) ;
#60544=VECTOR ( 'NONE', #35617, 1000.000000000000000 ) ;
#60545=CARTESIAN_POINT ( 'NONE',  ( -9.832129032723420536, 128.6979166632526983, 5.676582343749997150 ) ) ;
#60553=CARTESIAN_POINT ( 'NONE',  ( -3.042071309553173730, 124.3229166632526983, 11.35316468749999785 ) ) ;
#60554=CARTESIAN_POINT ( 'NONE',  ( 7.320508075688774596, 147.4999999931720538, -7.320508075688774596 ) ) ;
#60559=CARTESIAN_POINT ( 'NONE',  ( -8.311093377946836114, 112.9687499965860269, -8.311093377946837890 ) ) ;
#60563=CARTESIAN_POINT ( 'NONE',  ( 5.676582343749993598, 25.26041666325268764, 9.832129032723422313 ) ) ;
#60565=CARTESIAN_POINT ( 'NONE',  ( -1.836970198721029983E-15, 15.62499999317203248, 10.00000000000000178 ) ) ;
#60567=CARTESIAN_POINT ( 'NONE',  ( 10.00000000000000178, 116.8749999931720396, 0.000000000000000000 ) ) ;
#60571=CARTESIAN_POINT ( 'NONE',  ( 6.676582343750003368, 290.0156250017069510, -2.765530957081997254 ) ) ;
#60573=CARTESIAN_POINT ( 'NONE',  ( 9.832129032723416984, 215.6770833299193555, 5.676582343750006032 ) ) ;
#60575=CARTESIAN_POINT ( 'NONE',  ( 5.676582343750001591, 136.9270833299193555, -9.832129032723420536 ) ) ;
#60585=CARTESIAN_POINT ( 'NONE',  ( -10.00000000000010125, 172.7083333333333428, 2.679491924311248496 ) ) ;
#60589=CARTESIAN_POINT ( 'NONE',  ( 6.123233995736767268E-16, 28.12499999317203603, -10.00000000000000178 ) ) ;
#60591=CARTESIAN_POINT ( 'NONE',  ( -11.35316468750000141, 188.2812499965860127, -1.390361679473963753E-15 ) ) ;
#60593=DIRECTION ( 'NONE',  ( -0.000000000000000000, 1.000000000000000000, -0.000000000000000000 ) ) ;
#60594=CARTESIAN_POINT ( 'NONE',  ( -4.721056650415999201, 294.3281250017069510, -4.721056650415999201 ) ) ;
#60596=CARTESIAN_POINT ( 'NONE',  ( 4.999999999999993783, 131.0416666598387110, 8.660254037844390851 ) ) ;
#60606=CYLINDRICAL_SURFACE ( 'NONE', #29341, 10.00000000000000178 ) ;
#60607=CARTESIAN_POINT ( 'NONE',  ( 6.123233995736767268E-16, 163.1249999931720254, -10.00000000000000178 ) ) ;
#60609=CARTESIAN_POINT ( 'NONE',  ( 9.832129032723420536, 111.5104166632526841, -5.676582343749999815 ) ) ;
#60610=DIRECTION ( 'NONE',  ( -0.000000000000000000, 1.000000000000000000, -0.000000000000000000 ) ) ;
#60614=FACE_OUTER_BOUND ( 'NONE', #4112, .T. ) ;
#60617=CARTESIAN_POINT ( 'NONE',  ( 4.242640687119287435, 287.4375000034140157, 4.242640687119285658 ) ) ;
#60622=CARTESIAN_POINT ( 'NONE',  ( 8.311093377946837890, 196.7187499965860127, -8.311093377946837890 ) ) ;
#60625=CARTESIAN_POINT ( 'NONE',  ( 6.139223773318740029, 225.9999999999999147, 8.200589933689730771 ) ) ;
#60630=CARTESIAN_POINT ( 'NONE',  ( 8.311093377946834337, 80.15624999658599847, 8.311093377946839666 ) ) ;
#60638=CARTESIAN_POINT ( 'NONE',  ( -11.35316468749999785, 93.07291666325266988, -3.042071309553167513 ) ) ;
#60642=CARTESIAN_POINT ( 'NONE',  ( 0.000000000000000000, 300.0000000000000000, 10.00000000000000178 ) ) ;
#60646=CARTESIAN_POINT ( 'NONE',  ( 11.35316468749999963, 80.98958332991934128, -3.042071309553165293 ) ) ;
#60649=CARTESIAN_POINT ( 'NONE',  ( 8.660254037844389075, 167.2916666598387110, -5.000000000000000000 ) ) ;
#60652=CARTESIAN_POINT ( 'NONE',  ( 11.35316468749999785, 55.88541666325267698, 3.042071309553174174 ) ) ;
#60653=CARTESIAN_POINT ( 'NONE',  ( -6.676582343750001591, 295.4531250017069510, 0.000000000000000000 ) ) ;
#60655=CARTESIAN_POINT ( 'NONE',  ( -11.35316468750000141, 208.4895833299193555, 3.042071309553159963 ) ) ;
#60661=CARTESIAN_POINT ( 'NONE',  ( -9.832129032723420536, 188.6979166632526983, 5.676582343749997150 ) ) ;
#60668=CARTESIAN_POINT ( 'NONE',  ( 11.35316468749999785, 175.8854166632526983, 3.042071309553174174 ) ) ;
#60670=EDGE_CURVE ( 'NONE', #49815, #26710, #6771, .T. ) ;
#60677=AXIS2_PLACEMENT_3D ( 'NONE', #37862, #20112, #44631 ) ;
#60693=VERTEX_POINT ( 'NONE', #10711 ) ;
#60696=CARTESIAN_POINT ( 'NONE',  ( -9.832129032723420536, 74.01041666325268409, 5.676582343749997150 ) ) ;
#60701=CARTESIAN_POINT ( 'NONE',  ( 1.226468279477575784E-15, 295.8593750017070079, 6.676582343750001591 ) ) ;
#60712=CARTESIAN_POINT ( 'NONE',  ( -4.242640687119286547, 292.9375000034140157, -4.242640687119286547 ) ) ;
#60715=CARTESIAN_POINT ( 'NONE',  ( 4.242640687119287435, 288.4375000034140157, 4.242640687119285658 ) ) ;
#60718=CARTESIAN_POINT ( 'NONE',  ( 8.311093377946837890, 36.40624999658602690, -8.311093377946837890 ) ) ;
#60719=CARTESIAN_POINT ( 'NONE',  ( 10.00000000000000355, 149.7916666666666856, 2.679491924311236506 ) ) ;
#60720=CARTESIAN_POINT ( 'NONE',  ( 7.320508075688771044, 11.24999999317203248, 7.320508075688775484 ) ) ;
#60721=ORIENTED_EDGE ( 'NONE', *, *, #15445, .F. ) ;
#60724=CARTESIAN_POINT ( 'NONE',  ( 5.676582343749993598, 54.94791666325268409, 9.832129032723422313 ) ) ;
#60730=CARTESIAN_POINT ( 'NONE',  ( -5.676582343749998039, 32.44791666325268409, -9.832129032723420536 ) ) ;
#60732=CARTESIAN_POINT ( 'NONE',  ( -2.679491924311235174, 50.41666665983868967, 10.00000000000000000 ) ) ;
#60734=CARTESIAN_POINT ( 'NONE',  ( 8.311093377946834337, 165.1562499965860127, 8.311093377946839666 ) ) ;
#60735=CARTESIAN_POINT ( 'NONE',  ( 4.999999999999993783, 131.0416666598387110, 8.660254037844390851 ) ) ;
#60740=CARTESIAN_POINT ( 'NONE',  ( -9.832129032723418760, 18.17708332991935194, -5.676582343750004256 ) ) ;
#60747=CARTESIAN_POINT ( 'NONE',  ( -9.832129032723418760, 147.8645833299193555, -5.676582343750004256 ) ) ;
#60755=DIRECTION ( 'NONE',  ( -0.000000000000000000, 1.000000000000000000, -0.000000000000000000 ) ) ;
#60757=CARTESIAN_POINT ( 'NONE',  ( -8.311093377946836114, 102.9687499965859985, -8.311093377946837890 ) ) ;
#60759=EDGE_CURVE ( 'NONE', #15764, #58925, #68006, .T. ) ;
#60760=CARTESIAN_POINT ( 'NONE',  ( 5.000000000000006217, 15.83333333333333748, -8.660254037844394404 ) ) ;
#60776=CARTESIAN_POINT ( 'NONE',  ( -2.765530957081996810, 299.2656250017070079, -6.676582343750002480 ) ) ;
#60787=CARTESIAN_POINT ( 'NONE',  ( 10.00000000000000178, 105.0000000000000142, 0.000000000000000000 ) ) ;
#60789=CARTESIAN_POINT ( 'NONE',  ( 1.226468279477575784E-15, 291.8593750017070079, 6.676582343750001591 ) ) ;
#60795=CARTESIAN_POINT ( 'NONE',  ( -2.679491924311087736, 185.4166666598386826, 10.00000000000008349 ) ) ;
#60800=CARTESIAN_POINT ( 'NONE',  ( -11.35316468749999785, 8.072916663252682312, -3.042071309553167513 ) ) ;
#60802=CARTESIAN_POINT ( 'NONE',  ( 8.311093377946834337, 195.4687499965859843, 8.311093377946839666 ) ) ;
#60811=CARTESIAN_POINT ( 'NONE',  ( 5.676582343749993598, 9.947916663252682312, 9.832129032723422313 ) ) ;
#60817=CARTESIAN_POINT ( 'NONE',  ( -8.660254037844387298, 58.95833332650537528, -5.000000000000004441 ) ) ;
#60819=CARTESIAN_POINT ( 'NONE',  ( 6.951808397369818766E-16, 127.0312499965860269, -11.35316468750000141 ) ) ;
#60822=CARTESIAN_POINT ( 'NONE',  ( -2.679491924311225848, 93.33333332650538239, -10.00000000000000178 ) ) ;
#60829=CARTESIAN_POINT ( 'NONE',  ( -6.676582343750003368, 292.5468750017068942, -2.765530957081996810 ) ) ;
#60830=CARTESIAN_POINT ( 'NONE',  ( 10.00000000000000000, 186.6666666598386826, 2.679491924311235618 ) ) ;
#60832=CARTESIAN_POINT ( 'NONE',  ( 3.042071309553159519, 174.7395833299193555, 11.35316468750000141 ) ) ;
#60839=EDGE_CURVE ( 'NONE', #53888, #53638, #22162, .T. ) ;
#60842=CARTESIAN_POINT ( 'NONE',  ( -5.676582343750006032, 154.4270833299193555, 9.832129032723418760 ) ) ;
#60846=CARTESIAN_POINT ( 'NONE',  ( -2.085542519210945728E-15, 64.84374999658601268, 11.35316468750000141 ) ) ;
#60847=( BOUNDED_CURVE ( )  B_SPLINE_CURVE ( 2, ( #65323, #43045, #66822, #42678, #66064, #20787, #61157, #38156, #32121, #37786, #15124, #65690, #71344 ),
 .UNSPECIFIED., .F., .F. ) 
 B_SPLINE_CURVE_WITH_KNOTS ( ( 3, 2, 2, 2, 2, 2, 3 ),
 ( 1.554290449679109676, 1.559524058767997712, 1.564757667856885970, 1.569991276945774006, 1.575224886034662042, 1.580458495123550300, 1.585692104212438336 ),
 .UNSPECIFIED. ) 
 CURVE ( )  GEOMETRIC_REPRESENTATION_ITEM ( )  RATIONAL_B_SPLINE_CURVE ( ( 1.000000000000000000, 0.9659258262890683122, 1.000000000000000000, 0.9659258262890683122, 1.000000000000000000, 0.9659258262890683122, 1.000000000000000000, 0.9659258262890683122, 1.000000000000000000, 0.9659258262890683122, 1.000000000000000000, 0.9659258262890683122, 1.000000000000000000 ) ) 
 REPRESENTATION_ITEM ( '' )  );
#60853=CARTESIAN_POINT ( 'NONE',  ( 1.102182119232618108E-15, 288.3125000034140157, 6.000000000000001776 ) ) ;
#60867=EDGE_LOOP ( 'NONE', ( #35550, #17284, #39983, #12778 ) ) ;
#60868=CARTESIAN_POINT ( 'NONE',  ( 2.485281374238987873, 299.3125000000000000, 5.999999999999586997 ) ) ;
#60870=CARTESIAN_POINT ( 'NONE',  ( -1.836970198721029983E-15, 3.750000000000000444, 10.00000000000000178 ) ) ;
#60874=CARTESIAN_POINT ( 'NONE',  ( 8.660254037844385522, 74.58333333333332860, 5.000000000000005329 ) ) ;
#60876=CARTESIAN_POINT ( 'NONE',  ( -6.000000000000000888, 294.0625000000000000, 2.485281374238575758 ) ) ;
#60879=CARTESIAN_POINT ( 'NONE',  ( -8.660254037844390851, 127.0833333333333570, -5.000000000000007994 ) ) ;
#60890=CARTESIAN_POINT ( 'NONE',  ( -8.660254037844387298, 187.0833333333333428, -5.000000000000004441 ) ) ;
#60893=CARTESIAN_POINT ( 'NONE',  ( -9.832129032723418760, 158.1770833299193555, -5.676582343750004256 ) ) ;
#60894=LINE ( 'NONE', #50318, #52981 ) ;
#60896=CARTESIAN_POINT ( 'NONE',  ( 10.00000000000018652, 155.0000000000001137, 0.000000000000000000 ) ) ;
#60901=CARTESIAN_POINT ( 'NONE',  ( 11.35316468750000141, 6.093749996586017126, 0.000000000000000000 ) ) ;
#60906=CARTESIAN_POINT ( 'NONE',  ( -1.836970198721029983E-15, 55.62499999317203958, 10.00000000000000178 ) ) ;
#60909=CARTESIAN_POINT ( 'NONE',  ( 7.320508075688783478, 220.6250000000000284, -7.320508075688783478 ) ) ;
#60914=EDGE_LOOP ( 'NONE', ( #17532, #54151, #46024 ) ) ;
#60918=CARTESIAN_POINT ( 'NONE',  ( -5.676582343749998039, 127.4479166632526983, -9.832129032723420536 ) ) ;
#60920=CARTESIAN_POINT ( 'NONE',  ( 1.102182119232618108E-15, 298.2500000000000000, 6.000000000000001776 ) ) ;
#60926=FACE_OUTER_BOUND ( 'NONE', #35650, .T. ) ;
#60928=CARTESIAN_POINT ( 'NONE',  ( 9.832129032723420536, 126.1979166632526983, -5.676582343749999815 ) ) ;
#60933=CARTESIAN_POINT ( 'NONE',  ( 5.676582343749993598, 115.2604166632526983, 9.832129032723422313 ) ) ;
#60938=CARTESIAN_POINT ( 'NONE',  ( -9.832129032723418760, 28.17708332991935194, -5.676582343750004256 ) ) ;
#60946=CARTESIAN_POINT ( 'NONE',  ( 4.721056650415999201, 288.0781250017069510, -4.721056650415999201 ) ) ;
#60949=CARTESIAN_POINT ( 'NONE',  ( 1.102182119232618108E-15, 297.2500000000000000, 6.000000000000001776 ) ) ;
#60952=CARTESIAN_POINT ( 'NONE',  ( -9.832129032723418760, 143.1770833299193555, -5.676582343750004256 ) ) ;
#60958=ORIENTED_EDGE ( 'NONE', *, *, #65534, .T. ) ;
#60962=( BOUNDED_CURVE ( )  B_SPLINE_CURVE ( 2, ( #73359, #15627, #49217, #49972, #43942, #33020, #55278, #10359, #26575, #72615, #44688, #21293, #66951 ),
 .UNSPECIFIED., .F., .F. ) 
 B_SPLINE_CURVE_WITH_KNOTS ( ( 3, 2, 2, 2, 2, 2, 3 ),
 ( 2.778886174319656455, 2.784119686266136373, 2.789353198316371518, 2.794586710366607107, 2.799820222416842252, 2.805053734467077842, 2.810287246517312987 ),
 .UNSPECIFIED. ) 
 CURVE ( )  GEOMETRIC_REPRESENTATION_ITEM ( )  RATIONAL_B_SPLINE_CURVE ( ( 1.000000000000000000, 0.9659258262890683122, 1.000000000000000000, 0.9659258262890683122, 1.000000000000000000, 0.9659258262890683122, 1.000000000000000000, 0.9659258262890683122, 1.000000000000000000, 0.9659258262890683122, 1.000000000000000000, 0.9659258262890725311, 0.9999999999999957812 ) ) 
 REPRESENTATION_ITEM ( '' )  );
#60964=ORIENTED_EDGE ( 'NONE', *, *, #64194, .T. ) ;
#60968=CARTESIAN_POINT ( 'NONE',  ( -2.085542519210945728E-15, 189.5312499965860127, 11.35316468750000141 ) ) ;
#60971=CARTESIAN_POINT ( 'NONE',  ( -4.721056650415998313, 288.5781250017069510, 4.721056650416000089 ) ) ;
#60973=CARTESIAN_POINT ( 'NONE',  ( 8.660254037844383745, 95.41666666666667140, -4.999999999999997335 ) ) ;
#60977=CARTESIAN_POINT ( 'NONE',  ( 2.679491924311075302, 165.8333333265053398, 10.00000000000008704 ) ) ;
#60984=CARTESIAN_POINT ( 'NONE',  ( 9.832129032723416984, 120.6770833299193555, 5.676582343750006032 ) ) ;
#60989=EDGE_CURVE ( 'NONE', #55811, #20100, #39592, .T. ) ;
#60991=CARTESIAN_POINT ( 'NONE',  ( 11.35316468749999785, 220.5729166632526983, 3.042071309553174174 ) ) ;
#60995=CARTESIAN_POINT ( 'NONE',  ( 3.042071309553159519, 210.0520833299193555, 11.35316468750000141 ) ) ;
#60997=DIRECTION ( 'NONE',  ( 0.000000000000000000, 0.000000000000000000, 1.000000000000000000 ) ) ;
#61002=CARTESIAN_POINT ( 'NONE',  ( 5.676582343749993598, 84.94791666325268409, 9.832129032723422313 ) ) ;
#61008=CARTESIAN_POINT ( 'NONE',  ( 11.35316468749999785, 85.57291666325268409, 3.042071309553174174 ) ) ;
#61010=CARTESIAN_POINT ( 'NONE',  ( 8.660254037844389075, 207.2916666598387110, -5.000000000000000000 ) ) ;
#61017=CARTESIAN_POINT ( 'NONE',  ( -2.085542519210945728E-15, 84.53124999658602690, 11.35316468750000141 ) ) ;
#61022=CARTESIAN_POINT ( 'NONE',  ( 6.123233995736767268E-16, 163.1249999931720254, -10.00000000000000178 ) ) ;
#61024=CARTESIAN_POINT ( 'NONE',  ( 8.311093377946834337, 70.46874999658599847, 8.311093377946839666 ) ) ;
#61025=CARTESIAN_POINT ( 'NONE',  ( 2.765530957081996366, 292.1406250017070079, -6.676582343750003368 ) ) ;
#61028=CARTESIAN_POINT ( 'NONE',  ( 3.042071309553159519, 204.7395833299193271, 11.35316468750000141 ) ) ;
#61033=CARTESIAN_POINT ( 'NONE',  ( -3.042071309553173730, 204.3229166632526699, 11.35316468749999785 ) ) ;
#61039=CARTESIAN_POINT ( 'NONE',  ( -11.35316468750000141, 198.8020833299193555, 3.042071309553159963 ) ) ;
#61046=DIRECTION ( 'NONE',  ( 0.000000000000000000, 0.000000000000000000, 1.000000000000000000 ) ) ;
#61048=( BOUNDED_CURVE ( )  B_SPLINE_CURVE ( 2, ( #18241, #60352, #912, #55090, #46907, #31694, #70299, #41256, #64265, #30302, #54715, #60732, #3021 ),
 .UNSPECIFIED., .F., .F. ) 
 B_SPLINE_CURVE_WITH_KNOTS ( ( 3, 2, 2, 2, 2, 2, 3 ),
 ( 0.2010869565217391630, 0.2028985507246377218, 0.2047101449275362528, 0.2065217391304348116, 0.2083333333333333426, 0.2101449275362318736, 0.2119565217391304324 ),
 .UNSPECIFIED. ) 
 CURVE ( )  GEOMETRIC_REPRESENTATION_ITEM ( )  RATIONAL_B_SPLINE_CURVE ( ( 0.9999999999999994449, 0.9659258262890688673, 1.000000000000000000, 0.9659258262890683122, 1.000000000000000000, 0.9659258262890683122, 1.000000000000000000, 0.9659258262890683122, 1.000000000000000000, 0.9659258262890683122, 1.000000000000000000, 0.9659258262890683122, 1.000000000000000000 ) ) 
 REPRESENTATION_ITEM ( '' )  );
#61049=VERTEX_POINT ( 'NONE', #36976 ) ;
#61057=CARTESIAN_POINT ( 'NONE',  ( 1.224646799147353454E-15, 300.0000000000000000, -10.00000000000000178 ) ) ;
#61062=VECTOR ( 'NONE', #6765, 1000.000000000000000 ) ;
#61069=CARTESIAN_POINT ( 'NONE',  ( -3.042071309553164404, 72.55208332991934128, -11.35316468749999963 ) ) ;
#61074=CARTESIAN_POINT ( 'NONE',  ( -2.765530957081996810, 290.4218750017069510, -6.676582343750002480 ) ) ;
#61083=CARTESIAN_POINT ( 'NONE',  ( -7.320508075688778149, 19.99999999317203603, 7.320508075688769267 ) ) ;
#61088=CARTESIAN_POINT ( 'NONE',  ( -3.042071309553164404, 47.23958332991936260, -11.35316468749999963 ) ) ;
#61091=CARTESIAN_POINT ( 'NONE',  ( 2.679491924311222739, 25.83333332650536107, 10.00000000000000355 ) ) ;
#61093=ORIENTED_EDGE ( 'NONE', *, *, #51793, .T. ) ;
#61094=CARTESIAN_POINT ( 'NONE',  ( 7.320508075688774596, 142.4999999931720254, -7.320508075688774596 ) ) ;
#61096=CARTESIAN_POINT ( 'NONE',  ( -8.311093377946841443, 53.90624999658601979, 8.311093377946830785 ) ) ;
#61102=CARTESIAN_POINT ( 'NONE',  ( -8.311093377946836114, 47.65624999658601268, -8.311093377946837890 ) ) ;
#61105=CARTESIAN_POINT ( 'NONE',  ( -8.311093377946841443, 158.9062499965860411, 8.311093377946830785 ) ) ;
#61107=CARTESIAN_POINT ( 'NONE',  ( -7.320508075688778149, 134.9999999931720538, 7.320508075688769267 ) ) ;
#61109=ORIENTED_EDGE ( 'NONE', *, *, #55476, .F. ) ;
#61110=DIRECTION ( 'NONE',  ( 0.000000000000000000, 0.000000000000000000, 1.000000000000000000 ) ) ;
#61111=CARTESIAN_POINT ( 'NONE',  ( -3.042071309553163960, 37.55208332991935549, -11.35316468749999963 ) ) ;
#61118=CARTESIAN_POINT ( 'NONE',  ( -2.085542519210945728E-15, 169.5312499965860411, 11.35316468750000141 ) ) ;
#61128=CARTESIAN_POINT ( 'NONE',  ( 5.676582343750001591, 96.92708332991935549, -9.832129032723420536 ) ) ;
#61157=CARTESIAN_POINT ( 'NONE',  ( 10.00000000000000355, 125.0000000000000000, 0.000000000000000000 ) ) ;
#61161=CARTESIAN_POINT ( 'NONE',  ( 2.679491924305354544, 58.95833333333284543, 10.00000000000347988 ) ) ;
#61163=CARTESIAN_POINT ( 'NONE',  ( 7.320508075688771044, 109.3750000000000000, 7.320508075688775484 ) ) ;
#61165=CARTESIAN_POINT ( 'NONE',  ( -2.765530957081998586, 293.7968750017069510, 6.676582343750001591 ) ) ;
#61167=ADVANCED_FACE ( 'NONE', ( #11288 ), #55834, .T. ) ;
#61179=CARTESIAN_POINT ( 'NONE',  ( -7.320508075688778149, 94.99999999317202537, 7.320508075688769267 ) ) ;
#61180=CARTESIAN_POINT ( 'NONE',  ( 5.676582343750001591, 1.614583329919349719, -9.832129032723420536 ) ) ;
#61183=CARTESIAN_POINT ( 'NONE',  ( -3.042071309553164404, 192.5520833299193271, -11.35316468749999963 ) ) ;
#61184=CARTESIAN_POINT ( 'NONE',  ( -1.836970198721029983E-15, 135.6249999931720538, 10.00000000000000178 ) ) ;
#61186=CARTESIAN_POINT ( 'NONE',  ( 6.000000000000001776, 290.5000000000000000, -7.347880794884121708E-16 ) ) ;
#61191=CARTESIAN_POINT ( 'NONE',  ( -11.35316468749999785, 3.072916663252683200, -3.042071309553167513 ) ) ;
#61197=CARTESIAN_POINT ( 'NONE',  ( -8.311093377946841443, 8.906249996586016238, 8.311093377946834337 ) ) ;
#61199=CARTESIAN_POINT ( 'NONE',  ( -9.832129032723420536, 118.6979166632526841, 5.676582343749997150 ) ) ;
#61200=CARTESIAN_POINT ( 'NONE',  ( 5.000000000000001776, 82.70833332650536818, -8.660254037844389075 ) ) ;
#61203=CARTESIAN_POINT ( 'NONE',  ( -7.320508075688773708, 198.7499999931720254, -7.320508075688774596 ) ) ;
#61204=CARTESIAN_POINT ( 'NONE',  ( 7.320508075688779037, 145.6249999999999716, -7.320508075688779037 ) ) ;
#61206=CARTESIAN_POINT ( 'NONE',  ( -1.307295064324774714, 225.9999999999999432, -9.935834282059307299 ) ) ;
#61209=CARTESIAN_POINT ( 'NONE',  ( 4.721056650415999201, 289.2343750017069510, -4.721056650415999201 ) ) ;
#61210=CARTESIAN_POINT ( 'NONE',  ( 7.320508075688771044, 186.2499999931720254, 7.320508075688775484 ) ) ;
#61212=CARTESIAN_POINT ( 'NONE',  ( -10.00000000000000000, 209.1666666598386826, -2.679491924311229845 ) ) ;
#61219=CARTESIAN_POINT ( 'NONE',  ( 9.832129032723416984, 160.6770833299193555, 5.676582343750006032 ) ) ;
#61223=CARTESIAN_POINT ( 'NONE',  ( -9.832129032723418760, 63.17708332991934839, -5.676582343750004256 ) ) ;
#61230=CARTESIAN_POINT ( 'NONE',  ( -2.485281374238572649, 289.2500000034140157, 6.000000000000002665 ) ) ;
#61239=ORIENTED_EDGE ( 'NONE', *, *, #27472, .T. ) ;
#61248=CARTESIAN_POINT ( 'NONE',  ( -1.328591152368359007E-11, 1.250000000001033174, -10.00000000000000533 ) ) ;
#61252=CARTESIAN_POINT ( 'NONE',  ( -7.320508075688773708, 66.87500000000001421, -7.320508075688774596 ) ) ;
#61254=CARTESIAN_POINT ( 'NONE',  ( 1.102182119232618108E-15, 294.2500000000000000, 6.000000000000001776 ) ) ;
#61266=CARTESIAN_POINT ( 'NONE',  ( -7.320508075688778149, 188.1250000000000000, 7.320508075688769267 ) ) ;
#61270=CARTESIAN_POINT ( 'NONE',  ( 9.832129032723420536, 156.5104166632526983, -5.676582343749999815 ) ) ;
#61273=CARTESIAN_POINT ( 'NONE',  ( -2.249999999999999112, 284.0000000000000000, 5.562148865321749014 ) ) ;
#61274=CARTESIAN_POINT ( 'NONE',  ( -7.320508075688773708, 83.74999999317203958, -7.320508075688774596 ) ) ;
#61278=CARTESIAN_POINT ( 'NONE',  ( 3.042071309553167069, 22.13541666325268409, -11.35316468749999785 ) ) ;
#61285=CARTESIAN_POINT ( 'NONE',  ( 8.660254037844389075, 52.29166665983870388, -5.000000000000000000 ) ) ;
#61288=LINE ( 'NONE', #44310, #14401 ) ;
#61290=CARTESIAN_POINT ( 'NONE',  ( 0.000000000000000000, 300.0000000000000000, 0.000000000000000000 ) ) ;
#61300=CARTESIAN_POINT ( 'NONE',  ( 3.042071309553167069, 126.8229166632526841, -11.35316468749999785 ) ) ;
#61302=DIRECTION ( 'NONE',  ( 0.000000000000000000, 0.000000000000000000, 1.000000000000000000 ) ) ;
#61306=CARTESIAN_POINT ( 'NONE',  ( 0.000000000000000000, 300.0000000000000000, 0.000000000000000000 ) ) ;
#61308=CARTESIAN_POINT ( 'NONE',  ( -3.042071309553163960, 127.2395833299193555, -11.35316468749999963 ) ) ;
#61313=CARTESIAN_POINT ( 'NONE',  ( -11.35316468750000141, 113.8020833299193555, 3.042071309553159963 ) ) ;
#61317=CARTESIAN_POINT ( 'NONE',  ( 5.676582343749993598, 20.26041666325268409, 9.832129032723422313 ) ) ;
#61324=CARTESIAN_POINT ( 'NONE',  ( 1.226468279477575784E-15, 288.7031250017069510, 6.676582343750001591 ) ) ;
#61325=CARTESIAN_POINT ( 'NONE',  ( 10.00000000000000000, 111.6666666598387110, 2.679491924311235618 ) ) ;
#61327=CARTESIAN_POINT ( 'NONE',  ( 9.832129032723420536, 136.5104166632526983, -5.676582343749999815 ) ) ;
#61339=DIRECTION ( 'NONE',  ( -0.000000000000000000, 1.000000000000000000, -0.000000000000000000 ) ) ;
#61343=CARTESIAN_POINT ( 'NONE',  ( -2.249999999999999112, 284.0000000000000000, 7.677076266392047543 ) ) ;
#61344=CARTESIAN_POINT ( 'NONE',  ( 6.951808397369818766E-16, 187.0312499965860127, -11.35316468750000141 ) ) ;
#61348=CARTESIAN_POINT ( 'NONE',  ( 2.765530957081996366, 289.1406250017069510, -6.676582343750002480 ) ) ;
#61361=CARTESIAN_POINT ( 'NONE',  ( 9.832129032723420536, 116.5104166632526841, -5.676582343749999815 ) ) ;
#61362=CARTESIAN_POINT ( 'NONE',  ( -6.000000000000001776, 296.0000000000000000, 0.000000000000000000 ) ) ;
#61368=CARTESIAN_POINT ( 'NONE',  ( 9.865726904258298902, 225.1318477000477003, -1.659788900511623311 ) ) ;
#61369=EDGE_CURVE ( 'NONE', #18479, #48053, #47288, .T. ) ;
#61370=CARTESIAN_POINT ( 'NONE',  ( -5.676582343750006032, 224.1145833299193839, 9.832129032723418760 ) ) ;
#61373=CARTESIAN_POINT ( 'NONE',  ( 11.35316468750000141, 211.0937499965860411, 0.000000000000000000 ) ) ;
#61374=CARTESIAN_POINT ( 'NONE',  ( 6.517621199079068006, 225.9999999999999147, 7.979021773805921036 ) ) ;
#61380=CARTESIAN_POINT ( 'NONE',  ( 11.35316468750000141, 90.78124999658602690, 0.000000000000000000 ) ) ;
#61386=CARTESIAN_POINT ( 'NONE',  ( -5.676582343749998039, 82.44791666325268409, -9.832129032723420536 ) ) ;
#61394=CARTESIAN_POINT ( 'NONE',  ( 11.35316468750000141, 85.78124999658602690, 0.000000000000000000 ) ) ;
#61399=CARTESIAN_POINT ( 'NONE',  ( 7.320508075688771044, 186.2499999931719969, 7.320508075688775484 ) ) ;
#61401=CARTESIAN_POINT ( 'NONE',  ( 9.832129032723416984, 70.67708332991935549, 5.676582343750006032 ) ) ;
#61402=CARTESIAN_POINT ( 'NONE',  ( -2.765530957081996810, 295.2656250017070079, -6.676582343750003368 ) ) ;
#61404=CARTESIAN_POINT ( 'NONE',  ( -11.35316468749999785, 208.0729166632526983, -3.042071309553167513 ) ) ;
#61405=ORIENTED_EDGE ( 'NONE', *, *, #38700, .T. ) ;
#61406=CARTESIAN_POINT ( 'NONE',  ( -1.836970198721029983E-15, 70.62499999317203958, 10.00000000000000178 ) ) ;
#61410=CARTESIAN_POINT ( 'NONE',  ( 6.951808397369818766E-16, 212.0312499965860411, -11.35316468750000141 ) ) ;
#61412=LINE ( 'NONE', #27078, #45650 ) ;
#61414=CARTESIAN_POINT ( 'NONE',  ( 5.676582343750001591, 196.9270833299193839, -9.832129032723420536 ) ) ;
#61415=( BOUNDED_CURVE ( )  B_SPLINE_CURVE ( 2, ( #10900, #16919, #67865, #16534, #5619, #10526, #46341, #33191, #4877, #39942, #5249, #63316, #27872 ),
 .UNSPECIFIED., .F., .F. ) 
 B_SPLINE_CURVE_WITH_KNOTS ( ( 3, 2, 2, 2, 2, 2, 3 ),
 ( 2.590487804266785599, 2.595720217480772529, 2.600952630694759460, 2.606185043908746390, 2.611417457122733321, 2.616649870336720252, 2.621882283550707182 ),
 .UNSPECIFIED. ) 
 CURVE ( )  GEOMETRIC_REPRESENTATION_ITEM ( )  RATIONAL_B_SPLINE_CURVE ( ( 1.000000000000001776, 0.9659258262890662028, 0.9999999999999998890, 0.9659258262890683122, 0.9999999999999998890, 0.9659258262890683122, 0.9999999999999998890, 0.9659258262890683122, 0.9999999999999998890, 0.9659258262890683122, 0.9999999999999998890, 0.9659258262894191427, 0.9999999999996490585 ) ) 
 REPRESENTATION_ITEM ( '' )  );
#61422=CARTESIAN_POINT ( 'NONE',  ( 6.123233995736767268E-16, 11.25000000000000178, -10.00000000000000178 ) ) ;
#61432=ORIENTED_EDGE ( 'NONE', *, *, #4836, .F. ) ;
#61436=DIRECTION ( 'NONE',  ( 0.000000000000000000, 0.000000000000000000, 1.000000000000000000 ) ) ;
#61445=CARTESIAN_POINT ( 'NONE',  ( 3.042071309553167069, 72.13541666325268409, -11.35316468749999785 ) ) ;
#61450=CARTESIAN_POINT ( 'NONE',  ( -4.721056650415998313, 288.7343750017069510, 4.721056650416000089 ) ) ;
#61456=ORIENTED_EDGE ( 'NONE', *, *, #48868, .F. ) ;
#61459=CARTESIAN_POINT ( 'NONE',  ( 3.042071309553159519, 170.0520833299193271, 11.35316468750000141 ) ) ;
#61467=CARTESIAN_POINT ( 'NONE',  ( -11.35316468749999785, 48.07291666325268409, -3.042071309553167513 ) ) ;
#61469=CARTESIAN_POINT ( 'NONE',  ( -1.836970198721029983E-15, 25.62499999317203248, 10.00000000000000178 ) ) ;
#61474=CARTESIAN_POINT ( 'NONE',  ( 9.832129032723416984, 50.36458332991934839, 5.676582343750006032 ) ) ;
#61477=DIRECTION ( 'NONE',  ( 0.000000000000000000, 0.000000000000000000, 1.000000000000000000 ) ) ;
#61480=CARTESIAN_POINT ( 'NONE',  ( 5.676582343749993598, 49.94791666325268409, 9.832129032723422313 ) ) ;
#61483=CARTESIAN_POINT ( 'NONE',  ( 6.951808397369818766E-16, 167.0312499965860411, -11.35316468750000141 ) ) ;
#61485=CARTESIAN_POINT ( 'NONE',  ( -10.00000000000000000, 144.1666666598386541, -2.679491924311229845 ) ) ;
#61488=CARTESIAN_POINT ( 'NONE',  ( -9.832129032723418760, 38.17708332991935549, -5.676582343750004256 ) ) ;
#61495=CARTESIAN_POINT ( 'NONE',  ( 11.35316468749999785, 165.5729166632526699, 3.042071309553174174 ) ) ;
#61504=DIRECTION ( 'NONE',  ( -0.000000000000000000, 1.000000000000000000, -0.000000000000000000 ) ) ;
#61505=CARTESIAN_POINT ( 'NONE',  ( -11.35316468750000141, 118.8020833299193413, 3.042071309553159963 ) ) ;
#61508=CARTESIAN_POINT ( 'NONE',  ( 2.679491924297975558, 13.95833333333215087, 10.00000000000766676 ) ) ;
#61519=( BOUNDED_CURVE ( )  B_SPLINE_CURVE ( 2, ( #5274, #61862, #74292, #4527, #39598, #28643, #11299, #56589, #10184, #34332, #21857, #55846, #4904 ),
 .UNSPECIFIED., .F., .F. ) 
 B_SPLINE_CURVE_WITH_KNOTS ( ( 3, 2, 2, 2, 2, 2, 3 ),
 ( 0.3315217391304347561, 0.3333333333333333148, 0.3351449275362318736, 0.3369565217391303769, 0.3387681159420289356, 0.3405797101449274944, 0.3423913043478260532 ),
 .UNSPECIFIED. ) 
 CURVE ( )  GEOMETRIC_REPRESENTATION_ITEM ( )  RATIONAL_B_SPLINE_CURVE ( ( 1.000000000000000000, 0.9659258262890683122, 1.000000000000000000, 0.9659258262890683122, 1.000000000000000000, 0.9659258262890683122, 1.000000000000000000, 0.9659258262890683122, 1.000000000000000000, 0.9659258262890683122, 1.000000000000000000, 0.9659258262890693114, 0.9999999999999990008 ) ) 
 REPRESENTATION_ITEM ( '' )  );
#61523=ORIENTED_EDGE ( 'NONE', *, *, #11973, .F. ) ;
#61526=CARTESIAN_POINT ( 'NONE',  ( -2.679491924311235174, 225.4166666598387110, 10.00000000000000000 ) ) ;
#61539=CARTESIAN_POINT ( 'NONE',  ( -10.00000000000000178, 117.5000000000000142, -1.224646799147353454E-15 ) ) ;
#61541=CARTESIAN_POINT ( 'NONE',  ( -4.721056650415999201, 291.4843750017070079, -4.721056650415999201 ) ) ;
#61557=CARTESIAN_POINT ( 'NONE',  ( -9.832129032723418760, 7.864583329919350163, -5.676582343750004256 ) ) ;
#61559=CARTESIAN_POINT ( 'NONE',  ( -5.676582343750006032, 204.4270833299193555, 9.832129032723418760 ) ) ;
#61567=CARTESIAN_POINT ( 'NONE',  ( 5.676582343749993598, 4.947916663252683200, 9.832129032723422313 ) ) ;
#61575=CARTESIAN_POINT ( 'NONE',  ( -11.35316468750000141, 118.4895833299193697, 3.042071309553159963 ) ) ;
#61576=CARTESIAN_POINT ( 'NONE',  ( 8.660254037844389075, 87.29166665983869677, -5.000000000000000000 ) ) ;
#61581=CARTESIAN_POINT ( 'NONE',  ( -8.660254037844390851, 39.79166665983870388, 4.999999999999998224 ) ) ;
#61584=CARTESIAN_POINT ( 'NONE',  ( -2.765530957081998586, 288.7968750017069510, 6.676582343750001591 ) ) ;
#61590=CARTESIAN_POINT ( 'NONE',  ( 5.000000000000001776, 157.7083333265053966, -8.660254037844389075 ) ) ;
#61591=CARTESIAN_POINT ( 'NONE',  ( -9.832129032723420536, 149.0104166632526699, 5.676582343749997150 ) ) ;
#61592=( NAMED_UNIT ( * ) SI_UNIT ( $, .STERADIAN. ) SOLID_ANGLE_UNIT ( ) );
#61595=CARTESIAN_POINT ( 'NONE',  ( 11.35316468750000141, 76.09374999658602690, 0.000000000000000000 ) ) ;
#61601=CARTESIAN_POINT ( 'NONE',  ( -4.242640687119285658, 290.1875000034139589, 4.242640687119287435 ) ) ;
#61626=VERTEX_POINT ( 'NONE', #73454 ) ;
#61630=CARTESIAN_POINT ( 'NONE',  ( 7.320508075688771044, 64.37499999999998579, 7.320508075688775484 ) ) ;
#61633=CARTESIAN_POINT ( 'NONE',  ( 2.485281374238575314, 294.3125000000000000, 6.000000000000000888 ) ) ;
#61644=CARTESIAN_POINT ( 'NONE',  ( 10.00000000000000178, 190.2083333333333428, -2.679491924311226736 ) ) ;
#61647=CARTESIAN_POINT ( 'NONE',  ( 9.832129032723420536, 161.5104166632526983, -5.676582343749999815 ) ) ;
#61648=DIRECTION ( 'NONE',  ( -0.000000000000000000, 1.000000000000000000, -0.000000000000000000 ) ) ;
#61654=CARTESIAN_POINT ( 'NONE',  ( -9.832129032723420536, 29.01041666325268764, 5.676582343749997150 ) ) ;
#61656=CARTESIAN_POINT ( 'NONE',  ( 6.123233995736767268E-16, 98.12499999317203958, -10.00000000000000178 ) ) ;
#61661=CARTESIAN_POINT ( 'NONE',  ( 5.000000000000001776, 42.70833332650536818, -8.660254037844389075 ) ) ;
#61668=EDGE_LOOP ( 'NONE', ( #71994, #49834, #42893, #45690 ) ) ;
#61673=CARTESIAN_POINT ( 'NONE',  ( -3.042071309553173730, 139.3229166632526699, 11.35316468749999785 ) ) ;
#61680=CARTESIAN_POINT ( 'NONE',  ( 9.832129032723416984, 125.3645833299193413, 5.676582343750006032 ) ) ;
#61682=VERTEX_POINT ( 'NONE', #4065 ) ;
#61686=CARTESIAN_POINT ( 'NONE',  ( 8.311093377946837890, 111.7187499965859985, -8.311093377946837890 ) ) ;
#61690=CARTESIAN_POINT ( 'NONE',  ( -2.085542519210945728E-15, 24.84374999658601624, 11.35316468750000141 ) ) ;
#61697=CARTESIAN_POINT ( 'NONE',  ( -4.088227598258586603E-16, 288.2031250017069510, -6.676582343750001591 ) ) ;
#61702=CARTESIAN_POINT ( 'NONE',  ( -8.311093377946841443, 149.2187499965860411, 8.311093377946830785 ) ) ;
#61713=ORIENTED_EDGE ( 'NONE', *, *, #64967, .T. ) ;
#61717=CARTESIAN_POINT ( 'NONE',  ( 11.35316468750000141, 185.7812499965860411, 0.000000000000000000 ) ) ;
#61720=CARTESIAN_POINT ( 'NONE',  ( 1.226468279477575784E-15, 289.7031250017069510, 6.676582343750001591 ) ) ;
#61721=CARTESIAN_POINT ( 'NONE',  ( 8.660254037844381969, 34.58333333333332860, 5.000000000000003553 ) ) ;
#61723=VERTEX_POINT ( 'NONE', #67053 ) ;
#61732=CARTESIAN_POINT ( 'NONE',  ( 7.320508075688771044, 144.3750000000000284, 7.320508075688775484 ) ) ;
#61737=CARTESIAN_POINT ( 'NONE',  ( 8.311093377946834337, 110.4687499965860127, 8.311093377946839666 ) ) ;
#61738=CARTESIAN_POINT ( 'NONE',  ( -2.485281374238947016, 295.8125000000000000, -5.999999999999626965 ) ) ;
#61745=CARTESIAN_POINT ( 'NONE',  ( 7.358182744857522550, 224.4069354532862803, 6.797101760018821714 ) ) ;
#61746=CARTESIAN_POINT ( 'NONE',  ( 1.102182119232618108E-15, 287.3125000034140157, 6.000000000000001776 ) ) ;
#61749=CARTESIAN_POINT ( 'NONE',  ( -3.042071309553164404, 207.5520833299193555, -11.35316468749999963 ) ) ;
#61756=CARTESIAN_POINT ( 'NONE',  ( -9.832129032723418760, 92.86458332991935549, -5.676582343750004256 ) ) ;
#61762=CARTESIAN_POINT ( 'NONE',  ( -5.676582343750006032, 84.11458332991935549, 9.832129032723418760 ) ) ;
#61764=CARTESIAN_POINT ( 'NONE',  ( 5.000000000000001776, 207.7083333265053682, -8.660254037844389075 ) ) ;
#61770=CARTESIAN_POINT ( 'NONE',  ( -8.311093377946836114, 82.65624999658602690, -8.311093377946837890 ) ) ;
#61776=CARTESIAN_POINT ( 'NONE',  ( -10.00000000000000355, 184.5833333265053113, 2.679491924311223183 ) ) ;
#61777=CARTESIAN_POINT ( 'NONE',  ( 2.485281374238959895, 296.3750000034139589, 5.999999999999615419 ) ) ;
#61778=CARTESIAN_POINT ( 'NONE',  ( 9.832129032723416984, 80.67708332991935549, 5.676582343750006032 ) ) ;
#61779=CARTESIAN_POINT ( 'NONE',  ( 6.676582343750001591, 291.9531250017069510, -8.176455196517173205E-16 ) ) ;
#61781=CARTESIAN_POINT ( 'NONE',  ( 9.832129032723416984, 215.3645833299193555, 5.676582343750006032 ) ) ;
#61785=CARTESIAN_POINT ( 'NONE',  ( 6.000000000000001776, 291.5000000000000000, -7.347880794884121708E-16 ) ) ;
#61786=CARTESIAN_POINT ( 'NONE',  ( -5.676582343749998039, 207.4479166632527267, -9.832129032723420536 ) ) ;
#61789=ORIENTED_EDGE ( 'NONE', *, *, #10258, .T. ) ;
#61790=CARTESIAN_POINT ( 'NONE',  ( -11.35316468750000141, 188.5937499965860127, -1.390361679473963753E-15 ) ) ;
#61791=VECTOR ( 'NONE', #51837, 1000.000000000000000 ) ;
#61796=VECTOR ( 'NONE', #70686, 1000.000000000000000 ) ;
#61798=CARTESIAN_POINT ( 'NONE',  ( 5.000000000000001776, 15.83333333333333393, -8.660254037844389075 ) ) ;
#61800=ORIENTED_EDGE ( 'NONE', *, *, #32003, .F. ) ;
#61805=CARTESIAN_POINT ( 'NONE',  ( 5.000000000000001776, 17.70833332650536818, -8.660254037844389075 ) ) ;
#61814=ORIENTED_EDGE ( 'NONE', *, *, #33788, .T. ) ;
#61817=CARTESIAN_POINT ( 'NONE',  ( -2.085542519210945728E-15, 79.84374999658601268, 11.35316468750000141 ) ) ;
#61822=CARTESIAN_POINT ( 'NONE',  ( -4.088227598258586603E-16, 290.3593750017070079, -6.676582343750001591 ) ) ;
#61832=CARTESIAN_POINT ( 'NONE',  ( -8.311093377946836114, 167.9687499965859843, -8.311093377946837890 ) ) ;
#61840=CARTESIAN_POINT ( 'NONE',  ( 3.042071309553167069, 56.82291666325269119, -11.35316468749999785 ) ) ;
#61842=CARTESIAN_POINT ( 'NONE',  ( 4.999999999999993783, 26.04166665983870388, 8.660254037844390851 ) ) ;
#61847=CARTESIAN_POINT ( 'NONE',  ( -11.35316468750000141, 48.48958332991934839, 3.042071309553159963 ) ) ;
#61851=CARTESIAN_POINT ( 'NONE',  ( -10.00000000000000178, 12.50000000000000178, -1.224646799147353454E-15 ) ) ;
#61853=CARTESIAN_POINT ( 'NONE',  ( -8.311093377946841443, 48.90624999658600558, 8.311093377946834337 ) ) ;
#61856=CARTESIAN_POINT ( 'NONE',  ( 9.832129032723416984, 175.3645833299193555, 5.676582343750006032 ) ) ;
#61858=CARTESIAN_POINT ( 'NONE',  ( 7.320508075688774596, 147.4999999931720538, -7.320508075688774596 ) ) ;
#61861=CARTESIAN_POINT ( 'NONE',  ( 11.35316468749999785, 30.88541666325268409, 3.042071309553174174 ) ) ;
#61862=CARTESIAN_POINT ( 'NONE',  ( -2.679491924311226292, 78.33333332650536818, -10.00000000000000178 ) ) ;
#61863=ORIENTED_EDGE ( 'NONE', *, *, #29509, .T. ) ;
#61867=CARTESIAN_POINT ( 'NONE',  ( -2.679491924293753602, 6.458333333331768955, -10.00000000001010036 ) ) ;
#61868=CARTESIAN_POINT ( 'NONE',  ( 11.35316468750000141, 165.7812499965860411, 0.000000000000000000 ) ) ;
#61878=CARTESIAN_POINT ( 'NONE',  ( -9.832129032723418760, 118.1770833299193555, -5.676582343750004256 ) ) ;
#61892=AXIS2_PLACEMENT_3D ( 'NONE', #60539, #25452, #48467 ) ;
#61907=CARTESIAN_POINT ( 'NONE',  ( 7.320508075688771044, 124.3750000000000000, 7.320508075688775484 ) ) ;
#61909=CARTESIAN_POINT ( 'NONE',  ( 6.676582343750004256, 293.0468750017069510, 2.765530957081995478 ) ) ;
#61912=CARTESIAN_POINT ( 'NONE',  ( -7.320508075688778149, 174.9999999931720254, 7.320508075688769267 ) ) ;
#61923=CARTESIAN_POINT ( 'NONE',  ( -5.676582343750006032, 14.11458332991935016, 9.832129032723418760 ) ) ;
#61924=CARTESIAN_POINT ( 'NONE',  ( -8.311093377946836114, 207.9687499965859843, -8.311093377946837890 ) ) ;
#61932=CARTESIAN_POINT ( 'NONE',  ( -5.676582343750006032, 9.114583329919350163, 9.832129032723418760 ) ) ;
#61936=CARTESIAN_POINT ( 'NONE',  ( 0.000000000000000000, 300.0000000000000000, 0.000000000000000000 ) ) ;
#61938=CARTESIAN_POINT ( 'NONE',  ( -11.35316468749999785, 8.072916663252682312, -3.042071309553167957 ) ) ;
#61940=CARTESIAN_POINT ( 'NONE',  ( -9.832129032723418760, 127.8645833299193697, -5.676582343750004256 ) ) ;
#61941=CARTESIAN_POINT ( 'NONE',  ( -8.660254037844387298, 98.95833332650536818, -5.000000000000004441 ) ) ;
#61945=VERTEX_POINT ( 'NONE', #11202 ) ;
#61948=CARTESIAN_POINT ( 'NONE',  ( 2.765530957082001251, 288.9218750017069510, 6.676582343750000703 ) ) ;
#61958=CARTESIAN_POINT ( 'NONE',  ( -11.35316468750000141, 153.8020833299193271, 3.042071309553159963 ) ) ;
#61962=CARTESIAN_POINT ( 'NONE',  ( 11.35316468750000141, 81.09374999658601268, 0.000000000000000000 ) ) ;
#61966=ORIENTED_EDGE ( 'NONE', *, *, #22011, .F. ) ;
#61969=CARTESIAN_POINT ( 'NONE',  ( -1.836970198721029983E-15, 65.62499999317203958, 10.00000000000000178 ) ) ;
#61971=EDGE_CURVE ( 'NONE', #34804, #52532, #46267, .T. ) ;
#61990=VERTEX_POINT ( 'NONE', #13761 ) ;
#61997=CARTESIAN_POINT ( 'NONE',  ( -2.679491924311225848, 81.45833333333335702, -10.00000000000000178 ) ) ;
#61999=CARTESIAN_POINT ( 'NONE',  ( -4.242640687119286547, 293.8750000000000000, -4.242640687119286547 ) ) ;
#62001=EDGE_LOOP ( 'NONE', ( #11338, #57152, #44726, #70069 ) ) ;
#62005=CARTESIAN_POINT ( 'NONE',  ( 0.000000000000000000, 300.0000000000000000, 10.00000000000000178 ) ) ;
#62009=CARTESIAN_POINT ( 'NONE',  ( 8.660254037844389075, 200.4166666666666856, -5.000000000000000000 ) ) ;
#62012=CARTESIAN_POINT ( 'NONE',  ( -3.042071309553173730, 169.6354166632526699, 11.35316468749999785 ) ) ;
#62015=CARTESIAN_POINT ( 'NONE',  ( 8.660254037844545394, 155.4166666666667993, -5.000000000000092371 ) ) ;
#62019=CARTESIAN_POINT ( 'NONE',  ( -5.676582343749998039, 17.76041666325268409, -9.832129032723420536 ) ) ;
#62026=CARTESIAN_POINT ( 'NONE',  ( 6.123233995736767268E-16, 63.12499999317203248, -10.00000000000000178 ) ) ;
#62030=DIRECTION ( 'NONE',  ( -0.000000000000000000, 1.000000000000000000, -0.000000000000000000 ) ) ;
#62032=ORIENTED_EDGE ( 'NONE', *, *, #6089, .T. ) ;
#62034=ADVANCED_FACE ( 'NONE', ( #60175 ), #24726, .T. ) ;
#62037=CARTESIAN_POINT ( 'NONE',  ( -5.000000000000010658, 163.3333333333333428, 8.660254037844396180 ) ) ;
#62038=CARTESIAN_POINT ( 'NONE',  ( 11.35316468749999785, 145.5729166632527267, 3.042071309553174174 ) ) ;
#62046=CARTESIAN_POINT ( 'NONE',  ( 10.00000000000000178, 147.0833333265053966, -2.679491924311226736 ) ) ;
#62051=CARTESIAN_POINT ( 'NONE',  ( 11.35316468749999785, 120.8854166632526841, 3.042071309553174174 ) ) ;
#62055=CARTESIAN_POINT ( 'NONE',  ( 11.35316468749999963, 31.30208332991934839, -3.042071309553165293 ) ) ;
#62057=CYLINDRICAL_SURFACE ( 'NONE', #39305, 10.00000000000000178 ) ;
#62062=CARTESIAN_POINT ( 'NONE',  ( 6.676582343750004256, 288.8906250017070079, 2.765530957081995478 ) ) ;
#62066=( BOUNDED_CURVE ( )  B_SPLINE_CURVE ( 2, ( #28218, #68209, #45942, #68955, #17639, #11612, #73868, #41036, #63285, #17265, #5217, #58034, #51983 ),
 .UNSPECIFIED., .F., .F. ) 
 B_SPLINE_CURVE_WITH_KNOTS ( ( 3, 2, 2, 2, 2, 2, 3 ),
 ( 0.6467391304347827052, 0.6485507246376812640, 0.6503623188405798228, 0.6521739130434782705, 0.6539855072463768293, 0.6557971014492753881, 0.6576086956521739468 ),
 .UNSPECIFIED. ) 
 CURVE ( )  GEOMETRIC_REPRESENTATION_ITEM ( )  RATIONAL_B_SPLINE_CURVE ( ( 0.9999999999999978906, 0.9659258262890704216, 1.000000000000000000, 0.9659258262890683122, 1.000000000000000000, 0.9659258262890683122, 1.000000000000000000, 0.9659258262890683122, 1.000000000000000000, 0.9659258262890683122, 1.000000000000000000, 0.9659258262890683122, 1.000000000000000000 ) ) 
 REPRESENTATION_ITEM ( '' )  );
#62067=CARTESIAN_POINT ( 'NONE',  ( 8.311093377946834337, 155.4687499965859843, 8.311093377946839666 ) ) ;
#62072=CARTESIAN_POINT ( 'NONE',  ( 1.224646799147353454E-15, 300.0000000000000000, -10.00000000000000178 ) ) ;
#62083=DIRECTION ( 'NONE',  ( -0.000000000000000000, 1.000000000000000000, -0.000000000000000000 ) ) ;
#62085=CARTESIAN_POINT ( 'NONE',  ( 10.00000000000000000, 44.79166666666665719, 2.679491924311236062 ) ) ;
#62088=CARTESIAN_POINT ( 'NONE',  ( 4.721056650415999201, 290.0781250017069510, -4.721056650415999201 ) ) ;
#62089=FACE_OUTER_BOUND ( 'NONE', #31377, .T. ) ;
#62098=CARTESIAN_POINT ( 'NONE',  ( 7.320508075688774596, 145.6249999999999716, -7.320508075688774596 ) ) ;
#62102=CARTESIAN_POINT ( 'NONE',  ( 11.35316468749999785, 130.8854166632526699, 3.042071309553174174 ) ) ;
#62109=CARTESIAN_POINT ( 'NONE',  ( 3.738278573177460373, 224.0556613178885073, 9.279702309298665241 ) ) ;
#62113=CARTESIAN_POINT ( 'NONE',  ( -5.676582343750006032, 204.4270833299193555, 9.832129032723418760 ) ) ;
#62119=CARTESIAN_POINT ( 'NONE',  ( 8.311093377946837890, 91.40624999658604111, -8.311093377946837890 ) ) ;
#62122=CARTESIAN_POINT ( 'NONE',  ( -2.220555325575947149E-11, 176.2500000000017621, -10.00000000000000533 ) ) ;
#62124=CARTESIAN_POINT ( 'NONE',  ( -1.836970198721029983E-15, 38.75000000000000000, 10.00000000000000178 ) ) ;
#62126=CARTESIAN_POINT ( 'NONE',  ( -3.042071309553173730, 99.32291666325268409, 11.35316468749999785 ) ) ;
#62128=CARTESIAN_POINT ( 'NONE',  ( 4.999999999999993783, 206.0416666598387110, 8.660254037844390851 ) ) ;
#62134=CARTESIAN_POINT ( 'NONE',  ( -5.676582343749998039, 87.44791666325268409, -9.832129032723420536 ) ) ;
#62139=CARTESIAN_POINT ( 'NONE',  ( 7.320508075688774596, 177.4999999931720254, -7.320508075688774596 ) ) ;
#62142=CARTESIAN_POINT ( 'NONE',  ( 5.676582343750001591, 71.92708332991934128, -9.832129032723420536 ) ) ;
#62143=CARTESIAN_POINT ( 'NONE',  ( -4.721056650415998313, 291.5781250017069510, 4.721056650416000089 ) ) ;
#62146=CARTESIAN_POINT ( 'NONE',  ( -5.676582343749998039, 222.4479166632526983, -9.832129032723420536 ) ) ;
#62149=FACE_OUTER_BOUND ( 'NONE', #13064, .T. ) ;
#62151=CARTESIAN_POINT ( 'NONE',  ( 3.042071309553167513, 206.8229166632526699, -11.35316468749999785 ) ) ;
#62155=CARTESIAN_POINT ( 'NONE',  ( -2.085542519210945728E-15, 199.8437499965860127, 11.35316468750000141 ) ) ;
#62157=( BOUNDED_CURVE ( )  B_SPLINE_CURVE ( 2, ( #13982, #19657, #13254, #48700, #71707, #42671, #6876, #47960, #65682, #29886, #52899, #61526, #72848 ),
 .UNSPECIFIED., .F., .F. ) 
 B_SPLINE_CURVE_WITH_KNOTS ( ( 3, 2, 2, 2, 2, 2, 3 ),
 ( 0.9619565217391303769, 0.9637681159420288246, 0.9655797101449273834, 0.9673913043478259421, 0.9692028985507246119, 0.9710144927536231707, 0.9728260869565217295 ),
 .UNSPECIFIED. ) 
 CURVE ( )  GEOMETRIC_REPRESENTATION_ITEM ( )  RATIONAL_B_SPLINE_CURVE ( ( 1.000000000000001998, 0.9659258262890662028, 1.000000000000000000, 0.9659258262890683122, 1.000000000000000000, 0.9659258262890683122, 1.000000000000000000, 0.9659258262890683122, 1.000000000000000000, 0.9659258262890683122, 1.000000000000000000, 0.9659258262890683122, 1.000000000000000000 ) ) 
 REPRESENTATION_ITEM ( '' )  );
#62162=CARTESIAN_POINT ( 'NONE',  ( 10.00000000000000000, 19.79166666666666785, 2.679491924311236062 ) ) ;
#62183=CARTESIAN_POINT ( 'NONE',  ( -3.042071309553173730, 84.63541666325265567, 11.35316468749999785 ) ) ;
#62188=CARTESIAN_POINT ( 'NONE',  ( -2.765530957081996810, 288.4218750017069510, -6.676582343750002480 ) ) ;
#62192=CARTESIAN_POINT ( 'NONE',  ( 11.35316468749999963, 205.9895833299193271, -3.042071309553165293 ) ) ;
#62198=CARTESIAN_POINT ( 'NONE',  ( 11.35316468749999785, 160.8854166632526983, 3.042071309553174174 ) ) ;
#62205=CARTESIAN_POINT ( 'NONE',  ( -2.085542519210945728E-15, 49.53124999658601979, 11.35316468750000141 ) ) ;
#62208=CARTESIAN_POINT ( 'NONE',  ( 2.679491924311228956, 27.91666665983870033, -10.00000000000000000 ) ) ;
#62209=VERTEX_POINT ( 'NONE', #18715 ) ;
#62212=CARTESIAN_POINT ( 'NONE',  ( 5.676582343750001591, 66.61458332991935549, -9.832129032723420536 ) ) ;
#62218=CARTESIAN_POINT ( 'NONE',  ( -5.676582343749998039, 42.44791666325268409, -9.832129032723420536 ) ) ;
#62220=CARTESIAN_POINT ( 'NONE',  ( -3.190679070438223991E-13, 203.7500000000000000, 10.00000000000000533 ) ) ;
#62221=CARTESIAN_POINT ( 'NONE',  ( 11.35316468749999963, 170.9895833299193839, -3.042071309553165293 ) ) ;
#62222=CARTESIAN_POINT ( 'NONE',  ( 2.679491924311228956, 147.9166666598387110, -10.00000000000000000 ) ) ;
#62225=CARTESIAN_POINT ( 'NONE',  ( -5.676582343750006032, 39.42708332991935549, 9.832129032723418760 ) ) ;
#62227=CARTESIAN_POINT ( 'NONE',  ( -5.676582343749998039, 162.4479166632526983, -9.832129032723420536 ) ) ;
#62228=ORIENTED_EDGE ( 'NONE', *, *, #12710, .T. ) ;
#62233=CARTESIAN_POINT ( 'NONE',  ( -10.00000000000000711, 7.291666666666670515, -2.679491924311232065 ) ) ;
#62234=CARTESIAN_POINT ( 'NONE',  ( -11.35316468750000141, 163.4895833299193271, 3.042071309553159963 ) ) ;
#62242=CARTESIAN_POINT ( 'NONE',  ( -5.676582343749998039, 122.7604166632526841, -9.832129032723420536 ) ) ;
#62243=CARTESIAN_POINT ( 'NONE',  ( 10.00000000000000178, 12.08333332650536462, -2.679491924311226736 ) ) ;
#62246=ADVANCED_FACE ( 'NONE', ( #2098 ), #19438, .T. ) ;
#62261=( BOUNDED_CURVE ( )  B_SPLINE_CURVE ( 2, ( #58651, #59751, #70690, #8062, #58291, #19009, #30703, #31064, #64667, #36005, #59022, #41294, #52614 ),
 .UNSPECIFIED., .F., .F. ) 
 B_SPLINE_CURVE_WITH_KNOTS ( ( 3, 2, 2, 2, 2, 2, 3 ),
 ( 0.2663043478260869734, 0.2681159420289855322, 0.2699275362318840354, 0.2717391304347825942, 0.2735507246376811530, 0.2753623188405797118, 0.2771739130434782705 ),
 .UNSPECIFIED. ) 
 CURVE ( )  GEOMETRIC_REPRESENTATION_ITEM ( )  RATIONAL_B_SPLINE_CURVE ( ( 1.000000000000000000, 0.9659258262890683122, 1.000000000000000000, 0.9659258262890683122, 1.000000000000000000, 0.9659258262890683122, 1.000000000000000000, 0.9659258262890683122, 1.000000000000000000, 0.9659258262890683122, 1.000000000000000000, 0.9659258262890683122, 1.000000000000000000 ) ) 
 REPRESENTATION_ITEM ( '' )  );
#62263=CARTESIAN_POINT ( 'NONE',  ( 6.000000000000003553, 293.4374999999999432, 2.485281374238571317 ) ) ;
#62275=CARTESIAN_POINT ( 'NONE',  ( -7.320508075688783478, 128.1250000000000000, 7.320508075688775484 ) ) ;
#62276=CARTESIAN_POINT ( 'NONE',  ( -8.660254037844387298, 127.0833333333333570, -5.000000000000004441 ) ) ;
#62279=CARTESIAN_POINT ( 'NONE',  ( 4.721056650416000089, 287.9843750017070079, 4.721056650415999201 ) ) ;
#62292=CARTESIAN_POINT ( 'NONE',  ( 8.311093377946837890, 11.40624999658601624, -8.311093377946837890 ) ) ;
#62294=CARTESIAN_POINT ( 'NONE',  ( 11.35316468749999785, 205.8854166632526415, 3.042071309553174174 ) ) ;
#62301=CARTESIAN_POINT ( 'NONE',  ( -11.35316468749999785, 23.07291666325268054, -3.042071309553167513 ) ) ;
#62303=CARTESIAN_POINT ( 'NONE',  ( 6.000000000000003553, 292.4375000000000000, 2.485281374238571317 ) ) ;
#62306=CARTESIAN_POINT ( 'NONE',  ( -0.4499999999999996780, 283.9999999999998863, 5.815339556495201734 ) ) ;
#62308=CARTESIAN_POINT ( 'NONE',  ( -11.35316468750000141, 8.281249996586016238, -1.390361679473963753E-15 ) ) ;
#62310=CARTESIAN_POINT ( 'NONE',  ( 11.35316468750000141, 140.7812499965860411, 0.000000000000000000 ) ) ;
#62312=CARTESIAN_POINT ( 'NONE',  ( -7.320508075688778149, 99.99999999317203958, 7.320508075688769267 ) ) ;
#62314=CARTESIAN_POINT ( 'NONE',  ( 0.000000000000000000, 300.0000000000000000, 0.000000000000000000 ) ) ;
#62317=ORIENTED_EDGE ( 'NONE', *, *, #70768, .F. ) ;
#62319=CARTESIAN_POINT ( 'NONE',  ( 1.226468279477575784E-15, 287.8593750017070079, 6.676582343750001591 ) ) ;
#62323=CARTESIAN_POINT ( 'NONE',  ( -3.673940397442060854E-16, 296.8125000034140157, -6.000000000000001776 ) ) ;
#62329=CARTESIAN_POINT ( 'NONE',  ( 8.311093377946834337, 75.46874999658602690, 8.311093377946839666 ) ) ;
#62335=CARTESIAN_POINT ( 'NONE',  ( 9.999999999999998224, 114.7916666666666998, 2.679491924311235618 ) ) ;
#62342=EDGE_CURVE ( 'NONE', #2057, #18394, #34757, .T. ) ;
#62357=CARTESIAN_POINT ( 'NONE',  ( -10.00000000000000178, 82.50000000000000000, -1.224646799147353454E-15 ) ) ;
#62358=ADVANCED_FACE ( 'NONE', ( #20929 ), #22692, .T. ) ;
#62360=CARTESIAN_POINT ( 'NONE',  ( -2.485281374238572649, 291.1874999999999432, 6.000000000000002665 ) ) ;
#62363=ADVANCED_FACE ( 'NONE', ( #60926 ), #37926, .T. ) ;
#62370=CARTESIAN_POINT ( 'NONE',  ( -2.679491924305347439, 76.45833333333281701, -10.00000000000343903 ) ) ;
#62373=CARTESIAN_POINT ( 'NONE',  ( -1.836970198721029983E-15, 203.7500000000000284, 10.00000000000000178 ) ) ;
#62375=CARTESIAN_POINT ( 'NONE',  ( -3.042071309553164404, 162.5520833299193555, -11.35316468749999963 ) ) ;
#62381=CARTESIAN_POINT ( 'NONE',  ( 8.311093377946837890, 21.71874999658601268, -8.311093377946837890 ) ) ;
#62390=CARTESIAN_POINT ( 'NONE',  ( -2.679491924311235618, 65.41666665983871098, 10.00000000000000000 ) ) ;
#62393=CARTESIAN_POINT ( 'NONE',  ( 8.660254037844575592, 214.5833333333334849, 5.000000000000116351 ) ) ;
#62395=CARTESIAN_POINT ( 'NONE',  ( 10.00000000000000178, 165.0000000000000000, 0.000000000000000000 ) ) ;
#62402=CARTESIAN_POINT ( 'NONE',  ( -11.35316468749999785, 148.0729166632527267, -3.042071309553167513 ) ) ;
#62417=CARTESIAN_POINT ( 'NONE',  ( 8.311093377946837890, 131.7187499965860411, -8.311093377946837890 ) ) ;
#62421=CARTESIAN_POINT ( 'NONE',  ( 5.676582343750001591, 41.92708332991934839, -9.832129032723420536 ) ) ;
#62422=VERTEX_POINT ( 'NONE', #68722 ) ;
#62423=LINE ( 'NONE', #38690, #10388 ) ;
#62428=CARTESIAN_POINT ( 'NONE',  ( -2.485281374238571761, 296.8750000034139589, -6.000000000000003553 ) ) ;
#62431=CARTESIAN_POINT ( 'NONE',  ( 3.042071309553167069, 157.1354166632526983, -11.35316468749999785 ) ) ;
#62446=CARTESIAN_POINT ( 'NONE',  ( 5.000000000000001776, 40.83333333333333570, -8.660254037844389075 ) ) ;
#62458=FACE_OUTER_BOUND ( 'NONE', #27503, .T. ) ;
#62461=CARTESIAN_POINT ( 'NONE',  ( -2.679491924311225848, 166.4583333333333428, -10.00000000000000178 ) ) ;
#62465=CARTESIAN_POINT ( 'NONE',  ( -8.311093377946841443, 124.2187499965860127, 8.311093377946830785 ) ) ;
#62466=CARTESIAN_POINT ( 'NONE',  ( -6.000000000000001776, 294.0625000034140157, 0.000000000000000000 ) ) ;
#62470=CARTESIAN_POINT ( 'NONE',  ( -1.836970198721029983E-15, 115.6249999931720396, 10.00000000000000178 ) ) ;
#62471=ORIENTED_EDGE ( 'NONE', *, *, #58248, .F. ) ;
#62472=CARTESIAN_POINT ( 'NONE',  ( 9.207548596070616043, 225.3207043425250049, -3.912421826535780855 ) ) ;
#62473=CARTESIAN_POINT ( 'NONE',  ( -1.836970198721029983E-15, 135.6249999931720538, 10.00000000000000178 ) ) ;
#62477=CARTESIAN_POINT ( 'NONE',  ( -11.35316468749999785, 208.3854166632526415, -3.042071309553167513 ) ) ;
#62484=CARTESIAN_POINT ( 'NONE',  ( -9.832129032723420536, 93.69791666325269830, 5.676582343749997150 ) ) ;
#62491=CARTESIAN_POINT ( 'NONE',  ( -2.085542519210945728E-15, 99.53124999658602690, 11.35316468750000141 ) ) ;
#62493=CARTESIAN_POINT ( 'NONE',  ( 6.123233995736767268E-16, 63.12499999317203248, -10.00000000000000178 ) ) ;
#62495=CARTESIAN_POINT ( 'NONE',  ( -7.320508075688773708, 223.7499999931719969, -7.320508075688774596 ) ) ;
#62499=CARTESIAN_POINT ( 'NONE',  ( -2.085542519210945728E-15, 104.5312499965860269, 11.35316468750000141 ) ) ;
#62505=CARTESIAN_POINT ( 'NONE',  ( 2.679491924311222739, 175.8333333265053966, 10.00000000000000355 ) ) ;
#62508=ADVANCED_FACE ( 'NONE', ( #1198 ), #58176, .T. ) ;
#62509=CARTESIAN_POINT ( 'NONE',  ( -3.673940397442060854E-16, 296.8125000034140157, -6.000000000000001776 ) ) ;
#62510=CARTESIAN_POINT ( 'NONE',  ( 11.35316468749999963, 76.30208332991935549, -3.042071309553165293 ) ) ;
#62511=CARTESIAN_POINT ( 'NONE',  ( -6.676582343750003368, 289.3906250017069510, -2.765530957081996810 ) ) ;
#62515=CARTESIAN_POINT ( 'NONE',  ( -8.311093377946841443, 218.9062499965860127, 8.311093377946830785 ) ) ;
#62518=CARTESIAN_POINT ( 'NONE',  ( 9.832129032723420536, 211.1979166632526983, -5.676582343749999815 ) ) ;
#62522=CARTESIAN_POINT ( 'NONE',  ( 4.721056650416000089, 297.8281250017069510, 4.721056650415999201 ) ) ;
#62524=CARTESIAN_POINT ( 'NONE',  ( 9.832129032723416984, 200.6770833299193555, 5.676582343750006032 ) ) ;
#62527=ORIENTED_EDGE ( 'NONE', *, *, #8357, .F. ) ;
#62532=CARTESIAN_POINT ( 'NONE',  ( 10.00000000000000178, 20.20833333333333570, -2.679491924311226736 ) ) ;
#62539=CARTESIAN_POINT ( 'NONE',  ( 6.123233995736767268E-16, 18.12499999317203248, -10.00000000000000178 ) ) ;
#62544=PLANE ( 'NONE',  #71141 ) ;
#62552=CARTESIAN_POINT ( 'NONE',  ( 6.951808397369818766E-16, 92.34374999658602690, -11.35316468750000141 ) ) ;
#62553=DIRECTION ( 'NONE',  ( -0.000000000000000000, 1.000000000000000000, -0.000000000000000000 ) ) ;
#62557=CARTESIAN_POINT ( 'NONE',  ( -2.765530957081998142, 290.7968750017069510, 6.676582343750000703 ) ) ;
#62561=CARTESIAN_POINT ( 'NONE',  ( 11.35316468749999785, 200.5729166632526983, 3.042071309553174174 ) ) ;
#62567=CARTESIAN_POINT ( 'NONE',  ( -3.042071309553173730, 164.6354166632526983, 11.35316468749999785 ) ) ;
#62573=CARTESIAN_POINT ( 'NONE',  ( 8.311093377946834337, 55.15624999658601979, 8.311093377946839666 ) ) ;
#62579=CARTESIAN_POINT ( 'NONE',  ( 6.951808397369818766E-16, 57.03124999658601268, -11.35316468750000141 ) ) ;
#62583=CARTESIAN_POINT ( 'NONE',  ( -7.320508075688774596, 11.87500000000000000, -7.320508075688775484 ) ) ;
#62585=CARTESIAN_POINT ( 'NONE',  ( 5.676582343749993598, 39.94791666325268409, 9.832129032723422313 ) ) ;
#62588=CARTESIAN_POINT ( 'NONE',  ( 8.311093377946837890, 176.4062499965859843, -8.311093377946837890 ) ) ;
#62590=CARTESIAN_POINT ( 'NONE',  ( 8.660254037844385522, 141.4583333265053682, 5.000000000000005329 ) ) ;
#62593=CARTESIAN_POINT ( 'NONE',  ( 11.35316468749999963, 41.30208332991935549, -3.042071309553165293 ) ) ;
#62596=CARTESIAN_POINT ( 'NONE',  ( -11.35316468749999785, 183.0729166632526983, -3.042071309553167513 ) ) ;
#62603=CARTESIAN_POINT ( 'NONE',  ( 5.676582343749993598, 164.9479166632526983, 9.832129032723422313 ) ) ;
#62606=EDGE_CURVE ( 'NONE', #48612, #13169, #65577, .T. ) ;
#62613=CARTESIAN_POINT ( 'NONE',  ( 3.042071309553159519, 110.0520833299193271, 11.35316468750000141 ) ) ;
#62616=ORIENTED_EDGE ( 'NONE', *, *, #54211, .T. ) ;
#62629=ORIENTED_EDGE ( 'NONE', *, *, #12611, .F. ) ;
#62642=CARTESIAN_POINT ( 'NONE',  ( -6.000000000000003553, 290.0000000034140157, -2.485281374238571317 ) ) ;
#62644=CARTESIAN_POINT ( 'NONE',  ( -7.320508075688773708, 121.8750000000000000, -7.320508075688774596 ) ) ;
#62646=CARTESIAN_POINT ( 'NONE',  ( -2.765530957081998586, 289.7968750017070079, 6.676582343750001591 ) ) ;
#62659=CARTESIAN_POINT ( 'NONE',  ( -5.676582343750006032, 19.11458332991934839, 9.832129032723418760 ) ) ;
#62661=CARTESIAN_POINT ( 'NONE',  ( -5.676582343749998039, 212.7604166632526699, -9.832129032723420536 ) ) ;
#62662=DIRECTION ( 'NONE',  ( -0.000000000000000000, 1.000000000000000000, -0.000000000000000000 ) ) ;
#62665=CARTESIAN_POINT ( 'NONE',  ( -1.836970198721029983E-15, 30.62499999317203248, 10.00000000000000178 ) ) ;
#62668=CARTESIAN_POINT ( 'NONE',  ( 8.311093377946837890, 16.40624999658601268, -8.311093377946837890 ) ) ;
#62670=CARTESIAN_POINT ( 'NONE',  ( -3.166186134455097228E-13, 171.2500000000000284, -9.999999999999998224 ) ) ;
#62674=CARTESIAN_POINT ( 'NONE',  ( -3.042071309553173730, 4.322916663252682312, 11.35316468749999785 ) ) ;
#62676=CARTESIAN_POINT ( 'NONE',  ( -8.311093377946841443, 128.9062499965860411, 8.311093377946830785 ) ) ;
#62677=CARTESIAN_POINT ( 'NONE',  ( -2.679491924311225848, 108.3333333265053540, -10.00000000000000178 ) ) ;
#62679=CARTESIAN_POINT ( 'NONE',  ( -1.836970198721029983E-15, 5.624999993172032475, 10.00000000000000178 ) ) ;
#62684=CARTESIAN_POINT ( 'NONE',  ( -8.660254037844387298, 153.9583333265053682, -5.000000000000004441 ) ) ;
#62685=CARTESIAN_POINT ( 'NONE',  ( 6.676582343750001591, 291.1093750017069510, -8.176455196517173205E-16 ) ) ;
#62694=CARTESIAN_POINT ( 'NONE',  ( 7.320508075688774596, 217.4999999931720538, -7.320508075688774596 ) ) ;
#62697=CARTESIAN_POINT ( 'NONE',  ( 5.676582343750001591, 81.92708332991935549, -9.832129032723420536 ) ) ;
#62729=CARTESIAN_POINT ( 'NONE',  ( 2.679491924311228956, 76.04166666666665719, -10.00000000000000000 ) ) ;
#62731=CARTESIAN_POINT ( 'NONE',  ( 6.000000000000003553, 289.5625000000000568, -2.485281374238571761 ) ) ;
#62740=CARTESIAN_POINT ( 'NONE',  ( 10.00000000000000000, 204.7916666666666856, 2.679491924311236062 ) ) ;
#62742=CARTESIAN_POINT ( 'NONE',  ( -5.676582343749998039, 167.7604166632526983, -9.832129032723420536 ) ) ;
#62748=CARTESIAN_POINT ( 'NONE',  ( -3.042071309553173730, 34.63541666325269119, 11.35316468749999785 ) ) ;
#62751=CYLINDRICAL_SURFACE ( 'NONE', #34633, 10.00000000000000178 ) ;
#62757=CARTESIAN_POINT ( 'NONE',  ( 5.000000000000001776, 57.70833332650537528, -8.660254037844389075 ) ) ;
#62760=CARTESIAN_POINT ( 'NONE',  ( 5.000000000000020428, 64.16666666666669983, 8.660254037844437036 ) ) ;
#62762=CARTESIAN_POINT ( 'NONE',  ( 7.320508075688771044, 101.2499999931720254, 7.320508075688775484 ) ) ;
#62765=CARTESIAN_POINT ( 'NONE',  ( -2.679491924320392737, 198.5416666666659182, 9.999999999994837907 ) ) ;
#62768=CARTESIAN_POINT ( 'NONE',  ( -1.744157829248402118E-12, 86.25000000000015632, -10.00000000000000533 ) ) ;
#62769=CARTESIAN_POINT ( 'NONE',  ( 5.676582343750001591, 136.6145833299193555, -9.832129032723420536 ) ) ;
#62782=CARTESIAN_POINT ( 'NONE',  ( -2.085542519210945728E-15, 129.8437499965860127, 11.35316468750000141 ) ) ;
#62786=CARTESIAN_POINT ( 'NONE',  ( 9.832129032723416984, 30.67708332991935194, 5.676582343750006032 ) ) ;
#62796=CARTESIAN_POINT ( 'NONE',  ( -4.242640687119286547, 294.9375000034140157, -4.242640687119286547 ) ) ;
#62800=CARTESIAN_POINT ( 'NONE',  ( -8.311093377946841443, 159.2187499965860127, 8.311093377946830785 ) ) ;
#62806=VERTEX_POINT ( 'NONE', #30953 ) ;
#62812=CARTESIAN_POINT ( 'NONE',  ( -10.00000000000008171, 57.70833333333337833, 2.679491924311244500 ) ) ;
#62815=( BOUNDED_CURVE ( )  B_SPLINE_CURVE ( 2, ( #33648, #55912, #73618, #56654, #4969, #51345, #68699 ),
 .UNSPECIFIED., .F., .F. ) 
 B_SPLINE_CURVE_WITH_KNOTS ( ( 3, 2, 2, 3 ),
 ( 0.000000000000000000, 0.005232694955406646566, 0.01046538991081329313, 0.01569808486621994056 ),
 .UNSPECIFIED. ) 
 CURVE ( )  GEOMETRIC_REPRESENTATION_ITEM ( )  RATIONAL_B_SPLINE_CURVE ( ( 1.000000000000000000, 0.9659258262890684232, 1.000000000000000000, 0.9659258262890684232, 1.000000000000000000, 0.9659258262889811597, 1.000000000000087264 ) ) 
 REPRESENTATION_ITEM ( '' )  );
#62819=CARTESIAN_POINT ( 'NONE',  ( 7.320508075688774596, 40.62500000000000000, -7.320508075688774596 ) ) ;
#62823=FACE_OUTER_BOUND ( 'NONE', #53616, .T. ) ;
#62832=CARTESIAN_POINT ( 'NONE',  ( -2.679491924311226292, 138.3333333265053682, -10.00000000000000178 ) ) ;
#62833=CARTESIAN_POINT ( 'NONE',  ( -2.679491924311225848, 156.4583333333333712, -10.00000000000000178 ) ) ;
#62834=CARTESIAN_POINT ( 'NONE',  ( -3.673940397442060854E-16, 288.8125000034140157, -6.000000000000001776 ) ) ;
#62837=CARTESIAN_POINT ( 'NONE',  ( -8.311093377946841443, 134.2187499965860411, 8.311093377946830785 ) ) ;
#62840=VECTOR ( 'NONE', #28160, 1000.000000000000000 ) ;
#62843=CARTESIAN_POINT ( 'NONE',  ( 1.102182119232618108E-15, 298.2500000000000000, 6.000000000000001776 ) ) ;
#62846=CARTESIAN_POINT ( 'NONE',  ( 2.679491924318324614, 196.0416666666660888, -9.999999999996026290 ) ) ;
#62848=CARTESIAN_POINT ( 'NONE',  ( -9.832129032723420536, 219.0104166632526983, 5.676582343749997150 ) ) ;
#62855=CARTESIAN_POINT ( 'NONE',  ( -5.676582343750006032, 99.11458332991935549, 9.832129032723418760 ) ) ;
#62857=CARTESIAN_POINT ( 'NONE',  ( 0.000000000000000000, 300.0000000000000000, 0.000000000000000000 ) ) ;
#62862=CARTESIAN_POINT ( 'NONE',  ( 11.35316468749999963, 100.9895833299193555, -3.042071309553165293 ) ) ;
#62867=CARTESIAN_POINT ( 'NONE',  ( -10.00000000000000000, 214.1666666598386826, -2.679491924311229845 ) ) ;
#62871=CARTESIAN_POINT ( 'NONE',  ( 9.832129032723420536, 106.1979166632526983, -5.676582343749999815 ) ) ;
#62874=CARTESIAN_POINT ( 'NONE',  ( 8.660254037844461905, 174.5833333333333712, 5.000000000000049738 ) ) ;
#62876=CARTESIAN_POINT ( 'NONE',  ( 7.320508075688774596, 182.4999999931720254, -7.320508075688774596 ) ) ;
#62879=CARTESIAN_POINT ( 'NONE',  ( 6.951808397369818766E-16, 82.34374999658601268, -11.35316468750000141 ) ) ;
#62880=CARTESIAN_POINT ( 'NONE',  ( 6.676582343750004256, 289.8906250017069510, 2.765530957081995478 ) ) ;
#62883=CARTESIAN_POINT ( 'NONE',  ( 11.35316468749999785, 225.5729166632526983, 3.042071309553174174 ) ) ;
#62885=CARTESIAN_POINT ( 'NONE',  ( -10.00000000000000178, 69.37499999317203958, -1.224646799147353454E-15 ) ) ;
#62887=CARTESIAN_POINT ( 'NONE',  ( 6.000000000000003553, 291.4375000000000000, 2.485281374238571317 ) ) ;
#62888=CARTESIAN_POINT ( 'NONE',  ( 11.35316468749999963, 225.8887338474116007, -1.569472986416640570 ) ) ;
#62889=EDGE_CURVE ( 'NONE', #74042, #54835, #31705, .T. ) ;
#62891=CARTESIAN_POINT ( 'NONE',  ( 4.999999999999993783, 199.1666666666666856, 8.660254037844390851 ) ) ;
#62892=CARTESIAN_POINT ( 'NONE',  ( -2.765530957081998586, 298.6406250017069510, 6.676582343750001591 ) ) ;
#62895=CARTESIAN_POINT ( 'NONE',  ( -9.832129032723420536, 209.0104166632526699, 5.676582343749997150 ) ) ;
#62905=CARTESIAN_POINT ( 'NONE',  ( 7.320508075688771044, 9.375000000000001776, 7.320508075688775484 ) ) ;
#62932=CARTESIAN_POINT ( 'NONE',  ( 5.676582343750001591, 91.92708332991935549, -9.832129032723420536 ) ) ;
#62937=CARTESIAN_POINT ( 'NONE',  ( 10.00000000000000533, 70.00000000000001421, 0.000000000000000000 ) ) ;
#62940=CARTESIAN_POINT ( 'NONE',  ( 8.311093377946834337, 200.1562499965860695, 8.311093377946839666 ) ) ;
#62945=CARTESIAN_POINT ( 'NONE',  ( 9.832129032723420536, 166.5104166632526983, -5.676582343749999815 ) ) ;
#62952=CARTESIAN_POINT ( 'NONE',  ( 11.35316468749999963, 55.98958332991934128, -3.042071309553165293 ) ) ;
#62959=CARTESIAN_POINT ( 'NONE',  ( 8.311093377946834337, 60.15624999658601979, 8.311093377946839666 ) ) ;
#62963=CARTESIAN_POINT ( 'NONE',  ( -5.000000000000005329, 13.33333333333333570, 8.660254037844387298 ) ) ;
#62965=CARTESIAN_POINT ( 'NONE',  ( 3.042071309553167513, 56.82291666325268409, -11.35316468749999785 ) ) ;
#62969=CARTESIAN_POINT ( 'NONE',  ( 6.951808397369818766E-16, 172.0312499965860411, -11.35316468750000141 ) ) ;
#62970=CARTESIAN_POINT ( 'NONE',  ( 2.679491924311222739, 135.8333333265053966, 10.00000000000000355 ) ) ;
#62973=CARTESIAN_POINT ( 'NONE',  ( 5.000000000000006217, 20.83333333333333925, -8.660254037844392627 ) ) ;
#62974=CARTESIAN_POINT ( 'NONE',  ( 9.832129032723416984, 50.67708332991935549, 5.676582343750006032 ) ) ;
#62976=CARTESIAN_POINT ( 'NONE',  ( 2.485281374238950125, 295.3750000034140726, 5.999999999999625189 ) ) ;
#62977=CARTESIAN_POINT ( 'NONE',  ( -11.35316468749999785, 178.0729166632526415, -3.042071309553167513 ) ) ;
#62984=CARTESIAN_POINT ( 'NONE',  ( 5.676582343750001591, 181.6145833299193555, -9.832129032723420536 ) ) ;
#62993=CARTESIAN_POINT ( 'NONE',  ( 9.832129032723420536, 116.5104166632526841, -5.676582343749999815 ) ) ;
#63005=VERTEX_POINT ( 'NONE', #16191 ) ;
#63019=DIRECTION ( 'NONE',  ( 0.000000000000000000, 0.000000000000000000, 1.000000000000000000 ) ) ;
#63021=CARTESIAN_POINT ( 'NONE',  ( 7.320508075688774596, 120.6250000000000284, -7.320508075688774596 ) ) ;
#63024=CARTESIAN_POINT ( 'NONE',  ( 1.226468279477575784E-15, 289.8593750017070079, 6.676582343750001591 ) ) ;
#63036=( BOUNDED_CURVE ( )  B_SPLINE_CURVE ( 2, ( #41010, #69305, #40260, #35365, #11222, #34251, #57252, #29685, #17616, #669, #17992, #12689, #34622 ),
 .UNSPECIFIED., .F., .F. ) 
 B_SPLINE_CURVE_WITH_KNOTS ( ( 3, 2, 2, 2, 2, 2, 3 ),
 ( 0.1902173913043478104, 0.1920289855072463414, 0.1938405797101449279, 0.1956521739130434867, 0.1974637681159420177, 0.1992753623188406042, 0.2010869565217391630 ),
 .UNSPECIFIED. ) 
 CURVE ( )  GEOMETRIC_REPRESENTATION_ITEM ( )  RATIONAL_B_SPLINE_CURVE ( ( 1.000000000000000444, 0.9659258262890677571, 1.000000000000000000, 0.9659258262890683122, 1.000000000000000000, 0.9659258262890683122, 1.000000000000000000, 0.9659258262890683122, 1.000000000000000000, 0.9659258262890683122, 1.000000000000000000, 0.9659258262890677571, 1.000000000000000444 ) ) 
 REPRESENTATION_ITEM ( '' )  );
#63037=CARTESIAN_POINT ( 'NONE',  ( 11.35316468749999785, 15.57291666325268409, 3.042071309553174174 ) ) ;
#63039=CARTESIAN_POINT ( 'NONE',  ( 3.042071309553159519, 205.0520833299193271, 11.35316468750000141 ) ) ;
#63043=CARTESIAN_POINT ( 'NONE',  ( -10.00000000000016698, 42.70833333333342097, 2.679491924311266704 ) ) ;
#63046=CARTESIAN_POINT ( 'NONE',  ( -5.676582343750006032, 19.11458332991934839, 9.832129032723418760 ) ) ;
#63052=CARTESIAN_POINT ( 'NONE',  ( 3.042071309553159519, 14.73958332991935194, 11.35316468750000141 ) ) ;
#63055=CARTESIAN_POINT ( 'NONE',  ( 11.35316468750000141, 130.7812499965860127, 0.000000000000000000 ) ) ;
#63056=CARTESIAN_POINT ( 'NONE',  ( 2.679491924311222739, 100.8333333265053540, 10.00000000000000355 ) ) ;
#63058=DIRECTION ( 'NONE',  ( 0.000000000000000000, 0.000000000000000000, 1.000000000000000000 ) ) ;
#63062=CARTESIAN_POINT ( 'NONE',  ( -8.660254037844392627, 117.9166666666666856, 5.000000000000000888 ) ) ;
#63065=DIRECTION ( 'NONE',  ( -0.000000000000000000, 1.000000000000000000, -0.000000000000000000 ) ) ;
#63066=CARTESIAN_POINT ( 'NONE',  ( -4.721056650415998313, 287.7343750017069510, 4.721056650416000089 ) ) ;
#63067=CARTESIAN_POINT ( 'NONE',  ( 3.042071309553159519, 129.7395833299193555, 11.35316468750000141 ) ) ;
#63074=CARTESIAN_POINT ( 'NONE',  ( -1.836970198721029983E-15, 215.6249999931720538, 10.00000000000000178 ) ) ;
#63077=CARTESIAN_POINT ( 'NONE',  ( -5.676582343750006032, 79.42708332991935549, 9.832129032723418760 ) ) ;
#63082=AXIS2_PLACEMENT_3D ( 'NONE', #43732, #27494, #50507 ) ;
#63084=CARTESIAN_POINT ( 'NONE',  ( 4.999999999999993783, 114.1666666666666998, 8.660254037844390851 ) ) ;
#63092=ORIENTED_EDGE ( 'NONE', *, *, #55588, .F. ) ;
#63097=CARTESIAN_POINT ( 'NONE',  ( 0.000000000000000000, 0.000000000000000000, 0.000000000000000000 ) ) ;
#63108=CARTESIAN_POINT ( 'NONE',  ( -10.00000000000000178, 77.50000000000000000, -1.224646799147353454E-15 ) ) ;
#63110=CARTESIAN_POINT ( 'NONE',  ( -2.485281374238572649, 290.1875000000000000, 6.000000000000002665 ) ) ;
#63113=CARTESIAN_POINT ( 'NONE',  ( 6.000000000000001776, 294.5000000000000000, -7.347880794884121708E-16 ) ) ;
#63116=CARTESIAN_POINT ( 'NONE',  ( 1.224646799147353454E-15, 300.0000000000000000, -10.00000000000000178 ) ) ;
#63119=CARTESIAN_POINT ( 'NONE',  ( -6.000000000000003553, 292.9374999999999432, -2.485281374238571317 ) ) ;
#63121=CARTESIAN_POINT ( 'NONE',  ( 5.000000000000001776, 195.8333333333333712, -8.660254037844389075 ) ) ;
#63123=CARTESIAN_POINT ( 'NONE',  ( -3.042071309553173730, 174.6354166632526983, 11.35316468749999785 ) ) ;
#63124=CARTESIAN_POINT ( 'NONE',  ( -1.836970198721029983E-15, 38.75000000000000000, 10.00000000000000178 ) ) ;
#63128=EDGE_LOOP ( 'NONE', ( #27486, #11622 ) ) ;
#63131=CARTESIAN_POINT ( 'NONE',  ( -9.832129032723418760, 33.17708332991934839, -5.676582343750004256 ) ) ;
#63134=CARTESIAN_POINT ( 'NONE',  ( 0.000000000000000000, 300.0000000000000000, 0.000000000000000000 ) ) ;
#63139=EDGE_CURVE ( 'NONE', #34804, #36674, #19287, .T. ) ;
#63140=CARTESIAN_POINT ( 'NONE',  ( 7.320508075688771044, 66.24999999317203958, 7.320508075688775484 ) ) ;
#63143=CARTESIAN_POINT ( 'NONE',  ( 10.00000000000005329, 65.00000000000004263, 0.000000000000000000 ) ) ;
#63150=CARTESIAN_POINT ( 'NONE',  ( -2.765530957081998586, 295.7968750017070079, 6.676582343750001591 ) ) ;
#63153=CARTESIAN_POINT ( 'NONE',  ( -9.832129032723420536, 148.6979166632526983, 5.676582343749997150 ) ) ;
#63160=EDGE_LOOP ( 'NONE', ( #14449, #68014, #40818, #69900 ) ) ;
#63165=CARTESIAN_POINT ( 'NONE',  ( -11.35316468750000141, 133.8020833299193555, 3.042071309553159963 ) ) ;
#63169=CARTESIAN_POINT ( 'NONE',  ( -5.676582343749998039, 32.76041666325269119, -9.832129032723420536 ) ) ;
#63171=CARTESIAN_POINT ( 'NONE',  ( 6.123233995736767268E-16, 26.25000000000000355, -10.00000000000000178 ) ) ;
#63176=CARTESIAN_POINT ( 'NONE',  ( -6.000000000000001776, 296.0625000034140157, 0.000000000000000000 ) ) ;
#63178=CARTESIAN_POINT ( 'NONE',  ( -11.35316468749999785, 158.3854166632526699, -3.042071309553167513 ) ) ;
#63187=CARTESIAN_POINT ( 'NONE',  ( 0.000000000000000000, 300.0000000000000000, 10.00000000000000178 ) ) ;
#63189=ORIENTED_EDGE ( 'NONE', *, *, #55005, .T. ) ;
#63191=CARTESIAN_POINT ( 'NONE',  ( -2.485281374238979879, 297.8750000034140157, -5.999999999999594991 ) ) ;
#63193=CARTESIAN_POINT ( 'NONE',  ( 5.000000000000001776, 45.83333333333333570, -8.660254037844389075 ) ) ;
#63196=CARTESIAN_POINT ( 'NONE',  ( -2.485281374238571761, 298.8124999999999432, -6.000000000000003553 ) ) ;
#63204=CARTESIAN_POINT ( 'NONE',  ( -10.00000000000000000, 9.166666659838700326, -2.679491924311229845 ) ) ;
#63206=CARTESIAN_POINT ( 'NONE',  ( -6.338291171875001240, 287.8046875008534471, 0.000000000000000000 ) ) ;
#63207=CARTESIAN_POINT ( 'NONE',  ( 6.123233995736767268E-16, 166.2500000000000000, -10.00000000000000178 ) ) ;
#63211=CARTESIAN_POINT ( 'NONE',  ( -3.042071309553173730, 124.6354166632526699, 11.35316468749999785 ) ) ;
#63217=ORIENTED_EDGE ( 'NONE', *, *, #24668, .T. ) ;
#63223=CARTESIAN_POINT ( 'NONE',  ( -11.35316468750000141, 223.5937499965860127, -1.390361679473963753E-15 ) ) ;
#63230=CARTESIAN_POINT ( 'NONE',  ( 9.832129032723416984, 110.3645833299193555, 5.676582343750006032 ) ) ;
#63236=CARTESIAN_POINT ( 'NONE',  ( -2.085542519210945728E-15, 104.5312499965860269, 11.35316468750000141 ) ) ;
#63240=CARTESIAN_POINT ( 'NONE',  ( 8.660254037844385522, 216.4583333265053682, 5.000000000000005329 ) ) ;
#63244=CARTESIAN_POINT ( 'NONE',  ( -11.35316468750000141, 103.2812499965860269, -1.390361679473963753E-15 ) ) ;
#63250=CARTESIAN_POINT ( 'NONE',  ( 10.00000000000000000, 201.6666666598387110, 2.679491924311236062 ) ) ;
#63253=CARTESIAN_POINT ( 'NONE',  ( -11.35316468750000141, 88.80208332991934128, 3.042071309553159963 ) ) ;
#63254=CARTESIAN_POINT ( 'NONE',  ( 2.765530957081996366, 288.1406250017070647, -6.676582343750003368 ) ) ;
#63257=CARTESIAN_POINT ( 'NONE',  ( -3.042071309553173730, 224.3229166632527267, 11.35316468749999785 ) ) ;
#63259=DIRECTION ( 'NONE',  ( 0.000000000000000000, 0.000000000000000000, 1.000000000000000000 ) ) ;
#63260=CARTESIAN_POINT ( 'NONE',  ( 9.832129032723420536, 216.1979166632526983, -5.676582343749999815 ) ) ;
#63263=CARTESIAN_POINT ( 'NONE',  ( -6.676582343750003368, 295.3906250017068942, -2.765530957081996810 ) ) ;
#63267=CARTESIAN_POINT ( 'NONE',  ( 3.042071309553159519, 210.0520833299193555, 11.35316468750000141 ) ) ;
#63275=CARTESIAN_POINT ( 'NONE',  ( 2.679491924311222739, 33.95833333333333570, 10.00000000000000355 ) ) ;
#63285=CARTESIAN_POINT ( 'NONE',  ( 8.660254037844389075, 152.2916666598387110, -5.000000000000000000 ) ) ;
#63286=CARTESIAN_POINT ( 'NONE',  ( -6.676582343750002480, 295.3906250017069510, -2.765530957081996810 ) ) ;
#63296=CARTESIAN_POINT ( 'NONE',  ( 5.676582343749993598, 90.26041666325268409, 9.832129032723422313 ) ) ;
#63301=CARTESIAN_POINT ( 'NONE',  ( 9.498558403365325509E-13, 68.75000000000008527, 10.00000000000000178 ) ) ;
#63307=CARTESIAN_POINT ( 'NONE',  ( -11.35316468750000141, 198.2812499965860411, -1.390361679473963753E-15 ) ) ;
#63313=CARTESIAN_POINT ( 'NONE',  ( 8.311093377946837890, 176.7187499965860127, -8.311093377946837890 ) ) ;
#63316=CARTESIAN_POINT ( 'NONE',  ( -2.679491924335967834, 208.5416666666644687, 9.999999999985712762 ) ) ;
#63317=CARTESIAN_POINT ( 'NONE',  ( -9.999999999999996447, 112.7083333333333286, 2.679491924311221407 ) ) ;
#63321=CARTESIAN_POINT ( 'NONE',  ( -9.832129032723420536, 73.69791666325268409, 5.676582343749997150 ) ) ;
#63324=ORIENTED_EDGE ( 'NONE', *, *, #23121, .T. ) ;
#63327=CARTESIAN_POINT ( 'NONE',  ( 8.311093377946837890, 66.40624999658602690, -8.311093377946837890 ) ) ;
#63332=CARTESIAN_POINT ( 'NONE',  ( -9.832129032723418760, 57.86458332991935549, -5.676582343750004256 ) ) ;
#63336=CARTESIAN_POINT ( 'NONE',  ( 10.00000000000000178, 157.0833333265053113, -2.679491924311226736 ) ) ;
#63339=CARTESIAN_POINT ( 'NONE',  ( -8.311093377946836114, 47.96874999658601268, -8.311093377946837890 ) ) ;
#63341=CARTESIAN_POINT ( 'NONE',  ( 3.042071309553167069, 176.8229166632526415, -11.35316468749999785 ) ) ;
#63347=CARTESIAN_POINT ( 'NONE',  ( 11.35316468750000141, 185.7812499965860411, 0.000000000000000000 ) ) ;
#63353=CARTESIAN_POINT ( 'NONE',  ( -9.832129032723418760, 168.1770833299193555, -5.676582343750004256 ) ) ;
#63354=EDGE_CURVE ( 'NONE', #31698, #49230, #6331, .T. ) ;
#63356=CARTESIAN_POINT ( 'NONE',  ( 11.35316468749999785, 130.8854166632526699, 3.042071309553174174 ) ) ;
#63357=CARTESIAN_POINT ( 'NONE',  ( 2.679491924311238726, 12.91666665983870210, -9.999999999999996447 ) ) ;
#63377=VECTOR ( 'NONE', #25895, 1000.000000000000000 ) ;
#63383=LINE ( 'NONE', #69424, #17857 ) ;
#63386=PLANE ( 'NONE',  #73588 ) ;
#63387=CARTESIAN_POINT ( 'NONE',  ( 2.765530957082001251, 297.9218750017069510, 6.676582343749999815 ) ) ;
#63388=CARTESIAN_POINT ( 'NONE',  ( 8.660254037844389075, 130.4166666666666856, -5.000000000000000000 ) ) ;
#63390=CARTESIAN_POINT ( 'NONE',  ( 4.721056650415999201, 289.2343750017069510, -4.721056650415999201 ) ) ;
#63399=CARTESIAN_POINT ( 'NONE',  ( -2.249999999999999556, 255.9999999999998295, 5.427273995024871844 ) ) ;
#63405=CARTESIAN_POINT ( 'NONE',  ( 8.311093377946834337, 10.15624999658601801, 8.311093377946839666 ) ) ;
#63407=CARTESIAN_POINT ( 'NONE',  ( 9.832129032723420536, 226.5104166632526983, -5.676582343749999815 ) ) ;
#63410=CARTESIAN_POINT ( 'NONE',  ( -2.679491924311279138, 43.54166666666675667, 10.00000000000016342 ) ) ;
#63413=CARTESIAN_POINT ( 'NONE',  ( 9.832129032723420536, 21.19791666325268409, -5.676582343749999815 ) ) ;
#63416=CARTESIAN_POINT ( 'NONE',  ( -2.679491924293276206, 153.5416666666683057, 10.00000000001037925 ) ) ;
#63419=CARTESIAN_POINT ( 'NONE',  ( 9.832129032723420536, 26.19791666325268409, -5.676582343749999815 ) ) ;
#63421=CARTESIAN_POINT ( 'NONE',  ( -5.676582343750006032, 129.1145833299193839, 9.832129032723418760 ) ) ;
#63422=EDGE_CURVE ( 'NONE', #20466, #52730, #21715, .T. ) ;
#63423=CARTESIAN_POINT ( 'NONE',  ( -10.00000000000000355, 114.5833333265053682, 2.679491924311223183 ) ) ;
#63429=CARTESIAN_POINT ( 'NONE',  ( 5.676582343749993598, 10.26041666325268409, 9.832129032723422313 ) ) ;
#63430=EDGE_CURVE ( 'NONE', #48612, #1871, #58677, .T. ) ;
#63432=CARTESIAN_POINT ( 'NONE',  ( 2.765530957082001251, 296.7656250017069510, 6.676582343750000703 ) ) ;
#63433=CARTESIAN_POINT ( 'NONE',  ( 8.311093377946834337, 145.1562499965860127, 8.311093377946839666 ) ) ;
#63444=CARTESIAN_POINT ( 'NONE',  ( 11.35316468749999785, 85.88541666325268409, 3.042071309553174174 ) ) ;
#63445=ORIENTED_EDGE ( 'NONE', *, *, #2234, .F. ) ;
#63464=CARTESIAN_POINT ( 'NONE',  ( -9.832129032723418760, 52.86458332991934839, -5.676582343750004256 ) ) ;
#63476=CARTESIAN_POINT ( 'NONE',  ( -4.999999999999992006, 96.66666666666667140, -8.660254037844378416 ) ) ;
#63480=CARTESIAN_POINT ( 'NONE',  ( 10.00000000000000178, 75.00000000000001421, 0.000000000000000000 ) ) ;
#63482=CARTESIAN_POINT ( 'NONE',  ( -9.832129032723418760, 63.17708332991934839, -5.676582343750004256 ) ) ;
#63483=CARTESIAN_POINT ( 'NONE',  ( -2.485281374238571761, 288.8124999999999432, -6.000000000000003553 ) ) ;
#63485=VECTOR ( 'NONE', #72285, 1000.000000000000000 ) ;
#63486=DIRECTION ( 'NONE',  ( -0.000000000000000000, 1.000000000000000000, -0.000000000000000000 ) ) ;
#63492=CARTESIAN_POINT ( 'NONE',  ( -6.000000000000001776, 293.0000000000000000, 0.000000000000000000 ) ) ;
#63494=CARTESIAN_POINT ( 'NONE',  ( -2.679491924311235618, 203.5416666666666856, 10.00000000000000000 ) ) ;
#63497=CARTESIAN_POINT ( 'NONE',  ( 11.35316468749999963, 176.3020833299193839, -3.042071309553165293 ) ) ;
#63498=CARTESIAN_POINT ( 'NONE',  ( -9.999999999999998224, 37.29166666666665719, -2.679491924311230289 ) ) ;
#63501=CARTESIAN_POINT ( 'NONE',  ( 10.00000000000000178, 86.87499999317203958, 0.000000000000000000 ) ) ;
#63504=CARTESIAN_POINT ( 'NONE',  ( 3.042071309553159519, 35.05208332991935549, 11.35316468750000141 ) ) ;
#63508=CARTESIAN_POINT ( 'NONE',  ( 2.679491924311370177, 220.8333333265053682, 9.999999999999918288 ) ) ;
#63512=CARTESIAN_POINT ( 'NONE',  ( -1.836970198721029983E-15, 60.62499999317203958, 10.00000000000000178 ) ) ;
#63515=CARTESIAN_POINT ( 'NONE',  ( 10.00000000000005329, 65.20833333333337123, -2.679491924311240947 ) ) ;
#63517=CARTESIAN_POINT ( 'NONE',  ( 10.00000000000000178, 102.0833333265053682, -2.679491924311226736 ) ) ;
#63519=VERTEX_POINT ( 'NONE', #47336 ) ;
#63521=CARTESIAN_POINT ( 'NONE',  ( -2.765530957081996810, 298.4218750017069510, -6.676582343750003368 ) ) ;
#63523=VECTOR ( 'NONE', #45034, 1000.000000000000000 ) ;
#63524=CARTESIAN_POINT ( 'NONE',  ( -7.320508075688777261, 88.12500000000001421, 7.320508075688768379 ) ) ;
#63525=CARTESIAN_POINT ( 'NONE',  ( 9.832129032723416984, 155.3645833299193839, 5.676582343750006032 ) ) ;
#63534=CARTESIAN_POINT ( 'NONE',  ( -2.085542519210945728E-15, 124.8437499965860269, 11.35316468750000141 ) ) ;
#63538=CARTESIAN_POINT ( 'NONE',  ( -9.832129032723420536, 39.01041666325268409, 5.676582343749997150 ) ) ;
#63540=CARTESIAN_POINT ( 'NONE',  ( 8.660254037844385522, 36.45833332650536818, 5.000000000000005329 ) ) ;
#63545=CARTESIAN_POINT ( 'NONE',  ( -4.242640687119286547, 295.9375000034140157, -4.242640687119286547 ) ) ;
#63560=CARTESIAN_POINT ( 'NONE',  ( -7.320508075688834992, 58.12500000000003553, 7.320508075688828775 ) ) ;
#63568=CARTESIAN_POINT ( 'NONE',  ( -4.999999999999998224, 46.66666666666667140, -8.660254037844389075 ) ) ;
#63571=VECTOR ( 'NONE', #18148, 1000.000000000000000 ) ;
#63572=CARTESIAN_POINT ( 'NONE',  ( 6.123233995736767268E-16, 33.12499999317203248, -10.00000000000000178 ) ) ;
#63580=CARTESIAN_POINT ( 'NONE',  ( -8.660254037844387298, 157.0833333333333428, -5.000000000000004441 ) ) ;
#63581=CARTESIAN_POINT ( 'NONE',  ( -1.836970198721029983E-15, 225.6249999931720254, 10.00000000000000178 ) ) ;
#63584=CARTESIAN_POINT ( 'NONE',  ( -5.676582343749998039, 132.7604166632526983, -9.832129032723420536 ) ) ;
#63590=CARTESIAN_POINT ( 'NONE',  ( 3.042071309553167069, 2.135416663252682756, -11.35316468749999785 ) ) ;
#63596=CARTESIAN_POINT ( 'NONE',  ( 5.000000000000001776, 22.70833332650536818, -8.660254037844389075 ) ) ;
#63603=CARTESIAN_POINT ( 'NONE',  ( 5.676582343749993598, 114.9479166632526983, 9.832129032723422313 ) ) ;
#63607=FACE_OUTER_BOUND ( 'NONE', #72614, .T. ) ;
#63610=CARTESIAN_POINT ( 'NONE',  ( 5.676582343750001591, 111.6145833299193555, -9.832129032723420536 ) ) ;
#63614=CARTESIAN_POINT ( 'NONE',  ( -2.679491924311235618, 220.4166666598387110, 10.00000000000000000 ) ) ;
#63617=CARTESIAN_POINT ( 'NONE',  ( -6.338495502905945601E-13, 181.2500000000000853, -10.00000000000000533 ) ) ;
#63618=CARTESIAN_POINT ( 'NONE',  ( -11.35316468750000141, 103.4895833299193697, 3.042071309553159963 ) ) ;
#63622=CARTESIAN_POINT ( 'NONE',  ( -10.00000000000000000, 189.1666666598387394, -2.679491924311229845 ) ) ;
#63625=CARTESIAN_POINT ( 'NONE',  ( -11.35316468749999785, 83.38541666325265567, -3.042071309553167957 ) ) ;
#63629=CARTESIAN_POINT ( 'NONE',  ( -9.832129032723420536, 223.6979166632526983, 5.676582343749997150 ) ) ;
#63633=CARTESIAN_POINT ( 'NONE',  ( -3.042071309553173730, 224.3229166632527267, 11.35316468749999785 ) ) ;
#63636=CARTESIAN_POINT ( 'NONE',  ( 6.676582343750003368, 297.0156250017070079, -2.765530957081997254 ) ) ;
#63640=CARTESIAN_POINT ( 'NONE',  ( -9.832129032723418760, 213.1770833299193555, -5.676582343750004256 ) ) ;
#63652=CARTESIAN_POINT ( 'NONE',  ( 10.00000000000000178, 25.00000000000000000, 0.000000000000000000 ) ) ;
#63659=FACE_OUTER_BOUND ( 'NONE', #16187, .T. ) ;
#63663=CARTESIAN_POINT ( 'NONE',  ( 6.676582343750001591, 297.9531250017069510, -8.176455196517173205E-16 ) ) ;
#63665=CARTESIAN_POINT ( 'NONE',  ( -2.485281374238875962, 288.8750000034139020, -5.999999999999697131 ) ) ;
#63671=CARTESIAN_POINT ( 'NONE',  ( -11.35316468750000141, 88.80208332991935549, 3.042071309553159963 ) ) ;
#63678=CARTESIAN_POINT ( 'NONE',  ( -1.836970198721029983E-15, 75.62499999317203958, 10.00000000000000178 ) ) ;
#63681=CARTESIAN_POINT ( 'NONE',  ( 9.832129032723416984, 195.3645833299193839, 5.676582343750006032 ) ) ;
#63685=CARTESIAN_POINT ( 'NONE',  ( 5.676582343750001591, 176.9270833299193555, -9.832129032723420536 ) ) ;
#63687=CARTESIAN_POINT ( 'NONE',  ( -2.485281374238187180, 296.2500000034140157, 6.000000000000385469 ) ) ;
#63688=CARTESIAN_POINT ( 'NONE',  ( -8.660254037844385522, 107.9166666666666856, 4.999999999999996447 ) ) ;
#63692=CARTESIAN_POINT ( 'NONE',  ( 3.042071309553159519, 74.73958332991932707, 11.35316468750000141 ) ) ;
#63699=CARTESIAN_POINT ( 'NONE',  ( 3.042071309553167069, 56.82291666325268409, -11.35316468749999785 ) ) ;
#63700=VECTOR ( 'NONE', #18780, 1000.000000000000000 ) ;
#63705=CARTESIAN_POINT ( 'NONE',  ( -9.832129032723420536, 53.69791666325267698, 5.676582343749997150 ) ) ;
#63707=DIRECTION ( 'NONE',  ( 0.000000000000000000, 0.000000000000000000, 1.000000000000000000 ) ) ;
#63709=CARTESIAN_POINT ( 'NONE',  ( 7.320508075688774596, 157.4999999931720254, -7.320508075688774596 ) ) ;
#63712=CARTESIAN_POINT ( 'NONE',  ( -11.35316468750000141, 53.80208332991935549, 3.042071309553159963 ) ) ;
#63715=CARTESIAN_POINT ( 'NONE',  ( 9.832129032723416984, 180.3645833299193555, 5.676582343750006032 ) ) ;
#63718=( BOUNDED_CURVE ( )  B_SPLINE_CURVE ( 2, ( #44297, #33000, #27303, #15609, #32621, #10340, #60896, #37898, #62015, #44670, #5059, #55629, #3945 ),
 .UNSPECIFIED., .F., .F. ) 
 B_SPLINE_CURVE_WITH_KNOTS ( ( 3, 2, 2, 2, 2, 2, 3 ),
 ( 1.931089053012635004, 1.936321672528442228, 1.941554292044249452, 1.946786911560056677, 1.952019531075864123, 1.957252150591671347, 1.962484770107478571 ),
 .UNSPECIFIED. ) 
 CURVE ( )  GEOMETRIC_REPRESENTATION_ITEM ( )  RATIONAL_B_SPLINE_CURVE ( ( 0.9999999999997452038, 0.9659258262893231084, 1.000000000000000000, 0.9659258262890683122, 1.000000000000000000, 0.9659258262890683122, 1.000000000000000000, 0.9659258262890683122, 1.000000000000000000, 0.9659258262890683122, 1.000000000000000000, 0.9659258262894233615, 0.9999999999996449507 ) ) 
 REPRESENTATION_ITEM ( '' )  );
#63722=CARTESIAN_POINT ( 'NONE',  ( -3.042071309553173730, 184.3229166632526983, 11.35316468749999785 ) ) ;
#63728=CARTESIAN_POINT ( 'NONE',  ( 11.35316468750000141, 171.0937499965860127, 0.000000000000000000 ) ) ;
#63731=CARTESIAN_POINT ( 'NONE',  ( -2.085542519210945728E-15, 134.8437499965860127, 11.35316468750000141 ) ) ;
#63738=EDGE_CURVE ( 'NONE', #11319, #17570, #14915, .T. ) ;
#63745=ORIENTED_EDGE ( 'NONE', *, *, #36316, .F. ) ;
#63756=VERTEX_POINT ( 'NONE', #23193 ) ;
#63762=CARTESIAN_POINT ( 'NONE',  ( 6.676582343750001591, 298.1093750017069510, -8.176455196517173205E-16 ) ) ;
#63763=CARTESIAN_POINT ( 'NONE',  ( 8.660254037844389075, 140.4166666666666572, -5.000000000000000000 ) ) ;
#63765=CARTESIAN_POINT ( 'NONE',  ( 1.948298507267161028, 225.9999999999999716, 9.816171838510573622 ) ) ;
#63780=CARTESIAN_POINT ( 'NONE',  ( 5.676582343750001591, 26.61458332991935194, -9.832129032723420536 ) ) ;
#63782=CARTESIAN_POINT ( 'NONE',  ( -3.042071309553164404, 222.5520833299192986, -11.35316468749999963 ) ) ;
#63785=CARTESIAN_POINT ( 'NONE',  ( -10.00000000000016342, 42.29166666666676377, -2.679491924311274254 ) ) ;
#63786=ORIENTED_EDGE ( 'NONE', *, *, #23306, .T. ) ;
#63788=CARTESIAN_POINT ( 'NONE',  ( 3.042071309553159519, 24.73958332991934483, 11.35316468750000141 ) ) ;
#63791=LINE ( 'NONE', #29472, #27442 ) ;
#63793=CARTESIAN_POINT ( 'NONE',  ( -5.676582343750006032, 24.11458332991935194, 9.832129032723418760 ) ) ;
#63795=CARTESIAN_POINT ( 'NONE',  ( 11.35316468749999785, 140.5729166632526983, 3.042071309553174174 ) ) ;
#63797=CARTESIAN_POINT ( 'NONE',  ( 4.999999999999993783, 116.0416666598387110, 8.660254037844390851 ) ) ;
#63802=EDGE_LOOP ( 'NONE', ( #590, #59845, #58432, #13345, #49971, #18243, #5125, #2075, #49339, #56758, #39889, #251, #25767, #50474, #65591, #46942, #1197, #40122, #39070, #67104, #16409, #20524, #11403, #8396, #65973, #69581, #65012, #43149 ) ) ;
#63803=CARTESIAN_POINT ( 'NONE',  ( 3.042071309553159519, 10.05208332991935016, 11.35316468750000141 ) ) ;
#63807=CARTESIAN_POINT ( 'NONE',  ( 4.721056650415999201, 296.0781250017069510, -4.721056650415999201 ) ) ;
#63808=CARTESIAN_POINT ( 'NONE',  ( 5.676582343749993598, 139.9479166632526983, 9.832129032723422313 ) ) ;
#63814=VECTOR ( 'NONE', #28178, 1000.000000000000000 ) ;
#63820=CARTESIAN_POINT ( 'NONE',  ( 11.35316468749999785, 95.88541666325269830, 3.042071309553174174 ) ) ;
#63821=EDGE_LOOP ( 'NONE', ( #50273, #59356, #18071, #64994, #64249, #29533 ) ) ;
#63824=ORIENTED_EDGE ( 'NONE', *, *, #27472, .F. ) ;
#63825=ORIENTED_EDGE ( 'NONE', *, *, #50850, .F. ) ;
#63831=( BOUNDED_CURVE ( )  B_SPLINE_CURVE ( 2, ( #71670, #43758, #19990, #30949, #26011, #35243, #60358, #42998, #917 ),
 .UNSPECIFIED., .F., .F. ) 
 B_SPLINE_CURVE_WITH_KNOTS ( ( 3, 2, 2, 2, 3 ),
 ( 0.8958333333333318160, 0.9062499999999984457, 0.9166666666666650753, 0.9270833333333318160, 0.9374999999999984457 ),
 .UNSPECIFIED. ) 
 CURVE ( )  GEOMETRIC_REPRESENTATION_ITEM ( )  RATIONAL_B_SPLINE_CURVE ( ( 1.000000000000011324, 0.9238795325112754142, 1.000000000000000000, 0.9238795325112867385, 1.000000000000000000, 0.9238795325112867385, 1.000000000000000000, 0.9238795325112980628, 0.9999999999999886757 ) ) 
 REPRESENTATION_ITEM ( '' )  );
#63855=CARTESIAN_POINT ( 'NONE',  ( 10.00000000000000000, 94.79166666666668561, 2.679491924311236062 ) ) ;
#63857=CARTESIAN_POINT ( 'NONE',  ( 6.951808397369818766E-16, 67.34374999658601268, -11.35316468750000141 ) ) ;
#63858=CARTESIAN_POINT ( 'NONE',  ( -6.000000000000001776, 288.0000000000000000, 0.000000000000000000 ) ) ;
#63860=CARTESIAN_POINT ( 'NONE',  ( 2.485281374238929697, 294.3124999999999432, 5.999999999999645617 ) ) ;
#63864=CARTESIAN_POINT ( 'NONE',  ( -1.836970198721029983E-15, 105.6249999931720396, 10.00000000000000178 ) ) ;
#63869=CARTESIAN_POINT ( 'NONE',  ( -2.679491924311235618, 208.5416666666666856, 10.00000000000000000 ) ) ;
#63871=CARTESIAN_POINT ( 'NONE',  ( 8.311093377946837890, 186.7187499965860127, -8.311093377946837890 ) ) ;
#63872=CARTESIAN_POINT ( 'NONE',  ( -2.679491924309679529, 36.45833333333319359, -10.00000000000089351 ) ) ;
#63873=CARTESIAN_POINT ( 'NONE',  ( 7.320508075688774596, 177.4999999931720254, -7.320508075688774596 ) ) ;
#63874=DIRECTION ( 'NONE',  ( 0.000000000000000000, 0.000000000000000000, 1.000000000000000000 ) ) ;
#63878=CARTESIAN_POINT ( 'NONE',  ( 8.311093377946837890, 36.71874999658601979, -8.311093377946837890 ) ) ;
#63886=CARTESIAN_POINT ( 'NONE',  ( 8.660254037844389075, 77.29166665983871098, -5.000000000000000000 ) ) ;
#63891=DIRECTION ( 'NONE',  ( -0.000000000000000000, 1.000000000000000000, -0.000000000000000000 ) ) ;
#63895=CARTESIAN_POINT ( 'NONE',  ( -6.676582343750000703, 296.6718750017069510, 2.765530957082001251 ) ) ;
#63897=CARTESIAN_POINT ( 'NONE',  ( 11.35316468749999963, 155.9895833299193555, -3.042071309553165293 ) ) ;
#63898=B_SPLINE_CURVE_WITH_KNOTS ( 'NONE', 5,
 ( #15840, #50930, #18, #22620, #33980, #57725 ),
 .UNSPECIFIED., .F., .F.,
 ( 6, 6 ),
 ( 0.000000000000000000, 4.840251826652617773 ),
 .UNSPECIFIED. ) ;
#63910=CARTESIAN_POINT ( 'NONE',  ( 11.35316468749999963, 126.3020833299193555, -3.042071309553165293 ) ) ;
#63915=CARTESIAN_POINT ( 'NONE',  ( 9.832129032723420536, 51.51041666325269119, -5.676582343749999815 ) ) ;
#63924=CARTESIAN_POINT ( 'NONE',  ( -4.242640687119285658, 291.1875000034139589, 4.242640687119287435 ) ) ;
#63930=( BOUNDED_CURVE ( )  B_SPLINE_CURVE ( 2, ( #37536, #49593, #3577, #54893, #50332, #72609, #55644, #3204, #26192, #60909, #56015, #14873, #49212 ),
 .UNSPECIFIED., .F., .F. ) 
 B_SPLINE_CURVE_WITH_KNOTS ( ( 3, 2, 2, 2, 2, 2, 3 ),
 ( 2.747482230802302361, 2.752716221441485978, 2.757950211996366807, 2.763184202551248081, 2.768418193106129355, 2.773652183661010628, 2.778886174319656455 ),
 .UNSPECIFIED. ) 
 CURVE ( )  GEOMETRIC_REPRESENTATION_ITEM ( )  RATIONAL_B_SPLINE_CURVE ( ( 1.000000000000000000, 0.9659258262890683122, 1.000000000000000000, 0.9659258262890683122, 1.000000000000000000, 0.9659258262890683122, 1.000000000000000000, 0.9659258262890683122, 1.000000000000000000, 0.9659258262890683122, 1.000000000000000000, 0.9659258262890683122, 1.000000000000000000 ) ) 
 REPRESENTATION_ITEM ( '' )  );
#63935=EDGE_LOOP ( 'NONE', ( #43224, #3385, #68480, #45551 ) ) ;
#63942=DIRECTION ( 'NONE',  ( -0.000000000000000000, 1.000000000000000000, -0.000000000000000000 ) ) ;
#63948=CARTESIAN_POINT ( 'NONE',  ( -10.00000000000000355, 44.58333332650536818, 2.679491924311223183 ) ) ;
#63949=CARTESIAN_POINT ( 'NONE',  ( -5.000000000000005329, 48.33333333333334281, 8.660254037844387298 ) ) ;
#63952=CARTESIAN_POINT ( 'NONE',  ( -3.673940397442060854E-16, 298.7500000000000000, -6.000000000000001776 ) ) ;
#63961=CARTESIAN_POINT ( 'NONE',  ( -2.679491924304306938, 146.4583333333327175, -10.00000000000399680 ) ) ;
#63962=CARTESIAN_POINT ( 'NONE',  ( 7.320508075688771044, 201.2499999931720538, 7.320508075688775484 ) ) ;
#63963=CARTESIAN_POINT ( 'NONE',  ( 7.320508075688771044, 159.3749999999999716, 7.320508075688775484 ) ) ;
#63966=CARTESIAN_POINT ( 'NONE',  ( -2.085542519210945728E-15, 134.8437499965860127, 11.35316468750000141 ) ) ;
#63970=CARTESIAN_POINT ( 'NONE',  ( 8.660254037844385522, 106.4583333265053682, 5.000000000000005329 ) ) ;
#63972=ORIENTED_EDGE ( 'NONE', *, *, #64987, .T. ) ;
#63978=CARTESIAN_POINT ( 'NONE',  ( -10.00000000000000000, 39.16666665983870388, -2.679491924311229845 ) ) ;
#63984=CARTESIAN_POINT ( 'NONE',  ( -5.676582343749998039, 107.4479166632526983, -9.832129032723420536 ) ) ;
#63986=CARTESIAN_POINT ( 'NONE',  ( -2.249999999999999112, 284.0000000000000000, 7.677076266392047543 ) ) ;
#63991=CARTESIAN_POINT ( 'NONE',  ( 5.676582343750001591, 121.6145833299193555, -9.832129032723420536 ) ) ;
#63995=CARTESIAN_POINT ( 'NONE',  ( -2.679491924311235618, 215.4166666598387110, 10.00000000000000000 ) ) ;
#63999=CARTESIAN_POINT ( 'NONE',  ( 11.35316468749999963, 95.98958332991935549, -3.042071309553165293 ) ) ;
#64003=CARTESIAN_POINT ( 'NONE',  ( 7.320508075688771044, 169.3750000000000000, 7.320508075688775484 ) ) ;
#64005=CARTESIAN_POINT ( 'NONE',  ( -10.00000000000000355, 189.5833333265053682, 2.679491924311223183 ) ) ;
#64008=CARTESIAN_POINT ( 'NONE',  ( -11.35316468749999785, 88.38541666325268409, -3.042071309553167957 ) ) ;
#64013=CARTESIAN_POINT ( 'NONE',  ( 11.35316468749999785, 5.885416663252683200, 3.042071309553174174 ) ) ;
#64017=CARTESIAN_POINT ( 'NONE',  ( -2.085542519210945728E-15, 214.5312499965860411, 11.35316468750000141 ) ) ;
#64021=CARTESIAN_POINT ( 'NONE',  ( 5.000000000000001776, 200.8333333333333428, -8.660254037844389075 ) ) ;
#64022=CARTESIAN_POINT ( 'NONE',  ( 1.226468279477575784E-15, 298.7031250017070079, 6.676582343750001591 ) ) ;
#64025=CARTESIAN_POINT ( 'NONE',  ( -9.832129032723420536, 204.0104166632526983, 5.676582343749997150 ) ) ;
#64030=AXIS2_PLACEMENT_3D ( 'NONE', #2749, #8782, #71765 ) ;
#64033=CARTESIAN_POINT ( 'NONE',  ( -2.679491924311235618, 23.54166666666667140, 10.00000000000000000 ) ) ;
#64044=CARTESIAN_POINT ( 'NONE',  ( -6.676582343750001591, 296.4531250017069510, 0.000000000000000000 ) ) ;
#64047=( BOUNDED_CURVE ( )  B_SPLINE_CURVE ( 2, ( #13731, #71451, #18687, #42787, #41327, #65803, #54507, #30740, #14109 ),
 .UNSPECIFIED., .F., .F. ) 
 B_SPLINE_CURVE_WITH_KNOTS ( ( 3, 2, 2, 2, 3 ),
 ( 0.3541666666666646313, 0.3645833333333312609, 0.3749999999999980016, 0.3854166666666646868, 0.3958333333333313164 ),
 .UNSPECIFIED. ) 
 CURVE ( )  GEOMETRIC_REPRESENTATION_ITEM ( )  RATIONAL_B_SPLINE_CURVE ( ( 1.000000000000015099, 0.9238795325112717505, 1.000000000000000000, 0.9238795325112867385, 1.000000000000000000, 0.9238795325112867385, 1.000000000000000000, 0.9238795325113013934, 0.9999999999999853451 ) ) 
 REPRESENTATION_ITEM ( '' )  );
#64051=VERTEX_POINT ( 'NONE', #42383 ) ;
#64053=CARTESIAN_POINT ( 'NONE',  ( 3.042071309553159519, 95.05208332991935549, 11.35316468750000141 ) ) ;
#64058=CARTESIAN_POINT ( 'NONE',  ( 1.226468279477575784E-15, 287.8593750017070079, 6.676582343750001591 ) ) ;
#64059=VERTEX_POINT ( 'NONE', #24660 ) ;
#64063=CARTESIAN_POINT ( 'NONE',  ( -8.311093377946836114, 207.6562499965860411, -8.311093377946837890 ) ) ;
#64069=CARTESIAN_POINT ( 'NONE',  ( 8.311093377946837890, 181.7187499965859843, -8.311093377946837890 ) ) ;
#64072=CARTESIAN_POINT ( 'NONE',  ( 2.395154805519954641E-11, 111.2499999999981242, -9.999999999999998224 ) ) ;
#64076=CARTESIAN_POINT ( 'NONE',  ( 5.676582343749993598, 64.94791666325269830, 9.832129032723422313 ) ) ;
#64082=CARTESIAN_POINT ( 'NONE',  ( 3.042071309553159519, 74.73958332991932707, 11.35316468750000141 ) ) ;
#64087=CARTESIAN_POINT ( 'NONE',  ( -5.676582343749998039, 62.44791666325268409, -9.832129032723420536 ) ) ;
#64091=CARTESIAN_POINT ( 'NONE',  ( 8.660254037844389075, 162.2916666598387110, -5.000000000000000000 ) ) ;
#64094=CARTESIAN_POINT ( 'NONE',  ( -2.085542519210945728E-15, 54.84374999658601979, 11.35316468750000141 ) ) ;
#64096=CARTESIAN_POINT ( 'NONE',  ( 8.311093377946837890, 186.4062499965860411, -8.311093377946837890 ) ) ;
#64101=CARTESIAN_POINT ( 'NONE',  ( 8.311093377946834337, 175.1562499965859843, 8.311093377946839666 ) ) ;
#64106=CARTESIAN_POINT ( 'NONE',  ( -3.042071309553173730, 169.6354166632526699, 11.35316468749999785 ) ) ;
#64109=CARTESIAN_POINT ( 'NONE',  ( 3.042071309553159519, 125.0520833299193555, 11.35316468750000141 ) ) ;
#64112=VECTOR ( 'NONE', #56957, 1000.000000000000000 ) ;
#64138=CARTESIAN_POINT ( 'NONE',  ( -4.721056650415998313, 297.7343750017069510, 4.721056650416000089 ) ) ;
#64139=CARTESIAN_POINT ( 'NONE',  ( -2.679491924311235618, 133.5416666666666572, 10.00000000000000000 ) ) ;
#64156=CARTESIAN_POINT ( 'NONE',  ( -8.311093377946841443, 23.90624999658601979, 8.311093377946830785 ) ) ;
#64160=CARTESIAN_POINT ( 'NONE',  ( 8.311093377946834337, 215.4687499965860411, 8.311093377946839666 ) ) ;
#64169=CARTESIAN_POINT ( 'NONE',  ( -2.085542519210945728E-15, 34.53124999658601268, 11.35316468750000141 ) ) ;
#64175=CARTESIAN_POINT ( 'NONE',  ( 11.35316468749999963, 25.98958332991935194, -3.042071309553165293 ) ) ;
#64178=CARTESIAN_POINT ( 'NONE',  ( -3.042071309553164404, 147.2395833299193555, -11.35316468749999963 ) ) ;
#64179=CARTESIAN_POINT ( 'NONE',  ( -10.00000000000000355, 119.5833333265053824, 2.679491924311223183 ) ) ;
#64184=CARTESIAN_POINT ( 'NONE',  ( -3.042071309553163960, 7.552083329919350163, -11.35316468749999963 ) ) ;
#64187=CARTESIAN_POINT ( 'NONE',  ( 4.721056650415999201, 299.0781250017069510, -4.721056650415999201 ) ) ;
#64189=CARTESIAN_POINT ( 'NONE',  ( -3.042071309553173730, 144.3229166632526983, 11.35316468749999785 ) ) ;
#64194=EDGE_CURVE ( 'NONE', #71882, #63519, #62261, .T. ) ;
#64196=ORIENTED_EDGE ( 'NONE', *, *, #51917, .F. ) ;
#64197=CARTESIAN_POINT ( 'NONE',  ( 4.999999999999995559, 119.1666666666666714, 8.660254037844394404 ) ) ;
#64200=CARTESIAN_POINT ( 'NONE',  ( 3.042071309553159519, 90.05208332991932707, 11.35316468750000141 ) ) ;
#64228=CARTESIAN_POINT ( 'NONE',  ( 10.00000000000000178, 90.20833333333332860, -2.679491924311226736 ) ) ;
#64231=CARTESIAN_POINT ( 'NONE',  ( -11.35316468750000141, 58.80208332991933418, 3.042071309553159963 ) ) ;
#64232=CARTESIAN_POINT ( 'NONE',  ( -6.676582343750001591, 299.6093750017069510, 0.000000000000000000 ) ) ;
#64234=CARTESIAN_POINT ( 'NONE',  ( -8.660254037844387298, 143.9583333265053682, -5.000000000000004441 ) ) ;
#64237=CARTESIAN_POINT ( 'NONE',  ( 6.123233995736767268E-16, 38.12499999317203958, -10.00000000000000178 ) ) ;
#64242=CARTESIAN_POINT ( 'NONE',  ( 5.000000000000001776, 210.8333333333333428, -8.660254037844389075 ) ) ;
#64244=CARTESIAN_POINT ( 'NONE',  ( 9.832129032723420536, 181.5104166632526699, -5.676582343749999815 ) ) ;
#64246=CARTESIAN_POINT ( 'NONE',  ( 5.000000000000001776, 177.7083333265053682, -8.660254037844389075 ) ) ;
#64247=DIRECTION ( 'NONE',  ( -0.000000000000000000, 1.000000000000000000, -0.000000000000000000 ) ) ;
#64249=ORIENTED_EDGE ( 'NONE', *, *, #69377, .T. ) ;
#64253=CARTESIAN_POINT ( 'NONE',  ( 5.676582343749993598, 30.26041666325268409, 9.832129032723422313 ) ) ;
#64260=( BOUNDED_CURVE ( )  B_SPLINE_CURVE ( 2, ( #45565, #50852, #73490, #33904, #68578, #39167, #38803, #16887, #56903, #15392, #61805, #44455, #62539 ),
 .UNSPECIFIED., .F., .F. ) 
 B_SPLINE_CURVE_WITH_KNOTS ( ( 3, 2, 2, 2, 2, 2, 3 ),
 ( 0.05978260869565217572, 0.06159420289855072755, 0.06340579710144927938, 0.06521739130434782428, 0.06702898550724638305, 0.06884057971014492794, 0.07065217391304347283 ),
 .UNSPECIFIED. ) 
 CURVE ( )  GEOMETRIC_REPRESENTATION_ITEM ( )  RATIONAL_B_SPLINE_CURVE ( ( 1.000000000000000000, 0.9659258262890683122, 1.000000000000000000, 0.9659258262890683122, 1.000000000000000000, 0.9659258262890683122, 1.000000000000000000, 0.9659258262890683122, 1.000000000000000000, 0.9659258262890683122, 1.000000000000000000, 0.9659258262890683122, 1.000000000000000000 ) ) 
 REPRESENTATION_ITEM ( '' )  );
#64261=CARTESIAN_POINT ( 'NONE',  ( 8.660254037844385522, 81.45833332650536818, 5.000000000000005329 ) ) ;
#64265=CARTESIAN_POINT ( 'NONE',  ( -8.660254037844390851, 49.79166665983870388, 4.999999999999998224 ) ) ;
#64269=CARTESIAN_POINT ( 'NONE',  ( 4.721056650416000089, 298.9843750017070079, 4.721056650415999201 ) ) ;
#64271=CARTESIAN_POINT ( 'NONE',  ( 10.00000000000000178, 41.87499999317203248, 0.000000000000000000 ) ) ;
#64272=CARTESIAN_POINT ( 'NONE',  ( 9.832129032723420536, 156.1979166632526983, -5.676582343749999815 ) ) ;
#64275=DIRECTION ( 'NONE',  ( -0.000000000000000000, 1.000000000000000000, -0.000000000000000000 ) ) ;
#64281=( BOUNDED_CURVE ( )  B_SPLINE_CURVE ( 2, ( #53777, #2086, #71104, #36793, #59803, #31121, #48466, #49968, #21289 ),
 .UNSPECIFIED., .F., .F. ) 
 B_SPLINE_CURVE_WITH_KNOTS ( ( 3, 2, 2, 2, 3 ),
 ( 0.6041666666666648533, 0.6145833333333315940, 0.6249999999999982236, 0.6354166666666647423, 0.6458333333333314830 ),
 .UNSPECIFIED. ) 
 CURVE ( )  GEOMETRIC_REPRESENTATION_ITEM ( )  RATIONAL_B_SPLINE_CURVE ( ( 1.000000000000012879, 0.9238795325112737489, 1.000000000000000000, 0.9238795325112867385, 1.000000000000000000, 0.9238795325112867385, 1.000000000000000000, 0.9238795325113005052, 0.9999999999999862332 ) ) 
 REPRESENTATION_ITEM ( '' )  );
#64284=CARTESIAN_POINT ( 'NONE',  ( 6.951808397369818766E-16, 137.3437499965860127, -11.35316468750000141 ) ) ;
#64288=CARTESIAN_POINT ( 'NONE',  ( 3.042071309553159519, 55.05208332991934128, 11.35316468750000141 ) ) ;
#64290=CARTESIAN_POINT ( 'NONE',  ( -5.000000000000001776, 26.66666666666667496, -8.660254037844392627 ) ) ;
#64295=CARTESIAN_POINT ( 'NONE',  ( 1.102182119232618108E-15, 294.3125000034140157, 6.000000000000001776 ) ) ;
#64317=CARTESIAN_POINT ( 'NONE',  ( -8.660254037844387298, 43.95833332650536818, -5.000000000000004441 ) ) ;
#64318=CARTESIAN_POINT ( 'NONE',  ( 7.320508075688774596, 60.62500000000001421, -7.320508075688774596 ) ) ;
#64320=CARTESIAN_POINT ( 'NONE',  ( 4.242640687119287435, 299.3750000000000000, 4.242640687119285658 ) ) ;
#64321=CARTESIAN_POINT ( 'NONE',  ( -4.242640687119285658, 288.1875000034139589, 4.242640687119287435 ) ) ;
#64324=VERTEX_POINT ( 'NONE', #26513 ) ;
#64327=CARTESIAN_POINT ( 'NONE',  ( 9.999999999999982236, 89.79166666666667140, 2.679491924311231621 ) ) ;
#64331=ADVANCED_FACE ( 'NONE', ( #71791 ), #3151, .T. ) ;
#64332=CARTESIAN_POINT ( 'NONE',  ( 10.00000000000000000, 174.7916666666666288, 2.679491924311236062 ) ) ;
#64333=DIRECTION ( 'NONE',  ( 1.000000000000000000, 0.000000000000000000, 0.000000000000000000 ) ) ;
#64336=CARTESIAN_POINT ( 'NONE',  ( 3.042071309553159519, 135.0520833299193555, 11.35316468750000141 ) ) ;
#64348=CARTESIAN_POINT ( 'NONE',  ( 8.660254037844389075, 32.29166665983870388, -5.000000000000000000 ) ) ;
#64359=CARTESIAN_POINT ( 'NONE',  ( -7.950093002584606161, 225.9999999999999716, -6.101298592595878922 ) ) ;
#64360=CARTESIAN_POINT ( 'NONE',  ( -8.660254037844431707, 62.08333333333336412, -5.000000000000030198 ) ) ;
#64362=CARTESIAN_POINT ( 'NONE',  ( 8.311093377946837890, 116.4062499965860269, -8.311093377946837890 ) ) ;
#64370=CARTESIAN_POINT ( 'NONE',  ( -11.35316468750000141, 108.4895833299193413, 3.042071309553159963 ) ) ;
#64375=CARTESIAN_POINT ( 'NONE',  ( -7.320508075688773708, 198.7499999931720254, -7.320508075688774596 ) ) ;
#64379=CARTESIAN_POINT ( 'NONE',  ( -11.35316468750000141, 83.59374999658601268, -1.390361679473963753E-15 ) ) ;
#64385=CARTESIAN_POINT ( 'NONE',  ( 11.35316468750000141, 16.09374999658601979, 0.000000000000000000 ) ) ;
#64389=CARTESIAN_POINT ( 'NONE',  ( 3.042071309553159519, 224.7395833299193555, 11.35316468750000141 ) ) ;
#64394=CARTESIAN_POINT ( 'NONE',  ( -6.676582343750001591, 291.4531250017069510, 0.000000000000000000 ) ) ;
#64397=CARTESIAN_POINT ( 'NONE',  ( -5.676582343750006032, 204.4270833299193555, 9.832129032723418760 ) ) ;
#64401=( BOUNDED_CURVE ( )  B_SPLINE_CURVE ( 2, ( #7075, #30081, #53837, #53099, #2146, #48155, #2888, #71164, #65514, #42861, #14186, #13809, #59861 ),
 .UNSPECIFIED., .F., .F. ) 
 B_SPLINE_CURVE_WITH_KNOTS ( ( 3, 2, 2, 2, 2, 2, 3 ),
 ( 0.5815217391304348116, 0.5833333333333333703, 0.5851449275362319291, 0.5869565217391304879, 0.5887681159420289356, 0.5905797101449274944, 0.5923913043478260532 ),
 .UNSPECIFIED. ) 
 CURVE ( )  GEOMETRIC_REPRESENTATION_ITEM ( )  RATIONAL_B_SPLINE_CURVE ( ( 1.000000000000000000, 0.9659258262890683122, 1.000000000000000000, 0.9659258262890683122, 1.000000000000000000, 0.9659258262890683122, 1.000000000000000000, 0.9659258262890683122, 1.000000000000000000, 0.9659258262890683122, 1.000000000000000000, 0.9659258262890683122, 1.000000000000000000 ) ) 
 REPRESENTATION_ITEM ( '' )  );
#64406=CARTESIAN_POINT ( 'NONE',  ( 10.00000000000000000, 29.79166666666666785, 2.679491924311236062 ) ) ;
#64416=CARTESIAN_POINT ( 'NONE',  ( -6.676582343750002480, 298.3906250017070079, -2.765530957081996810 ) ) ;
#64425=ORIENTED_EDGE ( 'NONE', *, *, #68362, .F. ) ;
#64427=CARTESIAN_POINT ( 'NONE',  ( 11.35316468750000141, 106.0937499965860269, 0.000000000000000000 ) ) ;
#64436=CARTESIAN_POINT ( 'NONE',  ( 0.000000000000000000, 300.0000000000000000, 10.00000000000000178 ) ) ;
#64437=CARTESIAN_POINT ( 'NONE',  ( 3.042071309553167069, 206.8229166632526699, -11.35316468749999785 ) ) ;
#64441=CARTESIAN_POINT ( 'NONE',  ( 9.832129032723416984, 180.6770833299193555, 5.676582343750006032 ) ) ;
#64448=CARTESIAN_POINT ( 'NONE',  ( -3.042071309553164404, 67.23958332991935549, -11.35316468749999963 ) ) ;
#64450=CARTESIAN_POINT ( 'NONE',  ( -3.673940397442060854E-16, 298.7500000000000000, -6.000000000000001776 ) ) ;
#64453=CARTESIAN_POINT ( 'NONE',  ( -10.00000000000003020, 47.70833333333334281, 2.679491924311229401 ) ) ;
#64454=CARTESIAN_POINT ( 'NONE',  ( 6.123233995736767268E-16, 178.1249999931720538, -10.00000000000000178 ) ) ;
#64455=CARTESIAN_POINT ( 'NONE',  ( -9.832129032723418760, 77.86458332991935549, -5.676582343750004256 ) ) ;
#64460=CARTESIAN_POINT ( 'NONE',  ( 8.311093377946837890, 56.40624999658600558, -8.311093377946837890 ) ) ;
#64464=CARTESIAN_POINT ( 'NONE',  ( 10.00000000000000178, 156.8749999931720254, 0.000000000000000000 ) ) ;
#64466=VECTOR ( 'NONE', #11171, 1000.000000000000000 ) ;
#64467=CARTESIAN_POINT ( 'NONE',  ( 2.679491924311249829, 21.04166666666666785, -9.999999999999996447 ) ) ;
#64468=CARTESIAN_POINT ( 'NONE',  ( -3.042071309553163960, 52.55208332991934839, -11.35316468749999963 ) ) ;
#64470=CARTESIAN_POINT ( 'NONE',  ( 9.832129032723416984, 190.3645833299193839, 5.676582343750006032 ) ) ;
#64477=CARTESIAN_POINT ( 'NONE',  ( -11.35316468750000141, 178.4895833299193555, 3.042071309553159963 ) ) ;
#64480=DIRECTION ( 'NONE',  ( -0.000000000000000000, 1.000000000000000000, -0.000000000000000000 ) ) ;
#64482=CARTESIAN_POINT ( 'NONE',  ( -5.676582343749998039, 172.7604166632526983, -9.832129032723420536 ) ) ;
#64487=( BOUNDED_CURVE ( )  B_SPLINE_CURVE ( 2, ( #68787, #63872, #40866, #5058, #74445, #63498, #23134, #17472, #68051, #40118, #12184, #68413, #63124 ),
 .UNSPECIFIED., .F., .F. ) 
 B_SPLINE_CURVE_WITH_KNOTS ( ( 3, 2, 2, 2, 2, 2, 3 ),
 ( 0.4552960319598876593, 0.4605291305068314744, 0.4657622290537752896, 0.4709953276007191603, 0.4762284261476630309, 0.4814615246946068461, 0.4866946232415507168 ),
 .UNSPECIFIED. ) 
 CURVE ( )  GEOMETRIC_REPRESENTATION_ITEM ( )  RATIONAL_B_SPLINE_CURVE ( ( 1.000000000000021982, 0.9659258262890463298, 1.000000000000000000, 0.9659258262890682012, 1.000000000000000000, 0.9659258262890682012, 1.000000000000000000, 0.9659258262890682012, 1.000000000000000000, 0.9659258262890682012, 1.000000000000000000, 0.9659258262890593194, 1.000000000000008882 ) ) 
 REPRESENTATION_ITEM ( '' )  );
#64505=ORIENTED_EDGE ( 'NONE', *, *, #29069, .T. ) ;
#64514=CARTESIAN_POINT ( 'NONE',  ( 10.00000000000000178, 130.0000000000000000, 0.000000000000000000 ) ) ;
#64517=CARTESIAN_POINT ( 'NONE',  ( 1.102182119232618108E-15, 290.3125000034140157, 6.000000000000001776 ) ) ;
#64529=CARTESIAN_POINT ( 'NONE',  ( -8.311093377946841443, 33.90624999658602690, 8.311093377946830785 ) ) ;
#64531=CARTESIAN_POINT ( 'NONE',  ( 6.951808397369818766E-16, 217.3437499965860411, -11.35316468750000141 ) ) ;
#64537=CARTESIAN_POINT ( 'NONE',  ( -3.042071309553173730, 34.32291666325268409, 11.35316468749999785 ) ) ;
#64543=CARTESIAN_POINT ( 'NONE',  ( 11.35316468750000141, 20.78124999658601624, 0.000000000000000000 ) ) ;
#64546=CARTESIAN_POINT ( 'NONE',  ( 11.35316468750000141, 150.7812499965860411, 0.000000000000000000 ) ) ;
#64547=CARTESIAN_POINT ( 'NONE',  ( -4.999999999999998224, 113.5416666598387110, -8.660254037844389075 ) ) ;
#64549=CARTESIAN_POINT ( 'NONE',  ( 10.00000000000000000, 171.6666666598386826, 2.679491924311235618 ) ) ;
#64552=CARTESIAN_POINT ( 'NONE',  ( -5.676582343749998039, 2.760416663252683644, -9.832129032723420536 ) ) ;
#64555=CARTESIAN_POINT ( 'NONE',  ( 6.676582343750004256, 296.8906250017068942, 2.765530957081995478 ) ) ;
#64557=CARTESIAN_POINT ( 'NONE',  ( 5.676582343750001591, 136.6145833299193555, -9.832129032723420536 ) ) ;
#64560=EDGE_CURVE ( 'NONE', #30170, #16864, #31422, .T. ) ;
#64569=CARTESIAN_POINT ( 'NONE',  ( 11.35316468750000141, 91.09374999658602690, 0.000000000000000000 ) ) ;
#64585=EDGE_CURVE ( 'NONE', #1466, #23203, #18556, .T. ) ;
#64601=CARTESIAN_POINT ( 'NONE',  ( 2.679491924311228956, 101.0416666666666856, -10.00000000000000000 ) ) ;
#64603=CARTESIAN_POINT ( 'NONE',  ( 11.35316468749999963, 61.30208332991934839, -3.042071309553165293 ) ) ;
#64604=CARTESIAN_POINT ( 'NONE',  ( -4.088227598258586603E-16, 295.3593750017070079, -6.676582343750001591 ) ) ;
#64608=CARTESIAN_POINT ( 'NONE',  ( -10.00000000000000000, 144.1666666598386826, -2.679491924311229845 ) ) ;
#64616=CARTESIAN_POINT ( 'NONE',  ( 2.679491924311222739, 208.9583333333333712, 10.00000000000000355 ) ) ;
#64618=CARTESIAN_POINT ( 'NONE',  ( -5.676582343750006032, 184.4270833299193555, 9.832129032723418760 ) ) ;
#64625=CARTESIAN_POINT ( 'NONE',  ( -5.676582343750006032, 44.42708332991934839, 9.832129032723418760 ) ) ;
#64627=CARTESIAN_POINT ( 'NONE',  ( 11.35316468749999785, 225.8854166632526699, 3.042071309553174174 ) ) ;
#64630=CARTESIAN_POINT ( 'NONE',  ( -8.660254037844369535, 102.0833333333333286, -4.999999999999993783 ) ) ;
#64632=AXIS2_PLACEMENT_3D ( 'NONE', #59813, #31512, #42813 ) ;
#64633=CARTESIAN_POINT ( 'NONE',  ( -10.00000000000000355, 69.58333332650536818, 2.679491924311223183 ) ) ;
#64640=CARTESIAN_POINT ( 'NONE',  ( 4.721056650416000089, 295.9843750017070079, 4.721056650415999201 ) ) ;
#64641=CARTESIAN_POINT ( 'NONE',  ( -10.00000000000001599, 142.7083333333333428, 2.679491924311226292 ) ) ;
#64643=CARTESIAN_POINT ( 'NONE',  ( -11.35316468750000141, 153.4895833299193555, 3.042071309553159963 ) ) ;
#64651=CARTESIAN_POINT ( 'NONE',  ( 1.102182119232618108E-15, 296.3125000034140157, 6.000000000000001776 ) ) ;
#64652=CARTESIAN_POINT ( 'NONE',  ( 11.35316468749999785, 145.8854166632526983, 3.042071309553174174 ) ) ;
#64655=CARTESIAN_POINT ( 'NONE',  ( 8.311093377946837890, 46.71874999658602690, -8.311093377946837890 ) ) ;
#64661=CARTESIAN_POINT ( 'NONE',  ( -6.000000000000003553, 291.0000000034139589, -2.485281374238571317 ) ) ;
#64667=CARTESIAN_POINT ( 'NONE',  ( -8.660254037844390851, 64.79166665983871098, 4.999999999999998224 ) ) ;
#64684=CARTESIAN_POINT ( 'NONE',  ( 4.242640687119285658, 296.6250000000000000, -4.242640687119286547 ) ) ;
#64686=CARTESIAN_POINT ( 'NONE',  ( 8.660254037844385522, 54.58333333333333570, 5.000000000000005329 ) ) ;
#64688=CARTESIAN_POINT ( 'NONE',  ( 6.000000000000003553, 294.4375000000000568, 2.485281374238571317 ) ) ;
#64690=CARTESIAN_POINT ( 'NONE',  ( -10.00000000000000000, 34.16666665983870388, -2.679491924311229845 ) ) ;
#64701=CARTESIAN_POINT ( 'NONE',  ( 5.000000000000001776, 175.8333333333333428, -8.660254037844389075 ) ) ;
#64705=CARTESIAN_POINT ( 'NONE',  ( 8.311093377946837890, 141.7187499965859843, -8.311093377946837890 ) ) ;
#64717=( BOUNDED_CURVE ( )  B_SPLINE_CURVE ( 2, ( #3002, #54693, #72786, #49008, #25983, #21093, #60712, #9411, #26751 ),
 .UNSPECIFIED., .F., .F. ) 
 B_SPLINE_CURVE_WITH_KNOTS ( ( 3, 2, 2, 2, 3 ),
 ( 0.4791666666666647423, 0.4895833333333313719, 0.4999999999999981126, 0.5104166666666647423, 0.5208333333333314830 ),
 .UNSPECIFIED. ) 
 CURVE ( )  GEOMETRIC_REPRESENTATION_ITEM ( )  RATIONAL_B_SPLINE_CURVE ( ( 1.000000000000014211, 0.9238795325112725276, 1.000000000000000000, 0.9238795325112867385, 1.000000000000000000, 0.9238795325112867385, 1.000000000000000000, 0.9238795325113005052, 0.9999999999999862332 ) ) 
 REPRESENTATION_ITEM ( '' )  );
#64719=CARTESIAN_POINT ( 'NONE',  ( 2.679491924311222739, 30.83333332650536462, 10.00000000000000355 ) ) ;
#64724=CARTESIAN_POINT ( 'NONE',  ( 10.00000000000000178, 7.083333326505366401, -2.679491924311226736 ) ) ;
#64725=VERTEX_POINT ( 'NONE', #39636 ) ;
#64727=CARTESIAN_POINT ( 'NONE',  ( -7.320508075688813676, 61.87500000000003553, -7.320508075688814564 ) ) ;
#64729=CARTESIAN_POINT ( 'NONE',  ( 3.042071309553167069, 111.8229166632526983, -11.35316468749999785 ) ) ;
#64736=CARTESIAN_POINT ( 'NONE',  ( 1.479685137562080274E-15, 225.9999999999999432, -10.00000000000000178 ) ) ;
#64737=CARTESIAN_POINT ( 'NONE',  ( -8.311093377946836114, 107.6562499965860127, -8.311093377946837890 ) ) ;
#64741=CARTESIAN_POINT ( 'NONE',  ( -10.00000000000000355, 209.5833333265053398, 2.679491924311223183 ) ) ;
#64744=CARTESIAN_POINT ( 'NONE',  ( -11.35316468749999785, 98.38541666325268409, -3.042071309553167957 ) ) ;
#64748=CARTESIAN_POINT ( 'NONE',  ( -2.085542519210945728E-15, 4.843749996586016238, 11.35316468750000141 ) ) ;
#64750=CARTESIAN_POINT ( 'NONE',  ( -10.00000000000001066, 137.5000000000000000, -1.224646799147354637E-15 ) ) ;
#64756=CARTESIAN_POINT ( 'NONE',  ( -2.765530957081996810, 292.2656250017069510, -6.676582343750003368 ) ) ;
#64758=CARTESIAN_POINT ( 'NONE',  ( -8.311093377946836114, 222.9687499965860127, -8.311093377946837890 ) ) ;
#64766=CARTESIAN_POINT ( 'NONE',  ( 5.000000000000001776, 25.83333333333333570, -8.660254037844389075 ) ) ;
#64768=CARTESIAN_POINT ( 'NONE',  ( -8.660254037844469011, 172.0833333333333997, -5.000000000000053291 ) ) ;
#64770=VERTEX_POINT ( 'NONE', #69051 ) ;
#64774=CARTESIAN_POINT ( 'NONE',  ( 2.295000000000000373, 255.7199999999997715, 5.414444767710047124 ) ) ;
#64775=CARTESIAN_POINT ( 'NONE',  ( -2.765530957081998142, 297.6406250017070079, 6.676582343750000703 ) ) ;
#64788=CARTESIAN_POINT ( 'NONE',  ( 9.832129032723420536, 96.51041666325268409, -5.676582343749999815 ) ) ;
#64796=CARTESIAN_POINT ( 'NONE',  ( 11.35316468749999785, 215.5729166632526699, 3.042071309553174174 ) ) ;
#64801=CARTESIAN_POINT ( 'NONE',  ( -11.35316468750000141, 178.5937499965860411, -1.390361679473963753E-15 ) ) ;
#64808=CARTESIAN_POINT ( 'NONE',  ( 9.832129032723420536, 71.19791666325268409, -5.676582343749999815 ) ) ;
#64813=CARTESIAN_POINT ( 'NONE',  ( 6.123233995736767268E-16, 46.25000000000000711, -10.00000000000000178 ) ) ;
#64815=CARTESIAN_POINT ( 'NONE',  ( -3.042071309553164404, 72.23958332991935549, -11.35316468749999963 ) ) ;
#64820=CARTESIAN_POINT ( 'NONE',  ( -2.085542519210945728E-15, 69.53124999658602690, 11.35316468750000141 ) ) ;
#64822=CIRCLE ( 'NONE', #52768, 6.000000000000001776 ) ;
#64823=CARTESIAN_POINT ( 'NONE',  ( 2.679491924311228956, 131.0416666666666572, -10.00000000000000000 ) ) ;
#64824=CARTESIAN_POINT ( 'NONE',  ( 7.320508075688771044, 156.2499999931720538, 7.320508075688775484 ) ) ;
#64826=CARTESIAN_POINT ( 'NONE',  ( 5.676582343749993598, 60.26041666325268409, 9.832129032723422313 ) ) ;
#64828=CARTESIAN_POINT ( 'NONE',  ( -8.311093377946841443, 198.9062499965860695, 8.311093377946830785 ) ) ;
#64832=CARTESIAN_POINT ( 'NONE',  ( 10.00000000000000178, 62.08333332650536818, -2.679491924311226736 ) ) ;
#64834=CARTESIAN_POINT ( 'NONE',  ( 8.311093377946837890, 196.4062499965860411, -8.311093377946837890 ) ) ;
#64835=EDGE_CURVE ( 'NONE', #47752, #35448, #5877, .T. ) ;
#64840=ADVANCED_FACE ( 'NONE', ( #40635 ), #17617, .T. ) ;
#64841=CARTESIAN_POINT ( 'NONE',  ( 11.35316468750000141, 166.0937499965860127, 0.000000000000000000 ) ) ;
#64845=CARTESIAN_POINT ( 'NONE',  ( 6.380085505555389780, 226.0000000000000568, -8.310665951435517229 ) ) ;
#64856=CARTESIAN_POINT ( 'NONE',  ( 10.00000000000005329, 180.2083333333333712, -2.679491924311241391 ) ) ;
#64868=CARTESIAN_POINT ( 'NONE',  ( 4.999999999999993783, 91.04166665983871098, 8.660254037844390851 ) ) ;
#64873=CARTESIAN_POINT ( 'NONE',  ( 2.679491924311222739, 133.9583333333333144, 10.00000000000000355 ) ) ;
#64890=CARTESIAN_POINT ( 'NONE',  ( 3.042071309553159519, 29.73958332991934839, 11.35316468750000141 ) ) ;
#64892=CARTESIAN_POINT ( 'NONE',  ( 8.311093377946834337, 220.4687499965859843, 8.311093377946839666 ) ) ;
#64897=CARTESIAN_POINT ( 'NONE',  ( 9.832129032723420536, 41.19791666325268409, -5.676582343749999815 ) ) ;
#64902=CARTESIAN_POINT ( 'NONE',  ( -11.35316468749999785, 38.07291666325267698, -3.042071309553167957 ) ) ;
#64904=CARTESIAN_POINT ( 'NONE',  ( 3.042071309553167069, 151.8229166632526699, -11.35316468749999785 ) ) ;
#64905=CARTESIAN_POINT ( 'NONE',  ( 10.00000000000000178, 111.8749999931720396, 0.000000000000000000 ) ) ;
#64910=CARTESIAN_POINT ( 'NONE',  ( -3.042071309553163960, 2.552083329919349275, -11.35316468749999963 ) ) ;
#64914=CARTESIAN_POINT ( 'NONE',  ( -2.085542519210945728E-15, 144.5312499965860411, 11.35316468750000141 ) ) ;
#64925=CARTESIAN_POINT ( 'NONE',  ( -8.311093377946841443, 94.21874999658601268, 8.311093377946830785 ) ) ;
#64946=CARTESIAN_POINT ( 'NONE',  ( 5.000000000000001776, 122.7083333265053682, -8.660254037844389075 ) ) ;
#64951=CARTESIAN_POINT ( 'NONE',  ( -8.660254037844376640, 97.08333333333334281, -4.999999999999998224 ) ) ;
#64955=CARTESIAN_POINT ( 'NONE',  ( -8.660254037844387298, 92.08333333333334281, -5.000000000000004441 ) ) ;
#64957=CARTESIAN_POINT ( 'NONE',  ( 4.721056650416000089, 297.9843750017070079, 4.721056650415999201 ) ) ;
#64959=CARTESIAN_POINT ( 'NONE',  ( -10.00000000000000178, 174.3749999931720538, -1.224646799147353454E-15 ) ) ;
#64962=CARTESIAN_POINT ( 'NONE',  ( -1.836970198721029983E-15, 83.75000000000000000, 10.00000000000000178 ) ) ;
#64966=CARTESIAN_POINT ( 'NONE',  ( -2.679491924311235618, 213.5416666666666572, 10.00000000000000000 ) ) ;
#64967=EDGE_CURVE ( 'NONE', #26710, #74042, #10284, .T. ) ;
#64969=CARTESIAN_POINT ( 'NONE',  ( -11.35316468749999785, 178.3854166632526983, -3.042071309553167513 ) ) ;
#64972=CYLINDRICAL_SURFACE ( 'NONE', #58586, 10.00000000000000178 ) ;
#64978=CARTESIAN_POINT ( 'NONE',  ( -3.042071309553173730, 44.63541666325269119, 11.35316468749999785 ) ) ;
#64980=CARTESIAN_POINT ( 'NONE',  ( 3.042071309553167069, 222.1354166632526699, -11.35316468749999785 ) ) ;
#64984=CARTESIAN_POINT ( 'NONE',  ( -4.999999999999994671, 103.3333333333333286, 8.660254037844369535 ) ) ;
#64987=EDGE_CURVE ( 'NONE', #21228, #2370, #15992, .T. ) ;
#64988=CARTESIAN_POINT ( 'NONE',  ( -10.00000000000000178, 74.37499999317203958, -1.224646799147353454E-15 ) ) ;
#64991=CARTESIAN_POINT ( 'NONE',  ( -2.679491924311163231, 73.54166666666668561, 10.00000000000004796 ) ) ;
#64994=ORIENTED_EDGE ( 'NONE', *, *, #4010, .T. ) ;
#64996=CARTESIAN_POINT ( 'NONE',  ( 2.765530957082001251, 291.9218750017069510, 6.676582343750000703 ) ) ;
#64998=CARTESIAN_POINT ( 'NONE',  ( 6.951808397369818766E-16, 162.0312499965860127, -11.35316468750000141 ) ) ;
#64999=DIRECTION ( 'NONE',  ( -0.000000000000000000, 1.000000000000000000, -0.000000000000000000 ) ) ;
#65006=CARTESIAN_POINT ( 'NONE',  ( 5.676582343750001591, 136.9270833299193555, -9.832129032723420536 ) ) ;
#65008=CARTESIAN_POINT ( 'NONE',  ( 2.485281374238987873, 298.3750000034140157, 5.999999999999586997 ) ) ;
#65011=CARTESIAN_POINT ( 'NONE',  ( -11.35316468750000141, 43.59374999658601979, -1.390361679473963753E-15 ) ) ;
#65012=ORIENTED_EDGE ( 'NONE', *, *, #17399, .F. ) ;
#65017=CARTESIAN_POINT ( 'NONE',  ( 1.102182119232618108E-15, 293.3125000034140157, 6.000000000000001776 ) ) ;
#65022=( BOUNDED_CURVE ( )  B_SPLINE_CURVE ( 2, ( #3938, #62370, #73334, #15602, #56359, #15975, #21638, #49946, #21266, #44290, #11079, #68409, #38641 ),
 .UNSPECIFIED., .F., .F. ) 
 B_SPLINE_CURVE_WITH_KNOTS ( ( 3, 2, 2, 2, 2, 2, 3 ),
 ( 0.9576885471939067251, 0.9629223234525785546, 0.9681560997112503841, 0.9733898759699222136, 0.9786236522285940431, 0.9838574284872658726, 0.9890912047459377021 ),
 .UNSPECIFIED. ) 
 CURVE ( )  GEOMETRIC_REPRESENTATION_ITEM ( )  RATIONAL_B_SPLINE_CURVE ( ( 1.000000000000083489, 0.9659258262889847124, 1.000000000000000000, 0.9659258262890682012, 1.000000000000000000, 0.9659258262890682012, 1.000000000000000000, 0.9659258262890682012, 1.000000000000000000, 0.9659258262890682012, 1.000000000000000000, 0.9659258262890692004, 0.9999999999999990008 ) ) 
 REPRESENTATION_ITEM ( '' )  );
#65036=ORIENTED_EDGE ( 'NONE', *, *, #71229, .T. ) ;
#65040=CARTESIAN_POINT ( 'NONE',  ( -10.00000000000000000, 52.29166666666665719, -2.679491924311229845 ) ) ;
#65042=CARTESIAN_POINT ( 'NONE',  ( 4.242640687119287435, 295.3750000000000000, 4.242640687119285658 ) ) ;
#65043=CARTESIAN_POINT ( 'NONE',  ( -5.999999999999999112, 288.1250000034140157, 2.485281374238575314 ) ) ;
#65053=CARTESIAN_POINT ( 'NONE',  ( 7.320508075688771044, 169.3750000000000000, 7.320508075688775484 ) ) ;
#65054=CARTESIAN_POINT ( 'NONE',  ( 2.485281374238974994, 297.3750000034140157, 5.999999999999600320 ) ) ;
#65056=CARTESIAN_POINT ( 'NONE',  ( -11.35316468750000141, 138.8020833299193271, 3.042071309553159963 ) ) ;
#65061=CARTESIAN_POINT ( 'NONE',  ( 2.030339228148215693E-11, 166.2499999999984368, -10.00000000000000178 ) ) ;
#65063=CARTESIAN_POINT ( 'NONE',  ( -11.35316468750000141, 8.802083329919348387, 3.042071309553159963 ) ) ;
#65069=CARTESIAN_POINT ( 'NONE',  ( -2.679491924311235618, 30.41666665983869677, 10.00000000000000000 ) ) ;
#65074=CARTESIAN_POINT ( 'NONE',  ( 2.250000000000000000, 284.0000000000000000, 7.677076266392047543 ) ) ;
#65077=CARTESIAN_POINT ( 'NONE',  ( 4.242640687119287435, 292.4375000034140157, 4.242640687119285658 ) ) ;
#65081=CARTESIAN_POINT ( 'NONE',  ( 9.832129032723416984, 115.3645833299193555, 5.676582343750006032 ) ) ;
#65082=ORIENTED_EDGE ( 'NONE', *, *, #28892, .T. ) ;
#65087=FACE_OUTER_BOUND ( 'NONE', #914, .T. ) ;
#65091=CARTESIAN_POINT ( 'NONE',  ( -3.042071309553163960, 117.2395833299193697, -11.35316468749999963 ) ) ;
#65094=ORIENTED_EDGE ( 'NONE', *, *, #42404, .T. ) ;
#65096=CARTESIAN_POINT ( 'NONE',  ( 4.999999999999993783, 211.0416666598387110, 8.660254037844390851 ) ) ;
#65099=CARTESIAN_POINT ( 'NONE',  ( -5.676582343750006032, 99.42708332991935549, 9.832129032723418760 ) ) ;
#65103=CARTESIAN_POINT ( 'NONE',  ( 11.35316468749999963, 11.30208332991934839, -3.042071309553165293 ) ) ;
#65110=CARTESIAN_POINT ( 'NONE',  ( 8.660254037844385522, 199.5833333333333428, 5.000000000000005329 ) ) ;
#65111=CARTESIAN_POINT ( 'NONE',  ( -2.765530957081998586, 291.6406250017068942, 6.676582343750001591 ) ) ;
#65113=CARTESIAN_POINT ( 'NONE',  ( 8.660254037844389075, 127.2916666598387110, -5.000000000000000000 ) ) ;
#65114=CARTESIAN_POINT ( 'NONE',  ( 5.676582343750001591, 221.9270833299193555, -9.832129032723420536 ) ) ;
#65132=VECTOR ( 'NONE', #16544, 1000.000000000000000 ) ;
#65134=CARTESIAN_POINT ( 'NONE',  ( -4.721056650415998313, 292.5781250017069510, 4.721056650416000089 ) ) ;
#65145=CARTESIAN_POINT ( 'NONE',  ( 1.224646799147353454E-15, 300.0000000000000000, -10.00000000000000178 ) ) ;
#65146=CARTESIAN_POINT ( 'NONE',  ( -2.085542519210945728E-15, 104.8437499965860269, 11.35316468750000141 ) ) ;
#65147=CARTESIAN_POINT ( 'NONE',  ( -1.836970198721029983E-15, 210.6249999931720538, 10.00000000000000178 ) ) ;
#65153=EDGE_CURVE ( 'NONE', #13863, #27743, #67116, .T. ) ;
#65155=CARTESIAN_POINT ( 'NONE',  ( 5.676582343750001591, 211.6145833299193555, -9.832129032723420536 ) ) ;
#65159=CARTESIAN_POINT ( 'NONE',  ( 9.832129032723416984, 200.6770833299193555, 5.676582343750006032 ) ) ;
#65166=CARTESIAN_POINT ( 'NONE',  ( 11.35316468750000141, 75.78124999658602690, 0.000000000000000000 ) ) ;
#65171=CARTESIAN_POINT ( 'NONE',  ( 6.951808397369818766E-16, 72.03124999658602690, -11.35316468750000141 ) ) ;
#65179=CARTESIAN_POINT ( 'NONE',  ( 8.311093377946834337, 75.15624999658602690, 8.311093377946839666 ) ) ;
#65181=CARTESIAN_POINT ( 'NONE',  ( 2.679491924312694895, 128.9583333333334565, 9.999999999999154454 ) ) ;
#65182=CARTESIAN_POINT ( 'NONE',  ( 10.00000000000000000, 171.6666666598386826, 2.679491924311236062 ) ) ;
#65185=CARTESIAN_POINT ( 'NONE',  ( -11.35316468750000141, 58.80208332991934128, 3.042071309553159963 ) ) ;
#65187=CARTESIAN_POINT ( 'NONE',  ( -5.676582343750006032, 194.1145833299193839, 9.832129032723418760 ) ) ;
#65191=CARTESIAN_POINT ( 'NONE',  ( 4.999999999999993783, 161.0416666598387110, 8.660254037844390851 ) ) ;
#65193=CARTESIAN_POINT ( 'NONE',  ( 5.676582343750001591, 191.6145833299193839, -9.832129032723420536 ) ) ;
#65200=CARTESIAN_POINT ( 'NONE',  ( 3.042071309553159519, 180.0520833299193555, 11.35316468750000141 ) ) ;
#65210=CARTESIAN_POINT ( 'NONE',  ( -4.999999999999998224, 1.666666666666666741, -8.660254037844389075 ) ) ;
#65216=CIRCLE ( 'NONE', #52002, 10.00000000000000178 ) ;
#65226=ORIENTED_EDGE ( 'NONE', *, *, #34372, .F. ) ;
#65228=ORIENTED_EDGE ( 'NONE', *, *, #56984, .T. ) ;
#65230=CARTESIAN_POINT ( 'NONE',  ( -2.679491924311235174, 115.4166666598386968, 10.00000000000000000 ) ) ;
#65234=CARTESIAN_POINT ( 'NONE',  ( -4.721056650415999201, 293.4843750017070079, -4.721056650415999201 ) ) ;
#65235=CARTESIAN_POINT ( 'NONE',  ( 5.000000000000001776, 145.8333333333333428, -8.660254037844389075 ) ) ;
#65245=CYLINDRICAL_SURFACE ( 'NONE', #70857, 10.00000000000000178 ) ;
#65248=CARTESIAN_POINT ( 'NONE',  ( -7.320508075688778149, 133.1250000000000284, 7.320508075688770155 ) ) ;
#65253=CARTESIAN_POINT ( 'NONE',  ( -3.042071309553164404, 22.23958332991935549, -11.35316468749999963 ) ) ;
#65256=CARTESIAN_POINT ( 'NONE',  ( -7.320508075688778149, 9.999999993172032475, 7.320508075688769267 ) ) ;
#65258=LINE ( 'NONE', #1898, #15444 ) ;
#65260=CARTESIAN_POINT ( 'NONE',  ( 6.123233995736767268E-16, 128.1249999931720254, -10.00000000000000178 ) ) ;
#65262=CARTESIAN_POINT ( 'NONE',  ( 9.832129032723416984, 30.36458332991935194, 5.676582343750006032 ) ) ;
#65268=CARTESIAN_POINT ( 'NONE',  ( 5.676582343749993598, 34.94791666325268409, 9.832129032723422313 ) ) ;
#65270=CARTESIAN_POINT ( 'NONE',  ( -11.35316468750000141, 153.4895833299193555, 3.042071309553159963 ) ) ;
#65272=CARTESIAN_POINT ( 'NONE',  ( 7.320508075688774596, 132.4999999931720254, -7.320508075688774596 ) ) ;
#65278=CARTESIAN_POINT ( 'NONE',  ( 9.832129032723420536, 26.51041666325268409, -5.676582343749999815 ) ) ;
#65284=CARTESIAN_POINT ( 'NONE',  ( -9.832129032723418760, 152.8645833299193555, -5.676582343750004256 ) ) ;
#65292=EDGE_CURVE ( 'NONE', #26800, #5410, #49828, .T. ) ;
#65293=CARTESIAN_POINT ( 'NONE',  ( 6.123233995736767268E-16, 203.1249999931720538, -10.00000000000000178 ) ) ;
#65295=CARTESIAN_POINT ( 'NONE',  ( 11.35316468749999963, 106.3020833299193413, -3.042071309553165293 ) ) ;
#65298=ORIENTED_EDGE ( 'NONE', *, *, #62606, .F. ) ;
#65301=CARTESIAN_POINT ( 'NONE',  ( -1.836970198721029983E-15, 215.6249999931720538, 10.00000000000000178 ) ) ;
#65316=DIRECTION ( 'NONE',  ( -0.000000000000000000, 1.000000000000000000, -0.000000000000000000 ) ) ;
#65318=CARTESIAN_POINT ( 'NONE',  ( 6.123233995736767268E-16, 123.1249999931720396, -10.00000000000000178 ) ) ;
#65323=CARTESIAN_POINT ( 'NONE',  ( -1.836970198721029983E-15, 123.7500000000000142, 10.00000000000000178 ) ) ;
#65328=CARTESIAN_POINT ( 'NONE',  ( 2.679491924311222739, 98.95833333333334281, 10.00000000000000355 ) ) ;
#65331=CARTESIAN_POINT ( 'NONE',  ( -4.721056650415998313, 294.7343750017069510, 4.721056650416000089 ) ) ;
#65338=CARTESIAN_POINT ( 'NONE',  ( -2.143145793903030439E-12, 53.74999999999984368, 9.999999999999998224 ) ) ;
#65343=CARTESIAN_POINT ( 'NONE',  ( 7.320508075688774596, 215.6249999999999716, -7.320508075688774596 ) ) ;
#65346=CARTESIAN_POINT ( 'NONE',  ( -11.35316468750000141, 188.8020833299193555, 3.042071309553159963 ) ) ;
#65347=CARTESIAN_POINT ( 'NONE',  ( 8.660254037844389075, 192.2916666598387110, -5.000000000000000000 ) ) ;
#65354=CARTESIAN_POINT ( 'NONE',  ( -5.676582343750006032, 54.42708332991935549, 9.832129032723418760 ) ) ;
#65356=CARTESIAN_POINT ( 'NONE',  ( -5.676582343750006032, 214.4270833299193555, 9.832129032723418760 ) ) ;
#65358=CARTESIAN_POINT ( 'NONE',  ( -7.320508075688778149, 124.9999999931720396, 7.320508075688769267 ) ) ;
#65363=CARTESIAN_POINT ( 'NONE',  ( 11.35316468749999785, 110.5729166632526983, 3.042071309553174174 ) ) ;
#65364=CARTESIAN_POINT ( 'NONE',  ( -2.679491924311225848, 73.33333332650536818, -10.00000000000000178 ) ) ;
#65369=ORIENTED_EDGE ( 'NONE', *, *, #62889, .F. ) ;
#65371=CARTESIAN_POINT ( 'NONE',  ( 6.676582343750001591, 293.1093750017069510, -8.176455196517173205E-16 ) ) ;
#65373=CARTESIAN_POINT ( 'NONE',  ( 5.676582343749993598, 169.9479166632526983, 9.832129032723422313 ) ) ;
#65382=CARTESIAN_POINT ( 'NONE',  ( -5.676582343750006032, 144.4270833299193555, 9.832129032723418760 ) ) ;
#65386=CARTESIAN_POINT ( 'NONE',  ( 5.676582343749993598, 45.26041666325268409, 9.832129032723422313 ) ) ;
#65394=CARTESIAN_POINT ( 'NONE',  ( 2.485281374238571317, 290.7500000034139589, -6.000000000000003553 ) ) ;
#65395=CARTESIAN_POINT ( 'NONE',  ( 1.110124581937998163E-11, 98.75000000000088107, 10.00000000000000533 ) ) ;
#65401=VERTEX_POINT ( 'NONE', #51314 ) ;
#65413=CARTESIAN_POINT ( 'NONE',  ( -10.00000000000000178, 202.7083333333333144, 2.679491924311223183 ) ) ;
#65416=CARTESIAN_POINT ( 'NONE',  ( -10.00000000000000000, 57.29166666666667140, -2.679491924311229845 ) ) ;
#65419=CARTESIAN_POINT ( 'NONE',  ( -3.673940397442060854E-16, 297.7500000000000000, -6.000000000000001776 ) ) ;
#65429=DIRECTION ( 'NONE',  ( 0.000000000000000000, 0.000000000000000000, 1.000000000000000000 ) ) ;
#65431=CARTESIAN_POINT ( 'NONE',  ( 5.000000000000001776, 170.8333333333333428, -8.660254037844389075 ) ) ;
#65434=CARTESIAN_POINT ( 'NONE',  ( 8.311093377946837890, 136.7187499965860411, -8.311093377946837890 ) ) ;
#65438=CARTESIAN_POINT ( 'NONE',  ( 5.000000000000001776, 107.7083333265053682, -8.660254037844389075 ) ) ;
#65439=CARTESIAN_POINT ( 'NONE',  ( -4.242640687119285658, 294.1249999999999432, 4.242640687119287435 ) ) ;
#65442=CARTESIAN_POINT ( 'NONE',  ( -3.042071309553173730, 9.635416663252682312, 11.35316468749999785 ) ) ;
#65448=CARTESIAN_POINT ( 'NONE',  ( -7.320508075688778149, 39.99999999317201826, 7.320508075688769267 ) ) ;
#65455=ORIENTED_EDGE ( 'NONE', *, *, #67155, .F. ) ;
#65458=CARTESIAN_POINT ( 'NONE',  ( 4.242640687119285658, 292.6875000034139589, -4.242640687119286547 ) ) ;
#65461=CARTESIAN_POINT ( 'NONE',  ( -3.042071309553173730, 129.3229166632526983, 11.35316468749999785 ) ) ;
#65462=VERTEX_POINT ( 'NONE', #44174 ) ;
#65469=CARTESIAN_POINT ( 'NONE',  ( 5.676582343749993598, 109.9479166632526983, 9.832129032723422313 ) ) ;
#65471=CARTESIAN_POINT ( 'NONE',  ( 10.00000000000000178, 82.08333332650535397, -2.679491924311226736 ) ) ;
#65473=CARTESIAN_POINT ( 'NONE',  ( 5.000000000000001776, 212.7083333265053682, -8.660254037844389075 ) ) ;
#65477=CARTESIAN_POINT ( 'NONE',  ( 11.35316468750000141, 101.0937499965860127, 0.000000000000000000 ) ) ;
#65481=CARTESIAN_POINT ( 'NONE',  ( 8.311093377946834337, 10.46874999658601624, 8.311093377946839666 ) ) ;
#65482=( BOUNDED_SURFACE ( )  B_SPLINE_SURFACE ( 1, 2, ( 
 ( #32390, #19192, #42194, #31635, #2595, #2217, #32011, #43314, #65210, #71236, #26327, #14635, #42571, #37677, #1854, #13516, #47857, #25584, #19926, #55030, #13882, #3337, #24840, #70878, #42936, #49347, #7882, #25212, #65956, #30887, #53905, #72365, #20676, #14261, #37297, #43695, #60293, #8622, #54654, #67458, #56521, #38420, #33894, #38795, #27087, #62905, #4837, #3714, #50102, #33520, #50466, #44446, #11236, #72747, #61422, #73116, #45189, #44818, #68200, #15755, #44075, #28207, #55404, #10487, #21052, #67830, #26712, #27834, #67086, #9751, #21423, #50843, #68571, #73480, #73857, #74229, #61798, #56895, #32770, #39159, #10115, #33154, #16497, #56148, #55777, #5208, #49732, #16876, #15383, #4093, #4463, #22163, #27451, #21788, #16121, #62162, #39536, #62532, #10858, #51220, #22535, #45556, #39899, #17629, #57267, #11979, #69320, #70074, #28953, #18009, #5582, #35379, #11603, #64033, #12705, #40648, #28580, #41025, #12345, #7063, #63652, #29701, #34638, #35010, #64766, #35735, #47410, #34263, #58025, #51588, #70433, #52716, #6332, #74605, #6695, #69695, #22918, #312, #47038, #58390, #1050, #24403, #18380, #64406, #58753, #30070, #51973, #57644, #24028, #41394, #53084, #29336, #1419, #18749, #41758, #45932, #23289, #68943, #52345, #682, #17254, #40274, #5953, #63275, #23667, #46300, #46673, #51135, #27747, #74145, #17170, #56434, #11523, #22082, #5870, #16787, #10774, #74519, #34178, #39814, #68120, #16414, #45107, #29250, #11894, #56808, #51887, #50758, #45844, #73774, #34557, #57562, #39447, #4755, #22828, #62819, #62446, #11154, #57180, #23578, #33435, #33811, #68859, #22449, #5129, #23208, #28867, #28121, #45469, #40565, #227, #68484, #46220, #6246, #5497, #62085, #28497, #51506, #69237, #40190, #63193, #52262, #10407, #17546, #63568, #34928, #57940, #595, #46588, #16048, #39080, #2052, #63949, #24317, #12622, #35293, #25039, #19386, #36022, #12259, #58306, #70355, #17924, #47328, #18666, #35653, #41677, #30720, #13349, #36387, #42399, #65040, #29984, #59771, #42033, #2421, #6974, #47687, #59402, #7716, #12985, #53741, #64686, #24677, #8080, #6611, #70708, #59040, #7347, #53002, #31081, #48060, #58668, #71068, #54109, #65416, #13713, #29618, #30354, #53375, #36758, #1698, #19027, #25415, #52631, #966, #1335, #40940, #69609, #23949, #46958, #64318, #69986, #18294, #41310, #25782, #3541, #26917, #8828, #19762, #32218, #55236, #21254, #31839, #43901, #48802, #54858, #4292, #49931, #61630, #48430, #3169, #71433, #9949, #66913, #49176, #42770, #20880, #9197, #65786, #14464, #61252, #26533, #49557, #38629, #9583, #3927, #72946, #44279, #43144, #71811, #72576, #55609, #15218, #20499, #38249, #67290, #32601, #32982, #37501, #15589, #26158, #43514, #55982, #8445, #20129, #60127, #14838, #14090, #72186, #37125, #31465, #66159, #66527, #54490, #2795, #60501, #37878, #60874, #27284, #63480, #22737, #28038, #50301, #74431, #62729, #73322, #68031, #40103, #57091, #5407, #17454, #63108, #57475, #28777, #5781, #21999, #4666, #11067, #34471, #34095, #74059, #28409, #51792, #11434, #40475, #16325, #51417, #10688, #22359, #140, #61997, #27661, #38992, #68398, #21625, #62357, #45757, #68770, #15963, #17081, #56347, #10319, #45025, #44649, #23116, #46129, #67664, #56723, #39360, #33345, #69147, #11802, #16696, #50668, #73686, #51049, #33721, #5041, #45383, #39727, #34840, #57847, #24594, #47599, #53654, #1610, #41220, #70621, #36671, #18576, #23487, #35934, #64228, #6522, #13265, #18941, #46499, #52539, #30632, #41947, #877, #64955, #70987, #69519, #52176, #35566, #12536, #36302, #69895, #7258, #19303, #508, #58579, #1964, #63855, #29529, #6887, #12170, #35204, #59319, #30269, #17833, #23863, #53285, #42313, #7625, #58221, #18207, #24955, #46873, #47972, #29898, #52911, #13633, #65328, #29158, #1245, #58951, #40847, #24223, #47236, #6152, #70264, #41586, #64601, #12898, #25326, #15129, #9494, #26064, #54020, #2330, #60411, #7992, #14376, #8737, #2706, #31750, #20792, #3451, #26440, #32508, #55146, #60787, #8355, #37410, #38161, #71720, #37791, #49465, #72485, #3080, #43812, #54770, #14750, #49842, #48342, #9111, #49085, #72098, #20036, #72861, #66827, #48714, #61163, #21166, #55520, #3832, #71349, #20412, #43428, #26828, #66442, #32127, #44190, #19671, #42683, #43050, #30997, #67203, #66069, #15501, #54399, #59681, #65695, #13995, #37036, #60037, #31372, #25694, #9862, #22277, #45299, #11346, #73599, #34012, #38904, #21906, #69061, #40019, #51703, #38538, #44936, #61539, #49, #57007, #39275, #32890, #10977, #73971, #55892, #4575, #51331, #68313, #16610, #28689, #74340, #68683, #63021, #16992, #33259, #15872, #39647, #45668, #62644, #10604, #5320, #34381, #22648, #23033, #27573, #28322, #67944, #33632, #57381, #73233, #61907, #50212, #4953, #4206, #16238, #5691, #46042, #27196, #21539, #67575, #44563, #10231, #56259, #62276, #50581, #56638, #27953, #50958, #18855, #30547, #47884, #52453, #17366, #53563, #12812, #18118, #40390, #64514, #52821, #63388, #58131, #30177, #47147, #70179, #7541, #53194, #47514, #41862, #70540, #12081, #69430, #1156, #24510, #24134, #64139, #18488, #64873, #1530, #1879, #6440, #41498, #791, #12447, #13176, #52089, #17739, #29068, #58493, #11712, #23775, #35846, #58860, #6062, #7172, #46416, #421, #35117, #34752, #36212, #59229, #57757, #46778, #29442, #23401, #24865, #40754, #6799, #63763, #69802, #41132, #35479, #29811, #71631, #13909, #19953, #33087, #15692, #38734, #44754, #67390, #72006, #19580, #25611, #27386, #8268, #48996, #61732, #10050, #14285, #56084, #48624, #25973, #62098, #65235, #20321, #42962, #65981, #31282, #10421, #4393, #59953, #50405, #33451, #73419, #21724, #36578, #31662, #60320, #67767, #37323, #2989, #43337, #13539, #53930, #54310, #19218, #8648, #2621, #16061, #65610, #54683, #42223, #39095, #48254, #56451, #4769, #27761, #59591, #7904, #70903, #30910, #2243, #25237, #36948, #71261, #42595, #69250, #17560, #23592, #46233, #51901, #74158, #5510, #6261, #62833, #28882, #40578, #63580, #68874, #34941, #28510, #5884, #40954, #45121, #242, #22845, #45858, #11169, #63963, #11908, #39829, #57953, #12274, #29264, #52276, #16428, #11536, #40204, #612, #17184, #57575, #23222, #68133, #33825, #34192, #73787, #51519, #57195, #46601, #45482, #34568, #22096, #69624, #28136, #17938, #35308, #74534, #39464, #58320, #6627, #50773, #63207, #62461, #51150, #10790, #56822, #5143, #22462, #68501, #16801, #29631, #65800, #25053, #30369, #52644, #2065, #65053, #980, #70367, #42412, #59415, #7728, #19775, #65431, #59783, #31095, #8092, #24330, #6991, #13363, #36771, #36402, #1713, #30735, #54124, #13726, #42783, #18682, #53753, #12999, #24691, #2435, #64332, #30002, #41323, #70722, #23963, #64701, #48074, #71082, #18309, #19400, #58682, #12637, #47341, #46970, #25428, #48444, #70000, #59053, #41689, #35668, #71447, #14105, #19042, #53015, #37138, #1347, #36037, #60140, #7361, #53387, #47702, #42046, #9596, #48817, #3939, #14478, #72962, #9212, #3184, #66927, #26547, #32232, #60516, #8842, #37517, #21639, #4308, #49190, #44291, #20142, #38263, #43159, #26928, #49947, #31852, #71824, #15231, #55250, #54875, #60890, #21267, #39006, #20894, #25797, #61266, #43528, #26171, #15603, #67304, #66174, #72201, #32994, #38642, #20513, #61644, #73335, #66543, #54503, #37892, #14852, #9962, #3557, #32615, #44664, #2809, #49571, #55994, #72589, #43916, #55623, #27298, #50314, #67679, #15976, #8460, #31480, #34484, #23501, #57490, #45038, #74072, #63121, #68047, #40489, #45394, #33734, #69534, #11447, #10334, #56736, #40115, #57104, #51060, #17846, #4679, #16337, #5055, #51808, #51430, #155, #22373, #50681, #34854, #62009, #17093, #27675, #74442, #33359, #5795, #73699, #39375, #28050, #28792, #521, #5418, #23131, #6166, #68410, #63494, #62373, #45772, #16710, #39740, #46143, #62740, #10700, #11816, #56360, #46516, #22012, #11080, #34107, #28423, #22749, #68783, #69160, #17469, #57860, #29175, #52190, #35218, #41601, #63869, #70278, #64616, #58594, #12912, #1977, #59331, #7641, #13645, #36315, #41959, #64242, #18590, #70998, #52926, #18955, #30647, #53665, #58965, #24969, #35946, #70636, #31010, #58237, #64966, #7272, #30280, #1259, #54035, #47985, #29911, #19314, #2345, #42325, #65343, #6536, #1625, #53300, #36683, #24605, #47612, #13276, #29542, #23877, #24237, #12181, #59695, #47251, #8003, #35580, #25340, #52553, #48354, #18221, #71360, #40862, #892, #46887, #69910, #41236, #12552, #6900, #15145, #20049, #3094, #50228, #21181, #32906, #19685, #54783, #42695, #55911, #38177, #20426, #65707, #66842, #55162, #14012, #60426, #32525, #49481, #72500, #9878, #55538, #49859, #44207, #72877, #14392 ),
 ( #31386, #26079, #20809, #60049, #61180, #25707, #9511, #43442, #37426, #3467, #37804, #66457, #71734, #43066, #48727, #4223, #15515, #8753, #3848, #54412, #43827, #2719, #26844, #67219, #66082, #8370, #26456, #14766, #31763, #72113, #38556, #37048, #32141, #49100, #61557, #60800, #9125, #27211, #40034, #15889, #44953, #23047, #11361, #67960, #34396, #63405, #38921, #44580, #27969, #4968, #68698, #62292, #74354, #11731, #67593, #56653, #46058, #56274, #73616, #50974, #4593, #27587, #57397, #22664, #61923, #16253, #45683, #34771, #17008, #50597, #10620, #63037, #21922, #51718, #73988, #39291, #6078, #5705, #21554, #33647, #51344, #68329, #22291, #29086, #10248, #45314, #16626, #28704, #62659, #65, #39661, #33275, #69077, #73249, #28337, #10993, #34026, #57023, #17383, #5336, #40407, #57774, #47530, #65253, #70196, #1545, #70920, #58509, #30564, #58150, #35862, #64156, #6814, #41878, #29827, #35134, #1894, #59607, #13558, #52106, #40772, #46797, #24524, #17758, #63780, #12827, #53211, #12465, #41151, #70555, #36597, #46433, #35496, #24881, #6457, #52470, #52839, #29460, #806, #64890, #18871, #12097, #69819, #13191, #7920, #36229, #23793, #1172, #59246, #18135, #53580, #24151, #47164, #439, #7557, #23418, #18504, #30194, #41513, #64529, #69447, #58877, #7188, #47900, #19233, #42240, #43737, #19971, #19597, #3756, #30925, #60718, #71278, #20338, #2260, #9039, #42613, #13924, #48640, #26368, #44121, #49014, #55072, #49775, #37339, #9417, #36963, #14679, #42977, #60337, #20720, #8665, #59969, #55446, #38464, #67130, #53947, #65627, #25626, #3381, #8287, #31297, #66372, #32052, #65998, #54327, #14303, #49390, #2638, #72409, #71650, #66751, #31680, #54699, #37718, #72024, #3008, #25990, #43355, #15057, #15425, #26757, #38091, #61088, #32435, #72791, #21098, #61467, #25254, #48271, #73160, #16537, #33562, #15802, #62205, #28253, #40317, #22206, #27130, #39578, #44865, #10159, #16924, #51261, #50145, #56193, #34309, #22580, #4505, #45600, #63464, #21468, #55822, #39203, #16162, #5253, #56937, #45233, #32814, #50511, #68615, #62573, #10904, #22968, #39947, #62952, #11277, #57313, #27498, #61840, #68245, #5624, #33938, #56566, #74271, #28624, #51637, #45975, #73525, #68990, #67870, #4881, #17299, #44490, #33196, #67503, #50887, #4140, #10530, #9792, #38837, #21832, #27876, #73901, #23334, #58064, #34682, #35780, #70476, #57688, #18051, #6375, #28998, #18794, #13110, #29741, #5996, #52016, #64076, #11647, #41066, #12384, #29381, #35419, #24444, #7105, #30113, #36146, #58795, #64448, #12019, #58429, #41799, #724, #41436, #53130, #1463, #6737, #47452, #52756, #18422, #53498, #354, #12749, #1092, #24069, #23707, #1815, #64808, #52388, #59167, #24801, #7476, #30481, #46346, #47079, #70116, #47815, #70838, #19150, #63321, #69363, #17673, #46711, #40690, #63692, #69736, #35052, #36883, #25909, #65166, #43271, #19513, #71939, #20633, #2550, #13477, #48926, #20251, #14967, #25541, #37632, #42531, #48554, #72704, #43649, #55361, #42153, #71563, #36516, #3667, #60630, #42892, #59525, #65911, #7838, #14593, #2921, #30843, #8204, #54989, #66286, #8952, #32348, #3296, #72320, #66660, #38004, #59891, #65545, #31964, #49303, #26282, #14217, #61002, #9328, #26666, #49690, #31216, #53864, #19886, #37256, #2176, #25170, #13838, #48187, #8577, #71194, #60251, #54241, #31593, #54614, #68154, #50056, #55736, #15714, #67040, #16452, #28161, #15340, #50426, #38756, #61380, #51171, #45506, #62119, #38375, #9707, #21748, #44032, #73440, #44775, #61756, #67790, #56846, #39488, #62484, #68524, #10813, #22118, #44402, #16081, #74181, #33109, #73811, #33848, #5166, #39116, #22485, #10444, #50798, #11190, #32728, #45143, #33474, #56476, #56105, #34216, #16826, #10074, #39854, #57218, #62855, #5532, #4052, #4792, #27785, #28533, #51541, #21006, #27045, #73072, #21378, #4414, #67415, #27410, #34962, #36702, #69273, #59348, #22870, #1995, #51925, #30666, #54054, #57977, #45883, #7660, #53685, #48374, #6282, #71017, #263, #29289, #31404, #2364, #14030, #74558, #52299, #68898, #37068, #19332, #63984, #8021, #46626, #24987, #48003, #17207, #57597, #635, #40227, #23616, #69646, #59713, #17584, #42346, #63230, #65363, #23246, #13661, #25359, #17959, #11557, #31029, #71379, #19703, #40978, #42715, #46254, #13296, #34590, #65727, #60069, #5907, #36334, #28907, #8390, #40602, #63603, #11930, #26863, #15164, #2737, #20445, #67239, #9529, #32544, #44598, #15534, #9895, #55930, #32925, #49119, #31782, #38196, #61575, #61199, #26476, #55555, #4242, #38575, #67610, #43461, #3868, #37824, #49501, #27229, #14411, #54804, #66101, #20828, #25725, #14784, #49878, #72893, #43085, #21200, #8772, #37444, #72131, #48746, #44226, #50245, #71753, #9143, #66476, #20067, #73267, #21572, #43845, #60442, #3114, #55181, #26098, #32160, #3486, #60819, #72519, #15907, #38939, #61940, #10267, #54431, #66858, #56670, #62676, #63421, #45332, #11379, #23065, #87, #51362, #17400, #11011, #63055, #23434, #27604, #34413, #5352, #28354, #68347, #46449, #46074, #22307, #28722, #69466, #51737, #40423, #73635, #68715, #57416, #56292, #27988, #5722, #74372, #16644, #40789, #50616, #39312, #50992, #69093, #22683, #11749, #39677, #21941, #6098, #33294, #34787, #44970, #45701, #4609, #57790, #67976, #16271, #74004, #29104, #17775, #17026, #52123, #455, #34046, #63795, #62310, #40051, #57041, #10637, #33665, #4987, #69838, #36613, #19615, #25270, #12114, #824, #6832, #59262, #52486, #23810, #47548, #13209, #47181, #46813, #70213, #36247, #18152, #7574, #41167, #1912, #12842, #29845, #70572, #30209, #35879, #64178, #12482, #35512, #48289, #7938, #52856, #47916, #58525, #41894, #1188, #30578, #53600, #24169, #18522, #18888, #58897, #41530, #64546, #24899, #42629, #24540, #29476, #64904, #7206, #53229, #19247, #70935, #1561, #42259, #59623, #65270, #13575, #30943, #2276, #53964, #58168, #71296, #35152, #6473, #54716, #66768, #4156, #59986, #49030, #38480, #48656, #66013, #43372, #71665, #19985, #3772, #15072, #31313, #60353, #38106, #27145, #61105, #42994, #3022, #9434, #14319, #44138, #72038, #37353, #73178, #20736, #67149, #49792, #55840, #26006, #32452, #20354, #37735, #72806, #25642, #8680, #2652, #32069, #13940, #66388, #49406, #43754, #54341, #55462, #31695, #14695, #60734, #36981, #26774, #21115, #8302, #9056, #55091, #3398, #15443, #61483, #26382, #72427, #9808, #32830, #50162, #21486, #65643, #67887, #27892, #68630, #51276, #74286, #34325, #22596, #33955, #21850, #56582, #39964, #62221, #56952, #45616, #16939, #22221, #62969, #4896, #10920, #28638, #38852, #5269, #50903, #73917, #10547, #51652, #11293, #39221, #57327, #11677, #5638, #22983, #61856, #39593, #68260, #45989, #45248, #62588, #28269, #15817, #56208, #33579, #67518, #16555, #69005, #44507, #10176, #33211, #27516, #4521, #50527, #73542, #44882, #16178, #8540, #20968, #43992, #10038, #72281, #32691, #37592, #20593, #67755, #38719, #50390, #37218, #43609, #60216, #73406, #55700, #37969, #31554, #9671, #72666, #54578, #3259, #50019, #67002, #15301, #27371, #73034, #67378, #61717, #15677, #31928, #14555, #38338, #44365, #61344, #9288, #4016, #33073, #66622, #27006, #60591, #14927, #2883, #56069, #21710, #25871, #60968, #48890, #44737, #21345, #32310, #71902, #4378, #20215, #43235, #26247, #66250, #8916, #54950, #49266, #55325, #3630, #26627, #49650, #34671, #5612, #40679, #45219, #22955, #51249, #68601, #28986, #16910, #22194, #63681, #46700, #52375, #39188, #27864, #33926, #11634, #4869, #50874, #74640, #40306, #74258, #73890, #22566, #63307, #68229, #57674, #16526, #52004, #39934, #56925, #45963, #57300, #62940, #39565, #62561, #10892, #712, #35039, #5240, #341, #28241, #68978, #45587, #5982, #23322, #11265, #34296, #17287, #28611, #51622, #46334, #69350, #69725, #17659, #56554, #12008, #58053, #6364, #29369, #23695, #62192, #10518, #33550, #30830, #64437, #53852, #8193, #35409, #64063, #47439, #24433, #13465, #7093, #19138, #31203, #12373, #1452, #65535, #1080, #18409, #70465, #24058, #47067, #2165, #42142, #58418, #12736, #65155, #54229, #36503, #70105, #30101, #59514, #41425, #71184, #18782, #35767, #25530, #7827, #58784, #25159, #2538, #48176, #53119, #41785, #19503, #64796, #42519, #13098, #36135, #48543, #13826, #41055, #59155, #70826, #7465, #30470, #18040, #6725, #53487, #1803, #36871, #24790, #59878, #47803, #29731, #52746, #71552, #26654, #37243, #60991, #42880, #49677, #8565, #54603, #14583, #67029, #10063, #14955, #66647, #15326, #37993, #73061, #2910, #55350, #8941, #26271, #61370, #49291, #25896, #21367, #4405, #33100, #19875, #60240, #66275, #44019, #31580, #48915, #32338, #72692, #31953, #71927, #54977 ) ),
 .UNSPECIFIED., .F., .F., .F. ) 
 B_SPLINE_SURFACE_WITH_KNOTS ( ( 2, 2 ),
 ( 3, 2, 2, 2, 2, 2, 2, 2, 2, 2, 2, 2, 2, 2, 2, 2, 2, 2, 2, 2, 2, 2, 2, 2, 2, 2, 2, 2, 2, 2, 2, 2, 2, 2, 2, 2, 2, 2, 2, 2, 2, 2, 2, 2, 2, 2, 2, 2, 2, 2, 2, 2, 2, 2, 2, 2, 2, 2, 2, 2, 2, 2, 2, 2, 2, 2, 2, 2, 2, 2, 2, 2, 2, 2, 2, 2, 2, 2, 2, 2, 2, 2, 2, 2, 2, 2, 2, 2, 2, 2, 2, 2, 2, 2, 2, 2, 2, 2, 2, 2, 2, 2, 2, 2, 2, 2, 2, 2, 2, 2, 2, 2, 2, 2, 2, 2, 2, 2, 2, 2, 2, 2, 2, 2, 2, 2, 2, 2, 2, 2, 2, 2, 2, 2, 2, 2, 2, 2, 2, 2, 2, 2, 2, 2, 2, 2, 2, 2, 2, 2, 2, 2, 2, 2, 2, 2, 2, 2, 2, 2, 2, 2, 2, 2, 2, 2, 2, 2, 2, 2, 2, 2, 2, 2, 2, 2, 2, 2, 2, 2, 2, 2, 2, 2, 2, 2, 2, 2, 2, 2, 2, 2, 2, 2, 2, 2, 2, 2, 2, 2, 2, 2, 2, 2, 2, 2, 2, 2, 2, 2, 2, 2, 2, 2, 2, 2, 2, 2, 2, 2, 2, 2, 2, 2, 2, 2, 2, 2, 2, 2, 2, 2, 2, 2, 2, 2, 2, 2, 2, 2, 2, 2, 2, 2, 2, 2, 2, 2, 2, 2, 2, 2, 2, 2, 2, 2, 2, 2, 2, 2, 2, 2, 2, 2, 2, 2, 2, 2, 2, 2, 2, 2, 2, 2, 2, 2, 2, 2, 2, 2, 2, 2, 2, 2, 2, 2, 2, 2, 2, 2, 2, 2, 2, 2, 2, 2, 2, 2, 2, 2, 2, 2, 2, 2, 2, 2, 2, 2, 2, 2, 2, 2, 2, 2, 2, 2, 2, 2, 2, 2, 2, 2, 2, 2, 2, 2, 2, 2, 2, 2, 2, 2, 2, 2, 2, 2, 2, 2, 2, 2, 2, 2, 2, 2, 2, 2, 2, 2, 2, 2, 2, 2, 2, 2, 2, 2, 2, 2, 2, 2, 2, 2, 2, 2, 2, 2, 2, 2, 2, 2, 2, 2, 2, 2, 2, 2, 2, 2, 2, 2, 2, 2, 2, 2, 2, 2, 2, 2, 2, 2, 2, 2, 2, 2, 2, 2, 2, 2, 2, 2, 2, 2, 2, 2, 2, 2, 2, 2, 2, 2, 2, 2, 2, 2, 2, 2, 2, 2, 2, 2, 2, 2, 2, 2, 2, 2, 2, 2, 2, 2, 2, 2, 2, 2, 2, 2, 2, 2, 2, 2, 2, 2, 2, 2, 2, 2, 2, 2, 2, 2, 2, 2, 2, 2, 2, 2, 2, 2, 2, 2, 2, 2, 2, 2, 2, 2, 2, 2, 2, 2, 2, 2, 2, 2, 2, 2, 2, 2, 2, 2, 2, 2, 2, 2, 2, 2, 2, 2, 2, 2, 2, 2, 2, 2, 2, 2, 2, 2, 2, 2, 2, 2, 2, 2, 2, 2, 2, 2, 2, 2, 2, 2, 2, 2, 2, 2, 2, 2, 2, 2, 2, 2, 2, 2, 2, 2, 2, 2, 2, 2, 2, 2, 2, 2, 2, 2, 2, 2, 2, 2, 2, 2, 2, 2, 3 ),
 ( 0.000000000000000000, 1.000000000000000000 ),
 ( 0.000000000000000000, 0.001811594202898550747, 0.003623188405797101493, 0.005434782608695652023, 0.007246376811594202987, 0.009057971014492753950, 0.01086956521739130405, 0.01268115942028985588, 0.01449275362318840597, 0.01630434782608695607, 0.01811594202898550790, 0.01992753623188405626, 0.02173913043478260809, 0.02355072463768115992, 0.02536231884057971175, 0.02717391304347826012, 0.02898550724637681195, 0.03079710144927536378, 0.03260869565217391214, 0.03442028985507246397, 0.03623188405797101580, 0.03804347826086956763, 0.03985507246376811252, 0.04166666666666666435, 0.04347826086956521618, 0.04528985507246376802, 0.04710144927536231985, 0.04891304347826087168, 0.05072463768115942351, 0.05253623188405796840, 0.05434782608695652023, 0.05615942028985507206, 0.05797101449275362389, 0.05978260869565217572, 0.06159420289855072755, 0.06340579710144927938, 0.06521739130434782428, 0.06702898550724638305, 0.06884057971014492794, 0.07065217391304347283, 0.07246376811594203160, 0.07427536231884057649, 0.07608695652173913526, 0.07789855072463768015, 0.07971014492753622505, 0.08152173913043478382, 0.08333333333333332871, 0.08514492753623188748, 0.08695652173913043237, 0.08876811594202899114, 0.09057971014492753603, 0.09239130434782608092, 0.09420289855072463969, 0.09601449275362318458, 0.09782608695652174335, 0.09963768115942028825, 0.1014492753623188470, 0.1032608695652173919, 0.1050724637681159368, 0.1068840579710144956, 0.1086956521739130405, 0.1105072463768115992, 0.1123188405797101441, 0.1141304347826086890, 0.1159420289855072478, 0.1177536231884057927, 0.1195652173913043514, 0.1213768115942028963, 0.1231884057971014551, 0.1250000000000000000, 0.1268115942028985588, 0.1286231884057970898, 0.1304347826086956486, 0.1322463768115942073, 0.1340579710144927661, 0.1358695652173912971, 0.1376811594202898559, 0.1394927536231884146, 0.1413043478260869457, 0.1431159420289855044, 0.1449275362318840632, 0.1467391304347826220, 0.1485507246376811530, 0.1503623188405797118, 0.1521739130434782705, 0.1539855072463768015, 0.1557971014492753603, 0.1576086956521739191, 0.1594202898550724501, 0.1612318840579710089, 0.1630434782608695676, 0.1648550724637681264, 0.1666666666666666574, 0.1684782608695652162, 0.1702898550724637750, 0.1721014492753623060, 0.1739130434782608647, 0.1757246376811594235, 0.1775362318840579823, 0.1793478260869565133, 0.1811594202898550721, 0.1829710144927536308, 0.1847826086956521618, 0.1865942028985507206, 0.1884057971014492794, 0.1902173913043478382, 0.1920289855072463692, 0.1938405797101449279, 0.1956521739130434867, 0.1974637681159420177, 0.1992753623188405765, 0.2010869565217391353, 0.2028985507246376940, 0.2047101449275362250, 0.2065217391304347838, 0.2083333333333333426, 0.2101449275362318736, 0.2119565217391304324, 0.2137681159420289911, 0.2155797101449275499, 0.2173913043478260809, 0.2192028985507246397, 0.2210144927536231985, 0.2228260869565217295, 0.2246376811594202882, 0.2264492753623188470, 0.2282608695652173780, 0.2300724637681159368, 0.2318840579710144956, 0.2336956521739130543, 0.2355072463768115854, 0.2373188405797101441, 0.2391304347826087029, 0.2409420289855072339, 0.2427536231884057927, 0.2445652173913043514, 0.2463768115942029102, 0.2481884057971014412, 0.2500000000000000000, 0.2518115942028985588, 0.2536231884057971175, 0.2554347826086956763, 0.2572463768115941796, 0.2590579710144927383, 0.2608695652173912971, 0.2626811594202898559, 0.2644927536231884146, 0.2663043478260869734, 0.2681159420289855322, 0.2699275362318840354, 0.2717391304347825942, 0.2735507246376811530, 0.2753623188405797118, 0.2771739130434782705, 0.2789855072463768293, 0.2807971014492753881, 0.2826086956521738913, 0.2844202898550724501, 0.2862318840579710089, 0.2880434782608695676, 0.2898550724637681264, 0.2916666666666666852, 0.2934782608695652439, 0.2952898550724637472, 0.2971014492753623060, 0.2989130434782608647, 0.3007246376811594235, 0.3025362318840579823, 0.3043478260869565410, 0.3061594202898550998, 0.3079710144927536031, 0.3097826086956521618, 0.3115942028985507206, 0.3134057971014492794, 0.3152173913043478382, 0.3170289855072463969, 0.3188405797101449002, 0.3206521739130434590, 0.3224637681159420177, 0.3242753623188405765, 0.3260869565217391353, 0.3278985507246376940, 0.3297101449275362528, 0.3315217391304347561, 0.3333333333333333148, 0.3351449275362318736, 0.3369565217391304324, 0.3387681159420289911, 0.3405797101449275499, 0.3423913043478261087, 0.3442028985507246119, 0.3460144927536231707, 0.3478260869565217295, 0.3496376811594202882, 0.3514492753623188470, 0.3532608695652174058, 0.3550724637681159646, 0.3568840579710144678, 0.3586956521739130266, 0.3605072463768115854, 0.3623188405797101441, 0.3641304347826087029, 0.3659420289855072617, 0.3677536231884058204, 0.3695652173913043237, 0.3713768115942028825, 0.3731884057971014412, 0.3750000000000000000, 0.3768115942028985588, 0.3786231884057971175, 0.3804347826086956763, 0.3822463768115941796, 0.3840579710144927383, 0.3858695652173912971, 0.3876811594202898559, 0.3894927536231884146, 0.3913043478260869734, 0.3931159420289855322, 0.3949275362318840354, 0.3967391304347825942, 0.3985507246376811530, 0.4003623188405797118, 0.4021739130434782705, 0.4039855072463768293, 0.4057971014492753881, 0.4076086956521738913, 0.4094202898550724501, 0.4112318840579710089, 0.4130434782608695676, 0.4148550724637681264, 0.4166666666666666852, 0.4184782608695652439, 0.4202898550724637472, 0.4221014492753623060, 0.4239130434782608647, 0.4257246376811594235, 0.4275362318840579823, 0.4293478260869565410, 0.4311594202898550998, 0.4329710144927536031, 0.4347826086956521618, 0.4365942028985507206, 0.4384057971014492794, 0.4402173913043478382, 0.4420289855072463969, 0.4438405797101449002, 0.4456521739130434590, 0.4474637681159420177, 0.4492753623188405765, 0.4510869565217391353, 0.4528985507246376940, 0.4547101449275362528, 0.4565217391304347561, 0.4583333333333333148, 0.4601449275362318736, 0.4619565217391304324, 0.4637681159420289911, 0.4655797101449275499, 0.4673913043478261087, 0.4692028985507246119, 0.4710144927536231707, 0.4728260869565217295, 0.4746376811594202882, 0.4764492753623188470, 0.4782608695652174058, 0.4800724637681159646, 0.4818840579710144678, 0.4836956521739130266, 0.4855072463768115854, 0.4873188405797101441, 0.4891304347826087029, 0.4909420289855072617, 0.4927536231884058204, 0.4945652173913043237, 0.4963768115942028825, 0.4981884057971014412, 0.5000000000000000000, 0.5018115942028985588, 0.5036231884057971175, 0.5054347826086956763, 0.5072463768115942351, 0.5090579710144927938, 0.5108695652173913526, 0.5126811594202898004, 0.5144927536231883591, 0.5163043478260869179, 0.5181159420289854767, 0.5199275362318840354, 0.5217391304347825942, 0.5235507246376811530, 0.5253623188405797118, 0.5271739130434782705, 0.5289855072463768293, 0.5307971014492753881, 0.5326086956521739468, 0.5344202898550725056, 0.5362318840579710644, 0.5380434782608695121, 0.5398550724637680709, 0.5416666666666666297, 0.5434782608695651884, 0.5452898550724637472, 0.5471014492753623060, 0.5489130434782608647, 0.5507246376811594235, 0.5525362318840579823, 0.5543478260869565410, 0.5561594202898550998, 0.5579710144927536586, 0.5597826086956522174, 0.5615942028985507761, 0.5634057971014492239, 0.5652173913043477826, 0.5670289855072463414, 0.5688405797101449002, 0.5706521739130434590, 0.5724637681159420177, 0.5742753623188405765, 0.5760869565217391353, 0.5778985507246376940, 0.5797101449275362528, 0.5815217391304348116, 0.5833333333333333703, 0.5851449275362319291, 0.5869565217391304879, 0.5887681159420289356, 0.5905797101449274944, 0.5923913043478260532, 0.5942028985507246119, 0.5960144927536231707, 0.5978260869565217295, 0.5996376811594202882, 0.6014492753623188470, 0.6032608695652174058, 0.6050724637681159646, 0.6068840579710145233, 0.6086956521739130821, 0.6105072463768116409, 0.6123188405797101996, 0.6141304347826086474, 0.6159420289855072062, 0.6177536231884057649, 0.6195652173913043237, 0.6213768115942028825, 0.6231884057971014412, 0.6250000000000000000, 0.6268115942028985588, 0.6286231884057971175, 0.6304347826086956763, 0.6322463768115942351, 0.6340579710144927938, 0.6358695652173913526, 0.6376811594202898004, 0.6394927536231883591, 0.6413043478260869179, 0.6431159420289854767, 0.6449275362318840354, 0.6467391304347825942, 0.6485507246376811530, 0.6503623188405797118, 0.6521739130434782705, 0.6539855072463768293, 0.6557971014492753881, 0.6576086956521739468, 0.6594202898550725056, 0.6612318840579710644, 0.6630434782608695121, 0.6648550724637680709, 0.6666666666666666297, 0.6684782608695651884, 0.6702898550724637472, 0.6721014492753623060, 0.6739130434782608647, 0.6757246376811594235, 0.6775362318840579823, 0.6793478260869565410, 0.6811594202898550998, 0.6829710144927536586, 0.6847826086956522174, 0.6865942028985507761, 0.6884057971014492239, 0.6902173913043477826, 0.6920289855072463414, 0.6938405797101449002, 0.6956521739130434590, 0.6974637681159420177, 0.6992753623188405765, 0.7010869565217391353, 0.7028985507246376940, 0.7047101449275362528, 0.7065217391304348116, 0.7083333333333333703, 0.7101449275362319291, 0.7119565217391304879, 0.7137681159420289356, 0.7155797101449274944, 0.7173913043478260532, 0.7192028985507246119, 0.7210144927536231707, 0.7228260869565217295, 0.7246376811594202882, 0.7264492753623188470, 0.7282608695652174058, 0.7300724637681159646, 0.7318840579710145233, 0.7336956521739130821, 0.7355072463768116409, 0.7373188405797101996, 0.7391304347826086474, 0.7409420289855072062, 0.7427536231884057649, 0.7445652173913043237, 0.7463768115942028825, 0.7481884057971014412, 0.7500000000000000000, 0.7518115942028985588, 0.7536231884057971175, 0.7554347826086956763, 0.7572463768115942351, 0.7590579710144927938, 0.7608695652173913526, 0.7626811594202898004, 0.7644927536231883591, 0.7663043478260869179, 0.7681159420289854767, 0.7699275362318840354, 0.7717391304347825942, 0.7735507246376811530, 0.7753623188405797118, 0.7771739130434782705, 0.7789855072463768293, 0.7807971014492753881, 0.7826086956521739468, 0.7844202898550725056, 0.7862318840579710644, 0.7880434782608695121, 0.7898550724637680709, 0.7916666666666666297, 0.7934782608695651884, 0.7952898550724637472, 0.7971014492753623060, 0.7989130434782608647, 0.8007246376811594235, 0.8025362318840579823, 0.8043478260869565410, 0.8061594202898550998, 0.8079710144927536586, 0.8097826086956522174, 0.8115942028985507761, 0.8134057971014492239, 0.8152173913043477826, 0.8170289855072463414, 0.8188405797101449002, 0.8206521739130434590, 0.8224637681159420177, 0.8242753623188405765, 0.8260869565217391353, 0.8278985507246376940, 0.8297101449275362528, 0.8315217391304348116, 0.8333333333333333703, 0.8351449275362319291, 0.8369565217391304879, 0.8387681159420289356, 0.8405797101449274944, 0.8423913043478260532, 0.8442028985507246119, 0.8460144927536231707, 0.8478260869565217295, 0.8496376811594202882, 0.8514492753623188470, 0.8532608695652174058, 0.8550724637681159646, 0.8568840579710145233, 0.8586956521739130821, 0.8605072463768116409, 0.8623188405797101996, 0.8641304347826086474, 0.8659420289855072062, 0.8677536231884057649, 0.8695652173913043237, 0.8713768115942028825, 0.8731884057971014412, 0.8750000000000000000, 0.8768115942028985588, 0.8786231884057971175, 0.8804347826086956763, 0.8822463768115942351, 0.8840579710144927938, 0.8858695652173913526, 0.8876811594202898004, 0.8894927536231883591, 0.8913043478260869179, 0.8931159420289854767, 0.8949275362318840354, 0.8967391304347825942, 0.8985507246376811530, 0.9003623188405797118, 0.9021739130434782705, 0.9039855072463768293, 0.9057971014492753881, 0.9076086956521739468, 0.9094202898550725056, 0.9112318840579710644, 0.9130434782608695121, 0.9148550724637680709, 0.9166666666666666297, 0.9184782608695651884, 0.9202898550724637472, 0.9221014492753623060, 0.9239130434782608647, 0.9257246376811594235, 0.9275362318840579823, 0.9293478260869565410, 0.9311594202898550998, 0.9329710144927536586, 0.9347826086956522174, 0.9365942028985507761, 0.9384057971014492239, 0.9402173913043477826, 0.9420289855072463414, 0.9438405797101449002, 0.9456521739130434590, 0.9474637681159420177, 0.9492753623188405765, 0.9510869565217391353, 0.9528985507246376940, 0.9547101449275362528, 0.9565217391304348116, 0.9583333333333333703, 0.9601449275362319291, 0.9619565217391304879, 0.9637681159420289356, 0.9655797101449274944, 0.9673913043478260532, 0.9692028985507246119, 0.9710144927536231707, 0.9728260869565217295, 0.9746376811594202882, 0.9764492753623188470, 0.9782608695652174058, 0.9800724637681159646, 0.9818840579710145233, 0.9826096998908593338, 0.9924357968897679072 ),
 .UNSPECIFIED. ) 
 GEOMETRIC_REPRESENTATION_ITEM ( )  RATIONAL_B_SPLINE_SURFACE ( (
 ( 1.000000000000000000, 0.9659258262890683122, 1.000000000000000000, 0.9659258262890683122, 1.000000000000000000, 0.9659258262890683122, 1.000000000000000000, 0.9659258262890683122, 1.000000000000000000, 0.9659258262890683122, 1.000000000000000000, 0.9659258262890683122, 1.000000000000000000, 0.9659258262890683122, 1.000000000000000000, 0.9659258262890683122, 1.000000000000000000, 0.9659258262890683122, 1.000000000000000000, 0.9659258262890683122, 1.000000000000000000, 0.9659258262890683122, 1.000000000000000000, 0.9659258262890683122, 1.000000000000000000, 0.9659258262890683122, 1.000000000000000000, 0.9659258262890683122, 1.000000000000000000, 0.9659258262890683122, 1.000000000000000000, 0.9659258262890683122, 1.000000000000000000, 0.9659258262890683122, 1.000000000000000000, 0.9659258262890683122, 1.000000000000000000, 0.9659258262890683122, 1.000000000000000000, 0.9659258262890683122, 1.000000000000000000, 0.9659258262890683122, 1.000000000000000000, 0.9659258262890683122, 1.000000000000000000, 0.9659258262890683122, 1.000000000000000000, 0.9659258262890683122, 1.000000000000000000, 0.9659258262890683122, 1.000000000000000000, 0.9659258262890683122, 1.000000000000000000, 0.9659258262890683122, 1.000000000000000000, 0.9659258262890683122, 1.000000000000000000, 0.9659258262890683122, 1.000000000000000000, 0.9659258262890683122, 1.000000000000000000, 0.9659258262890683122, 1.000000000000000000, 0.9659258262890683122, 1.000000000000000000, 0.9659258262890683122, 1.000000000000000000, 0.9659258262890683122, 1.000000000000000000, 0.9659258262890683122, 1.000000000000000000, 0.9659258262890683122, 1.000000000000000000, 0.9659258262890683122, 1.000000000000000000, 0.9659258262890683122, 1.000000000000000000, 0.9659258262890683122, 1.000000000000000000, 0.9659258262890683122, 1.000000000000000000, 0.9659258262890683122, 1.000000000000000000, 0.9659258262890683122, 1.000000000000000000, 0.9659258262890683122, 1.000000000000000000, 0.9659258262890683122, 1.000000000000000000, 0.9659258262890683122, 1.000000000000000000, 0.9659258262890683122, 1.000000000000000000, 0.9659258262890683122, 1.000000000000000000, 0.9659258262890683122, 1.000000000000000000, 0.9659258262890683122, 1.000000000000000000, 0.9659258262890683122, 1.000000000000000000, 0.9659258262890683122, 1.000000000000000000, 0.9659258262890683122, 1.000000000000000000, 0.9659258262890683122, 1.000000000000000000, 0.9659258262890683122, 1.000000000000000000, 0.9659258262890683122, 1.000000000000000000, 0.9659258262890683122, 1.000000000000000000, 0.9659258262890683122, 1.000000000000000000, 0.9659258262890683122, 1.000000000000000000, 0.9659258262890683122, 1.000000000000000000, 0.9659258262890683122, 1.000000000000000000, 0.9659258262890683122, 1.000000000000000000, 0.9659258262890683122, 1.000000000000000000, 0.9659258262890683122, 1.000000000000000000, 0.9659258262890683122, 1.000000000000000000, 0.9659258262890683122, 1.000000000000000000, 0.9659258262890683122, 1.000000000000000000, 0.9659258262890683122, 1.000000000000000000, 0.9659258262890683122, 1.000000000000000000, 0.9659258262890683122, 1.000000000000000000, 0.9659258262890683122, 1.000000000000000000, 0.9659258262890683122, 1.000000000000000000, 0.9659258262890683122, 1.000000000000000000, 0.9659258262890683122, 1.000000000000000000, 0.9659258262890683122, 1.000000000000000000, 0.9659258262890683122, 1.000000000000000000, 0.9659258262890683122, 1.000000000000000000, 0.9659258262890683122, 1.000000000000000000, 0.9659258262890683122, 1.000000000000000000, 0.9659258262890683122, 1.000000000000000000, 0.9659258262890683122, 1.000000000000000000, 0.9659258262890683122, 1.000000000000000000, 0.9659258262890683122, 1.000000000000000000, 0.9659258262890683122, 1.000000000000000000, 0.9659258262890683122, 1.000000000000000000, 0.9659258262890683122, 1.000000000000000000, 0.9659258262890683122, 1.000000000000000000, 0.9659258262890683122, 1.000000000000000000, 0.9659258262890683122, 1.000000000000000000, 0.9659258262890683122, 1.000000000000000000, 0.9659258262890683122, 1.000000000000000000, 0.9659258262890683122, 1.000000000000000000, 0.9659258262890683122, 1.000000000000000000, 0.9659258262890683122, 1.000000000000000000, 0.9659258262890683122, 1.000000000000000000, 0.9659258262890683122, 1.000000000000000000, 0.9659258262890683122, 1.000000000000000000, 0.9659258262890683122, 1.000000000000000000, 0.9659258262890683122, 1.000000000000000000, 0.9659258262890683122, 1.000000000000000000, 0.9659258262890683122, 1.000000000000000000, 0.9659258262890683122, 1.000000000000000000, 0.9659258262890683122, 1.000000000000000000, 0.9659258262890683122, 1.000000000000000000, 0.9659258262890683122, 1.000000000000000000, 0.9659258262890683122, 1.000000000000000000, 0.9659258262890683122, 1.000000000000000000, 0.9659258262890683122, 1.000000000000000000, 0.9659258262890683122, 1.000000000000000000, 0.9659258262890683122, 1.000000000000000000, 0.9659258262890683122, 1.000000000000000000, 0.9659258262890683122, 1.000000000000000000, 0.9659258262890683122, 1.000000000000000000, 0.9659258262890683122, 1.000000000000000000, 0.9659258262890683122, 1.000000000000000000, 0.9659258262890683122, 1.000000000000000000, 0.9659258262890683122, 1.000000000000000000, 0.9659258262890683122, 1.000000000000000000, 0.9659258262890683122, 1.000000000000000000, 0.9659258262890683122, 1.000000000000000000, 0.9659258262890683122, 1.000000000000000000, 0.9659258262890683122, 1.000000000000000000, 0.9659258262890683122, 1.000000000000000000, 0.9659258262890683122, 1.000000000000000000, 0.9659258262890683122, 1.000000000000000000, 0.9659258262890683122, 1.000000000000000000, 0.9659258262890683122, 1.000000000000000000, 0.9659258262890683122, 1.000000000000000000, 0.9659258262890683122, 1.000000000000000000, 0.9659258262890683122, 1.000000000000000000, 0.9659258262890683122, 1.000000000000000000, 0.9659258262890683122, 1.000000000000000000, 0.9659258262890683122, 1.000000000000000000, 0.9659258262890683122, 1.000000000000000000, 0.9659258262890683122, 1.000000000000000000, 0.9659258262890683122, 1.000000000000000000, 0.9659258262890683122, 1.000000000000000000, 0.9659258262890683122, 1.000000000000000000, 0.9659258262890683122, 1.000000000000000000, 0.9659258262890683122, 1.000000000000000000, 0.9659258262890683122, 1.000000000000000000, 0.9659258262890683122, 1.000000000000000000, 0.9659258262890683122, 1.000000000000000000, 0.9659258262890683122, 1.000000000000000000, 0.9659258262890683122, 1.000000000000000000, 0.9659258262890683122, 1.000000000000000000, 0.9659258262890683122, 1.000000000000000000, 0.9659258262890683122, 1.000000000000000000, 0.9659258262890683122, 1.000000000000000000, 0.9659258262890683122, 1.000000000000000000, 0.9659258262890683122, 1.000000000000000000, 0.9659258262890683122, 1.000000000000000000, 0.9659258262890683122, 1.000000000000000000, 0.9659258262890683122, 1.000000000000000000, 0.9659258262890683122, 1.000000000000000000, 0.9659258262890683122, 1.000000000000000000, 0.9659258262890683122, 1.000000000000000000, 0.9659258262890683122, 1.000000000000000000, 0.9659258262890683122, 1.000000000000000000, 0.9659258262890683122, 1.000000000000000000, 0.9659258262890683122, 1.000000000000000000, 0.9659258262890683122, 1.000000000000000000, 0.9659258262890683122, 1.000000000000000000, 0.9659258262890683122, 1.000000000000000000, 0.9659258262890683122, 1.000000000000000000, 0.9659258262890683122, 1.000000000000000000, 0.9659258262890683122, 1.000000000000000000, 0.9659258262890683122, 1.000000000000000000, 0.9659258262890683122, 1.000000000000000000, 0.9659258262890683122, 1.000000000000000000, 0.9659258262890683122, 1.000000000000000000, 0.9659258262890683122, 1.000000000000000000, 0.9659258262890683122, 1.000000000000000000, 0.9659258262890683122, 1.000000000000000000, 0.9659258262890683122, 1.000000000000000000, 0.9659258262890683122, 1.000000000000000000, 0.9659258262890683122, 1.000000000000000000, 0.9659258262890683122, 1.000000000000000000, 0.9659258262890683122, 1.000000000000000000, 0.9659258262890683122, 1.000000000000000000, 0.9659258262890683122, 1.000000000000000000, 0.9659258262890683122, 1.000000000000000000, 0.9659258262890683122, 1.000000000000000000, 0.9659258262890683122, 1.000000000000000000, 0.9659258262890683122, 1.000000000000000000, 0.9659258262890683122, 1.000000000000000000, 0.9659258262890683122, 1.000000000000000000, 0.9659258262890683122, 1.000000000000000000, 0.9659258262890683122, 1.000000000000000000, 0.9659258262890683122, 1.000000000000000000, 0.9659258262890683122, 1.000000000000000000, 0.9659258262890683122, 1.000000000000000000, 0.9659258262890683122, 1.000000000000000000, 0.9659258262890683122, 1.000000000000000000, 0.9659258262890683122, 1.000000000000000000, 0.9659258262890683122, 1.000000000000000000, 0.9659258262890683122, 1.000000000000000000, 0.9659258262890683122, 1.000000000000000000, 0.9659258262890683122, 1.000000000000000000, 0.9659258262890683122, 1.000000000000000000, 0.9659258262890683122, 1.000000000000000000, 0.9659258262890683122, 1.000000000000000000, 0.9659258262890683122, 1.000000000000000000, 0.9659258262890683122, 1.000000000000000000, 0.9659258262890683122, 1.000000000000000000, 0.9659258262890683122, 1.000000000000000000, 0.9659258262890683122, 1.000000000000000000, 0.9659258262890683122, 1.000000000000000000, 0.9659258262890683122, 1.000000000000000000, 0.9659258262890683122, 1.000000000000000000, 0.9659258262890683122, 1.000000000000000000, 0.9659258262890683122, 1.000000000000000000, 0.9659258262890683122, 1.000000000000000000, 0.9659258262890683122, 1.000000000000000000, 0.9659258262890683122, 1.000000000000000000, 0.9659258262890683122, 1.000000000000000000, 0.9659258262890683122, 1.000000000000000000, 0.9659258262890683122, 1.000000000000000000, 0.9659258262890683122, 1.000000000000000000, 0.9659258262890683122, 1.000000000000000000, 0.9659258262890683122, 1.000000000000000000, 0.9659258262890683122, 1.000000000000000000, 0.9659258262890683122, 1.000000000000000000, 0.9659258262890683122, 1.000000000000000000, 0.9659258262890683122, 1.000000000000000000, 0.9659258262890683122, 1.000000000000000000, 0.9659258262890683122, 1.000000000000000000, 0.9659258262890683122, 1.000000000000000000, 0.9659258262890683122, 1.000000000000000000, 0.9659258262890683122, 1.000000000000000000, 0.9659258262890683122, 1.000000000000000000, 0.9659258262890683122, 1.000000000000000000, 0.9659258262890683122, 1.000000000000000000, 0.9659258262890683122, 1.000000000000000000, 0.9659258262890683122, 1.000000000000000000, 0.9659258262890683122, 1.000000000000000000, 0.9659258262890683122, 1.000000000000000000, 0.9659258262890683122, 1.000000000000000000, 0.9659258262890683122, 1.000000000000000000, 0.9659258262890683122, 1.000000000000000000, 0.9659258262890683122, 1.000000000000000000, 0.9659258262890683122, 1.000000000000000000, 0.9659258262890683122, 1.000000000000000000, 0.9659258262890683122, 1.000000000000000000, 0.9659258262890683122, 1.000000000000000000, 0.9659258262890683122, 1.000000000000000000, 0.9659258262890683122, 1.000000000000000000, 0.9659258262890683122, 1.000000000000000000, 0.9659258262890683122, 1.000000000000000000, 0.9659258262890683122, 1.000000000000000000, 0.9659258262890683122, 1.000000000000000000, 0.9659258262890683122, 1.000000000000000000, 0.9659258262890683122, 1.000000000000000000, 0.9659258262890683122, 1.000000000000000000, 0.9659258262890683122, 1.000000000000000000, 0.9659258262890683122, 1.000000000000000000, 0.9659258262890683122, 1.000000000000000000, 0.9659258262890683122, 1.000000000000000000, 0.9659258262890683122, 1.000000000000000000, 0.9659258262890683122, 1.000000000000000000, 0.9659258262890683122, 1.000000000000000000, 0.9659258262890683122, 1.000000000000000000, 0.9659258262890683122, 1.000000000000000000, 0.9659258262890683122, 1.000000000000000000, 0.9659258262890683122, 1.000000000000000000, 0.9659258262890683122, 1.000000000000000000, 0.9659258262890683122, 1.000000000000000000, 0.9659258262890683122, 1.000000000000000000, 0.9659258262890683122, 1.000000000000000000, 0.9659258262890683122, 1.000000000000000000, 0.9659258262890683122, 1.000000000000000000, 0.9659258262890683122, 1.000000000000000000, 0.9659258262890683122, 1.000000000000000000, 0.9659258262890683122, 1.000000000000000000, 0.9659258262890683122, 1.000000000000000000, 0.9659258262890683122, 1.000000000000000000, 0.9659258262890683122, 1.000000000000000000, 0.9659258262890683122, 1.000000000000000000, 0.9659258262890683122, 1.000000000000000000, 0.9659258262890683122, 1.000000000000000000, 0.9659258262890683122, 1.000000000000000000, 0.9659258262890683122, 1.000000000000000000, 0.9659258262890683122, 1.000000000000000000, 0.9659258262890683122, 1.000000000000000000, 0.9659258262890683122, 1.000000000000000000, 0.9659258262890683122, 1.000000000000000000, 0.9659258262890683122, 1.000000000000000000, 0.9659258262890683122, 1.000000000000000000, 0.9659258262890683122, 1.000000000000000000, 0.9659258262890683122, 1.000000000000000000, 0.9659258262890683122, 1.000000000000000000, 0.9659258262890683122, 1.000000000000000000, 0.9659258262890683122, 1.000000000000000000, 0.9659258262890683122, 1.000000000000000000, 0.9659258262890683122, 1.000000000000000000, 0.9659258262890683122, 1.000000000000000000, 0.9659258262890683122, 1.000000000000000000, 0.9659258262890683122, 1.000000000000000000, 0.9659258262890683122, 1.000000000000000000, 0.9659258262890683122, 1.000000000000000000, 0.9659258262890683122, 1.000000000000000000, 0.9659258262890683122, 1.000000000000000000, 0.9659258262890683122, 1.000000000000000000, 0.9659258262890683122, 1.000000000000000000, 0.9659258262890683122, 1.000000000000000000, 0.9659258262890683122, 1.000000000000000000, 0.9659258262890683122, 1.000000000000000000, 0.9659258262890683122, 1.000000000000000000, 0.9659258262890683122, 1.000000000000000000, 0.9659258262890683122, 1.000000000000000000, 0.9659258262890683122, 1.000000000000000000, 0.9659258262890683122, 1.000000000000000000, 0.9659258262890683122, 1.000000000000000000, 0.9659258262890683122, 1.000000000000000000, 0.9659258262890683122, 1.000000000000000000, 0.9659258262890683122, 1.000000000000000000, 0.9659258262890683122, 1.000000000000000000, 0.9659258262890683122, 1.000000000000000000, 0.9659258262890683122, 1.000000000000000000, 0.9659258262890683122, 1.000000000000000000, 0.9659258262890683122, 1.000000000000000000, 0.9659258262890683122, 1.000000000000000000, 0.9659258262890683122, 1.000000000000000000, 0.9659258262890683122, 1.000000000000000000, 0.9659258262890683122, 1.000000000000000000, 0.9659258262890683122, 1.000000000000000000, 0.9659258262890683122, 1.000000000000000000, 0.9659258262890683122, 1.000000000000000000, 0.9659258262890683122, 1.000000000000000000, 0.9659258262890683122, 1.000000000000000000, 0.9659258262890683122, 1.000000000000000000, 0.9659258262890683122, 1.000000000000000000, 0.9659258262890683122, 1.000000000000000000, 0.9659258262890683122, 1.000000000000000000, 0.9659258262890683122, 1.000000000000000000, 0.9659258262890683122, 1.000000000000000000, 0.9659258262890683122, 1.000000000000000000, 0.9659258262890683122, 1.000000000000000000, 0.9659258262890683122, 1.000000000000000000, 0.9659258262890683122, 1.000000000000000000, 0.9659258262890683122, 1.000000000000000000, 0.9659258262890683122, 1.000000000000000000, 0.9659258262890683122, 1.000000000000000000, 0.9659258262890683122, 1.000000000000000000, 0.9659258262890683122, 1.000000000000000000, 0.9659258262890683122, 1.000000000000000000, 0.9659258262890683122, 1.000000000000000000, 0.9659258262890683122, 1.000000000000000000, 0.9659258262890683122, 1.000000000000000000, 0.9659258262890683122, 1.000000000000000000, 0.9659258262890683122, 1.000000000000000000, 0.9659258262890683122, 1.000000000000000000, 0.9659258262890683122, 1.000000000000000000, 0.9659258262890683122, 1.000000000000000000, 0.9659258262890683122, 1.000000000000000000, 0.9659258262890683122, 1.000000000000000000, 0.9659258262890683122, 1.000000000000000000, 0.9659258262890683122, 1.000000000000000000, 0.9659258262890683122, 1.000000000000000000, 0.9659258262890683122, 1.000000000000000000, 0.9659258262890683122, 1.000000000000000000, 0.9659258262890683122, 1.000000000000000000, 0.9659258262890683122, 1.000000000000000000, 0.9659258262890683122, 1.000000000000000000, 0.9659258262890683122, 1.000000000000000000, 0.9659258262890683122, 1.000000000000000000, 0.9659258262890683122, 1.000000000000000000, 0.9659258262890683122, 1.000000000000000000, 0.9659258262890683122, 1.000000000000000000, 0.9659258262890683122, 1.000000000000000000, 0.9659258262890683122, 1.000000000000000000, 0.9659258262890683122, 1.000000000000000000, 0.9659258262890683122, 1.000000000000000000, 0.9659258262890683122, 1.000000000000000000, 0.9659258262890683122, 1.000000000000000000, 0.9659258262890683122, 1.000000000000000000, 0.9659258262890683122, 1.000000000000000000, 0.9659258262890683122, 1.000000000000000000, 0.9659258262890683122, 1.000000000000000000, 0.9659258262890683122, 1.000000000000000000, 0.9659258262890683122, 1.000000000000000000, 0.9659258262890683122, 1.000000000000000000, 0.9659258262890683122, 1.000000000000000000, 0.9659258262890683122, 1.000000000000000000, 0.9659258262890683122, 1.000000000000000000, 0.9659258262890683122, 1.000000000000000000, 0.9659258262890683122, 1.000000000000000000, 0.9659258262890683122, 1.000000000000000000, 0.9659258262890683122, 1.000000000000000000, 0.9659258262890683122, 1.000000000000000000, 0.9659258262890683122, 1.000000000000000000, 0.9659258262890683122, 1.000000000000000000, 0.9659258262890683122, 1.000000000000000000, 0.9659258262890683122, 1.000000000000000000, 0.9659258262890683122, 1.000000000000000000, 0.9659258262890683122, 1.000000000000000000, 0.9659258262890683122, 1.000000000000000000, 0.9659258262890683122, 1.000000000000000000, 0.9659258262890683122, 1.000000000000000000, 0.9659258262890683122, 1.000000000000000000, 0.9659258262890683122, 1.000000000000000000, 0.9659258262890683122, 1.000000000000000000, 0.9659258262890683122, 1.000000000000000000, 0.9659258262890683122, 1.000000000000000000, 0.9659258262890683122, 1.000000000000000000, 0.9659258262890683122, 1.000000000000000000, 0.9659258262890683122, 1.000000000000000000, 0.9659258262890683122, 1.000000000000000000, 0.9659258262890683122, 1.000000000000000000, 0.9659258262890683122, 1.000000000000000000, 0.9659258262890683122, 1.000000000000000000, 0.9659258262890683122, 1.000000000000000000, 0.9659258262890683122, 1.000000000000000000, 0.9659258262890683122, 1.000000000000000000, 0.9659258262890683122, 1.000000000000000000, 0.9659258262890683122, 1.000000000000000000, 0.9659258262890683122, 1.000000000000000000, 0.9659258262890683122, 1.000000000000000000, 0.9659258262890683122, 1.000000000000000000, 0.9659258262890683122, 1.000000000000000000, 0.9659258262890683122, 1.000000000000000000, 0.9659258262890683122, 1.000000000000000000, 0.9659258262890683122, 1.000000000000000000, 0.9659258262890683122, 1.000000000000000000, 0.9659258262890683122, 1.000000000000000000, 0.9659258262890683122, 1.000000000000000000, 0.9659258262890683122, 1.000000000000000000, 0.9659258262890683122, 1.000000000000000000, 0.9659258262890683122, 1.000000000000000000, 0.9659258262890683122, 1.000000000000000000, 0.9659258262890683122, 1.000000000000000000, 0.9659258262890683122, 1.000000000000000000, 0.9659258262890683122, 1.000000000000000000, 0.9659258262890683122, 1.000000000000000000, 0.9659258262890683122, 1.000000000000000000, 0.9659258262890683122, 1.000000000000000000, 0.9659258262890683122, 1.000000000000000000, 0.9659258262890683122, 1.000000000000000000, 0.9659258262890683122, 1.000000000000000000, 0.9659258262890683122, 1.000000000000000000, 0.9659258262890683122, 1.000000000000000000, 0.9659258262890683122, 1.000000000000000000, 0.9659258262890683122, 1.000000000000000000, 0.9659258262890683122, 1.000000000000000000, 0.9659258262890683122, 1.000000000000000000, 0.9659258262890683122, 1.000000000000000000, 0.9659258262890683122, 1.000000000000000000, 0.9659258262890683122, 1.000000000000000000, 0.9659258262890683122, 1.000000000000000000, 0.9659258262890683122, 1.000000000000000000, 0.9659258262890683122, 1.000000000000000000, 0.9659258262890683122, 1.000000000000000000, 0.9659258262890683122, 1.000000000000000000, 0.9659258262890683122, 1.000000000000000000, 0.9659258262890683122, 1.000000000000000000, 0.9659258262890683122, 1.000000000000000000, 0.9659258262890683122, 1.000000000000000000, 0.9659258262890683122, 1.000000000000000000, 0.9659258262890683122, 1.000000000000000000, 0.9659258262890683122, 1.000000000000000000, 0.9659258262890683122, 1.000000000000000000, 0.9659258262890683122, 1.000000000000000000, 0.9659258262890683122, 1.000000000000000000, 0.9659258262890683122, 1.000000000000000000, 0.9659258262890683122, 1.000000000000000000, 0.9659258262890683122, 1.000000000000000000, 0.9659258262890683122, 1.000000000000000000, 0.9659258262890683122, 1.000000000000000000, 0.9659258262890683122, 1.000000000000000000, 0.9659258262890683122, 1.000000000000000000, 0.9659258262890683122, 1.000000000000000000, 0.9659258262890683122, 1.000000000000000000, 0.9659258262890683122, 1.000000000000000000, 0.9659258262890683122, 1.000000000000000000, 0.9659258262890683122, 1.000000000000000000, 0.9659258262890683122, 1.000000000000000000, 0.9659258262890683122, 1.000000000000000000, 0.9659258262890683122, 1.000000000000000000, 0.9659258262890683122, 1.000000000000000000, 0.9659258262890683122, 1.000000000000000000, 0.9659258262890683122, 1.000000000000000000, 0.9659258262890683122, 1.000000000000000000, 0.9659258262890683122, 1.000000000000000000, 0.9659258262890683122, 1.000000000000000000, 0.9659258262890683122, 1.000000000000000000, 0.9659258262890683122, 1.000000000000000000, 0.9659258262890683122, 1.000000000000000000, 0.9659258262890683122, 1.000000000000000000, 0.9659258262890683122, 1.000000000000000000, 0.9659258262890683122, 1.000000000000000000, 0.9659258262890683122, 1.000000000000000000, 0.9659258262890683122, 1.000000000000000000, 0.9659258262890683122, 1.000000000000000000, 0.9659258262890683122, 1.000000000000000000, 0.9659258262890683122, 1.000000000000000000, 0.9659258262890683122, 1.000000000000000000, 0.9659258262890683122, 1.000000000000000000, 0.9659258262890683122, 1.000000000000000000, 0.9659258262890683122, 1.000000000000000000, 0.9659258262890683122, 1.000000000000000000, 0.9659258262890683122, 1.000000000000000000, 0.9659258262890683122, 1.000000000000000000, 0.9659258262890683122, 1.000000000000000000, 0.9659258262890683122, 1.000000000000000000, 0.9659258262890683122, 1.000000000000000000, 0.9659258262890683122, 1.000000000000000000, 0.9659258262890683122, 1.000000000000000000, 0.9659258262890683122, 1.000000000000000000, 0.9659258262890683122, 1.000000000000000000, 0.9659258262890683122, 1.000000000000000000, 0.9659258262890683122, 1.000000000000000000, 0.9659258262890683122, 1.000000000000000000, 0.9659258262890683122, 1.000000000000000000, 0.9659258262890683122, 1.000000000000000000, 0.9659258262890683122, 1.000000000000000000, 0.9659258262890683122, 1.000000000000000000, 0.9659258262890683122, 1.000000000000000000, 0.9659258262890683122, 1.000000000000000000, 0.9659258262890683122, 1.000000000000000000, 0.9659258262890683122, 1.000000000000000000, 0.9659258262890683122, 1.000000000000000000, 0.9659258262890683122, 1.000000000000000000, 0.9659258262890683122, 1.000000000000000000, 0.9659258262890683122, 1.000000000000000000, 0.9659258262890683122, 1.000000000000000000, 0.9659258262890683122, 1.000000000000000000, 0.9659258262890683122, 1.000000000000000000, 0.9659258262890683122, 1.000000000000000000, 0.9659258262890683122, 1.000000000000000000, 0.9659258262890683122, 1.000000000000000000, 0.9659258262890683122, 1.000000000000000000, 0.9659258262890683122, 1.000000000000000000, 0.9659258262890683122, 1.000000000000000000, 0.9659258262890683122, 1.000000000000000000, 0.9659258262890683122, 1.000000000000000000, 0.9659258262890683122, 1.000000000000000000, 0.9659258262890683122, 1.000000000000000000, 0.9659258262890683122, 1.000000000000000000, 0.9659258262890683122, 1.000000000000000000, 0.9659258262890683122, 1.000000000000000000, 0.9659258262890683122, 1.000000000000000000, 0.9659258262890683122, 1.000000000000000000, 0.9659258262890683122, 1.000000000000000000, 0.9863514418465433309, 0.9836368620925994843, 0.9836368620925994843, 0.9836368620925994843),
 ( 1.000000000000000000, 0.9659258262890683122, 1.000000000000000000, 0.9659258262890683122, 1.000000000000000000, 0.9659258262890683122, 1.000000000000000000, 0.9659258262890683122, 1.000000000000000000, 0.9659258262890683122, 1.000000000000000000, 0.9659258262890683122, 1.000000000000000000, 0.9659258262890683122, 1.000000000000000000, 0.9659258262890683122, 1.000000000000000000, 0.9659258262890683122, 1.000000000000000000, 0.9659258262890683122, 1.000000000000000000, 0.9659258262890683122, 1.000000000000000000, 0.9659258262890683122, 1.000000000000000000, 0.9659258262890683122, 1.000000000000000000, 0.9659258262890683122, 1.000000000000000000, 0.9659258262890683122, 1.000000000000000000, 0.9659258262890683122, 1.000000000000000000, 0.9659258262890683122, 1.000000000000000000, 0.9659258262890683122, 1.000000000000000000, 0.9659258262890683122, 1.000000000000000000, 0.9659258262890683122, 1.000000000000000000, 0.9659258262890683122, 1.000000000000000000, 0.9659258262890683122, 1.000000000000000000, 0.9659258262890683122, 1.000000000000000000, 0.9659258262890683122, 1.000000000000000000, 0.9659258262890683122, 1.000000000000000000, 0.9659258262890683122, 1.000000000000000000, 0.9659258262890683122, 1.000000000000000000, 0.9659258262890683122, 1.000000000000000000, 0.9659258262890683122, 1.000000000000000000, 0.9659258262890683122, 1.000000000000000000, 0.9659258262890683122, 1.000000000000000000, 0.9659258262890683122, 1.000000000000000000, 0.9659258262890683122, 1.000000000000000000, 0.9659258262890683122, 1.000000000000000000, 0.9659258262890683122, 1.000000000000000000, 0.9659258262890683122, 1.000000000000000000, 0.9659258262890683122, 1.000000000000000000, 0.9659258262890683122, 1.000000000000000000, 0.9659258262890683122, 1.000000000000000000, 0.9659258262890683122, 1.000000000000000000, 0.9659258262890683122, 1.000000000000000000, 0.9659258262890683122, 1.000000000000000000, 0.9659258262890683122, 1.000000000000000000, 0.9659258262890683122, 1.000000000000000000, 0.9659258262890683122, 1.000000000000000000, 0.9659258262890683122, 1.000000000000000000, 0.9659258262890683122, 1.000000000000000000, 0.9659258262890683122, 1.000000000000000000, 0.9659258262890683122, 1.000000000000000000, 0.9659258262890683122, 1.000000000000000000, 0.9659258262890683122, 1.000000000000000000, 0.9659258262890683122, 1.000000000000000000, 0.9659258262890683122, 1.000000000000000000, 0.9659258262890683122, 1.000000000000000000, 0.9659258262890683122, 1.000000000000000000, 0.9659258262890683122, 1.000000000000000000, 0.9659258262890683122, 1.000000000000000000, 0.9659258262890683122, 1.000000000000000000, 0.9659258262890683122, 1.000000000000000000, 0.9659258262890683122, 1.000000000000000000, 0.9659258262890683122, 1.000000000000000000, 0.9659258262890683122, 1.000000000000000000, 0.9659258262890683122, 1.000000000000000000, 0.9659258262890683122, 1.000000000000000000, 0.9659258262890683122, 1.000000000000000000, 0.9659258262890683122, 1.000000000000000000, 0.9659258262890683122, 1.000000000000000000, 0.9659258262890683122, 1.000000000000000000, 0.9659258262890683122, 1.000000000000000000, 0.9659258262890683122, 1.000000000000000000, 0.9659258262890683122, 1.000000000000000000, 0.9659258262890683122, 1.000000000000000000, 0.9659258262890683122, 1.000000000000000000, 0.9659258262890683122, 1.000000000000000000, 0.9659258262890683122, 1.000000000000000000, 0.9659258262890683122, 1.000000000000000000, 0.9659258262890683122, 1.000000000000000000, 0.9659258262890683122, 1.000000000000000000, 0.9659258262890683122, 1.000000000000000000, 0.9659258262890683122, 1.000000000000000000, 0.9659258262890683122, 1.000000000000000000, 0.9659258262890683122, 1.000000000000000000, 0.9659258262890683122, 1.000000000000000000, 0.9659258262890683122, 1.000000000000000000, 0.9659258262890683122, 1.000000000000000000, 0.9659258262890683122, 1.000000000000000000, 0.9659258262890683122, 1.000000000000000000, 0.9659258262890683122, 1.000000000000000000, 0.9659258262890683122, 1.000000000000000000, 0.9659258262890683122, 1.000000000000000000, 0.9659258262890683122, 1.000000000000000000, 0.9659258262890683122, 1.000000000000000000, 0.9659258262890683122, 1.000000000000000000, 0.9659258262890683122, 1.000000000000000000, 0.9659258262890683122, 1.000000000000000000, 0.9659258262890683122, 1.000000000000000000, 0.9659258262890683122, 1.000000000000000000, 0.9659258262890683122, 1.000000000000000000, 0.9659258262890683122, 1.000000000000000000, 0.9659258262890683122, 1.000000000000000000, 0.9659258262890683122, 1.000000000000000000, 0.9659258262890683122, 1.000000000000000000, 0.9659258262890683122, 1.000000000000000000, 0.9659258262890683122, 1.000000000000000000, 0.9659258262890683122, 1.000000000000000000, 0.9659258262890683122, 1.000000000000000000, 0.9659258262890683122, 1.000000000000000000, 0.9659258262890683122, 1.000000000000000000, 0.9659258262890683122, 1.000000000000000000, 0.9659258262890683122, 1.000000000000000000, 0.9659258262890683122, 1.000000000000000000, 0.9659258262890683122, 1.000000000000000000, 0.9659258262890683122, 1.000000000000000000, 0.9659258262890683122, 1.000000000000000000, 0.9659258262890683122, 1.000000000000000000, 0.9659258262890683122, 1.000000000000000000, 0.9659258262890683122, 1.000000000000000000, 0.9659258262890683122, 1.000000000000000000, 0.9659258262890683122, 1.000000000000000000, 0.9659258262890683122, 1.000000000000000000, 0.9659258262890683122, 1.000000000000000000, 0.9659258262890683122, 1.000000000000000000, 0.9659258262890683122, 1.000000000000000000, 0.9659258262890683122, 1.000000000000000000, 0.9659258262890683122, 1.000000000000000000, 0.9659258262890683122, 1.000000000000000000, 0.9659258262890683122, 1.000000000000000000, 0.9659258262890683122, 1.000000000000000000, 0.9659258262890683122, 1.000000000000000000, 0.9659258262890683122, 1.000000000000000000, 0.9659258262890683122, 1.000000000000000000, 0.9659258262890683122, 1.000000000000000000, 0.9659258262890683122, 1.000000000000000000, 0.9659258262890683122, 1.000000000000000000, 0.9659258262890683122, 1.000000000000000000, 0.9659258262890683122, 1.000000000000000000, 0.9659258262890683122, 1.000000000000000000, 0.9659258262890683122, 1.000000000000000000, 0.9659258262890683122, 1.000000000000000000, 0.9659258262890683122, 1.000000000000000000, 0.9659258262890683122, 1.000000000000000000, 0.9659258262890683122, 1.000000000000000000, 0.9659258262890683122, 1.000000000000000000, 0.9659258262890683122, 1.000000000000000000, 0.9659258262890683122, 1.000000000000000000, 0.9659258262890683122, 1.000000000000000000, 0.9659258262890683122, 1.000000000000000000, 0.9659258262890683122, 1.000000000000000000, 0.9659258262890683122, 1.000000000000000000, 0.9659258262890683122, 1.000000000000000000, 0.9659258262890683122, 1.000000000000000000, 0.9659258262890683122, 1.000000000000000000, 0.9659258262890683122, 1.000000000000000000, 0.9659258262890683122, 1.000000000000000000, 0.9659258262890683122, 1.000000000000000000, 0.9659258262890683122, 1.000000000000000000, 0.9659258262890683122, 1.000000000000000000, 0.9659258262890683122, 1.000000000000000000, 0.9659258262890683122, 1.000000000000000000, 0.9659258262890683122, 1.000000000000000000, 0.9659258262890683122, 1.000000000000000000, 0.9659258262890683122, 1.000000000000000000, 0.9659258262890683122, 1.000000000000000000, 0.9659258262890683122, 1.000000000000000000, 0.9659258262890683122, 1.000000000000000000, 0.9659258262890683122, 1.000000000000000000, 0.9659258262890683122, 1.000000000000000000, 0.9659258262890683122, 1.000000000000000000, 0.9659258262890683122, 1.000000000000000000, 0.9659258262890683122, 1.000000000000000000, 0.9659258262890683122, 1.000000000000000000, 0.9659258262890683122, 1.000000000000000000, 0.9659258262890683122, 1.000000000000000000, 0.9659258262890683122, 1.000000000000000000, 0.9659258262890683122, 1.000000000000000000, 0.9659258262890683122, 1.000000000000000000, 0.9659258262890683122, 1.000000000000000000, 0.9659258262890683122, 1.000000000000000000, 0.9659258262890683122, 1.000000000000000000, 0.9659258262890683122, 1.000000000000000000, 0.9659258262890683122, 1.000000000000000000, 0.9659258262890683122, 1.000000000000000000, 0.9659258262890683122, 1.000000000000000000, 0.9659258262890683122, 1.000000000000000000, 0.9659258262890683122, 1.000000000000000000, 0.9659258262890683122, 1.000000000000000000, 0.9659258262890683122, 1.000000000000000000, 0.9659258262890683122, 1.000000000000000000, 0.9659258262890683122, 1.000000000000000000, 0.9659258262890683122, 1.000000000000000000, 0.9659258262890683122, 1.000000000000000000, 0.9659258262890683122, 1.000000000000000000, 0.9659258262890683122, 1.000000000000000000, 0.9659258262890683122, 1.000000000000000000, 0.9659258262890683122, 1.000000000000000000, 0.9659258262890683122, 1.000000000000000000, 0.9659258262890683122, 1.000000000000000000, 0.9659258262890683122, 1.000000000000000000, 0.9659258262890683122, 1.000000000000000000, 0.9659258262890683122, 1.000000000000000000, 0.9659258262890683122, 1.000000000000000000, 0.9659258262890683122, 1.000000000000000000, 0.9659258262890683122, 1.000000000000000000, 0.9659258262890683122, 1.000000000000000000, 0.9659258262890683122, 1.000000000000000000, 0.9659258262890683122, 1.000000000000000000, 0.9659258262890683122, 1.000000000000000000, 0.9659258262890683122, 1.000000000000000000, 0.9659258262890683122, 1.000000000000000000, 0.9659258262890683122, 1.000000000000000000, 0.9659258262890683122, 1.000000000000000000, 0.9659258262890683122, 1.000000000000000000, 0.9659258262890683122, 1.000000000000000000, 0.9659258262890683122, 1.000000000000000000, 0.9659258262890683122, 1.000000000000000000, 0.9659258262890683122, 1.000000000000000000, 0.9659258262890683122, 1.000000000000000000, 0.9659258262890683122, 1.000000000000000000, 0.9659258262890683122, 1.000000000000000000, 0.9659258262890683122, 1.000000000000000000, 0.9659258262890683122, 1.000000000000000000, 0.9659258262890683122, 1.000000000000000000, 0.9659258262890683122, 1.000000000000000000, 0.9659258262890683122, 1.000000000000000000, 0.9659258262890683122, 1.000000000000000000, 0.9659258262890683122, 1.000000000000000000, 0.9659258262890683122, 1.000000000000000000, 0.9659258262890683122, 1.000000000000000000, 0.9659258262890683122, 1.000000000000000000, 0.9659258262890683122, 1.000000000000000000, 0.9659258262890683122, 1.000000000000000000, 0.9659258262890683122, 1.000000000000000000, 0.9659258262890683122, 1.000000000000000000, 0.9659258262890683122, 1.000000000000000000, 0.9659258262890683122, 1.000000000000000000, 0.9659258262890683122, 1.000000000000000000, 0.9659258262890683122, 1.000000000000000000, 0.9659258262890683122, 1.000000000000000000, 0.9659258262890683122, 1.000000000000000000, 0.9659258262890683122, 1.000000000000000000, 0.9659258262890683122, 1.000000000000000000, 0.9659258262890683122, 1.000000000000000000, 0.9659258262890683122, 1.000000000000000000, 0.9659258262890683122, 1.000000000000000000, 0.9659258262890683122, 1.000000000000000000, 0.9659258262890683122, 1.000000000000000000, 0.9659258262890683122, 1.000000000000000000, 0.9659258262890683122, 1.000000000000000000, 0.9659258262890683122, 1.000000000000000000, 0.9659258262890683122, 1.000000000000000000, 0.9659258262890683122, 1.000000000000000000, 0.9659258262890683122, 1.000000000000000000, 0.9659258262890683122, 1.000000000000000000, 0.9659258262890683122, 1.000000000000000000, 0.9659258262890683122, 1.000000000000000000, 0.9659258262890683122, 1.000000000000000000, 0.9659258262890683122, 1.000000000000000000, 0.9659258262890683122, 1.000000000000000000, 0.9659258262890683122, 1.000000000000000000, 0.9659258262890683122, 1.000000000000000000, 0.9659258262890683122, 1.000000000000000000, 0.9659258262890683122, 1.000000000000000000, 0.9659258262890683122, 1.000000000000000000, 0.9659258262890683122, 1.000000000000000000, 0.9659258262890683122, 1.000000000000000000, 0.9659258262890683122, 1.000000000000000000, 0.9659258262890683122, 1.000000000000000000, 0.9659258262890683122, 1.000000000000000000, 0.9659258262890683122, 1.000000000000000000, 0.9659258262890683122, 1.000000000000000000, 0.9659258262890683122, 1.000000000000000000, 0.9659258262890683122, 1.000000000000000000, 0.9659258262890683122, 1.000000000000000000, 0.9659258262890683122, 1.000000000000000000, 0.9659258262890683122, 1.000000000000000000, 0.9659258262890683122, 1.000000000000000000, 0.9659258262890683122, 1.000000000000000000, 0.9659258262890683122, 1.000000000000000000, 0.9659258262890683122, 1.000000000000000000, 0.9659258262890683122, 1.000000000000000000, 0.9659258262890683122, 1.000000000000000000, 0.9659258262890683122, 1.000000000000000000, 0.9659258262890683122, 1.000000000000000000, 0.9659258262890683122, 1.000000000000000000, 0.9659258262890683122, 1.000000000000000000, 0.9659258262890683122, 1.000000000000000000, 0.9659258262890683122, 1.000000000000000000, 0.9659258262890683122, 1.000000000000000000, 0.9659258262890683122, 1.000000000000000000, 0.9659258262890683122, 1.000000000000000000, 0.9659258262890683122, 1.000000000000000000, 0.9659258262890683122, 1.000000000000000000, 0.9659258262890683122, 1.000000000000000000, 0.9659258262890683122, 1.000000000000000000, 0.9659258262890683122, 1.000000000000000000, 0.9659258262890683122, 1.000000000000000000, 0.9659258262890683122, 1.000000000000000000, 0.9659258262890683122, 1.000000000000000000, 0.9659258262890683122, 1.000000000000000000, 0.9659258262890683122, 1.000000000000000000, 0.9659258262890683122, 1.000000000000000000, 0.9659258262890683122, 1.000000000000000000, 0.9659258262890683122, 1.000000000000000000, 0.9659258262890683122, 1.000000000000000000, 0.9659258262890683122, 1.000000000000000000, 0.9659258262890683122, 1.000000000000000000, 0.9659258262890683122, 1.000000000000000000, 0.9659258262890683122, 1.000000000000000000, 0.9659258262890683122, 1.000000000000000000, 0.9659258262890683122, 1.000000000000000000, 0.9659258262890683122, 1.000000000000000000, 0.9659258262890683122, 1.000000000000000000, 0.9659258262890683122, 1.000000000000000000, 0.9659258262890683122, 1.000000000000000000, 0.9659258262890683122, 1.000000000000000000, 0.9659258262890683122, 1.000000000000000000, 0.9659258262890683122, 1.000000000000000000, 0.9659258262890683122, 1.000000000000000000, 0.9659258262890683122, 1.000000000000000000, 0.9659258262890683122, 1.000000000000000000, 0.9659258262890683122, 1.000000000000000000, 0.9659258262890683122, 1.000000000000000000, 0.9659258262890683122, 1.000000000000000000, 0.9659258262890683122, 1.000000000000000000, 0.9659258262890683122, 1.000000000000000000, 0.9659258262890683122, 1.000000000000000000, 0.9659258262890683122, 1.000000000000000000, 0.9659258262890683122, 1.000000000000000000, 0.9659258262890683122, 1.000000000000000000, 0.9659258262890683122, 1.000000000000000000, 0.9659258262890683122, 1.000000000000000000, 0.9659258262890683122, 1.000000000000000000, 0.9659258262890683122, 1.000000000000000000, 0.9659258262890683122, 1.000000000000000000, 0.9659258262890683122, 1.000000000000000000, 0.9659258262890683122, 1.000000000000000000, 0.9659258262890683122, 1.000000000000000000, 0.9659258262890683122, 1.000000000000000000, 0.9659258262890683122, 1.000000000000000000, 0.9659258262890683122, 1.000000000000000000, 0.9659258262890683122, 1.000000000000000000, 0.9659258262890683122, 1.000000000000000000, 0.9659258262890683122, 1.000000000000000000, 0.9659258262890683122, 1.000000000000000000, 0.9659258262890683122, 1.000000000000000000, 0.9659258262890683122, 1.000000000000000000, 0.9659258262890683122, 1.000000000000000000, 0.9659258262890683122, 1.000000000000000000, 0.9659258262890683122, 1.000000000000000000, 0.9659258262890683122, 1.000000000000000000, 0.9659258262890683122, 1.000000000000000000, 0.9659258262890683122, 1.000000000000000000, 0.9659258262890683122, 1.000000000000000000, 0.9659258262890683122, 1.000000000000000000, 0.9659258262890683122, 1.000000000000000000, 0.9659258262890683122, 1.000000000000000000, 0.9659258262890683122, 1.000000000000000000, 0.9659258262890683122, 1.000000000000000000, 0.9659258262890683122, 1.000000000000000000, 0.9659258262890683122, 1.000000000000000000, 0.9659258262890683122, 1.000000000000000000, 0.9659258262890683122, 1.000000000000000000, 0.9659258262890683122, 1.000000000000000000, 0.9659258262890683122, 1.000000000000000000, 0.9659258262890683122, 1.000000000000000000, 0.9659258262890683122, 1.000000000000000000, 0.9659258262890683122, 1.000000000000000000, 0.9659258262890683122, 1.000000000000000000, 0.9659258262890683122, 1.000000000000000000, 0.9659258262890683122, 1.000000000000000000, 0.9659258262890683122, 1.000000000000000000, 0.9659258262890683122, 1.000000000000000000, 0.9659258262890683122, 1.000000000000000000, 0.9659258262890683122, 1.000000000000000000, 0.9659258262890683122, 1.000000000000000000, 0.9659258262890683122, 1.000000000000000000, 0.9659258262890683122, 1.000000000000000000, 0.9659258262890683122, 1.000000000000000000, 0.9659258262890683122, 1.000000000000000000, 0.9659258262890683122, 1.000000000000000000, 0.9659258262890683122, 1.000000000000000000, 0.9659258262890683122, 1.000000000000000000, 0.9659258262890683122, 1.000000000000000000, 0.9659258262890683122, 1.000000000000000000, 0.9659258262890683122, 1.000000000000000000, 0.9659258262890683122, 1.000000000000000000, 0.9659258262890683122, 1.000000000000000000, 0.9659258262890683122, 1.000000000000000000, 0.9659258262890683122, 1.000000000000000000, 0.9659258262890683122, 1.000000000000000000, 0.9659258262890683122, 1.000000000000000000, 0.9659258262890683122, 1.000000000000000000, 0.9659258262890683122, 1.000000000000000000, 0.9659258262890683122, 1.000000000000000000, 0.9659258262890683122, 1.000000000000000000, 0.9659258262890683122, 1.000000000000000000, 0.9659258262890683122, 1.000000000000000000, 0.9659258262890683122, 1.000000000000000000, 0.9659258262890683122, 1.000000000000000000, 0.9659258262890683122, 1.000000000000000000, 0.9659258262890683122, 1.000000000000000000, 0.9659258262890683122, 1.000000000000000000, 0.9659258262890683122, 1.000000000000000000, 0.9659258262890683122, 1.000000000000000000, 0.9659258262890683122, 1.000000000000000000, 0.9659258262890683122, 1.000000000000000000, 0.9659258262890683122, 1.000000000000000000, 0.9659258262890683122, 1.000000000000000000, 0.9659258262890683122, 1.000000000000000000, 0.9659258262890683122, 1.000000000000000000, 0.9659258262890683122, 1.000000000000000000, 0.9659258262890683122, 1.000000000000000000, 0.9659258262890683122, 1.000000000000000000, 0.9659258262890683122, 1.000000000000000000, 0.9659258262890683122, 1.000000000000000000, 0.9659258262890683122, 1.000000000000000000, 0.9659258262890683122, 1.000000000000000000, 0.9659258262890683122, 1.000000000000000000, 0.9659258262890683122, 1.000000000000000000, 0.9659258262890683122, 1.000000000000000000, 0.9659258262890683122, 1.000000000000000000, 0.9659258262890683122, 1.000000000000000000, 0.9659258262890683122, 1.000000000000000000, 0.9659258262890683122, 1.000000000000000000, 0.9659258262890683122, 1.000000000000000000, 0.9659258262890683122, 1.000000000000000000, 0.9659258262890683122, 1.000000000000000000, 0.9659258262890683122, 1.000000000000000000, 0.9659258262890683122, 1.000000000000000000, 0.9659258262890683122, 1.000000000000000000, 0.9659258262890683122, 1.000000000000000000, 0.9659258262890683122, 1.000000000000000000, 0.9659258262890683122, 1.000000000000000000, 0.9659258262890683122, 1.000000000000000000, 0.9659258262890683122, 1.000000000000000000, 0.9659258262890683122, 1.000000000000000000, 0.9659258262890683122, 1.000000000000000000, 0.9659258262890683122, 1.000000000000000000, 0.9659258262890683122, 1.000000000000000000, 0.9659258262890683122, 1.000000000000000000, 0.9659258262890683122, 1.000000000000000000, 0.9659258262890683122, 1.000000000000000000, 0.9659258262890683122, 1.000000000000000000, 0.9659258262890683122, 1.000000000000000000, 0.9659258262890683122, 1.000000000000000000, 0.9659258262890683122, 1.000000000000000000, 0.9659258262890683122, 1.000000000000000000, 0.9659258262890683122, 1.000000000000000000, 0.9659258262890683122, 1.000000000000000000, 0.9659258262890683122, 1.000000000000000000, 0.9659258262890683122, 1.000000000000000000, 0.9659258262890683122, 1.000000000000000000, 0.9659258262890683122, 1.000000000000000000, 0.9659258262890683122, 1.000000000000000000, 0.9659258262890683122, 1.000000000000000000, 0.9659258262890683122, 1.000000000000000000, 0.9659258262890683122, 1.000000000000000000, 0.9659258262890683122, 1.000000000000000000, 0.9659258262890683122, 1.000000000000000000, 0.9659258262890683122, 1.000000000000000000, 0.9659258262890683122, 1.000000000000000000, 0.9659258262890683122, 1.000000000000000000, 0.9659258262890683122, 1.000000000000000000, 0.9659258262890683122, 1.000000000000000000, 0.9659258262890683122, 1.000000000000000000, 0.9659258262890683122, 1.000000000000000000, 0.9659258262890683122, 1.000000000000000000, 0.9659258262890683122, 1.000000000000000000, 0.9659258262890683122, 1.000000000000000000, 0.9659258262890683122, 1.000000000000000000, 0.9659258262890683122, 1.000000000000000000, 0.9659258262890683122, 1.000000000000000000, 0.9659258262890683122, 1.000000000000000000, 0.9659258262890683122, 1.000000000000000000, 0.9659258262890683122, 1.000000000000000000, 0.9659258262890683122, 1.000000000000000000, 0.9659258262890683122, 1.000000000000000000, 0.9659258262890683122, 1.000000000000000000, 0.9659258262890683122, 1.000000000000000000, 0.9659258262890683122, 1.000000000000000000, 0.9659258262890683122, 1.000000000000000000, 0.9659258262890683122, 1.000000000000000000, 0.9659258262890683122, 1.000000000000000000, 0.9659258262890683122, 1.000000000000000000, 0.9659258262890683122, 1.000000000000000000, 0.9659258262890683122, 1.000000000000000000, 0.9659258262890683122, 1.000000000000000000, 0.9659258262890683122, 1.000000000000000000, 0.9659258262890683122, 1.000000000000000000, 0.9659258262890683122, 1.000000000000000000, 0.9659258262890683122, 1.000000000000000000, 0.9659258262890683122, 1.000000000000000000, 0.9659258262890683122, 1.000000000000000000, 0.9659258262890683122, 1.000000000000000000, 0.9659258262890683122, 1.000000000000000000, 0.9659258262890683122, 1.000000000000000000, 0.9659258262890683122, 1.000000000000000000, 0.9659258262890683122, 1.000000000000000000, 0.9659258262890683122, 1.000000000000000000, 0.9659258262890683122, 1.000000000000000000, 0.9659258262890683122, 1.000000000000000000, 0.9659258262890683122, 1.000000000000000000, 0.9659258262890683122, 1.000000000000000000, 0.9659258262890683122, 1.000000000000000000, 0.9659258262890683122, 1.000000000000000000, 0.9659258262890683122, 1.000000000000000000, 0.9659258262890683122, 1.000000000000000000, 0.9659258262890683122, 1.000000000000000000, 0.9659258262890683122, 1.000000000000000000, 0.9659258262890683122, 1.000000000000000000, 0.9659258262890683122, 1.000000000000000000, 0.9659258262890683122, 1.000000000000000000, 0.9659258262890683122, 1.000000000000000000, 0.9659258262890683122, 1.000000000000000000, 0.9659258262890683122, 1.000000000000000000, 0.9659258262890683122, 1.000000000000000000, 0.9659258262890683122, 1.000000000000000000, 0.9659258262890683122, 1.000000000000000000, 0.9659258262890683122, 1.000000000000000000, 0.9659258262890683122, 1.000000000000000000, 0.9659258262890683122, 1.000000000000000000, 0.9659258262890683122, 1.000000000000000000, 0.9659258262890683122, 1.000000000000000000, 0.9659258262890683122, 1.000000000000000000, 0.9659258262890683122, 1.000000000000000000, 0.9659258262890683122, 1.000000000000000000, 0.9659258262890683122, 1.000000000000000000, 0.9659258262890683122, 1.000000000000000000, 0.9659258262890683122, 1.000000000000000000, 0.9659258262890683122, 1.000000000000000000, 0.9659258262890683122, 1.000000000000000000, 0.9659258262890683122, 1.000000000000000000, 0.9659258262890683122, 1.000000000000000000, 0.9659258262890683122, 1.000000000000000000, 0.9659258262890683122, 1.000000000000000000, 0.9659258262890683122, 1.000000000000000000, 0.9659258262890683122, 1.000000000000000000, 0.9659258262890683122, 1.000000000000000000, 0.9659258262890683122, 1.000000000000000000, 0.9659258262890683122, 1.000000000000000000, 0.9659258262890683122, 1.000000000000000000, 0.9659258262890683122, 1.000000000000000000, 0.9863514418465433309, 0.9836368620925994843, 0.9836368620925994843, 0.9836368620925994843) ) ) 
 REPRESENTATION_ITEM ( '' )  SURFACE ( )  );
#65489=CARTESIAN_POINT ( 'NONE',  ( -4.999999999999998224, 148.5416666598387110, -8.660254037844389075 ) ) ;
#65490=CARTESIAN_POINT ( 'NONE',  ( 6.676582343750001591, 290.9531250017069510, -8.176455196517173205E-16 ) ) ;
#65493=CARTESIAN_POINT ( 'NONE',  ( -3.042071309553164404, 132.5520833299193555, -11.35316468749999963 ) ) ;
#65512=CARTESIAN_POINT ( 'NONE',  ( -2.765530957081996810, 292.2656250017069510, -6.676582343750002480 ) ) ;
#65514=CARTESIAN_POINT ( 'NONE',  ( 8.660254037844389075, 137.2916666598387110, -5.000000000000000000 ) ) ;
#65526=CARTESIAN_POINT ( 'NONE',  ( -5.676582343750006032, 99.42708332991935549, 9.832129032723418760 ) ) ;
#65534=EDGE_CURVE ( 'NONE', #47954, #39497, #72846, .T. ) ;
#65535=CARTESIAN_POINT ( 'NONE',  ( -2.085542519210945728E-15, 209.5312499965860411, 11.35316468750000141 ) ) ;
#65539=CARTESIAN_POINT ( 'NONE',  ( -11.35316468750000141, 198.8020833299193839, 3.042071309553159963 ) ) ;
#65545=CARTESIAN_POINT ( 'NONE',  ( -8.311093377946841443, 83.90624999658602690, 8.311093377946830785 ) ) ;
#65550=CARTESIAN_POINT ( 'NONE',  ( -2.085542519210945728E-15, 69.53124999658602690, 11.35316468750000141 ) ) ;
#65551=ORIENTED_EDGE ( 'NONE', *, *, #56608, .T. ) ;
#65557=CARTESIAN_POINT ( 'NONE',  ( -5.676582343750006032, 79.11458332991935549, 9.832129032723418760 ) ) ;
#65560=CARTESIAN_POINT ( 'NONE',  ( -2.679491924311235618, 165.4166666598387110, 10.00000000000000000 ) ) ;
#65563=CARTESIAN_POINT ( 'NONE',  ( -11.35316468750000141, 63.80208332991934839, 3.042071309553159963 ) ) ;
#65565=CARTESIAN_POINT ( 'NONE',  ( -3.042071309553164404, 192.2395833299193555, -11.35316468749999963 ) ) ;
#65566=ORIENTED_EDGE ( 'NONE', *, *, #27397, .F. ) ;
#65569=CARTESIAN_POINT ( 'NONE',  ( -4.242640687119285658, 288.1249999999999432, 4.242640687119287435 ) ) ;
#65571=CARTESIAN_POINT ( 'NONE',  ( 6.951808397369818766E-16, 192.0312499965860127, -11.35316468750000141 ) ) ;
#65572=CARTESIAN_POINT ( 'NONE',  ( -7.320508075688773708, 193.7499999931720538, -7.320508075688774596 ) ) ;
#65574=CARTESIAN_POINT ( 'NONE',  ( -5.000000000000005329, 190.2083333265053966, 8.660254037844387298 ) ) ;
#65576=CARTESIAN_POINT ( 'NONE',  ( 5.676582343750001591, 176.9270833299193555, -9.832129032723420536 ) ) ;
#65577=( BOUNDED_CURVE ( )  B_SPLINE_CURVE ( 2, ( #24550, #24909, #70580, #47556, #46457, #6482, #58906, #30220, #23820 ),
 .UNSPECIFIED., .F., .F. ) 
 B_SPLINE_CURVE_WITH_KNOTS ( ( 3, 2, 2, 2, 3 ),
 ( 0.8541666666666649643, 0.8645833333333317050, 0.8749999999999984457, 0.8854166666666650753, 0.8958333333333318160 ),
 .UNSPECIFIED. ) 
 CURVE ( )  GEOMETRIC_REPRESENTATION_ITEM ( )  RATIONAL_B_SPLINE_CURVE ( ( 1.000000000000012212, 0.9238795325112745260, 1.000000000000000000, 0.9238795325112867385, 1.000000000000000000, 0.9238795325112867385, 1.000000000000000000, 0.9238795325112980628, 0.9999999999999886757 ) ) 
 REPRESENTATION_ITEM ( '' )  );
#65585=( BOUNDED_CURVE ( )  B_SPLINE_CURVE ( 2, ( #49654, #54208, #60596, #44370, #72671, #2518, #14185, #71907, #8173, #21348, #48894, #55704, #49270 ),
 .UNSPECIFIED., .F., .F. ) 
 B_SPLINE_CURVE_WITH_KNOTS ( ( 3, 2, 2, 2, 2, 2, 3 ),
 ( 0.5597826086956521063, 0.5615942028985506651, 0.5634057971014491129, 0.5652173913043476716, 0.5670289855072463414, 0.5688405797101449002, 0.5706521739130434590 ),
 .UNSPECIFIED. ) 
 CURVE ( )  GEOMETRIC_REPRESENTATION_ITEM ( )  RATIONAL_B_SPLINE_CURVE ( ( 1.000000000000001998, 0.9659258262890662028, 1.000000000000000000, 0.9659258262890683122, 1.000000000000000000, 0.9659258262890683122, 1.000000000000000000, 0.9659258262890683122, 1.000000000000000000, 0.9659258262890683122, 1.000000000000000000, 0.9659258262890683122, 1.000000000000000000 ) ) 
 REPRESENTATION_ITEM ( '' )  );
#65591=ORIENTED_EDGE ( 'NONE', *, *, #48437, .F. ) ;
#65595=DIRECTION ( 'NONE',  ( 0.000000000000000000, 0.000000000000000000, 1.000000000000000000 ) ) ;
#65603=ORIENTED_EDGE ( 'NONE', *, *, #43051, .T. ) ;
#65605=CARTESIAN_POINT ( 'NONE',  ( 2.679491924311222739, 90.83333332650536818, 10.00000000000000355 ) ) ;
#65607=DIRECTION ( 'NONE',  ( -0.000000000000000000, 1.000000000000000000, -0.000000000000000000 ) ) ;
#65609=CARTESIAN_POINT ( 'NONE',  ( -2.765530957081998142, 292.7968750017070079, 6.676582343750000703 ) ) ;
#65610=CARTESIAN_POINT ( 'NONE',  ( 6.123233995736767268E-16, 151.2500000000000284, -10.00000000000000178 ) ) ;
#65627=CARTESIAN_POINT ( 'NONE',  ( 3.042071309553167069, 41.82291666325269119, -11.35316468749999785 ) ) ;
#65628=CARTESIAN_POINT ( 'NONE',  ( 2.679491924297531913, 148.9583333333321207, 10.00000000000791367 ) ) ;
#65629=CARTESIAN_POINT ( 'NONE',  ( 5.000000000000001776, 12.70833332650536640, -8.660254037844389075 ) ) ;
#65635=CARTESIAN_POINT ( 'NONE',  ( -2.085542519210945728E-15, 29.53124999658601624, 11.35316468750000141 ) ) ;
#65641=CARTESIAN_POINT ( 'NONE',  ( -3.042071309553173730, 29.32291666325268764, 11.35316468749999785 ) ) ;
#65643=CARTESIAN_POINT ( 'NONE',  ( -11.35316468750000141, 168.4895833299193839, 3.042071309553159963 ) ) ;
#65644=CARTESIAN_POINT ( 'NONE',  ( 8.660254037844389075, 127.2916666598387110, -5.000000000000000000 ) ) ;
#65649=CARTESIAN_POINT ( 'NONE',  ( -5.676582343750006032, 19.42708332991934839, 9.832129032723418760 ) ) ;
#65650=EDGE_LOOP ( 'NONE', ( #48902, #15612, #28011, #841 ) ) ;
#65651=DIRECTION ( 'NONE',  ( 0.000000000000000000, 0.000000000000000000, 1.000000000000000000 ) ) ;
#65652=DIRECTION ( 'NONE',  ( -0.000000000000000000, 1.000000000000000000, -0.000000000000000000 ) ) ;
#65654=CARTESIAN_POINT ( 'NONE',  ( 11.35316468749999785, 150.5729166632526699, 3.042071309553174174 ) ) ;
#65663=CARTESIAN_POINT ( 'NONE',  ( -11.35316468750000141, 108.5937499965860269, -1.390361679473963753E-15 ) ) ;
#65680=EDGE_CURVE ( 'NONE', #64324, #53638, #59212, .T. ) ;
#65682=CARTESIAN_POINT ( 'NONE',  ( -8.660254037844390851, 224.7916666598387110, 4.999999999999998224 ) ) ;
#65690=CARTESIAN_POINT ( 'NONE',  ( 2.679491924311229401, 126.0416666666666572, -10.00000000000000178 ) ) ;
#65695=CARTESIAN_POINT ( 'NONE',  ( -2.679491924311235618, 113.5416666666666714, 10.00000000000000000 ) ) ;
#65697=CARTESIAN_POINT ( 'NONE',  ( -6.676582343750001591, 294.6093750017069510, 0.000000000000000000 ) ) ;
#65699=CARTESIAN_POINT ( 'NONE',  ( 5.000000000000014211, 189.1666666666667140, 8.660254037844426378 ) ) ;
#65704=DIRECTION ( 'NONE',  ( -0.000000000000000000, 1.000000000000000000, -0.000000000000000000 ) ) ;
#65707=CARTESIAN_POINT ( 'NONE',  ( 2.679491924311222739, 223.9583333333333428, 10.00000000000000355 ) ) ;
#65708=EDGE_CURVE ( 'NONE', #55468, #18660, #46849, .T. ) ;
#65710=CARTESIAN_POINT ( 'NONE',  ( -11.35316468749999785, 198.3854166632526699, -3.042071309553167513 ) ) ;
#65714=DIRECTION ( 'NONE',  ( 0.000000000000000000, 0.000000000000000000, 1.000000000000000000 ) ) ;
#65718=CARTESIAN_POINT ( 'NONE',  ( 6.951808397369818766E-16, 47.34374999658602690, -11.35316468750000141 ) ) ;
#65727=CARTESIAN_POINT ( 'NONE',  ( -11.35316468750000141, 113.4895833299193413, 3.042071309553159963 ) ) ;
#65728=CARTESIAN_POINT ( 'NONE',  ( 10.00000000000000178, 92.08333332650536818, -2.679491924311226736 ) ) ;
#65736=CARTESIAN_POINT ( 'NONE',  ( -9.935834282059264666, 225.9999999999999716, 1.307295064324885070 ) ) ;
#65737=ORIENTED_EDGE ( 'NONE', *, *, #10496, .F. ) ;
#65739=CARTESIAN_POINT ( 'NONE',  ( 4.721056650415999201, 292.2343750017069510, -4.721056650415999201 ) ) ;
#65742=CARTESIAN_POINT ( 'NONE',  ( -11.35316468750000141, 173.4895833299193839, 3.042071309553159963 ) ) ;
#65747=EDGE_LOOP ( 'NONE', ( #10478, #9161, #65755, #25080 ) ) ;
#65749=CARTESIAN_POINT ( 'NONE',  ( 0.000000000000000000, 300.0000000000000000, 6.000000000000001776 ) ) ;
#65750=CARTESIAN_POINT ( 'NONE',  ( 9.832129032723416984, 145.6770833299193555, 5.676582343750006032 ) ) ;
#65754=CARTESIAN_POINT ( 'NONE',  ( 8.311093377946834337, 60.46874999658602690, 8.311093377946839666 ) ) ;
#65755=ORIENTED_EDGE ( 'NONE', *, *, #24658, .T. ) ;
#65781=EDGE_LOOP ( 'NONE', ( #28058, #16670, #18398, #63445 ) ) ;
#65786=CARTESIAN_POINT ( 'NONE',  ( -2.679491924311225848, 66.45833333333334281, -10.00000000000000178 ) ) ;
#65788=CARTESIAN_POINT ( 'NONE',  ( -2.485281374238572649, 298.1875000000000000, 6.000000000000002665 ) ) ;
#65800=CARTESIAN_POINT ( 'NONE',  ( -5.000000000000005329, 168.3333333333333428, 8.660254037844387298 ) ) ;
#65802=CARTESIAN_POINT ( 'NONE',  ( 9.832129032723416984, 160.6770833299193555, 5.676582343750006032 ) ) ;
#65803=CARTESIAN_POINT ( 'NONE',  ( 6.000000000000003553, 294.5000000034139589, 2.485281374238571317 ) ) ;
#65804=DIRECTION ( 'NONE',  ( -0.000000000000000000, 1.000000000000000000, -0.000000000000000000 ) ) ;
#65809=CARTESIAN_POINT ( 'NONE',  ( -5.676582343749998039, 12.76041666325268409, -9.832129032723420536 ) ) ;
#65810=CARTESIAN_POINT ( 'NONE',  ( 4.999999999999993783, 96.04166665983871098, 8.660254037844390851 ) ) ;
#65811=CARTESIAN_POINT ( 'NONE',  ( 7.320508075688774596, 32.49999999317203248, -7.320508075688774596 ) ) ;
#65815=CARTESIAN_POINT ( 'NONE',  ( -2.679491924311235618, 45.41666665983869677, 10.00000000000000000 ) ) ;
#65821=CARTESIAN_POINT ( 'NONE',  ( 6.123233995736767268E-16, 8.124999993172032475, -10.00000000000000178 ) ) ;
#65823=CARTESIAN_POINT ( 'NONE',  ( -3.673940397442060854E-16, 292.8125000034140157, -6.000000000000001776 ) ) ;
#65826=CARTESIAN_POINT ( 'NONE',  ( -2.085542519210945728E-15, 124.5312499965860269, 11.35316468750000141 ) ) ;
#65833=CARTESIAN_POINT ( 'NONE',  ( 5.000000000000014211, 45.83333333333334991, -8.660254037844408614 ) ) ;
#65834=CARTESIAN_POINT ( 'NONE',  ( 3.042071309553167513, 111.8229166632526983, -11.35316468749999785 ) ) ;
#65837=CARTESIAN_POINT ( 'NONE',  ( 8.660254037844385522, 81.45833332650536818, 5.000000000000005329 ) ) ;
#65839=LINE ( 'NONE', #14147, #970 ) ;
#65841=CARTESIAN_POINT ( 'NONE',  ( 3.042071309553159519, 105.0520833299193271, 11.35316468750000141 ) ) ;
#65845=CARTESIAN_POINT ( 'NONE',  ( 5.676582343750001591, 26.92708332991935194, -9.832129032723420536 ) ) ;
#65847=CARTESIAN_POINT ( 'NONE',  ( 7.320508075688774596, 182.4999999931720254, -7.320508075688774596 ) ) ;
#65849=CARTESIAN_POINT ( 'NONE',  ( 7.320508075688774596, 117.4999999931720396, -7.320508075688774596 ) ) ;
#65853=CARTESIAN_POINT ( 'NONE',  ( 6.676582343750004256, 293.8906250017069510, 2.765530957081995478 ) ) ;
#65855=CARTESIAN_POINT ( 'NONE',  ( -2.085542519210945728E-15, 224.8437499965860127, 11.35316468750000141 ) ) ;
#65857=CARTESIAN_POINT ( 'NONE',  ( 9.832129032723416984, 125.6770833299193697, 5.676582343750006032 ) ) ;
#65864=ORIENTED_EDGE ( 'NONE', *, *, #10876, .T. ) ;
#65868=CARTESIAN_POINT ( 'NONE',  ( -7.320508075688847427, 173.1250000000000284, 7.320508075688839433 ) ) ;
#65874=CARTESIAN_POINT ( 'NONE',  ( -4.999999999999998224, 28.54166665983870033, -8.660254037844389075 ) ) ;
#65878=CARTESIAN_POINT ( 'NONE',  ( -4.088227598258586603E-16, 294.2031250017069510, -6.676582343750001591 ) ) ;
#65891=CARTESIAN_POINT ( 'NONE',  ( 3.042071309553167069, 112.1354166632526699, -11.35316468749999785 ) ) ;
#65892=CARTESIAN_POINT ( 'NONE',  ( -2.679491924311234285, 123.5416666666666714, 9.999999999999996447 ) ) ;
#65897=VERTEX_POINT ( 'NONE', #22543 ) ;
#65901=AXIS2_PLACEMENT_3D ( 'NONE', #22453, #38724, #10041 ) ;
#65904=CARTESIAN_POINT ( 'NONE',  ( 3.042071309553159519, 195.0520833299193271, 11.35316468750000141 ) ) ;
#65911=CARTESIAN_POINT ( 'NONE',  ( 11.35316468750000141, 80.78124999658602690, 0.000000000000000000 ) ) ;
#65918=CARTESIAN_POINT ( 'NONE',  ( -9.832129032723420536, 93.69791666325269830, 5.676582343749997150 ) ) ;
#65923=CARTESIAN_POINT ( 'NONE',  ( 5.000000000000018652, 75.83333333333335702, -8.660254037844415720 ) ) ;
#65925=CARTESIAN_POINT ( 'NONE',  ( -3.042071309553173730, 74.32291666325268409, 11.35316468749999785 ) ) ;
#65930=CARTESIAN_POINT ( 'NONE',  ( 7.320508075688774596, 162.4999999931720538, -7.320508075688774596 ) ) ;
#65933=CARTESIAN_POINT ( 'NONE',  ( -9.832129032723418760, 68.17708332991935549, -5.676582343750004256 ) ) ;
#65934=CARTESIAN_POINT ( 'NONE',  ( -6.676582343750001591, 293.4531250017069510, 0.000000000000000000 ) ) ;
#65936=CARTESIAN_POINT ( 'NONE',  ( -11.35316468750000141, 203.4895833299193271, 3.042071309553159963 ) ) ;
#65938=CARTESIAN_POINT ( 'NONE',  ( 0.000000000000000000, 300.0000000000000000, 0.000000000000000000 ) ) ;
#65942=CARTESIAN_POINT ( 'NONE',  ( 3.042071309553167513, 196.8229166632526983, -11.35316468749999785 ) ) ;
#65946=EDGE_CURVE ( 'NONE', #73838, #26730, #64260, .T. ) ;
#65950=CARTESIAN_POINT ( 'NONE',  ( -8.311093377946836114, 182.9687499965859843, -8.311093377946837890 ) ) ;
#65956=CARTESIAN_POINT ( 'NONE',  ( 5.000000000000001776, 5.833333333333333925, -8.660254037844389075 ) ) ;
#65962=ORIENTED_EDGE ( 'NONE', *, *, #67838, .T. ) ;
#65963=CARTESIAN_POINT ( 'NONE',  ( 6.000000000000001776, 293.5625000034140157, -7.347880794884121708E-16 ) ) ;
#65965=CARTESIAN_POINT ( 'NONE',  ( -10.00000000000011902, 82.70833333333339965, 2.679491924311253825 ) ) ;
#65973=ORIENTED_EDGE ( 'NONE', *, *, #570, .F. ) ;
#65975=CARTESIAN_POINT ( 'NONE',  ( -5.676582343749998039, 57.76041666325268409, -9.832129032723420536 ) ) ;
#65976=CARTESIAN_POINT ( 'NONE',  ( 8.660254037844389075, 92.29166665983871098, -5.000000000000000000 ) ) ;
#65980=CARTESIAN_POINT ( 'NONE',  ( 4.721056650415999201, 294.2343750017069510, -4.721056650415999201 ) ) ;
#65981=CARTESIAN_POINT ( 'NONE',  ( -2.679491924311225848, 146.4583333333332860, -10.00000000000000178 ) ) ;
#65998=CARTESIAN_POINT ( 'NONE',  ( -11.35316468750000141, 43.28124999658601268, -1.390361679473963753E-15 ) ) ;
#66000=CARTESIAN_POINT ( 'NONE',  ( -2.679491924311235618, 15.41666665983869855, 10.00000000000000000 ) ) ;
#66004=CARTESIAN_POINT ( 'NONE',  ( 6.951808397369818766E-16, 47.03124999658601979, -11.35316468750000141 ) ) ;
#66010=CARTESIAN_POINT ( 'NONE',  ( -8.311093377946836114, 32.65624999658600558, -8.311093377946837890 ) ) ;
#66013=CARTESIAN_POINT ( 'NONE',  ( 3.042071309553167069, 156.8229166632526983, -11.35316468749999785 ) ) ;
#66015=CARTESIAN_POINT ( 'NONE',  ( 2.679491924311228956, 132.9166666598386541, -10.00000000000000000 ) ) ;
#66019=CARTESIAN_POINT ( 'NONE',  ( 11.35316468749999785, 15.88541666325268409, 3.042071309553174174 ) ) ;
#66022=FACE_OUTER_BOUND ( 'NONE', #73401, .T. ) ;
#66026=CARTESIAN_POINT ( 'NONE',  ( -8.311093377946841443, 148.9062499965860127, 8.311093377946834337 ) ) ;
#66037=CARTESIAN_POINT ( 'NONE',  ( -1.836970198721029983E-15, 45.62499999317203958, 10.00000000000000178 ) ) ;
#66038=CARTESIAN_POINT ( 'NONE',  ( -9.832129032723420536, 109.0104166632526841, 5.676582343749997150 ) ) ;
#66042=ORIENTED_EDGE ( 'NONE', *, *, #50624, .F. ) ;
#66057=VECTOR ( 'NONE', #68241, 1000.000000000000000 ) ;
#66059=CARTESIAN_POINT ( 'NONE',  ( -2.765530957081998142, 298.6406250017069510, 6.676582343750000703 ) ) ;
#66062=ORIENTED_EDGE ( 'NONE', *, *, #33989, .T. ) ;
#66064=CARTESIAN_POINT ( 'NONE',  ( 8.660254037844387298, 124.5833333333333428, 5.000000000000006217 ) ) ;
#66068=CARTESIAN_POINT ( 'NONE',  ( -9.999999999999998224, 32.50000000000000000, -1.224646799147352862E-15 ) ) ;
#66069=CARTESIAN_POINT ( 'NONE',  ( -10.00000000000000355, 112.7083333333333428, 2.679491924311223183 ) ) ;
#66071=CARTESIAN_POINT ( 'NONE',  ( -6.676582343750000703, 297.6718750017070079, 2.765530957082001251 ) ) ;
#66074=CARTESIAN_POINT ( 'NONE',  ( -1.836970198721029983E-15, 175.6249999931720538, 10.00000000000000178 ) ) ;
#66077=CARTESIAN_POINT ( 'NONE',  ( 10.00000000000000178, 0.000000000000000000, 0.000000000000000000 ) ) ;
#66082=CARTESIAN_POINT ( 'NONE',  ( 11.35316468750000141, 5.781249996586016238, 0.000000000000000000 ) ) ;
#66084=CARTESIAN_POINT ( 'NONE',  ( 9.832129032723416984, 195.6770833299193839, 5.676582343750006032 ) ) ;
#66085=CARTESIAN_POINT ( 'NONE',  ( 10.00000000000000178, 191.8749999931720254, 0.000000000000000000 ) ) ;
#66089=CARTESIAN_POINT ( 'NONE',  ( 2.485281374238959895, 297.3125000000000000, 5.999999999999615419 ) ) ;
#66093=CARTESIAN_POINT ( 'NONE',  ( 5.676582343750001591, 46.92708332991934839, -9.832129032723420536 ) ) ;
#66101=CARTESIAN_POINT ( 'NONE',  ( 8.311093377946837890, 121.4062499965860127, -8.311093377946837890 ) ) ;
#66103=CARTESIAN_POINT ( 'NONE',  ( -2.679491924311225848, 88.33333332650535397, -10.00000000000000178 ) ) ;
#66107=DIRECTION ( 'NONE',  ( 0.000000000000000000, 0.000000000000000000, 1.000000000000000000 ) ) ;
#66111=CARTESIAN_POINT ( 'NONE',  ( 2.765530957081996366, 295.2968750017069510, -6.676582343750003368 ) ) ;
#66114=CARTESIAN_POINT ( 'NONE',  ( -11.35316468749999785, 168.0729166632526699, -3.042071309553167513 ) ) ;
#66121=CARTESIAN_POINT ( 'NONE',  ( -1.836970198721029983E-15, 155.6249999931720254, 10.00000000000000178 ) ) ;
#66122=CARTESIAN_POINT ( 'NONE',  ( 11.35316468749999785, 160.8854166632526699, 3.042071309553174174 ) ) ;
#66126=CARTESIAN_POINT ( 'NONE',  ( -11.35316468750000141, 63.59374999658601268, -1.390361679473963753E-15 ) ) ;
#66135=CARTESIAN_POINT ( 'NONE',  ( 4.242640687119287435, 288.4375000034140157, 4.242640687119285658 ) ) ;
#66155=CARTESIAN_POINT ( 'NONE',  ( -9.999999999999996447, 2.499999999999997780, -1.224646799147353059E-15 ) ) ;
#66159=CARTESIAN_POINT ( 'NONE',  ( -5.000000000000005329, 73.33333333333332860, 8.660254037844387298 ) ) ;
#66163=CARTESIAN_POINT ( 'NONE',  ( 2.485281374238571317, 294.6874999999999432, -6.000000000000003553 ) ) ;
#66174=CARTESIAN_POINT ( 'NONE',  ( 4.999999999999993783, 189.1666666666666856, 8.660254037844390851 ) ) ;
#66177=CARTESIAN_POINT ( 'NONE',  ( 11.35316468749999963, 161.3020833299193555, -3.042071309553165293 ) ) ;
#66184=CARTESIAN_POINT ( 'NONE',  ( 9.832129032723420536, 6.510416663252683200, -5.676582343749999815 ) ) ;
#66185=CARTESIAN_POINT ( 'NONE',  ( 2.679491924311222739, 95.83333332650535397, 10.00000000000000355 ) ) ;
#66187=CARTESIAN_POINT ( 'NONE',  ( 2.679491924311228956, 32.91666665983869677, -10.00000000000000000 ) ) ;
#66190=CARTESIAN_POINT ( 'NONE',  ( 6.123233995736767268E-16, 53.12499999317203958, -10.00000000000000178 ) ) ;
#66196=CARTESIAN_POINT ( 'NONE',  ( 2.679491924311375506, 158.9583333333333997, 9.999999999999939604 ) ) ;
#66202=CARTESIAN_POINT ( 'NONE',  ( -5.676582343749998039, 132.4479166632526983, -9.832129032723420536 ) ) ;
#66209=CARTESIAN_POINT ( 'NONE',  ( 10.00000000000002665, 45.20833333333334281, -2.679491924311233841 ) ) ;
#66210=CARTESIAN_POINT ( 'NONE',  ( 11.35316468749999963, 120.9895833299193555, -3.042071309553165293 ) ) ;
#66213=ADVANCED_FACE ( 'NONE', ( #63659 ), #69326, .T. ) ;
#66214=CARTESIAN_POINT ( 'NONE',  ( -1.836970198721029983E-15, 25.62499999317203248, 10.00000000000000178 ) ) ;
#66216=CARTESIAN_POINT ( 'NONE',  ( -3.042071309553163960, 97.55208332991934128, -11.35316468749999963 ) ) ;
#66220=CARTESIAN_POINT ( 'NONE',  ( -8.311093377946836114, 17.96874999658601979, -8.311093377946837890 ) ) ;
#66223=EDGE_CURVE ( 'NONE', #5520, #55260, #12696, .T. ) ;
#66230=CARTESIAN_POINT ( 'NONE',  ( 2.765530957082001251, 290.7656250017069510, 6.676582343750000703 ) ) ;
#66232=CARTESIAN_POINT ( 'NONE',  ( -6.362988438888832046E-13, 223.7499999999999147, 9.999999999999998224 ) ) ;
#66234=CARTESIAN_POINT ( 'NONE',  ( -3.042071309553164404, 137.5520833299193555, -11.35316468749999963 ) ) ;
#66245=CARTESIAN_POINT ( 'NONE',  ( -10.00000000000009770, 172.2916666666666856, -2.679491924311255602 ) ) ;
#66249=DIRECTION ( 'NONE',  ( -0.000000000000000000, 1.000000000000000000, -0.000000000000000000 ) ) ;
#66250=CARTESIAN_POINT ( 'NONE',  ( 5.676582343750001591, 191.6145833299193839, -9.832129032723420536 ) ) ;
#66253=CARTESIAN_POINT ( 'NONE',  ( -4.721056650415999201, 293.3281250017069510, -4.721056650415999201 ) ) ;
#66257=VECTOR ( 'NONE', #63486, 1000.000000000000000 ) ;
#66267=CARTESIAN_POINT ( 'NONE',  ( -2.085542519210945728E-15, 119.8437499965860269, 11.35316468750000141 ) ) ;
#66275=CARTESIAN_POINT ( 'NONE',  ( 11.35316468750000141, 225.7812499965860127, 0.000000000000000000 ) ) ;
#66279=CARTESIAN_POINT ( 'NONE',  ( -5.676582343750006032, 194.4270833299193839, 9.832129032723418760 ) ) ;
#66286=CARTESIAN_POINT ( 'NONE',  ( -3.042071309553164404, 82.23958332991935549, -11.35316468749999963 ) ) ;
#66288=EDGE_CURVE ( 'NONE', #53587, #17827, #5971, .T. ) ;
#66293=CYLINDRICAL_SURFACE ( 'NONE', #52154, 10.00000000000000178 ) ;
#66294=CARTESIAN_POINT ( 'NONE',  ( 11.35316468749999785, 90.57291666325268409, 3.042071309553174174 ) ) ;
#66302=CARTESIAN_POINT ( 'NONE',  ( 5.676582343750001591, 66.61458332991935549, -9.832129032723420536 ) ) ;
#66304=CARTESIAN_POINT ( 'NONE',  ( 10.00000000000000178, 130.0000000000000000, 0.000000000000000000 ) ) ;
#66306=CARTESIAN_POINT ( 'NONE',  ( 10.00000000000000000, 166.6666666598387110, 2.679491924311236062 ) ) ;
#66309=CARTESIAN_POINT ( 'NONE',  ( -8.311093377946841443, 59.21874999658601268, 8.311093377946834337 ) ) ;
#66310=CARTESIAN_POINT ( 'NONE',  ( -4.088227598258586603E-16, 293.2031250017069510, -6.676582343750001591 ) ) ;
#66312=CARTESIAN_POINT ( 'NONE',  ( 11.35316468749999785, 205.5729166632526699, 3.042071309553174174 ) ) ;
#66318=CARTESIAN_POINT ( 'NONE',  ( 5.676582343749993598, 194.9479166632526983, 9.832129032723422313 ) ) ;
#66321=DIRECTION ( 'NONE',  ( -0.000000000000000000, 1.000000000000000000, -0.000000000000000000 ) ) ;
#66322=ORIENTED_EDGE ( 'NONE', *, *, #34629, .T. ) ;
#66323=CARTESIAN_POINT ( 'NONE',  ( 8.311093377946837890, 181.7187499965859843, -8.311093377946837890 ) ) ;
#66326=CARTESIAN_POINT ( 'NONE',  ( -9.999999999999992895, 92.29166666666665719, -2.679491924311228068 ) ) ;
#66330=FACE_OUTER_BOUND ( 'NONE', #49507, .T. ) ;
#66349=EDGE_LOOP ( 'NONE', ( #24948, #10584, #47800, #35690 ) ) ;
#66351=CARTESIAN_POINT ( 'NONE',  ( 11.35316468750000141, 76.09374999658602690, 0.000000000000000000 ) ) ;
#66352=CARTESIAN_POINT ( 'NONE',  ( 7.320508075688774596, 92.49999999317203958, -7.320508075688774596 ) ) ;
#66356=CARTESIAN_POINT ( 'NONE',  ( 4.721056650415999201, 295.2343750017069510, -4.721056650415999201 ) ) ;
#66367=CARTESIAN_POINT ( 'NONE',  ( 1.224646799147353454E-15, 300.0000000000000000, -10.00000000000000178 ) ) ;
#66372=CARTESIAN_POINT ( 'NONE',  ( -9.832129032723418760, 42.86458332991935549, -5.676582343750004256 ) ) ;
#66374=CARTESIAN_POINT ( 'NONE',  ( 2.679491924311228956, 7.916666659838700326, -10.00000000000000000 ) ) ;
#66378=CARTESIAN_POINT ( 'NONE',  ( -5.676582343750006032, 54.11458332991934839, 9.832129032723418760 ) ) ;
#66385=CARTESIAN_POINT ( 'NONE',  ( -3.042071309553173730, 34.32291666325268409, 11.35316468749999785 ) ) ;
#66387=CARTESIAN_POINT ( 'NONE',  ( 0.000000000000000000, 300.0000000000000000, 0.000000000000000000 ) ) ;
#66388=CARTESIAN_POINT ( 'NONE',  ( -9.832129032723420536, 163.6979166632526983, 5.676582343749997150 ) ) ;
#66389=CARTESIAN_POINT ( 'NONE',  ( -2.679491924311235618, 135.4166666598386826, 10.00000000000000000 ) ) ;
#66394=CARTESIAN_POINT ( 'NONE',  ( 11.35316468749999963, 21.30208332991934839, -3.042071309553165293 ) ) ;
#66395=CARTESIAN_POINT ( 'NONE',  ( 1.224646799147353454E-15, 300.0000000000000000, -10.00000000000000178 ) ) ;
#66396=VERTEX_POINT ( 'NONE', #60607 ) ;
#66401=CARTESIAN_POINT ( 'NONE',  ( 3.042071309553159519, 149.7395833299193271, 11.35316468750000141 ) ) ;
#66409=CARTESIAN_POINT ( 'NONE',  ( -11.35316468750000141, 103.8020833299193413, 3.042071309553159963 ) ) ;
#66420=EDGE_CURVE ( 'NONE', #25788, #49698, #14944, .T. ) ;
#66426=AXIS2_PLACEMENT_3D ( 'NONE', #57052, #15917, #27616 ) ;
#66441=CARTESIAN_POINT ( 'NONE',  ( 10.00000000000007994, 60.00000000000004974, 0.000000000000000000 ) ) ;
#66442=CARTESIAN_POINT ( 'NONE',  ( 2.679491924311228956, 111.0416666666666572, -10.00000000000000000 ) ) ;
#66446=CARTESIAN_POINT ( 'NONE',  ( 6.676582343750003368, 292.1718750017070079, -2.765530957081997254 ) ) ;
#66450=FACE_OUTER_BOUND ( 'NONE', #34284, .T. ) ;
#66457=CARTESIAN_POINT ( 'NONE',  ( -11.35316468749999785, 3.072916663252683200, -3.042071309553167513 ) ) ;
#66459=CARTESIAN_POINT ( 'NONE',  ( 8.311093377946834337, 200.4687499965860411, 8.311093377946839666 ) ) ;
#66465=ORIENTED_EDGE ( 'NONE', *, *, #13614, .T. ) ;
#66467=CARTESIAN_POINT ( 'NONE',  ( -9.832129032723418760, 12.86458332991935194, -5.676582343750004256 ) ) ;
#66476=CARTESIAN_POINT ( 'NONE',  ( 3.042071309553159519, 124.7395833299193555, 11.35316468750000141 ) ) ;
#66477=CARTESIAN_POINT ( 'NONE',  ( -10.00000000000000355, 89.58333332650535397, 2.679491924311223183 ) ) ;
#66480=CARTESIAN_POINT ( 'NONE',  ( -2.679491924311235174, 200.4166666598386826, 10.00000000000000000 ) ) ;
#66481=CARTESIAN_POINT ( 'NONE',  ( -7.320508075688778149, 39.99999999317202537, 7.320508075688769267 ) ) ;
#66484=CARTESIAN_POINT ( 'NONE',  ( -6.676582343750000703, 294.6718750017070079, 2.765530957082001251 ) ) ;
#66486=CARTESIAN_POINT ( 'NONE',  ( -9.832129032723418760, 167.8645833299193555, -5.676582343750004256 ) ) ;
#66489=CARTESIAN_POINT ( 'NONE',  ( -10.00000000000004619, 192.5000000000000284, -1.224646799147358779E-15 ) ) ;
#66493=CARTESIAN_POINT ( 'NONE',  ( -3.042071309553163960, 157.5520833299193555, -11.35316468749999963 ) ) ;
#66494=CARTESIAN_POINT ( 'NONE',  ( -8.660254037844390851, 217.0833333333333428, -5.000000000000006217 ) ) ;
#66497=CARTESIAN_POINT ( 'NONE',  ( 8.311093377946837890, 56.71874999658601979, -8.311093377946837890 ) ) ;
#66503=CARTESIAN_POINT ( 'NONE',  ( -6.000000000000001776, 287.0625000034140157, 0.000000000000000000 ) ) ;
#66517=CARTESIAN_POINT ( 'NONE',  ( -4.242640687119286547, 289.8750000000000000, -4.242640687119286547 ) ) ;
#66527=CARTESIAN_POINT ( 'NONE',  ( -2.679491924311235618, 73.54166666666667140, 10.00000000000000000 ) ) ;
#66530=CARTESIAN_POINT ( 'NONE',  ( -6.000000000000003553, 290.9375000000000568, -2.485281374238571317 ) ) ;
#66532=CARTESIAN_POINT ( 'NONE',  ( -2.679491924311227624, 126.4583333333333428, -10.00000000000000711 ) ) ;
#66533=ORIENTED_EDGE ( 'NONE', *, *, #29509, .F. ) ;
#66543=CARTESIAN_POINT ( 'NONE',  ( 7.320508075688774596, 190.6250000000000284, -7.320508075688774596 ) ) ;
#66546=CARTESIAN_POINT ( 'NONE',  ( -9.832129032723418760, 153.1770833299193555, -5.676582343750004256 ) ) ;
#66553=CARTESIAN_POINT ( 'NONE',  ( -3.042071309553164404, 7.552083329919349275, -11.35316468749999963 ) ) ;
#66554=EDGE_CURVE ( 'NONE', #30602, #63756, #20389, .T. ) ;
#66561=CARTESIAN_POINT ( 'NONE',  ( 5.000000000000001776, 52.70833332650536818, -8.660254037844389075 ) ) ;
#66564=CARTESIAN_POINT ( 'NONE',  ( 9.999999999999985789, 100.2083333333333286, -2.679491924311223183 ) ) ;
#66567=CARTESIAN_POINT ( 'NONE',  ( 2.679491924311235174, 161.0416666666667140, -10.00000000000001954 ) ) ;
#66569=ORIENTED_EDGE ( 'NONE', *, *, #53918, .F. ) ;
#66573=CARTESIAN_POINT ( 'NONE',  ( -5.000000000000003553, 161.6666666666666856, -8.660254037844397956 ) ) ;
#66576=CARTESIAN_POINT ( 'NONE',  ( -9.832129032723420536, 123.6979166632526983, 5.676582343749997150 ) ) ;
#66583=DIRECTION ( 'NONE',  ( -0.000000000000000000, 1.000000000000000000, -0.000000000000000000 ) ) ;
#66585=CARTESIAN_POINT ( 'NONE',  ( 3.042071309553159519, 119.7395833299193555, 11.35316468750000141 ) ) ;
#66589=EDGE_CURVE ( 'NONE', #12039, #48053, #25884, .T. ) ;
#66591=CARTESIAN_POINT ( 'NONE',  ( -2.085542519210945728E-15, 114.8437499965860127, 11.35316468750000141 ) ) ;
#66595=CARTESIAN_POINT ( 'NONE',  ( -9.832129032723418760, 23.17708332991934839, -5.676582343750004256 ) ) ;
#66597=DIRECTION ( 'NONE',  ( -0.000000000000000000, 1.000000000000000000, -0.000000000000000000 ) ) ;
#66602=CARTESIAN_POINT ( 'NONE',  ( -6.676582343750003368, 289.3906250017069510, -2.765530957081996810 ) ) ;
#66605=ORIENTED_EDGE ( 'NONE', *, *, #57172, .T. ) ;
#66606=CARTESIAN_POINT ( 'NONE',  ( 5.676582343750001591, 146.9270833299193555, -9.832129032723420536 ) ) ;
#66620=CYLINDRICAL_SURFACE ( 'NONE', #14972, 10.00000000000000178 ) ;
#66622=CARTESIAN_POINT ( 'NONE',  ( -9.832129032723418760, 187.8645833299193839, -5.676582343750004256 ) ) ;
#66625=CARTESIAN_POINT ( 'NONE',  ( -6.676582343749999815, 287.5156250017069510, 2.765530957082001251 ) ) ;
#66639=CARTESIAN_POINT ( 'NONE',  ( 11.35316468750000141, 116.0937499965860127, 0.000000000000000000 ) ) ;
#66645=ORIENTED_EDGE ( 'NONE', *, *, #38365, .F. ) ;
#66647=CARTESIAN_POINT ( 'NONE',  ( -5.676582343749998039, 222.4479166632526983, -9.832129032723420536 ) ) ;
#66652=CARTESIAN_POINT ( 'NONE',  ( 11.35316468749999963, 191.3020833299193839, -3.042071309553165293 ) ) ;
#66655=CARTESIAN_POINT ( 'NONE',  ( 0.000000000000000000, 300.0000000000000000, 0.000000000000000000 ) ) ;
#66660=CARTESIAN_POINT ( 'NONE',  ( -11.35316468750000141, 83.28124999658602690, -1.390361679473963753E-15 ) ) ;
#66668=CARTESIAN_POINT ( 'NONE',  ( -11.35316468750000141, 93.48958332991934128, 3.042071309553159963 ) ) ;
#66676=CARTESIAN_POINT ( 'NONE',  ( 3.042071309553167513, 81.82291666325268409, -11.35316468749999785 ) ) ;
#66680=( BOUNDED_CURVE ( )  B_SPLINE_CURVE ( 2, ( #70977, #42301, #70612, #18932, #41938, #19292, #36291, #60027, #46862, #6878, #64946, #54008, #65318 ),
 .UNSPECIFIED., .F., .F. ) 
 B_SPLINE_CURVE_WITH_KNOTS ( ( 3, 2, 2, 2, 2, 2, 3 ),
 ( 0.5163043478260869179, 0.5181159420289854767, 0.5199275362318840354, 0.5217391304347825942, 0.5235507246376811530, 0.5253623188405797118, 0.5271739130434782705 ),
 .UNSPECIFIED. ) 
 CURVE ( )  GEOMETRIC_REPRESENTATION_ITEM ( )  RATIONAL_B_SPLINE_CURVE ( ( 1.000000000000000000, 0.9659258262890683122, 1.000000000000000000, 0.9659258262890683122, 1.000000000000000000, 0.9659258262890683122, 1.000000000000000000, 0.9659258262890683122, 1.000000000000000000, 0.9659258262890683122, 1.000000000000000000, 0.9659258262890683122, 1.000000000000000000 ) ) 
 REPRESENTATION_ITEM ( '' )  );
#66681=CARTESIAN_POINT ( 'NONE',  ( -5.000000000000005329, 165.2083333265053682, 8.660254037844387298 ) ) ;
#66683=CARTESIAN_POINT ( 'NONE',  ( 11.35316468750000141, 71.09374999658601268, 0.000000000000000000 ) ) ;
#66684=CARTESIAN_POINT ( 'NONE',  ( -2.765530957081998586, 292.6406250017070079, 6.676582343750001591 ) ) ;
#66687=CARTESIAN_POINT ( 'NONE',  ( -11.35316468749999785, 203.0729166632526415, -3.042071309553167513 ) ) ;
#66688=EDGE_LOOP ( 'NONE', ( #34702, #61713, #14812, #7887 ) ) ;
#66693=CARTESIAN_POINT ( 'NONE',  ( 9.832129032723416984, 200.3645833299193555, 5.676582343750006032 ) ) ;
#66697=FACE_OUTER_BOUND ( 'NONE', #27634, .T. ) ;
#66699=CARTESIAN_POINT ( 'NONE',  ( 11.35316468749999963, 176.3020833299193555, -3.042071309553165293 ) ) ;
#66703=ORIENTED_EDGE ( 'NONE', *, *, #42404, .F. ) ;
#66704=EDGE_CURVE ( 'NONE', #73838, #56251, #27388, .T. ) ;
#66719=CARTESIAN_POINT ( 'NONE',  ( -5.000000000000062172, 83.33333333333341386, 8.660254037844486774 ) ) ;
#66730=CARTESIAN_POINT ( 'NONE',  ( 11.35316468749999785, 80.88541666325269830, 3.042071309553174174 ) ) ;
#66734=CARTESIAN_POINT ( 'NONE',  ( 6.676582343750003368, 292.0468750017070079, 2.765530957081995478 ) ) ;
#66735=VECTOR ( 'NONE', #17634, 1000.000000000000114 ) ;
#66746=CARTESIAN_POINT ( 'NONE',  ( 6.123233995736767268E-16, 193.1249999931720254, -10.00000000000000178 ) ) ;
#66751=CARTESIAN_POINT ( 'NONE',  ( 3.042071309553159519, 44.73958332991936260, 11.35316468750000141 ) ) ;
#66754=CARTESIAN_POINT ( 'NONE',  ( 7.320508075688774596, 12.49999999317203425, -7.320508075688774596 ) ) ;
#66759=CARTESIAN_POINT ( 'NONE',  ( 8.311093377946834337, 55.15624999658601268, 8.311093377946839666 ) ) ;
#66765=CARTESIAN_POINT ( 'NONE',  ( -2.085542519210945728E-15, 49.53124999658601268, 11.35316468750000141 ) ) ;
#66768=CARTESIAN_POINT ( 'NONE',  ( 11.35316468749999785, 155.5729166632527267, 3.042071309553174174 ) ) ;
#66769=CARTESIAN_POINT ( 'NONE',  ( 7.320508075688771044, 126.2499999931720538, 7.320508075688775484 ) ) ;
#66772=CARTESIAN_POINT ( 'NONE',  ( 0.000000000000000000, 300.0000000000000000, 0.000000000000000000 ) ) ;
#66773=CARTESIAN_POINT ( 'NONE',  ( -5.676582343749998039, 32.76041666325269119, -9.832129032723420536 ) ) ;
#66774=CARTESIAN_POINT ( 'NONE',  ( -1.183492779173324630E-13, 16.25000000000001066, -10.00000000000000178 ) ) ;
#66780=CARTESIAN_POINT ( 'NONE',  ( 8.311093377946837890, 146.4062499965860127, -8.311093377946837890 ) ) ;
#66787=EDGE_CURVE ( 'NONE', #64770, #62806, #73789, .T. ) ;
#66789=CARTESIAN_POINT ( 'NONE',  ( 5.676582343750001591, 101.9270833299193555, -9.832129032723420536 ) ) ;
#66790=( BOUNDED_CURVE ( )  B_SPLINE_CURVE ( 2, ( #17312, #18064, #5637, #6751, #29754, #47091, #58078, #51275, #16938, #34323, #11660, #74285, #69004 ),
 .UNSPECIFIED., .F., .F. ) 
 B_SPLINE_CURVE_WITH_KNOTS ( ( 3, 2, 2, 2, 2, 2, 3 ),
 ( 0.04891304347826086474, 0.05072463768115941657, 0.05253623188405796146, 0.05434782608695651329, 0.05615942028985507206, 0.05797101449275362389, 0.05978260869565217572 ),
 .UNSPECIFIED. ) 
 CURVE ( )  GEOMETRIC_REPRESENTATION_ITEM ( )  RATIONAL_B_SPLINE_CURVE ( ( 1.000000000000000000, 0.9659258262890682012, 1.000000000000000000, 0.9659258262890683122, 1.000000000000000000, 0.9659258262890683122, 1.000000000000000000, 0.9659258262890683122, 1.000000000000000000, 0.9659258262890683122, 1.000000000000000000, 0.9659258262890683122, 1.000000000000000000 ) ) 
 REPRESENTATION_ITEM ( '' )  );
#66796=AXIS2_PLACEMENT_3D ( 'NONE', #17091, #40113, #29540 ) ;
#66814=CARTESIAN_POINT ( 'NONE',  ( 0.000000000000000000, 255.9999999999999432, 10.00000000000000178 ) ) ;
#66816=CARTESIAN_POINT ( 'NONE',  ( -6.676582343750002480, 299.3906250017069510, -2.765530957081996810 ) ) ;
#66820=ORIENTED_EDGE ( 'NONE', *, *, #27605, .F. ) ;
#66822=CARTESIAN_POINT ( 'NONE',  ( 4.999999999999994671, 124.1666666666666714, 8.660254037844392627 ) ) ;
#66827=CARTESIAN_POINT ( 'NONE',  ( 2.679491924311222739, 108.9583333333333144, 10.00000000000000355 ) ) ;
#66829=CARTESIAN_POINT ( 'NONE',  ( -2.765530957081998586, 290.7968750017069510, 6.676582343750001591 ) ) ;
#66841=CARTESIAN_POINT ( 'NONE',  ( -10.00000000000000355, 94.58333332650535397, 2.679491924311223183 ) ) ;
#66842=CARTESIAN_POINT ( 'NONE',  ( 4.999999999999993783, 224.1666666666666856, 8.660254037844390851 ) ) ;
#66844=CARTESIAN_POINT ( 'NONE',  ( 5.676582343750001591, 191.9270833299193555, -9.832129032723420536 ) ) ;
#66852=CARTESIAN_POINT ( 'NONE',  ( -11.35316468750000141, 13.48958332991935016, 3.042071309553159963 ) ) ;
#66858=CARTESIAN_POINT ( 'NONE',  ( -11.35316468750000141, 128.4895833299193555, 3.042071309553159963 ) ) ;
#66859=CARTESIAN_POINT ( 'NONE',  ( 6.123233995736767268E-16, 83.12499999317203958, -10.00000000000000178 ) ) ;
#66866=CARTESIAN_POINT ( 'NONE',  ( 2.765530957082001251, 287.9218750017069510, 6.676582343750000703 ) ) ;
#66870=CARTESIAN_POINT ( 'NONE',  ( 7.320508075688771044, 206.2499999931720254, 7.320508075688775484 ) ) ;
#66879=CARTESIAN_POINT ( 'NONE',  ( -11.35316468750000141, 158.8020833299193555, 3.042071309553159963 ) ) ;
#66880=CARTESIAN_POINT ( 'NONE',  ( -5.000000000000007105, 218.3333333333333428, 8.660254037844390851 ) ) ;
#66883=CARTESIAN_POINT ( 'NONE',  ( 11.35316468750000141, 61.09374999658602690, 0.000000000000000000 ) ) ;
#66884=ORIENTED_EDGE ( 'NONE', *, *, #16361, .F. ) ;
#66890=CARTESIAN_POINT ( 'NONE',  ( 1.102182119232618108E-15, 289.3125000034140157, 6.000000000000001776 ) ) ;
#66913=CARTESIAN_POINT ( 'NONE',  ( 8.660254037844389075, 65.41666666666667140, -5.000000000000000000 ) ) ;
#66915=CARTESIAN_POINT ( 'NONE',  ( -4.242640687119285658, 292.1249999999999432, 4.242640687119287435 ) ) ;
#66917=ORIENTED_EDGE ( 'NONE', *, *, #66589, .F. ) ;
#66918=CARTESIAN_POINT ( 'NONE',  ( 1.224646799147353454E-15, 300.0000000000000000, -10.00000000000000178 ) ) ;
#66927=CARTESIAN_POINT ( 'NONE',  ( -8.660254037844390851, 182.9166666666666856, 4.999999999999998224 ) ) ;
#66930=CARTESIAN_POINT ( 'NONE',  ( -2.085542519210945728E-15, 154.8437499965860127, 11.35316468750000141 ) ) ;
#66936=CARTESIAN_POINT ( 'NONE',  ( 3.042071309553159519, 25.05208332991934483, 11.35316468750000141 ) ) ;
#66942=CARTESIAN_POINT ( 'NONE',  ( 4.999999999999993783, 51.04166665983870388, 8.660254037844390851 ) ) ;
#66945=CARTESIAN_POINT ( 'NONE',  ( 4.999999999999993783, 100.8333333333333428, -8.660254037844376640 ) ) ;
#66948=CARTESIAN_POINT ( 'NONE',  ( 10.00000000000001954, 159.7916666666666856, 2.679491924311241835 ) ) ;
#66949=ORIENTED_EDGE ( 'NONE', *, *, #22503, .F. ) ;
#66950=EDGE_LOOP ( 'NONE', ( #15494, #69710, #53217, #35927 ) ) ;
#66951=CARTESIAN_POINT ( 'NONE',  ( -6.362988438888832046E-13, 223.7499999999999147, 9.999999999999998224 ) ) ;
#66954=CARTESIAN_POINT ( 'NONE',  ( -2.085542519210945728E-15, 129.5312499965860127, 11.35316468750000141 ) ) ;
#66962=CARTESIAN_POINT ( 'NONE',  ( -9.832129032723420536, 123.6979166632526983, 5.676582343749997150 ) ) ;
#66967=CARTESIAN_POINT ( 'NONE',  ( -8.311093377946841443, 114.2187499965860127, 8.311093377946834337 ) ) ;
#66971=CARTESIAN_POINT ( 'NONE',  ( -5.676582343750006032, 24.42708332991935194, 9.832129032723418760 ) ) ;
#66979=CARTESIAN_POINT ( 'NONE',  ( -4.242640687119286547, 298.9375000034140157, -4.242640687119286547 ) ) ;
#66981=CARTESIAN_POINT ( 'NONE',  ( 1.224646799147353454E-15, 300.0000000000000000, -10.00000000000000178 ) ) ;
#66985=CARTESIAN_POINT ( 'NONE',  ( 9.832129032723420536, 141.5104166632526699, -5.676582343749999815 ) ) ;
#67002=CARTESIAN_POINT ( 'NONE',  ( 3.042071309553159519, 184.7395833299193839, 11.35316468750000141 ) ) ;
#67005=CARTESIAN_POINT ( 'NONE',  ( -6.676582343749999815, 289.5156250017070647, 2.765530957082001251 ) ) ;
#67015=( BOUNDED_CURVE ( )  B_SPLINE_CURVE ( 2, ( #17212, #13753, #59443, #64727, #64360, #58348, #18707, #7018, #29655, #19429, #36797, #30395, #6653 ),
 .UNSPECIFIED., .F., .F. ) 
 B_SPLINE_CURVE_WITH_KNOTS ( ( 3, 2, 2, 2, 2, 2, 3 ),
 ( 0.7692923867907990321, 0.7745262106001035152, 0.7797600344094078872, 0.7849938582187123703, 0.7902276820280168534, 0.7954615058373213365, 0.8006953296466258196 ),
 .UNSPECIFIED. ) 
 CURVE ( )  GEOMETRIC_REPRESENTATION_ITEM ( )  RATIONAL_B_SPLINE_CURVE ( ( 0.9999999999998058220, 0.9659258262892623792, 1.000000000000000000, 0.9659258262890682012, 1.000000000000000000, 0.9659258262890682012, 1.000000000000000000, 0.9659258262890682012, 1.000000000000000000, 0.9659258262890682012, 1.000000000000000000, 0.9659258262890682012, 1.000000000000000000 ) ) 
 REPRESENTATION_ITEM ( '' )  );
#67020=CARTESIAN_POINT ( 'NONE',  ( -11.35316468750000141, 113.5937499965860127, -1.390361679473963753E-15 ) ) ;
#67027=CARTESIAN_POINT ( 'NONE',  ( 4.805230186056123287, 224.1490657562575848, 8.774718480194076520 ) ) ;
#67029=CARTESIAN_POINT ( 'NONE',  ( 3.042071309553167069, 221.8229166632527267, -11.35316468749999785 ) ) ;
#67033=CARTESIAN_POINT ( 'NONE',  ( -9.832129032723418760, 203.1770833299193555, -5.676582343750004256 ) ) ;
#67040=CARTESIAN_POINT ( 'NONE',  ( -2.085542519210945728E-15, 89.53124999658602690, 11.35316468750000141 ) ) ;
#67046=CARTESIAN_POINT ( 'NONE',  ( 11.35316468749999963, 90.98958332991935549, -3.042071309553165293 ) ) ;
#67053=CARTESIAN_POINT ( 'NONE',  ( 6.123233995736767268E-16, 3.124999993172032919, -10.00000000000000178 ) ) ;
#67056=CARTESIAN_POINT ( 'NONE',  ( 9.832129032723420536, 81.19791666325269830, -5.676582343749999815 ) ) ;
#67061=CARTESIAN_POINT ( 'NONE',  ( 7.320508075688774596, 187.4999999931719969, -7.320508075688774596 ) ) ;
#67063=CARTESIAN_POINT ( 'NONE',  ( -11.35316468750000141, 73.80208332991934128, 3.042071309553159963 ) ) ;
#67064=CARTESIAN_POINT ( 'NONE',  ( 6.676582343750001591, 294.9531250017069510, -8.176455196517173205E-16 ) ) ;
#67066=CARTESIAN_POINT ( 'NONE',  ( -3.042071309553173730, 209.3229166632526983, 11.35316468749999785 ) ) ;
#67072=CARTESIAN_POINT ( 'NONE',  ( 11.35316468749999785, 200.5729166632526983, 3.042071309553174174 ) ) ;
#67077=CARTESIAN_POINT ( 'NONE',  ( 9.832129032723420536, 196.5104166632526983, -5.676582343749999815 ) ) ;
#67086=CARTESIAN_POINT ( 'NONE',  ( 4.999999999999993783, 14.16666666666666785, 8.660254037844390851 ) ) ;
#67104=ORIENTED_EDGE ( 'NONE', *, *, #60839, .F. ) ;
#67107=CARTESIAN_POINT ( 'NONE',  ( -8.311093377946836114, 72.96874999658602690, -8.311093377946837890 ) ) ;
#67112=CARTESIAN_POINT ( 'NONE',  ( -6.676582343750001591, 290.6093750017069510, 0.000000000000000000 ) ) ;
#67116=( BOUNDED_CURVE ( )  B_SPLINE_CURVE ( 2, ( #25113, #70059, #65489, #59110, #13781, #36825, #2492, #47398, #25485, #29686, #71505, #52702, #24016 ),
 .UNSPECIFIED., .F., .F. ) 
 B_SPLINE_CURVE_WITH_KNOTS ( ( 3, 2, 2, 2, 2, 2, 3 ),
 ( 0.6358695652173913526, 0.6376811594202898004, 0.6394927536231883591, 0.6413043478260869179, 0.6431159420289855877, 0.6449275362318841465, 0.6467391304347827052 ),
 .UNSPECIFIED. ) 
 CURVE ( )  GEOMETRIC_REPRESENTATION_ITEM ( )  RATIONAL_B_SPLINE_CURVE ( ( 1.000000000000000000, 0.9659258262890683122, 1.000000000000000000, 0.9659258262890683122, 1.000000000000000000, 0.9659258262890683122, 1.000000000000000000, 0.9659258262890683122, 1.000000000000000000, 0.9659258262890683122, 1.000000000000000000, 0.9659258262890662028, 1.000000000000001998 ) ) 
 REPRESENTATION_ITEM ( '' )  );
#67122=CARTESIAN_POINT ( 'NONE',  ( -11.35316468749999785, 168.3854166632526699, -3.042071309553167513 ) ) ;
#67125=CARTESIAN_POINT ( 'NONE',  ( 4.242640687119285658, 289.6875000034139589, -4.242640687119286547 ) ) ;
#67130=CARTESIAN_POINT ( 'NONE',  ( 8.311093377946837890, 41.40624999658601268, -8.311093377946837890 ) ) ;
#67132=CARTESIAN_POINT ( 'NONE',  ( 8.660254037844385522, 21.45833332650536818, 5.000000000000005329 ) ) ;
#67134=ORIENTED_EDGE ( 'NONE', *, *, #60839, .T. ) ;
#67139=CARTESIAN_POINT ( 'NONE',  ( -9.832129032723418760, 42.86458332991934839, -5.676582343750004256 ) ) ;
#67145=CARTESIAN_POINT ( 'NONE',  ( 6.951808397369818766E-16, 52.03124999658601979, -11.35316468750000141 ) ) ;
#67149=CARTESIAN_POINT ( 'NONE',  ( 11.35316468749999963, 160.9895833299193839, -3.042071309553165293 ) ) ;
#67150=( BOUNDED_CURVE ( )  B_SPLINE_CURVE ( 2, ( #42816, #8130, #13762, #43567, #71484, #9248, #19810, #66209, #3977, #60176, #65833, #32270, #31515 ),
 .UNSPECIFIED., .F., .F. ) 
 B_SPLINE_CURVE_WITH_KNOTS ( ( 3, 2, 2, 2, 2, 2, 3 ),
 ( 0.5494935699762487635, 0.5547273339465774722, 0.5599610979169062919, 0.5651948618872351116, 0.5704286258575639312, 0.5756623898278927509, 0.5808961537982215706 ),
 .UNSPECIFIED. ) 
 CURVE ( )  GEOMETRIC_REPRESENTATION_ITEM ( )  RATIONAL_B_SPLINE_CURVE ( ( 1.000000000000000000, 0.9659258262890683122, 1.000000000000000000, 0.9659258262890683122, 1.000000000000000000, 0.9659258262890683122, 1.000000000000000000, 0.9659258262890683122, 1.000000000000000000, 0.9659258262890683122, 1.000000000000000000, 0.9659258262890693114, 0.9999999999999990008 ) ) 
 REPRESENTATION_ITEM ( '' )  );
#67151=CARTESIAN_POINT ( 'NONE',  ( -10.00000000000000355, 144.5833333265053398, 2.679491924311223183 ) ) ;
#67154=CARTESIAN_POINT ( 'NONE',  ( 8.311093377946834337, 30.46874999658601979, 8.311093377946839666 ) ) ;
#67155=EDGE_CURVE ( 'NONE', #19205, #16317, #31665, .T. ) ;
#67156=CARTESIAN_POINT ( 'NONE',  ( -7.320508075688779925, 16.87500000000000355, -7.320508075688779925 ) ) ;
#67161=CARTESIAN_POINT ( 'NONE',  ( -7.320508075688779037, 6.875000000000002665, -7.320508075688779925 ) ) ;
#67162=CARTESIAN_POINT ( 'NONE',  ( 11.35316468749999963, 165.9895833299193271, -3.042071309553165293 ) ) ;
#67168=ORIENTED_EDGE ( 'NONE', *, *, #66223, .T. ) ;
#67169=AXIS2_PLACEMENT_3D ( 'NONE', #56001, #39013, #50688 ) ;
#67170=CARTESIAN_POINT ( 'NONE',  ( -8.660254037844387298, 118.9583333265053824, -5.000000000000004441 ) ) ;
#67171=FACE_OUTER_BOUND ( 'NONE', #2387, .T. ) ;
#67172=CARTESIAN_POINT ( 'NONE',  ( -5.676582343749998039, 117.7604166632526841, -9.832129032723420536 ) ) ;
#67187=ORIENTED_EDGE ( 'NONE', *, *, #66704, .T. ) ;
#67193=CARTESIAN_POINT ( 'NONE',  ( -4.721056650415998313, 298.5781250017069510, 4.721056650416000089 ) ) ;
#67195=ORIENTED_EDGE ( 'NONE', *, *, #22503, .T. ) ;
#67202=CARTESIAN_POINT ( 'NONE',  ( 2.679491924297558114, 61.04166666666794328, -10.00000000000798472 ) ) ;
#67203=CARTESIAN_POINT ( 'NONE',  ( -10.00000000000000178, 112.5000000000000000, -1.224646799147353454E-15 ) ) ;
#67205=CARTESIAN_POINT ( 'NONE',  ( 2.765530957082001251, 293.9218750017069510, 6.676582343750000703 ) ) ;
#67219=CARTESIAN_POINT ( 'NONE',  ( 11.35316468749999785, 5.572916663252682312, 3.042071309553174174 ) ) ;
#67222=CARTESIAN_POINT ( 'NONE',  ( 11.35316468750000141, 206.0937499965860411, 0.000000000000000000 ) ) ;
#67230=CARTESIAN_POINT ( 'NONE',  ( -8.311093377946841443, 13.90624999658601801, 8.311093377946830785 ) ) ;
#67234=CARTESIAN_POINT ( 'NONE',  ( 7.347880794884121708E-16, 300.0000000000000000, -6.000000000000001776 ) ) ;
#67236=CARTESIAN_POINT ( 'NONE',  ( -3.042071309553163960, 7.239583329919349275, -11.35316468749999963 ) ) ;
#67239=CARTESIAN_POINT ( 'NONE',  ( 9.832129032723420536, 116.1979166632526841, -5.676582343749999815 ) ) ;
#67240=CARTESIAN_POINT ( 'NONE',  ( 7.320508075688771044, 86.24999999317205379, 7.320508075688775484 ) ) ;
#67244=CARTESIAN_POINT ( 'NONE',  ( 2.679491924318150975, 146.0416666666660603, -9.999999999996013855 ) ) ;
#67247=( BOUNDED_CURVE ( )  B_SPLINE_CURVE ( 2, ( #16298, #44999, #63084, #39338, #39703, #62335, #74404, #34445, #67640, #22712, #5752, #56700, #57444 ),
 .UNSPECIFIED., .F., .F. ) 
 B_SPLINE_CURVE_WITH_KNOTS ( ( 3, 2, 2, 2, 2, 2, 3 ),
 ( 1.428688857047360816, 1.433922811121159269, 1.439156765194957721, 1.444390719268755952, 1.449624673342554404, 1.454858627416352856, 1.460092581490151309 ),
 .UNSPECIFIED. ) 
 CURVE ( )  GEOMETRIC_REPRESENTATION_ITEM ( )  RATIONAL_B_SPLINE_CURVE ( ( 0.9999999999999998890, 0.9659258262890682012, 0.9999999999999998890, 0.9659258262890682012, 0.9999999999999998890, 0.9659258262890682012, 0.9999999999999998890, 0.9659258262890682012, 0.9999999999999998890, 0.9659258262890682012, 0.9999999999999998890, 0.9659258262891224911, 0.9999999999999455991 ) ) 
 REPRESENTATION_ITEM ( '' )  );
#67249=CARTESIAN_POINT ( 'NONE',  ( -2.765530957081996810, 289.4218750017069510, -6.676582343750003368 ) ) ;
#67253=CARTESIAN_POINT ( 'NONE',  ( -10.00000000000000355, 204.5833333265053966, 2.679491924311223183 ) ) ;
#67256=ORIENTED_EDGE ( 'NONE', *, *, #74038, .T. ) ;
#67258=CARTESIAN_POINT ( 'NONE',  ( 8.311093377946834337, 150.4687499965860127, 8.311093377946839666 ) ) ;
#67259=DIRECTION ( 'NONE',  ( -0.000000000000000000, 1.000000000000000000, 0.000000000000000000 ) ) ;
#67262=CARTESIAN_POINT ( 'NONE',  ( 3.042071309553159519, 70.05208332991934128, 11.35316468750000141 ) ) ;
#67268=CARTESIAN_POINT ( 'NONE',  ( 6.000000000000001776, 287.5625000034140157, -7.347880794884121708E-16 ) ) ;
#67273=VECTOR ( 'NONE', #32637, 1000.000000000000000 ) ;
#67290=CARTESIAN_POINT ( 'NONE',  ( 10.00000000000000178, 70.00000000000000000, 0.000000000000000000 ) ) ;
#67292=CARTESIAN_POINT ( 'NONE',  ( 2.485281374238575314, 293.3124999999999432, 6.000000000000000888 ) ) ;
#67294=ORIENTED_EDGE ( 'NONE', *, *, #2306, .T. ) ;
#67296=EDGE_CURVE ( 'NONE', #413, #512, #55995, .T. ) ;
#67304=CARTESIAN_POINT ( 'NONE',  ( 2.679491924311222739, 188.9583333333332860, 10.00000000000000355 ) ) ;
#67305=B_SPLINE_CURVE_WITH_KNOTS ( 'NONE', 3,
 ( #47755, #59832, #53068, #54552 ),
 .UNSPECIFIED., .F., .F.,
 ( 4, 4 ),
 ( 0.000000000000000000, 0.004469278299739564905 ),
 .UNSPECIFIED. ) ;
#67308=CARTESIAN_POINT ( 'NONE',  ( -5.676582343750006032, 149.4270833299193555, 9.832129032723418760 ) ) ;
#67312=DIRECTION ( 'NONE',  ( -0.000000000000000000, 1.000000000000000000, -0.000000000000000000 ) ) ;
#67316=CARTESIAN_POINT ( 'NONE',  ( 5.676582343750001591, 26.92708332991935194, -9.832129032723420536 ) ) ;
#67322=CARTESIAN_POINT ( 'NONE',  ( -10.00000000000000355, 49.58333332650536107, 2.679491924311223183 ) ) ;
#67327=CARTESIAN_POINT ( 'NONE',  ( 4.999999999999993783, 164.1666666666666856, 8.660254037844390851 ) ) ;
#67334=CARTESIAN_POINT ( 'NONE',  ( -8.311093377946836114, 142.6562499965860127, -8.311093377946837890 ) ) ;
#67341=CARTESIAN_POINT ( 'NONE',  ( -8.311093377946836114, 127.6562499965860411, -8.311093377946837890 ) ) ;
#67345=CARTESIAN_POINT ( 'NONE',  ( -11.35316468749999785, 113.3854166632526983, -3.042071309553167957 ) ) ;
#67349=CARTESIAN_POINT ( 'NONE',  ( 9.832129032723420536, 16.51041666325268054, -5.676582343749999815 ) ) ;
#67356=CARTESIAN_POINT ( 'NONE',  ( -2.765530957081996810, 288.2656250017069510, -6.676582343750003368 ) ) ;
#67357=LINE ( 'NONE', #66981, #26889 ) ;
#67360=( BOUNDED_CURVE ( )  B_SPLINE_CURVE ( 2, ( #65293, #47567, #70234, #18542, #6490, #843, #25291, #24190, #12864, #1209, #2294, #47202, #13598 ),
 .UNSPECIFIED., .F., .F. ) 
 B_SPLINE_CURVE_WITH_KNOTS ( ( 3, 2, 2, 2, 2, 2, 3 ),
 ( 0.8750000000000000000, 0.8768115942028985588, 0.8786231884057971175, 0.8804347826086955653, 0.8822463768115941241, 0.8840579710144926828, 0.8858695652173912416 ),
 .UNSPECIFIED. ) 
 CURVE ( )  GEOMETRIC_REPRESENTATION_ITEM ( )  RATIONAL_B_SPLINE_CURVE ( ( 1.000000000000000000, 0.9659258262890683122, 1.000000000000000000, 0.9659258262890683122, 1.000000000000000000, 0.9659258262890683122, 1.000000000000000000, 0.9659258262890683122, 1.000000000000000000, 0.9659258262890683122, 1.000000000000000000, 0.9659258262890704216, 0.9999999999999978906 ) ) 
 REPRESENTATION_ITEM ( '' )  );
#67361=CARTESIAN_POINT ( 'NONE',  ( -11.35316468749999785, 138.3854166632526983, -3.042071309553167513 ) ) ;
#67378=CARTESIAN_POINT ( 'NONE',  ( 11.35316468749999785, 185.5729166632526983, 3.042071309553174174 ) ) ;
#67381=CYLINDRICAL_SURFACE ( 'NONE', #65901, 10.00000000000000178 ) ;
#67382=ORIENTED_EDGE ( 'NONE', *, *, #23812, .T. ) ;
#67390=CARTESIAN_POINT ( 'NONE',  ( -8.660254037844390851, 142.9166666666666572, 4.999999999999998224 ) ) ;
#67394=CARTESIAN_POINT ( 'NONE',  ( -11.35316468749999785, 118.3854166632526557, -3.042071309553167513 ) ) ;
#67400=ORIENTED_EDGE ( 'NONE', *, *, #35813, .T. ) ;
#67401=EDGE_CURVE ( 'NONE', #49815, #52317, #16339, .T. ) ;
#67404=CARTESIAN_POINT ( 'NONE',  ( 6.000000000000001776, 287.5625000034140157, -7.347880794884121708E-16 ) ) ;
#67408=CARTESIAN_POINT ( 'NONE',  ( 11.35316468750000141, 206.0937499965860411, 0.000000000000000000 ) ) ;
#67409=FACE_OUTER_BOUND ( 'NONE', #50121, .T. ) ;
#67410=CARTESIAN_POINT ( 'NONE',  ( 0.000000000000000000, 300.0000000000000000, 0.000000000000000000 ) ) ;
#67415=CARTESIAN_POINT ( 'NONE',  ( 5.676582343750001591, 101.6145833299193697, -9.832129032723420536 ) ) ;
#67421=CARTESIAN_POINT ( 'NONE',  ( -8.311093377946836114, 92.65624999658602690, -8.311093377946837890 ) ) ;
#67423=CARTESIAN_POINT ( 'NONE',  ( 7.320508075688771044, 206.2499999931720254, 7.320508075688775484 ) ) ;
#67431=CARTESIAN_POINT ( 'NONE',  ( 9.832129032723420536, 91.19791666325269830, -5.676582343749999815 ) ) ;
#67436=CARTESIAN_POINT ( 'NONE',  ( -4.999999999999998224, 183.5416666598387110, -8.660254037844389075 ) ) ;
#67438=CARTESIAN_POINT ( 'NONE',  ( -8.311093377946841443, 79.21874999658601268, 8.311093377946834337 ) ) ;
#67439=CARTESIAN_POINT ( 'NONE',  ( 2.765530957082001251, 292.7656250017069510, 6.676582343750000703 ) ) ;
#67441=CARTESIAN_POINT ( 'NONE',  ( -8.311093377946841443, 213.9062499965860411, 8.311093377946830785 ) ) ;
#67447=CARTESIAN_POINT ( 'NONE',  ( 8.311093377946837890, 211.4062499965860127, -8.311093377946837890 ) ) ;
#67449=CYLINDRICAL_SURFACE ( 'NONE', #56508, 10.00000000000000178 ) ;
#67451=CARTESIAN_POINT ( 'NONE',  ( 9.832129032723416984, 190.6770833299193555, 5.676582343750006032 ) ) ;
#67458=CARTESIAN_POINT ( 'NONE',  ( -7.320508075688778149, 8.125000000000000000, 7.320508075688769267 ) ) ;
#67467=VECTOR ( 'NONE', #50702, 1000.000000000000000 ) ;
#67468=ORIENTED_EDGE ( 'NONE', *, *, #9436, .T. ) ;
#67471=LINE ( 'NONE', #61057, #56705 ) ;
#67481=CARTESIAN_POINT ( 'NONE',  ( -9.832129032723418760, 78.17708332991935549, -5.676582343750004256 ) ) ;
#67482=CARTESIAN_POINT ( 'NONE',  ( 0.000000000000000000, 300.0000000000000000, 0.000000000000000000 ) ) ;
#67486=CARTESIAN_POINT ( 'NONE',  ( -4.721056650415998313, 291.7343750017069510, 4.721056650416000089 ) ) ;
#67496=CARTESIAN_POINT ( 'NONE',  ( 5.676582343750001591, 161.9270833299193555, -9.832129032723420536 ) ) ;
#67498=CARTESIAN_POINT ( 'NONE',  ( -8.660254037844390851, 19.79166665983870033, 4.999999999999998224 ) ) ;
#67503=CARTESIAN_POINT ( 'NONE',  ( 8.311093377946834337, 60.15624999658601979, 8.311093377946839666 ) ) ;
#67505=CARTESIAN_POINT ( 'NONE',  ( -4.999999999999998224, 28.54166665983870033, -8.660254037844389075 ) ) ;
#67509=CARTESIAN_POINT ( 'NONE',  ( -7.320508075688778149, 169.9999999931720254, 7.320508075688769267 ) ) ;
#67510=CARTESIAN_POINT ( 'NONE',  ( 11.35316468749999785, 50.57291666325268409, 3.042071309553174174 ) ) ;
#67515=CARTESIAN_POINT ( 'NONE',  ( 3.042071309553167513, 46.82291666325268409, -11.35316468749999785 ) ) ;
#67518=CARTESIAN_POINT ( 'NONE',  ( -5.676582343749998039, 177.4479166632526983, -9.832129032723420536 ) ) ;
#67520=CARTESIAN_POINT ( 'NONE',  ( 4.999999999999993783, 146.0416666598387110, 8.660254037844390851 ) ) ;
#67523=CARTESIAN_POINT ( 'NONE',  ( -11.35316468750000141, 28.59374999658601624, -1.390361679473963753E-15 ) ) ;
#67530=CARTESIAN_POINT ( 'NONE',  ( 11.35316468749999785, 170.5729166632526983, 3.042071309553174174 ) ) ;
#67540=EDGE_CURVE ( 'NONE', #33017, #61626, #21283, .T. ) ;
#67542=CARTESIAN_POINT ( 'NONE',  ( 8.311093377946834337, 110.4687499965860127, 8.311093377946839666 ) ) ;
#67563=AXIS2_PLACEMENT_3D ( 'NONE', #22646, #788, #45666 ) ;
#67575=CARTESIAN_POINT ( 'NONE',  ( 6.123233995736767268E-16, 126.2500000000000000, -10.00000000000000178 ) ) ;
#67577=CARTESIAN_POINT ( 'NONE',  ( 4.721056650415999201, 293.2343750017069510, -4.721056650415999201 ) ) ;
#67593=CARTESIAN_POINT ( 'NONE',  ( 6.951808397369818766E-16, 12.03124999658601801, -11.35316468750000141 ) ) ;
#67595=CARTESIAN_POINT ( 'NONE',  ( -5.676582343749998039, 207.7604166632526983, -9.832129032723420536 ) ) ;
#67602=CARTESIAN_POINT ( 'NONE',  ( 11.35316468749999963, 10.98958332991935016, -3.042071309553165293 ) ) ;
#67608=CARTESIAN_POINT ( 'NONE',  ( 9.832129032723420536, 11.19791666325268409, -5.676582343749999815 ) ) ;
#67610=CARTESIAN_POINT ( 'NONE',  ( 3.042071309553159519, 119.7395833299193413, 11.35316468750000141 ) ) ;
#67612=CARTESIAN_POINT ( 'NONE',  ( -5.000000000000005329, 100.2083333265053682, 8.660254037844387298 ) ) ;
#67620=CARTESIAN_POINT ( 'NONE',  ( 1.226468279477575784E-15, 288.8593750017070079, 6.676582343750001591 ) ) ;
#67629=CARTESIAN_POINT ( 'NONE',  ( 9.832129032723416984, 150.6770833299193555, 5.676582343750006032 ) ) ;
#67634=CARTESIAN_POINT ( 'NONE',  ( -9.832129032723420536, 79.01041666325268409, 5.676582343749997150 ) ) ;
#67638=ORIENTED_EDGE ( 'NONE', *, *, #71663, .T. ) ;
#67640=CARTESIAN_POINT ( 'NONE',  ( 8.660254037844389075, 115.4166666666666998, -5.000000000000000000 ) ) ;
#67645=CARTESIAN_POINT ( 'NONE',  ( 2.679491924311221407, 108.9583333333333286, 10.00000000000000000 ) ) ;
#67664=CARTESIAN_POINT ( 'NONE',  ( 10.00000000000000000, 84.79166666666667140, 2.679491924311236062 ) ) ;
#67667=CARTESIAN_POINT ( 'NONE',  ( 6.000000000000001776, 291.5000000000000000, -7.347880794884121708E-16 ) ) ;
#67673=CARTESIAN_POINT ( 'NONE',  ( 10.00000000000000000, 56.66666665983869677, 2.679491924311235618 ) ) ;
#67679=CARTESIAN_POINT ( 'NONE',  ( 2.679491924311222739, 193.9583333333333428, 10.00000000000000355 ) ) ;
#67682=CARTESIAN_POINT ( 'NONE',  ( 5.676582343750001591, 161.9270833299193555, -9.832129032723420536 ) ) ;
#67689=CARTESIAN_POINT ( 'NONE',  ( 5.676582343749993598, 20.26041666325268409, 9.832129032723422313 ) ) ;
#67695=CARTESIAN_POINT ( 'NONE',  ( 2.679491924311222739, 55.83333332650535397, 10.00000000000000355 ) ) ;
#67696=VECTOR ( 'NONE', #42280, 1000.000000000000000 ) ;
#67699=CARTESIAN_POINT ( 'NONE',  ( -2.664923566518097392E-11, 208.7499999999979252, 10.00000000000000178 ) ) ;
#67706=CARTESIAN_POINT ( 'NONE',  ( -2.679491924310502871, 163.5416666666667425, 10.00000000000043343 ) ) ;
#67708=CARTESIAN_POINT ( 'NONE',  ( 8.311093377946837890, 141.4062499965860127, -8.311093377946837890 ) ) ;
#67720=CARTESIAN_POINT ( 'NONE',  ( -3.042071309553163960, 112.5520833299193413, -11.35316468749999963 ) ) ;
#67724=CARTESIAN_POINT ( 'NONE',  ( 8.311093377946834337, 30.46874999658601979, 8.311093377946839666 ) ) ;
#67732=CARTESIAN_POINT ( 'NONE',  ( 2.765530957081996366, 289.1406250017069510, -6.676582343750003368 ) ) ;
#67735=VERTEX_POINT ( 'NONE', #68942 ) ;
#67738=CARTESIAN_POINT ( 'NONE',  ( 3.042071309553159519, 140.0520833299193271, 11.35316468750000141 ) ) ;
#67754=LINE ( 'NONE', #61343, #8957 ) ;
#67755=CARTESIAN_POINT ( 'NONE',  ( 5.676582343750001591, 181.6145833299193555, -9.832129032723420536 ) ) ;
#67757=LINE ( 'NONE', #43611, #19654 ) ;
#67759=CARTESIAN_POINT ( 'NONE',  ( 1.459323541827198180E-11, 81.24999999999886313, -10.00000000000000533 ) ) ;
#67760=ORIENTED_EDGE ( 'NONE', *, *, #38096, .F. ) ;
#67767=CARTESIAN_POINT ( 'NONE',  ( 2.679491924311222739, 148.9583333333333144, 10.00000000000000355 ) ) ;
#67771=CARTESIAN_POINT ( 'NONE',  ( -11.35316468750000141, 128.8020833299193555, 3.042071309553159963 ) ) ;
#67779=CARTESIAN_POINT ( 'NONE',  ( 9.770781909996177461, 224.8281321452039379, 2.149070136972248246 ) ) ;
#67780=DIRECTION ( 'NONE',  ( -0.000000000000000000, 1.000000000000000000, -0.000000000000000000 ) ) ;
#67783=CARTESIAN_POINT ( 'NONE',  ( -9.832129032723420536, 204.0104166632526983, 5.676582343749997150 ) ) ;
#67790=CARTESIAN_POINT ( 'NONE',  ( -11.35316468749999785, 93.07291666325266988, -3.042071309553167513 ) ) ;
#67796=CARTESIAN_POINT ( 'NONE',  ( 11.35316468750000141, 105.7812499965860269, 0.000000000000000000 ) ) ;
#67797=ORIENTED_EDGE ( 'NONE', *, *, #57729, .T. ) ;
#67804=CARTESIAN_POINT ( 'NONE',  ( 3.042071309553159519, 84.73958332991936970, 11.35316468750000141 ) ) ;
#67807=( BOUNDED_CURVE ( )  B_SPLINE_CURVE ( 2, ( #19948, #31657, #24505, #47509, #14280, #8643, #70898, #7900, #47879, #19213, #42218, #65230, #36573 ),
 .UNSPECIFIED., .F., .F. ) 
 B_SPLINE_CURVE_WITH_KNOTS ( ( 3, 2, 2, 2, 2, 2, 3 ),
 ( 0.4836956521739130266, 0.4855072463768115854, 0.4873188405797101441, 0.4891304347826087029, 0.4909420289855072617, 0.4927536231884058204, 0.4945652173913043237 ),
 .UNSPECIFIED. ) 
 CURVE ( )  GEOMETRIC_REPRESENTATION_ITEM ( )  RATIONAL_B_SPLINE_CURVE ( ( 1.000000000000000000, 0.9659258262890683122, 1.000000000000000000, 0.9659258262890683122, 1.000000000000000000, 0.9659258262890683122, 1.000000000000000000, 0.9659258262890683122, 1.000000000000000000, 0.9659258262890683122, 1.000000000000000000, 0.9659258262890683122, 1.000000000000000000 ) ) 
 REPRESENTATION_ITEM ( '' )  );
#67808=CARTESIAN_POINT ( 'NONE',  ( 8.660254037844385522, 176.4583333265053682, 5.000000000000005329 ) ) ;
#67810=CARTESIAN_POINT ( 'NONE',  ( 8.311093377946834337, 80.46874999658601268, 8.311093377946839666 ) ) ;
#67811=CARTESIAN_POINT ( 'NONE',  ( -6.676582343750000703, 289.5156250017070647, 2.765530957082001251 ) ) ;
#67813=CARTESIAN_POINT ( 'NONE',  ( 5.676582343749993598, 224.9479166632526983, 9.832129032723422313 ) ) ;
#67817=CARTESIAN_POINT ( 'NONE',  ( 2.485281374238878627, 291.3125000000000000, 5.999999999999694467 ) ) ;
#67818=CARTESIAN_POINT ( 'NONE',  ( 3.042071309553167513, 201.8229166632526415, -11.35316468749999785 ) ) ;
#67822=CARTESIAN_POINT ( 'NONE',  ( 8.311093377946834337, 190.4687499965860411, 8.311093377946839666 ) ) ;
#67830=CARTESIAN_POINT ( 'NONE',  ( -2.679491924311235618, 13.54166666666666785, 10.00000000000000000 ) ) ;
#67838=EDGE_CURVE ( 'NONE', #59649, #55260, #3254, .T. ) ;
#67846=VERTEX_POINT ( 'NONE', #55319 ) ;
#67849=CARTESIAN_POINT ( 'NONE',  ( -11.35316468750000141, 68.80208332991935549, 3.042071309553159963 ) ) ;
#67854=CARTESIAN_POINT ( 'NONE',  ( 6.676582343750002480, 290.1718750017070079, -2.765530957081997254 ) ) ;
#67862=CARTESIAN_POINT ( 'NONE',  ( -8.311093377946841443, 164.2187499965860411, 8.311093377946830785 ) ) ;
#67865=CARTESIAN_POINT ( 'NONE',  ( -4.999999999999995559, 206.6666666666667425, -8.660254037844385522 ) ) ;
#67870=CARTESIAN_POINT ( 'NONE',  ( -5.676582343750006032, 59.11458332991935549, 9.832129032723418760 ) ) ;
#67872=CARTESIAN_POINT ( 'NONE',  ( -2.679491924311235618, 20.41666665983870033, 10.00000000000000000 ) ) ;
#67878=CARTESIAN_POINT ( 'NONE',  ( 11.35316468750000141, 60.78124999658601979, 0.000000000000000000 ) ) ;
#67884=CARTESIAN_POINT ( 'NONE',  ( 3.042071309553167513, 41.82291666325269119, -11.35316468749999785 ) ) ;
#67886=CARTESIAN_POINT ( 'NONE',  ( 2.679491924311375950, 206.0416666666666572, -9.999999999999911182 ) ) ;
#67887=CARTESIAN_POINT ( 'NONE',  ( -9.832129032723420536, 168.6979166632526983, 5.676582343749997150 ) ) ;
#67888=CARTESIAN_POINT ( 'NONE',  ( 8.660254037844385522, 146.4583333265053682, 5.000000000000005329 ) ) ;
#67891=CARTESIAN_POINT ( 'NONE',  ( -11.35316468750000141, 38.59374999658601979, -1.390361679473963753E-15 ) ) ;
#67892=( BOUNDED_CURVE ( )  B_SPLINE_CURVE ( 2, ( #27973, #50977, #39664, #33278, #72503, #38180, #55541, #55914, #20812, #9514, #21925, #27214, #61184 ),
 .UNSPECIFIED., .F., .F. ) 
 B_SPLINE_CURVE_WITH_KNOTS ( ( 3, 2, 2, 2, 2, 2, 3 ),
 ( 0.5706521739130434590, 0.5724637681159420177, 0.5742753623188405765, 0.5760869565217391353, 0.5778985507246376940, 0.5797101449275362528, 0.5815217391304348116 ),
 .UNSPECIFIED. ) 
 CURVE ( )  GEOMETRIC_REPRESENTATION_ITEM ( )  RATIONAL_B_SPLINE_CURVE ( ( 1.000000000000000000, 0.9659258262890683122, 1.000000000000000000, 0.9659258262890683122, 1.000000000000000000, 0.9659258262890683122, 1.000000000000000000, 0.9659258262890683122, 1.000000000000000000, 0.9659258262890683122, 1.000000000000000000, 0.9659258262890683122, 1.000000000000000000 ) ) 
 REPRESENTATION_ITEM ( '' )  );
#67893=CARTESIAN_POINT ( 'NONE',  ( 6.000000000000003553, 295.5000000034139589, 2.485281374238571317 ) ) ;
#67894=CARTESIAN_POINT ( 'NONE',  ( 9.832129032723416984, 165.3645833299193555, 5.676582343750006032 ) ) ;
#67901=CARTESIAN_POINT ( 'NONE',  ( -3.042071309553173730, 169.3229166632526699, 11.35316468749999785 ) ) ;
#67909=CARTESIAN_POINT ( 'NONE',  ( 1.567784982238203817E-13, 73.75000000000002842, 10.00000000000000533 ) ) ;
#67910=CARTESIAN_POINT ( 'NONE',  ( -11.35316468750000141, 113.5937499965860127, -1.390361679473963753E-15 ) ) ;
#67914=ORIENTED_EDGE ( 'NONE', *, *, #17826, .F. ) ;
#67943=CARTESIAN_POINT ( 'NONE',  ( -10.00000000000000888, 127.5000000000000000, -1.224646799147354243E-15 ) ) ;
#67944=CARTESIAN_POINT ( 'NONE',  ( -2.679491924311235618, 123.5416666666666572, 10.00000000000000000 ) ) ;
#67958=CARTESIAN_POINT ( 'NONE',  ( -2.679491924311300011, 93.33333332650538239, -9.999999999999959144 ) ) ;
#67960=CARTESIAN_POINT ( 'NONE',  ( 3.042071309553159519, 9.739583329919350163, 11.35316468750000141 ) ) ;
#67962=CARTESIAN_POINT ( 'NONE',  ( -3.042071309553164404, 212.5520833299193839, -11.35316468749999963 ) ) ;
#67968=CARTESIAN_POINT ( 'NONE',  ( -11.35316468750000141, 13.28124999658601624, -1.390361679473963753E-15 ) ) ;
#67974=CARTESIAN_POINT ( 'NONE',  ( 3.042071309553167513, 1.822916663252682756, -11.35316468749999785 ) ) ;
#67976=CARTESIAN_POINT ( 'NONE',  ( -9.832129032723420536, 138.6979166632526983, 5.676582343749997150 ) ) ;
#67977=CARTESIAN_POINT ( 'NONE',  ( 4.999999999999993783, 106.0416666598387110, 8.660254037844390851 ) ) ;
#67981=CARTESIAN_POINT ( 'NONE',  ( -8.660254037844387298, 38.95833332650536818, -5.000000000000004441 ) ) ;
#67984=CARTESIAN_POINT ( 'NONE',  ( 4.721056650416000089, 288.9843750017070079, 4.721056650415999201 ) ) ;
#67993=CARTESIAN_POINT ( 'NONE',  ( -5.676582343750006032, 164.4270833299193555, 9.832129032723418760 ) ) ;
#67996=CARTESIAN_POINT ( 'NONE',  ( 3.042071309553159519, 80.05208332991935549, 11.35316468750000141 ) ) ;
#68006=( BOUNDED_CURVE ( )  B_SPLINE_CURVE ( 2, ( #1906, #46443, #58162, #6827, #24894, #47176, #47911, #17394, #69461, #18883, #40418, #63416, #52118 ),
 .UNSPECIFIED., .F., .F. ) 
 B_SPLINE_CURVE_WITH_KNOTS ( ( 3, 2, 2, 2, 2, 2, 3 ),
 ( 1.899690555530577418, 1.904923638444253831, 1.910156721357930021, 1.915389804271605989, 1.920622887185282401, 1.925855970098958592, 1.931089053012635004 ),
 .UNSPECIFIED. ) 
 CURVE ( )  GEOMETRIC_REPRESENTATION_ITEM ( )  RATIONAL_B_SPLINE_CURVE ( ( 1.000000000000022871, 0.9659258262890453306, 1.000000000000000000, 0.9659258262890683122, 1.000000000000000000, 0.9659258262890683122, 1.000000000000000000, 0.9659258262890683122, 1.000000000000000000, 0.9659258262890683122, 1.000000000000000000, 0.9659258262888135160, 1.000000000000254685 ) ) 
 REPRESENTATION_ITEM ( '' )  );
#68013=CARTESIAN_POINT ( 'NONE',  ( 0.000000000000000000, 300.0000000000000000, 0.000000000000000000 ) ) ;
#68014=ORIENTED_EDGE ( 'NONE', *, *, #25630, .T. ) ;
#68031=CARTESIAN_POINT ( 'NONE',  ( -2.679491924311225848, 76.45833333333331439, -10.00000000000000178 ) ) ;
#68034=CARTESIAN_POINT ( 'NONE',  ( -6.000000000000001776, 293.0000000000000000, 0.000000000000000000 ) ) ;
#68039=EDGE_CURVE ( 'NONE', #5538, #51786, #20844, .T. ) ;
#68047=CARTESIAN_POINT ( 'NONE',  ( 2.679491924311228956, 196.0416666666666856, -10.00000000000000000 ) ) ;
#68050=CARTESIAN_POINT ( 'NONE',  ( -9.832129032723420536, 174.0104166632526983, 5.676582343749997150 ) ) ;
#68051=CARTESIAN_POINT ( 'NONE',  ( -8.660254037844389075, 37.91666666666667140, 4.999999999999996447 ) ) ;
#68054=CARTESIAN_POINT ( 'NONE',  ( 10.00000000000000178, 87.08333332650535397, -2.679491924311226736 ) ) ;
#68056=CARTESIAN_POINT ( 'NONE',  ( 6.951808397369818766E-16, 17.34374999658601624, -11.35316468750000141 ) ) ;
#68063=CARTESIAN_POINT ( 'NONE',  ( -7.320508075688773708, 63.74999999317202537, -7.320508075688774596 ) ) ;
#68070=ORIENTED_EDGE ( 'NONE', *, *, #58248, .T. ) ;
#68072=CARTESIAN_POINT ( 'NONE',  ( -5.000000000000052403, 196.6666666666667140, -8.660254037844479669 ) ) ;
#68074=CARTESIAN_POINT ( 'NONE',  ( -8.660254037844396180, 162.0833333333333712, -5.000000000000009770 ) ) ;
#68077=CARTESIAN_POINT ( 'NONE',  ( -9.832129032723420536, 143.6979166632526699, 5.676582343749997150 ) ) ;
#68085=EDGE_CURVE ( 'NONE', #64051, #54774, #69229, .T. ) ;
#68087=ORIENTED_EDGE ( 'NONE', *, *, #68445, .T. ) ;
#68090=CARTESIAN_POINT ( 'NONE',  ( 5.676582343750001591, 126.9270833299193697, -9.832129032723420536 ) ) ;
#68094=EDGE_CURVE ( 'NONE', #23868, #51437, #69602, .T. ) ;
#68095=CARTESIAN_POINT ( 'NONE',  ( 6.951808397369818766E-16, 32.34374999658601268, -11.35316468750000141 ) ) ;
#68101=CARTESIAN_POINT ( 'NONE',  ( 4.242640687119287435, 298.4375000034140157, 4.242640687119285658 ) ) ;
#68102=CARTESIAN_POINT ( 'NONE',  ( -1.836970198721029983E-15, 110.6249999931720396, 10.00000000000000178 ) ) ;
#68104=CARTESIAN_POINT ( 'NONE',  ( 8.311093377946837890, 151.7187499965860127, -8.311093377946837890 ) ) ;
#68120=CARTESIAN_POINT ( 'NONE',  ( -10.00000000000000178, 37.50000000000000711, -1.224646799147353454E-15 ) ) ;
#68124=CARTESIAN_POINT ( 'NONE',  ( 5.000000000000000000, 35.83333333333333570, -8.660254037844385522 ) ) ;
#68132=CARTESIAN_POINT ( 'NONE',  ( 6.123233995736767268E-16, 138.1249999931720538, -10.00000000000000178 ) ) ;
#68133=CARTESIAN_POINT ( 'NONE',  ( -10.00000000000000000, 162.2916666666666288, -2.679491924311229845 ) ) ;
#68137=CARTESIAN_POINT ( 'NONE',  ( 9.832129032723416984, 130.6770833299193555, 5.676582343750006032 ) ) ;
#68144=CARTESIAN_POINT ( 'NONE',  ( 0.2954385633113796872, 223.7729706610164726, 10.00000000000001776 ) ) ;
#68145=CARTESIAN_POINT ( 'NONE',  ( 6.123233995736767268E-16, 148.1249999931720538, -10.00000000000000178 ) ) ;
#68148=CARTESIAN_POINT ( 'NONE',  ( 3.042071309553167069, 202.1354166632526983, -11.35316468749999785 ) ) ;
#68154=CARTESIAN_POINT ( 'NONE',  ( -9.832129032723420536, 88.69791666325268409, 5.676582343749997150 ) ) ;
#68155=ORIENTED_EDGE ( 'NONE', *, *, #43137, .T. ) ;
#68160=CARTESIAN_POINT ( 'NONE',  ( -8.311093377946841443, 103.9062499965860269, 8.311093377946830785 ) ) ;
#68164=CARTESIAN_POINT ( 'NONE',  ( -10.00000000000000178, 214.3749999931720538, -1.224646799147353454E-15 ) ) ;
#68168=CARTESIAN_POINT ( 'NONE',  ( -3.042071309553163960, 92.23958332991935549, -11.35316468749999963 ) ) ;
#68175=CARTESIAN_POINT ( 'NONE',  ( -2.679491924311225848, 178.3333333265053966, -10.00000000000000178 ) ) ;
#68179=CARTESIAN_POINT ( 'NONE',  ( 8.311093377946834337, 75.46874999658602690, 8.311093377946839666 ) ) ;
#68180=CARTESIAN_POINT ( 'NONE',  ( 1.226468279477575784E-15, 288.7031250017069510, 6.676582343750001591 ) ) ;
#68184=CARTESIAN_POINT ( 'NONE',  ( 11.35316468749999963, 1.302083329919349941, -3.042071309553165293 ) ) ;
#68189=CARTESIAN_POINT ( 'NONE',  ( -9.832129032723420536, 203.6979166632526983, 5.676582343749997150 ) ) ;
#68192=CARTESIAN_POINT ( 'NONE',  ( -4.721056650415999201, 297.3281250017069510, -4.721056650415999201 ) ) ;
#68194=CARTESIAN_POINT ( 'NONE',  ( -11.35316468750000141, 193.5937499965860127, -1.390361679473963753E-15 ) ) ;
#68200=CARTESIAN_POINT ( 'NONE',  ( -8.660254037844387298, 12.08333333333333570, -5.000000000000004441 ) ) ;
#68209=CARTESIAN_POINT ( 'NONE',  ( 2.679491924311370177, 150.8333333265053398, 9.999999999999918288 ) ) ;
#68214=ORIENTED_EDGE ( 'NONE', *, *, #68039, .T. ) ;
#68221=CARTESIAN_POINT ( 'NONE',  ( 8.311093377946834337, 85.46874999658599847, 8.311093377946839666 ) ) ;
#68226=CARTESIAN_POINT ( 'NONE',  ( -6.676582343750001591, 289.6093750017069510, 0.000000000000000000 ) ) ;
#68229=CARTESIAN_POINT ( 'NONE',  ( -11.35316468750000141, 198.4895833299193555, 3.042071309553159963 ) ) ;
#68238=CARTESIAN_POINT ( 'NONE',  ( -9.832129032723418760, 163.1770833299193839, -5.676582343750004256 ) ) ;
#68241=DIRECTION ( 'NONE',  ( -0.000000000000000000, 1.000000000000000000, -0.000000000000000000 ) ) ;
#68245=CARTESIAN_POINT ( 'NONE',  ( 6.951808397369818766E-16, 57.03124999658601268, -11.35316468750000141 ) ) ;
#68250=CARTESIAN_POINT ( 'NONE',  ( -2.679491924311382611, 170.4166666598386826, 9.999999999999914735 ) ) ;
#68251=CARTESIAN_POINT ( 'NONE',  ( 6.951808397369818766E-16, 62.03124999658601979, -11.35316468750000141 ) ) ;
#68257=CARTESIAN_POINT ( 'NONE',  ( -11.35316468749999785, 48.07291666325268409, -3.042071309553167957 ) ) ;
#68260=CARTESIAN_POINT ( 'NONE',  ( 11.35316468750000141, 175.7812499965860411, 0.000000000000000000 ) ) ;
#68261=CARTESIAN_POINT ( 'NONE',  ( 10.00000000000000178, 137.0833333265053966, -2.679491924311226736 ) ) ;
#68264=CARTESIAN_POINT ( 'NONE',  ( 9.832129032723416984, 40.67708332991935549, 5.676582343750006032 ) ) ;
#68266=CARTESIAN_POINT ( 'NONE',  ( 5.676582343749993598, 184.9479166632526983, 9.832129032723422313 ) ) ;
#68273=CARTESIAN_POINT ( 'NONE',  ( 8.311093377946834337, 165.1562499965860127, 8.311093377946839666 ) ) ;
#68282=CARTESIAN_POINT ( 'NONE',  ( 11.35316468750000141, 121.0937499965860269, 0.000000000000000000 ) ) ;
#68309=CIRCLE ( 'NONE', #56256, 15.99999999999998579 ) ;
#68312=CARTESIAN_POINT ( 'NONE',  ( 1.224646799147353454E-15, 300.0000000000000000, -10.00000000000000178 ) ) ;
#68313=CARTESIAN_POINT ( 'NONE',  ( 8.660254037844385522, 119.5833333333333428, 5.000000000000005329 ) ) ;
#68316=CARTESIAN_POINT ( 'NONE',  ( -6.676582343750000703, 288.6718750017069510, 2.765530957082001251 ) ) ;
#68326=CARTESIAN_POINT ( 'NONE',  ( -10.00000000000000000, 94.16666665983869677, -2.679491924311229845 ) ) ;
#68329=CARTESIAN_POINT ( 'NONE',  ( -8.311093377946836114, 17.65624999658601979, -8.311093377946837890 ) ) ;
#68331=CARTESIAN_POINT ( 'NONE',  ( 8.311093377946837890, 206.7187499965859843, -8.311093377946837890 ) ) ;
#68332=CARTESIAN_POINT ( 'NONE',  ( 5.676582343750001591, 1.614583329919349497, -9.832129032723420536 ) ) ;
#68333=CARTESIAN_POINT ( 'NONE',  ( -8.660254037844390851, 219.7916666598387110, 4.999999999999998224 ) ) ;
#68335=FACE_OUTER_BOUND ( 'NONE', #21073, .T. ) ;
#68339=ADVANCED_FACE ( 'NONE', ( #8072 ), #19378, .T. ) ;
#68340=CARTESIAN_POINT ( 'NONE',  ( 6.951808397369818766E-16, 17.03124999658601624, -11.35316468750000141 ) ) ;
#68347=CARTESIAN_POINT ( 'NONE',  ( 6.951808397369818766E-16, 132.0312499965860127, -11.35316468750000141 ) ) ;
#68350=CARTESIAN_POINT ( 'NONE',  ( 10.00000000000000178, 97.08333332650536818, -2.679491924311226736 ) ) ;
#68355=EDGE_LOOP ( 'NONE', ( #12217, #67382, #59529, #33416 ) ) ;
#68359=CARTESIAN_POINT ( 'NONE',  ( -2.765530957081998586, 287.7968750017070079, 6.676582343750001591 ) ) ;
#68361=DIRECTION ( 'NONE',  ( -0.000000000000000000, 1.000000000000000000, -0.000000000000000000 ) ) ;
#68362=EDGE_CURVE ( 'NONE', #29110, #23989, #42025, .T. ) ;
#68368=CARTESIAN_POINT ( 'NONE',  ( -9.832129032723418760, 73.17708332991934128, -5.676582343750004256 ) ) ;
#68392=CARTESIAN_POINT ( 'NONE',  ( -5.394762896564973355E-12, 18.74999999999958433, 10.00000000000000178 ) ) ;
#68398=CARTESIAN_POINT ( 'NONE',  ( -8.660254037844387298, 82.08333333333334281, -5.000000000000004441 ) ) ;
#68401=CARTESIAN_POINT ( 'NONE',  ( -6.000000000000000888, 289.0625000000000000, 2.485281374238575758 ) ) ;
#68406=CARTESIAN_POINT ( 'NONE',  ( 4.999999999999993783, 56.04166665983870388, 8.660254037844390851 ) ) ;
#68409=CARTESIAN_POINT ( 'NONE',  ( -2.679491924311318662, 78.54166666666668561, 9.999999999999994671 ) ) ;
#68410=CARTESIAN_POINT ( 'NONE',  ( -5.000000000000005329, 203.3333333333333428, 8.660254037844387298 ) ) ;
#68412=CARTESIAN_POINT ( 'NONE',  ( -11.35316468750000141, 168.5937499965860127, -1.390361679473963753E-15 ) ) ;
#68413=CARTESIAN_POINT ( 'NONE',  ( -2.679491924310609452, 38.54166666666672114, 10.00000000000036060 ) ) ;
#68416=DIRECTION ( 'NONE',  ( 0.000000000000000000, 0.000000000000000000, 1.000000000000000000 ) ) ;
#68419=CARTESIAN_POINT ( 'NONE',  ( -5.676582343749998039, 27.76041666325268409, -9.832129032723420536 ) ) ;
#68422=CARTESIAN_POINT ( 'NONE',  ( 10.00000000000000178, 221.8749999931720254, 0.000000000000000000 ) ) ;
#68426=CARTESIAN_POINT ( 'NONE',  ( 8.660254037844389075, 57.29166665983870388, -5.000000000000000000 ) ) ;
#68429=CARTESIAN_POINT ( 'NONE',  ( 2.679491924305834605, 213.9583333333329733, 10.00000000000336797 ) ) ;
#68437=CARTESIAN_POINT ( 'NONE',  ( -3.042071309553164404, 137.2395833299193271, -11.35316468749999963 ) ) ;
#68439=CARTESIAN_POINT ( 'NONE',  ( 2.679491924311372841, 106.0416666666666572, -9.999999999999898748 ) ) ;
#68443=CYLINDRICAL_SURFACE ( 'NONE', #32852, 10.00000000000000178 ) ;
#68445=EDGE_CURVE ( 'NONE', #71352, #64324, #7855, .T. ) ;
#68453=CARTESIAN_POINT ( 'NONE',  ( 3.042071309553167513, 127.1354166632526699, -11.35316468749999785 ) ) ;
#68457=CARTESIAN_POINT ( 'NONE',  ( 8.311093377946837890, 41.71874999658601979, -8.311093377946837890 ) ) ;
#68460=CARTESIAN_POINT ( 'NONE',  ( -7.320508075688778149, 194.9999999931720538, 7.320508075688769267 ) ) ;
#68465=CARTESIAN_POINT ( 'NONE',  ( 6.000000000000001776, 297.5625000034140157, -7.347880794884121708E-16 ) ) ;
#68468=CARTESIAN_POINT ( 'NONE',  ( -9.832129032723420536, 159.0104166632526983, 5.676582343749997150 ) ) ;
#68480=ORIENTED_EDGE ( 'NONE', *, *, #39625, .F. ) ;
#68484=CARTESIAN_POINT ( 'NONE',  ( 2.679491924311222739, 43.95833333333333570, 10.00000000000000355 ) ) ;
#68488=CARTESIAN_POINT ( 'NONE',  ( 2.485281374238575314, 299.3125000000001137, 6.000000000000000888 ) ) ;
#68490=CARTESIAN_POINT ( 'NONE',  ( 7.320508075688854532, 79.37500000000007105, 7.320508075688858085 ) ) ;
#68500=EDGE_CURVE ( 'NONE', #3122, #48612, #43519, .T. ) ;
#68501=CARTESIAN_POINT ( 'NONE',  ( -10.00000000000000355, 167.7083333333333428, 2.679491924311223183 ) ) ;
#68505=CARTESIAN_POINT ( 'NONE',  ( -8.311093377946836114, 132.9687499965860411, -8.311093377946837890 ) ) ;
#68517=CARTESIAN_POINT ( 'NONE',  ( 6.951808397369818766E-16, 212.3437499965860411, -11.35316468750000141 ) ) ;
#68524=CARTESIAN_POINT ( 'NONE',  ( -8.311093377946841443, 93.90624999658599847, 8.311093377946830785 ) ) ;
#68526=DIRECTION ( 'NONE',  ( 0.000000000000000000, 0.000000000000000000, 1.000000000000000000 ) ) ;
#68530=CARTESIAN_POINT ( 'NONE',  ( -9.832129032723418760, 107.8645833299193555, -5.676582343750004256 ) ) ;
#68534=CARTESIAN_POINT ( 'NONE',  ( -5.000000000000005329, 215.2083333265053682, 8.660254037844387298 ) ) ;
#68538=CARTESIAN_POINT ( 'NONE',  ( 11.35316468749999963, 105.9895833299193413, -3.042071309553165293 ) ) ;
#68543=CARTESIAN_POINT ( 'NONE',  ( 8.660254037844385522, 181.4583333265053682, 5.000000000000005329 ) ) ;
#68548=CARTESIAN_POINT ( 'NONE',  ( -3.042071309553173730, 89.63541666325266988, 11.35316468749999785 ) ) ;
#68549=CARTESIAN_POINT ( 'NONE',  ( 2.765530957082001251, 290.7656250017069510, 6.676582343750000703 ) ) ;
#68552=CARTESIAN_POINT ( 'NONE',  ( 8.311093377946837890, 216.4062499965860127, -8.311093377946837890 ) ) ;
#68557=CARTESIAN_POINT ( 'NONE',  ( 11.35316468749999785, 225.5729166632526983, 3.042071309553174174 ) ) ;
#68560=CARTESIAN_POINT ( 'NONE',  ( -1.967015505459129087E-11, 198.7499999999984936, 10.00000000000000533 ) ) ;
#68561=CARTESIAN_POINT ( 'NONE',  ( -2.765530957081998586, 295.6406250017069510, 6.676582343750001591 ) ) ;
#68563=CARTESIAN_POINT ( 'NONE',  ( 11.35316468750000141, 191.0937499965860127, 0.000000000000000000 ) ) ;
#68571=CARTESIAN_POINT ( 'NONE',  ( 10.00000000000000178, 15.00000000000000178, 0.000000000000000000 ) ) ;
#68578=CARTESIAN_POINT ( 'NONE',  ( 8.660254037844385522, 16.45833332650536818, 5.000000000000005329 ) ) ;
#68590=EDGE_LOOP ( 'NONE', ( #10202, #37975, #47189, #33782, #44686 ) ) ;
#68594=CARTESIAN_POINT ( 'NONE',  ( -9.832129032723418760, 93.17708332991935549, -5.676582343750004256 ) ) ;
#68598=CARTESIAN_POINT ( 'NONE',  ( 8.660254037844390851, 70.41666666666668561, -5.000000000000001776 ) ) ;
#68599=CARTESIAN_POINT ( 'NONE',  ( 4.999999999999993783, 76.04166665983871098, 8.660254037844390851 ) ) ;
#68600=DIRECTION ( 'NONE',  ( -0.000000000000000000, 1.000000000000000000, -0.000000000000000000 ) ) ;
#68601=CARTESIAN_POINT ( 'NONE',  ( -2.085542519210945728E-15, 194.5312499965860127, 11.35316468750000141 ) ) ;
#68607=CARTESIAN_POINT ( 'NONE',  ( -8.311093377946836114, 172.9687499965860127, -8.311093377946837890 ) ) ;
#68615=CARTESIAN_POINT ( 'NONE',  ( 5.676582343749993598, 54.94791666325269119, 9.832129032723422313 ) ) ;
#68618=ORIENTED_EDGE ( 'NONE', *, *, #26764, .T. ) ;
#68620=CARTESIAN_POINT ( 'NONE',  ( -1.836970198721029983E-15, 170.6249999931720538, 10.00000000000000178 ) ) ;
#68621=CARTESIAN_POINT ( 'NONE',  ( -3.042071309553164404, 62.23958332991934128, -11.35316468749999963 ) ) ;
#68627=CARTESIAN_POINT ( 'NONE',  ( 3.042071309553159519, 64.73958332991935549, 11.35316468750000141 ) ) ;
#68630=CARTESIAN_POINT ( 'NONE',  ( -5.676582343750006032, 169.1145833299193555, 9.832129032723418760 ) ) ;
#68632=CARTESIAN_POINT ( 'NONE',  ( -8.660254037844387298, 148.9583333265053682, -5.000000000000004441 ) ) ;
#68634=CARTESIAN_POINT ( 'NONE',  ( -10.00000000000000000, 54.16666665983869677, -2.679491924311229845 ) ) ;
#68635=CARTESIAN_POINT ( 'NONE',  ( -8.311093377946836114, 42.96874999658601268, -8.311093377946837890 ) ) ;
#68637=CARTESIAN_POINT ( 'NONE',  ( -9.832129032723420536, 183.6979166632526983, 5.676582343749997150 ) ) ;
#68644=CARTESIAN_POINT ( 'NONE',  ( 8.311093377946834337, 160.1562499965860411, 8.311093377946839666 ) ) ;
#68652=CARTESIAN_POINT ( 'NONE',  ( 5.676582343749993598, 110.2604166632526841, 9.832129032723422313 ) ) ;
#68653=CARTESIAN_POINT ( 'NONE',  ( -1.183492779173324630E-13, 16.25000000000001066, -10.00000000000000178 ) ) ;
#68681=CARTESIAN_POINT ( 'NONE',  ( 1.934925017735378189E-11, 153.7500000000015348, 10.00000000000000533 ) ) ;
#68682=LINE ( 'NONE', #25787, #103 ) ;
#68683=CARTESIAN_POINT ( 'NONE',  ( 8.660254037844389075, 120.4166666666666714, -5.000000000000000000 ) ) ;
#68698=CARTESIAN_POINT ( 'NONE',  ( 9.832129032723420536, 11.19791666325268409, -5.676582343749999815 ) ) ;
#68699=CARTESIAN_POINT ( 'NONE',  ( -1.328591152368359007E-11, 1.250000000001033174, -10.00000000000000533 ) ) ;
#68700=CARTESIAN_POINT ( 'NONE',  ( -9.832129032723420536, 214.0104166632526699, 5.676582343749997150 ) ) ;
#68705=ORIENTED_EDGE ( 'NONE', *, *, #34708, .F. ) ;
#68707=CARTESIAN_POINT ( 'NONE',  ( -8.311093377946836114, 27.65624999658602334, -8.311093377946837890 ) ) ;
#68713=CARTESIAN_POINT ( 'NONE',  ( 5.676582343749993598, 24.94791666325268764, 9.832129032723422313 ) ) ;
#68715=CARTESIAN_POINT ( 'NONE',  ( -8.311093377946841443, 133.9062499965860411, 8.311093377946830785 ) ) ;
#68716=CARTESIAN_POINT ( 'NONE',  ( -4.999999999999998224, 98.54166665983871098, -8.660254037844389075 ) ) ;
#68718=CYLINDRICAL_SURFACE ( 'NONE', #39718, 10.00000000000000178 ) ;
#68720=ORIENTED_EDGE ( 'NONE', *, *, #39790, .T. ) ;
#68721=CARTESIAN_POINT ( 'NONE',  ( -7.320508075688781702, 118.1250000000000000, 7.320508075688773708 ) ) ;
#68722=CARTESIAN_POINT ( 'NONE',  ( 6.123233995736767268E-16, 28.12499999317203603, -10.00000000000000178 ) ) ;
#68723=CARTESIAN_POINT ( 'NONE',  ( 1.226468279477575784E-15, 295.7031250017069510, 6.676582343750001591 ) ) ;
#68724=CARTESIAN_POINT ( 'NONE',  ( 5.676582343750001591, 126.6145833299193697, -9.832129032723420536 ) ) ;
#68737=CARTESIAN_POINT ( 'NONE',  ( 9.832129032723420536, 76.51041666325268409, -5.676582343749999815 ) ) ;
#68738=ORIENTED_EDGE ( 'NONE', *, *, #12239, .T. ) ;
#68748=AXIS2_PLACEMENT_3D ( 'NONE', #17723, #39262, #69048 ) ;
#68751=LINE ( 'NONE', #55967, #3595 ) ;
#68752=ORIENTED_EDGE ( 'NONE', *, *, #3174, .F. ) ;
#68763=( BOUNDED_CURVE ( )  B_SPLINE_CURVE ( 2, ( #29306, #40245, #22504, #64003, #34607, #45901, #45525, #23999, #23263, #52316, #5925, #28927, #652 ),
 .UNSPECIFIED., .F., .F. ) 
 B_SPLINE_CURVE_WITH_KNOTS ( ( 3, 2, 2, 2, 2, 2, 3 ),
 ( 2.119489495730878748, 2.124722698272372590, 2.129955900813865988, 2.135189103355359386, 2.140422305896853228, 2.145655508438346626, 2.150888710979840468 ),
 .UNSPECIFIED. ) 
 CURVE ( )  GEOMETRIC_REPRESENTATION_ITEM ( )  RATIONAL_B_SPLINE_CURVE ( ( 1.000000000000014655, 0.9659258262890536573, 1.000000000000000000, 0.9659258262890683122, 1.000000000000000000, 0.9659258262890683122, 1.000000000000000000, 0.9659258262890683122, 1.000000000000000000, 0.9659258262890683122, 1.000000000000000000, 0.9659258262890662028, 1.000000000000001998 ) ) 
 REPRESENTATION_ITEM ( '' )  );
#68764=CARTESIAN_POINT ( 'NONE',  ( -6.676582343750001591, 287.4531250017069510, 0.000000000000000000 ) ) ;
#68770=CARTESIAN_POINT ( 'NONE',  ( -8.660254037844390851, 82.91666666666667140, 4.999999999999998224 ) ) ;
#68772=CARTESIAN_POINT ( 'NONE',  ( 4.242640687119285658, 288.6249999999999432, -4.242640687119286547 ) ) ;
#68783=CARTESIAN_POINT ( 'NONE',  ( -7.320508075688773708, 206.8750000000000000, -7.320508075688774596 ) ) ;
#68786=CARTESIAN_POINT ( 'NONE',  ( -11.35316468750000141, 173.8020833299193839, 3.042071309553159963 ) ) ;
#68787=CARTESIAN_POINT ( 'NONE',  ( 3.410844894484189267E-12, 36.24999999999974420, -10.00000000000000178 ) ) ;
#68792=CARTESIAN_POINT ( 'NONE',  ( -11.35316468750000141, 33.80208332991934839, 3.042071309553159963 ) ) ;
#68795=CARTESIAN_POINT ( 'NONE',  ( -2.249999999999999112, 284.0000000000000000, 7.677076266392047543 ) ) ;
#68800=CARTESIAN_POINT ( 'NONE',  ( 8.660254037844385522, 61.45833332650536818, 5.000000000000005329 ) ) ;
#68803=CARTESIAN_POINT ( 'NONE',  ( 4.999999999999999112, 55.83333333333332860, -8.660254037844385522 ) ) ;
#68810=CARTESIAN_POINT ( 'NONE',  ( -4.999999999999998224, 86.66666666666667140, -8.660254037844387298 ) ) ;
#68811=CARTESIAN_POINT ( 'NONE',  ( 9.832129032723416984, 145.3645833299193555, 5.676582343750006032 ) ) ;
#68823=CARTESIAN_POINT ( 'NONE',  ( -5.676582343750006032, 129.4270833299193555, 9.832129032723418760 ) ) ;
#68827=CARTESIAN_POINT ( 'NONE',  ( 11.35316468749999785, 30.88541666325268409, 3.042071309553174174 ) ) ;
#68829=CARTESIAN_POINT ( 'NONE',  ( -10.00000000000000711, 27.29166666666666785, -2.679491924311232065 ) ) ;
#68833=AXIS2_PLACEMENT_3D ( 'NONE', #29548, #74079, #68416 ) ;
#68836=CARTESIAN_POINT ( 'NONE',  ( -6.000000000000001776, 298.0625000034140157, 0.000000000000000000 ) ) ;
#68841=CARTESIAN_POINT ( 'NONE',  ( 9.832129032723416984, 150.6770833299193555, 5.676582343750006032 ) ) ;
#68855=EDGE_LOOP ( 'NONE', ( #40350, #49827, #66322, #6361 ) ) ;
#68859=CARTESIAN_POINT ( 'NONE',  ( -8.660254037844387298, 42.08333333333333570, -5.000000000000004441 ) ) ;
#68864=CARTESIAN_POINT ( 'NONE',  ( 10.00000000000011369, 80.20833333333341386, -2.679491924311257378 ) ) ;
#68874=CARTESIAN_POINT ( 'NONE',  ( -10.00000000000000000, 157.2916666666666572, -2.679491924311229845 ) ) ;
#68878=CARTESIAN_POINT ( 'NONE',  ( -11.35316468750000141, 123.8020833299193271, 3.042071309553159963 ) ) ;
#68886=DIRECTION ( 'NONE',  ( -0.000000000000000000, 1.000000000000000000, -0.000000000000000000 ) ) ;
#68891=CARTESIAN_POINT ( 'NONE',  ( -11.35316468749999785, 218.3854166632526415, -3.042071309553167513 ) ) ;
#68898=CARTESIAN_POINT ( 'NONE',  ( 3.042071309553167069, 106.8229166632526699, -11.35316468749999785 ) ) ;
#68904=CARTESIAN_POINT ( 'NONE',  ( -8.311093377946841443, 98.90624999658604111, 8.311093377946830785 ) ) ;
#68908=CARTESIAN_POINT ( 'NONE',  ( -8.660254037844387298, 218.9583333265053966, -5.000000000000004441 ) ) ;
#68912=CARTESIAN_POINT ( 'NONE',  ( 11.35316468749999963, 100.9895833299193555, -3.042071309553165293 ) ) ;
#68915=CARTESIAN_POINT ( 'NONE',  ( 7.320508075688838545, 175.6250000000000568, -7.320508075688838545 ) ) ;
#68916=VERTEX_POINT ( 'NONE', #58211 ) ;
#68917=CARTESIAN_POINT ( 'NONE',  ( -1.836970198721029983E-15, 190.6249999931720254, 10.00000000000000178 ) ) ;
#68920=CARTESIAN_POINT ( 'NONE',  ( 6.951808397369818766E-16, 87.34374999658602690, -11.35316468750000141 ) ) ;
#68921=CARTESIAN_POINT ( 'NONE',  ( 4.721056650416000089, 289.8281250017069510, 4.721056650415999201 ) ) ;
#68924=CARTESIAN_POINT ( 'NONE',  ( -2.085542519210945728E-15, 219.5312499965860411, 11.35316468750000141 ) ) ;
#68925=ORIENTED_EDGE ( 'NONE', *, *, #48563, .T. ) ;
#68927=DIRECTION ( 'NONE',  ( -0.000000000000000000, 1.000000000000000000, -0.000000000000000000 ) ) ;
#68928=CARTESIAN_POINT ( 'NONE',  ( -8.311093377946841443, 218.9062499965860127, 8.311093377946834337 ) ) ;
#68931=CARTESIAN_POINT ( 'NONE',  ( -6.676582343750000703, 295.5156250017070079, 2.765530957082001251 ) ) ;
#68934=CARTESIAN_POINT ( 'NONE',  ( -9.832129032723418760, 208.1770833299193555, -5.676582343750004256 ) ) ;
#68936=EDGE_CURVE ( 'NONE', #33772, #31972, #66680, .T. ) ;
#68942=CARTESIAN_POINT ( 'NONE',  ( -2.249999999999999556, 255.9999999999998295, 5.427273995024871844 ) ) ;
#68943=CARTESIAN_POINT ( 'NONE',  ( -10.00000000000000355, 32.70833333333333570, 2.679491924311223183 ) ) ;
#68946=FACE_OUTER_BOUND ( 'NONE', #26729, .T. ) ;
#68955=CARTESIAN_POINT ( 'NONE',  ( 7.320508075688771044, 151.2499999931720538, 7.320508075688775484 ) ) ;
#68956=CARTESIAN_POINT ( 'NONE',  ( 2.765530957082001251, 294.7656250017070079, 6.676582343749999815 ) ) ;
#68967=VERTEX_POINT ( 'NONE', #29889 ) ;
#68969=CARTESIAN_POINT ( 'NONE',  ( -8.311093377946841443, 84.21874999658599847, 8.311093377946830785 ) ) ;
#68974=CARTESIAN_POINT ( 'NONE',  ( 6.676582343750002480, 288.1718750017070079, -2.765530957081997254 ) ) ;
#68976=CARTESIAN_POINT ( 'NONE',  ( 10.00000000000000178, 76.87499999317203958, 0.000000000000000000 ) ) ;
#68978=CARTESIAN_POINT ( 'NONE',  ( 6.951808397369818766E-16, 202.0312499965860411, -11.35316468750000141 ) ) ;
#68982=CARTESIAN_POINT ( 'NONE',  ( -9.832129032723420536, 184.0104166632526983, 5.676582343749997150 ) ) ;
#68986=CARTESIAN_POINT ( 'NONE',  ( -4.999999999999994671, 111.6666666666666572, -8.660254037844383745 ) ) ;
#68990=CARTESIAN_POINT ( 'NONE',  ( -8.311093377946841443, 58.90624999658600558, 8.311093377946830785 ) ) ;
#68997=CARTESIAN_POINT ( 'NONE',  ( -8.311093377946841443, 58.90624999658600558, 8.311093377946830785 ) ) ;
#69002=CARTESIAN_POINT ( 'NONE',  ( 5.676582343750001591, 61.61458332991934839, -9.832129032723420536 ) ) ;
#69004=CARTESIAN_POINT ( 'NONE',  ( -1.836970198721029983E-15, 15.62499999317203248, 10.00000000000000178 ) ) ;
#69005=CARTESIAN_POINT ( 'NONE',  ( -9.832129032723418760, 177.8645833299193555, -5.676582343750004256 ) ) ;
#69006=CARTESIAN_POINT ( 'NONE',  ( -10.00000000000000178, 159.3749999931720254, -1.224646799147353454E-15 ) ) ;
#69009=CARTESIAN_POINT ( 'NONE',  ( -2.679491924311198314, 55.41666665983871098, 10.00000000000002309 ) ) ;
#69010=CARTESIAN_POINT ( 'NONE',  ( 11.35316468749999963, 46.30208332991934128, -3.042071309553165293 ) ) ;
#69013=CARTESIAN_POINT ( 'NONE',  ( 11.35316468749999963, 180.9895833299193555, -3.042071309553165293 ) ) ;
#69020=CARTESIAN_POINT ( 'NONE',  ( 3.042071309553159519, 184.7395833299193555, 11.35316468750000141 ) ) ;
#69030=CARTESIAN_POINT ( 'NONE',  ( -5.676582343749998039, 132.7604166632526983, -9.832129032723420536 ) ) ;
#69032=CARTESIAN_POINT ( 'NONE',  ( 10.00000000000000000, 11.66666665983870033, 2.679491924311235618 ) ) ;
#69038=EDGE_CURVE ( 'NONE', #59562, #12039, #12152, .T. ) ;
#69048=DIRECTION ( 'NONE',  ( 0.000000000000000000, 0.000000000000000000, 1.000000000000000000 ) ) ;
#69051=CARTESIAN_POINT ( 'NONE',  ( 1.959434878635763554E-15, 225.9999999999999432, -15.99999999999998579 ) ) ;
#69060=CARTESIAN_POINT ( 'NONE',  ( -6.676582343750002480, 297.5468750017070079, -2.765530957081996810 ) ) ;
#69061=CARTESIAN_POINT ( 'NONE',  ( -2.679491924311225848, 116.4583333333333286, -10.00000000000000178 ) ) ;
#69064=CARTESIAN_POINT ( 'NONE',  ( -6.676582343750000703, 287.6718750017070079, 2.765530957082001251 ) ) ;
#69077=CARTESIAN_POINT ( 'NONE',  ( 5.676582343749993598, 19.94791666325268409, 9.832129032723422313 ) ) ;
#69079=CARTESIAN_POINT ( 'NONE',  ( -9.832129032723420536, 224.0104166632526983, 5.676582343749997150 ) ) ;
#69082=CARTESIAN_POINT ( 'NONE',  ( -10.00000000000016698, 42.50000000000009948, -1.224646799147373372E-15 ) ) ;
#69085=CARTESIAN_POINT ( 'NONE',  ( -5.676582343749998039, 22.44791666325268409, -9.832129032723420536 ) ) ;
#69091=CARTESIAN_POINT ( 'NONE',  ( -3.042071309553173730, 24.32291666325268409, 11.35316468749999785 ) ) ;
#69093=CARTESIAN_POINT ( 'NONE',  ( 9.832129032723420536, 136.1979166632526983, -5.676582343749999815 ) ) ;
#69094=CARTESIAN_POINT ( 'NONE',  ( 10.00000000000000178, 106.8749999931720396, 0.000000000000000000 ) ) ;
#69100=ORIENTED_EDGE ( 'NONE', *, *, #37201, .T. ) ;
#69101=CARTESIAN_POINT ( 'NONE',  ( 6.951808397369818766E-16, 12.34374999658601801, -11.35316468750000141 ) ) ;
#69103=CARTESIAN_POINT ( 'NONE',  ( -6.676582343750001591, 287.6093750017069510, 0.000000000000000000 ) ) ;
#69104=CARTESIAN_POINT ( 'NONE',  ( 6.951808397369818766E-16, 142.0312499965860411, -11.35316468750000141 ) ) ;
#69114=CARTESIAN_POINT ( 'NONE',  ( -8.311093377946836114, 87.96874999658602690, -8.311093377946837890 ) ) ;
#69147=CARTESIAN_POINT ( 'NONE',  ( 7.320508075688774596, 85.62500000000000000, -7.320508075688774596 ) ) ;
#69149=CARTESIAN_POINT ( 'NONE',  ( -9.832129032723420536, 64.01041666325268409, 5.676582343749997150 ) ) ;
#69150=CARTESIAN_POINT ( 'NONE',  ( 2.485281374238575314, 289.3125000000000000, 6.000000000000000888 ) ) ;
#69160=CARTESIAN_POINT ( 'NONE',  ( -8.660254037844387298, 207.0833333333333428, -5.000000000000004441 ) ) ;
#69162=CARTESIAN_POINT ( 'NONE',  ( -8.311093377946841443, 164.2187499965860411, 8.311093377946830785 ) ) ;
#69164=CARTESIAN_POINT ( 'NONE',  ( 10.00000000000000000, 176.6666666598387110, 2.679491924311235618 ) ) ;
#69169=CARTESIAN_POINT ( 'NONE',  ( 5.676582343750001591, 41.92708332991934839, -9.832129032723420536 ) ) ;
#69177=EDGE_CURVE ( 'NONE', #19919, #56133, #25580, .T. ) ;
#69178=CARTESIAN_POINT ( 'NONE',  ( -5.000000000000005329, 60.20833332650536818, 8.660254037844387298 ) ) ;
#69181=CARTESIAN_POINT ( 'NONE',  ( 2.679491924338774922, 66.04166666666422714, -9.999999999984156673 ) ) ;
#69186=CARTESIAN_POINT ( 'NONE',  ( -5.000000000000059508, 198.3333333333333997, 8.660254037844477892 ) ) ;
#69187=CARTESIAN_POINT ( 'NONE',  ( 6.676582343750001591, 299.1093750017069510, -8.176455196517173205E-16 ) ) ;
#69188=CARTESIAN_POINT ( 'NONE',  ( -1.836970198721029983E-15, 40.62499999317203248, 10.00000000000000178 ) ) ;
#69189=CARTESIAN_POINT ( 'NONE',  ( 8.311093377946837890, 151.4062499965859843, -8.311093377946837890 ) ) ;
#69201=CARTESIAN_POINT ( 'NONE',  ( 9.832129032723420536, 131.5104166632526983, -5.676582343749999815 ) ) ;
#69205=CARTESIAN_POINT ( 'NONE',  ( -11.35316468749999785, 38.38541666325268409, -3.042071309553167513 ) ) ;
#69211=CARTESIAN_POINT ( 'NONE',  ( 4.242640687119285658, 294.6875000034139589, -4.242640687119286547 ) ) ;
#69216=CARTESIAN_POINT ( 'NONE',  ( 5.676582343750001591, 151.9270833299193555, -9.832129032723420536 ) ) ;
#69222=UNCERTAINTY_MEASURE_WITH_UNIT (LENGTH_MEASURE( 1.000000000000000082E-05 ), #29887, 'distance_accuracy_value', 'NONE');
#69229=LINE ( 'NONE', #63187, #4301 ) ;
#69235=CARTESIAN_POINT ( 'NONE',  ( -10.00000000000000355, 209.5833333265053966, 2.679491924311223183 ) ) ;
#69236=CARTESIAN_POINT ( 'NONE',  ( -1.836970198721029983E-15, 45.62499999317203958, 10.00000000000000178 ) ) ;
#69237=CARTESIAN_POINT ( 'NONE',  ( 8.660254037844389075, 45.41666666666666430, -5.000000000000000000 ) ) ;
#69243=ORIENTED_EDGE ( 'NONE', *, *, #32003, .T. ) ;
#69249=DIRECTION ( 'NONE',  ( 0.000000000000000000, 0.000000000000000000, 1.000000000000000000 ) ) ;
#69250=CARTESIAN_POINT ( 'NONE',  ( 10.00000000000000000, 154.7916666666666856, 2.679491924311236062 ) ) ;
#69254=CARTESIAN_POINT ( 'NONE',  ( 5.676582343750001591, 131.9270833299193555, -9.832129032723420536 ) ) ;
#69266=CARTESIAN_POINT ( 'NONE',  ( -5.000000000000005329, 20.20833332650536462, 8.660254037844387298 ) ) ;
#69273=CARTESIAN_POINT ( 'NONE',  ( -5.676582343749998039, 102.4479166632526841, -9.832129032723420536 ) ) ;
#69279=CARTESIAN_POINT ( 'NONE',  ( -11.35316468750000141, 103.4895833299193697, 3.042071309553159963 ) ) ;
#69280=ORIENTED_EDGE ( 'NONE', *, *, #24035, .F. ) ;
#69285=CARTESIAN_POINT ( 'NONE',  ( -8.660254037844390851, 224.7916666598387110, 4.999999999999998224 ) ) ;
#69288=CARTESIAN_POINT ( 'NONE',  ( -11.35316468750000141, 93.48958332991934128, 3.042071309553159963 ) ) ;
#69294=CARTESIAN_POINT ( 'NONE',  ( 4.999999999999993783, 201.0416666598387110, 8.660254037844390851 ) ) ;
#69296=CARTESIAN_POINT ( 'NONE',  ( -8.311093377946836114, 92.96874999658602690, -8.311093377946837890 ) ) ;
#69297=CARTESIAN_POINT ( 'NONE',  ( 6.676582343750001591, 288.9531250017069510, -8.176455196517173205E-16 ) ) ;
#69300=CARTESIAN_POINT ( 'NONE',  ( -9.832129032723420536, 218.6979166632526983, 5.676582343749997150 ) ) ;
#69302=CARTESIAN_POINT ( 'NONE',  ( -2.062184786512628451E-11, 138.7499999999984084, 10.00000000000000178 ) ) ;
#69304=CARTESIAN_POINT ( 'NONE',  ( 9.832129032723420536, 221.1979166632526983, -5.676582343749999815 ) ) ;
#69305=CARTESIAN_POINT ( 'NONE',  ( 2.679491924311185880, 45.83333332650536818, 10.00000000000002487 ) ) ;
#69306=CARTESIAN_POINT ( 'NONE',  ( -10.00000000000018652, 157.7083333333334565, 2.679491924311272921 ) ) ;
#69307=CARTESIAN_POINT ( 'NONE',  ( 4.721056650415999201, 298.0781250017069510, -4.721056650415999201 ) ) ;
#69309=ADVANCED_FACE ( 'NONE', ( #62823 ), #35742, .F. ) ;
#69310=ORIENTED_EDGE ( 'NONE', *, *, #3789, .F. ) ;
#69312=CARTESIAN_POINT ( 'NONE',  ( 5.676582343750001591, 206.9270833299193555, -9.832129032723420536 ) ) ;
#69320=CARTESIAN_POINT ( 'NONE',  ( -8.660254037844387298, 22.08333333333333215, -5.000000000000004441 ) ) ;
#69323=VERTEX_POINT ( 'NONE', #424 ) ;
#69326=CYLINDRICAL_SURFACE ( 'NONE', #6622, 10.00000000000000178 ) ;
#69329=CARTESIAN_POINT ( 'NONE',  ( -6.676582343749999815, 296.5156250017069510, 2.765530957082001251 ) ) ;
#69333=( BOUNDED_CURVE ( )  B_SPLINE_CURVE ( 2, ( #58849, #17075, #57085, #5401, #22731, #28403, #51411, #74425, #40097 ),
 .UNSPECIFIED., .F., .F. ) 
 B_SPLINE_CURVE_WITH_KNOTS ( ( 3, 2, 2, 2, 3 ),
 ( 0.6458333333333314830, 0.6562499999999981126, 0.6666666666666647423, 0.6770833333333315940, 0.6874999999999982236 ),
 .UNSPECIFIED. ) 
 CURVE ( )  GEOMETRIC_REPRESENTATION_ITEM ( )  RATIONAL_B_SPLINE_CURVE ( ( 1.000000000000013767, 0.9238795325112729717, 1.000000000000000000, 0.9238795325112867385, 1.000000000000000000, 0.9238795325112867385, 1.000000000000000000, 0.9238795325112997281, 0.9999999999999870104 ) ) 
 REPRESENTATION_ITEM ( '' )  );
#69339=CARTESIAN_POINT ( 'NONE',  ( 9.832129032723416984, 90.67708332991934128, 5.676582343750006032 ) ) ;
#69344=CARTESIAN_POINT ( 'NONE',  ( 8.660254037844387298, 69.58333333333335702, 5.000000000000007105 ) ) ;
#69350=CARTESIAN_POINT ( 'NONE',  ( -5.676582343750006032, 204.1145833299193555, 9.832129032723418760 ) ) ;
#69355=CARTESIAN_POINT ( 'NONE',  ( 5.676582343749993598, 175.2604166632526699, 9.832129032723422313 ) ) ;
#69359=CARTESIAN_POINT ( 'NONE',  ( -10.00000000000000000, 89.16666665983868256, -2.679491924311229845 ) ) ;
#69363=CARTESIAN_POINT ( 'NONE',  ( -8.311093377946841443, 73.90624999658601268, 8.311093377946830785 ) ) ;
#69369=CARTESIAN_POINT ( 'NONE',  ( -8.311093377946841443, 68.90624999658602690, 8.311093377946830785 ) ) ;
#69374=CARTESIAN_POINT ( 'NONE',  ( 9.832129032723416984, 65.36458332991935549, 5.676582343750006032 ) ) ;
#69377=EDGE_CURVE ( 'NONE', #512, #34861, #73972, .T. ) ;
#69378=CARTESIAN_POINT ( 'NONE',  ( 4.999999999999993783, 156.0416666598387110, 8.660254037844390851 ) ) ;
#69381=CARTESIAN_POINT ( 'NONE',  ( 5.676582343750001591, 51.92708332991935549, -9.832129032723420536 ) ) ;
#69383=B_SPLINE_CURVE_WITH_KNOTS ( 'NONE', 1,
 ( #13722, #42408 ),
 .UNSPECIFIED., .F., .F.,
 ( 2, 2 ),
 ( 0.000000000000000000, 1.000000000000000000 ),
 .UNSPECIFIED. ) ;
#69384=CARTESIAN_POINT ( 'NONE',  ( -11.35316468750000141, 183.2812499965860411, -1.390361679473963753E-15 ) ) ;
#69390=CARTESIAN_POINT ( 'NONE',  ( 11.35316468749999785, 175.5729166632526699, 3.042071309553174174 ) ) ;
#69397=CARTESIAN_POINT ( 'NONE',  ( 5.676582343749993598, 170.2604166632526983, 9.832129032723422313 ) ) ;
#69401=CARTESIAN_POINT ( 'NONE',  ( -9.832129032723418760, 133.1770833299193555, -5.676582343750004256 ) ) ;
#69405=( GEOMETRIC_REPRESENTATION_CONTEXT ( 3 ) GLOBAL_UNCERTAINTY_ASSIGNED_CONTEXT ( ( #69222 ) ) GLOBAL_UNIT_ASSIGNED_CONTEXT ( ( #29887, #29518, #18564 ) ) REPRESENTATION_CONTEXT ( 'NONE', 'WORKASPACE' ) );
#69413=VERTEX_POINT ( 'NONE', #70541 ) ;
#69424=CARTESIAN_POINT ( 'NONE',  ( 1.224646799147353454E-15, 300.0000000000000000, -10.00000000000000178 ) ) ;
#69427=DIRECTION ( 'NONE',  ( -0.000000000000000000, 1.000000000000000000, 0.000000000000000000 ) ) ;
#69429=CARTESIAN_POINT ( 'NONE',  ( -2.765530957081996810, 297.4218750017069510, -6.676582343750002480 ) ) ;
#69430=CARTESIAN_POINT ( 'NONE',  ( -10.00000000000000355, 132.7083333333333144, 2.679491924311223183 ) ) ;
#69432=CARTESIAN_POINT ( 'NONE',  ( 0.3928675183479075073, 225.9999999999999716, 10.00000000000000178 ) ) ;
#69447=CARTESIAN_POINT ( 'NONE',  ( -5.676582343750006032, 34.11458332991934839, 9.832129032723418760 ) ) ;
#69452=CARTESIAN_POINT ( 'NONE',  ( 4.643173273996913153, 227.0088038288673715, -10.42876803732836599 ) ) ;
#69458=CARTESIAN_POINT ( 'NONE',  ( 6.951808397369818766E-16, 27.03124999658601979, -11.35316468750000141 ) ) ;
#69461=CARTESIAN_POINT ( 'NONE',  ( -8.660254037844396180, 152.9166666666666856, 5.000000000000001776 ) ) ;
#69464=CARTESIAN_POINT ( 'NONE',  ( 8.311093377946834337, 15.15624999658601624, 8.311093377946839666 ) ) ;
#69466=CARTESIAN_POINT ( 'NONE',  ( -11.35316468749999785, 133.0729166632526983, -3.042071309553167513 ) ) ;
#69468=CARTESIAN_POINT ( 'NONE',  ( 7.320508075688774596, 117.4999999931720396, -7.320508075688774596 ) ) ;
#69470=CARTESIAN_POINT ( 'NONE',  ( -1.836970198721029983E-15, 170.6249999931720538, 10.00000000000000178 ) ) ;
#69474=CARTESIAN_POINT ( 'NONE',  ( -3.042071309553173730, 9.635416663252682312, 11.35316468749999785 ) ) ;
#69476=CARTESIAN_POINT ( 'NONE',  ( -2.765530957081998586, 298.6406250017069510, 6.676582343750001591 ) ) ;
#69477=CARTESIAN_POINT ( 'NONE',  ( -8.311093377946836114, 142.6562499965860127, -8.311093377946837890 ) ) ;
#69489=CARTESIAN_POINT ( 'NONE',  ( -9.832129032723420536, 94.01041666325268409, 5.676582343749997150 ) ) ;
#69519=CARTESIAN_POINT ( 'NONE',  ( -10.00000000000000178, 92.50000000000001421, -1.224646799147353454E-15 ) ) ;
#69521=CARTESIAN_POINT ( 'NONE',  ( 3.042071309553159519, 60.05208332991934128, 11.35316468750000141 ) ) ;
#69522=CARTESIAN_POINT ( 'NONE',  ( 6.676582343750003368, 299.1718750017069510, -2.765530957081997254 ) ) ;
#69530=DIRECTION ( 'NONE',  ( -0.000000000000000000, 1.000000000000000000, -0.000000000000000000 ) ) ;
#69534=CARTESIAN_POINT ( 'NONE',  ( -7.320508075688773708, 196.8750000000000568, -7.320508075688774596 ) ) ;
#69537=CARTESIAN_POINT ( 'NONE',  ( -3.042071309553173730, 179.6354166632526699, 11.35316468749999785 ) ) ;
#69541=CARTESIAN_POINT ( 'NONE',  ( 7.320508075688774596, 87.49999999317202537, -7.320508075688774596 ) ) ;
#69544=CARTESIAN_POINT ( 'NONE',  ( 5.676582343749993598, 35.26041666325269119, 9.832129032723422313 ) ) ;
#69552=CARTESIAN_POINT ( 'NONE',  ( 5.000000000000001776, 72.70833332650536818, -8.660254037844389075 ) ) ;
#69555=CARTESIAN_POINT ( 'NONE',  ( 5.000000000000112799, 215.8333333333334849, -8.660254037844579145 ) ) ;
#69561=CARTESIAN_POINT ( 'NONE',  ( 6.676582343750004256, 297.0468750017068942, 2.765530957081995478 ) ) ;
#69564=CARTESIAN_POINT ( 'NONE',  ( 11.35316468749999785, 155.5729166632527267, 3.042071309553174174 ) ) ;
#69565=CARTESIAN_POINT ( 'NONE',  ( 2.679491924304078232, 103.9583333333326891, 10.00000000000411049 ) ) ;
#69571=ORIENTED_EDGE ( 'NONE', *, *, #25630, .F. ) ;
#69572=( BOUNDED_CURVE ( )  B_SPLINE_CURVE ( 2, ( #63617, #11944, #18345, #34976, #57992, #7766, #6296, #53423, #58357, #29302, #70401, #648, #6662 ),
 .UNSPECIFIED., .F., .F. ) 
 B_SPLINE_CURVE_WITH_KNOTS ( ( 3, 2, 2, 2, 2, 2, 3 ),
 ( 2.276484824319521039, 2.281718076880095758, 2.286951329440670477, 2.292184582001245197, 2.297417834561819472, 2.302651087122394191, 2.307884339682968911 ),
 .UNSPECIFIED. ) 
 CURVE ( )  GEOMETRIC_REPRESENTATION_ITEM ( )  RATIONAL_B_SPLINE_CURVE ( ( 0.9999999999999956701, 0.9659258262890724200, 0.9999999999999998890, 0.9659258262890682012, 0.9999999999999998890, 0.9659258262890682012, 0.9999999999999998890, 0.9659258262890682012, 0.9999999999999998890, 0.9659258262890682012, 0.9999999999999998890, 0.9659258262890598745, 1.000000000000008216 ) ) 
 REPRESENTATION_ITEM ( '' )  );
#69576=CARTESIAN_POINT ( 'NONE',  ( 8.311093377946834337, 125.4687499965860269, 8.311093377946839666 ) ) ;
#69580=CARTESIAN_POINT ( 'NONE',  ( -5.676582343750006032, 54.42708332991935549, 9.832129032723418760 ) ) ;
#69581=ORIENTED_EDGE ( 'NONE', *, *, #20527, .F. ) ;
#69587=CARTESIAN_POINT ( 'NONE',  ( -6.000000000000000888, 298.1250000034140157, 2.485281374238575758 ) ) ;
#69602=LINE ( 'NONE', #11518, #30795 ) ;
#69609=CARTESIAN_POINT ( 'NONE',  ( 10.00000000000000178, 60.00000000000000711, 0.000000000000000000 ) ) ;
#69612=CARTESIAN_POINT ( 'NONE',  ( -4.242640687119285658, 299.1250000000000000, 4.242640687119287435 ) ) ;
#69623=PLANE ( 'NONE',  #23447 ) ;
#69624=CARTESIAN_POINT ( 'NONE',  ( 7.320508075688771044, 164.3750000000000284, 7.320508075688775484 ) ) ;
#69628=CARTESIAN_POINT ( 'NONE',  ( -5.676582343749998039, 142.7604166632526699, -9.832129032723420536 ) ) ;
#69635=CARTESIAN_POINT ( 'NONE',  ( -8.311093377946836114, 2.968749996586016238, -8.311093377946837890 ) ) ;
#69639=CARTESIAN_POINT ( 'NONE',  ( 4.999999999999993783, 16.04166665983870033, 8.660254037844390851 ) ) ;
#69645=DIRECTION ( 'NONE',  ( -0.000000000000000000, 1.000000000000000000, -0.000000000000000000 ) ) ;
#69646=CARTESIAN_POINT ( 'NONE',  ( -2.085542519210945728E-15, 109.5312499965860269, 11.35316468750000141 ) ) ;
#69652=CARTESIAN_POINT ( 'NONE',  ( 5.676582343749993598, 109.9479166632526983, 9.832129032723422313 ) ) ;
#69656=CARTESIAN_POINT ( 'NONE',  ( 7.320508075688774596, 217.4999999931720538, -7.320508075688774596 ) ) ;
#69660=CARTESIAN_POINT ( 'NONE',  ( -5.676582343750006032, 99.11458332991935549, 9.832129032723418760 ) ) ;
#69665=CARTESIAN_POINT ( 'NONE',  ( -7.320508075688773708, 193.7499999931720538, -7.320508075688774596 ) ) ;
#69668=CARTESIAN_POINT ( 'NONE',  ( 8.311093377946834337, 90.46874999658601268, 8.311093377946839666 ) ) ;
#69673=CARTESIAN_POINT ( 'NONE',  ( 9.832129032723420536, 6.510416663252683200, -5.676582343749999815 ) ) ;
#69674=ORIENTED_EDGE ( 'NONE', *, *, #32572, .F. ) ;
#69677=CARTESIAN_POINT ( 'NONE',  ( -3.042071309553173730, 219.3229166632526699, 11.35316468749999785 ) ) ;
#69680=CARTESIAN_POINT ( 'NONE',  ( -10.00000000000000000, 99.16666665983871098, -2.679491924311229845 ) ) ;
#69681=CARTESIAN_POINT ( 'NONE',  ( -4.721056650415998313, 295.5781250017069510, 4.721056650416000089 ) ) ;
#69685=CARTESIAN_POINT ( 'NONE',  ( -2.085542519210945728E-15, 214.8437499965860411, 11.35316468750000141 ) ) ;
#69695=CARTESIAN_POINT ( 'NONE',  ( -7.320508075688778149, 28.12500000000000355, 7.320508075688769267 ) ) ;
#69706=CARTESIAN_POINT ( 'NONE',  ( 2.765530957081996366, 298.1406250017069510, -6.676582343750002480 ) ) ;
#69710=ORIENTED_EDGE ( 'NONE', *, *, #51302, .T. ) ;
#69715=CARTESIAN_POINT ( 'NONE',  ( 11.35316468749999963, 101.3020833299193555, -3.042071309553165293 ) ) ;
#69725=CARTESIAN_POINT ( 'NONE',  ( -3.042071309553173730, 204.3229166632526699, 11.35316468749999785 ) ) ;
#69729=CARTESIAN_POINT ( 'NONE',  ( 3.042071309553167069, 187.1354166632526983, -11.35316468749999785 ) ) ;
#69732=CARTESIAN_POINT ( 'NONE',  ( -9.999999999999996447, 107.2916666666666714, -2.679491924311228956 ) ) ;
#69736=CARTESIAN_POINT ( 'NONE',  ( 5.676582343749993598, 74.94791666325269830, 9.832129032723422313 ) ) ;
#69739=ORIENTED_EDGE ( 'NONE', *, *, #1586, .T. ) ;
#69742=CARTESIAN_POINT ( 'NONE',  ( -11.35316468750000141, 73.48958332991932707, 3.042071309553159963 ) ) ;
#69743=AXIS2_PLACEMENT_3D ( 'NONE', #24476, #64480, #41466 ) ;
#69748=CARTESIAN_POINT ( 'NONE',  ( 8.311093377946834337, 60.15624999658601979, 8.311093377946839666 ) ) ;
#69752=CARTESIAN_POINT ( 'NONE',  ( -8.660254037844390851, 149.7916666598387110, 4.999999999999998224 ) ) ;
#69755=CARTESIAN_POINT ( 'NONE',  ( -3.042071309553173730, 44.63541666325268409, 11.35316468749999785 ) ) ;
#69757=CARTESIAN_POINT ( 'NONE',  ( -3.042071309553173730, 179.3229166632526699, 11.35316468749999785 ) ) ;
#69761=CARTESIAN_POINT ( 'NONE',  ( 10.00000000000000178, 162.0833333265053682, -2.679491924311226736 ) ) ;
#69763=CARTESIAN_POINT ( 'NONE',  ( 8.311093377946837890, 176.4062499965859843, -8.311093377946837890 ) ) ;
#69764=CYLINDRICAL_SURFACE ( 'NONE', #74318, 10.00000000000000178 ) ;
#69768=CARTESIAN_POINT ( 'NONE',  ( 6.951808397369818766E-16, 172.3437499965860127, -11.35316468750000141 ) ) ;
#69769=CARTESIAN_POINT ( 'NONE',  ( 1.102182119232618108E-15, 293.3125000034140157, 6.000000000000001776 ) ) ;
#69770=CARTESIAN_POINT ( 'NONE',  ( -9.832129032723418760, 128.1770833299193555, -5.676582343750004256 ) ) ;
#69775=( BOUNDED_CURVE ( )  B_SPLINE_CURVE ( 2, ( #70535, #65605, #64868, #1874, #54305, #24860, #2616, #48619, #65976, #66352, #54678, #59586, #14656 ),
 .UNSPECIFIED., .F., .F. ) 
 B_SPLINE_CURVE_WITH_KNOTS ( ( 3, 2, 2, 2, 2, 2, 3 ),
 ( 0.3858695652173912971, 0.3876811594202898559, 0.3894927536231884146, 0.3913043478260870289, 0.3931159420289855877, 0.3949275362318840910, 0.3967391304347826497 ),
 .UNSPECIFIED. ) 
 CURVE ( )  GEOMETRIC_REPRESENTATION_ITEM ( )  RATIONAL_B_SPLINE_CURVE ( ( 1.000000000000000000, 0.9659258262890683122, 1.000000000000000000, 0.9659258262890683122, 1.000000000000000000, 0.9659258262890683122, 1.000000000000000000, 0.9659258262890683122, 1.000000000000000000, 0.9659258262890683122, 1.000000000000000000, 0.9659258262890673130, 1.000000000000001110 ) ) 
 REPRESENTATION_ITEM ( '' )  );
#69776=AXIS2_PLACEMENT_3D ( 'NONE', #23314, #16901, #40296 ) ;
#69785=CARTESIAN_POINT ( 'NONE',  ( -5.000000000000024869, 176.6666666666666856, -8.660254037844437036 ) ) ;
#69799=CARTESIAN_POINT ( 'NONE',  ( -3.673940397442060854E-16, 289.8125000034140157, -6.000000000000001776 ) ) ;
#69801=CARTESIAN_POINT ( 'NONE',  ( -4.721056650415999201, 296.4843750017070079, -4.721056650415999201 ) ) ;
#69802=CARTESIAN_POINT ( 'NONE',  ( 7.320508075688774596, 140.6250000000000000, -7.320508075688774596 ) ) ;
#69819=CARTESIAN_POINT ( 'NONE',  ( 9.832129032723416984, 30.36458332991935194, 5.676582343750006032 ) ) ;
#69821=CARTESIAN_POINT ( 'NONE',  ( 10.00000000000000178, 2.083333326505365957, -2.679491924311226736 ) ) ;
#69829=CARTESIAN_POINT ( 'NONE',  ( 5.676582343749993598, 19.94791666325268409, 9.832129032723422313 ) ) ;
#69832=CARTESIAN_POINT ( 'NONE',  ( -3.673940397442060854E-16, 294.8125000034140157, -6.000000000000001776 ) ) ;
#69835=CARTESIAN_POINT ( 'NONE',  ( -9.832129032723420536, 23.69791666325268409, 5.676582343749997150 ) ) ;
#69838=CARTESIAN_POINT ( 'NONE',  ( 6.951808397369818766E-16, 142.0312499965860411, -11.35316468750000141 ) ) ;
#69840=CARTESIAN_POINT ( 'NONE',  ( -2.679491924311225848, 118.3333333265053682, -10.00000000000000178 ) ) ;
#69841=EDGE_CURVE ( 'NONE', #61682, #5256, #17895, .T. ) ;
#69843=CARTESIAN_POINT ( 'NONE',  ( 7.320508075688774596, 172.4999999931719969, -7.320508075688774596 ) ) ;
#69846=CARTESIAN_POINT ( 'NONE',  ( -5.676582343750006032, 14.42708332991935016, 9.832129032723418760 ) ) ;
#69849=CARTESIAN_POINT ( 'NONE',  ( -6.676582343750003368, 298.3906250017070079, -2.765530957081996810 ) ) ;
#69851=CARTESIAN_POINT ( 'NONE',  ( 11.35316468749999963, 145.9895833299193839, -3.042071309553165293 ) ) ;
#69861=CARTESIAN_POINT ( 'NONE',  ( -11.35316468749999785, 93.38541666325269830, -3.042071309553167513 ) ) ;
#69884=VECTOR ( 'NONE', #58757, 1000.000000000000000 ) ;
#69887=ORIENTED_EDGE ( 'NONE', *, *, #58759, .T. ) ;
#69888=( BOUNDED_CURVE ( )  B_SPLINE_CURVE ( 2, ( #70652, #11831, #17860, #41618, #64630, #6915, #41250, #40878, #47630, #29926, #64984, #12567, #69925 ),
 .UNSPECIFIED., .F., .F. ) 
 B_SPLINE_CURVE_WITH_KNOTS ( ( 3, 2, 2, 2, 2, 2, 3 ),
 ( 1.271689704932325693, 1.276922700034719860, 1.282155695137113804, 1.287388690239507971, 1.292621685341902138, 1.297854680444296305, 1.303087675546690472 ),
 .UNSPECIFIED. ) 
 CURVE ( )  GEOMETRIC_REPRESENTATION_ITEM ( )  RATIONAL_B_SPLINE_CURVE ( ( 1.000000000000000000, 0.9659258262890683122, 1.000000000000000000, 0.9659258262890683122, 1.000000000000000000, 0.9659258262890683122, 1.000000000000000000, 0.9659258262890683122, 1.000000000000000000, 0.9659258262890683122, 1.000000000000000000, 0.9659258262891695646, 0.9999999999998987477 ) ) 
 REPRESENTATION_ITEM ( '' )  );
#69891=CARTESIAN_POINT ( 'NONE',  ( -7.320508075688769267, 98.12499999999997158, 7.320508075688761274 ) ) ;
#69895=CARTESIAN_POINT ( 'NONE',  ( -2.679491924311235618, 93.54166666666668561, 10.00000000000000000 ) ) ;
#69896=AXIS2_PLACEMENT_3D ( 'NONE', #73720, #38283, #31872 ) ;
#69898=CARTESIAN_POINT ( 'NONE',  ( 5.676582343750001591, 56.92708332991935549, -9.832129032723420536 ) ) ;
#69899=CARTESIAN_POINT ( 'NONE',  ( 6.676582343750003368, 298.1718750017070079, -2.765530957081997254 ) ) ;
#69900=ORIENTED_EDGE ( 'NONE', *, *, #43462, .F. ) ;
#69901=CARTESIAN_POINT ( 'NONE',  ( 2.485281374238216490, 294.6875000000000568, -6.000000000000357048 ) ) ;
#69905=CARTESIAN_POINT ( 'NONE',  ( -7.320508075688778149, 104.9999999931720396, 7.320508075688769267 ) ) ;
#69910=CARTESIAN_POINT ( 'NONE',  ( 7.320508075688774596, 220.6250000000000284, -7.320508075688774596 ) ) ;
#69913=CARTESIAN_POINT ( 'NONE',  ( -5.676582343749998039, 182.7604166632526699, -9.832129032723420536 ) ) ;
#69916=CARTESIAN_POINT ( 'NONE',  ( 0.000000000000000000, 300.0000000000000000, 0.000000000000000000 ) ) ;
#69920=CARTESIAN_POINT ( 'NONE',  ( -5.676582343749998039, 42.76041666325268409, -9.832129032723420536 ) ) ;
#69925=CARTESIAN_POINT ( 'NONE',  ( -1.522892193876115035E-11, 103.7499999999988205, 10.00000000000000178 ) ) ;
#69927=CARTESIAN_POINT ( 'NONE',  ( -7.320508075688773708, 73.74999999317203958, -7.320508075688774596 ) ) ;
#69936=CARTESIAN_POINT ( 'NONE',  ( 6.123233995736767268E-16, 23.12499999317203603, -10.00000000000000178 ) ) ;
#69937=CARTESIAN_POINT ( 'NONE',  ( 6.676582343750001591, 296.1093750017069510, -8.176455196517173205E-16 ) ) ;
#69940=CARTESIAN_POINT ( 'NONE',  ( -11.35316468749999785, 158.0729166632526699, -3.042071309553167513 ) ) ;
#69949=CARTESIAN_POINT ( 'NONE',  ( 5.676582343750001591, 141.9270833299193555, -9.832129032723420536 ) ) ;
#69953=CARTESIAN_POINT ( 'NONE',  ( -11.35316468750000141, 53.80208332991935549, 3.042071309553159963 ) ) ;
#69955=CARTESIAN_POINT ( 'NONE',  ( 0.000000000000000000, 300.0000000000000000, 0.000000000000000000 ) ) ;
#69962=CARTESIAN_POINT ( 'NONE',  ( -6.000000000000000888, 294.1250000034140157, 2.485281374238575758 ) ) ;
#69980=ORIENTED_EDGE ( 'NONE', *, *, #34708, .T. ) ;
#69986=CARTESIAN_POINT ( 'NONE',  ( 5.000000000000001776, 60.83333333333333570, -8.660254037844389075 ) ) ;
#69988=CARTESIAN_POINT ( 'NONE',  ( 2.485281374238571317, 299.6874999999999432, -6.000000000000003553 ) ) ;
#69997=CARTESIAN_POINT ( 'NONE',  ( -1.836970198721029983E-15, 75.62499999317203958, 10.00000000000000178 ) ) ;
#69999=CARTESIAN_POINT ( 'NONE',  ( -7.320508075688778149, 139.9999999931720254, 7.320508075688769267 ) ) ;
#70000=CARTESIAN_POINT ( 'NONE',  ( -7.320508075688778149, 178.1250000000000284, 7.320508075688769267 ) ) ;
#70004=CARTESIAN_POINT ( 'NONE',  ( 5.676582343750001591, 136.9270833299193555, -9.832129032723420536 ) ) ;
#70017=CARTESIAN_POINT ( 'NONE',  ( -10.00000000000000178, 34.37499999317203248, -1.224646799147353454E-15 ) ) ;
#70025=CARTESIAN_POINT ( 'NONE',  ( -8.679233769290393141, 225.9999999999999716, 5.010062319349841253 ) ) ;
#70029=CARTESIAN_POINT ( 'NONE',  ( -3.042071309553164404, 122.2395833299193271, -11.35316468749999963 ) ) ;
#70030=ORIENTED_EDGE ( 'NONE', *, *, #51793, .F. ) ;
#70036=CARTESIAN_POINT ( 'NONE',  ( 2.592975333673598559, 225.9999999999999716, -9.672265883052229896 ) ) ;
#70037=CARTESIAN_POINT ( 'NONE',  ( -2.085542519210945728E-15, 109.5312499965860269, 11.35316468750000141 ) ) ;
#70043=CARTESIAN_POINT ( 'NONE',  ( 7.320508075688774596, 197.4999999931719969, -7.320508075688774596 ) ) ;
#70046=CARTESIAN_POINT ( 'NONE',  ( -3.042071309553163960, 87.55208332991935549, -11.35316468749999963 ) ) ;
#70050=CARTESIAN_POINT ( 'NONE',  ( 5.676582343749993598, 15.26041666325268409, 9.832129032723422313 ) ) ;
#70054=CARTESIAN_POINT ( 'NONE',  ( -11.35316468749999785, 223.0729166632527267, -3.042071309553167957 ) ) ;
#70058=FACE_OUTER_BOUND ( 'NONE', #62001, .T. ) ;
#70059=CARTESIAN_POINT ( 'NONE',  ( -2.679491924311226292, 148.3333333265053682, -10.00000000000000178 ) ) ;
#70060=CARTESIAN_POINT ( 'NONE',  ( -6.676582343750001591, 294.4531250017069510, 0.000000000000000000 ) ) ;
#70063=CARTESIAN_POINT ( 'NONE',  ( 3.042071309553167513, 207.1354166632526699, -11.35316468749999785 ) ) ;
#70069=ORIENTED_EDGE ( 'NONE', *, *, #74316, .F. ) ;
#70074=CARTESIAN_POINT ( 'NONE',  ( -10.00000000000000000, 22.29166666666666430, -2.679491924311229845 ) ) ;
#70084=CARTESIAN_POINT ( 'NONE',  ( -2.765530957081996810, 296.2656250017069510, -6.676582343750002480 ) ) ;
#70094=CARTESIAN_POINT ( 'NONE',  ( 3.042071309553159519, 100.0520833299193555, 11.35316468750000141 ) ) ;
#70099=CARTESIAN_POINT ( 'NONE',  ( 7.320508075688773708, 69.37499999999998579, 7.320508075688777261 ) ) ;
#70101=ORIENTED_EDGE ( 'NONE', *, *, #5493, .T. ) ;
#70105=CARTESIAN_POINT ( 'NONE',  ( -3.042071309553164404, 212.2395833299193839, -11.35316468749999963 ) ) ;
#70109=CARTESIAN_POINT ( 'NONE',  ( 8.311093377946834337, 175.4687499965860127, 8.311093377946839666 ) ) ;
#70111=DIRECTION ( 'NONE',  ( -0.000000000000000000, 1.000000000000000000, -0.000000000000000000 ) ) ;
#70116=CARTESIAN_POINT ( 'NONE',  ( -9.832129032723418760, 72.86458332991935549, -5.676582343750004256 ) ) ;
#70117=( BOUNDED_CURVE ( )  B_SPLINE_CURVE ( 2, ( #24983, #46899, #47264, #13290, #12925, #24619, #41616, #18969, #70650, #41972, #24252, #18233, #12193 ),
 .UNSPECIFIED., .F., .F. ) 
 B_SPLINE_CURVE_WITH_KNOTS ( ( 3, 2, 2, 2, 2, 2, 3 ),
 ( 0.1098959258685624774, 0.1151295451665490382, 0.1203631644645356269, 0.1255967837625222294, 0.1308304030605088042, 0.1360640223584954067, 0.1412976416564819815 ),
 .UNSPECIFIED. ) 
 CURVE ( )  GEOMETRIC_REPRESENTATION_ITEM ( )  RATIONAL_B_SPLINE_CURVE ( ( 1.000000000000000000, 0.9659258262890682012, 1.000000000000000000, 0.9659258262890684232, 1.000000000000000000, 0.9659258262890684232, 1.000000000000000000, 0.9659258262890684232, 1.000000000000000000, 0.9659258262890684232, 1.000000000000000000, 0.9659258262890677571, 1.000000000000000666 ) ) 
 REPRESENTATION_ITEM ( '' )  );
#70119=ORIENTED_EDGE ( 'NONE', *, *, #67838, .F. ) ;
#70122=CARTESIAN_POINT ( 'NONE',  ( 8.311093377946837890, 76.40624999658602690, -8.311093377946837890 ) ) ;
#70127=CARTESIAN_POINT ( 'NONE',  ( -11.35316468750000141, 63.28124999658601979, -1.390361679473963753E-15 ) ) ;
#70131=CARTESIAN_POINT ( 'NONE',  ( -1.836970198721029983E-15, 155.6249999931720254, 10.00000000000000178 ) ) ;
#70133=CARTESIAN_POINT ( 'NONE',  ( 10.00000000000000888, 20.20833333333333925, -2.679491924311228956 ) ) ;
#70134=CARTESIAN_POINT ( 'NONE',  ( -5.676582343750006032, 49.42708332991935549, 9.832129032723418760 ) ) ;
#70136=CARTESIAN_POINT ( 'NONE',  ( -11.35316468749999785, 198.0729166632526983, -3.042071309553167513 ) ) ;
#70142=CARTESIAN_POINT ( 'NONE',  ( -11.35316468750000141, 178.2812499965860411, -1.390361679473963753E-15 ) ) ;
#70144=EDGE_CURVE ( 'NONE', #70231, #26901, #49196, .T. ) ;
#70148=CARTESIAN_POINT ( 'NONE',  ( -11.35316468750000141, 163.5937499965860127, -1.390361679473963753E-15 ) ) ;
#70150=CARTESIAN_POINT ( 'NONE',  ( -8.311093377946836114, 127.9687499965860269, -8.311093377946837890 ) ) ;
#70178=CARTESIAN_POINT ( 'NONE',  ( 4.721056650415999201, 296.2343750017069510, -4.721056650415999201 ) ) ;
#70179=CARTESIAN_POINT ( 'NONE',  ( 6.123233995736767268E-16, 131.2500000000000000, -10.00000000000000178 ) ) ;
#70196=CARTESIAN_POINT ( 'NONE',  ( -5.676582343749998039, 22.44791666325268409, -9.832129032723420536 ) ) ;
#70197=CARTESIAN_POINT ( 'NONE',  ( 8.660254037844673292, 25.41666666666685970, -5.000000000000164313 ) ) ;
#70198=CARTESIAN_POINT ( 'NONE',  ( 8.311093377946837890, 221.7187499965860127, -8.311093377946837890 ) ) ;
#70205=CARTESIAN_POINT ( 'NONE',  ( 5.676582343749993598, 34.94791666325268409, 9.832129032723422313 ) ) ;
#70209=CYLINDRICAL_SURFACE ( 'NONE', #39527, 10.00000000000000178 ) ;
#70211=CARTESIAN_POINT ( 'NONE',  ( -11.35316468750000141, 23.48958332991934839, 3.042071309553159963 ) ) ;
#70213=CARTESIAN_POINT ( 'NONE',  ( 5.676582343749993598, 144.9479166632526983, 9.832129032723422313 ) ) ;
#70214=CARTESIAN_POINT ( 'NONE',  ( -10.00000000000000178, 114.3749999931720396, -1.224646799147353454E-15 ) ) ;
#70219=CARTESIAN_POINT ( 'NONE',  ( -8.311093377946836114, 7.968749996586014461, -8.311093377946837890 ) ) ;
#70220=VERTEX_POINT ( 'NONE', #39012 ) ;
#70222=CARTESIAN_POINT ( 'NONE',  ( -4.721056650415999201, 299.3281250017069510, -4.721056650415999201 ) ) ;
#70224=CARTESIAN_POINT ( 'NONE',  ( -8.311093377946841443, 133.9062499965860411, 8.311093377946834337 ) ) ;
#70231=VERTEX_POINT ( 'NONE', #15982 ) ;
#70234=CARTESIAN_POINT ( 'NONE',  ( -4.999999999999998224, 203.5416666598387110, -8.660254037844389075 ) ) ;
#70236=CARTESIAN_POINT ( 'NONE',  ( 5.676582343749993598, 90.26041666325268409, 9.832129032723422313 ) ) ;
#70240=VERTEX_POINT ( 'NONE', #61273 ) ;
#70250=ORIENTED_EDGE ( 'NONE', *, *, #71229, .F. ) ;
#70264=CARTESIAN_POINT ( 'NONE',  ( 7.320508075688774596, 100.6250000000000142, -7.320508075688774596 ) ) ;
#70266=CARTESIAN_POINT ( 'NONE',  ( 8.311093377946837890, 56.71874999658601979, -8.311093377946837890 ) ) ;
#70267=CARTESIAN_POINT ( 'NONE',  ( 2.765530957082001251, 294.9218750017070647, 6.676582343750000703 ) ) ;
#70269=CARTESIAN_POINT ( 'NONE',  ( 8.660254037844422825, 190.4166666666667140, -5.000000000000020428 ) ) ;
#70273=CARTESIAN_POINT ( 'NONE',  ( -4.999999999999999112, 51.66666666666667851, -8.660254037844390851 ) ) ;
#70278=CARTESIAN_POINT ( 'NONE',  ( -1.836970198721029983E-15, 208.7500000000000284, 10.00000000000000178 ) ) ;
#70280=CARTESIAN_POINT ( 'NONE',  ( 11.35316468749999785, 175.8854166632527267, 3.042071309553174174 ) ) ;
#70287=CARTESIAN_POINT ( 'NONE',  ( -11.35316468749999785, 33.38541666325269119, -3.042071309553167513 ) ) ;
#70289=CARTESIAN_POINT ( 'NONE',  ( 5.676582343749993598, 225.2604166632526983, 9.832129032723422313 ) ) ;
#70295=CARTESIAN_POINT ( 'NONE',  ( 10.00000000000000000, 71.66666665983871098, 2.679491924311236062 ) ) ;
#70298=CARTESIAN_POINT ( 'NONE',  ( -1.538508811358849613E-11, 71.25000000000120792, -10.00000000000000178 ) ) ;
#70299=CARTESIAN_POINT ( 'NONE',  ( -10.00000000000000178, 49.37499999317203248, -1.224646799147353454E-15 ) ) ;
#70300=CARTESIAN_POINT ( 'NONE',  ( 0.000000000000000000, 300.0000000000000000, 0.000000000000000000 ) ) ;
#70303=CARTESIAN_POINT ( 'NONE',  ( 6.676582343750004256, 296.0468750017069510, 2.765530957081995478 ) ) ;
#70304=CARTESIAN_POINT ( 'NONE',  ( -10.00000000000001421, 142.5000000000000284, -1.224646799147355031E-15 ) ) ;
#70306=CARTESIAN_POINT ( 'NONE',  ( 11.35316468749999785, 160.5729166632526699, 3.042071309553174174 ) ) ;
#70308=CARTESIAN_POINT ( 'NONE',  ( 5.000000000000002665, 5.833333333333334814, -8.660254037844389075 ) ) ;
#70313=EDGE_CURVE ( 'NONE', #58925, #47752, #63718, .T. ) ;
#70316=CARTESIAN_POINT ( 'NONE',  ( -5.676582343749998039, 137.7604166632526983, -9.832129032723420536 ) ) ;
#70318=CARTESIAN_POINT ( 'NONE',  ( 1.102182119232618108E-15, 298.3125000034140157, 6.000000000000001776 ) ) ;
#70321=CARTESIAN_POINT ( 'NONE',  ( 5.676582343749993598, 50.26041666325269119, 9.832129032723422313 ) ) ;
#70323=CARTESIAN_POINT ( 'NONE',  ( 7.320508075688774596, 37.49999999317203958, -7.320508075688774596 ) ) ;
#70328=CARTESIAN_POINT ( 'NONE',  ( 4.242640687119287435, 292.4375000034140157, 4.242640687119285658 ) ) ;
#70351=ORIENTED_EDGE ( 'NONE', *, *, #37486, .T. ) ;
#70355=CARTESIAN_POINT ( 'NONE',  ( 10.00000000000000178, 50.20833333333333570, -2.679491924311226736 ) ) ;
#70357=CARTESIAN_POINT ( 'NONE',  ( 6.000000000000003553, 294.5625000000000000, -2.485281374238571761 ) ) ;
#70363=CARTESIAN_POINT ( 'NONE',  ( 2.679491924311225404, 91.04166666666667140, -9.999999999999982236 ) ) ;
#70364=DIRECTION ( 'NONE',  ( -0.000000000000000000, 1.000000000000000000, -0.000000000000000000 ) ) ;
#70366=CARTESIAN_POINT ( 'NONE',  ( 10.00000000000000178, 202.0833333265053682, -2.679491924311226736 ) ) ;
#70367=CARTESIAN_POINT ( 'NONE',  ( 10.00000000000000000, 169.7916666666666856, 2.679491924311236062 ) ) ;
#70370=CARTESIAN_POINT ( 'NONE',  ( 3.042071309553167069, 137.1354166632526983, -11.35316468749999785 ) ) ;
#70373=CARTESIAN_POINT ( 'NONE',  ( 2.679491924311155682, 107.9166666598386968, -10.00000000000004441 ) ) ;
#70382=CARTESIAN_POINT ( 'NONE',  ( 10.00000000000000178, 41.87499999317203248, 0.000000000000000000 ) ) ;
#70392=FACE_OUTER_BOUND ( 'NONE', #30870, .T. ) ;
#70394=CARTESIAN_POINT ( 'NONE',  ( -3.042071309553173730, 109.3229166632526983, 11.35316468749999785 ) ) ;
#70401=CARTESIAN_POINT ( 'NONE',  ( -5.000000000000004441, 183.3333333333333712, 8.660254037844385522 ) ) ;
#70402=CARTESIAN_POINT ( 'NONE',  ( -11.35316468750000141, 108.2812499965860269, -1.390361679473963753E-15 ) ) ;
#70404=CARTESIAN_POINT ( 'NONE',  ( -1.836970198721029983E-15, 80.62499999317203958, 10.00000000000000178 ) ) ;
#70406=CARTESIAN_POINT ( 'NONE',  ( -5.000000000000005329, 190.2083333265053966, 8.660254037844387298 ) ) ;
#70409=CARTESIAN_POINT ( 'NONE',  ( 6.951808397369818766E-16, 97.34374999658601268, -11.35316468750000141 ) ) ;
#70413=CARTESIAN_POINT ( 'NONE',  ( -8.311093377946841443, 4.218749996586018014, 8.311093377946830785 ) ) ;
#70414=ORIENTED_EDGE ( 'NONE', *, *, #54865, .T. ) ;
#70419=AXIS2_PLACEMENT_3D ( 'NONE', #47249, #17467, #12550 ) ;
#70422=CARTESIAN_POINT ( 'NONE',  ( -6.676582343750000703, 292.5156250017068942, 2.765530957082001251 ) ) ;
#70424=CARTESIAN_POINT ( 'NONE',  ( -8.311093377946836114, 217.9687499965860127, -8.311093377946837890 ) ) ;
#70429=ORIENTED_EDGE ( 'NONE', *, *, #23010, .F. ) ;
#70433=CARTESIAN_POINT ( 'NONE',  ( -8.660254037844387298, 27.08333333333333570, -5.000000000000004441 ) ) ;
#70444=CARTESIAN_POINT ( 'NONE',  ( -4.721056650415999201, 298.3281250017069510, -4.721056650415999201 ) ) ;
#70453=CARTESIAN_POINT ( 'NONE',  ( 0.000000000000000000, 300.0000000000000000, 6.000000000000001776 ) ) ;
#70454=CARTESIAN_POINT ( 'NONE',  ( 5.676582343750001591, 101.9270833299193555, -9.832129032723420536 ) ) ;
#70455=CARTESIAN_POINT ( 'NONE',  ( 0.000000000000000000, 255.9999999999999432, 0.000000000000000000 ) ) ;
#70464=EDGE_CURVE ( 'NONE', #24671, #1694, #53583, .T. ) ;
#70465=CARTESIAN_POINT ( 'NONE',  ( 8.311093377946834337, 210.1562499965860411, 8.311093377946839666 ) ) ;
#70469=CARTESIAN_POINT ( 'NONE',  ( -3.042071309553173730, 179.6354166632526699, 11.35316468749999785 ) ) ;
#70476=CARTESIAN_POINT ( 'NONE',  ( -9.832129032723418760, 62.86458332991935549, -5.676582343750004256 ) ) ;
#70482=CARTESIAN_POINT ( 'NONE',  ( 8.311093377946834337, 70.15624999658602690, 8.311093377946839666 ) ) ;
#70487=CARTESIAN_POINT ( 'NONE',  ( -8.311093377946836114, 67.65624999658601268, -8.311093377946837890 ) ) ;
#70490=CARTESIAN_POINT ( 'NONE',  ( 3.170472398252169882E-12, 128.7500000000002558, 10.00000000000000178 ) ) ;
#70491=CARTESIAN_POINT ( 'NONE',  ( 7.320508075688771044, 161.2499999931720538, 7.320508075688775484 ) ) ;
#70494=CARTESIAN_POINT ( 'NONE',  ( 9.832129032723420536, 66.51041666325268409, -5.676582343749999815 ) ) ;
#70496=CARTESIAN_POINT ( 'NONE',  ( -9.832129032723420536, 198.6979166632526983, 5.676582343749997150 ) ) ;
#70502=CARTESIAN_POINT ( 'NONE',  ( -11.35316468749999785, 173.0729166632526983, -3.042071309553167957 ) ) ;
#70503=DIRECTION ( 'NONE',  ( 0.000000000000000000, 0.000000000000000000, 1.000000000000000000 ) ) ;
#70505=CARTESIAN_POINT ( 'NONE',  ( -7.320508075688773708, 188.7499999931720538, -7.320508075688774596 ) ) ;
#70507=CARTESIAN_POINT ( 'NONE',  ( 6.951808397369818766E-16, 162.3437499965860127, -11.35316468750000141 ) ) ;
#70509=CARTESIAN_POINT ( 'NONE',  ( 7.486112537844476833, 225.9999999999999716, -7.575605162435675943 ) ) ;
#70522=CARTESIAN_POINT ( 'NONE',  ( 5.000000000000021316, 179.1666666666666856, 8.660254037844438812 ) ) ;
#70524=ORIENTED_EDGE ( 'NONE', *, *, #37843, .T. ) ;
#70526=ADVANCED_FACE ( 'NONE', ( #30284 ), #64972, .T. ) ;
#70535=CARTESIAN_POINT ( 'NONE',  ( -1.836970198721029983E-15, 90.62499999317203958, 10.00000000000000178 ) ) ;
#70539=CARTESIAN_POINT ( 'NONE',  ( -4.721056650415999201, 299.4843750017070079, -4.721056650415999201 ) ) ;
#70540=CARTESIAN_POINT ( 'NONE',  ( -10.00000000000000000, 132.2916666666666288, -2.679491924311229845 ) ) ;
#70541=CARTESIAN_POINT ( 'NONE',  ( 6.123233995736767268E-16, 13.12499999317203425, -10.00000000000000178 ) ) ;
#70550=CARTESIAN_POINT ( 'NONE',  ( -10.00000000000000178, 132.5000000000000284, -1.224646799147353454E-15 ) ) ;
#70555=CARTESIAN_POINT ( 'NONE',  ( -8.311093377946836114, 27.65624999658602334, -8.311093377946837890 ) ) ;
#70557=CARTESIAN_POINT ( 'NONE',  ( 9.832129032723416984, 225.6770833299193839, 5.676582343750006032 ) ) ;
#70563=CARTESIAN_POINT ( 'NONE',  ( -11.35316468750000141, 33.28124999658601268, -1.390361679473963753E-15 ) ) ;
#70566=EDGE_CURVE ( 'NONE', #29716, #62209, #13281, .T. ) ;
#70570=CARTESIAN_POINT ( 'NONE',  ( -3.042071309553163960, 37.23958332991934839, -11.35316468749999963 ) ) ;
#70572=CARTESIAN_POINT ( 'NONE',  ( 5.676582343750001591, 146.6145833299193555, -9.832129032723420536 ) ) ;
#70573=CARTESIAN_POINT ( 'NONE',  ( -5.000000000000005329, 110.2083333265053682, 8.660254037844387298 ) ) ;
#70578=CARTESIAN_POINT ( 'NONE',  ( -9.832129032723418760, 3.177083329919349719, -5.676582343750004256 ) ) ;
#70580=CARTESIAN_POINT ( 'NONE',  ( 4.242640687119285658, 289.6249999999999432, -4.242640687119286547 ) ) ;
#70582=CARTESIAN_POINT ( 'NONE',  ( -9.832129032723418760, 142.8645833299193555, -5.676582343750004256 ) ) ;
#70592=CARTESIAN_POINT ( 'NONE',  ( 8.311093377946834337, 85.46874999658599847, 8.311093377946839666 ) ) ;
#70595=EDGE_LOOP ( 'NONE', ( #66917, #59355, #16293, #11150 ) ) ;
#70610=CYLINDRICAL_SURFACE ( 'NONE', #18946, 10.00000000000000178 ) ;
#70612=CARTESIAN_POINT ( 'NONE',  ( 4.999999999999993783, 121.0416666598386968, 8.660254037844390851 ) ) ;
#70614=ORIENTED_EDGE ( 'NONE', *, *, #6508, .T. ) ;
#70615=ORIENTED_EDGE ( 'NONE', *, *, #53428, .F. ) ;
#70621=CARTESIAN_POINT ( 'NONE',  ( 4.999999999999993783, 89.16666666666667140, 8.660254037844390851 ) ) ;
#70625=CARTESIAN_POINT ( 'NONE',  ( 2.765530957081996366, 294.2968750017070079, -6.676582343750003368 ) ) ;
#70631=CARTESIAN_POINT ( 'NONE',  ( -7.320508075688775484, 51.87500000000000000, -7.320508075688776373 ) ) ;
#70636=CARTESIAN_POINT ( 'NONE',  ( -8.660254037844390851, 212.9166666666666572, 4.999999999999998224 ) ) ;
#70638=CARTESIAN_POINT ( 'NONE',  ( 5.676582343749993598, 180.2604166632526699, 9.832129032723422313 ) ) ;
#70645=CARTESIAN_POINT ( 'NONE',  ( 3.042071309553167069, 52.13541666325268409, -11.35316468749999785 ) ) ;
#70647=CARTESIAN_POINT ( 'NONE',  ( -2.085542519210945728E-15, 219.8437499965860411, 11.35316468750000141 ) ) ;
#70650=CARTESIAN_POINT ( 'NONE',  ( 8.660254037844389075, 10.41666666666666963, -5.000000000000000888 ) ) ;
#70652=CARTESIAN_POINT ( 'NONE',  ( 6.123233995736767268E-16, 101.2500000000000000, -10.00000000000000178 ) ) ;
#70654=( BOUNDED_CURVE ( )  B_SPLINE_CURVE ( 2, ( #18907, #12501, #64197, #41914, #13230, #46835, #29496, #58548, #53619, #36635, #59643, #70952, #41187 ),
 .UNSPECIFIED., .F., .F. ) 
 B_SPLINE_CURVE_WITH_KNOTS ( ( 3, 2, 2, 2, 2, 2, 3 ),
 ( 1.491489498479788400, 1.496722359883964071, 1.501955221288139519, 1.507188082692314968, 1.512420944096490638, 1.517653805500666087, 1.522886666904841757 ),
 .UNSPECIFIED. ) 
 CURVE ( )  GEOMETRIC_REPRESENTATION_ITEM ( )  RATIONAL_B_SPLINE_CURVE ( ( 0.9999999999999978906, 0.9659258262890704216, 1.000000000000000000, 0.9659258262890683122, 1.000000000000000000, 0.9659258262890683122, 1.000000000000000000, 0.9659258262890683122, 1.000000000000000000, 0.9659258262890683122, 1.000000000000000000, 0.9659258262890474400, 1.000000000000020872 ) ) 
 REPRESENTATION_ITEM ( '' )  );
#70656=CARTESIAN_POINT ( 'NONE',  ( -8.660254037844390851, 69.79166665983869677, 4.999999999999998224 ) ) ;
#70664=CARTESIAN_POINT ( 'NONE',  ( -4.721056650415999201, 296.4843750017070079, -4.721056650415999201 ) ) ;
#70667=CARTESIAN_POINT ( 'NONE',  ( 9.832129032723420536, 151.1979166632526983, -5.676582343749999815 ) ) ;
#70675=CARTESIAN_POINT ( 'NONE',  ( 8.311093377946837890, 136.7187499965860127, -8.311093377946837890 ) ) ;
#70679=CARTESIAN_POINT ( 'NONE',  ( -5.676582343749998039, 52.76041666325269119, -9.832129032723420536 ) ) ;
#70685=CARTESIAN_POINT ( 'NONE',  ( 2.485281374238571317, 292.7500000034140157, -6.000000000000003553 ) ) ;
#70686=DIRECTION ( 'NONE',  ( -0.000000000000000000, 1.000000000000000000, -0.000000000000000000 ) ) ;
#70690=CARTESIAN_POINT ( 'NONE',  ( -4.999999999999998224, 63.54166665983869677, -8.660254037844389075 ) ) ;
#70692=ORIENTED_EDGE ( 'NONE', *, *, #2542, .T. ) ;
#70704=ORIENTED_EDGE ( 'NONE', *, *, #2234, .T. ) ;
#70708=CARTESIAN_POINT ( 'NONE',  ( 8.660254037844389075, 55.41666666666667140, -5.000000000000000000 ) ) ;
#70711=CARTESIAN_POINT ( 'NONE',  ( -6.000000000000000888, 297.0624999999999432, 2.485281374238575758 ) ) ;
#70718=CARTESIAN_POINT ( 'NONE',  ( -2.679491924311161455, 75.41666665983871098, 10.00000000000004441 ) ) ;
#70721=CARTESIAN_POINT ( 'NONE',  ( -2.679491924311235174, 140.4166666598387110, 10.00000000000000000 ) ) ;
#70722=CARTESIAN_POINT ( 'NONE',  ( 8.660254037844389075, 175.4166666666666572, -5.000000000000000000 ) ) ;
#70726=CARTESIAN_POINT ( 'NONE',  ( 11.35316468749999963, 141.3020833299193271, -3.042071309553165293 ) ) ;
#70733=CARTESIAN_POINT ( 'NONE',  ( 6.951808397369818766E-16, 7.343749996586017126, -11.35316468750000141 ) ) ;
#70739=EDGE_CURVE ( 'NONE', #55811, #48555, #9516, .T. ) ;
#70741=CARTESIAN_POINT ( 'NONE',  ( 7.320508075688771044, 31.24999999317203248, 7.320508075688775484 ) ) ;
#70749=( BOUNDED_SURFACE ( )  B_SPLINE_SURFACE ( 1, 2, ( 
 ( #26847, #57027, #73991, #45317, #68332, #49862, #21185, #44210, #38930, #15155, #55173, #61191, #14776, #50238, #54794, #16263, #39303, #73259, #9521, #15526, #61567, #27596, #49492, #38567, #49869, #8764, #3105, #3478, #21932, #72511, #72885, #32536, #32917, #31774, #55547, #21564, #37816, #44962, #4601, #26091, #61932, #38187, #26468, #3860, #60811, #44590, #49111, #72123, #20437, #67602, #26855, #9888, #55923, #50607, #20819, #4233, #21192, #43453, #66467, #43837, #67968, #66852, #44217, #67230, #27221, #9135, #15899, #10259, #33284, #56283, #73627, #32152, #23056, #11003, #46065, #62668, #4978, #45692, #68340, #814, #23802, #5345, #29468, #16635, #447, #11741, #27979, #57783, #63046, #34036, #52478, #17391, #69829, #40416, #50984, #57033, #46805, #73997, #63413, #39669, #6465, #34779, #28714, #6090, #69085, #33656, #18144, #62301, #56662, #5714, #28346, #22675, #10629, #12106, #17766, #63788, #22299, #29095, #23426, #78, #52115, #51353, #46440, #45323, #40782, #74364, #69458, #11371, #35144, #68707, #34405, #17018, #40042, #57407, #51729, #58158, #18879, #24161, #65635, #58888, #53955, #2644, #65262, #35870, #30570, #48648, #7197, #7930, #48281, #47173, #13567, #1553, #36238, #52848, #53592, #42620, #70563, #71287, #58517, #36605, #6823, #64537, #64169, #18514, #70205, #31305, #13200, #19607, #13931, #7566, #35504, #25633, #30200, #2268, #29836, #53221, #47908, #12473, #41521, #24532, #1180, #71656, #12834, #25262, #36972, #47540, #41886, #59615, #59254, #70927, #1903, #30934, #42249, #19239, #64897, #59978, #8294, #24890, #54333, #41159, #72797, #38098, #67139, #15433, #26765, #56199, #72417, #9046, #9798, #72029, #50152, #73169, #38844, #55452, #19977, #14310, #3014, #3388, #42985, #31686, #21106, #26373, #66004, #49021, #32821, #4512, #32060, #21475, #20727, #61847, #10167, #27506, #54706, #49783, #55831, #4147, #25996, #44129, #61474, #67510, #3763, #55080, #33203, #27137, #37345, #38471, #49397, #44497, #15063, #15808, #60343, #8671, #50517, #20345, #43362, #61096, #66378, #43745, #14685, #37726, #60724, #66759, #9424, #32443, #73908, #22975, #40696, #52022, #57694, #63699, #62579, #39583, #44872, #11653, #10911, #29388, #51643, #40323, #22212, #68997, #50893, #12025, #39954, #45239, #34687, #62959, #6382, #46352, #67878, #28630, #10538, #51267, #36974, #11285, #68251, #68621, #34315, #16546, #57319, #33944, #16169, #56943, #4886, #35058, #58071, #5259, #73532, #27882, #6003, #45981, #39211, #17304, #74277, #28260, #21840, #63327, #62212, #29004, #33569, #22587, #56573, #45606, #360, #16930, #17679, #23342, #5630, #69369, #59173, #23713, #65550, #59897, #46717, #70482, #47084, #12755, #36887, #2183, #7844, #53872, #52395, #13116, #65171, #64815, #36152, #29747, #7482, #8211, #30851, #69742, #13483, #1469, #30487, #41443, #24450, #64082, #13844, #47459, #731, #42159, #30119, #35427, #25178, #70122, #36522, #18057, #1822, #18428, #41805, #41072, #64455, #19156, #59532, #58434, #24808, #35787, #18801, #12392, #53504, #48193, #7112, #71201, #6744, #47823, #52761, #1098, #24075, #58801, #53136, #70844, #19519, #42537, #61386, #37640, #2928, #8959, #37263, #72710, #2558, #38763, #61762, #21014, #31971, #38010, #9334, #50064, #71945, #61008, #72326, #31222, #25547, #25915, #44408, #20256, #20641, #54996, #55368, #54248, #3303, #44038, #32354, #48560, #71570, #31599, #54620, #3674, #73078, #9712, #15346, #21385, #43278, #66294, #19892, #67046, #14601, #42898, #26673, #38382, #48933, #49697, #8584, #67421, #43656, #60638, #32734, #66668, #65918, #4059, #14222, #55742, #60257, #26289, #49309, #15720, #14974, #27052, #34596, #51179, #4421, #46260, #73817, #45890, #50432, #4798, #16833, #56112, #39122, #22125, #33118, #40608, #27416, #68904, #17214, #62126, #62491, #5537, #5171, #39860, #56853, #34223, #11195, #62862, #16459, #57225, #51932, #74187, #45150, #39496, #28539, #28167, #51547, #74565, #22877, #69279, #10819, #68160, #40233, #10450, #63236, #11563, #28915, #45514, #10080, #73447, #67796, #33854, #21754, #44783, #57603, #22492, #16087, #33480, #5913, #17590, #68530, #270, #23252, #56482, #27792, #50806, #641, #70394, #1739, #47729, #69652, #41717, #30398, #36432, #24361, #1008, #53783, #70753, #63610, #64729, #18338, #53416, #58710, #47368, #6289, #57985, #24720, #19069, #52305, #7020, #42072, #23988, #40983, #11937, #41352, #17965, #65081, #34968, #71110, #19431, #13394, #64362, #18709, #13027, #7759, #29657, #36064, #30029, #29295, #23623, #35338, #2092, #52672, #53044, #12664, #59081, #46632, #35695, #59445, #7391, #1377, #58350, #30762, #25085, #12306, #48101, #63991, #6655, #46997, #70029, #55655, #3971, #60170, #9625, #71477, #55281, #66576, #8123, #37921, #43186, #65826, #32645, #72231, #49974, #20546, #59809, #37168, #26958, #31126, #43560, #19803, #61300, #14881, #8869, #60918, #49220, #13755, #72991, #42443, #36799, #60545, #8489, #2834, #65461, #66954, #72619, #43945, #54156, #3212, #3585, #54903, #26200, #42809, #9241, #2467, #20923, #25458, #26579, #66202, #32263, #31508, #14506, #48473, #14133, #37545, #54528, #49604, #20168, #25825, #15258, #48844, #38292, #71853, #31880, #16006, #10729, #28821, #39036, #62769, #28453, #27326, #68437, #56388, #16366, #33024, #33762, #22779, #50713, #51459, #38671, #45424, #61673, #44692, #44321, #73363, #50340, #34515, #17123, #15631, #74472, #27702, #67708, #56763, #21667, #51090, #51838, #45801, #67334, #57135, #45064, #5084, #10363, #68077, #56026, #57520, #39403, #5825, #11112, #73729, #4335, #68811, #62038, #34136, #21297, #16741, #33388, #28077, #9994, #4708, #5451, #40148, #22037, #39767, #62402, #74103, #22402, #63153, #11480, #29573, #30308, #17502, #24269, #40519, #23532, #23160, #52218, #29205, #13307, #70667, #69189, #53328, #6566, #46545, #52583, #6196, #41632, #46173, #7671, #30677, #64643, #922, #6931, #52956, #18984, #40892, #29941, #41264, #184, #63525, #69564, #36344, #63897, #64272, #23905, #47280, #11847, #46915, #12941, #1290, #12580, #17875, #69940, #35609, #12209, #58624, #550, #34884, #58265, #35247, #59359, #57889, #18248, #41987, #70306, #35978, #18621, #58997, #7302, #1653, #24634, #64998, #47645, #62227, #8784, #71026, #48387, #39227, #19344, #54817, #8032, #72531, #3128, #20083, #31796, #60454, #24997, #67894, #10554, #48014, #71767, #71391, #14044, #53696, #3499, #9156, #55193, #2007, #14422, #66486, #66114, #31040, #44889, #43097, #54064, #14796, #37456, #42357, #26487, #65373, #26111, #13673, #31416, #2374, #16186, #25738, #32173, #49512, #49131, #36712, #59724, #42728, #37834, #25370, #19716, #72143, #65742, #37080, #60083, #8403, #54443, #2751, #60832, #21858, #48759, #20455, #43473, #28644, #40339, #5644, #57709, #34701, #63341, #39970, #6015, #745, #22990, #45623, #62977, #11666, #51659, #29019, #52038, #374, #69757, #11300, #22602, #23355, #10926, #63715, #12038, #52410, #69013, #33585, #27900, #16562, #16946, #56590, #45254, #46369, #34333, #4905, #62596, #69384, #18070, #68637, #35072, #57334, #23728, #46733, #41086, #68266, #17693, #40710, #58084, #39599, #6395, #29401, #64096, #17319, #2, #50909, #73923, #22228, #33963, #45996, #56960, #5275, #28277, #51283, #74293, #25195, #19536, #1113, #7496, #71216, #24465, #64470, #12405, #19172, #58449, #29761, #12768, #35800, #36537, #54265, #65565, #42554, #2575, #1484, #53150, #6757, #48208, #47473, #42917, #65187, #53887, #58816, #7864, #30501, #24089, #1839, #13862, #41818, #36905, #52775, #59548, #47098, #7126, #35439, #30134, #41457, #25564, #8229, #70136, #59913, #18814, #70496, #64828, #18443, #2199, #13132, #19910, #36166, #31239, #59186, #42175, #13499, #48577, #53520, #30869, #24825, #47839, #70861, #71587, #4442, #55013, #32371, #66687, #15365, #65936, #14990, #32752, #21032, #3695, #37657, #61028, #26693, #14618, #49714, #66312, #8601, #49330, #71961, #27433, #50448, #8977, #33136, #20275, #4076, #38401, #31615, #61404, #38028, #60655, #56132, #44056, #73465, #67066, #54636, #31992, #21773, #2945, #9730, #43298, #10099, #55761, #55386, #27070, #72728, #37281, #14244, #60274, #25934, #9352, #3319, #26307, #48950, #15739, #21404, #67441, #72346, #50084, #73097, #44426, #38778, #20658, #61781, #43675, #292, #16105, #5936, #68552, #28561, #33875, #16855, #56502, #58006, #39881, #6312, #34617, #22514, #27815, #69300, #62515, #57623, #29316, #68924, #39517, #34244, #52325, #10841, #11582, #51954, #50826, #17234, #5191, #34991, #74585, #662, #22899, #62146, #56875, #44800, #10469, #45911, #73837, #63629, #40255, #11216, #63257, #51568, #39142, #67813, #33500, #4819, #62883, #28188, #51199, #22143, #17611, #23272, #46281, #45172 ),
 ( #28936, #68184, #16480, #57246, #74210, #40629, #5559, #45535, #11959, #17986, #53438, #35359, #1397, #52695, #13774, #70413, #53803, #48123, #64748, #41005, #59828, #12683, #59465, #64013, #18360, #30417, #69673, #1029, #35717, #46654, #54178, #12327, #7778, #30783, #24009, #24383, #19088, #18730, #1760, #41738, #47751, #24740, #70774, #30051, #42091, #65481, #13046, #58732, #53064, #65103, #36084, #13414, #36452, #2113, #8143, #47391, #7043, #25106, #47018, #71129, #19452, #42465, #59103, #23647, #58370, #6675, #7410, #29679, #70050, #36818, #31147, #41374, #64385, #31526, #67349, #49237, #32663, #26978, #43580, #71497, #38688, #66220, #38311, #42827, #71872, #9259, #48494, #54548, #14526, #25476, #33043, #19821, #61317, #9642, #2855, #54921, #72638, #72252, #32282, #20565, #26600, #3602, #55296, #8887, #49621, #44338, #66595, #37564, #31900, #20941, #14900, #43962, #66971, #15275, #61690, #3230, #60563, #55672, #25843, #3988, #49991, #21316, #37938, #2484, #65845, #60188, #26217, #14155, #37188, #73007, #60938, #8510, #48863, #15647, #10012, #20186, #43205, #33780, #23175, #199, #17516, #67724, #62786, #68827, #40164, #62055, #34151, #22796, #28836, #16758, #68095, #46187, #63169, #56043, #57151, #10746, #45816, #51107, #39783, #73378, #50359, #17139, #11495, #44709, #74119, #34529, #16383, #33406, #4352, #11128, #27343, #21683, #56406, #10380, #57534, #5843, #51855, #56780, #39053, #69205, #73746, #40532, #63538, #5467, #50731, #45442, #11863, #22053, #16022, #4725, #27720, #28468, #39422, #22421, #45080, #68457, #62421, #5101, #28092, #51477, #74489, #48028, #30691, #29219, #65011, #41278, #6580, #12594, #40906, #1667, #6213, #42371, #65386, #24647, #35622, #41645, #12953, #53709, #937, #64655, #1302, #34899, #52232, #29586, #71038, #23919, #24284, #58636, #59010, #57905, #6944, #47658, #35993, #47297, #52599, #29956, #70321, #58278, #18636, #35263, #564, #18263, #63915, #19357, #23547, #46928, #2020, #12226, #70679, #7315, #46559, #30322, #52969, #69953, #25009, #53340, #69580, #18996, #17891, #64288, #42002, #13319, #36357, #59372, #7683, #37849, #54830, #66497, #20465, #59738, #26884, #21224, #8046, #31809, #8415, #48772, #72915, #38218, #43868, #15190, #13684, #49143, #26500, #26123, #72155, #65754, #43485, #44250, #66883, #31051, #49524, #37466, #14808, #2764, #60467, #49901, #19729, #72544, #61223, #3510, #66126, #71404, #9553, #31430, #20850, #36725, #60846, #54457, #3139, #54078, #25751, #55205, #32567, #42739, #9167, #71779, #8796, #25383, #32184, #55575, #43109, #3891, #2386, #48400, #14057, #37093, #60097, #20095, #14433, #45354, #73656, #67262, #21593, #5375, #51760, #56314, #45723, #44991, #34438, #11402, #28744, #4263, #74024, #28376, #51384, #73291, #68368, #34066, #40072, #28007, #4633, #57438, #74397, #15557, #16665, #21965, #57062, #62329, #51016, #9914, #61595, #22706, #68737, #55953, #10656, #17050, #27629, #44619, #38596, #22327, #32946, #27253, #50638, #50268, #67634, #15929, #63077, #5743, #107, #67996, #33316, #38959, #23085, #16292, #61962, #39696, #10290, #39332, #62697, #33689, #56692, #5009, #11034, #7229, #35534, #53621, #18909, #40445, #1212, #57814, #23831, #476, #36269, #18174, #1579, #70592, #12503, #63444, #7593, #35173, #30232, #11769, #40813, #52881, #17421, #23456, #58188, #69114, #1933, #34807, #53251, #24562, #46468, #46838, #41551, #41189, #24192, #64200, #70236, #47204, #18544, #52509, #64569, #13233, #58550, #6492, #846, #12866, #6854, #35902, #58920, #47569, #30599, #69861, #29499, #41915, #69489, #64925, #59285, #46096, #29866, #6121, #29125, #52142, #17799, #63820, #12136, #72060, #20379, #31717, #61128, #2674, #13961, #14719, #2295, #55114, #3418, #43777, #60376, #24921, #19270, #7962, #8325, #47936, #36637, #3047, #31335, #70953, #53985, #37758, #9459, #37004, #26405, #25663, #66789, #15094, #32475, #59645, #54739, #60757, #9079, #30966, #26032, #66409, #72452, #8703, #60007, #38128, #32093, #42281, #49053, #54365, #49433, #20007, #43395, #65295, #13600, #20760, #55484, #25293, #43016, #48310, #48680, #71318, #19637, #42652, #65663, #71687, #66038, #14345, #37375, #15467, #56976, #62613, #68652, #67542, #44529, #49811, #16578, #15839, #34350, #56607, #45271, #4178, #73939, #55862, #16963, #44905, #27165, #39615, #67910, #11316, #51298, #72827, #33600, #38505, #56228, #32856, #39987, #50552, #33979, #28291, #16203, #21134, #62993, #38873, #10945, #44157, #73202, #10570, #67172, #50182, #61878, #26797, #3797, #61505, #5291, #74311, #21509, #4543, #22241, #73566, #4923, #21876, #27918, #50928, #68282, #10200, #22619, #45637, #39243, #33230, #27538, #9828, #62242, #17, #52052, #42839, #23004, #58463, #11681, #2496, #6773, #23746, #35451, #64109, #28658, #71510, #65857, #51672, #759, #389, #17709, #14166, #8153, #13788, #59839, #57347, #18085, #70150, #69770, #41102, #34718, #12418, #5659, #36831, #46010, #18458, #6409, #29777, #46384, #29414, #19833, #63356, #42477, #31159, #47114, #35086, #40354, #54189, #23371, #65493, #69030, #52792, #69401, #46749, #17334, #40724, #24103, #25490, #57724, #1127, #63731, #52424, #6030, #48504, #29035, #12053, #58097, #54560, #61327, #2867, #60575, #60198, #14536, #66234, #50372, #33055, #31538, #67361, #43591, #8900, #14912, #43216, #3999, #8523, #44721, #67738, #26988, #37952, #43974, #15286, #56054, #3243, #66985, #3615, #37199, #25854, #31913, #73390, #26229, #26610, #60952, #9655, #48875, #9270, #50002, #38322, #49634, #54934, #32292, #72650, #49249, #20952, #37576, #71884, #20578, #72264, #21695, #20198, #66606, #4363, #55307, #73019, #32675, #55684, #21330, #44351, #15659, #27354, #38701, #61702, #10023, #23190, #46202, #39431, #211, #73757, #68841, #28480, #33417, #74498, #74130, #68104, #69216, #57161, #17527, #5478, #10392, #16394, #40544, #56417, #51488, #22064, #51870, #22807, #16768, #45828, #17154, #39065, #16033, #62067, #50742, #40175, #5112, #45451, #4738, #27732, #45090, #62431, #10756, #28847, #33795, #56793, #28102, #63178, #51118, #22432, #68468, #62800, #39795, #11140, #34161, #11505, #34538, #57545, #5853, #62198, #5246, #10897, #16916, #15794, #67496, #72783, #39571, #38829, #57305, #4874, #68238, #27122, #22199, #4131, #39939, #67862, #50137, #62567, #16155, #34301, #74265, #21090, #56559, #38457, #4497, #55814, #62945, #73517, #56931, #51254, #39196, #44113, #11269, #61832, #33931, #67122, #21460, #33555, #15417, #73152, #10151, #49766, #26748, #61459, #28246, #22573, #44482, #27490, #45226, #21824, #27869, #44857, #50880, #73895, #16531, #33188, #45593, #68607, #10523, #56185, #50503, #9785, #32806, #52750, #1086, #12377, #41792, #58057, #69355, #70109, #57680, #24437, #41059, #5616, #74644, #63313, #63685, #28616, #17291, #58423, #12012, #51629, #34675, #18415, #64801, #17665, #58788, #6368, #47445, #70469, #13103, #40310, #35413, #41429, #64441, #11639, #6731, #47072, #53123, #64069, #40683, #18787, #12742, #22959, #29735, #35045, #35773, #716, #24062, #45968, #68982, #7098, #30106, #5988, #23700, #1456, #29374, #28990, #52008, #36139, #346, #23326, #46338, #52381, #46705, #69729, #18044, #43264, #49296, #48181, #25164, #30474, #71932, #71188, #14960, #37248, #25902, #59518, #54607, #36509, #72313, #25534, #7831, #20244, #48547, #66652, #31957, #53491, #14210, #70831, #36876, #13470, #20626, #31209, #14586, #8945, #71557, #1808, #43642, #19507, #66279, #24795, #53857, #65904, #47808, #30836, #42525, #7469, #59160, #19143, #37625, #60622, #2169, #59884, #2914, #54234, #60244, #2543, #8570, #31586, #48919, #65539, #54982, #26275, #19879, #13830, #8197, #3289, #42885, #42146, #65159, #44769, #74174, #15707, #27037, #27778, #15332, #68148, #16445, #9321, #73804, #45136, #67033, #38749, #33467, #33102, #67783, #10066, #62113, #39109, #16075, #44394, #10437, #5160, #27404, #50048, #67408, #56469, #56099, #4785, #50791, #22112, #22478, #61749, #73064, #39481, #38367, #62477, #10807, #56839, #73433, #37997, #32342, #20998, #21370, #60995, #49682, #33841, #4408, #55354, #61373, #28152, #45499, #50419, #51165, #21741, #68517, #3659, #26659, #72696, #44024, #9699, #32720, #55728, #4044, #59342, #65356, #53312, #29922, #8016, #24980, #16819, #18967, #47262, #7654, #12923, #1636, #34208, #11184, #30660, #47997, #5525, #35957, #1990, #52940, #68891, #39847, #24617, #62848, #57211, #47626, #28526, #70647, #41970, #71011, #19326, #31023, #6911, #58605, #51534, #53678, #1270, #48368, #64980, #42339, #17201, #13288, #40220, #54047, #58977, #63223, #13656, #7284, #25352, #36696, #74551, #36328, #22862, #70289, #45877, #2358, #64627, #59708, #11550, #30292, #35591, #24250, #18603, #41613 ) ),
 .UNSPECIFIED., .F., .F., .F. ) 
 B_SPLINE_SURFACE_WITH_KNOTS ( ( 2, 2 ),
 ( 3, 2, 2, 2, 2, 2, 2, 2, 2, 2, 2, 2, 2, 2, 2, 2, 2, 2, 2, 2, 2, 2, 2, 2, 2, 2, 2, 2, 2, 2, 2, 2, 2, 2, 2, 2, 2, 2, 2, 2, 2, 2, 2, 2, 2, 2, 2, 2, 2, 2, 2, 2, 2, 2, 2, 2, 2, 2, 2, 2, 2, 2, 2, 2, 2, 2, 2, 2, 2, 2, 2, 2, 2, 2, 2, 2, 2, 2, 2, 2, 2, 2, 2, 2, 2, 2, 2, 2, 2, 2, 2, 2, 2, 2, 2, 2, 2, 2, 2, 2, 2, 2, 2, 2, 2, 2, 2, 2, 2, 2, 2, 2, 2, 2, 2, 2, 2, 2, 2, 2, 2, 2, 2, 2, 2, 2, 2, 2, 2, 2, 2, 2, 2, 2, 2, 2, 2, 2, 2, 2, 2, 2, 2, 2, 2, 2, 2, 2, 2, 2, 2, 2, 2, 2, 2, 2, 2, 2, 2, 2, 2, 2, 2, 2, 2, 2, 2, 2, 2, 2, 2, 2, 2, 2, 2, 2, 2, 2, 2, 2, 2, 2, 2, 2, 2, 2, 2, 2, 2, 2, 2, 2, 2, 2, 2, 2, 2, 2, 2, 2, 2, 2, 2, 2, 2, 2, 2, 2, 2, 2, 2, 2, 2, 2, 2, 2, 2, 2, 2, 2, 2, 2, 2, 2, 2, 2, 2, 2, 2, 2, 2, 2, 2, 2, 2, 2, 2, 2, 2, 2, 2, 2, 2, 2, 2, 2, 2, 2, 2, 2, 2, 2, 2, 2, 2, 2, 2, 2, 2, 2, 2, 2, 2, 2, 2, 2, 2, 2, 2, 2, 2, 2, 2, 2, 2, 2, 2, 2, 2, 2, 2, 2, 2, 2, 2, 2, 2, 2, 2, 2, 2, 2, 2, 2, 2, 2, 2, 2, 2, 2, 2, 2, 2, 2, 2, 2, 2, 2, 2, 2, 2, 2, 2, 2, 2, 2, 2, 2, 2, 2, 2, 2, 2, 2, 2, 2, 2, 2, 2, 2, 2, 2, 2, 2, 2, 2, 2, 2, 2, 2, 2, 2, 2, 2, 2, 2, 2, 2, 2, 2, 2, 2, 2, 2, 2, 2, 2, 2, 2, 2, 2, 2, 2, 2, 2, 2, 2, 2, 2, 2, 2, 2, 2, 2, 2, 2, 2, 2, 2, 2, 2, 2, 2, 2, 2, 2, 2, 2, 2, 2, 2, 2, 2, 2, 2, 2, 2, 2, 2, 2, 2, 2, 2, 2, 2, 2, 2, 2, 2, 2, 2, 2, 2, 2, 2, 2, 2, 2, 2, 2, 2, 2, 2, 2, 2, 2, 2, 2, 2, 2, 2, 2, 2, 2, 2, 2, 2, 2, 2, 2, 2, 2, 2, 2, 2, 2, 2, 2, 2, 2, 2, 2, 2, 2, 2, 2, 2, 2, 2, 2, 2, 2, 2, 2, 2, 2, 2, 2, 2, 2, 2, 2, 2, 2, 2, 2, 2, 2, 2, 2, 2, 2, 2, 2, 2, 2, 2, 2, 2, 2, 2, 2, 2, 2, 2, 2, 2, 2, 2, 2, 2, 2, 2, 2, 2, 2, 2, 2, 2, 2, 2, 2, 2, 2, 2, 2, 2, 2, 2, 2, 2, 2, 2, 2, 2, 2, 2, 2, 2, 2, 2, 2, 2, 2, 2, 2, 2, 2, 2, 2, 2, 2, 2, 3 ),
 ( 0.000000000000000000, 1.000000000000000000 ),
 ( 0.000000000000000000, 0.001811594202898550747, 0.003623188405797101493, 0.005434782608695652023, 0.007246376811594202987, 0.009057971014492753950, 0.01086956521739130405, 0.01268115942028985588, 0.01449275362318840597, 0.01630434782608695607, 0.01811594202898550790, 0.01992753623188405626, 0.02173913043478260809, 0.02355072463768115992, 0.02536231884057971175, 0.02717391304347826012, 0.02898550724637681195, 0.03079710144927536378, 0.03260869565217391214, 0.03442028985507246397, 0.03623188405797101580, 0.03804347826086956763, 0.03985507246376811252, 0.04166666666666666435, 0.04347826086956521618, 0.04528985507246376802, 0.04710144927536231985, 0.04891304347826087168, 0.05072463768115942351, 0.05253623188405796840, 0.05434782608695652023, 0.05615942028985507206, 0.05797101449275362389, 0.05978260869565217572, 0.06159420289855072755, 0.06340579710144927938, 0.06521739130434782428, 0.06702898550724638305, 0.06884057971014492794, 0.07065217391304347283, 0.07246376811594203160, 0.07427536231884057649, 0.07608695652173913526, 0.07789855072463768015, 0.07971014492753622505, 0.08152173913043478382, 0.08333333333333332871, 0.08514492753623188748, 0.08695652173913043237, 0.08876811594202899114, 0.09057971014492753603, 0.09239130434782608092, 0.09420289855072463969, 0.09601449275362318458, 0.09782608695652174335, 0.09963768115942028825, 0.1014492753623188470, 0.1032608695652173919, 0.1050724637681159368, 0.1068840579710144956, 0.1086956521739130405, 0.1105072463768115992, 0.1123188405797101441, 0.1141304347826086890, 0.1159420289855072478, 0.1177536231884057927, 0.1195652173913043514, 0.1213768115942028963, 0.1231884057971014551, 0.1250000000000000000, 0.1268115942028985588, 0.1286231884057970898, 0.1304347826086956486, 0.1322463768115942073, 0.1340579710144927661, 0.1358695652173912971, 0.1376811594202898559, 0.1394927536231884146, 0.1413043478260869457, 0.1431159420289855044, 0.1449275362318840632, 0.1467391304347826220, 0.1485507246376811530, 0.1503623188405797118, 0.1521739130434782705, 0.1539855072463768015, 0.1557971014492753603, 0.1576086956521739191, 0.1594202898550724501, 0.1612318840579710089, 0.1630434782608695676, 0.1648550724637681264, 0.1666666666666666574, 0.1684782608695652162, 0.1702898550724637750, 0.1721014492753623060, 0.1739130434782608647, 0.1757246376811594235, 0.1775362318840579823, 0.1793478260869565133, 0.1811594202898550721, 0.1829710144927536308, 0.1847826086956521618, 0.1865942028985507206, 0.1884057971014492794, 0.1902173913043478382, 0.1920289855072463692, 0.1938405797101449279, 0.1956521739130434867, 0.1974637681159420177, 0.1992753623188405765, 0.2010869565217391353, 0.2028985507246376940, 0.2047101449275362250, 0.2065217391304347838, 0.2083333333333333426, 0.2101449275362318736, 0.2119565217391304324, 0.2137681159420289911, 0.2155797101449275499, 0.2173913043478260809, 0.2192028985507246397, 0.2210144927536231985, 0.2228260869565217295, 0.2246376811594202882, 0.2264492753623188470, 0.2282608695652173780, 0.2300724637681159368, 0.2318840579710144956, 0.2336956521739130543, 0.2355072463768115854, 0.2373188405797101441, 0.2391304347826087029, 0.2409420289855072339, 0.2427536231884057927, 0.2445652173913043514, 0.2463768115942029102, 0.2481884057971014412, 0.2500000000000000000, 0.2518115942028985588, 0.2536231884057971175, 0.2554347826086956763, 0.2572463768115941796, 0.2590579710144927383, 0.2608695652173912971, 0.2626811594202898559, 0.2644927536231884146, 0.2663043478260869734, 0.2681159420289855322, 0.2699275362318840354, 0.2717391304347825942, 0.2735507246376811530, 0.2753623188405797118, 0.2771739130434782705, 0.2789855072463768293, 0.2807971014492753881, 0.2826086956521738913, 0.2844202898550724501, 0.2862318840579710089, 0.2880434782608695676, 0.2898550724637681264, 0.2916666666666666852, 0.2934782608695652439, 0.2952898550724637472, 0.2971014492753623060, 0.2989130434782608647, 0.3007246376811594235, 0.3025362318840579823, 0.3043478260869565410, 0.3061594202898550998, 0.3079710144927536031, 0.3097826086956521618, 0.3115942028985507206, 0.3134057971014492794, 0.3152173913043478382, 0.3170289855072463969, 0.3188405797101449002, 0.3206521739130434590, 0.3224637681159420177, 0.3242753623188405765, 0.3260869565217391353, 0.3278985507246376940, 0.3297101449275362528, 0.3315217391304347561, 0.3333333333333333148, 0.3351449275362318736, 0.3369565217391304324, 0.3387681159420289911, 0.3405797101449275499, 0.3423913043478261087, 0.3442028985507246119, 0.3460144927536231707, 0.3478260869565217295, 0.3496376811594202882, 0.3514492753623188470, 0.3532608695652174058, 0.3550724637681159646, 0.3568840579710144678, 0.3586956521739130266, 0.3605072463768115854, 0.3623188405797101441, 0.3641304347826087029, 0.3659420289855072617, 0.3677536231884058204, 0.3695652173913043237, 0.3713768115942028825, 0.3731884057971014412, 0.3750000000000000000, 0.3768115942028985588, 0.3786231884057971175, 0.3804347826086956763, 0.3822463768115941796, 0.3840579710144927383, 0.3858695652173912971, 0.3876811594202898559, 0.3894927536231884146, 0.3913043478260869734, 0.3931159420289855322, 0.3949275362318840354, 0.3967391304347825942, 0.3985507246376811530, 0.4003623188405797118, 0.4021739130434782705, 0.4039855072463768293, 0.4057971014492753881, 0.4076086956521738913, 0.4094202898550724501, 0.4112318840579710089, 0.4130434782608695676, 0.4148550724637681264, 0.4166666666666666852, 0.4184782608695652439, 0.4202898550724637472, 0.4221014492753623060, 0.4239130434782608647, 0.4257246376811594235, 0.4275362318840579823, 0.4293478260869565410, 0.4311594202898550998, 0.4329710144927536031, 0.4347826086956521618, 0.4365942028985507206, 0.4384057971014492794, 0.4402173913043478382, 0.4420289855072463969, 0.4438405797101449002, 0.4456521739130434590, 0.4474637681159420177, 0.4492753623188405765, 0.4510869565217391353, 0.4528985507246376940, 0.4547101449275362528, 0.4565217391304347561, 0.4583333333333333148, 0.4601449275362318736, 0.4619565217391304324, 0.4637681159420289911, 0.4655797101449275499, 0.4673913043478261087, 0.4692028985507246119, 0.4710144927536231707, 0.4728260869565217295, 0.4746376811594202882, 0.4764492753623188470, 0.4782608695652174058, 0.4800724637681159646, 0.4818840579710144678, 0.4836956521739130266, 0.4855072463768115854, 0.4873188405797101441, 0.4891304347826087029, 0.4909420289855072617, 0.4927536231884058204, 0.4945652173913043237, 0.4963768115942028825, 0.4981884057971014412, 0.5000000000000000000, 0.5018115942028985588, 0.5036231884057971175, 0.5054347826086956763, 0.5072463768115942351, 0.5090579710144927938, 0.5108695652173913526, 0.5126811594202898004, 0.5144927536231883591, 0.5163043478260869179, 0.5181159420289854767, 0.5199275362318840354, 0.5217391304347825942, 0.5235507246376811530, 0.5253623188405797118, 0.5271739130434782705, 0.5289855072463768293, 0.5307971014492753881, 0.5326086956521739468, 0.5344202898550725056, 0.5362318840579710644, 0.5380434782608695121, 0.5398550724637680709, 0.5416666666666666297, 0.5434782608695651884, 0.5452898550724637472, 0.5471014492753623060, 0.5489130434782608647, 0.5507246376811594235, 0.5525362318840579823, 0.5543478260869565410, 0.5561594202898550998, 0.5579710144927536586, 0.5597826086956522174, 0.5615942028985507761, 0.5634057971014492239, 0.5652173913043477826, 0.5670289855072463414, 0.5688405797101449002, 0.5706521739130434590, 0.5724637681159420177, 0.5742753623188405765, 0.5760869565217391353, 0.5778985507246376940, 0.5797101449275362528, 0.5815217391304348116, 0.5833333333333333703, 0.5851449275362319291, 0.5869565217391304879, 0.5887681159420289356, 0.5905797101449274944, 0.5923913043478260532, 0.5942028985507246119, 0.5960144927536231707, 0.5978260869565217295, 0.5996376811594202882, 0.6014492753623188470, 0.6032608695652174058, 0.6050724637681159646, 0.6068840579710145233, 0.6086956521739130821, 0.6105072463768116409, 0.6123188405797101996, 0.6141304347826086474, 0.6159420289855072062, 0.6177536231884057649, 0.6195652173913043237, 0.6213768115942028825, 0.6231884057971014412, 0.6250000000000000000, 0.6268115942028985588, 0.6286231884057971175, 0.6304347826086956763, 0.6322463768115942351, 0.6340579710144927938, 0.6358695652173913526, 0.6376811594202898004, 0.6394927536231883591, 0.6413043478260869179, 0.6431159420289854767, 0.6449275362318840354, 0.6467391304347825942, 0.6485507246376811530, 0.6503623188405797118, 0.6521739130434782705, 0.6539855072463768293, 0.6557971014492753881, 0.6576086956521739468, 0.6594202898550725056, 0.6612318840579710644, 0.6630434782608695121, 0.6648550724637680709, 0.6666666666666666297, 0.6684782608695651884, 0.6702898550724637472, 0.6721014492753623060, 0.6739130434782608647, 0.6757246376811594235, 0.6775362318840579823, 0.6793478260869565410, 0.6811594202898550998, 0.6829710144927536586, 0.6847826086956522174, 0.6865942028985507761, 0.6884057971014492239, 0.6902173913043477826, 0.6920289855072463414, 0.6938405797101449002, 0.6956521739130434590, 0.6974637681159420177, 0.6992753623188405765, 0.7010869565217391353, 0.7028985507246376940, 0.7047101449275362528, 0.7065217391304348116, 0.7083333333333333703, 0.7101449275362319291, 0.7119565217391304879, 0.7137681159420289356, 0.7155797101449274944, 0.7173913043478260532, 0.7192028985507246119, 0.7210144927536231707, 0.7228260869565217295, 0.7246376811594202882, 0.7264492753623188470, 0.7282608695652174058, 0.7300724637681159646, 0.7318840579710145233, 0.7336956521739130821, 0.7355072463768116409, 0.7373188405797101996, 0.7391304347826086474, 0.7409420289855072062, 0.7427536231884057649, 0.7445652173913043237, 0.7463768115942028825, 0.7481884057971014412, 0.7500000000000000000, 0.7518115942028985588, 0.7536231884057971175, 0.7554347826086956763, 0.7572463768115942351, 0.7590579710144927938, 0.7608695652173913526, 0.7626811594202898004, 0.7644927536231883591, 0.7663043478260869179, 0.7681159420289854767, 0.7699275362318840354, 0.7717391304347825942, 0.7735507246376811530, 0.7753623188405797118, 0.7771739130434782705, 0.7789855072463768293, 0.7807971014492753881, 0.7826086956521739468, 0.7844202898550725056, 0.7862318840579710644, 0.7880434782608695121, 0.7898550724637680709, 0.7916666666666666297, 0.7934782608695651884, 0.7952898550724637472, 0.7971014492753623060, 0.7989130434782608647, 0.8007246376811594235, 0.8025362318840579823, 0.8043478260869565410, 0.8061594202898550998, 0.8079710144927536586, 0.8097826086956522174, 0.8115942028985507761, 0.8134057971014492239, 0.8152173913043477826, 0.8170289855072463414, 0.8188405797101449002, 0.8206521739130434590, 0.8224637681159420177, 0.8242753623188405765, 0.8260869565217391353, 0.8278985507246376940, 0.8297101449275362528, 0.8315217391304348116, 0.8333333333333333703, 0.8351449275362319291, 0.8369565217391304879, 0.8387681159420289356, 0.8405797101449274944, 0.8423913043478260532, 0.8442028985507246119, 0.8460144927536231707, 0.8478260869565217295, 0.8496376811594202882, 0.8514492753623188470, 0.8532608695652174058, 0.8550724637681159646, 0.8568840579710145233, 0.8586956521739130821, 0.8605072463768116409, 0.8623188405797101996, 0.8641304347826086474, 0.8659420289855072062, 0.8677536231884057649, 0.8695652173913043237, 0.8713768115942028825, 0.8731884057971014412, 0.8750000000000000000, 0.8768115942028985588, 0.8786231884057971175, 0.8804347826086956763, 0.8822463768115942351, 0.8840579710144927938, 0.8858695652173913526, 0.8876811594202898004, 0.8894927536231883591, 0.8913043478260869179, 0.8931159420289854767, 0.8949275362318840354, 0.8967391304347825942, 0.8985507246376811530, 0.9003623188405797118, 0.9021739130434782705, 0.9039855072463768293, 0.9057971014492753881, 0.9076086956521739468, 0.9094202898550725056, 0.9112318840579710644, 0.9130434782608695121, 0.9148550724637680709, 0.9166666666666666297, 0.9184782608695651884, 0.9202898550724637472, 0.9221014492753623060, 0.9239130434782608647, 0.9257246376811594235, 0.9275362318840579823, 0.9293478260869565410, 0.9311594202898550998, 0.9329710144927536586, 0.9347826086956522174, 0.9365942028985507761, 0.9384057971014492239, 0.9402173913043477826, 0.9420289855072463414, 0.9438405797101449002, 0.9456521739130434590, 0.9474637681159420177, 0.9492753623188405765, 0.9510869565217391353, 0.9528985507246376940, 0.9547101449275362528, 0.9565217391304348116, 0.9583333333333333703, 0.9601449275362319291, 0.9619565217391304879, 0.9637681159420289356, 0.9655797101449274944, 0.9673913043478260532, 0.9692028985507246119, 0.9710144927536231707, 0.9728260869565217295, 0.9746376811594202882, 0.9764492753623188470, 0.9782608695652174058, 0.9800724637681159646, 0.9818840579710145233, 0.9826096903791191606 ),
 .UNSPECIFIED. ) 
 GEOMETRIC_REPRESENTATION_ITEM ( )  RATIONAL_B_SPLINE_SURFACE ( (
 ( 1.000000000000000000, 0.9659258262890683122, 1.000000000000000000, 0.9659258262890683122, 1.000000000000000000, 0.9659258262890683122, 1.000000000000000000, 0.9659258262890683122, 1.000000000000000000, 0.9659258262890683122, 1.000000000000000000, 0.9659258262890683122, 1.000000000000000000, 0.9659258262890683122, 1.000000000000000000, 0.9659258262890683122, 1.000000000000000000, 0.9659258262890683122, 1.000000000000000000, 0.9659258262890683122, 1.000000000000000000, 0.9659258262890683122, 1.000000000000000000, 0.9659258262890683122, 1.000000000000000000, 0.9659258262890683122, 1.000000000000000000, 0.9659258262890683122, 1.000000000000000000, 0.9659258262890683122, 1.000000000000000000, 0.9659258262890683122, 1.000000000000000000, 0.9659258262890683122, 1.000000000000000000, 0.9659258262890683122, 1.000000000000000000, 0.9659258262890683122, 1.000000000000000000, 0.9659258262890683122, 1.000000000000000000, 0.9659258262890683122, 1.000000000000000000, 0.9659258262890683122, 1.000000000000000000, 0.9659258262890683122, 1.000000000000000000, 0.9659258262890683122, 1.000000000000000000, 0.9659258262890683122, 1.000000000000000000, 0.9659258262890683122, 1.000000000000000000, 0.9659258262890683122, 1.000000000000000000, 0.9659258262890683122, 1.000000000000000000, 0.9659258262890683122, 1.000000000000000000, 0.9659258262890683122, 1.000000000000000000, 0.9659258262890683122, 1.000000000000000000, 0.9659258262890683122, 1.000000000000000000, 0.9659258262890683122, 1.000000000000000000, 0.9659258262890683122, 1.000000000000000000, 0.9659258262890683122, 1.000000000000000000, 0.9659258262890683122, 1.000000000000000000, 0.9659258262890683122, 1.000000000000000000, 0.9659258262890683122, 1.000000000000000000, 0.9659258262890683122, 1.000000000000000000, 0.9659258262890683122, 1.000000000000000000, 0.9659258262890683122, 1.000000000000000000, 0.9659258262890683122, 1.000000000000000000, 0.9659258262890683122, 1.000000000000000000, 0.9659258262890683122, 1.000000000000000000, 0.9659258262890683122, 1.000000000000000000, 0.9659258262890683122, 1.000000000000000000, 0.9659258262890683122, 1.000000000000000000, 0.9659258262890683122, 1.000000000000000000, 0.9659258262890683122, 1.000000000000000000, 0.9659258262890683122, 1.000000000000000000, 0.9659258262890683122, 1.000000000000000000, 0.9659258262890683122, 1.000000000000000000, 0.9659258262890683122, 1.000000000000000000, 0.9659258262890683122, 1.000000000000000000, 0.9659258262890683122, 1.000000000000000000, 0.9659258262890683122, 1.000000000000000000, 0.9659258262890683122, 1.000000000000000000, 0.9659258262890683122, 1.000000000000000000, 0.9659258262890683122, 1.000000000000000000, 0.9659258262890683122, 1.000000000000000000, 0.9659258262890683122, 1.000000000000000000, 0.9659258262890683122, 1.000000000000000000, 0.9659258262890683122, 1.000000000000000000, 0.9659258262890683122, 1.000000000000000000, 0.9659258262890683122, 1.000000000000000000, 0.9659258262890683122, 1.000000000000000000, 0.9659258262890683122, 1.000000000000000000, 0.9659258262890683122, 1.000000000000000000, 0.9659258262890683122, 1.000000000000000000, 0.9659258262890683122, 1.000000000000000000, 0.9659258262890683122, 1.000000000000000000, 0.9659258262890683122, 1.000000000000000000, 0.9659258262890683122, 1.000000000000000000, 0.9659258262890683122, 1.000000000000000000, 0.9659258262890683122, 1.000000000000000000, 0.9659258262890683122, 1.000000000000000000, 0.9659258262890683122, 1.000000000000000000, 0.9659258262890683122, 1.000000000000000000, 0.9659258262890683122, 1.000000000000000000, 0.9659258262890683122, 1.000000000000000000, 0.9659258262890683122, 1.000000000000000000, 0.9659258262890683122, 1.000000000000000000, 0.9659258262890683122, 1.000000000000000000, 0.9659258262890683122, 1.000000000000000000, 0.9659258262890683122, 1.000000000000000000, 0.9659258262890683122, 1.000000000000000000, 0.9659258262890683122, 1.000000000000000000, 0.9659258262890683122, 1.000000000000000000, 0.9659258262890683122, 1.000000000000000000, 0.9659258262890683122, 1.000000000000000000, 0.9659258262890683122, 1.000000000000000000, 0.9659258262890683122, 1.000000000000000000, 0.9659258262890683122, 1.000000000000000000, 0.9659258262890683122, 1.000000000000000000, 0.9659258262890683122, 1.000000000000000000, 0.9659258262890683122, 1.000000000000000000, 0.9659258262890683122, 1.000000000000000000, 0.9659258262890683122, 1.000000000000000000, 0.9659258262890683122, 1.000000000000000000, 0.9659258262890683122, 1.000000000000000000, 0.9659258262890683122, 1.000000000000000000, 0.9659258262890683122, 1.000000000000000000, 0.9659258262890683122, 1.000000000000000000, 0.9659258262890683122, 1.000000000000000000, 0.9659258262890683122, 1.000000000000000000, 0.9659258262890683122, 1.000000000000000000, 0.9659258262890683122, 1.000000000000000000, 0.9659258262890683122, 1.000000000000000000, 0.9659258262890683122, 1.000000000000000000, 0.9659258262890683122, 1.000000000000000000, 0.9659258262890683122, 1.000000000000000000, 0.9659258262890683122, 1.000000000000000000, 0.9659258262890683122, 1.000000000000000000, 0.9659258262890683122, 1.000000000000000000, 0.9659258262890683122, 1.000000000000000000, 0.9659258262890683122, 1.000000000000000000, 0.9659258262890683122, 1.000000000000000000, 0.9659258262890683122, 1.000000000000000000, 0.9659258262890683122, 1.000000000000000000, 0.9659258262890683122, 1.000000000000000000, 0.9659258262890683122, 1.000000000000000000, 0.9659258262890683122, 1.000000000000000000, 0.9659258262890683122, 1.000000000000000000, 0.9659258262890683122, 1.000000000000000000, 0.9659258262890683122, 1.000000000000000000, 0.9659258262890683122, 1.000000000000000000, 0.9659258262890683122, 1.000000000000000000, 0.9659258262890683122, 1.000000000000000000, 0.9659258262890683122, 1.000000000000000000, 0.9659258262890683122, 1.000000000000000000, 0.9659258262890683122, 1.000000000000000000, 0.9659258262890683122, 1.000000000000000000, 0.9659258262890683122, 1.000000000000000000, 0.9659258262890683122, 1.000000000000000000, 0.9659258262890683122, 1.000000000000000000, 0.9659258262890683122, 1.000000000000000000, 0.9659258262890683122, 1.000000000000000000, 0.9659258262890683122, 1.000000000000000000, 0.9659258262890683122, 1.000000000000000000, 0.9659258262890683122, 1.000000000000000000, 0.9659258262890683122, 1.000000000000000000, 0.9659258262890683122, 1.000000000000000000, 0.9659258262890683122, 1.000000000000000000, 0.9659258262890683122, 1.000000000000000000, 0.9659258262890683122, 1.000000000000000000, 0.9659258262890683122, 1.000000000000000000, 0.9659258262890683122, 1.000000000000000000, 0.9659258262890683122, 1.000000000000000000, 0.9659258262890683122, 1.000000000000000000, 0.9659258262890683122, 1.000000000000000000, 0.9659258262890683122, 1.000000000000000000, 0.9659258262890683122, 1.000000000000000000, 0.9659258262890683122, 1.000000000000000000, 0.9659258262890683122, 1.000000000000000000, 0.9659258262890683122, 1.000000000000000000, 0.9659258262890683122, 1.000000000000000000, 0.9659258262890683122, 1.000000000000000000, 0.9659258262890683122, 1.000000000000000000, 0.9659258262890683122, 1.000000000000000000, 0.9659258262890683122, 1.000000000000000000, 0.9659258262890683122, 1.000000000000000000, 0.9659258262890683122, 1.000000000000000000, 0.9659258262890683122, 1.000000000000000000, 0.9659258262890683122, 1.000000000000000000, 0.9659258262890683122, 1.000000000000000000, 0.9659258262890683122, 1.000000000000000000, 0.9659258262890683122, 1.000000000000000000, 0.9659258262890683122, 1.000000000000000000, 0.9659258262890683122, 1.000000000000000000, 0.9659258262890683122, 1.000000000000000000, 0.9659258262890683122, 1.000000000000000000, 0.9659258262890683122, 1.000000000000000000, 0.9659258262890683122, 1.000000000000000000, 0.9659258262890683122, 1.000000000000000000, 0.9659258262890683122, 1.000000000000000000, 0.9659258262890683122, 1.000000000000000000, 0.9659258262890683122, 1.000000000000000000, 0.9659258262890683122, 1.000000000000000000, 0.9659258262890683122, 1.000000000000000000, 0.9659258262890683122, 1.000000000000000000, 0.9659258262890683122, 1.000000000000000000, 0.9659258262890683122, 1.000000000000000000, 0.9659258262890683122, 1.000000000000000000, 0.9659258262890683122, 1.000000000000000000, 0.9659258262890683122, 1.000000000000000000, 0.9659258262890683122, 1.000000000000000000, 0.9659258262890683122, 1.000000000000000000, 0.9659258262890683122, 1.000000000000000000, 0.9659258262890683122, 1.000000000000000000, 0.9659258262890683122, 1.000000000000000000, 0.9659258262890683122, 1.000000000000000000, 0.9659258262890683122, 1.000000000000000000, 0.9659258262890683122, 1.000000000000000000, 0.9659258262890683122, 1.000000000000000000, 0.9659258262890683122, 1.000000000000000000, 0.9659258262890683122, 1.000000000000000000, 0.9659258262890683122, 1.000000000000000000, 0.9659258262890683122, 1.000000000000000000, 0.9659258262890683122, 1.000000000000000000, 0.9659258262890683122, 1.000000000000000000, 0.9659258262890683122, 1.000000000000000000, 0.9659258262890683122, 1.000000000000000000, 0.9659258262890683122, 1.000000000000000000, 0.9659258262890683122, 1.000000000000000000, 0.9659258262890683122, 1.000000000000000000, 0.9659258262890683122, 1.000000000000000000, 0.9659258262890683122, 1.000000000000000000, 0.9659258262890683122, 1.000000000000000000, 0.9659258262890683122, 1.000000000000000000, 0.9659258262890683122, 1.000000000000000000, 0.9659258262890683122, 1.000000000000000000, 0.9659258262890683122, 1.000000000000000000, 0.9659258262890683122, 1.000000000000000000, 0.9659258262890683122, 1.000000000000000000, 0.9659258262890683122, 1.000000000000000000, 0.9659258262890683122, 1.000000000000000000, 0.9659258262890683122, 1.000000000000000000, 0.9659258262890683122, 1.000000000000000000, 0.9659258262890683122, 1.000000000000000000, 0.9659258262890683122, 1.000000000000000000, 0.9659258262890683122, 1.000000000000000000, 0.9659258262890683122, 1.000000000000000000, 0.9659258262890683122, 1.000000000000000000, 0.9659258262890683122, 1.000000000000000000, 0.9659258262890683122, 1.000000000000000000, 0.9659258262890683122, 1.000000000000000000, 0.9659258262890683122, 1.000000000000000000, 0.9659258262890683122, 1.000000000000000000, 0.9659258262890683122, 1.000000000000000000, 0.9659258262890683122, 1.000000000000000000, 0.9659258262890683122, 1.000000000000000000, 0.9659258262890683122, 1.000000000000000000, 0.9659258262890683122, 1.000000000000000000, 0.9659258262890683122, 1.000000000000000000, 0.9659258262890683122, 1.000000000000000000, 0.9659258262890683122, 1.000000000000000000, 0.9659258262890683122, 1.000000000000000000, 0.9659258262890683122, 1.000000000000000000, 0.9659258262890683122, 1.000000000000000000, 0.9659258262890683122, 1.000000000000000000, 0.9659258262890683122, 1.000000000000000000, 0.9659258262890683122, 1.000000000000000000, 0.9659258262890683122, 1.000000000000000000, 0.9659258262890683122, 1.000000000000000000, 0.9659258262890683122, 1.000000000000000000, 0.9659258262890683122, 1.000000000000000000, 0.9659258262890683122, 1.000000000000000000, 0.9659258262890683122, 1.000000000000000000, 0.9659258262890683122, 1.000000000000000000, 0.9659258262890683122, 1.000000000000000000, 0.9659258262890683122, 1.000000000000000000, 0.9659258262890683122, 1.000000000000000000, 0.9659258262890683122, 1.000000000000000000, 0.9659258262890683122, 1.000000000000000000, 0.9659258262890683122, 1.000000000000000000, 0.9659258262890683122, 1.000000000000000000, 0.9659258262890683122, 1.000000000000000000, 0.9659258262890683122, 1.000000000000000000, 0.9659258262890683122, 1.000000000000000000, 0.9659258262890683122, 1.000000000000000000, 0.9659258262890683122, 1.000000000000000000, 0.9659258262890683122, 1.000000000000000000, 0.9659258262890683122, 1.000000000000000000, 0.9659258262890683122, 1.000000000000000000, 0.9659258262890683122, 1.000000000000000000, 0.9659258262890683122, 1.000000000000000000, 0.9659258262890683122, 1.000000000000000000, 0.9659258262890683122, 1.000000000000000000, 0.9659258262890683122, 1.000000000000000000, 0.9659258262890683122, 1.000000000000000000, 0.9659258262890683122, 1.000000000000000000, 0.9659258262890683122, 1.000000000000000000, 0.9659258262890683122, 1.000000000000000000, 0.9659258262890683122, 1.000000000000000000, 0.9659258262890683122, 1.000000000000000000, 0.9659258262890683122, 1.000000000000000000, 0.9659258262890683122, 1.000000000000000000, 0.9659258262890683122, 1.000000000000000000, 0.9659258262890683122, 1.000000000000000000, 0.9659258262890683122, 1.000000000000000000, 0.9659258262890683122, 1.000000000000000000, 0.9659258262890683122, 1.000000000000000000, 0.9659258262890683122, 1.000000000000000000, 0.9659258262890683122, 1.000000000000000000, 0.9659258262890683122, 1.000000000000000000, 0.9659258262890683122, 1.000000000000000000, 0.9659258262890683122, 1.000000000000000000, 0.9659258262890683122, 1.000000000000000000, 0.9659258262890683122, 1.000000000000000000, 0.9659258262890683122, 1.000000000000000000, 0.9659258262890683122, 1.000000000000000000, 0.9659258262890683122, 1.000000000000000000, 0.9659258262890683122, 1.000000000000000000, 0.9659258262890683122, 1.000000000000000000, 0.9659258262890683122, 1.000000000000000000, 0.9659258262890683122, 1.000000000000000000, 0.9659258262890683122, 1.000000000000000000, 0.9659258262890683122, 1.000000000000000000, 0.9659258262890683122, 1.000000000000000000, 0.9659258262890683122, 1.000000000000000000, 0.9659258262890683122, 1.000000000000000000, 0.9659258262890683122, 1.000000000000000000, 0.9659258262890683122, 1.000000000000000000, 0.9659258262890683122, 1.000000000000000000, 0.9659258262890683122, 1.000000000000000000, 0.9659258262890683122, 1.000000000000000000, 0.9659258262890683122, 1.000000000000000000, 0.9659258262890683122, 1.000000000000000000, 0.9659258262890683122, 1.000000000000000000, 0.9659258262890683122, 1.000000000000000000, 0.9659258262890683122, 1.000000000000000000, 0.9659258262890683122, 1.000000000000000000, 0.9659258262890683122, 1.000000000000000000, 0.9659258262890683122, 1.000000000000000000, 0.9659258262890683122, 1.000000000000000000, 0.9659258262890683122, 1.000000000000000000, 0.9659258262890683122, 1.000000000000000000, 0.9659258262890683122, 1.000000000000000000, 0.9659258262890683122, 1.000000000000000000, 0.9659258262890683122, 1.000000000000000000, 0.9659258262890683122, 1.000000000000000000, 0.9659258262890683122, 1.000000000000000000, 0.9659258262890683122, 1.000000000000000000, 0.9659258262890683122, 1.000000000000000000, 0.9659258262890683122, 1.000000000000000000, 0.9659258262890683122, 1.000000000000000000, 0.9659258262890683122, 1.000000000000000000, 0.9659258262890683122, 1.000000000000000000, 0.9659258262890683122, 1.000000000000000000, 0.9659258262890683122, 1.000000000000000000, 0.9659258262890683122, 1.000000000000000000, 0.9659258262890683122, 1.000000000000000000, 0.9659258262890683122, 1.000000000000000000, 0.9659258262890683122, 1.000000000000000000, 0.9659258262890683122, 1.000000000000000000, 0.9659258262890683122, 1.000000000000000000, 0.9659258262890683122, 1.000000000000000000, 0.9659258262890683122, 1.000000000000000000, 0.9659258262890683122, 1.000000000000000000, 0.9659258262890683122, 1.000000000000000000, 0.9659258262890683122, 1.000000000000000000, 0.9659258262890683122, 1.000000000000000000, 0.9659258262890683122, 1.000000000000000000, 0.9659258262890683122, 1.000000000000000000, 0.9659258262890683122, 1.000000000000000000, 0.9659258262890683122, 1.000000000000000000, 0.9659258262890683122, 1.000000000000000000, 0.9659258262890683122, 1.000000000000000000, 0.9659258262890683122, 1.000000000000000000, 0.9659258262890683122, 1.000000000000000000, 0.9659258262890683122, 1.000000000000000000, 0.9659258262890683122, 1.000000000000000000, 0.9659258262890683122, 1.000000000000000000, 0.9659258262890683122, 1.000000000000000000, 0.9659258262890683122, 1.000000000000000000, 0.9659258262890683122, 1.000000000000000000, 0.9659258262890683122, 1.000000000000000000, 0.9659258262890683122, 1.000000000000000000, 0.9659258262890683122, 1.000000000000000000, 0.9659258262890683122, 1.000000000000000000, 0.9659258262890683122, 1.000000000000000000, 0.9659258262890683122, 1.000000000000000000, 0.9659258262890683122, 1.000000000000000000, 0.9659258262890683122, 1.000000000000000000, 0.9659258262890683122, 1.000000000000000000, 0.9659258262890683122, 1.000000000000000000, 0.9659258262890683122, 1.000000000000000000, 0.9659258262890683122, 1.000000000000000000, 0.9659258262890683122, 1.000000000000000000, 0.9659258262890683122, 1.000000000000000000, 0.9659258262890683122, 1.000000000000000000, 0.9659258262890683122, 1.000000000000000000, 0.9659258262890683122, 1.000000000000000000, 0.9659258262890683122, 1.000000000000000000, 0.9659258262890683122, 1.000000000000000000, 0.9659258262890683122, 1.000000000000000000, 0.9659258262890683122, 1.000000000000000000, 0.9659258262890683122, 1.000000000000000000, 0.9659258262890683122, 1.000000000000000000, 0.9659258262890683122, 1.000000000000000000, 0.9659258262890683122, 1.000000000000000000, 0.9659258262890683122, 1.000000000000000000, 0.9659258262890683122, 1.000000000000000000, 0.9659258262890683122, 1.000000000000000000, 0.9659258262890683122, 1.000000000000000000, 0.9659258262890683122, 1.000000000000000000, 0.9659258262890683122, 1.000000000000000000, 0.9659258262890683122, 1.000000000000000000, 0.9659258262890683122, 1.000000000000000000, 0.9659258262890683122, 1.000000000000000000, 0.9659258262890683122, 1.000000000000000000, 0.9659258262890683122, 1.000000000000000000, 0.9659258262890683122, 1.000000000000000000, 0.9659258262890683122, 1.000000000000000000, 0.9659258262890683122, 1.000000000000000000, 0.9659258262890683122, 1.000000000000000000, 0.9659258262890683122, 1.000000000000000000, 0.9659258262890683122, 1.000000000000000000, 0.9659258262890683122, 1.000000000000000000, 0.9659258262890683122, 1.000000000000000000, 0.9659258262890683122, 1.000000000000000000, 0.9659258262890683122, 1.000000000000000000, 0.9659258262890683122, 1.000000000000000000, 0.9659258262890683122, 1.000000000000000000, 0.9659258262890683122, 1.000000000000000000, 0.9659258262890683122, 1.000000000000000000, 0.9659258262890683122, 1.000000000000000000, 0.9659258262890683122, 1.000000000000000000, 0.9659258262890683122, 1.000000000000000000, 0.9659258262890683122, 1.000000000000000000, 0.9659258262890683122, 1.000000000000000000, 0.9659258262890683122, 1.000000000000000000, 0.9659258262890683122, 1.000000000000000000, 0.9659258262890683122, 1.000000000000000000, 0.9659258262890683122, 1.000000000000000000, 0.9659258262890683122, 1.000000000000000000, 0.9659258262890683122, 1.000000000000000000, 0.9659258262890683122, 1.000000000000000000, 0.9659258262890683122, 1.000000000000000000, 0.9659258262890683122, 1.000000000000000000, 0.9659258262890683122, 1.000000000000000000, 0.9659258262890683122, 1.000000000000000000, 0.9659258262890683122, 1.000000000000000000, 0.9659258262890683122, 1.000000000000000000, 0.9659258262890683122, 1.000000000000000000, 0.9659258262890683122, 1.000000000000000000, 0.9659258262890683122, 1.000000000000000000, 0.9659258262890683122, 1.000000000000000000, 0.9659258262890683122, 1.000000000000000000, 0.9659258262890683122, 1.000000000000000000, 0.9659258262890683122, 1.000000000000000000, 0.9659258262890683122, 1.000000000000000000, 0.9659258262890683122, 1.000000000000000000, 0.9659258262890683122, 1.000000000000000000, 0.9659258262890683122, 1.000000000000000000, 0.9659258262890683122, 1.000000000000000000, 0.9659258262890683122, 1.000000000000000000, 0.9659258262890683122, 1.000000000000000000, 0.9659258262890683122, 1.000000000000000000, 0.9659258262890683122, 1.000000000000000000, 0.9659258262890683122, 1.000000000000000000, 0.9659258262890683122, 1.000000000000000000, 0.9659258262890683122, 1.000000000000000000, 0.9659258262890683122, 1.000000000000000000, 0.9659258262890683122, 1.000000000000000000, 0.9659258262890683122, 1.000000000000000000, 0.9659258262890683122, 1.000000000000000000, 0.9659258262890683122, 1.000000000000000000, 0.9659258262890683122, 1.000000000000000000, 0.9659258262890683122, 1.000000000000000000, 0.9659258262890683122, 1.000000000000000000, 0.9659258262890683122, 1.000000000000000000, 0.9659258262890683122, 1.000000000000000000, 0.9659258262890683122, 1.000000000000000000, 0.9659258262890683122, 1.000000000000000000, 0.9659258262890683122, 1.000000000000000000, 0.9659258262890683122, 1.000000000000000000, 0.9659258262890683122, 1.000000000000000000, 0.9659258262890683122, 1.000000000000000000, 0.9659258262890683122, 1.000000000000000000, 0.9659258262890683122, 1.000000000000000000, 0.9659258262890683122, 1.000000000000000000, 0.9659258262890683122, 1.000000000000000000, 0.9659258262890683122, 1.000000000000000000, 0.9659258262890683122, 1.000000000000000000, 0.9659258262890683122, 1.000000000000000000, 0.9659258262890683122, 1.000000000000000000, 0.9659258262890683122, 1.000000000000000000, 0.9659258262890683122, 1.000000000000000000, 0.9659258262890683122, 1.000000000000000000, 0.9659258262890683122, 1.000000000000000000, 0.9659258262890683122, 1.000000000000000000, 0.9659258262890683122, 1.000000000000000000, 0.9659258262890683122, 1.000000000000000000, 0.9659258262890683122, 1.000000000000000000, 0.9659258262890683122, 1.000000000000000000, 0.9659258262890683122, 1.000000000000000000, 0.9659258262890683122, 1.000000000000000000, 0.9659258262890683122, 1.000000000000000000, 0.9659258262890683122, 1.000000000000000000, 0.9659258262890683122, 1.000000000000000000, 0.9659258262890683122, 1.000000000000000000, 0.9659258262890683122, 1.000000000000000000, 0.9659258262890683122, 1.000000000000000000, 0.9659258262890683122, 1.000000000000000000, 0.9659258262890683122, 1.000000000000000000, 0.9659258262890683122, 1.000000000000000000, 0.9659258262890683122, 1.000000000000000000, 0.9659258262890683122, 1.000000000000000000, 0.9659258262890683122, 1.000000000000000000, 0.9659258262890683122, 1.000000000000000000, 0.9659258262890683122, 1.000000000000000000, 0.9659258262890683122, 1.000000000000000000, 0.9659258262890683122, 1.000000000000000000, 0.9659258262890683122, 1.000000000000000000, 0.9659258262890683122, 1.000000000000000000, 0.9659258262890683122, 1.000000000000000000, 0.9659258262890683122, 1.000000000000000000, 0.9659258262890683122, 1.000000000000000000, 0.9659258262890683122, 1.000000000000000000, 0.9659258262890683122, 1.000000000000000000, 0.9659258262890683122, 1.000000000000000000, 0.9659258262890683122, 1.000000000000000000, 0.9659258262890683122, 1.000000000000000000, 0.9659258262890683122, 1.000000000000000000, 0.9659258262890683122, 1.000000000000000000, 0.9659258262890683122, 1.000000000000000000, 0.9659258262890683122, 1.000000000000000000, 0.9659258262890683122, 1.000000000000000000, 0.9659258262890683122, 1.000000000000000000, 0.9659258262890683122, 1.000000000000000000, 0.9659258262890683122, 1.000000000000000000, 0.9659258262890683122, 1.000000000000000000, 0.9659258262890683122, 1.000000000000000000, 0.9659258262890683122, 1.000000000000000000, 0.9659258262890683122, 1.000000000000000000, 0.9659258262890683122, 1.000000000000000000, 0.9659258262890683122, 1.000000000000000000, 0.9659258262890683122, 1.000000000000000000, 0.9659258262890683122, 1.000000000000000000, 0.9659258262890683122, 1.000000000000000000, 0.9659258262890683122, 1.000000000000000000, 0.9659258262890683122, 1.000000000000000000, 0.9659258262890683122, 1.000000000000000000, 0.9659258262890683122, 1.000000000000000000, 0.9659258262890683122, 1.000000000000000000, 0.9659258262890683122, 1.000000000000000000, 0.9659258262890683122, 1.000000000000000000, 0.9659258262890683122, 1.000000000000000000, 0.9659258262890683122, 1.000000000000000000, 0.9659258262890683122, 1.000000000000000000, 0.9659258262890683122, 1.000000000000000000, 0.9659258262890683122, 1.000000000000000000, 0.9659258262890683122, 1.000000000000000000, 0.9659258262890683122, 1.000000000000000000, 0.9659258262890683122, 1.000000000000000000, 0.9659258262890683122, 1.000000000000000000, 0.9659258262890683122, 1.000000000000000000, 0.9659258262890683122, 1.000000000000000000, 0.9659258262890683122, 1.000000000000000000, 0.9659258262890683122, 1.000000000000000000, 0.9659258262890683122, 1.000000000000000000, 0.9863516207523304047, 0.9836369332600947146),
 ( 1.000000000000000000, 0.9659258262890683122, 1.000000000000000000, 0.9659258262890683122, 1.000000000000000000, 0.9659258262890683122, 1.000000000000000000, 0.9659258262890683122, 1.000000000000000000, 0.9659258262890683122, 1.000000000000000000, 0.9659258262890683122, 1.000000000000000000, 0.9659258262890683122, 1.000000000000000000, 0.9659258262890683122, 1.000000000000000000, 0.9659258262890683122, 1.000000000000000000, 0.9659258262890683122, 1.000000000000000000, 0.9659258262890683122, 1.000000000000000000, 0.9659258262890683122, 1.000000000000000000, 0.9659258262890683122, 1.000000000000000000, 0.9659258262890683122, 1.000000000000000000, 0.9659258262890683122, 1.000000000000000000, 0.9659258262890683122, 1.000000000000000000, 0.9659258262890683122, 1.000000000000000000, 0.9659258262890683122, 1.000000000000000000, 0.9659258262890683122, 1.000000000000000000, 0.9659258262890683122, 1.000000000000000000, 0.9659258262890683122, 1.000000000000000000, 0.9659258262890683122, 1.000000000000000000, 0.9659258262890683122, 1.000000000000000000, 0.9659258262890683122, 1.000000000000000000, 0.9659258262890683122, 1.000000000000000000, 0.9659258262890683122, 1.000000000000000000, 0.9659258262890683122, 1.000000000000000000, 0.9659258262890683122, 1.000000000000000000, 0.9659258262890683122, 1.000000000000000000, 0.9659258262890683122, 1.000000000000000000, 0.9659258262890683122, 1.000000000000000000, 0.9659258262890683122, 1.000000000000000000, 0.9659258262890683122, 1.000000000000000000, 0.9659258262890683122, 1.000000000000000000, 0.9659258262890683122, 1.000000000000000000, 0.9659258262890683122, 1.000000000000000000, 0.9659258262890683122, 1.000000000000000000, 0.9659258262890683122, 1.000000000000000000, 0.9659258262890683122, 1.000000000000000000, 0.9659258262890683122, 1.000000000000000000, 0.9659258262890683122, 1.000000000000000000, 0.9659258262890683122, 1.000000000000000000, 0.9659258262890683122, 1.000000000000000000, 0.9659258262890683122, 1.000000000000000000, 0.9659258262890683122, 1.000000000000000000, 0.9659258262890683122, 1.000000000000000000, 0.9659258262890683122, 1.000000000000000000, 0.9659258262890683122, 1.000000000000000000, 0.9659258262890683122, 1.000000000000000000, 0.9659258262890683122, 1.000000000000000000, 0.9659258262890683122, 1.000000000000000000, 0.9659258262890683122, 1.000000000000000000, 0.9659258262890683122, 1.000000000000000000, 0.9659258262890683122, 1.000000000000000000, 0.9659258262890683122, 1.000000000000000000, 0.9659258262890683122, 1.000000000000000000, 0.9659258262890683122, 1.000000000000000000, 0.9659258262890683122, 1.000000000000000000, 0.9659258262890683122, 1.000000000000000000, 0.9659258262890683122, 1.000000000000000000, 0.9659258262890683122, 1.000000000000000000, 0.9659258262890683122, 1.000000000000000000, 0.9659258262890683122, 1.000000000000000000, 0.9659258262890683122, 1.000000000000000000, 0.9659258262890683122, 1.000000000000000000, 0.9659258262890683122, 1.000000000000000000, 0.9659258262890683122, 1.000000000000000000, 0.9659258262890683122, 1.000000000000000000, 0.9659258262890683122, 1.000000000000000000, 0.9659258262890683122, 1.000000000000000000, 0.9659258262890683122, 1.000000000000000000, 0.9659258262890683122, 1.000000000000000000, 0.9659258262890683122, 1.000000000000000000, 0.9659258262890683122, 1.000000000000000000, 0.9659258262890683122, 1.000000000000000000, 0.9659258262890683122, 1.000000000000000000, 0.9659258262890683122, 1.000000000000000000, 0.9659258262890683122, 1.000000000000000000, 0.9659258262890683122, 1.000000000000000000, 0.9659258262890683122, 1.000000000000000000, 0.9659258262890683122, 1.000000000000000000, 0.9659258262890683122, 1.000000000000000000, 0.9659258262890683122, 1.000000000000000000, 0.9659258262890683122, 1.000000000000000000, 0.9659258262890683122, 1.000000000000000000, 0.9659258262890683122, 1.000000000000000000, 0.9659258262890683122, 1.000000000000000000, 0.9659258262890683122, 1.000000000000000000, 0.9659258262890683122, 1.000000000000000000, 0.9659258262890683122, 1.000000000000000000, 0.9659258262890683122, 1.000000000000000000, 0.9659258262890683122, 1.000000000000000000, 0.9659258262890683122, 1.000000000000000000, 0.9659258262890683122, 1.000000000000000000, 0.9659258262890683122, 1.000000000000000000, 0.9659258262890683122, 1.000000000000000000, 0.9659258262890683122, 1.000000000000000000, 0.9659258262890683122, 1.000000000000000000, 0.9659258262890683122, 1.000000000000000000, 0.9659258262890683122, 1.000000000000000000, 0.9659258262890683122, 1.000000000000000000, 0.9659258262890683122, 1.000000000000000000, 0.9659258262890683122, 1.000000000000000000, 0.9659258262890683122, 1.000000000000000000, 0.9659258262890683122, 1.000000000000000000, 0.9659258262890683122, 1.000000000000000000, 0.9659258262890683122, 1.000000000000000000, 0.9659258262890683122, 1.000000000000000000, 0.9659258262890683122, 1.000000000000000000, 0.9659258262890683122, 1.000000000000000000, 0.9659258262890683122, 1.000000000000000000, 0.9659258262890683122, 1.000000000000000000, 0.9659258262890683122, 1.000000000000000000, 0.9659258262890683122, 1.000000000000000000, 0.9659258262890683122, 1.000000000000000000, 0.9659258262890683122, 1.000000000000000000, 0.9659258262890683122, 1.000000000000000000, 0.9659258262890683122, 1.000000000000000000, 0.9659258262890683122, 1.000000000000000000, 0.9659258262890683122, 1.000000000000000000, 0.9659258262890683122, 1.000000000000000000, 0.9659258262890683122, 1.000000000000000000, 0.9659258262890683122, 1.000000000000000000, 0.9659258262890683122, 1.000000000000000000, 0.9659258262890683122, 1.000000000000000000, 0.9659258262890683122, 1.000000000000000000, 0.9659258262890683122, 1.000000000000000000, 0.9659258262890683122, 1.000000000000000000, 0.9659258262890683122, 1.000000000000000000, 0.9659258262890683122, 1.000000000000000000, 0.9659258262890683122, 1.000000000000000000, 0.9659258262890683122, 1.000000000000000000, 0.9659258262890683122, 1.000000000000000000, 0.9659258262890683122, 1.000000000000000000, 0.9659258262890683122, 1.000000000000000000, 0.9659258262890683122, 1.000000000000000000, 0.9659258262890683122, 1.000000000000000000, 0.9659258262890683122, 1.000000000000000000, 0.9659258262890683122, 1.000000000000000000, 0.9659258262890683122, 1.000000000000000000, 0.9659258262890683122, 1.000000000000000000, 0.9659258262890683122, 1.000000000000000000, 0.9659258262890683122, 1.000000000000000000, 0.9659258262890683122, 1.000000000000000000, 0.9659258262890683122, 1.000000000000000000, 0.9659258262890683122, 1.000000000000000000, 0.9659258262890683122, 1.000000000000000000, 0.9659258262890683122, 1.000000000000000000, 0.9659258262890683122, 1.000000000000000000, 0.9659258262890683122, 1.000000000000000000, 0.9659258262890683122, 1.000000000000000000, 0.9659258262890683122, 1.000000000000000000, 0.9659258262890683122, 1.000000000000000000, 0.9659258262890683122, 1.000000000000000000, 0.9659258262890683122, 1.000000000000000000, 0.9659258262890683122, 1.000000000000000000, 0.9659258262890683122, 1.000000000000000000, 0.9659258262890683122, 1.000000000000000000, 0.9659258262890683122, 1.000000000000000000, 0.9659258262890683122, 1.000000000000000000, 0.9659258262890683122, 1.000000000000000000, 0.9659258262890683122, 1.000000000000000000, 0.9659258262890683122, 1.000000000000000000, 0.9659258262890683122, 1.000000000000000000, 0.9659258262890683122, 1.000000000000000000, 0.9659258262890683122, 1.000000000000000000, 0.9659258262890683122, 1.000000000000000000, 0.9659258262890683122, 1.000000000000000000, 0.9659258262890683122, 1.000000000000000000, 0.9659258262890683122, 1.000000000000000000, 0.9659258262890683122, 1.000000000000000000, 0.9659258262890683122, 1.000000000000000000, 0.9659258262890683122, 1.000000000000000000, 0.9659258262890683122, 1.000000000000000000, 0.9659258262890683122, 1.000000000000000000, 0.9659258262890683122, 1.000000000000000000, 0.9659258262890683122, 1.000000000000000000, 0.9659258262890683122, 1.000000000000000000, 0.9659258262890683122, 1.000000000000000000, 0.9659258262890683122, 1.000000000000000000, 0.9659258262890683122, 1.000000000000000000, 0.9659258262890683122, 1.000000000000000000, 0.9659258262890683122, 1.000000000000000000, 0.9659258262890683122, 1.000000000000000000, 0.9659258262890683122, 1.000000000000000000, 0.9659258262890683122, 1.000000000000000000, 0.9659258262890683122, 1.000000000000000000, 0.9659258262890683122, 1.000000000000000000, 0.9659258262890683122, 1.000000000000000000, 0.9659258262890683122, 1.000000000000000000, 0.9659258262890683122, 1.000000000000000000, 0.9659258262890683122, 1.000000000000000000, 0.9659258262890683122, 1.000000000000000000, 0.9659258262890683122, 1.000000000000000000, 0.9659258262890683122, 1.000000000000000000, 0.9659258262890683122, 1.000000000000000000, 0.9659258262890683122, 1.000000000000000000, 0.9659258262890683122, 1.000000000000000000, 0.9659258262890683122, 1.000000000000000000, 0.9659258262890683122, 1.000000000000000000, 0.9659258262890683122, 1.000000000000000000, 0.9659258262890683122, 1.000000000000000000, 0.9659258262890683122, 1.000000000000000000, 0.9659258262890683122, 1.000000000000000000, 0.9659258262890683122, 1.000000000000000000, 0.9659258262890683122, 1.000000000000000000, 0.9659258262890683122, 1.000000000000000000, 0.9659258262890683122, 1.000000000000000000, 0.9659258262890683122, 1.000000000000000000, 0.9659258262890683122, 1.000000000000000000, 0.9659258262890683122, 1.000000000000000000, 0.9659258262890683122, 1.000000000000000000, 0.9659258262890683122, 1.000000000000000000, 0.9659258262890683122, 1.000000000000000000, 0.9659258262890683122, 1.000000000000000000, 0.9659258262890683122, 1.000000000000000000, 0.9659258262890683122, 1.000000000000000000, 0.9659258262890683122, 1.000000000000000000, 0.9659258262890683122, 1.000000000000000000, 0.9659258262890683122, 1.000000000000000000, 0.9659258262890683122, 1.000000000000000000, 0.9659258262890683122, 1.000000000000000000, 0.9659258262890683122, 1.000000000000000000, 0.9659258262890683122, 1.000000000000000000, 0.9659258262890683122, 1.000000000000000000, 0.9659258262890683122, 1.000000000000000000, 0.9659258262890683122, 1.000000000000000000, 0.9659258262890683122, 1.000000000000000000, 0.9659258262890683122, 1.000000000000000000, 0.9659258262890683122, 1.000000000000000000, 0.9659258262890683122, 1.000000000000000000, 0.9659258262890683122, 1.000000000000000000, 0.9659258262890683122, 1.000000000000000000, 0.9659258262890683122, 1.000000000000000000, 0.9659258262890683122, 1.000000000000000000, 0.9659258262890683122, 1.000000000000000000, 0.9659258262890683122, 1.000000000000000000, 0.9659258262890683122, 1.000000000000000000, 0.9659258262890683122, 1.000000000000000000, 0.9659258262890683122, 1.000000000000000000, 0.9659258262890683122, 1.000000000000000000, 0.9659258262890683122, 1.000000000000000000, 0.9659258262890683122, 1.000000000000000000, 0.9659258262890683122, 1.000000000000000000, 0.9659258262890683122, 1.000000000000000000, 0.9659258262890683122, 1.000000000000000000, 0.9659258262890683122, 1.000000000000000000, 0.9659258262890683122, 1.000000000000000000, 0.9659258262890683122, 1.000000000000000000, 0.9659258262890683122, 1.000000000000000000, 0.9659258262890683122, 1.000000000000000000, 0.9659258262890683122, 1.000000000000000000, 0.9659258262890683122, 1.000000000000000000, 0.9659258262890683122, 1.000000000000000000, 0.9659258262890683122, 1.000000000000000000, 0.9659258262890683122, 1.000000000000000000, 0.9659258262890683122, 1.000000000000000000, 0.9659258262890683122, 1.000000000000000000, 0.9659258262890683122, 1.000000000000000000, 0.9659258262890683122, 1.000000000000000000, 0.9659258262890683122, 1.000000000000000000, 0.9659258262890683122, 1.000000000000000000, 0.9659258262890683122, 1.000000000000000000, 0.9659258262890683122, 1.000000000000000000, 0.9659258262890683122, 1.000000000000000000, 0.9659258262890683122, 1.000000000000000000, 0.9659258262890683122, 1.000000000000000000, 0.9659258262890683122, 1.000000000000000000, 0.9659258262890683122, 1.000000000000000000, 0.9659258262890683122, 1.000000000000000000, 0.9659258262890683122, 1.000000000000000000, 0.9659258262890683122, 1.000000000000000000, 0.9659258262890683122, 1.000000000000000000, 0.9659258262890683122, 1.000000000000000000, 0.9659258262890683122, 1.000000000000000000, 0.9659258262890683122, 1.000000000000000000, 0.9659258262890683122, 1.000000000000000000, 0.9659258262890683122, 1.000000000000000000, 0.9659258262890683122, 1.000000000000000000, 0.9659258262890683122, 1.000000000000000000, 0.9659258262890683122, 1.000000000000000000, 0.9659258262890683122, 1.000000000000000000, 0.9659258262890683122, 1.000000000000000000, 0.9659258262890683122, 1.000000000000000000, 0.9659258262890683122, 1.000000000000000000, 0.9659258262890683122, 1.000000000000000000, 0.9659258262890683122, 1.000000000000000000, 0.9659258262890683122, 1.000000000000000000, 0.9659258262890683122, 1.000000000000000000, 0.9659258262890683122, 1.000000000000000000, 0.9659258262890683122, 1.000000000000000000, 0.9659258262890683122, 1.000000000000000000, 0.9659258262890683122, 1.000000000000000000, 0.9659258262890683122, 1.000000000000000000, 0.9659258262890683122, 1.000000000000000000, 0.9659258262890683122, 1.000000000000000000, 0.9659258262890683122, 1.000000000000000000, 0.9659258262890683122, 1.000000000000000000, 0.9659258262890683122, 1.000000000000000000, 0.9659258262890683122, 1.000000000000000000, 0.9659258262890683122, 1.000000000000000000, 0.9659258262890683122, 1.000000000000000000, 0.9659258262890683122, 1.000000000000000000, 0.9659258262890683122, 1.000000000000000000, 0.9659258262890683122, 1.000000000000000000, 0.9659258262890683122, 1.000000000000000000, 0.9659258262890683122, 1.000000000000000000, 0.9659258262890683122, 1.000000000000000000, 0.9659258262890683122, 1.000000000000000000, 0.9659258262890683122, 1.000000000000000000, 0.9659258262890683122, 1.000000000000000000, 0.9659258262890683122, 1.000000000000000000, 0.9659258262890683122, 1.000000000000000000, 0.9659258262890683122, 1.000000000000000000, 0.9659258262890683122, 1.000000000000000000, 0.9659258262890683122, 1.000000000000000000, 0.9659258262890683122, 1.000000000000000000, 0.9659258262890683122, 1.000000000000000000, 0.9659258262890683122, 1.000000000000000000, 0.9659258262890683122, 1.000000000000000000, 0.9659258262890683122, 1.000000000000000000, 0.9659258262890683122, 1.000000000000000000, 0.9659258262890683122, 1.000000000000000000, 0.9659258262890683122, 1.000000000000000000, 0.9659258262890683122, 1.000000000000000000, 0.9659258262890683122, 1.000000000000000000, 0.9659258262890683122, 1.000000000000000000, 0.9659258262890683122, 1.000000000000000000, 0.9659258262890683122, 1.000000000000000000, 0.9659258262890683122, 1.000000000000000000, 0.9659258262890683122, 1.000000000000000000, 0.9659258262890683122, 1.000000000000000000, 0.9659258262890683122, 1.000000000000000000, 0.9659258262890683122, 1.000000000000000000, 0.9659258262890683122, 1.000000000000000000, 0.9659258262890683122, 1.000000000000000000, 0.9659258262890683122, 1.000000000000000000, 0.9659258262890683122, 1.000000000000000000, 0.9659258262890683122, 1.000000000000000000, 0.9659258262890683122, 1.000000000000000000, 0.9659258262890683122, 1.000000000000000000, 0.9659258262890683122, 1.000000000000000000, 0.9659258262890683122, 1.000000000000000000, 0.9659258262890683122, 1.000000000000000000, 0.9659258262890683122, 1.000000000000000000, 0.9659258262890683122, 1.000000000000000000, 0.9659258262890683122, 1.000000000000000000, 0.9659258262890683122, 1.000000000000000000, 0.9659258262890683122, 1.000000000000000000, 0.9659258262890683122, 1.000000000000000000, 0.9659258262890683122, 1.000000000000000000, 0.9659258262890683122, 1.000000000000000000, 0.9659258262890683122, 1.000000000000000000, 0.9659258262890683122, 1.000000000000000000, 0.9659258262890683122, 1.000000000000000000, 0.9659258262890683122, 1.000000000000000000, 0.9659258262890683122, 1.000000000000000000, 0.9659258262890683122, 1.000000000000000000, 0.9659258262890683122, 1.000000000000000000, 0.9659258262890683122, 1.000000000000000000, 0.9659258262890683122, 1.000000000000000000, 0.9659258262890683122, 1.000000000000000000, 0.9659258262890683122, 1.000000000000000000, 0.9659258262890683122, 1.000000000000000000, 0.9659258262890683122, 1.000000000000000000, 0.9659258262890683122, 1.000000000000000000, 0.9659258262890683122, 1.000000000000000000, 0.9659258262890683122, 1.000000000000000000, 0.9659258262890683122, 1.000000000000000000, 0.9659258262890683122, 1.000000000000000000, 0.9659258262890683122, 1.000000000000000000, 0.9659258262890683122, 1.000000000000000000, 0.9659258262890683122, 1.000000000000000000, 0.9659258262890683122, 1.000000000000000000, 0.9659258262890683122, 1.000000000000000000, 0.9659258262890683122, 1.000000000000000000, 0.9659258262890683122, 1.000000000000000000, 0.9659258262890683122, 1.000000000000000000, 0.9659258262890683122, 1.000000000000000000, 0.9659258262890683122, 1.000000000000000000, 0.9659258262890683122, 1.000000000000000000, 0.9659258262890683122, 1.000000000000000000, 0.9659258262890683122, 1.000000000000000000, 0.9659258262890683122, 1.000000000000000000, 0.9659258262890683122, 1.000000000000000000, 0.9659258262890683122, 1.000000000000000000, 0.9659258262890683122, 1.000000000000000000, 0.9659258262890683122, 1.000000000000000000, 0.9659258262890683122, 1.000000000000000000, 0.9659258262890683122, 1.000000000000000000, 0.9659258262890683122, 1.000000000000000000, 0.9659258262890683122, 1.000000000000000000, 0.9659258262890683122, 1.000000000000000000, 0.9659258262890683122, 1.000000000000000000, 0.9659258262890683122, 1.000000000000000000, 0.9659258262890683122, 1.000000000000000000, 0.9659258262890683122, 1.000000000000000000, 0.9659258262890683122, 1.000000000000000000, 0.9659258262890683122, 1.000000000000000000, 0.9659258262890683122, 1.000000000000000000, 0.9659258262890683122, 1.000000000000000000, 0.9659258262890683122, 1.000000000000000000, 0.9659258262890683122, 1.000000000000000000, 0.9659258262890683122, 1.000000000000000000, 0.9659258262890683122, 1.000000000000000000, 0.9659258262890683122, 1.000000000000000000, 0.9659258262890683122, 1.000000000000000000, 0.9659258262890683122, 1.000000000000000000, 0.9659258262890683122, 1.000000000000000000, 0.9659258262890683122, 1.000000000000000000, 0.9659258262890683122, 1.000000000000000000, 0.9659258262890683122, 1.000000000000000000, 0.9659258262890683122, 1.000000000000000000, 0.9659258262890683122, 1.000000000000000000, 0.9659258262890683122, 1.000000000000000000, 0.9659258262890683122, 1.000000000000000000, 0.9659258262890683122, 1.000000000000000000, 0.9659258262890683122, 1.000000000000000000, 0.9659258262890683122, 1.000000000000000000, 0.9659258262890683122, 1.000000000000000000, 0.9659258262890683122, 1.000000000000000000, 0.9659258262890683122, 1.000000000000000000, 0.9659258262890683122, 1.000000000000000000, 0.9659258262890683122, 1.000000000000000000, 0.9659258262890683122, 1.000000000000000000, 0.9659258262890683122, 1.000000000000000000, 0.9659258262890683122, 1.000000000000000000, 0.9659258262890683122, 1.000000000000000000, 0.9659258262890683122, 1.000000000000000000, 0.9659258262890683122, 1.000000000000000000, 0.9659258262890683122, 1.000000000000000000, 0.9659258262890683122, 1.000000000000000000, 0.9659258262890683122, 1.000000000000000000, 0.9659258262890683122, 1.000000000000000000, 0.9659258262890683122, 1.000000000000000000, 0.9659258262890683122, 1.000000000000000000, 0.9659258262890683122, 1.000000000000000000, 0.9659258262890683122, 1.000000000000000000, 0.9659258262890683122, 1.000000000000000000, 0.9659258262890683122, 1.000000000000000000, 0.9659258262890683122, 1.000000000000000000, 0.9659258262890683122, 1.000000000000000000, 0.9659258262890683122, 1.000000000000000000, 0.9659258262890683122, 1.000000000000000000, 0.9659258262890683122, 1.000000000000000000, 0.9659258262890683122, 1.000000000000000000, 0.9659258262890683122, 1.000000000000000000, 0.9659258262890683122, 1.000000000000000000, 0.9659258262890683122, 1.000000000000000000, 0.9659258262890683122, 1.000000000000000000, 0.9659258262890683122, 1.000000000000000000, 0.9659258262890683122, 1.000000000000000000, 0.9659258262890683122, 1.000000000000000000, 0.9659258262890683122, 1.000000000000000000, 0.9659258262890683122, 1.000000000000000000, 0.9659258262890683122, 1.000000000000000000, 0.9659258262890683122, 1.000000000000000000, 0.9659258262890683122, 1.000000000000000000, 0.9659258262890683122, 1.000000000000000000, 0.9659258262890683122, 1.000000000000000000, 0.9659258262890683122, 1.000000000000000000, 0.9659258262890683122, 1.000000000000000000, 0.9659258262890683122, 1.000000000000000000, 0.9659258262890683122, 1.000000000000000000, 0.9659258262890683122, 1.000000000000000000, 0.9659258262890683122, 1.000000000000000000, 0.9659258262890683122, 1.000000000000000000, 0.9659258262890683122, 1.000000000000000000, 0.9659258262890683122, 1.000000000000000000, 0.9659258262890683122, 1.000000000000000000, 0.9659258262890683122, 1.000000000000000000, 0.9659258262890683122, 1.000000000000000000, 0.9659258262890683122, 1.000000000000000000, 0.9659258262890683122, 1.000000000000000000, 0.9659258262890683122, 1.000000000000000000, 0.9659258262890683122, 1.000000000000000000, 0.9659258262890683122, 1.000000000000000000, 0.9659258262890683122, 1.000000000000000000, 0.9659258262890683122, 1.000000000000000000, 0.9659258262890683122, 1.000000000000000000, 0.9659258262890683122, 1.000000000000000000, 0.9659258262890683122, 1.000000000000000000, 0.9659258262890683122, 1.000000000000000000, 0.9659258262890683122, 1.000000000000000000, 0.9659258262890683122, 1.000000000000000000, 0.9659258262890683122, 1.000000000000000000, 0.9659258262890683122, 1.000000000000000000, 0.9659258262890683122, 1.000000000000000000, 0.9659258262890683122, 1.000000000000000000, 0.9659258262890683122, 1.000000000000000000, 0.9659258262890683122, 1.000000000000000000, 0.9659258262890683122, 1.000000000000000000, 0.9659258262890683122, 1.000000000000000000, 0.9659258262890683122, 1.000000000000000000, 0.9659258262890683122, 1.000000000000000000, 0.9659258262890683122, 1.000000000000000000, 0.9659258262890683122, 1.000000000000000000, 0.9659258262890683122, 1.000000000000000000, 0.9659258262890683122, 1.000000000000000000, 0.9659258262890683122, 1.000000000000000000, 0.9659258262890683122, 1.000000000000000000, 0.9659258262890683122, 1.000000000000000000, 0.9659258262890683122, 1.000000000000000000, 0.9659258262890683122, 1.000000000000000000, 0.9659258262890683122, 1.000000000000000000, 0.9659258262890683122, 1.000000000000000000, 0.9659258262890683122, 1.000000000000000000, 0.9659258262890683122, 1.000000000000000000, 0.9659258262890683122, 1.000000000000000000, 0.9659258262890683122, 1.000000000000000000, 0.9659258262890683122, 1.000000000000000000, 0.9659258262890683122, 1.000000000000000000, 0.9659258262890683122, 1.000000000000000000, 0.9659258262890683122, 1.000000000000000000, 0.9659258262890683122, 1.000000000000000000, 0.9659258262890683122, 1.000000000000000000, 0.9659258262890683122, 1.000000000000000000, 0.9659258262890683122, 1.000000000000000000, 0.9659258262890683122, 1.000000000000000000, 0.9659258262890683122, 1.000000000000000000, 0.9659258262890683122, 1.000000000000000000, 0.9659258262890683122, 1.000000000000000000, 0.9659258262890683122, 1.000000000000000000, 0.9659258262890683122, 1.000000000000000000, 0.9659258262890683122, 1.000000000000000000, 0.9659258262890683122, 1.000000000000000000, 0.9659258262890683122, 1.000000000000000000, 0.9659258262890683122, 1.000000000000000000, 0.9659258262890683122, 1.000000000000000000, 0.9659258262890683122, 1.000000000000000000, 0.9659258262890683122, 1.000000000000000000, 0.9659258262890683122, 1.000000000000000000, 0.9659258262890683122, 1.000000000000000000, 0.9659258262890683122, 1.000000000000000000, 0.9659258262890683122, 1.000000000000000000, 0.9659258262890683122, 1.000000000000000000, 0.9659258262890683122, 1.000000000000000000, 0.9659258262890683122, 1.000000000000000000, 0.9659258262890683122, 1.000000000000000000, 0.9659258262890683122, 1.000000000000000000, 0.9659258262890683122, 1.000000000000000000, 0.9659258262890683122, 1.000000000000000000, 0.9863516207523304047, 0.9836369332600947146) ) ) 
 REPRESENTATION_ITEM ( '' )  SURFACE ( )  );
#70753=CARTESIAN_POINT ( 'NONE',  ( 8.311093377946837890, 111.4062499965860269, -8.311093377946837890 ) ) ;
#70761=CARTESIAN_POINT ( 'NONE',  ( 8.311093377946834337, 110.1562499965860269, 8.311093377946839666 ) ) ;
#70763=CARTESIAN_POINT ( 'NONE',  ( 1.681385197618709730E-11, 51.24999999999869971, -10.00000000000000178 ) ) ;
#70766=CARTESIAN_POINT ( 'NONE',  ( 4.999999999999993783, 206.0416666598387110, 8.660254037844390851 ) ) ;
#70768=EDGE_CURVE ( 'NONE', #24662, #3122, #68, .T. ) ;
#70770=CARTESIAN_POINT ( 'NONE',  ( 6.951808397369818766E-16, 102.3437499965860127, -11.35316468750000141 ) ) ;
#70774=CARTESIAN_POINT ( 'NONE',  ( -2.085542519210945728E-15, 9.843749996586018014, 11.35316468750000141 ) ) ;
#70776=ORIENTED_EDGE ( 'NONE', *, *, #5924, .T. ) ;
#70782=CARTESIAN_POINT ( 'NONE',  ( -4.088227598258586603E-16, 294.2031250017069510, -6.676582343750001591 ) ) ;
#70784=CARTESIAN_POINT ( 'NONE',  ( 3.042071309553167513, 222.1354166632526699, -11.35316468749999785 ) ) ;
#70797=VERTEX_POINT ( 'NONE', #73254 ) ;
#70802=CARTESIAN_POINT ( 'NONE',  ( 2.295000000000000373, 261.4319999999996753, 5.413231402905805290 ) ) ;
#70803=CARTESIAN_POINT ( 'NONE',  ( 6.676582343750001591, 292.9531250017069510, -8.176455196517173205E-16 ) ) ;
#70807=APPLICATION_CONTEXT ( 'automotive_design' ) ;
#70817=CARTESIAN_POINT ( 'NONE',  ( -11.35316468750000141, 103.5937499965860269, -1.390361679473963753E-15 ) ) ;
#70818=CARTESIAN_POINT ( 'NONE',  ( -7.320508075688776373, 123.1250000000000284, 7.320508075688768379 ) ) ;
#70826=CARTESIAN_POINT ( 'NONE',  ( -3.042071309553164404, 217.2395833299192986, -11.35316468749999963 ) ) ;
#70831=CARTESIAN_POINT ( 'NONE',  ( 3.042071309553167069, 192.1354166632526130, -11.35316468749999785 ) ) ;
#70838=CARTESIAN_POINT ( 'NONE',  ( -11.35316468750000141, 73.28124999658602690, -1.390361679473963753E-15 ) ) ;
#70844=CARTESIAN_POINT ( 'NONE',  ( 3.042071309553167069, 81.82291666325268409, -11.35316468749999785 ) ) ;
#70849=CARTESIAN_POINT ( 'NONE',  ( 2.679491924317126905, 76.04166666666614560, -9.999999999996632027 ) ) ;
#70851=CARTESIAN_POINT ( 'NONE',  ( -11.35316468750000141, 73.28124999658602690, -1.390361679473963753E-15 ) ) ;
#70855=CARTESIAN_POINT ( 'NONE',  ( 5.000000000000001776, 167.7083333265053682, -8.660254037844389075 ) ) ;
#70857=AXIS2_PLACEMENT_3D ( 'NONE', #13550, #36588, #59599 ) ;
#70859=CARTESIAN_POINT ( 'NONE',  ( 8.311093377946834337, 60.46874999658602690, 8.311093377946839666 ) ) ;
#70861=CARTESIAN_POINT ( 'NONE',  ( 6.951808397369818766E-16, 202.0312499965860411, -11.35316468750000141 ) ) ;
#70862=ORIENTED_EDGE ( 'NONE', *, *, #32581, .F. ) ;
#70867=CARTESIAN_POINT ( 'NONE',  ( -11.35316468749999785, 198.0729166632526983, -3.042071309553167957 ) ) ;
#70868=LINE ( 'NONE', #46740, #61062 ) ;
#70872=CARTESIAN_POINT ( 'NONE',  ( 5.676582343749993598, 185.2604166632526983, 9.832129032723422313 ) ) ;
#70878=CARTESIAN_POINT ( 'NONE',  ( 10.00000000000000000, 4.791666666666666075, 2.679491924311236062 ) ) ;
#70884=CARTESIAN_POINT ( 'NONE',  ( -5.000000000000007105, 188.3333333333333428, 8.660254037844389075 ) ) ;
#70887=CARTESIAN_POINT ( 'NONE',  ( 2.679491924294600480, 178.9583333333318649, 10.00000000000966160 ) ) ;
#70895=VERTEX_POINT ( 'NONE', #33651 ) ;
#70898=CARTESIAN_POINT ( 'NONE',  ( -10.00000000000000178, 114.3749999931720396, -1.224646799147353454E-15 ) ) ;
#70902=CARTESIAN_POINT ( 'NONE',  ( 6.676582343750001591, 294.1093750017069510, -8.176455196517173205E-16 ) ) ;
#70903=CARTESIAN_POINT ( 'NONE',  ( -5.000000000000005329, 153.3333333333333428, 8.660254037844387298 ) ) ;
#70915=CARTESIAN_POINT ( 'NONE',  ( -10.00000000000000355, 132.7083333333333428, 2.679491924311223183 ) ) ;
#70920=CARTESIAN_POINT ( 'NONE',  ( -9.832129032723418760, 22.86458332991934839, -5.676582343750004256 ) ) ;
#70921=CARTESIAN_POINT ( 'NONE',  ( 7.320508075688771044, 6.249999993172032475, 7.320508075688775484 ) ) ;
#70923=CARTESIAN_POINT ( 'NONE',  ( 1.269536070779894168E-12, 186.2499999999999147, -10.00000000000000178 ) ) ;
#70927=CARTESIAN_POINT ( 'NONE',  ( 8.311093377946834337, 40.15624999658601268, 8.311093377946839666 ) ) ;
#70933=CARTESIAN_POINT ( 'NONE',  ( 11.35316468750000141, 35.78124999658601268, 0.000000000000000000 ) ) ;
#70935=CARTESIAN_POINT ( 'NONE',  ( -8.311093377946836114, 152.6562499965859843, -8.311093377946837890 ) ) ;
#70936=CARTESIAN_POINT ( 'NONE',  ( 10.00000000000000000, 116.6666666598387110, 2.679491924311236062 ) ) ;
#70938=CYLINDRICAL_SURFACE ( 'NONE', #22809, 6.000000000000001776 ) ;
#70941=CARTESIAN_POINT ( 'NONE',  ( 11.35316468750000141, 21.09374999658601624, 0.000000000000000000 ) ) ;
#70945=CARTESIAN_POINT ( 'NONE',  ( 11.35316468749999963, 150.9895833299193271, -3.042071309553165293 ) ) ;
#70952=CARTESIAN_POINT ( 'NONE',  ( 2.679491924309757689, 121.0416666666668135, -10.00000000000085443 ) ) ;
#70953=CARTESIAN_POINT ( 'NONE',  ( 8.311093377946834337, 100.4687499965860269, 8.311093377946839666 ) ) ;
#70977=CARTESIAN_POINT ( 'NONE',  ( -1.836970198721029983E-15, 120.6249999931720396, 10.00000000000000178 ) ) ;
#70987=CARTESIAN_POINT ( 'NONE',  ( -10.00000000000000000, 92.29166666666667140, -2.679491924311229845 ) ) ;
#70989=CARTESIAN_POINT ( 'NONE',  ( -6.676582343750003368, 295.5468750017069510, -2.765530957081996810 ) ) ;
#70993=DIRECTION ( 'NONE',  ( -0.000000000000000000, 1.000000000000000000, -0.000000000000000000 ) ) ;
#70994=DIRECTION ( 'NONE',  ( 0.000000000000000000, 0.000000000000000000, 1.000000000000000000 ) ) ;
#70998=CARTESIAN_POINT ( 'NONE',  ( 6.123233995736767268E-16, 211.2500000000000284, -10.00000000000000178 ) ) ;
#71000=CARTESIAN_POINT ( 'NONE',  ( -11.35316468750000141, 188.5937499965860127, -1.390361679473963753E-15 ) ) ;
#71001=DIRECTION ( 'NONE',  ( -0.000000000000000000, 1.000000000000000000, -0.000000000000000000 ) ) ;
#71009=CARTESIAN_POINT ( 'NONE',  ( -11.35316468750000141, 53.80208332991935549, 3.042071309553159963 ) ) ;
#71011=CARTESIAN_POINT ( 'NONE',  ( 5.676582343749993598, 220.2604166632526983, 9.832129032723422313 ) ) ;
#71017=CARTESIAN_POINT ( 'NONE',  ( 8.311093377946834337, 105.1562499965860269, 8.311093377946839666 ) ) ;
#71018=CARTESIAN_POINT ( 'NONE',  ( 7.320508075688771044, 81.24999999317201116, 7.320508075688775484 ) ) ;
#71024=CARTESIAN_POINT ( 'NONE',  ( -4.721056650415998313, 294.7343750017069510, 4.721056650416000089 ) ) ;
#71025=CARTESIAN_POINT ( 'NONE',  ( -7.320508075688783478, 141.8750000000000000, -7.320508075688784366 ) ) ;
#71026=CARTESIAN_POINT ( 'NONE',  ( -9.832129032723418760, 162.8645833299193839, -5.676582343750004256 ) ) ;
#71027=DIRECTION ( 'NONE',  ( 0.000000000000000000, 0.000000000000000000, 1.000000000000000000 ) ) ;
#71034=CARTESIAN_POINT ( 'NONE',  ( -11.35316468750000141, 143.5937499965860411, -1.390361679473963753E-15 ) ) ;
#71038=CARTESIAN_POINT ( 'NONE',  ( -5.676582343749998039, 47.76041666325269119, -9.832129032723420536 ) ) ;
#71039=ORIENTED_EDGE ( 'NONE', *, *, #66223, .F. ) ;
#71042=ADVANCED_FACE ( 'NONE', ( #58512 ), #74358, .T. ) ;
#71044=CARTESIAN_POINT ( 'NONE',  ( -2.485281374238572649, 291.2500000034140157, 6.000000000000002665 ) ) ;
#71045=LINE ( 'NONE', #53349, #61796 ) ;
#71049=VECTOR ( 'NONE', #32975, 1000.000000000000000 ) ;
#71068=CARTESIAN_POINT ( 'NONE',  ( -7.320508075688773708, 56.87500000000000711, -7.320508075688774596 ) ) ;
#71070=CARTESIAN_POINT ( 'NONE',  ( -4.242640687119285658, 298.1250000000000000, 4.242640687119287435 ) ) ;
#71078=CARTESIAN_POINT ( 'NONE',  ( -8.660254037844390851, 74.79166665983871098, 4.999999999999998224 ) ) ;
#71082=CARTESIAN_POINT ( 'NONE',  ( 6.123233995736767268E-16, 176.2500000000000284, -10.00000000000000178 ) ) ;
#71086=CARTESIAN_POINT ( 'NONE',  ( -11.35316468749999785, 138.3854166632526983, -3.042071309553167513 ) ) ;
#71093=CARTESIAN_POINT ( 'NONE',  ( -2.085542519210945728E-15, 14.84374999658601624, 11.35316468750000141 ) ) ;
#71099=CARTESIAN_POINT ( 'NONE',  ( -10.00000000000000178, 39.37499999317203958, -1.224646799147353454E-15 ) ) ;
#71104=CARTESIAN_POINT ( 'NONE',  ( 4.242640687119285658, 291.6875000034139589, -4.242640687119286547 ) ) ;
#71110=CARTESIAN_POINT ( 'NONE',  ( 11.35316468750000141, 115.7812499965860269, 0.000000000000000000 ) ) ;
#71119=CARTESIAN_POINT ( 'NONE',  ( -3.042071309553163960, 107.2395833299193413, -11.35316468749999963 ) ) ;
#71121=CARTESIAN_POINT ( 'NONE',  ( 6.123233995736767268E-16, 83.12499999317203958, -10.00000000000000178 ) ) ;
#71123=CARTESIAN_POINT ( 'NONE',  ( 10.00000000000000178, 212.0833333265053682, -2.679491924311226736 ) ) ;
#71125=CARTESIAN_POINT ( 'NONE',  ( 11.35316468749999963, 106.3020833299193413, -3.042071309553165293 ) ) ;
#71129=CARTESIAN_POINT ( 'NONE',  ( -11.35316468749999785, 13.38541666325268409, -3.042071309553167513 ) ) ;
#71133=CARTESIAN_POINT ( 'NONE',  ( 2.679491924311228956, 117.9166666598386968, -10.00000000000000000 ) ) ;
#71138=CARTESIAN_POINT ( 'NONE',  ( 6.676582343750004256, 291.8906250017069510, 2.765530957081995478 ) ) ;
#71139=CARTESIAN_POINT ( 'NONE',  ( 10.00000000000000000, 126.6666666598386684, 2.679491924311235618 ) ) ;
#71141=AXIS2_PLACEMENT_3D ( 'NONE', #49360, #61436, #55417 ) ;
#71162=CARTESIAN_POINT ( 'NONE',  ( 6.676582343750001591, 291.9531250017069510, -8.176455196517173205E-16 ) ) ;
#71164=CARTESIAN_POINT ( 'NONE',  ( 10.00000000000000178, 137.0833333265053682, -2.679491924311226736 ) ) ;
#71175=CARTESIAN_POINT ( 'NONE',  ( 3.042071309553167069, 97.13541666325266988, -11.35316468749999785 ) ) ;
#71184=CARTESIAN_POINT ( 'NONE',  ( -11.35316468749999785, 213.0729166632527267, -3.042071309553167513 ) ) ;
#71188=CARTESIAN_POINT ( 'NONE',  ( -11.35316468750000141, 188.8020833299193555, 3.042071309553159963 ) ) ;
#71194=CARTESIAN_POINT ( 'NONE',  ( -8.311093377946836114, 87.65624999658601268, -8.311093377946837890 ) ) ;
#71201=CARTESIAN_POINT ( 'NONE',  ( 8.311093377946834337, 80.15624999658599847, 8.311093377946839666 ) ) ;
#71208=CARTESIAN_POINT ( 'NONE',  ( -8.311093377946836114, 77.65624999658601268, -8.311093377946837890 ) ) ;
#71211=CARTESIAN_POINT ( 'NONE',  ( 8.660254037844385522, 166.4583333265053682, 5.000000000000005329 ) ) ;
#71214=CARTESIAN_POINT ( 'NONE',  ( 11.35316468749999785, 60.88541666325268409, 3.042071309553174174 ) ) ;
#71216=CARTESIAN_POINT ( 'NONE',  ( 5.676582343749993598, 189.9479166632526983, 9.832129032723422313 ) ) ;
#71220=CARTESIAN_POINT ( 'NONE',  ( 1.102182119232618108E-15, 288.2500000000000000, 6.000000000000001776 ) ) ;
#71222=CARTESIAN_POINT ( 'NONE',  ( -9.832129032723418760, 192.8645833299193839, -5.676582343750004256 ) ) ;
#71228=CARTESIAN_POINT ( 'NONE',  ( -11.35316468750000141, 183.8020833299193271, 3.042071309553159963 ) ) ;
#71229=EDGE_CURVE ( 'NONE', #63005, #53778, #51153, .T. ) ;
#71236=CARTESIAN_POINT ( 'NONE',  ( -7.320508075688773708, 1.875000000000000222, -7.320508075688774596 ) ) ;
#71246=CARTESIAN_POINT ( 'NONE',  ( 7.320508075688810123, 179.3750000000000284, 7.320508075688813676 ) ) ;
#71253=ADVANCED_FACE ( 'NONE', ( #36600, #47533 ), #7923, .T. ) ;
#71260=CARTESIAN_POINT ( 'NONE',  ( 6.676582343750003368, 294.0468750017070079, 2.765530957081995478 ) ) ;
#71261=CARTESIAN_POINT ( 'NONE',  ( 7.320508075688771044, 154.3750000000000284, 7.320508075688775484 ) ) ;
#71278=CARTESIAN_POINT ( 'NONE',  ( 5.676582343750001591, 36.61458332991934839, -9.832129032723420536 ) ) ;
#71280=CARTESIAN_POINT ( 'NONE',  ( -2.679491924311235618, 10.41666665983870033, 10.00000000000000000 ) ) ;
#71287=CARTESIAN_POINT ( 'NONE',  ( -11.35316468750000141, 33.48958332991934128, 3.042071309553159963 ) ) ;
#71292=CARTESIAN_POINT ( 'NONE',  ( -8.311093377946841443, 33.90624999658601268, 8.311093377946834337 ) ) ;
#71295=( BOUNDED_CURVE ( )  B_SPLINE_CURVE ( 2, ( #47868, #70887, #70522, #71246, #13161, #41847, #6785, #64856, #36198, #59938, #30896, #19202, #29795 ),
 .UNSPECIFIED., .F., .F. ) 
 B_SPLINE_CURVE_WITH_KNOTS ( ( 3, 2, 2, 2, 2, 2, 3 ),
 ( 2.245089840338815534, 2.250322337668932970, 2.255554834999050851, 2.260787332329168287, 2.266019829659286167, 2.271252326989403603, 2.276484824319521039 ),
 .UNSPECIFIED. ) 
 CURVE ( )  GEOMETRIC_REPRESENTATION_ITEM ( )  RATIONAL_B_SPLINE_CURVE ( ( 1.000000000000236033, 0.9659258262888323898, 1.000000000000000000, 0.9659258262890683122, 1.000000000000000000, 0.9659258262890683122, 1.000000000000000000, 0.9659258262890683122, 1.000000000000000000, 0.9659258262890683122, 1.000000000000000000, 0.9659258262890640934, 1.000000000000004219 ) ) 
 REPRESENTATION_ITEM ( '' )  );
#71296=CARTESIAN_POINT ( 'NONE',  ( 3.042071309553159519, 154.7395833299193555, 11.35316468750000141 ) ) ;
#71297=CARTESIAN_POINT ( 'NONE',  ( -10.00000000000000000, 129.1666666598387110, -2.679491924311229845 ) ) ;
#71302=CARTESIAN_POINT ( 'NONE',  ( -8.311093377946841443, 24.21874999658601979, 8.311093377946834337 ) ) ;
#71308=CARTESIAN_POINT ( 'NONE',  ( 8.311093377946834337, 150.1562499965860127, 8.311093377946839666 ) ) ;
#71318=CARTESIAN_POINT ( 'NONE',  ( -8.311093377946836114, 107.9687499965860269, -8.311093377946837890 ) ) ;
#71322=ORIENTED_EDGE ( 'NONE', *, *, #27499, .F. ) ;
#71336=CARTESIAN_POINT ( 'NONE',  ( 0.000000000000000000, 300.0000000000000000, 0.000000000000000000 ) ) ;
#71344=CARTESIAN_POINT ( 'NONE',  ( 6.123233995736767268E-16, 126.2500000000000000, -10.00000000000000178 ) ) ;
#71349=CARTESIAN_POINT ( 'NONE',  ( 10.00000000000000178, 110.2083333333333144, -2.679491924311226736 ) ) ;
#71351=CARTESIAN_POINT ( 'NONE',  ( 6.676582343750003368, 295.1718750017070079, -2.765530957081997254 ) ) ;
#71352=VERTEX_POINT ( 'NONE', #42616 ) ;
#71360=CARTESIAN_POINT ( 'NONE',  ( 10.00000000000000000, 219.7916666666667140, 2.679491924311236062 ) ) ;
#71362=CARTESIAN_POINT ( 'NONE',  ( -11.35316468750000141, 193.8020833299193271, 3.042071309553159963 ) ) ;
#71368=B_SPLINE_CURVE_WITH_KNOTS ( 'NONE', 3,
 ( #20993, #68144, #21366, #5521, #39106, #38746, #56835, #62109, #28521, #45493, #67027, #27775, #9695, #73430, #61745, #72691, #44765, #28147, #16812, #10432, #15325, #67779, #44018, #10062, #38362, #33462, #4039, #39475, #61368, #32716, #56095, #62472, #4780, #73799, #45132, #39842, #4404, #27398, #51161, #74169, #52656, #53027, #29642, #11546, #23973, #18693 ),
 .UNSPECIFIED., .F., .F.,
 ( 4, 2, 2, 2, 2, 2, 2, 2, 2, 2, 2, 2, 2, 2, 2, 2, 2, 2, 2, 2, 2, 2, 4 ),
 ( 2.810287246517312987, 2.811170068070839356, 2.812052889624365726, 2.813818532731418909, 2.814701354284945278, 2.815584175838471648, 2.817349818945524831, 2.819115462052577570, 2.820881105159630753, 2.822646748266683492, 2.823529569820209861, 2.824412391373736231, 2.826178034480789414, 2.827060856034315783, 2.827943677587842153, 2.829709320694895336, 2.830592142248421705, 2.831474963801948075, 2.833240606909001258, 2.834123428462527627, 2.835006250016053997, 2.836771893123107180, 2.838537536230159919 ),
 .UNSPECIFIED. ) ;
#71370=CARTESIAN_POINT ( 'NONE',  ( -5.676582343750006032, 49.42708332991935549, 9.832129032723418760 ) ) ;
#71379=CARTESIAN_POINT ( 'NONE',  ( 6.951808397369818766E-16, 112.0312499965860269, -11.35316468750000141 ) ) ;
#71380=CARTESIAN_POINT ( 'NONE',  ( -7.320508075688778149, 89.99999999317203958, 7.320508075688769267 ) ) ;
#71388=CARTESIAN_POINT ( 'NONE',  ( -2.765530957081998586, 294.7968750017069510, 6.676582343750001591 ) ) ;
#71391=CARTESIAN_POINT ( 'NONE',  ( 9.832129032723420536, 166.1979166632526983, -5.676582343749999815 ) ) ;
#71394=CARTESIAN_POINT ( 'NONE',  ( -5.000000000000020428, 191.6666666666667140, -8.660254037844426378 ) ) ;
#71400=CARTESIAN_POINT ( 'NONE',  ( -8.311093377946841443, 144.2187499965860127, 8.311093377946834337 ) ) ;
#71404=CARTESIAN_POINT ( 'NONE',  ( -11.35316468750000141, 63.80208332991934839, 3.042071309553159963 ) ) ;
#71413=CARTESIAN_POINT ( 'NONE',  ( 6.000000000000003553, 290.5000000034141294, 2.485281374238571317 ) ) ;
#71429=ORIENTED_EDGE ( 'NONE', *, *, #4894, .F. ) ;
#71433=CARTESIAN_POINT ( 'NONE',  ( 10.00000000000000178, 65.00000000000000000, 0.000000000000000000 ) ) ;
#71435=CARTESIAN_POINT ( 'NONE',  ( 6.000000000000003553, 295.5625000000000000, -2.485281374238571761 ) ) ;
#71447=CARTESIAN_POINT ( 'NONE',  ( 2.679491924311222739, 178.9583333333333428, 10.00000000000000355 ) ) ;
#71448=CARTESIAN_POINT ( 'NONE',  ( 6.000000000000003553, 297.5000000034140157, 2.485281374238571317 ) ) ;
#71450=CARTESIAN_POINT ( 'NONE',  ( 5.676582343749993598, 150.2604166632526699, 9.832129032723422313 ) ) ;
#71451=CARTESIAN_POINT ( 'NONE',  ( 2.485281374238196062, 294.7500000034139589, -6.000000000000377476 ) ) ;
#71460=CARTESIAN_POINT ( 'NONE',  ( -11.35316468750000141, 3.593749996586016682, -1.390361679473963753E-15 ) ) ;
#71466=CARTESIAN_POINT ( 'NONE',  ( -1.836970198721029983E-15, 35.62499999317203248, 10.00000000000000178 ) ) ;
#71471=CARTESIAN_POINT ( 'NONE',  ( 0.000000000000000000, 300.0000000000000000, 0.000000000000000000 ) ) ;
#71477=CARTESIAN_POINT ( 'NONE',  ( -11.35316468750000141, 123.2812499965860269, -1.390361679473963753E-15 ) ) ;
#71481=CARTESIAN_POINT ( 'NONE',  ( 3.090149533464540799, 227.8745411751044685, -9.510571794630905629 ) ) ;
#71484=CARTESIAN_POINT ( 'NONE',  ( 8.660254037844405062, 44.58333333333334281, 5.000000000000017764 ) ) ;
#71485=CARTESIAN_POINT ( 'NONE',  ( -8.311093377946836114, 112.6562499965860269, -8.311093377946837890 ) ) ;
#71488=CARTESIAN_POINT ( 'NONE',  ( 1.425702245604163669E-12, 48.75000000000012079, 10.00000000000000178 ) ) ;
#71493=CARTESIAN_POINT ( 'NONE',  ( 8.311093377946834337, 105.4687499965860127, 8.311093377946839666 ) ) ;
#71497=CARTESIAN_POINT ( 'NONE',  ( -3.042071309553164404, 17.55208332991935194, -11.35316468749999963 ) ) ;
#71505=CARTESIAN_POINT ( 'NONE',  ( -5.000000000000005329, 150.2083333265053682, 8.660254037844387298 ) ) ;
#71506=CARTESIAN_POINT ( 'NONE',  ( 2.765530957082001251, 293.7656250017068942, 6.676582343750000703 ) ) ;
#71508=CARTESIAN_POINT ( 'NONE',  ( 6.951808397369818766E-16, 217.3437499965860411, -11.35316468750000141 ) ) ;
#71510=CARTESIAN_POINT ( 'NONE',  ( 8.311093377946834337, 125.4687499965860127, 8.311093377946839666 ) ) ;
#71520=CARTESIAN_POINT ( 'NONE',  ( -7.320508075688842986, 171.8750000000000000, -7.320508075688843874 ) ) ;
#71525=ADVANCED_FACE ( 'NONE', ( #68946 ), #45559, .T. ) ;
#71528=CARTESIAN_POINT ( 'NONE',  ( 6.676582343750003368, 292.8906250017069510, 2.765530957081995478 ) ) ;
#71542=CARTESIAN_POINT ( 'NONE',  ( 8.311093377946837890, 111.7187499965859985, -8.311093377946837890 ) ) ;
#71547=CYLINDRICAL_SURFACE ( 'NONE', #1320, 10.00000000000000178 ) ;
#71552=CARTESIAN_POINT ( 'NONE',  ( 5.676582343749993598, 219.9479166632526983, 9.832129032723422313 ) ) ;
#71557=CARTESIAN_POINT ( 'NONE',  ( -11.35316468750000141, 193.5937499965860127, -1.390361679473963753E-15 ) ) ;
#71559=CARTESIAN_POINT ( 'NONE',  ( 8.261209813499636567, 225.9999999999997726, 6.632190850709866581 ) ) ;
#71563=CARTESIAN_POINT ( 'NONE',  ( -2.085542519210945728E-15, 79.53124999658602690, 11.35316468750000141 ) ) ;
#71570=CARTESIAN_POINT ( 'NONE',  ( -9.832129032723420536, 88.69791666325268409, 5.676582343749997150 ) ) ;
#71571=ORIENTED_EDGE ( 'NONE', *, *, #28739, .T. ) ;
#71577=CARTESIAN_POINT ( 'NONE',  ( -8.311093377946841443, 78.90624999658601268, 8.311093377946834337 ) ) ;
#71581=CARTESIAN_POINT ( 'NONE',  ( -8.660254037844390851, 174.7916666598387110, 4.999999999999998224 ) ) ;
#71584=CARTESIAN_POINT ( 'NONE',  ( -9.832129032723418760, 58.17708332991936260, -5.676582343750004256 ) ) ;
#71585=CARTESIAN_POINT ( 'NONE',  ( -4.721056650415999201, 295.3281250017069510, -4.721056650415999201 ) ) ;
#71587=CARTESIAN_POINT ( 'NONE',  ( -3.042071309553164404, 202.2395833299193271, -11.35316468749999963 ) ) ;
#71593=CARTESIAN_POINT ( 'NONE',  ( 11.35316468749999785, 195.5729166632526983, 3.042071309553174174 ) ) ;
#71598=CARTESIAN_POINT ( 'NONE',  ( 9.832129032723420536, 186.5104166632526983, -5.676582343749999815 ) ) ;
#71601=CARTESIAN_POINT ( 'NONE',  ( -5.000000000000001776, 93.33333333333334281, 8.660254037844381969 ) ) ;
#71605=( BOUNDED_CURVE ( )  B_SPLINE_CURVE ( 2, ( #70298, #19338, #37072, #19707, #54059, #60075, #7294, #35969, #41255, #2368, #53321, #64991, #18240 ),
 .UNSPECIFIED., .F., .F. ) 
 B_SPLINE_CURVE_WITH_KNOTS ( ( 3, 2, 2, 2, 2, 2, 3 ),
 ( 0.8948938610911654212, 0.9001271886622317364, 0.9053605162332980516, 0.9105938438043643668, 0.9158271713754306820, 0.9210604989464967751, 0.9262938265175630903 ),
 .UNSPECIFIED. ) 
 CURVE ( )  GEOMETRIC_REPRESENTATION_ITEM ( )  RATIONAL_B_SPLINE_CURVE ( ( 0.9999999999999248379, 0.9659258262891434743, 1.000000000000000000, 0.9659258262890683122, 1.000000000000000000, 0.9659258262890683122, 1.000000000000000000, 0.9659258262890683122, 1.000000000000000000, 0.9659258262890683122, 1.000000000000000000, 0.9659258262890673130, 1.000000000000001110 ) ) 
 REPRESENTATION_ITEM ( '' )  );
#71612=EDGE_LOOP ( 'NONE', ( #13167, #11590, #26504, #4317 ) ) ;
#71613=CARTESIAN_POINT ( 'NONE',  ( 2.485281374238929697, 293.3750000034140157, 5.999999999999645617 ) ) ;
#71625=CARTESIAN_POINT ( 'NONE',  ( -2.085542519210945728E-15, 59.84374999658602690, 11.35316468750000141 ) ) ;
#71630=CARTESIAN_POINT ( 'NONE',  ( 6.676582343750002480, 296.1718750017070079, -2.765530957081997254 ) ) ;
#71631=CARTESIAN_POINT ( 'NONE',  ( -2.679491924311225848, 141.4583333333333712, -10.00000000000000178 ) ) ;
#71650=CARTESIAN_POINT ( 'NONE',  ( -2.085542519210945728E-15, 44.53124999658601979, 11.35316468750000141 ) ) ;
#71652=CARTESIAN_POINT ( 'NONE',  ( -1.836970198721029983E-15, 15.62499999317203248, 10.00000000000000178 ) ) ;
#71654=CARTESIAN_POINT ( 'NONE',  ( -5.000000000000005329, 130.2083333265053966, 8.660254037844387298 ) ) ;
#71656=CARTESIAN_POINT ( 'NONE',  ( -11.35316468750000141, 38.48958332991935549, 3.042071309553159963 ) ) ;
#71662=CARTESIAN_POINT ( 'NONE',  ( -3.042071309553163960, 27.23958332991934839, -11.35316468749999963 ) ) ;
#71663=EDGE_CURVE ( 'NONE', #33382, #28855, #17437, .T. ) ;
#71665=CARTESIAN_POINT ( 'NONE',  ( -3.042071309553164404, 157.2395833299193555, -11.35316468749999963 ) ) ;
#71667=CARTESIAN_POINT ( 'NONE',  ( 6.123233995736767268E-16, 123.1249999931720396, -10.00000000000000178 ) ) ;
#71669=ORIENTED_EDGE ( 'NONE', *, *, #54026, .F. ) ;
#71670=CARTESIAN_POINT ( 'NONE',  ( 1.102182119232618108E-15, 289.2500000000000000, 6.000000000000001776 ) ) ;
#71671=CARTESIAN_POINT ( 'NONE',  ( -11.35316468749999785, 28.38541666325268054, -3.042071309553167957 ) ) ;
#71677=CARTESIAN_POINT ( 'NONE',  ( 3.042071309553167513, 156.8229166632526983, -11.35316468749999785 ) ) ;
#71685=CARTESIAN_POINT ( 'NONE',  ( 0.000000000000000000, 300.0000000000000000, 10.00000000000000178 ) ) ;
#71687=CARTESIAN_POINT ( 'NONE',  ( -11.35316468750000141, 108.8020833299193555, 3.042071309553159963 ) ) ;
#71707=CARTESIAN_POINT ( 'NONE',  ( -8.660254037844387298, 223.9583333265053966, -5.000000000000004441 ) ) ;
#71710=CARTESIAN_POINT ( 'NONE',  ( -4.721056650415999201, 299.3281250017069510, -4.721056650415999201 ) ) ;
#71712=VERTEX_POINT ( 'NONE', #73080 ) ;
#71720=CARTESIAN_POINT ( 'NONE',  ( 5.000000000000001776, 105.8333333333333286, -8.660254037844389075 ) ) ;
#71722=CARTESIAN_POINT ( 'NONE',  ( -4.721056650415998313, 297.7343750017069510, 4.721056650416000089 ) ) ;
#71729=DIRECTION ( 'NONE',  ( -0.000000000000000000, 1.000000000000000000, -0.000000000000000000 ) ) ;
#71734=CARTESIAN_POINT ( 'NONE',  ( -11.35316468750000141, 3.281249996586016238, -1.390361679473963753E-15 ) ) ;
#71736=CARTESIAN_POINT ( 'NONE',  ( -11.35316468750000141, 198.8020833299193839, 3.042071309553159963 ) ) ;
#71742=ORIENTED_EDGE ( 'NONE', *, *, #67540, .F. ) ;
#71744=CARTESIAN_POINT ( 'NONE',  ( 8.311093377946837890, 46.71874999658602690, -8.311093377946837890 ) ) ;
#71753=CARTESIAN_POINT ( 'NONE',  ( -3.042071309553173730, 124.3229166632526983, 11.35316468749999785 ) ) ;
#71755=CARTESIAN_POINT ( 'NONE',  ( -8.660254037844390851, 94.79166665983871098, 4.999999999999998224 ) ) ;
#71762=CARTESIAN_POINT ( 'NONE',  ( -1.224646799147353454E-15, 225.9999999999999432, 10.00000000000000178 ) ) ;
#71764=CARTESIAN_POINT ( 'NONE',  ( 2.765530957081996366, 292.2968750017070647, -6.676582343750003368 ) ) ;
#71765=DIRECTION ( 'NONE',  ( 0.000000000000000000, 0.000000000000000000, 1.000000000000000000 ) ) ;
#71767=CARTESIAN_POINT ( 'NONE',  ( 11.35316468749999963, 165.9895833299193271, -3.042071309553165293 ) ) ;
#71770=CARTESIAN_POINT ( 'NONE',  ( -7.320508075688805683, 191.8750000000000568, -7.320508075688805683 ) ) ;
#71775=CARTESIAN_POINT ( 'NONE',  ( 3.042071309553159519, 155.0520833299193271, 11.35316468750000141 ) ) ;
#71779=CARTESIAN_POINT ( 'NONE',  ( 8.311093377946837890, 66.71874999658602690, -8.311093377946837890 ) ) ;
#71786=CARTESIAN_POINT ( 'NONE',  ( 6.000000000000003553, 289.6250000034140726, -2.485281374238571761 ) ) ;
#71791=FACE_OUTER_BOUND ( 'NONE', #52440, .T. ) ;
#71793=VERTEX_POINT ( 'NONE', #3676 ) ;
#71796=EDGE_CURVE ( 'NONE', #26622, #30484, #4423, .T. ) ;
#71804=EDGE_CURVE ( 'NONE', #14049, #51233, #48274, .T. ) ;
#71808=LINE ( 'NONE', #50665, #31610 ) ;
#71811=CARTESIAN_POINT ( 'NONE',  ( -1.836970198721029983E-15, 68.75000000000000000, 10.00000000000000178 ) ) ;
#71813=CARTESIAN_POINT ( 'NONE',  ( -6.000000000000003553, 294.9375000000000000, -2.485281374238571317 ) ) ;
#71822=B_SPLINE_CURVE_WITH_KNOTS ( 'NONE', 3,
 ( #63399, #34021, #27964, #44947 ),
 .UNSPECIFIED., .F., .F.,
 ( 4, 4 ),
 ( 0.000000000000000000, 1.000000000000000000 ),
 .UNSPECIFIED. ) ;
#71824=CARTESIAN_POINT ( 'NONE',  ( 6.123233995736767268E-16, 186.2500000000000000, -10.00000000000000178 ) ) ;
#71828=CARTESIAN_POINT ( 'NONE',  ( -11.35316468750000141, 153.8020833299192986, 3.042071309553159963 ) ) ;
#71835=CARTESIAN_POINT ( 'NONE',  ( -9.832129032723420536, 9.010416663252684089, 5.676582343749997150 ) ) ;
#71840=CARTESIAN_POINT ( 'NONE',  ( 7.320508075688771044, 46.24999999317202537, 7.320508075688775484 ) ) ;
#71845=CYLINDRICAL_SURFACE ( 'NONE', #51589, 10.00000000000000178 ) ;
#71853=CARTESIAN_POINT ( 'NONE',  ( 9.832129032723416984, 135.3645833299193555, 5.676582343750006032 ) ) ;
#71857=CARTESIAN_POINT ( 'NONE',  ( 0.000000000000000000, 0.000000000000000000, 0.000000000000000000 ) ) ;
#71859=DIRECTION ( 'NONE',  ( -0.000000000000000000, 1.000000000000000000, -0.000000000000000000 ) ) ;
#71861=CARTESIAN_POINT ( 'NONE',  ( 8.311093377946837890, 121.4062499965860127, -8.311093377946837890 ) ) ;
#71868=CARTESIAN_POINT ( 'NONE',  ( -8.311093377946841443, 99.21874999658601268, 8.311093377946834337 ) ) ;
#71872=CARTESIAN_POINT ( 'NONE',  ( -11.35316468750000141, 18.59374999658601979, -1.390361679473963753E-15 ) ) ;
#71879=CARTESIAN_POINT ( 'NONE',  ( 2.765530957081996366, 290.1406250017069510, -6.676582343750003368 ) ) ;
#71881=CARTESIAN_POINT ( 'NONE',  ( 5.676582343749993598, 225.2604166632526983, 9.832129032723422313 ) ) ;
#71882=VERTEX_POINT ( 'NONE', #62493 ) ;
#71884=CARTESIAN_POINT ( 'NONE',  ( 11.35316468749999785, 145.8854166632526983, 3.042071309553174174 ) ) ;
#71901=DIRECTION ( 'NONE',  ( 0.000000000000000000, 0.000000000000000000, 1.000000000000000000 ) ) ;
#71902=CARTESIAN_POINT ( 'NONE',  ( 11.35316468749999785, 190.5729166632526699, 3.042071309553174174 ) ) ;
#71906=CARTESIAN_POINT ( 'NONE',  ( -2.765530957081996810, 293.2656250017068942, -6.676582343750002480 ) ) ;
#71907=CARTESIAN_POINT ( 'NONE',  ( 10.00000000000000178, 132.0833333265053398, -2.679491924311226736 ) ) ;
#71913=CARTESIAN_POINT ( 'NONE',  ( 10.00000000000000000, 166.6666666598387110, 2.679491924311235618 ) ) ;
#71919=CARTESIAN_POINT ( 'NONE',  ( -5.676582343749998039, 112.7604166632526841, -9.832129032723420536 ) ) ;
#71927=CARTESIAN_POINT ( 'NONE',  ( -11.90180034005860144, 227.9280165645365628, -15.80450607135647623 ) ) ;
#71929=VECTOR ( 'NONE', #4063, 1000.000000000000000 ) ;
#71932=CARTESIAN_POINT ( 'NONE',  ( -11.35316468750000141, 188.5937499965860127, -1.390361679473963753E-15 ) ) ;
#71939=CARTESIAN_POINT ( 'NONE',  ( 8.311093377946837890, 76.40624999658602690, -8.311093377946837890 ) ) ;
#71944=CARTESIAN_POINT ( 'NONE',  ( -3.673940397442060854E-16, 289.8125000034140157, -6.000000000000001776 ) ) ;
#71945=CARTESIAN_POINT ( 'NONE',  ( 9.832129032723416984, 85.36458332991936970, 5.676582343750006032 ) ) ;
#71950=CARTESIAN_POINT ( 'NONE',  ( 3.042071309553167513, 66.82291666325265567, -11.35316468749999785 ) ) ;
#71954=CARTESIAN_POINT ( 'NONE',  ( 8.660254037844389075, 172.2916666598387110, -5.000000000000000000 ) ) ;
#71957=DIRECTION ( 'NONE',  ( -0.000000000000000000, 1.000000000000000000, -0.000000000000000000 ) ) ;
#71958=CARTESIAN_POINT ( 'NONE',  ( 6.951808397369818766E-16, 57.34374999658601979, -11.35316468750000141 ) ) ;
#71959=CARTESIAN_POINT ( 'NONE',  ( 1.226468279477575784E-15, 294.7031250017069510, 6.676582343750001591 ) ) ;
#71961=CARTESIAN_POINT ( 'NONE',  ( 9.832129032723420536, 206.1979166632526983, -5.676582343749999815 ) ) ;
#71967=CARTESIAN_POINT ( 'NONE',  ( -2.085542519210945728E-15, 194.5312499965860127, 11.35316468750000141 ) ) ;
#71971=CARTESIAN_POINT ( 'NONE',  ( -10.00000000000000000, 189.1666666598387110, -2.679491924311229845 ) ) ;
#71973=CARTESIAN_POINT ( 'NONE',  ( -5.676582343749998039, 177.7604166632526699, -9.832129032723420536 ) ) ;
#71978=EDGE_CURVE ( 'NONE', #10283, #58068, #17592, .T. ) ;
#71994=ORIENTED_EDGE ( 'NONE', *, *, #73766, .T. ) ;
#72000=CARTESIAN_POINT ( 'NONE',  ( 9.832129032723416984, 80.67708332991935549, 5.676582343750006032 ) ) ;
#72005=CARTESIAN_POINT ( 'NONE',  ( 6.676582343750003368, 295.0468750017069510, 2.765530957081995478 ) ) ;
#72006=CARTESIAN_POINT ( 'NONE',  ( -7.320508075688778149, 143.1250000000000000, 7.320508075688769267 ) ) ;
#72008=CARTESIAN_POINT ( 'NONE',  ( -7.320508075688773708, 163.7499999931720538, -7.320508075688774596 ) ) ;
#72018=CARTESIAN_POINT ( 'NONE',  ( 2.485281374238266672, 289.7500000034140157, -6.000000000000306422 ) ) ;
#72024=CARTESIAN_POINT ( 'NONE',  ( 11.35316468749999785, 45.57291666325266988, 3.042071309553174174 ) ) ;
#72026=CARTESIAN_POINT ( 'NONE',  ( -10.00000000000000178, 9.374999993172032475, -1.224646799147353454E-15 ) ) ;
#72028=DIRECTION ( 'NONE',  ( -0.000000000000000000, 1.000000000000000000, -0.000000000000000000 ) ) ;
#72029=CARTESIAN_POINT ( 'NONE',  ( -3.042071309553173730, 44.32291666325268409, 11.35316468749999785 ) ) ;
#72033=CARTESIAN_POINT ( 'NONE',  ( 6.123233995736767268E-16, 11.25000000000000178, -10.00000000000000178 ) ) ;
#72035=CARTESIAN_POINT ( 'NONE',  ( 6.951808397369818766E-16, 32.03124999658601268, -11.35316468750000141 ) ) ;
#72038=CARTESIAN_POINT ( 'NONE',  ( 8.311093377946834337, 160.1562499965860411, 8.311093377946839666 ) ) ;
#72039=CARTESIAN_POINT ( 'NONE',  ( -4.999999999999998224, 128.5416666598387110, -8.660254037844389075 ) ) ;
#72042=CARTESIAN_POINT ( 'NONE',  ( 10.00000000000000000, 21.66666665983870388, 2.679491924311235618 ) ) ;
#72043=CARTESIAN_POINT ( 'NONE',  ( -11.35316468750000141, 18.80208332991934839, 3.042071309553159963 ) ) ;
#72050=CARTESIAN_POINT ( 'NONE',  ( -3.042071309553173730, 159.3229166632526699, 11.35316468749999785 ) ) ;
#72057=VERTEX_POINT ( 'NONE', #25460 ) ;
#72060=CARTESIAN_POINT ( 'NONE',  ( 11.35316468749999963, 96.30208332991934128, -3.042071309553165293 ) ) ;
#72074=CARTESIAN_POINT ( 'NONE',  ( -2.679491924311226292, 158.3333333265053398, -10.00000000000000178 ) ) ;
#72088=CARTESIAN_POINT ( 'NONE',  ( 10.00000000000000178, 71.87499999317203958, 0.000000000000000000 ) ) ;
#72091=ORIENTED_EDGE ( 'NONE', *, *, #19272, .T. ) ;
#72098=CARTESIAN_POINT ( 'NONE',  ( -5.000000000000005329, 108.3333333333333428, 8.660254037844387298 ) ) ;
#72101=CARTESIAN_POINT ( 'NONE',  ( -2.765530957081996810, 290.4218750017068942, -6.676582343750003368 ) ) ;
#72113=CARTESIAN_POINT ( 'NONE',  ( 3.042071309553167069, 6.822916663252682312, -11.35316468749999785 ) ) ;
#72115=CARTESIAN_POINT ( 'NONE',  ( -5.676582343749998039, 192.7604166632526983, -9.832129032723420536 ) ) ;
#72119=CARTESIAN_POINT ( 'NONE',  ( 0.000000000000000000, 300.0000000000000000, 0.000000000000000000 ) ) ;
#72123=CARTESIAN_POINT ( 'NONE',  ( 11.35316468749999785, 10.57291666325268409, 3.042071309553174174 ) ) ;
#72131=CARTESIAN_POINT ( 'NONE',  ( -11.35316468750000141, 123.4895833299193555, 3.042071309553159963 ) ) ;
#72133=CARTESIAN_POINT ( 'NONE',  ( -5.000000000000005329, 95.20833332650536818, 8.660254037844387298 ) ) ;
#72140=CARTESIAN_POINT ( 'NONE',  ( -2.765530957081996810, 293.4218750017070079, -6.676582343750003368 ) ) ;
#72143=CARTESIAN_POINT ( 'NONE',  ( -11.35316468750000141, 173.2812499965860411, -1.390361679473963753E-15 ) ) ;
#72150=CARTESIAN_POINT ( 'NONE',  ( -3.042071309553173730, 154.6354166632526699, 11.35316468749999785 ) ) ;
#72155=CARTESIAN_POINT ( 'NONE',  ( 5.676582343749993598, 60.26041666325268409, 9.832129032723422313 ) ) ;
#72161=CARTESIAN_POINT ( 'NONE',  ( 2.485281374238575314, 289.3750000034139589, 6.000000000000000888 ) ) ;
#72179=ADVANCED_FACE ( 'NONE', ( #21669 ), #56028, .T. ) ;
#72180=CARTESIAN_POINT ( 'NONE',  ( 6.000000000000003553, 299.4374999999999432, 2.485281374238571317 ) ) ;
#72186=CARTESIAN_POINT ( 'NONE',  ( -10.00000000000000355, 72.70833333333332860, 2.679491924311223183 ) ) ;
#72189=CARTESIAN_POINT ( 'NONE',  ( 4.242640687119287435, 293.3750000000000000, 4.242640687119285658 ) ) ;
#72193=LINE ( 'NONE', #66918, #6028 ) ;
#72201=CARTESIAN_POINT ( 'NONE',  ( 7.320508075688771044, 189.3750000000000000, 7.320508075688775484 ) ) ;
#72204=CARTESIAN_POINT ( 'NONE',  ( 8.311093377946837890, 151.7187499965860127, -8.311093377946837890 ) ) ;
#72207=CARTESIAN_POINT ( 'NONE',  ( 7.347880794884121708E-16, 300.0000000000000000, -6.000000000000001776 ) ) ;
#72209=CARTESIAN_POINT ( 'NONE',  ( 1.224646799147353454E-15, 300.0000000000000000, -10.00000000000000178 ) ) ;
#72212=CARTESIAN_POINT ( 'NONE',  ( -8.311093377946841443, 9.218749996586016238, 8.311093377946830785 ) ) ;
#72218=CARTESIAN_POINT ( 'NONE',  ( -8.660254037844387298, 53.95833332650536818, -5.000000000000004441 ) ) ;
#72224=CARTESIAN_POINT ( 'NONE',  ( 8.660254037844385522, 164.5833333333333428, 5.000000000000005329 ) ) ;
#72228=LINE ( 'NONE', #26576, #30251 ) ;
#72231=CARTESIAN_POINT ( 'NONE',  ( 5.676582343749993598, 124.9479166632526983, 9.832129032723422313 ) ) ;
#72232=ORIENTED_EDGE ( 'NONE', *, *, #41524, .T. ) ;
#72237=CARTESIAN_POINT ( 'NONE',  ( -2.679491924311235174, 155.4166666598387110, 10.00000000000000000 ) ) ;
#72239=CARTESIAN_POINT ( 'NONE',  ( -5.676582343750006032, 129.1145833299193839, 9.832129032723418760 ) ) ;
#72244=CARTESIAN_POINT ( 'NONE',  ( -10.00000000000000000, 24.16666665983869677, -2.679491924311229845 ) ) ;
#72246=CARTESIAN_POINT ( 'NONE',  ( 8.311093377946837890, 121.7187499965860269, -8.311093377946837890 ) ) ;
#72251=EDGE_CURVE ( 'NONE', #17783, #61945, #35311, .T. ) ;
#72252=CARTESIAN_POINT ( 'NONE',  ( 11.35316468749999963, 21.30208332991935194, -3.042071309553165293 ) ) ;
#72260=CARTESIAN_POINT ( 'NONE',  ( -2.485281374238571761, 298.8750000034140726, -6.000000000000003553 ) ) ;
#72261=CYLINDRICAL_SURFACE ( 'NONE', #5206, 10.00000000000000178 ) ;
#72264=CARTESIAN_POINT ( 'NONE',  ( 11.35316468749999963, 146.3020833299193555, -3.042071309553165293 ) ) ;
#72271=ORIENTED_EDGE ( 'NONE', *, *, #65534, .F. ) ;
#72281=CARTESIAN_POINT ( 'NONE',  ( 11.35316468750000141, 180.7812499965860411, 0.000000000000000000 ) ) ;
#72283=CARTESIAN_POINT ( 'NONE',  ( 2.485281374238196062, 295.6875000000000000, -6.000000000000377476 ) ) ;
#72284=CARTESIAN_POINT ( 'NONE',  ( -2.765530957081998142, 293.6406250017069510, 6.676582343750000703 ) ) ;
#72285=DIRECTION ( 'NONE',  ( -0.000000000000000000, -0.000000000000000000, 1.000000000000000000 ) ) ;
#72286=CARTESIAN_POINT ( 'NONE',  ( -10.00000000000000533, 67.50000000000001421, -1.224646799147354045E-15 ) ) ;
#72288=VECTOR ( 'NONE', #21171, 1000.000000000000000 ) ;
#72299=CARTESIAN_POINT ( 'NONE',  ( 3.042071309553167069, 117.1354166632526557, -11.35316468749999785 ) ) ;
#72310=EDGE_CURVE ( 'NONE', #54835, #13929, #6868, .T. ) ;
#72313=CARTESIAN_POINT ( 'NONE',  ( 5.676582343749993598, 190.2604166632526983, 9.832129032723422313 ) ) ;
#72315=FACE_OUTER_BOUND ( 'NONE', #65781, .T. ) ;
#72320=CARTESIAN_POINT ( 'NONE',  ( -11.35316468749999785, 83.07291666325268409, -3.042071309553167513 ) ) ;
#72324=CARTESIAN_POINT ( 'NONE',  ( 10.00000000000015987, 39.79166666666675667, 2.679491924311278250 ) ) ;
#72326=CARTESIAN_POINT ( 'NONE',  ( 11.35316468750000141, 85.78124999658602690, 0.000000000000000000 ) ) ;
#72334=CARTESIAN_POINT ( 'NONE',  ( -8.311093377946836114, 92.65624999658601268, -8.311093377946837890 ) ) ;
#72339=CARTESIAN_POINT ( 'NONE',  ( -1.836970198721029983E-15, 175.6249999931720538, 10.00000000000000178 ) ) ;
#72342=CARTESIAN_POINT ( 'NONE',  ( 5.676582343749993598, 70.26041666325268409, 9.832129032723422313 ) ) ;
#72343=CARTESIAN_POINT ( 'NONE',  ( 2.765530957081996366, 295.1406250017069510, -6.676582343750003368 ) ) ;
#72346=CARTESIAN_POINT ( 'NONE',  ( -5.676582343750006032, 214.1145833299193555, 9.832129032723418760 ) ) ;
#72347=ORIENTED_EDGE ( 'NONE', *, *, #14822, .T. ) ;
#72348=CARTESIAN_POINT ( 'NONE',  ( 11.35316468750000141, 0.7812499965860163487, 0.000000000000000000 ) ) ;
#72352=CARTESIAN_POINT ( 'NONE',  ( 8.311093377946837890, 201.4062499965859843, -8.311093377946837890 ) ) ;
#72357=CARTESIAN_POINT ( 'NONE',  ( -8.311093377946841443, 179.2187499965859843, 8.311093377946834337 ) ) ;
#72365=CARTESIAN_POINT ( 'NONE',  ( -2.679491924311225848, 6.458333333333333037, -10.00000000000000178 ) ) ;
#72383=ORIENTED_EDGE ( 'NONE', *, *, #21851, .F. ) ;
#72385=CARTESIAN_POINT ( 'NONE',  ( 3.042071309553159519, 80.05208332991935549, 11.35316468750000141 ) ) ;
#72390=CARTESIAN_POINT ( 'NONE',  ( -6.676582343750002480, 292.5468750017069510, -2.765530957081996810 ) ) ;
#72403=CARTESIAN_POINT ( 'NONE',  ( 6.000000000000003553, 289.5000000034140726, 2.485281374238571317 ) ) ;
#72406=CARTESIAN_POINT ( 'NONE',  ( 6.000000000000001776, 288.5625000034140157, -7.347880794884121708E-16 ) ) ;
#72409=CARTESIAN_POINT ( 'NONE',  ( -3.042071309553173730, 44.32291666325268409, 11.35316468749999785 ) ) ;
#72411=CARTESIAN_POINT ( 'NONE',  ( -10.00000000000000355, 4.583333326505366401, 2.679491924311223183 ) ) ;
#72414=CARTESIAN_POINT ( 'NONE',  ( 8.660254037844385522, 141.4583333265053682, 5.000000000000005329 ) ) ;
#72417=CARTESIAN_POINT ( 'NONE',  ( -9.832129032723420536, 43.69791666325268409, 5.676582343749997150 ) ) ;
#72424=CARTESIAN_POINT ( 'NONE',  ( 11.35316468749999963, 45.98958332991934128, -3.042071309553165293 ) ) ;
#72427=CARTESIAN_POINT ( 'NONE',  ( -5.676582343749998039, 167.4479166632526983, -9.832129032723420536 ) ) ;
#72428=( BOUNDED_CURVE ( )  B_SPLINE_CURVE ( 2, ( #51073, #63508, #51822, #57119, #74086, #6181, #68422, #52202, #34868, #16725, #29189, #5432, #58251 ),
 .UNSPECIFIED., .F., .F. ) 
 B_SPLINE_CURVE_WITH_KNOTS ( ( 3, 2, 2, 2, 2, 2, 3 ),
 ( 0.9510869565217392463, 0.9528985507246378051, 0.9547101449275362528, 0.9565217391304348116, 0.9583333333333333703, 0.9601449275362318181, 0.9619565217391303769 ),
 .UNSPECIFIED. ) 
 CURVE ( )  GEOMETRIC_REPRESENTATION_ITEM ( )  RATIONAL_B_SPLINE_CURVE ( ( 0.9999999999999978906, 0.9659258262890704216, 1.000000000000000000, 0.9659258262890683122, 1.000000000000000000, 0.9659258262890683122, 1.000000000000000000, 0.9659258262890683122, 1.000000000000000000, 0.9659258262890683122, 1.000000000000000000, 0.9659258262890704216, 0.9999999999999978906 ) ) 
 REPRESENTATION_ITEM ( '' )  );
#72429=CARTESIAN_POINT ( 'NONE',  ( -8.660254037844390851, 129.7916666598387110, 4.999999999999998224 ) ) ;
#72434=CARTESIAN_POINT ( 'NONE',  ( -8.311093377946841443, 19.21874999658601979, 8.311093377946834337 ) ) ;
#72440=CARTESIAN_POINT ( 'NONE',  ( -10.00000000000000888, 7.500000000000005329, -1.224646799147354440E-15 ) ) ;
#72441=CARTESIAN_POINT ( 'NONE',  ( 6.951808397369818766E-16, 147.0312499965860411, -11.35316468750000141 ) ) ;
#72449=ORIENTED_EDGE ( 'NONE', *, *, #6918, .F. ) ;
#72452=CARTESIAN_POINT ( 'NONE',  ( -9.832129032723420536, 104.0104166632526841, 5.676582343749997150 ) ) ;
#72485=CARTESIAN_POINT ( 'NONE',  ( -2.679491924311225848, 106.4583333333333286, -10.00000000000000178 ) ) ;
#72488=CARTESIAN_POINT ( 'NONE',  ( 4.721056650416000089, 292.9843750017070079, 4.721056650415999201 ) ) ;
#72500=CARTESIAN_POINT ( 'NONE',  ( 8.660254037844389075, 225.4166666666666856, -5.000000000000000000 ) ) ;
#72502=CARTESIAN_POINT ( 'NONE',  ( 6.951808397369818766E-16, 197.3437499965860127, -11.35316468750000141 ) ) ;
#72503=CARTESIAN_POINT ( 'NONE',  ( -8.660254037844387298, 133.9583333265053682, -5.000000000000004441 ) ) ;
#72505=CARTESIAN_POINT ( 'NONE',  ( 6.000000000000003553, 290.4375000000000000, 2.485281374238571317 ) ) ;
#72511=CARTESIAN_POINT ( 'NONE',  ( 3.042071309553167069, 6.822916663252682312, -11.35316468749999785 ) ) ;
#72519=CARTESIAN_POINT ( 'NONE',  ( -3.042071309553164404, 127.2395833299193555, -11.35316468749999963 ) ) ;
#72521=CARTESIAN_POINT ( 'NONE',  ( 7.320508075688774596, 87.49999999317202537, -7.320508075688774596 ) ) ;
#72524=CARTESIAN_POINT ( 'NONE',  ( -10.00000000000000355, 39.58333332650536107, 2.679491924311223183 ) ) ;
#72528=CARTESIAN_POINT ( 'NONE',  ( -4.721056650415999201, 291.4843750017070079, -4.721056650415999201 ) ) ;
#72531=CARTESIAN_POINT ( 'NONE',  ( -5.676582343750006032, 164.1145833299193555, 9.832129032723418760 ) ) ;
#72533=CARTESIAN_POINT ( 'NONE',  ( -1.836970198721029983E-15, 205.6249999931720538, 10.00000000000000178 ) ) ;
#72535=ADVANCED_FACE ( 'NONE', ( #25279 ), #3032, .T. ) ;
#72540=CARTESIAN_POINT ( 'NONE',  ( 5.676582343750001591, 151.9270833299193555, -9.832129032723420536 ) ) ;
#72541=CARTESIAN_POINT ( 'NONE',  ( -10.00000000000000355, 217.2916666666667140, -2.679491924311231621 ) ) ;
#72544=CARTESIAN_POINT ( 'NONE',  ( -8.311093377946836114, 62.96874999658601979, -8.311093377946837890 ) ) ;
#72551=CARTESIAN_POINT ( 'NONE',  ( -4.999999999999998224, 108.5416666598387110, -8.660254037844389075 ) ) ;
#72576=CARTESIAN_POINT ( 'NONE',  ( 2.679491924311222739, 68.95833333333334281, 10.00000000000000355 ) ) ;
#72578=CARTESIAN_POINT ( 'NONE',  ( -4.242640687119286547, 291.8750000000000000, -4.242640687119286547 ) ) ;
#72589=CARTESIAN_POINT ( 'NONE',  ( -8.660254037844390851, 192.9166666666666856, 4.999999999999998224 ) ) ;
#72592=CARTESIAN_POINT ( 'NONE',  ( -11.35316468750000141, 158.8020833299193555, 3.042071309553159963 ) ) ;
#72599=CARTESIAN_POINT ( 'NONE',  ( 11.35316468749999963, 21.30208332991935194, -3.042071309553165293 ) ) ;
#72600=CARTESIAN_POINT ( 'NONE',  ( 8.660254037844389075, 97.29166665983871098, -5.000000000000000000 ) ) ;
#72606=CARTESIAN_POINT ( 'NONE',  ( -7.320508075688778149, 44.99999999317203958, 7.320508075688769267 ) ) ;
#72609=CARTESIAN_POINT ( 'NONE',  ( 10.00000000000001066, 219.7916666666666856, 2.679491924311238282 ) ) ;
#72614=EDGE_LOOP ( 'NONE', ( #20009, #34113, #1485, #65369 ) ) ;
#72615=CARTESIAN_POINT ( 'NONE',  ( -7.320508075688778149, 223.1250000000000284, 7.320508075688769267 ) ) ;
#72619=CARTESIAN_POINT ( 'NONE',  ( 3.042071309553159519, 129.7395833299193555, 11.35316468750000141 ) ) ;
#72627=CARTESIAN_POINT ( 'NONE',  ( -11.35316468750000141, 123.4895833299193555, 3.042071309553159963 ) ) ;
#72628=LINE ( 'NONE', #37929, #21688 ) ;
#72629=ORIENTED_EDGE ( 'NONE', *, *, #43058, .T. ) ;
#72630=ADVANCED_FACE ( 'NONE', ( #30952 ), #14705, .T. ) ;
#72633=CARTESIAN_POINT ( 'NONE',  ( 8.311093377946834337, 110.4687499965860127, 8.311093377946839666 ) ) ;
#72637=ADVANCED_FACE ( 'NONE', ( #66022 ), #32078, .T. ) ;
#72638=CARTESIAN_POINT ( 'NONE',  ( 11.35316468750000141, 21.09374999658601624, 0.000000000000000000 ) ) ;
#72640=DIRECTION ( 'NONE',  ( -0.000000000000000000, 1.000000000000000000, -0.000000000000000000 ) ) ;
#72645=CARTESIAN_POINT ( 'NONE',  ( 4.721056650416000089, 289.8281250017069510, 4.721056650415999201 ) ) ;
#72646=CARTESIAN_POINT ( 'NONE',  ( 0.000000000000000000, 300.0000000000000000, 0.000000000000000000 ) ) ;
#72650=CARTESIAN_POINT ( 'NONE',  ( 3.042071309553159519, 145.0520833299193555, 11.35316468750000141 ) ) ;
#72656=EDGE_LOOP ( 'NONE', ( #19814, #12628, #65962, #71039 ) ) ;
#72666=CARTESIAN_POINT ( 'NONE',  ( -8.311093377946841443, 183.9062499965860411, 8.311093377946830785 ) ) ;
#72669=CARTESIAN_POINT ( 'NONE',  ( 6.676582343750001591, 289.9531250017069510, -8.176455196517173205E-16 ) ) ;
#72671=CARTESIAN_POINT ( 'NONE',  ( 8.660254037844385522, 131.4583333265053682, 5.000000000000005329 ) ) ;
#72674=ORIENTED_EDGE ( 'NONE', *, *, #63354, .F. ) ;
#72680=ADVANCED_FACE ( 'NONE', ( #4 ), #4529, .T. ) ;
#72682=CARTESIAN_POINT ( 'NONE',  ( 1.959434878635763554E-15, 300.0000000000000000, -15.99999999999998579 ) ) ;
#72684=CARTESIAN_POINT ( 'NONE',  ( 3.042071309553159519, 120.0520833299193697, 11.35316468750000141 ) ) ;
#72689=CARTESIAN_POINT ( 'NONE',  ( 6.000000000000003553, 298.5624999999999432, -2.485281374238571761 ) ) ;
#72691=CARTESIAN_POINT ( 'NONE',  ( 8.101764136504522540, 224.5008269190864780, 5.891083390957826182 ) ) ;
#72692=CARTESIAN_POINT ( 'NONE',  ( 4.643170207286937412, 226.6963040713783357, -10.42876980789419683 ) ) ;
#72696=CARTESIAN_POINT ( 'NONE',  ( -8.311093377946836114, 212.9687499965860411, -8.311093377946837890 ) ) ;
#72703=CARTESIAN_POINT ( 'NONE',  ( 9.999999999999994671, 185.2083333333333144, -2.679491924311226292 ) ) ;
#72704=CARTESIAN_POINT ( 'NONE',  ( -9.832129032723420536, 78.69791666325269830, 5.676582343749997150 ) ) ;
#72705=ORIENTED_EDGE ( 'NONE', *, *, #23196, .F. ) ;
#72710=CARTESIAN_POINT ( 'NONE',  ( -11.35316468750000141, 83.48958332991935549, 3.042071309553159963 ) ) ;
#72718=CARTESIAN_POINT ( 'NONE',  ( 6.951808397369818766E-16, 82.03124999658602690, -11.35316468750000141 ) ) ;
#72722=CARTESIAN_POINT ( 'NONE',  ( -7.320508075688778149, 184.9999999931719969, 7.320508075688769267 ) ) ;
#72725=CARTESIAN_POINT ( 'NONE',  ( -5.676582343750006032, 74.42708332991934128, 9.832129032723418760 ) ) ;
#72726=CARTESIAN_POINT ( 'NONE',  ( -6.676582343750001591, 294.4531250017069510, 0.000000000000000000 ) ) ;
#72728=CARTESIAN_POINT ( 'NONE',  ( 5.676582343750001591, 211.6145833299193555, -9.832129032723420536 ) ) ;
#72734=CARTESIAN_POINT ( 'NONE',  ( 8.311093377946834337, 200.1562499965860411, 8.311093377946839666 ) ) ;
#72738=CARTESIAN_POINT ( 'NONE',  ( 2.765530957081996366, 299.1406250017068942, -6.676582343750003368 ) ) ;
#72740=CARTESIAN_POINT ( 'NONE',  ( 8.311093377946837890, 201.7187499965860411, -8.311093377946837890 ) ) ;
#72747=CARTESIAN_POINT ( 'NONE',  ( 2.679491924311228956, 11.04166666666666785, -10.00000000000000000 ) ) ;
#72755=EDGE_LOOP ( 'NONE', ( #19747, #66605, #223, #52952 ) ) ;
#72759=CARTESIAN_POINT ( 'NONE',  ( 1.459323541827198180E-11, 81.24999999999886313, -10.00000000000000533 ) ) ;
#72769=CARTESIAN_POINT ( 'NONE',  ( -9.832129032723418760, 73.17708332991934128, -5.676582343750004256 ) ) ;
#72774=CARTESIAN_POINT ( 'NONE',  ( 1.226468279477575784E-15, 290.8593750017070079, 6.676582343750001591 ) ) ;
#72777=CARTESIAN_POINT ( 'NONE',  ( -2.679491924311382611, 165.4166666598386826, 9.999999999999914735 ) ) ;
#72783=CARTESIAN_POINT ( 'NONE',  ( 3.042071309553167069, 162.1354166632526983, -11.35316468749999785 ) ) ;
#72786=CARTESIAN_POINT ( 'NONE',  ( -4.242640687119285658, 293.1875000034139589, 4.242640687119287435 ) ) ;
#72787=CYLINDRICAL_SURFACE ( 'NONE', #63082, 10.00000000000000178 ) ;
#72791=CARTESIAN_POINT ( 'NONE',  ( -8.311093377946836114, 47.65624999658601979, -8.311093377946837890 ) ) ;
#72793=CARTESIAN_POINT ( 'NONE',  ( 8.660254037844389075, 22.29166665983870033, -5.000000000000000000 ) ) ;
#72797=CARTESIAN_POINT ( 'NONE',  ( -5.676582343749998039, 42.44791666325268409, -9.832129032723420536 ) ) ;
#72803=CARTESIAN_POINT ( 'NONE',  ( 11.35316468749999963, 50.98958332991934839, -3.042071309553165293 ) ) ;
#72806=CARTESIAN_POINT ( 'NONE',  ( -5.676582343749998039, 162.4479166632526983, -9.832129032723420536 ) ) ;
#72808=CARTESIAN_POINT ( 'NONE',  ( 5.000000000000001776, 132.7083333265053682, -8.660254037844389075 ) ) ;
#72812=CARTESIAN_POINT ( 'NONE',  ( 9.832129032723420536, 36.51041666325267698, -5.676582343749999815 ) ) ;
#72818=CARTESIAN_POINT ( 'NONE',  ( -10.00000000000001066, 7.708333333333335702, 2.679491924311224960 ) ) ;
#72819=CARTESIAN_POINT ( 'NONE',  ( 9.832129032723420536, 171.1979166632526983, -5.676582343749999815 ) ) ;
#72827=CARTESIAN_POINT ( 'NONE',  ( -8.311093377946841443, 114.2187499965860269, 8.311093377946830785 ) ) ;
#72846=( BOUNDED_CURVE ( )  B_SPLINE_CURVE ( 2, ( #58109, #6044, #69785, #13159, #57740, #58475, #35100, #29426, #24116, #40737, #47129, #58842, #12428 ),
 .UNSPECIFIED., .F., .F. ) 
 B_SPLINE_CURVE_WITH_KNOTS ( ( 3, 2, 2, 2, 2, 2, 3 ),
 ( 2.213686939631518857, 2.218920756416068230, 2.224154573200617602, 2.229388389985166974, 2.234622206769716790, 2.239856023554266162, 2.245089840338815534 ),
 .UNSPECIFIED. ) 
 CURVE ( )  GEOMETRIC_REPRESENTATION_ITEM ( )  RATIONAL_B_SPLINE_CURVE ( ( 0.9999999999997807310, 0.9659258262892875813, 1.000000000000000000, 0.9659258262890683122, 1.000000000000000000, 0.9659258262890683122, 1.000000000000000000, 0.9659258262890683122, 1.000000000000000000, 0.9659258262890683122, 1.000000000000000000, 0.9659258262893042346, 0.9999999999997640776 ) ) 
 REPRESENTATION_ITEM ( '' )  );
#72848=CARTESIAN_POINT ( 'NONE',  ( -1.836970198721029983E-15, 225.6249999931720254, 10.00000000000000178 ) ) ;
#72850=CARTESIAN_POINT ( 'NONE',  ( 6.676582343750003368, 298.8906250017069510, 2.765530957081995478 ) ) ;
#72860=CARTESIAN_POINT ( 'NONE',  ( -1.966770576099810657E-11, 61.25000000000153477, -9.999999999999998224 ) ) ;
#72861=CARTESIAN_POINT ( 'NONE',  ( -1.836970198721029983E-15, 108.7500000000000142, 10.00000000000000178 ) ) ;
#72863=CARTESIAN_POINT ( 'NONE',  ( -2.765530957081996810, 292.4218750017069510, -6.676582343750003368 ) ) ;
#72877=CARTESIAN_POINT ( 'NONE',  ( -10.48324468785576080, 227.1467665679505785, -13.92079345837155735 ) ) ;
#72879=CARTESIAN_POINT ( 'NONE',  ( -9.832129032723418760, 208.1770833299193555, -5.676582343750004256 ) ) ;
#72881=CARTESIAN_POINT ( 'NONE',  ( 2.485281374238878627, 290.3124999999999432, 5.999999999999694467 ) ) ;
#72885=CARTESIAN_POINT ( 'NONE',  ( 6.951808397369818766E-16, 7.031249996586016238, -11.35316468750000141 ) ) ;
#72891=CARTESIAN_POINT ( 'NONE',  ( 3.042071309553159519, 9.739583329919350163, 11.35316468750000141 ) ) ;
#72893=CARTESIAN_POINT ( 'NONE',  ( -5.676582343749998039, 122.4479166632526983, -9.832129032723420536 ) ) ;
#72894=CARTESIAN_POINT ( 'NONE',  ( 6.123233995736767268E-16, 93.12499999317203958, -10.00000000000000178 ) ) ;
#72900=CARTESIAN_POINT ( 'NONE',  ( 0.000000000000000000, 300.0000000000000000, 10.00000000000000178 ) ) ;
#72901=CARTESIAN_POINT ( 'NONE',  ( -6.676582343750000703, 291.6718750017069510, 2.765530957082001251 ) ) ;
#72905=CARTESIAN_POINT ( 'NONE',  ( -10.00000000000000000, 204.1666666598387394, -2.679491924311229845 ) ) ;
#72906=CARTESIAN_POINT ( 'NONE',  ( -2.679491924311394158, 193.5416666666666288, 9.999999999999959144 ) ) ;
#72912=CARTESIAN_POINT ( 'NONE',  ( 11.35316468750000141, 151.0937499965860411, 0.000000000000000000 ) ) ;
#72915=CARTESIAN_POINT ( 'NONE',  ( -11.35316468750000141, 58.59374999658601979, -1.390361679473963753E-15 ) ) ;
#72921=CARTESIAN_POINT ( 'NONE',  ( -3.673940397442060854E-16, 287.8125000034140157, -6.000000000000001776 ) ) ;
#72942=CARTESIAN_POINT ( 'NONE',  ( -10.00000000000000000, 2.708333333333331261, 2.679491924311222295 ) ) ;
#72943=CARTESIAN_POINT ( 'NONE',  ( -10.00000000000000178, 202.5000000000000000, -1.224646799147353454E-15 ) ) ;
#72946=CARTESIAN_POINT ( 'NONE',  ( -7.320508075688778149, 68.12500000000001421, 7.320508075688769267 ) ) ;
#72948=CARTESIAN_POINT ( 'NONE',  ( 2.485281374238571317, 291.6874999999999432, -6.000000000000003553 ) ) ;
#72962=CARTESIAN_POINT ( 'NONE',  ( -10.00000000000000000, 182.2916666666666856, -2.679491924311229845 ) ) ;
#72965=CARTESIAN_POINT ( 'NONE',  ( 11.35316468749999785, 150.8854166632527267, 3.042071309553174174 ) ) ;
#72969=LINE ( 'NONE', #72209, #25020 ) ;
#72971=EDGE_LOOP ( 'NONE', ( #8469, #26089, #1114, #33350 ) ) ;
#72972=CARTESIAN_POINT ( 'NONE',  ( -3.042071309553173730, 24.63541666325268054, 11.35316468749999785 ) ) ;
#72978=CARTESIAN_POINT ( 'NONE',  ( 8.660254037844385522, 51.45833332650536818, 5.000000000000005329 ) ) ;
#72981=CARTESIAN_POINT ( 'NONE',  ( 8.660254037844381969, 54.58333333333333570, 5.000000000000002665 ) ) ;
#72986=EDGE_LOOP ( 'NONE', ( #40662, #16834, #54391, #9731 ) ) ;
#72987=CARTESIAN_POINT ( 'NONE',  ( 2.997893585525398702E-11, 31.24999999999767653, -10.00000000000000178 ) ) ;
#72989=CARTESIAN_POINT ( 'NONE',  ( 10.00000000000000178, 1.874999993172032697, 0.000000000000000000 ) ) ;
#72991=CARTESIAN_POINT ( 'NONE',  ( -11.35316468749999785, 128.0729166632526983, -3.042071309553167513 ) ) ;
#72992=ORIENTED_EDGE ( 'NONE', *, *, #36559, .F. ) ;
#72993=CARTESIAN_POINT ( 'NONE',  ( -4.242640687119286547, 297.8750000000000000, -4.242640687119286547 ) ) ;
#72998=CARTESIAN_POINT ( 'NONE',  ( 8.311093377946837890, 126.4062499965860411, -8.311093377946837890 ) ) ;
#73001=CARTESIAN_POINT ( 'NONE',  ( -8.660254037844390851, 24.79166665983870033, 4.999999999999998224 ) ) ;
#73003=CARTESIAN_POINT ( 'NONE',  ( -8.311093377946841443, 119.2187499965860127, 8.311093377946834337 ) ) ;
#73007=CARTESIAN_POINT ( 'NONE',  ( -8.311093377946836114, 27.96874999658601624, -8.311093377946837890 ) ) ;
#73009=FACE_OUTER_BOUND ( 'NONE', #44356, .T. ) ;
#73015=CARTESIAN_POINT ( 'NONE',  ( -6.676582343750001591, 288.4531250017069510, 0.000000000000000000 ) ) ;
#73019=CARTESIAN_POINT ( 'NONE',  ( -3.042071309553164404, 147.5520833299193271, -11.35316468749999963 ) ) ;
#73024=ORIENTED_EDGE ( 'NONE', *, *, #39622, .T. ) ;
#73034=CARTESIAN_POINT ( 'NONE',  ( 9.832129032723416984, 185.3645833299193555, 5.676582343750006032 ) ) ;
#73040=CARTESIAN_POINT ( 'NONE',  ( 8.660254037844380193, 94.58333333333334281, 5.000000000000002665 ) ) ;
#73042=ADVANCED_FACE ( 'NONE', ( #14992 ), #32373, .T. ) ;
#73051=CARTESIAN_POINT ( 'NONE',  ( -8.311093377946841443, 109.2187499965860269, 8.311093377946830785 ) ) ;
#73061=CARTESIAN_POINT ( 'NONE',  ( -11.35316468749999785, 223.0729166632527267, -3.042071309553167513 ) ) ;
#73064=CARTESIAN_POINT ( 'NONE',  ( -5.676582343749998039, 207.7604166632526983, -9.832129032723420536 ) ) ;
#73066=FACE_OUTER_BOUND ( 'NONE', #20450, .T. ) ;
#73070=CARTESIAN_POINT ( 'NONE',  ( 8.660254037844380193, 184.5833333333333428, 5.000000000000002665 ) ) ;
#73072=CARTESIAN_POINT ( 'NONE',  ( 11.35316468749999963, 100.9895833299193555, -3.042071309553165293 ) ) ;
#73073=VERTEX_POINT ( 'NONE', #8979 ) ;
#73078=CARTESIAN_POINT ( 'NONE',  ( -2.085542519210945728E-15, 89.53124999658602690, 11.35316468750000141 ) ) ;
#73079=ORIENTED_EDGE ( 'NONE', *, *, #50850, .T. ) ;
#73080=CARTESIAN_POINT ( 'NONE',  ( 1.102182119232618108E-15, 291.3125000034140157, 6.000000000000001776 ) ) ;
#73086=CARTESIAN_POINT ( 'NONE',  ( 11.35316468749999785, 90.57291666325269830, 3.042071309553174174 ) ) ;
#73090=( BOUNDED_CURVE ( )  B_SPLINE_CURVE ( 2, ( #63074, #11767, #28373, #16662, #39693, #27624, #21960, #46466, #45351, #62694, #51012, #23454, #74021 ),
 .UNSPECIFIED., .F., .F. ) 
 B_SPLINE_CURVE_WITH_KNOTS ( ( 3, 2, 2, 2, 2, 2, 3 ),
 ( 0.9293478260869566521, 0.9311594202898552108, 0.9329710144927537696, 0.9347826086956523284, 0.9365942028985509982, 0.9384057971014494459, 0.9402173913043480047 ),
 .UNSPECIFIED. ) 
 CURVE ( )  GEOMETRIC_REPRESENTATION_ITEM ( )  RATIONAL_B_SPLINE_CURVE ( ( 0.9999999999999978906, 0.9659258262890704216, 1.000000000000000000, 0.9659258262890683122, 1.000000000000000000, 0.9659258262890683122, 1.000000000000000000, 0.9659258262890683122, 1.000000000000000000, 0.9659258262890683122, 1.000000000000000000, 0.9659258262890640934, 1.000000000000004219 ) ) 
 REPRESENTATION_ITEM ( '' )  );
#73092=CARTESIAN_POINT ( 'NONE',  ( 6.123233995736767268E-16, 188.1249999931720254, -10.00000000000000178 ) ) ;
#73094=CARTESIAN_POINT ( 'NONE',  ( 9.832129032723416984, 75.67708332991934128, 5.676582343750006032 ) ) ;
#73095=CARTESIAN_POINT ( 'NONE',  ( 1.226468279477575784E-15, 292.7031250017069510, 6.676582343750001591 ) ) ;
#73097=CARTESIAN_POINT ( 'NONE',  ( -2.085542519210945728E-15, 214.5312499965860411, 11.35316468750000141 ) ) ;
#73103=CARTESIAN_POINT ( 'NONE',  ( 6.951808397369818766E-16, 202.0312499965860411, -11.35316468750000141 ) ) ;
#73107=CARTESIAN_POINT ( 'NONE',  ( 8.311093377946834337, 195.4687499965860127, 8.311093377946839666 ) ) ;
#73116=CARTESIAN_POINT ( 'NONE',  ( -2.679491924311225848, 11.45833333333333393, -10.00000000000000178 ) ) ;
#73124=CARTESIAN_POINT ( 'NONE',  ( 1.224646799147353454E-15, 237.9999999999999716, -10.00000000000000178 ) ) ;
#73132=EDGE_CURVE ( 'NONE', #33509, #19205, #22966, .T. ) ;
#73139=CARTESIAN_POINT ( 'NONE',  ( 11.35316468749999963, 76.30208332991935549, -3.042071309553165293 ) ) ;
#73144=CARTESIAN_POINT ( 'NONE',  ( -2.765530957081998142, 291.7968750017070079, 6.676582343750000703 ) ) ;
#73152=CARTESIAN_POINT ( 'NONE',  ( -8.311093377946841443, 169.2187499965859843, 8.311093377946830785 ) ) ;
#73153=FACE_OUTER_BOUND ( 'NONE', #3103, .T. ) ;
#73160=CARTESIAN_POINT ( 'NONE',  ( -9.832129032723420536, 48.69791666325268409, 5.676582343749997150 ) ) ;
#73163=CARTESIAN_POINT ( 'NONE',  ( -2.679491924311225848, 18.33333332650536818, -10.00000000000000178 ) ) ;
#73169=CARTESIAN_POINT ( 'NONE',  ( 3.042071309553159519, 44.73958332991934839, 11.35316468750000141 ) ) ;
#73175=CARTESIAN_POINT ( 'NONE',  ( -5.676582343749998039, 47.44791666325268409, -9.832129032723420536 ) ) ;
#73178=CARTESIAN_POINT ( 'NONE',  ( 11.35316468749999785, 160.5729166632526699, 3.042071309553174174 ) ) ;
#73179=CARTESIAN_POINT ( 'NONE',  ( -4.999999999999998224, 138.5416666598387110, -8.660254037844389075 ) ) ;
#73183=CARTESIAN_POINT ( 'NONE',  ( -9.832129032723420536, 34.01041666325269119, 5.676582343749997150 ) ) ;
#73191=CARTESIAN_POINT ( 'NONE',  ( 9.832129032723416984, 160.3645833299193839, 5.676582343750006032 ) ) ;
#73197=ORIENTED_EDGE ( 'NONE', *, *, #37961, .F. ) ;
#73202=CARTESIAN_POINT ( 'NONE',  ( 6.951808397369818766E-16, 117.3437499965860127, -11.35316468750000141 ) ) ;
#73233=CARTESIAN_POINT ( 'NONE',  ( 4.999999999999993783, 124.1666666666666714, 8.660254037844390851 ) ) ;
#73235=CARTESIAN_POINT ( 'NONE',  ( 6.676582343750003368, 293.1718750017070647, -2.765530957081997254 ) ) ;
#73248=DIRECTION ( 'NONE',  ( -0.000000000000000000, 1.000000000000000000, -0.000000000000000000 ) ) ;
#73249=CARTESIAN_POINT ( 'NONE',  ( 8.311093377946834337, 20.15624999658600913, 8.311093377946839666 ) ) ;
#73251=CARTESIAN_POINT ( 'NONE',  ( 9.832129032723420536, 206.5104166632526983, -5.676582343749999815 ) ) ;
#73252=LINE ( 'NONE', #4226, #58985 ) ;
#73254=CARTESIAN_POINT ( 'NONE',  ( -3.190679070438028606E-13, 193.7500000000000000, 10.00000000000000533 ) ) ;
#73256=DIRECTION ( 'NONE',  ( 0.000000000000000000, 0.000000000000000000, 1.000000000000000000 ) ) ;
#73259=CARTESIAN_POINT ( 'NONE',  ( -3.042071309553173730, 4.322916663252682312, 11.35316468749999785 ) ) ;
#73265=CARTESIAN_POINT ( 'NONE',  ( -5.676582343750006032, 9.114583329919350163, 9.832129032723418760 ) ) ;
#73267=CARTESIAN_POINT ( 'NONE',  ( 8.311093377946834337, 125.1562499965860411, 8.311093377946839666 ) ) ;
#73269=CARTESIAN_POINT ( 'NONE',  ( 6.123233995736767268E-16, 98.12499999317203958, -10.00000000000000178 ) ) ;
#73273=CARTESIAN_POINT ( 'NONE',  ( 10.00000000000000888, 145.0000000000000284, 0.000000000000000000 ) ) ;
#73275=CARTESIAN_POINT ( 'NONE',  ( -5.000000000000000888, 116.6666666666666856, -8.660254037844390851 ) ) ;
#73276=CARTESIAN_POINT ( 'NONE',  ( -4.721056650415999201, 288.4843750017070079, -4.721056650415999201 ) ) ;
#73285=CARTESIAN_POINT ( 'NONE',  ( 10.00000000000000178, 156.8749999931720254, 0.000000000000000000 ) ) ;
#73286=CARTESIAN_POINT ( 'NONE',  ( 3.042071309553167513, 152.1354166632526983, -11.35316468749999785 ) ) ;
#73291=CARTESIAN_POINT ( 'NONE',  ( -8.311093377946836114, 72.96874999658602690, -8.311093377946837890 ) ) ;
#73297=CARTESIAN_POINT ( 'NONE',  ( 2.485281374238575314, 287.3750000034140157, 6.000000000000000888 ) ) ;
#73322=CARTESIAN_POINT ( 'NONE',  ( 6.123233995736767268E-16, 76.25000000000000000, -10.00000000000000178 ) ) ;
#73324=CARTESIAN_POINT ( 'NONE',  ( 4.242640687119285658, 291.6249999999999432, -4.242640687119286547 ) ) ;
#73334=CARTESIAN_POINT ( 'NONE',  ( -5.000000000000016875, 76.66666666666669983, -8.660254037844419273 ) ) ;
#73335=CARTESIAN_POINT ( 'NONE',  ( 8.660254037844389075, 190.4166666666666856, -5.000000000000000000 ) ) ;
#73338=CARTESIAN_POINT ( 'NONE',  ( -11.35316468750000141, 173.5937499965860411, -1.390361679473963753E-15 ) ) ;
#73339=DIRECTION ( 'NONE',  ( -0.000000000000000000, 1.000000000000000000, -0.000000000000000000 ) ) ;
#73345=CARTESIAN_POINT ( 'NONE',  ( -2.085542519210945728E-15, 29.84374999658601624, 11.35316468750000141 ) ) ;
#73351=CARTESIAN_POINT ( 'NONE',  ( -1.836970198721029983E-15, 65.62499999317203958, 10.00000000000000178 ) ) ;
#73354=CARTESIAN_POINT ( 'NONE',  ( -2.143145793903030439E-12, 53.74999999999984368, 9.999999999999998224 ) ) ;
#73358=ORIENTED_EDGE ( 'NONE', *, *, #51117, .T. ) ;
#73359=CARTESIAN_POINT ( 'NONE',  ( 6.123233995736767268E-16, 221.2500000000000000, -10.00000000000000178 ) ) ;
#73363=CARTESIAN_POINT ( 'NONE',  ( 5.676582343749993598, 139.9479166632526983, 9.832129032723422313 ) ) ;
#73364=ORIENTED_EDGE ( 'NONE', *, *, #23335, .F. ) ;
#73371=VERTEX_POINT ( 'NONE', #21406 ) ;
#73374=CARTESIAN_POINT ( 'NONE',  ( -2.085542519210945728E-15, 109.8437499965860269, 11.35316468750000141 ) ) ;
#73378=CARTESIAN_POINT ( 'NONE',  ( -8.311093377946841443, 34.21874999658601979, 8.311093377946830785 ) ) ;
#73385=CARTESIAN_POINT ( 'NONE',  ( 6.676582343750001591, 288.9531250017069510, -8.176455196517173205E-16 ) ) ;
#73387=CARTESIAN_POINT ( 'NONE',  ( 7.320508075688771044, 111.2499999931720680, 7.320508075688775484 ) ) ;
#73388=DIRECTION ( 'NONE',  ( 0.000000000000000000, 0.000000000000000000, 1.000000000000000000 ) ) ;
#73390=CARTESIAN_POINT ( 'NONE',  ( -3.042071309553164404, 142.5520833299193271, -11.35316468749999963 ) ) ;
#73401=EDGE_LOOP ( 'NONE', ( #20114, #68720, #8585, #54070 ) ) ;
#73402=( BOUNDED_CURVE ( )  B_SPLINE_CURVE ( 2, ( #6079, #52471, #6458, #41152, #7190, #24152, #440, #47531, #70197, #52841, #46798, #18136, #12466 ),
 .UNSPECIFIED., .F., .F. ) 
 B_SPLINE_CURVE_WITH_KNOTS ( ( 3, 2, 2, 2, 2, 2, 3 ),
 ( 0.2982911931063731426, 0.3035251194131430852, 0.3087590457199130833, 0.3139929720266829705, 0.3192268983334529686, 0.3244608246402229113, 0.3296947509469928539 ),
 .UNSPECIFIED. ) 
 CURVE ( )  GEOMETRIC_REPRESENTATION_ITEM ( )  RATIONAL_B_SPLINE_CURVE ( ( 1.000000000000305977, 0.9659258262887623347, 1.000000000000000000, 0.9659258262890683122, 1.000000000000000000, 0.9659258262890683122, 1.000000000000000000, 0.9659258262890683122, 1.000000000000000000, 0.9659258262890683122, 1.000000000000000000, 0.9659258262890683122, 1.000000000000000000 ) ) 
 REPRESENTATION_ITEM ( '' )  );
#73404=CYLINDRICAL_SURFACE ( 'NONE', #13495, 10.00000000000000178 ) ;
#73406=CARTESIAN_POINT ( 'NONE',  ( -9.832129032723418760, 182.8645833299193555, -5.676582343750004256 ) ) ;
#73408=CARTESIAN_POINT ( 'NONE',  ( 6.000000000000003553, 295.4374999999999432, 2.485281374238571317 ) ) ;
#73409=CARTESIAN_POINT ( 'NONE',  ( 4.721056650415999201, 288.0781250017069510, -4.721056650415999201 ) ) ;
#73410=CARTESIAN_POINT ( 'NONE',  ( 10.00000000000011191, 79.79166666666672825, 2.679491924311265372 ) ) ;
#73419=CARTESIAN_POINT ( 'NONE',  ( -8.660254037844390851, 147.9166666666666572, 4.999999999999998224 ) ) ;
#73423=CARTESIAN_POINT ( 'NONE',  ( -11.35316468750000141, 128.5937499965860127, -1.390361679473963753E-15 ) ) ;
#73424=CARTESIAN_POINT ( 'NONE',  ( -4.242640687119286547, 295.8750000000000000, -4.242640687119286547 ) ) ;
#73430=CARTESIAN_POINT ( 'NONE',  ( 6.945059804708960449, 224.3593915618296251, 7.219287879128159169 ) ) ;
#73433=CARTESIAN_POINT ( 'NONE',  ( -9.832129032723420536, 209.0104166632526699, 5.676582343749997150 ) ) ;
#73440=CARTESIAN_POINT ( 'NONE',  ( -5.676582343749998039, 92.44791666325269830, -9.832129032723420536 ) ) ;
#73447=CARTESIAN_POINT ( 'NONE',  ( 11.35316468749999785, 105.5729166632526983, 3.042071309553174174 ) ) ;
#73450=EDGE_CURVE ( 'NONE', #14543, #59562, #14699, .T. ) ;
#73452=CARTESIAN_POINT ( 'NONE',  ( -2.679491924311277806, 21.45833333333352400, -10.00000000000035350 ) ) ;
#73454=CARTESIAN_POINT ( 'NONE',  ( -1.836970198721029983E-15, 160.6249999931720254, 10.00000000000000178 ) ) ;
#73455=CARTESIAN_POINT ( 'NONE',  ( 11.35316468750000141, 90.78124999658602690, 0.000000000000000000 ) ) ;
#73460=CARTESIAN_POINT ( 'NONE',  ( -7.320508075688773708, 188.7499999931720254, -7.320508075688774596 ) ) ;
#73462=CARTESIAN_POINT ( 'NONE',  ( -8.311093377946836114, 77.96874999658599847, -8.311093377946837890 ) ) ;
#73463=CARTESIAN_POINT ( 'NONE',  ( -6.676582343750000703, 291.5156250017069510, 2.765530957082001251 ) ) ;
#73465=CARTESIAN_POINT ( 'NONE',  ( -5.676582343750006032, 209.1145833299193555, 9.832129032723418760 ) ) ;
#73466=ORIENTED_EDGE ( 'NONE', *, *, #12145, .F. ) ;
#73469=CARTESIAN_POINT ( 'NONE',  ( 9.832129032723420536, 206.1979166632526983, -5.676582343749999815 ) ) ;
#73474=CARTESIAN_POINT ( 'NONE',  ( -3.042071309553163960, 197.5520833299193555, -11.35316468749999963 ) ) ;
#73480=CARTESIAN_POINT ( 'NONE',  ( 10.00000000000000178, 15.20833333333333215, -2.679491924311226736 ) ) ;
#73488=VECTOR ( 'NONE', #7367, 1000.000000000000000 ) ;
#73490=CARTESIAN_POINT ( 'NONE',  ( 4.999999999999993783, 16.04166665983870033, 8.660254037844390851 ) ) ;
#73502=CARTESIAN_POINT ( 'NONE',  ( 8.311093377946834337, 75.46874999658602690, 8.311093377946839666 ) ) ;
#73507=CARTESIAN_POINT ( 'NONE',  ( -6.676582343750001591, 288.6093750017069510, 0.000000000000000000 ) ) ;
#73514=EDGE_LOOP ( 'NONE', ( #21609, #4528, #34812, #22322 ) ) ;
#73517=CARTESIAN_POINT ( 'NONE',  ( 8.311093377946837890, 166.7187499965859843, -8.311093377946837890 ) ) ;
#73525=CARTESIAN_POINT ( 'NONE',  ( -9.832129032723420536, 58.69791666325269119, 5.676582343749997150 ) ) ;
#73527=CARTESIAN_POINT ( 'NONE',  ( 7.320508075688774596, 22.49999999317202892, -7.320508075688774596 ) ) ;
#73531=CARTESIAN_POINT ( 'NONE',  ( -2.679491924311226292, 168.3333333265053682, -10.00000000000000178 ) ) ;
#73532=CARTESIAN_POINT ( 'NONE',  ( -2.085542519210945728E-15, 64.53124999658602690, 11.35316468750000141 ) ) ;
#73538=CARTESIAN_POINT ( 'NONE',  ( 5.676582343750001591, 46.61458332991934839, -9.832129032723420536 ) ) ;
#73539=EDGE_CURVE ( 'NONE', #38468, #42156, #53721, .T. ) ;
#73541=CARTESIAN_POINT ( 'NONE',  ( 5.000000000000000888, 205.8333333333333428, -8.660254037844387298 ) ) ;
#73542=CARTESIAN_POINT ( 'NONE',  ( -3.042071309553173730, 179.3229166632526699, 11.35316468749999785 ) ) ;
#73545=CARTESIAN_POINT ( 'NONE',  ( 2.679491924311228956, 137.9166666598387110, -10.00000000000000000 ) ) ;
#73548=CARTESIAN_POINT ( 'NONE',  ( -5.676582343750006032, 29.42708332991935194, 9.832129032723418760 ) ) ;
#73549=CARTESIAN_POINT ( 'NONE',  ( 1.102182119232618108E-15, 295.3125000034140157, 6.000000000000001776 ) ) ;
#73550=ORIENTED_EDGE ( 'NONE', *, *, #43967, .F. ) ;
#73556=CARTESIAN_POINT ( 'NONE',  ( -8.311093377946836114, 172.6562499965860127, -8.311093377946837890 ) ) ;
#73566=CARTESIAN_POINT ( 'NONE',  ( 3.042071309553159519, 120.0520833299193697, 11.35316468750000141 ) ) ;
#73588=AXIS2_PLACEMENT_3D ( 'NONE', #46775, #69427, #63019 ) ;
#73591=ORIENTED_EDGE ( 'NONE', *, *, #10411, .F. ) ;
#73599=CARTESIAN_POINT ( 'NONE',  ( 7.320508075688774596, 115.6249999999999858, -7.320508075688774596 ) ) ;
#73601=CARTESIAN_POINT ( 'NONE',  ( -6.676582343750003368, 293.5468750017070079, -2.765530957081996810 ) ) ;
#73616=CARTESIAN_POINT ( 'NONE',  ( -9.832129032723418760, 12.86458332991935194, -5.676582343750004256 ) ) ;
#73618=CARTESIAN_POINT ( 'NONE',  ( 8.660254037844389075, 0.4166666666666657415, -5.000000000000000000 ) ) ;
#73619=CARTESIAN_POINT ( 'NONE',  ( -11.35316468750000141, 213.5937499965860411, -1.390361679473963753E-15 ) ) ;
#73627=CARTESIAN_POINT ( 'NONE',  ( 9.832129032723416984, 15.36458332991935016, 5.676582343750006032 ) ) ;
#73631=CARTESIAN_POINT ( 'NONE',  ( -1.349999999999998757, 283.9999999999998863, 5.686528119825505989 ) ) ;
#73633=CARTESIAN_POINT ( 'NONE',  ( -5.676582343749998039, 7.447916663252683200, -9.832129032723420536 ) ) ;
#73635=CARTESIAN_POINT ( 'NONE',  ( -9.832129032723420536, 133.6979166632526983, 5.676582343749997150 ) ) ;
#73636=CARTESIAN_POINT ( 'NONE',  ( 8.660254037844385522, 101.4583333265053824, 5.000000000000005329 ) ) ;
#73643=( BOUNDED_CURVE ( )  B_SPLINE_CURVE ( 2, ( #63301, #11262, #17283, #70099, #69344, #39931, #62937, #17654, #68598, #40673, #57670, #58780, #22950 ),
 .UNSPECIFIED., .F., .F. ) 
 B_SPLINE_CURVE_WITH_KNOTS ( ( 3, 2, 2, 2, 2, 2, 3 ),
 ( 0.8634897946621500342, 0.8687238057336525987, 0.8739578168051551632, 0.8791918278766578387, 0.8844258389481604032, 0.8896598500196628567, 0.8948938610911654212 ),
 .UNSPECIFIED. ) 
 CURVE ( )  GEOMETRIC_REPRESENTATION_ITEM ( )  RATIONAL_B_SPLINE_CURVE ( ( 0.9999999999999947820, 0.9659258262890735303, 1.000000000000000000, 0.9659258262890683122, 1.000000000000000000, 0.9659258262890683122, 1.000000000000000000, 0.9659258262890683122, 1.000000000000000000, 0.9659258262890683122, 1.000000000000000000, 0.9659258262889931501, 1.000000000000075273 ) ) 
 REPRESENTATION_ITEM ( '' )  );
#73644=CARTESIAN_POINT ( 'NONE',  ( -4.721056650415999201, 289.4843750017070079, -4.721056650415999201 ) ) ;
#73652=CARTESIAN_POINT ( 'NONE',  ( -11.35316468750000141, 173.8020833299193555, 3.042071309553159963 ) ) ;
#73656=CARTESIAN_POINT ( 'NONE',  ( -2.085542519210945728E-15, 69.84374999658601268, 11.35316468750000141 ) ) ;
#73657=EDGE_LOOP ( 'NONE', ( #65082, #15133, #55481, #15122 ) ) ;
#73664=CARTESIAN_POINT ( 'NONE',  ( 10.00000000000000000, 66.66666665983869677, 2.679491924311235618 ) ) ;
#73681=CARTESIAN_POINT ( 'NONE',  ( 6.123233995736767268E-16, 221.2500000000000000, -10.00000000000000178 ) ) ;
#73686=CARTESIAN_POINT ( 'NONE',  ( -2.679491924311225848, 86.45833333333335702, -10.00000000000000178 ) ) ;
#73689=CARTESIAN_POINT ( 'NONE',  ( -2.485281374238571761, 290.8124999999999432, -6.000000000000003553 ) ) ;
#73699=CARTESIAN_POINT ( 'NONE',  ( -4.999999999999998224, 201.6666666666666856, -8.660254037844389075 ) ) ;
#73703=CARTESIAN_POINT ( 'NONE',  ( 8.311093377946837890, 171.7187499965860127, -8.311093377946837890 ) ) ;
#73704=CARTESIAN_POINT ( 'NONE',  ( -8.660254037844582697, 212.9166666666667709, 5.000000000000109246 ) ) ;
#73710=CARTESIAN_POINT ( 'NONE',  ( -2.085542519210945728E-15, 19.84374999658601979, 11.35316468750000141 ) ) ;
#73716=CARTESIAN_POINT ( 'NONE',  ( 2.679491924311222739, 60.83333332650536818, 10.00000000000000355 ) ) ;
#73720=CARTESIAN_POINT ( 'NONE',  ( 0.000000000000000000, 300.0000000000000000, 0.000000000000000000 ) ) ;
#73722=CARTESIAN_POINT ( 'NONE',  ( 7.320508075688789695, 160.6250000000000568, -7.320508075688789695 ) ) ;
#73729=CARTESIAN_POINT ( 'NONE',  ( 5.676582343749993598, 144.9479166632526983, 9.832129032723422313 ) ) ;
#73742=CARTESIAN_POINT ( 'NONE',  ( -5.676582343750006032, 114.4270833299193555, 9.832129032723418760 ) ) ;
#73746=CARTESIAN_POINT ( 'NONE',  ( -11.35316468750000141, 38.59374999658601979, -1.390361679473963753E-15 ) ) ;
#73747=VERTEX_POINT ( 'NONE', #2486 ) ;
#73753=CARTESIAN_POINT ( 'NONE',  ( -3.673940397442060854E-16, 294.8125000034140157, -6.000000000000001776 ) ) ;
#73757=CARTESIAN_POINT ( 'NONE',  ( 8.311093377946834337, 150.4687499965860127, 8.311093377946839666 ) ) ;
#73766=EDGE_CURVE ( 'NONE', #15967, #30885, #48412, .T. ) ;
#73772=CARTESIAN_POINT ( 'NONE',  ( -7.320508075688778149, 209.9999999931719969, 7.320508075688769267 ) ) ;
#73774=CARTESIAN_POINT ( 'NONE',  ( 7.320508075688771044, 39.37500000000000000, 7.320508075688775484 ) ) ;
#73777=CARTESIAN_POINT ( 'NONE',  ( -2.765530957081998142, 288.6406250017069510, 6.676582343750000703 ) ) ;
#73787=CARTESIAN_POINT ( 'NONE',  ( -8.660254037844390851, 162.9166666666666856, 4.999999999999998224 ) ) ;
#73788=CARTESIAN_POINT ( 'NONE',  ( 1.224646799147353454E-15, 300.0000000000000000, -10.00000000000000178 ) ) ;
#73789=LINE ( 'NONE', #72682, #57190 ) ;
#73791=CARTESIAN_POINT ( 'NONE',  ( 8.311093377946837890, 131.7187499965860127, -8.311093377946837890 ) ) ;
#73796=CARTESIAN_POINT ( 'NONE',  ( 0.000000000000000000, 300.0000000000000000, 10.00000000000000178 ) ) ;
#73799=CARTESIAN_POINT ( 'NONE',  ( 8.825936903735748018, 225.3907168698384282, -4.710639689128314878 ) ) ;
#73801=CARTESIAN_POINT ( 'NONE',  ( 1.592277918221149080E-13, 106.2500000000000142, -10.00000000000000178 ) ) ;
#73804=CARTESIAN_POINT ( 'NONE',  ( -5.676582343749998039, 202.7604166632526983, -9.832129032723420536 ) ) ;
#73811=CARTESIAN_POINT ( 'NONE',  ( 9.832129032723416984, 95.36458332991935549, 5.676582343750006032 ) ) ;
#73817=CARTESIAN_POINT ( 'NONE',  ( 5.676582343750001591, 96.61458332991935549, -9.832129032723420536 ) ) ;
#73819=CARTESIAN_POINT ( 'NONE',  ( 10.00000000000000178, 207.0833333265053966, -2.679491924311226736 ) ) ;
#73825=CARTESIAN_POINT ( 'NONE',  ( -9.832129032723418760, 87.86458332991935549, -5.676582343750004256 ) ) ;
#73830=CARTESIAN_POINT ( 'NONE',  ( 5.000000000000001776, 182.7083333265053682, -8.660254037844389075 ) ) ;
#73833=CARTESIAN_POINT ( 'NONE',  ( -5.676582343750006032, 79.42708332991935549, 9.832129032723418760 ) ) ;
#73834=CARTESIAN_POINT ( 'NONE',  ( -6.676582343750000703, 288.5156250017069510, 2.765530957082001251 ) ) ;
#73837=CARTESIAN_POINT ( 'NONE',  ( -11.35316468750000141, 223.4895833299193555, 3.042071309553159963 ) ) ;
#73838=VERTEX_POINT ( 'NONE', #60565 ) ;
#73842=CARTESIAN_POINT ( 'NONE',  ( 11.35316468749999785, 210.5729166632526983, 3.042071309553174174 ) ) ;
#73844=CARTESIAN_POINT ( 'NONE',  ( -2.679491924311308448, 100.4166666598386826, 9.999999999999957367 ) ) ;
#73845=CARTESIAN_POINT ( 'NONE',  ( -6.676582343750000703, 296.5156250017069510, 2.765530957082001251 ) ) ;
#73847=CARTESIAN_POINT ( 'NONE',  ( 3.042071309553159519, 190.0520833299193555, 11.35316468750000141 ) ) ;
#73855=ADVANCED_FACE ( 'NONE', ( #9261 ), #24742, .T. ) ;
#73857=CARTESIAN_POINT ( 'NONE',  ( 8.660254037844389075, 15.41666666666666785, -5.000000000000000000 ) ) ;
#73868=CARTESIAN_POINT ( 'NONE',  ( 10.00000000000000178, 151.8749999931720538, 0.000000000000000000 ) ) ;
#73878=ORIENTED_EDGE ( 'NONE', *, *, #9760, .T. ) ;
#73881=CARTESIAN_POINT ( 'NONE',  ( -3.042071309553164404, 87.55208332991936970, -11.35316468749999963 ) ) ;
#73886=CARTESIAN_POINT ( 'NONE',  ( 4.721056650416000089, 291.9843750017070079, 4.721056650415999201 ) ) ;
#73890=CARTESIAN_POINT ( 'NONE',  ( -9.832129032723418760, 197.8645833299193555, -5.676582343750004256 ) ) ;
#73892=ORIENTED_EDGE ( 'NONE', *, *, #6918, .T. ) ;
#73895=CARTESIAN_POINT ( 'NONE',  ( 3.042071309553167069, 172.1354166632526983, -11.35316468749999785 ) ) ;
#73901=CARTESIAN_POINT ( 'NONE',  ( 3.042071309553167069, 61.82291666325266988, -11.35316468749999785 ) ) ;
#73908=CARTESIAN_POINT ( 'NONE',  ( 11.35316468750000141, 55.78124999658601268, 0.000000000000000000 ) ) ;
#73914=CARTESIAN_POINT ( 'NONE',  ( 3.042071309553167513, 51.82291666325266988, -11.35316468749999785 ) ) ;
#73917=CARTESIAN_POINT ( 'NONE',  ( -11.35316468750000141, 173.4895833299193839, 3.042071309553159963 ) ) ;
#73918=CARTESIAN_POINT ( 'NONE',  ( 10.00000000000000000, 136.6666666598387110, 2.679491924311236062 ) ) ;
#73921=CARTESIAN_POINT ( 'NONE',  ( -8.311093377946841443, 39.21874999658601268, 8.311093377946834337 ) ) ;
#73923=CARTESIAN_POINT ( 'NONE',  ( -3.042071309553164404, 187.2395833299193839, -11.35316468749999963 ) ) ;
#73930=CARTESIAN_POINT ( 'NONE',  ( -9.832129032723420536, 163.6979166632526983, 5.676582343749997150 ) ) ;
#73937=AXIS2_PLACEMENT_3D ( 'NONE', #45710, #63065, #17035 ) ;
#73939=CARTESIAN_POINT ( 'NONE',  ( 6.951808397369818766E-16, 112.3437499965860127, -11.35316468750000141 ) ) ;
#73942=( BOUNDED_CURVE ( )  B_SPLINE_CURVE ( 2, ( #27237, #50253, #73275, #11020, #26871, #51369, #74380, #57049, #63062, #68721, #15542, #11386, #55562 ),
 .UNSPECIFIED., .F., .F. ) 
 B_SPLINE_CURVE_WITH_KNOTS ( ( 3, 2, 2, 2, 2, 2, 3 ),
 ( 1.460092581490151309, 1.465325400988424231, 1.470558220486697154, 1.475791039984970077, 1.481023859483242555, 1.486256678981515478, 1.491489498479788400 ),
 .UNSPECIFIED. ) 
 CURVE ( )  GEOMETRIC_REPRESENTATION_ITEM ( )  RATIONAL_B_SPLINE_CURVE ( ( 1.000000000000054401, 0.9659258262890140223, 1.000000000000000000, 0.9659258262890683122, 1.000000000000000000, 0.9659258262890683122, 1.000000000000000000, 0.9659258262890683122, 1.000000000000000000, 0.9659258262890683122, 1.000000000000000000, 0.9659258262890662028, 1.000000000000001998 ) ) 
 REPRESENTATION_ITEM ( '' )  );
#73959=( BOUNDED_CURVE ( )  B_SPLINE_CURVE ( 2, ( #35069, #35436, #18440, #24086, #29016, #41453, #58445, #70133, #28641, #47095, #62973, #64467, #7123 ),
 .UNSPECIFIED., .F., .F. ) 
 B_SPLINE_CURVE_WITH_KNOTS ( ( 3, 2, 2, 2, 2, 2, 3 ),
 ( 0.2354970748259125335, 0.2407300466676793871, 0.2459630185094462407, 0.2511959903512130943, 0.2564289621929799479, 0.2616619340347468015, 0.2668949058765136551 ),
 .UNSPECIFIED. ) 
 CURVE ( )  GEOMETRIC_REPRESENTATION_ITEM ( )  RATIONAL_B_SPLINE_CURVE ( ( 1.000000000000086153, 0.9659258262889821589, 1.000000000000000000, 0.9659258262890683122, 1.000000000000000000, 0.9659258262890683122, 1.000000000000000000, 0.9659258262890683122, 1.000000000000000000, 0.9659258262890683122, 1.000000000000000000, 0.9659258262890685343, 0.9999999999999997780 ) ) 
 REPRESENTATION_ITEM ( '' )  );
#73971=CARTESIAN_POINT ( 'NONE',  ( -1.836970198721029983E-15, 118.7500000000000142, 10.00000000000000178 ) ) ;
#73972=B_SPLINE_CURVE_WITH_KNOTS ( 'NONE', 3,
 ( #46418, #69432, #17741, #50961, #63765, #12083, #16240, #35119, #6443, #23777 ),
 .UNSPECIFIED., .F., .F.,
 ( 4, 2, 2, 2, 4 ),
 ( 0.000000000000000000, 0.01870349236796609027, 0.03740698473593218054, 0.05611047710389827081, 0.07481396947186436108 ),
 .UNSPECIFIED. ) ;
#73974=CARTESIAN_POINT ( 'NONE',  ( 6.676582343750001591, 289.1093750017069510, -8.176455196517173205E-16 ) ) ;
#73980=( BOUNDED_CURVE ( )  B_SPLINE_CURVE ( 2, ( #63171, #57536, #64290, #12597, #58638, #68829, #6946, #24286, #29958, #47299, #52971, #19731, #14059 ),
 .UNSPECIFIED., .F., .F. ) 
 B_SPLINE_CURVE_WITH_KNOTS ( ( 3, 2, 2, 2, 2, 2, 3 ),
 ( 0.3296947509469928539, 0.3349284467208895055, 0.3401621424947861572, 0.3453958382686828088, 0.3506295340425794604, 0.3558632298164761121, 0.3610969255903727637 ),
 .UNSPECIFIED. ) 
 CURVE ( )  GEOMETRIC_REPRESENTATION_ITEM ( )  RATIONAL_B_SPLINE_CURVE ( ( 1.000000000000000000, 0.9659258262890684232, 1.000000000000000000, 0.9659258262890684232, 1.000000000000000000, 0.9659258262890684232, 1.000000000000000000, 0.9659258262890684232, 1.000000000000000000, 0.9659258262890684232, 1.000000000000000000, 0.9659258262890684232, 1.000000000000000000 ) ) 
 REPRESENTATION_ITEM ( '' )  );
#73988=CARTESIAN_POINT ( 'NONE',  ( 9.832129032723420536, 16.19791666325268054, -5.676582343749999815 ) ) ;
#73990=CARTESIAN_POINT ( 'NONE',  ( -3.042071309553173730, 214.6354166632526983, 11.35316468749999785 ) ) ;
#73991=CARTESIAN_POINT ( 'NONE',  ( 9.832129032723420536, 1.197916663252682756, -5.676582343749999815 ) ) ;
#73994=CARTESIAN_POINT ( 'NONE',  ( -2.679491924289517879, 41.45833333333146697, -10.00000000001272582 ) ) ;
#73997=CARTESIAN_POINT ( 'NONE',  ( 11.35316468749999963, 20.98958332991935549, -3.042071309553165293 ) ) ;
#73999=CARTESIAN_POINT ( 'NONE',  ( 0.000000000000000000, 225.9999999999999432, 0.000000000000000000 ) ) ;
#74002=CARTESIAN_POINT ( 'NONE',  ( 8.311093377946834337, 5.156249996586016238, 8.311093377946839666 ) ) ;
#74004=CARTESIAN_POINT ( 'NONE',  ( -5.676582343750006032, 139.1145833299193555, 9.832129032723418760 ) ) ;
#74005=CARTESIAN_POINT ( 'NONE',  ( -10.00000000000000355, 104.5833333265053824, 2.679491924311223183 ) ) ;
#74006=ADVANCED_FACE ( 'NONE', ( #73009 ), #62057, .T. ) ;
#74008=DIRECTION ( 'NONE',  ( -0.000000000000000000, 1.000000000000000000, -0.000000000000000000 ) ) ;
#74014=CARTESIAN_POINT ( 'NONE',  ( -4.088227598258586603E-16, 288.3593750017070079, -6.676582343750001591 ) ) ;
#74021=CARTESIAN_POINT ( 'NONE',  ( 6.123233995736767268E-16, 218.1249999931720538, -10.00000000000000178 ) ) ;
#74022=CARTESIAN_POINT ( 'NONE',  ( -1.836970198721029983E-15, 28.75000000000000000, 10.00000000000000178 ) ) ;
#74024=CARTESIAN_POINT ( 'NONE',  ( 6.951808397369818766E-16, 72.34374999658602690, -11.35316468750000141 ) ) ;
#74030=CARTESIAN_POINT ( 'NONE',  ( -5.000000000000005329, 110.2083333265053682, 8.660254037844387298 ) ) ;
#74038=EDGE_CURVE ( 'NONE', #50631, #52730, #62423, .T. ) ;
#74039=CARTESIAN_POINT ( 'NONE',  ( 2.395154805519954641E-11, 111.2499999999981242, -9.999999999999998224 ) ) ;
#74042=VERTEX_POINT ( 'NONE', #33408 ) ;
#74053=EDGE_CURVE ( 'NONE', #41900, #23624, #46503, .T. ) ;
#74059=CARTESIAN_POINT ( 'NONE',  ( 7.320508075688771044, 79.37500000000000000, 7.320508075688775484 ) ) ;
#74062=CARTESIAN_POINT ( 'NONE',  ( 4.721056650415999201, 299.2343750017069510, -4.721056650415999201 ) ) ;
#74063=ORIENTED_EDGE ( 'NONE', *, *, #23121, .F. ) ;
#74065=EDGE_CURVE ( 'NONE', #30885, #60165, #16385, .T. ) ;
#74072=CARTESIAN_POINT ( 'NONE',  ( 7.320508075688774596, 195.6250000000000568, -7.320508075688774596 ) ) ;
#74073=( BOUNDED_CURVE ( )  B_SPLINE_CURVE ( 2, ( #35240, #45795, #40139, #62762, #177, #11105, #22772, #63517, #913, #28445, #74096, #17117, #17495 ),
 .UNSPECIFIED., .F., .F. ) 
 B_SPLINE_CURVE_WITH_KNOTS ( ( 3, 2, 2, 2, 2, 2, 3 ),
 ( 0.4293478260869564855, 0.4311594202898550443, 0.4329710144927535476, 0.4347826086956521063, 0.4365942028985507206, 0.4384057971014492794, 0.4402173913043478382 ),
 .UNSPECIFIED. ) 
 CURVE ( )  GEOMETRIC_REPRESENTATION_ITEM ( )  RATIONAL_B_SPLINE_CURVE ( ( 1.000000000000001110, 0.9659258262890673130, 1.000000000000000000, 0.9659258262890683122, 1.000000000000000000, 0.9659258262890683122, 1.000000000000000000, 0.9659258262890683122, 1.000000000000000000, 0.9659258262890683122, 1.000000000000000000, 0.9659258262890683122, 1.000000000000000000 ) ) 
 REPRESENTATION_ITEM ( '' )  );
#74075=CARTESIAN_POINT ( 'NONE',  ( -11.35316468750000141, 168.8020833299193271, 3.042071309553159963 ) ) ;
#74076=CARTESIAN_POINT ( 'NONE',  ( -2.679491924316742324, 213.5416666666662877, 9.999999999997077893 ) ) ;
#74079=DIRECTION ( 'NONE',  ( -0.000000000000000000, 1.000000000000000000, -0.000000000000000000 ) ) ;
#74082=CARTESIAN_POINT ( 'NONE',  ( 5.676582343750001591, 16.92708332991935194, -9.832129032723420536 ) ) ;
#74086=CARTESIAN_POINT ( 'NONE',  ( 8.660254037844385522, 221.4583333265053966, 5.000000000000005329 ) ) ;
#74090=CARTESIAN_POINT ( 'NONE',  ( 2.679491924311222739, 65.83333332650538239, 10.00000000000000355 ) ) ;
#74094=CARTESIAN_POINT ( 'NONE',  ( 2.679491924311227624, 56.04166666666666430, -9.999999999999994671 ) ) ;
#74096=CARTESIAN_POINT ( 'NONE',  ( 5.000000000000001776, 102.7083333265053824, -8.660254037844389075 ) ) ;
#74099=CARTESIAN_POINT ( 'NONE',  ( -10.00000000000010836, 197.2916666666667709, -2.679491924311259599 ) ) ;
#74103=CARTESIAN_POINT ( 'NONE',  ( -11.35316468750000141, 148.2812499965860411, -1.390361679473963753E-15 ) ) ;
#74115=CARTESIAN_POINT ( 'NONE',  ( -3.042071309553173730, 129.6354166632526415, 11.35316468749999785 ) ) ;
#74119=CARTESIAN_POINT ( 'NONE',  ( 5.676582343749993598, 35.26041666325269119, 9.832129032723422313 ) ) ;
#74126=CARTESIAN_POINT ( 'NONE',  ( -4.242640687119285658, 295.1875000034139589, 4.242640687119287435 ) ) ;
#74130=CARTESIAN_POINT ( 'NONE',  ( 9.832129032723420536, 151.5104166632526699, -5.676582343749999815 ) ) ;
#74145=CARTESIAN_POINT ( 'NONE',  ( 10.00000000000000178, 35.20833333333332149, -2.679491924311226736 ) ) ;
#74148=CARTESIAN_POINT ( 'NONE',  ( 4.721056650416000089, 287.8281250017069510, 4.721056650415999201 ) ) ;
#74155=CARTESIAN_POINT ( 'NONE',  ( -4.242640687119285658, 287.1875000034139589, 4.242640687119287435 ) ) ;
#74158=CARTESIAN_POINT ( 'NONE',  ( 5.000000000000001776, 155.8333333333333428, -8.660254037844389075 ) ) ;
#74162=CARTESIAN_POINT ( 'NONE',  ( -5.676582343750006032, 124.4270833299193555, 9.832129032723418760 ) ) ;
#74168=ORIENTED_EDGE ( 'NONE', *, *, #55671, .T. ) ;
#74169=CARTESIAN_POINT ( 'NONE',  ( 6.649952966877521021, 225.6719221872985486, -7.474339169392074211 ) ) ;
#74174=CARTESIAN_POINT ( 'NONE',  ( 11.35316468750000141, 201.0937499965860127, 0.000000000000000000 ) ) ;
#74181=CARTESIAN_POINT ( 'NONE',  ( 5.676582343749993598, 94.94791666325269830, 9.832129032723422313 ) ) ;
#74187=CARTESIAN_POINT ( 'NONE',  ( 3.042071309553167069, 101.8229166632526699, -11.35316468749999785 ) ) ;
#74191=CARTESIAN_POINT ( 'NONE',  ( 4.999999999999993783, 216.0416666598387110, 8.660254037844390851 ) ) ;
#74195=CARTESIAN_POINT ( 'NONE',  ( -5.676582343750006032, 104.1145833299193697, 9.832129032723418760 ) ) ;
#74201=CARTESIAN_POINT ( 'NONE',  ( 10.00000000000000000, 186.6666666598386826, 2.679491924311236062 ) ) ;
#74206=CARTESIAN_POINT ( 'NONE',  ( 11.35316468749999963, 86.30208332991935549, -3.042071309553165293 ) ) ;
#74207=CARTESIAN_POINT ( 'NONE',  ( -2.765530957081998586, 289.6406250017070079, 6.676582343750001591 ) ) ;
#74210=CARTESIAN_POINT ( 'NONE',  ( 5.676582343750001591, 1.927083329919350163, -9.832129032723420536 ) ) ;
#74211=ORIENTED_EDGE ( 'NONE', *, *, #16722, .F. ) ;
#74215=CARTESIAN_POINT ( 'NONE',  ( 8.311093377946837890, 221.4062499965860411, -8.311093377946837890 ) ) ;
#74218=CARTESIAN_POINT ( 'NONE',  ( 6.676582343750003368, 296.0156250017069510, -2.765530957081997254 ) ) ;
#74220=CARTESIAN_POINT ( 'NONE',  ( -2.085542519210945728E-15, 194.8437499965860127, 11.35316468750000141 ) ) ;
#74221=EDGE_CURVE ( 'NONE', #64051, #23294, #7008, .T. ) ;
#74229=CARTESIAN_POINT ( 'NONE',  ( 7.320508075688774596, 15.62499999999999822, -7.320508075688774596 ) ) ;
#74234=CARTESIAN_POINT ( 'NONE',  ( -3.673940397442060854E-16, 299.7500000000000000, -6.000000000000001776 ) ) ;
#74248=ORIENTED_EDGE ( 'NONE', *, *, #32959, .F. ) ;
#74250=CARTESIAN_POINT ( 'NONE',  ( -11.35316468750000141, 93.80208332991934128, 3.042071309553159963 ) ) ;
#74255=CARTESIAN_POINT ( 'NONE',  ( 6.676582343750002480, 291.1718750017070647, -2.765530957081997254 ) ) ;
#74258=CARTESIAN_POINT ( 'NONE',  ( -8.311093377946836114, 197.6562499965860695, -8.311093377946837890 ) ) ;
#74265=CARTESIAN_POINT ( 'NONE',  ( 5.676582343749993598, 165.2604166632526983, 9.832129032723422313 ) ) ;
#74268=CARTESIAN_POINT ( 'NONE',  ( -10.00000000000000178, 89.37499999317203958, -1.224646799147353454E-15 ) ) ;
#74271=CARTESIAN_POINT ( 'NONE',  ( -9.832129032723418760, 57.86458332991935549, -5.676582343750004256 ) ) ;
#74275=CARTESIAN_POINT ( 'NONE',  ( 7.347880794884121708E-16, 300.0000000000000000, -6.000000000000001776 ) ) ;
#74277=CARTESIAN_POINT ( 'NONE',  ( 11.35316468750000141, 65.78124999658602690, 0.000000000000000000 ) ) ;
#74283=CARTESIAN_POINT ( 'NONE',  ( -5.676582343750006032, 64.11458332991935549, 9.832129032723418760 ) ) ;
#74285=CARTESIAN_POINT ( 'NONE',  ( -2.679491924311235174, 15.41666665983869855, 10.00000000000000000 ) ) ;
#74286=CARTESIAN_POINT ( 'NONE',  ( -2.085542519210945728E-15, 169.5312499965860411, 11.35316468750000141 ) ) ;
#74287=CARTESIAN_POINT ( 'NONE',  ( -8.660254037844387298, 138.9583333265053682, -5.000000000000004441 ) ) ;
#74289=FACE_OUTER_BOUND ( 'NONE', #53151, .T. ) ;
#74290=CARTESIAN_POINT ( 'NONE',  ( -2.085542519210945728E-15, 29.84374999658601624, 11.35316468750000141 ) ) ;
#74292=CARTESIAN_POINT ( 'NONE',  ( -4.999999999999998224, 78.54166665983871098, -8.660254037844389075 ) ) ;
#74293=CARTESIAN_POINT ( 'NONE',  ( -8.311093377946841443, 188.9062499965859843, 8.311093377946830785 ) ) ;
#74301=CARTESIAN_POINT ( 'NONE',  ( -3.042071309553173730, 164.3229166632526699, 11.35316468749999785 ) ) ;
#74305=ADVANCED_FACE ( 'NONE', ( #23921 ), #46930, .T. ) ;
#74308=PRODUCT_DEFINITION_FORMATION_WITH_SPECIFIED_SOURCE ( 'ANY', '', #51772, .NOT_KNOWN. ) ;
#74311=CARTESIAN_POINT ( 'NONE',  ( -8.311093377946841443, 119.2187499965860127, 8.311093377946830785 ) ) ;
#74316=EDGE_CURVE ( 'NONE', #60284, #18004, #73980, .T. ) ;
#74318=AXIS2_PLACEMENT_3D ( 'NONE', #18822, #47479, #70503 ) ;
#74330=ORIENTED_EDGE ( 'NONE', *, *, #4986, .T. ) ;
#74338=CARTESIAN_POINT ( 'NONE',  ( -4.242640687119286547, 289.9375000034140157, -4.242640687119286547 ) ) ;
#74340=CARTESIAN_POINT ( 'NONE',  ( 10.00000000000000178, 120.2083333333333570, -2.679491924311226736 ) ) ;
#74342=CARTESIAN_POINT ( 'NONE',  ( -4.721056650415998313, 289.7343750017069510, 4.721056650416000089 ) ) ;
#74354=CARTESIAN_POINT ( 'NONE',  ( 5.676582343750001591, 11.61458332991935016, -9.832129032723420536 ) ) ;
#74355=CARTESIAN_POINT ( 'NONE',  ( 11.35316468750000141, 1.093749996586016682, 0.000000000000000000 ) ) ;
#74356=CARTESIAN_POINT ( 'NONE',  ( 5.676582343750001591, 201.9270833299193555, -9.832129032723420536 ) ) ;
#74358=CYLINDRICAL_SURFACE ( 'NONE', #40374, 10.00000000000000178 ) ;
#74360=DIRECTION ( 'NONE',  ( 0.000000000000000000, 0.000000000000000000, 1.000000000000000000 ) ) ;
#74364=CARTESIAN_POINT ( 'NONE',  ( 3.042071309553167069, 26.82291666325268054, -11.35316468749999785 ) ) ;
#74366=CARTESIAN_POINT ( 'NONE',  ( 5.000000000000002665, 210.8333333333333428, -8.660254037844389075 ) ) ;
#74368=CARTESIAN_POINT ( 'NONE',  ( 0.4499999999999998446, 283.9999999999998863, 5.815332135057944107 ) ) ;
#74370=CARTESIAN_POINT ( 'NONE',  ( -9.832129032723420536, 8.697916663252684089, 5.676582343749997150 ) ) ;
#74372=CARTESIAN_POINT ( 'NONE',  ( 5.676582343749993598, 134.9479166632526983, 9.832129032723422313 ) ) ;
#74374=CARTESIAN_POINT ( 'NONE',  ( -8.660254037844387298, 108.9583333265053682, -5.000000000000004441 ) ) ;
#74376=CARTESIAN_POINT ( 'NONE',  ( -10.00000000000000178, 4.374999993172032475, -1.224646799147353454E-15 ) ) ;
#74380=CARTESIAN_POINT ( 'NONE',  ( -10.00000000000000711, 117.5000000000000142, -1.224646799147354045E-15 ) ) ;
#74382=CARTESIAN_POINT ( 'NONE',  ( -4.088227598258586603E-16, 296.2031250017070079, -6.676582343750001591 ) ) ;
#74383=CARTESIAN_POINT ( 'NONE',  ( 9.832129032723416984, 120.3645833299193697, 5.676582343750006032 ) ) ;
#74391=ORIENTED_EDGE ( 'NONE', *, *, #5493, .F. ) ;
#74397=CARTESIAN_POINT ( 'NONE',  ( -5.676582343750006032, 74.42708332991934128, 9.832129032723418760 ) ) ;
#74404=CARTESIAN_POINT ( 'NONE',  ( 10.00000000000000178, 115.0000000000000284, 0.000000000000000000 ) ) ;
#74425=CARTESIAN_POINT ( 'NONE',  ( -2.485281374238895502, 291.8125000000000568, -5.999999999999677591 ) ) ;
#74428=CARTESIAN_POINT ( 'NONE',  ( 6.123233995736767268E-16, 118.1249999931720396, -10.00000000000000178 ) ) ;
#74431=CARTESIAN_POINT ( 'NONE',  ( 5.000000000000001776, 75.83333333333334281, -8.660254037844389075 ) ) ;
#74433=CARTESIAN_POINT ( 'NONE',  ( 1.102182119232618108E-15, 288.2500000000000000, 6.000000000000001776 ) ) ;
#74438=CARTESIAN_POINT ( 'NONE',  ( 10.00000000000000178, 56.87499999317203248, 0.000000000000000000 ) ) ;
#74442=CARTESIAN_POINT ( 'NONE',  ( 2.679491924311228956, 201.0416666666666572, -10.00000000000000000 ) ) ;
#74444=CARTESIAN_POINT ( 'NONE',  ( 5.676582343750001591, 171.9270833299193555, -9.832129032723420536 ) ) ;
#74445=CARTESIAN_POINT ( 'NONE',  ( -8.660254037844385522, 37.08333333333332860, -5.000000000000002665 ) ) ;
#74450=CARTESIAN_POINT ( 'NONE',  ( 11.35316468749999963, 41.30208332991936260, -3.042071309553165293 ) ) ;
#74459=CARTESIAN_POINT ( 'NONE',  ( -2.679491924311225848, 68.33333332650535397, -10.00000000000000178 ) ) ;
#74462=CARTESIAN_POINT ( 'NONE',  ( -6.676582343750001591, 299.6093750017069510, 0.000000000000000000 ) ) ;
#74468=CARTESIAN_POINT ( 'NONE',  ( 1.522769729196201526E-11, 196.2499999999988063, -10.00000000000000178 ) ) ;
#74471=CARTESIAN_POINT ( 'NONE',  ( -6.362988438888832046E-13, 88.74999999999995737, 9.999999999999998224 ) ) ;
#74472=CARTESIAN_POINT ( 'NONE',  ( 11.35316468749999963, 140.9895833299193555, -3.042071309553165293 ) ) ;
#74473=CARTESIAN_POINT ( 'NONE',  ( 4.999999999999986677, 104.1666666666666714, 8.660254037844380193 ) ) ;
#74481=EDGE_LOOP ( 'NONE', ( #65298, #16296, #47099, #33264 ) ) ;
#74485=CARTESIAN_POINT ( 'NONE',  ( 9.832129032723420536, 126.5104166632526841, -5.676582343749999815 ) ) ;
#74489=CARTESIAN_POINT ( 'NONE',  ( -5.676582343749998039, 42.76041666325268409, -9.832129032723420536 ) ) ;
#74491=CARTESIAN_POINT ( 'NONE',  ( -10.00000000000000178, 194.3749999931720254, -1.224646799147353454E-15 ) ) ;
#74495=CARTESIAN_POINT ( 'NONE',  ( -2.485281374238571761, 297.8750000034139589, -6.000000000000003553 ) ) ;
#74498=CARTESIAN_POINT ( 'NONE',  ( 11.35316468749999963, 151.3020833299193555, -3.042071309553165293 ) ) ;
#74519=CARTESIAN_POINT ( 'NONE',  ( -7.320508075688773708, 36.87500000000000711, -7.320508075688774596 ) ) ;
#74523=CARTESIAN_POINT ( 'NONE',  ( 2.485281374238571317, 298.6875000000000000, -6.000000000000003553 ) ) ;
#74524=CARTESIAN_POINT ( 'NONE',  ( 5.000000000000050626, 79.16666666666674246, 8.660254037844488550 ) ) ;
#74525=CARTESIAN_POINT ( 'NONE',  ( 7.320508075688771044, 196.2499999931720254, 7.320508075688775484 ) ) ;
#74534=CARTESIAN_POINT ( 'NONE',  ( 10.00000000000000178, 165.2083333333333712, -2.679491924311226736 ) ) ;
#74538=CARTESIAN_POINT ( 'NONE',  ( -5.676582343750006032, 134.4270833299193555, 9.832129032723418760 ) ) ;
#74540=CARTESIAN_POINT ( 'NONE',  ( 1.102182119232618108E-15, 288.3125000034140157, 6.000000000000001776 ) ) ;
#74551=CARTESIAN_POINT ( 'NONE',  ( -3.042071309553173730, 224.6354166632526983, 11.35316468749999785 ) ) ;
#74558=CARTESIAN_POINT ( 'NONE',  ( 8.311093377946837890, 106.4062499965859985, -8.311093377946837890 ) ) ;
#74559=ORIENTED_EDGE ( 'NONE', *, *, #8997, .F. ) ;
#74565=CARTESIAN_POINT ( 'NONE',  ( -11.35316468749999785, 103.0729166632526841, -3.042071309553167513 ) ) ;
#74569=CARTESIAN_POINT ( 'NONE',  ( -2.679491924311225848, 218.3333333265053966, -10.00000000000000178 ) ) ;
#74573=CARTESIAN_POINT ( 'NONE',  ( 11.35316468749999785, 100.5729166632526699, 3.042071309553174174 ) ) ;
#74577=CARTESIAN_POINT ( 'NONE',  ( 7.320508075688771044, 201.2499999931720538, 7.320508075688775484 ) ) ;
#74579=CARTESIAN_POINT ( 'NONE',  ( 5.676582343749993598, 85.26041666325268409, 9.832129032723422313 ) ) ;
#74580=CARTESIAN_POINT ( 'NONE',  ( -4.721056650415999201, 288.3281250017069510, -4.721056650415999201 ) ) ;
#74585=CARTESIAN_POINT ( 'NONE',  ( 3.042071309553167069, 221.8229166632527267, -11.35316468749999785 ) ) ;
#74590=CARTESIAN_POINT ( 'NONE',  ( 5.676582343750001591, 216.6145833299193555, -9.832129032723420536 ) ) ;
#74593=CARTESIAN_POINT ( 'NONE',  ( -4.999999999999998224, 98.54166665983871098, -8.660254037844389075 ) ) ;
#74594=CARTESIAN_POINT ( 'NONE',  ( -4.721056650415998313, 296.5781250017069510, 4.721056650416000089 ) ) ;
#74597=CARTESIAN_POINT ( 'NONE',  ( -5.676582343750006032, 209.4270833299193555, 9.832129032723418760 ) ) ;
#74605=CARTESIAN_POINT ( 'NONE',  ( -10.00000000000000355, 27.70833333333332860, 2.679491924311223183 ) ) ;
#74616=CARTESIAN_POINT ( 'NONE',  ( 6.676582343750001591, 294.9531250017069510, -8.176455196517173205E-16 ) ) ;
#74619=CARTESIAN_POINT ( 'NONE',  ( -6.000000000000003553, 289.0000000034140157, -2.485281374238571317 ) ) ;
#74629=CARTESIAN_POINT ( 'NONE',  ( -2.085542519210945728E-15, 89.84374999658602690, 11.35316468750000141 ) ) ;
#74637=CARTESIAN_POINT ( 'NONE',  ( 7.320508075688774596, 77.49999999317205379, -7.320508075688774596 ) ) ;
#74640=CARTESIAN_POINT ( 'NONE',  ( -3.042071309553164404, 197.2395833299193555, -11.35316468749999963 ) ) ;
#74644=CARTESIAN_POINT ( 'NONE',  ( 9.832129032723420536, 176.5104166632526699, -5.676582343749999815 ) ) ;
#74650=CARTESIAN_POINT ( 'NONE',  ( -11.35316468750000141, 43.80208332991934839, 3.042071309553159963 ) ) ;
#74686=COLOUR_RGB('Sky Blue',0.24,0.69,0.87);
#74687=FILL_AREA_STYLE_COLOUR('',#74686);
#74688=FILL_AREA_STYLE('',(#74687));
#74689=SURFACE_STYLE_FILL_AREA(#74688);
#74690=SURFACE_SIDE_STYLE('',(#74689));
#74691=SURFACE_STYLE_USAGE(.BOTH.,#74690);
#74692=PRESENTATION_STYLE_ASSIGNMENT((#74691));
ENDSEC;
END-ISO-10303-21;
